ISO-10303-21;
HEADER;
/* Generated by software containing ST-Developer
 * from STEP Tools, Inc. (www.steptools.com) 
 */

FILE_DESCRIPTION(
/* description */ (''),
/* implementation_level */ '2;1');

FILE_NAME(
/* name */ 'Screw_02.step',
/* time_stamp */ '2026-10-04T16:49:01-07:00',
/* author */ (''),
/* organization */ (''),
/* preprocessor_version */ 'ST-DEVELOPER v20.2',
/* originating_system */ 'Autodesk Translation Framework v15.15.0.0',
/* authorisation */ '');

FILE_SCHEMA (('AUTOMOTIVE_DESIGN { 1 0 10303 214 3 1 1 }'));
ENDSEC;

DATA;
#10=MECHANICAL_DESIGN_GEOMETRIC_PRESENTATION_REPRESENTATION('',(#85),#51553);
#62=B_SPLINE_SURFACE_WITH_KNOTS('',3,3,((#49814,#49815,#49816,#49817,#49818,
#49819,#49820,#49821,#49822,#49823,#49824,#49825,#49826,#49827,#49828,#49829,
#49830,#49831,#49832,#49833,#49834,#49835,#49836,#49837,#49838,#49839,#49840,
#49841,#49842,#49843,#49844,#49845,#49846,#49847,#49848,#49849,#49850,#49851,
#49852,#49853,#49854,#49855,#49856,#49857,#49858,#49859,#49860,#49861,#49862,
#49863,#49864,#49865,#49866,#49867,#49868,#49869,#49870,#49871,#49872,#49873,
#49874,#49875,#49876,#49877,#49878,#49879,#49880,#49881,#49882,#49883,#49884,
#49885,#49886,#49887,#49888,#49889,#49890,#49891,#49892,#49893,#49894,#49895,
#49896,#49897,#49898,#49899,#49900,#49901,#49902,#49903,#49904,#49905,#49906,
#49907,#49908,#49909,#49910,#49911,#49912,#49913,#49914,#49915,#49916,#49917,
#49918,#49919,#49920,#49921,#49922,#49923,#49924,#49925,#49926,#49927,#49928,
#49929,#49930,#49931,#49932,#49933,#49934,#49935,#49936,#49937,#49938,#49939,
#49940,#49941,#49942,#49943,#49944),(#49945,#49946,#49947,#49948,#49949,
#49950,#49951,#49952,#49953,#49954,#49955,#49956,#49957,#49958,#49959,#49960,
#49961,#49962,#49963,#49964,#49965,#49966,#49967,#49968,#49969,#49970,#49971,
#49972,#49973,#49974,#49975,#49976,#49977,#49978,#49979,#49980,#49981,#49982,
#49983,#49984,#49985,#49986,#49987,#49988,#49989,#49990,#49991,#49992,#49993,
#49994,#49995,#49996,#49997,#49998,#49999,#50000,#50001,#50002,#50003,#50004,
#50005,#50006,#50007,#50008,#50009,#50010,#50011,#50012,#50013,#50014,#50015,
#50016,#50017,#50018,#50019,#50020,#50021,#50022,#50023,#50024,#50025,#50026,
#50027,#50028,#50029,#50030,#50031,#50032,#50033,#50034,#50035,#50036,#50037,
#50038,#50039,#50040,#50041,#50042,#50043,#50044,#50045,#50046,#50047,#50048,
#50049,#50050,#50051,#50052,#50053,#50054,#50055,#50056,#50057,#50058,#50059,
#50060,#50061,#50062,#50063,#50064,#50065,#50066,#50067,#50068,#50069,#50070,
#50071,#50072,#50073,#50074,#50075),(#50076,#50077,#50078,#50079,#50080,
#50081,#50082,#50083,#50084,#50085,#50086,#50087,#50088,#50089,#50090,#50091,
#50092,#50093,#50094,#50095,#50096,#50097,#50098,#50099,#50100,#50101,#50102,
#50103,#50104,#50105,#50106,#50107,#50108,#50109,#50110,#50111,#50112,#50113,
#50114,#50115,#50116,#50117,#50118,#50119,#50120,#50121,#50122,#50123,#50124,
#50125,#50126,#50127,#50128,#50129,#50130,#50131,#50132,#50133,#50134,#50135,
#50136,#50137,#50138,#50139,#50140,#50141,#50142,#50143,#50144,#50145,#50146,
#50147,#50148,#50149,#50150,#50151,#50152,#50153,#50154,#50155,#50156,#50157,
#50158,#50159,#50160,#50161,#50162,#50163,#50164,#50165,#50166,#50167,#50168,
#50169,#50170,#50171,#50172,#50173,#50174,#50175,#50176,#50177,#50178,#50179,
#50180,#50181,#50182,#50183,#50184,#50185,#50186,#50187,#50188,#50189,#50190,
#50191,#50192,#50193,#50194,#50195,#50196,#50197,#50198,#50199,#50200,#50201,
#50202,#50203,#50204,#50205,#50206),(#50207,#50208,#50209,#50210,#50211,
#50212,#50213,#50214,#50215,#50216,#50217,#50218,#50219,#50220,#50221,#50222,
#50223,#50224,#50225,#50226,#50227,#50228,#50229,#50230,#50231,#50232,#50233,
#50234,#50235,#50236,#50237,#50238,#50239,#50240,#50241,#50242,#50243,#50244,
#50245,#50246,#50247,#50248,#50249,#50250,#50251,#50252,#50253,#50254,#50255,
#50256,#50257,#50258,#50259,#50260,#50261,#50262,#50263,#50264,#50265,#50266,
#50267,#50268,#50269,#50270,#50271,#50272,#50273,#50274,#50275,#50276,#50277,
#50278,#50279,#50280,#50281,#50282,#50283,#50284,#50285,#50286,#50287,#50288,
#50289,#50290,#50291,#50292,#50293,#50294,#50295,#50296,#50297,#50298,#50299,
#50300,#50301,#50302,#50303,#50304,#50305,#50306,#50307,#50308,#50309,#50310,
#50311,#50312,#50313,#50314,#50315,#50316,#50317,#50318,#50319,#50320,#50321,
#50322,#50323,#50324,#50325,#50326,#50327,#50328,#50329,#50330,#50331,#50332,
#50333,#50334,#50335,#50336,#50337)),.UNSPECIFIED.,.F.,.F.,.F.,(4,4),(4,
1,1,1,1,1,1,1,1,1,1,1,1,1,1,1,1,1,1,1,1,1,1,1,1,1,1,1,1,1,1,1,1,1,1,1,1,
1,1,1,1,1,1,1,1,1,1,1,1,1,1,1,1,1,1,1,1,1,1,1,1,1,1,1,1,1,1,1,1,1,1,1,1,
1,1,1,1,1,1,1,1,1,1,1,1,1,1,1,1,1,1,1,1,1,1,1,1,1,1,1,1,1,1,1,1,1,1,1,1,
1,1,1,1,1,1,1,1,1,1,1,1,1,1,1,1,1,1,1,4),(-0.000669933452207598,0.082357279631371),
(8.31473274985794,9.31258359158534,10.3104344333127,11.3082852750401,12.3061361167675,
13.3039869584949,14.3018378002224,15.2996886419498,16.2975394836772,17.2953903254046,
18.293241167132,19.2910920088594,20.2889428505868,21.2867936923142,22.2846445340416,
23.282495375769,24.2803462174964,25.2781970592238,26.2760479009512,27.2738987426786,
28.271749584406,29.2696004261334,30.2674512678608,31.2653021095882,32.2631529513156,
33.261003793043,34.2588546347704,35.2567054764978,36.2545563182252,37.2524071599526,
38.25025800168,39.2481088434074,40.2459596851348,41.2438105268622,42.2416613685896,
43.239512210317,44.2373630520444,45.2352138937718,46.2330647354992,47.2309155772266,
48.228766418954,49.2266172606814,50.2244681024088,51.2223189441362,52.2201697858636,
53.218020627591,54.2158714693185,55.2137223110459,56.2115731527733,57.2094239945007,
58.2072748362281,59.2051256779555,60.2029765196829,61.2008273614103,62.1986782031377,
63.1965290448651,64.1943798865925,65.1922307283199,66.1900815700473,67.1879324117747,
68.1857832535021,69.1836340952295,70.1814849369569,71.1793357786843,72.1771866204117,
73.1750374621391,74.1728883038665,75.1707391455939,76.1685899873213,77.1664408290487,
78.1642916707761,79.1621425125035,80.1599933542309,81.1578441959583,82.1556950376857,
83.1535458794131,84.1513967211405,85.1492475628679,86.1470984045953,87.1449492463227,
88.1428000880501,89.1406509297776,90.1385017715049,91.1363526132323,92.1342034549598,
93.1320542966872,94.1299051384146,95.127755980142,96.1256068218694,97.1234576635968,
98.1213085053242,99.1191593470516,100.117010188779,101.114861030506,102.112711872234,
103.110562713961,104.108413555689,105.106264397416,106.104115239143,107.101966080871,
108.099816922598,109.097667764326,110.095518606053,111.09336944778,112.091220289508,
113.089071131235,114.086921972963,115.08477281469,116.082623656417,117.080474498145,
118.078325339872,119.0761761816,120.074027023327,121.071877865054,122.069728706782,
123.067579548509,124.065430390237,125.063281231964,126.061132073691,127.058982915419,
128.056833757146,129.054684598874,130.052535440601,131.050386282328,132.048237124056,
133.046087965783,134.043938807511,135.041789649238,136.040310424417),
 .UNSPECIFIED.);
#63=B_SPLINE_SURFACE_WITH_KNOTS('',3,3,((#50529,#50530,#50531,#50532,#50533,
#50534,#50535,#50536,#50537,#50538,#50539,#50540,#50541,#50542,#50543,#50544,
#50545,#50546,#50547,#50548,#50549,#50550,#50551,#50552,#50553,#50554,#50555,
#50556,#50557,#50558,#50559,#50560,#50561,#50562,#50563,#50564,#50565,#50566,
#50567,#50568,#50569,#50570,#50571,#50572,#50573,#50574,#50575,#50576,#50577,
#50578,#50579,#50580,#50581,#50582,#50583,#50584,#50585,#50586,#50587,#50588,
#50589,#50590,#50591,#50592,#50593,#50594,#50595,#50596,#50597,#50598,#50599,
#50600,#50601,#50602,#50603,#50604,#50605,#50606,#50607,#50608,#50609,#50610,
#50611,#50612,#50613,#50614,#50615,#50616,#50617,#50618,#50619,#50620,#50621,
#50622,#50623,#50624,#50625,#50626,#50627,#50628,#50629,#50630,#50631,#50632,
#50633,#50634,#50635,#50636,#50637,#50638,#50639,#50640,#50641,#50642,#50643,
#50644,#50645,#50646,#50647,#50648,#50649,#50650,#50651,#50652,#50653,#50654,
#50655,#50656,#50657,#50658,#50659),(#50660,#50661,#50662,#50663,#50664,
#50665,#50666,#50667,#50668,#50669,#50670,#50671,#50672,#50673,#50674,#50675,
#50676,#50677,#50678,#50679,#50680,#50681,#50682,#50683,#50684,#50685,#50686,
#50687,#50688,#50689,#50690,#50691,#50692,#50693,#50694,#50695,#50696,#50697,
#50698,#50699,#50700,#50701,#50702,#50703,#50704,#50705,#50706,#50707,#50708,
#50709,#50710,#50711,#50712,#50713,#50714,#50715,#50716,#50717,#50718,#50719,
#50720,#50721,#50722,#50723,#50724,#50725,#50726,#50727,#50728,#50729,#50730,
#50731,#50732,#50733,#50734,#50735,#50736,#50737,#50738,#50739,#50740,#50741,
#50742,#50743,#50744,#50745,#50746,#50747,#50748,#50749,#50750,#50751,#50752,
#50753,#50754,#50755,#50756,#50757,#50758,#50759,#50760,#50761,#50762,#50763,
#50764,#50765,#50766,#50767,#50768,#50769,#50770,#50771,#50772,#50773,#50774,
#50775,#50776,#50777,#50778,#50779,#50780,#50781,#50782,#50783,#50784,#50785,
#50786,#50787,#50788,#50789,#50790),(#50791,#50792,#50793,#50794,#50795,
#50796,#50797,#50798,#50799,#50800,#50801,#50802,#50803,#50804,#50805,#50806,
#50807,#50808,#50809,#50810,#50811,#50812,#50813,#50814,#50815,#50816,#50817,
#50818,#50819,#50820,#50821,#50822,#50823,#50824,#50825,#50826,#50827,#50828,
#50829,#50830,#50831,#50832,#50833,#50834,#50835,#50836,#50837,#50838,#50839,
#50840,#50841,#50842,#50843,#50844,#50845,#50846,#50847,#50848,#50849,#50850,
#50851,#50852,#50853,#50854,#50855,#50856,#50857,#50858,#50859,#50860,#50861,
#50862,#50863,#50864,#50865,#50866,#50867,#50868,#50869,#50870,#50871,#50872,
#50873,#50874,#50875,#50876,#50877,#50878,#50879,#50880,#50881,#50882,#50883,
#50884,#50885,#50886,#50887,#50888,#50889,#50890,#50891,#50892,#50893,#50894,
#50895,#50896,#50897,#50898,#50899,#50900,#50901,#50902,#50903,#50904,#50905,
#50906,#50907,#50908,#50909,#50910,#50911,#50912,#50913,#50914,#50915,#50916,
#50917,#50918,#50919,#50920,#50921),(#50922,#50923,#50924,#50925,#50926,
#50927,#50928,#50929,#50930,#50931,#50932,#50933,#50934,#50935,#50936,#50937,
#50938,#50939,#50940,#50941,#50942,#50943,#50944,#50945,#50946,#50947,#50948,
#50949,#50950,#50951,#50952,#50953,#50954,#50955,#50956,#50957,#50958,#50959,
#50960,#50961,#50962,#50963,#50964,#50965,#50966,#50967,#50968,#50969,#50970,
#50971,#50972,#50973,#50974,#50975,#50976,#50977,#50978,#50979,#50980,#50981,
#50982,#50983,#50984,#50985,#50986,#50987,#50988,#50989,#50990,#50991,#50992,
#50993,#50994,#50995,#50996,#50997,#50998,#50999,#51000,#51001,#51002,#51003,
#51004,#51005,#51006,#51007,#51008,#51009,#51010,#51011,#51012,#51013,#51014,
#51015,#51016,#51017,#51018,#51019,#51020,#51021,#51022,#51023,#51024,#51025,
#51026,#51027,#51028,#51029,#51030,#51031,#51032,#51033,#51034,#51035,#51036,
#51037,#51038,#51039,#51040,#51041,#51042,#51043,#51044,#51045,#51046,#51047,
#51048,#51049,#51050,#51051,#51052)),.UNSPECIFIED.,.F.,.F.,.F.,(4,4),(4,
1,1,1,1,1,1,1,1,1,1,1,1,1,1,1,1,1,1,1,1,1,1,1,1,1,1,1,1,1,1,1,1,1,1,1,1,
1,1,1,1,1,1,1,1,1,1,1,1,1,1,1,1,1,1,1,1,1,1,1,1,1,1,1,1,1,1,1,1,1,1,1,1,
1,1,1,1,1,1,1,1,1,1,1,1,1,1,1,1,1,1,1,1,1,1,1,1,1,1,1,1,1,1,1,1,1,1,1,1,
1,1,1,1,1,1,1,1,1,1,1,1,1,1,1,1,1,1,1,4),(-0.000386098416431568,0.0827034127833099),
(11.6145234207097,12.613065069482,13.6109159112094,14.6087667529368,15.6066175946642,
16.6044684363917,17.6023192781191,18.6001701198465,19.5980209615739,20.5958718033013,
21.5937226450287,22.5915734867561,23.5894243284835,24.5872751702109,25.5851260119383,
26.5829768536657,27.5808276953931,28.5786785371205,29.5765293788479,30.5743802205753,
31.5722310623027,32.5700819040301,33.5679327457575,34.5657835874849,35.5636344292123,
36.5614852709397,37.5593361126671,38.5571869543945,39.5550377961219,40.5528886378493,
41.5507394795767,42.5485903213041,43.5464411630315,44.5442920047589,45.5421428464863,
46.5399936882137,47.5378445299411,48.5356953716685,49.5335462133959,50.5313970551233,
51.5292478968507,52.5270987385781,53.5249495803055,54.522800422033,55.5206512637604,
56.5185021054878,57.5163529472152,58.5142037889426,59.51205463067,60.5099054723974,
61.5077563141248,62.5056071558522,63.5034579975796,64.501308839307,65.4991596810344,
66.4970105227618,67.4948613644892,68.4927122062166,69.490563047944,70.4884138896714,
71.4862647313988,72.4841155731262,73.4819664148536,74.479817256581,75.4776680983084,
76.4755189400358,77.4733697817632,78.4712206234906,79.469071465218,80.4669223069454,
81.4647731486728,82.4626239904002,83.4604748321276,84.458325673855,85.4561765155824,
86.4540273573098,87.4518781990372,88.4497290407646,89.4475798824921,90.4454307242194,
91.4432815659468,92.4411324076742,93.4389832494017,94.4368340911291,95.4346849328565,
96.4325357745839,97.4303866163113,98.4282374580387,99.4260882997661,100.423939141493,
101.421789983221,102.419640824948,103.417491666676,104.415342508403,105.41319335013,
106.411044191858,107.408895033585,108.406745875313,109.40459671704,110.402447558768,
111.400298400495,112.398149242222,113.39600008395,114.393850925677,115.391701767405,
116.389552609132,117.387403450859,118.385254292587,119.383105134314,120.380955976042,
121.378806817769,122.376657659496,123.374508501224,124.372359342951,125.370210184679,
126.368061026406,127.365911868133,128.363762709861,129.361613551588,130.359464393316,
131.357315235043,132.35516607677,133.353016918498,134.350867760225,135.348718601953,
136.34656944368,137.344420285407,138.342271127135,139.340121968862),
 .UNSPECIFIED.);
#69=SHAPE_REPRESENTATION_RELATIONSHIP('SRR','None',#51590,#77);
#77=ADVANCED_BREP_SHAPE_REPRESENTATION('',(#94),#51550);
#85=STYLED_ITEM('',(#51634),#94);
#94=MANIFOLD_SOLID_BREP('Body1',#4264);
#157=PLANE('',#4557);
#158=PLANE('',#4558);
#302=FACE_OUTER_BOUND('',#509,.T.);
#303=FACE_OUTER_BOUND('',#510,.T.);
#304=FACE_OUTER_BOUND('',#511,.T.);
#305=FACE_OUTER_BOUND('',#512,.T.);
#306=FACE_OUTER_BOUND('',#513,.T.);
#307=FACE_OUTER_BOUND('',#514,.T.);
#308=FACE_OUTER_BOUND('',#515,.T.);
#309=FACE_OUTER_BOUND('',#516,.T.);
#310=FACE_OUTER_BOUND('',#517,.T.);
#311=FACE_OUTER_BOUND('',#518,.T.);
#312=FACE_OUTER_BOUND('',#519,.T.);
#313=FACE_OUTER_BOUND('',#520,.T.);
#314=FACE_OUTER_BOUND('',#521,.T.);
#315=FACE_OUTER_BOUND('',#522,.T.);
#316=FACE_OUTER_BOUND('',#523,.T.);
#317=FACE_OUTER_BOUND('',#524,.T.);
#318=FACE_OUTER_BOUND('',#525,.T.);
#319=FACE_OUTER_BOUND('',#526,.T.);
#320=FACE_OUTER_BOUND('',#527,.T.);
#321=FACE_OUTER_BOUND('',#528,.T.);
#322=FACE_OUTER_BOUND('',#529,.T.);
#323=FACE_OUTER_BOUND('',#530,.T.);
#324=FACE_OUTER_BOUND('',#531,.T.);
#325=FACE_OUTER_BOUND('',#532,.T.);
#326=FACE_OUTER_BOUND('',#533,.T.);
#327=FACE_OUTER_BOUND('',#534,.T.);
#509=EDGE_LOOP('',(#3435,#3436,#3437,#3438));
#510=EDGE_LOOP('',(#3439,#3440,#3441,#3442,#3443));
#511=EDGE_LOOP('',(#3444,#3445,#3446,#3447,#3448));
#512=EDGE_LOOP('',(#3449,#3450,#3451,#3452,#3453));
#513=EDGE_LOOP('',(#3454,#3455,#3456,#3457,#3458));
#514=EDGE_LOOP('',(#3459,#3460,#3461,#3462,#3463));
#515=EDGE_LOOP('',(#3464,#3465,#3466,#3467,#3468));
#516=EDGE_LOOP('',(#3469,#3470,#3471,#3472,#3473));
#517=EDGE_LOOP('',(#3474,#3475,#3476,#3477,#3478));
#518=EDGE_LOOP('',(#3479,#3480,#3481,#3482,#3483));
#519=EDGE_LOOP('',(#3484,#3485,#3486,#3487,#3488));
#520=EDGE_LOOP('',(#3489,#3490,#3491,#3492,#3493));
#521=EDGE_LOOP('',(#3494,#3495,#3496,#3497,#3498));
#522=EDGE_LOOP('',(#3499,#3500,#3501,#3502,#3503));
#523=EDGE_LOOP('',(#3504,#3505,#3506,#3507,#3508));
#524=EDGE_LOOP('',(#3509,#3510,#3511,#3512,#3513));
#525=EDGE_LOOP('',(#3514,#3515,#3516,#3517,#3518));
#526=EDGE_LOOP('',(#3519,#3520,#3521,#3522,#3523));
#527=EDGE_LOOP('',(#3524,#3525,#3526,#3527,#3528));
#528=EDGE_LOOP('',(#3529,#3530,#3531,#3532,#3533,#3534));
#529=EDGE_LOOP('',(#3535,#3536,#3537,#3538,#3539,#3540,#3541,#3542,#3543,
#3544,#3545,#3546,#3547,#3548,#3549,#3550,#3551,#3552,#3553,#3554,#3555,
#3556,#3557,#3558,#3559,#3560,#3561,#3562,#3563,#3564,#3565,#3566,#3567,
#3568,#3569,#3570,#3571,#3572,#3573,#3574,#3575,#3576,#3577,#3578));
#530=EDGE_LOOP('',(#3579,#3580,#3581,#3582,#3583));
#531=EDGE_LOOP('',(#3584,#3585,#3586,#3587,#3588,#3589,#3590,#3591,#3592,
#3593,#3594,#3595,#3596,#3597,#3598,#3599,#3600,#3601,#3602,#3603,#3604,
#3605,#3606,#3607,#3608,#3609,#3610,#3611,#3612,#3613,#3614,#3615,#3616,
#3617,#3618,#3619,#3620,#3621,#3622,#3623,#3624,#3625,#3626,#3627,#3628,
#3629,#3630,#3631,#3632,#3633,#3634,#3635,#3636,#3637,#3638));
#532=EDGE_LOOP('',(#3639,#3640,#3641,#3642,#3643,#3644,#3645,#3646,#3647,
#3648,#3649,#3650,#3651,#3652,#3653,#3654,#3655,#3656,#3657,#3658,#3659,
#3660,#3661,#3662,#3663,#3664,#3665,#3666,#3667,#3668,#3669,#3670,#3671,
#3672,#3673,#3674,#3675,#3676,#3677,#3678,#3679,#3680,#3681,#3682,#3683,
#3684,#3685,#3686,#3687,#3688,#3689,#3690,#3691,#3692,#3693));
#533=EDGE_LOOP('',(#3694,#3695,#3696,#3697,#3698));
#534=EDGE_LOOP('',(#3699,#3700,#3701,#3702));
#653=CIRCLE('',#4532,3.22274999999998);
#654=CIRCLE('',#4553,3.933);
#655=CIRCLE('',#4554,3.933);
#656=CIRCLE('',#4556,3.22274999999998);
#852=LINE('',#31903,#1080);
#853=LINE('',#32095,#1081);
#854=LINE('',#32527,#1082);
#855=LINE('',#32996,#1083);
#856=LINE('',#33439,#1084);
#857=LINE('',#33898,#1085);
#858=LINE('',#34349,#1086);
#859=LINE('',#34784,#1087);
#860=LINE('',#35231,#1088);
#861=LINE('',#35666,#1089);
#862=LINE('',#36109,#1090);
#863=LINE('',#36550,#1091);
#864=LINE('',#37013,#1092);
#865=LINE('',#37484,#1093);
#866=LINE('',#37927,#1094);
#867=LINE('',#38370,#1095);
#868=LINE('',#38837,#1096);
#869=LINE('',#39298,#1097);
#870=LINE('',#39737,#1098);
#871=LINE('',#40181,#1099);
#1080=VECTOR('',#5162,3.22274999999998);
#1081=VECTOR('',#5167,3.22274999999998);
#1082=VECTOR('',#5170,3.22274999999998);
#1083=VECTOR('',#5173,3.22274999999998);
#1084=VECTOR('',#5176,3.22274999999998);
#1085=VECTOR('',#5179,3.22274999999998);
#1086=VECTOR('',#5182,3.22274999999998);
#1087=VECTOR('',#5185,3.22274999999998);
#1088=VECTOR('',#5188,3.22274999999998);
#1089=VECTOR('',#5191,3.22274999999998);
#1090=VECTOR('',#5194,3.22274999999998);
#1091=VECTOR('',#5197,3.22274999999998);
#1092=VECTOR('',#5200,3.22274999999998);
#1093=VECTOR('',#5203,3.22274999999998);
#1094=VECTOR('',#5206,3.22274999999998);
#1095=VECTOR('',#5209,3.22274999999998);
#1096=VECTOR('',#5212,3.22274999999998);
#1097=VECTOR('',#5215,3.22274999999998);
#1098=VECTOR('',#5218,3.22274999999998);
#1099=VECTOR('',#5221,3.22274999999998);
#1369=B_SPLINE_CURVE_WITH_KNOTS('',3,(#31905,#31906,#31907,#31908,#31909,
#31910,#31911,#31912,#31913,#31914,#31915,#31916,#31917,#31918,#31919,#31920,
#31921,#31922,#31923,#31924,#31925,#31926,#31927,#31928,#31929,#31930,#31931,
#31932,#31933,#31934,#31935,#31936,#31937,#31938,#31939,#31940,#31941,#31942,
#31943,#31944,#31945,#31946,#31947,#31948,#31949,#31950,#31951,#31952,#31953,
#31954,#31955,#31956,#31957,#31958,#31959,#31960,#31961,#31962,#31963,#31964,
#31965,#31966,#31967,#31968,#31969,#31970,#31971,#31972,#31973,#31974,#31975,
#31976,#31977,#31978,#31979,#31980,#31981,#31982,#31983,#31984,#31985,#31986,
#31987,#31988,#31989,#31990,#31991,#31992,#31993,#31994,#31995,#31996,#31997,
#31998,#31999,#32000,#32001,#32002,#32003,#32004,#32005,#32006,#32007,#32008,
#32009,#32010,#32011,#32012,#32013),.UNSPECIFIED.,.F.,.F.,(4,3,3,3,3,3,
3,3,3,3,3,3,3,3,3,3,3,3,3,3,3,3,3,3,3,3,3,3,3,3,3,3,3,3,3,3,4),(10.3763408596307,
10.4685035879595,10.5605450798931,10.6540126042865,10.7459016202891,10.8377629934542,
10.9296224595031,11.0242881633874,11.1162731126776,11.2122791938588,11.3082852750401,
11.4015231451061,11.4946379598422,11.5876571073663,11.6806117932315,11.7735333702322,
11.8664464519442,11.9593756382665,12.0524050043333,12.1454872708207,12.2387236347795,
12.3061361167675,12.3991530832475,12.4920433843522,12.5848347338002,12.6775576307686,
12.7702450445746,12.8629218677855,12.9556129776305,13.0484029190153,13.1412446433811,
13.2342411237987,13.3039869584949,13.3970673240037,13.4900377484096,13.5829076752469,
13.662003513089),.UNSPECIFIED.);
#1370=B_SPLINE_CURVE_WITH_KNOTS('',3,(#32016,#32017,#32018,#32019,#32020,
#32021,#32022,#32023,#32024,#32025,#32026,#32027,#32028,#32029,#32030,#32031,
#32032,#32033,#32034,#32035,#32036,#32037,#32038,#32039,#32040,#32041,#32042,
#32043,#32044,#32045,#32046,#32047,#32048,#32049,#32050,#32051,#32052,#32053,
#32054,#32055,#32056,#32057,#32058,#32059,#32060,#32061,#32062,#32063,#32064,
#32065,#32066,#32067,#32068,#32069,#32070,#32071,#32072,#32073,#32074,#32075,
#32076,#32077,#32078,#32079,#32080,#32081,#32082,#32083,#32084,#32085,#32086,
#32087,#32088,#32089,#32090,#32091),.UNSPECIFIED.,.F.,.F.,(4,2,2,2,2,2,
2,2,2,2,2,2,2,2,2,2,2,2,2,2,2,2,2,2,2,2,2,2,2,2,2,2,2,2,2,2,2,4),(-3.35381526931575,
-3.35208315295462,-3.34983146774722,-3.34483876368488,-3.32619197630295,
-3.27122359195305,-3.22306543606155,-3.21388437505902,-3.20858010275596,
-3.20392890877022,-3.19813032562173,-3.18910420019164,-3.13190644661067,
-3.085595133377,-3.0428844389819,-3.03704710102653,-3.03458254610874,-3.03213833675085,
-3.02994487981598,-3.02689266704973,-3.01892914498056,-2.97007407985262,
-2.8972840853171,-2.88320402228536,-2.87743187246694,-2.87328482018027,
-2.86951031673175,-2.86444987637415,-2.85214471248006,-2.77985001500164,
-2.72230605211448,-2.71296395890366,-2.70954291846262,-2.70717462614405,
-2.70497732276349,-2.70196675866152,-2.69435955099127,-2.69261509225713),
 .UNSPECIFIED.);
#1371=B_SPLINE_CURVE_WITH_KNOTS('',3,(#32097,#32098,#32099,#32100,#32101,
#32102,#32103,#32104,#32105,#32106,#32107,#32108,#32109,#32110,#32111,#32112,
#32113,#32114,#32115,#32116,#32117,#32118,#32119,#32120,#32121,#32122,#32123,
#32124,#32125,#32126,#32127,#32128,#32129,#32130,#32131,#32132,#32133,#32134,
#32135,#32136,#32137,#32138,#32139,#32140,#32141,#32142,#32143,#32144,#32145,
#32146,#32147,#32148,#32149,#32150,#32151,#32152,#32153,#32154,#32155,#32156,
#32157,#32158,#32159,#32160,#32161,#32162,#32163,#32164,#32165,#32166,#32167,
#32168,#32169,#32170,#32171,#32172,#32173,#32174,#32175,#32176,#32177,#32178,
#32179,#32180,#32181,#32182,#32183,#32184,#32185,#32186,#32187,#32188,#32189,
#32190,#32191,#32192,#32193,#32194,#32195,#32196,#32197,#32198,#32199,#32200,
#32201,#32202,#32203,#32204,#32205,#32206,#32207,#32208,#32209,#32210,#32211,
#32212,#32213,#32214,#32215,#32216,#32217,#32218,#32219,#32220,#32221,#32222,
#32223,#32224,#32225,#32226,#32227,#32228,#32229,#32230,#32231,#32232,#32233,
#32234,#32235,#32236,#32237,#32238,#32239,#32240,#32241,#32242,#32243,#32244,
#32245,#32246,#32247,#32248,#32249,#32250),.UNSPECIFIED.,.F.,.F.,(4,2,2,
2,2,2,2,2,2,2,2,2,2,2,2,2,2,2,2,2,2,2,2,2,2,2,2,2,2,2,2,2,2,2,2,2,2,2,2,
2,2,2,2,2,2,2,2,2,2,2,2,2,2,2,2,2,2,2,2,2,2,2,2,2,2,2,2,2,2,2,2,2,2,2,2,
2,4),(-1.37017729781545,-1.35353780576373,-1.33257834742348,-1.32548122187877,
-1.32094726490235,-1.31668689964161,-1.31096736598667,-1.29797497597591,
-1.28014171544337,-1.22883793443645,-1.17254957458835,-1.16452266794228,
-1.16142937281249,-1.15920630467273,-1.15677107461307,-1.15323034881184,
-1.14384503173126,-1.12960173098574,-1.07886840906787,-1.01403121697174,
-1.00580271677102,-1.00054113135373,-0.996340483931179,-0.991578637763216,
-0.983437132773718,-0.94758375686734,-0.900429253094662,-0.850308959919973,
-0.842205213330912,-0.839101245359232,-0.836875455818964,-0.834442726563618,
-0.830915196301282,-0.821620279122071,-0.807562779774907,-0.707110833613374,
-0.687412651737281,-0.680481782934284,-0.675983987862879,-0.671707272617472,
-0.665887232896476,-0.652307404813528,-0.63340940348293,-0.52946292793793,
-0.520056255652633,-0.516402835476207,-0.514188674404075,-0.511743014886738,
-0.508153924649882,-0.498442083047438,-0.437387510478215,-0.374545774329483,
-0.36194259260325,-0.356351857845128,-0.352095452245071,-0.351582388850521,
-0.346996720500453,-0.339433075634769,-0.330361169326727,-0.31215093911564,
-0.258879006166635,-0.205305953728267,-0.197214129082237,-0.194111637054782,
-0.191885985176512,-0.189453999882711,-0.185926160343614,-0.176621297251876,
-0.162541792995744,-0.0693764045847394,-0.0438024477556163,-0.0361792526774839,
-0.0315321654369022,-0.0274544150076456,-0.0233724540897795,-0.0181340863993818,
-0.000954368308936828),.UNSPECIFIED.);
#1372=B_SPLINE_CURVE_WITH_KNOTS('',3,(#32251,#32252,#32253,#32254,#32255,
#32256,#32257,#32258,#32259,#32260,#32261,#32262,#32263,#32264,#32265,#32266,
#32267,#32268,#32269,#32270,#32271,#32272,#32273,#32274,#32275,#32276,#32277,
#32278,#32279,#32280,#32281,#32282,#32283,#32284,#32285,#32286,#32287,#32288,
#32289,#32290,#32291,#32292,#32293,#32294,#32295,#32296,#32297,#32298,#32299,
#32300,#32301,#32302,#32303,#32304,#32305,#32306,#32307,#32308,#32309,#32310,
#32311,#32312,#32313,#32314,#32315,#32316,#32317),.UNSPECIFIED.,.F.,.F.,
(4,3,3,3,3,3,3,3,3,3,3,3,3,3,3,3,3,3,3,3,3,3,4),(13.662003513089,13.7547833390107,
13.8475493001619,13.9403261705392,14.0331997127964,14.1261218245434,14.2192021029353,
14.3018378002224,14.3949470159261,14.4879308398322,14.5808168538984,14.6736357436152,
14.7664199360917,14.8591942106715,14.9519833318896,15.0448715509177,15.1378118541448,
15.2309063867031,15.2996886419498,15.4024334558436,15.5048979103914,15.6068616102991,
15.7079632677851),.UNSPECIFIED.);
#1373=B_SPLINE_CURVE_WITH_KNOTS('',3,(#32318,#32319,#32320,#32321,#32322,
#32323,#32324,#32325,#32326,#32327,#32328,#32329,#32330,#32331,#32332,#32333,
#32334,#32335,#32336,#32337,#32338,#32339,#32340,#32341,#32342,#32343,#32344,
#32345,#32346,#32347,#32348,#32349,#32350,#32351,#32352,#32353,#32354,#32355,
#32356,#32357,#32358,#32359,#32360,#32361,#32362,#32363,#32364,#32365,#32366,
#32367,#32368,#32369,#32370,#32371,#32372,#32373,#32374,#32375,#32376,#32377,
#32378,#32379,#32380,#32381,#32382,#32383,#32384,#32385,#32386,#32387,#32388,
#32389,#32390,#32391,#32392,#32393,#32394,#32395,#32396,#32397,#32398,#32399,
#32400,#32401,#32402,#32403,#32404,#32405,#32406,#32407,#32408,#32409,#32410,
#32411,#32412,#32413,#32414,#32415,#32416,#32417,#32418,#32419,#32420,#32421,
#32422,#32423,#32424,#32425,#32426,#32427,#32428,#32429,#32430,#32431,#32432,
#32433,#32434,#32435,#32436,#32437,#32438,#32439,#32440,#32441,#32442,#32443,
#32444,#32445,#32446,#32447,#32448,#32449,#32450,#32451,#32452,#32453,#32454,
#32455,#32456,#32457,#32458,#32459,#32460,#32461,#32462,#32463,#32464,#32465,
#32466,#32467,#32468,#32469,#32470,#32471,#32472,#32473,#32474,#32475,#32476,
#32477,#32478,#32479,#32480,#32481,#32482,#32483,#32484,#32485,#32486,#32487,
#32488,#32489,#32490,#32491,#32492,#32493,#32494,#32495,#32496,#32497,#32498,
#32499,#32500,#32501,#32502,#32503,#32504,#32505,#32506,#32507,#32508,#32509,
#32510,#32511,#32512,#32513,#32514,#32515,#32516,#32517,#32518,#32519,#32520,
#32521,#32522,#32523),.UNSPECIFIED.,.F.,.F.,(4,2,2,2,2,2,2,2,2,2,2,2,2,
2,2,2,2,2,2,2,2,2,2,2,2,2,2,2,2,2,2,2,2,2,2,2,2,2,2,2,2,2,2,2,2,2,2,2,2,
2,2,2,2,2,2,2,2,2,2,2,2,2,2,2,2,2,2,2,2,2,2,2,2,2,2,2,2,2,2,2,2,2,2,2,2,
2,2,2,2,2,2,2,2,2,2,2,2,2,2,2,2,2,4),(-2.69261509225713,-2.62840556418915,
-2.58320465660134,-2.5581209019691,-2.55077455147651,-2.54615710481637,
-2.54186963989729,-2.53628654202243,-2.52389960895418,-2.45910092414662,
-2.4210319306056,-2.40355810669151,-2.39304293511801,-2.38930168080884,
-2.38679274096041,-2.3845680187088,-2.38153097868239,-2.37396463106057,
-2.30781275498151,-2.26343067004595,-2.2387077651925,-2.23141206564109,
-2.22681501059143,-2.2225389684779,-2.21696070820388,-2.2045480219227,-2.13407070170969,
-2.09168152552772,-2.07873550345086,-2.06998367493561,-2.06652831838317,
-2.06410214583396,-2.06154906462413,-2.05743810090315,-2.04471366480278,
-1.98789225372189,-1.94149850550134,-1.92468076243408,-1.91226986600097,
-1.9066669592139,-1.90243878318937,-1.89788730673565,-1.89065283231372,
-1.86838897281277,-1.77038951237406,-1.75641322232236,-1.74716598949256,
-1.7436560940739,-1.74123374683306,-1.73900610856686,-1.73590083064744,
-1.72778977032303,-1.67764324502658,-1.60086409733971,-1.58888035541318,
-1.58339341499287,-1.57914615353389,-1.57453929754588,-1.56713943598796,
-1.54113295901057,-1.49279730227811,-1.4325400897938,-1.42466346939064,
-1.4215877574702,-1.41936452244751,-1.41691652161779,-1.41333076945456,
-1.40366591344044,-1.34341237495997,-1.27959500561132,-1.2682908828538,
-1.26214778234246,-1.25785023721058,-1.25344256823369,-1.24696345539816,
-1.22907832395468,-1.20167432452606,-1.14575664002757,-1.10638950402625,
-1.1013280534111,-1.09828618603912,-1.0959209094728,-1.09319654623698,-1.08833367065206,
-1.06433817920143,-0.998898346786502,-0.95149052745457,-0.943379214362556,
-0.938151699456961,-0.93395191356894,-0.929162535952773,-0.920901870025552,
-0.883096196407596,-0.838553402197201,-0.787896978384544,-0.779795442219594,
-0.776690718998467,-0.77446410452002,-0.77202874119717,-0.768496558743206,
-0.759185453215502,-0.745099087974622,-0.662096941273505),.UNSPECIFIED.);
#1374=B_SPLINE_CURVE_WITH_KNOTS('',3,(#32528,#32529,#32530,#32531,#32532,
#32533,#32534,#32535,#32536,#32537,#32538,#32539,#32540,#32541,#32542,#32543,
#32544,#32545,#32546,#32547,#32548,#32549,#32550,#32551,#32552,#32553,#32554,
#32555,#32556,#32557,#32558,#32559,#32560,#32561,#32562,#32563,#32564,#32565,
#32566,#32567,#32568,#32569,#32570,#32571,#32572,#32573,#32574,#32575,#32576,
#32577,#32578,#32579,#32580,#32581,#32582,#32583,#32584,#32585,#32586,#32587,
#32588,#32589,#32590,#32591,#32592,#32593,#32594,#32595,#32596,#32597,#32598,
#32599,#32600,#32601,#32602,#32603,#32604,#32605,#32606,#32607,#32608,#32609,
#32610,#32611,#32612,#32613,#32614,#32615,#32616,#32617,#32618,#32619,#32620,
#32621,#32622,#32623,#32624,#32625,#32626,#32627,#32628,#32629,#32630,#32631,
#32632,#32633,#32634,#32635,#32636,#32637,#32638,#32639,#32640,#32641,#32642,
#32643,#32644,#32645,#32646,#32647,#32648,#32649,#32650,#32651,#32652,#32653,
#32654,#32655,#32656,#32657,#32658,#32659,#32660,#32661,#32662,#32663,#32664,
#32665,#32666,#32667,#32668,#32669,#32670,#32671,#32672,#32673,#32674,#32675,
#32676,#32677,#32678,#32679,#32680,#32681,#32682,#32683,#32684,#32685,#32686,
#32687,#32688,#32689,#32690,#32691,#32692,#32693,#32694,#32695,#32696,#32697,
#32698,#32699,#32700,#32701,#32702,#32703,#32704,#32705,#32706,#32707,#32708,
#32709,#32710,#32711,#32712,#32713,#32714,#32715,#32716,#32717,#32718,#32719,
#32720,#32721,#32722,#32723,#32724,#32725,#32726,#32727,#32728,#32729,#32730,
#32731,#32732,#32733,#32734,#32735,#32736,#32737,#32738,#32739,#32740,#32741,
#32742,#32743),.UNSPECIFIED.,.F.,.F.,(4,2,2,2,2,2,2,2,2,2,2,2,2,2,2,2,2,
2,2,2,2,2,2,2,2,2,2,2,2,2,2,2,2,2,2,2,2,2,2,2,2,2,2,2,2,2,2,2,2,2,2,2,2,
2,2,2,2,2,2,2,2,2,2,2,2,2,2,2,2,2,2,2,2,2,2,2,2,2,2,2,2,2,2,2,2,2,2,2,2,
2,2,2,2,2,2,2,2,2,2,2,2,2,2,2,2,2,2,4),(-3.40019978283383,-3.33785962504013,
-3.27156335607859,-3.26196291641992,-3.25689126660038,-3.25274339360484,
-3.24785601059373,-3.23936276391376,-3.20122700787053,-3.13428425247534,
-3.11273789666227,-3.10425562390685,-3.09792357910148,-3.09489880588864,
-3.0925428382484,-3.08977834312619,-3.08485968336625,-3.06265332848916,
-3.05368678966229,-2.97168692317334,-2.95423949296249,-2.94146336005877,
-2.93578327087505,-2.93153065855957,-2.92753524058326,-2.92087524358251,
-2.90309438654935,-2.80027475110723,-2.78612759229225,-2.77679034859233,
-2.77325708904298,-2.77082366780496,-2.7685997250947,-2.76550173993936,
-2.75743816373339,-2.70348014953057,-2.69708672421599,-2.64887963959844,
-2.6316680928851,-2.61902423762827,-2.61336685598548,-2.60911709669841,
-2.60511402393393,-2.59841657818522,-2.58038378126111,-2.47785358116976,
-2.46371480757022,-2.45438115837674,-2.4508479951634,-2.44841424146137,
-2.44618967052223,-2.44309039405311,-2.43502044916619,-2.38084305956231,
-2.32807198872925,-2.30995858474924,-2.29680936902852,-2.29106277359642,
-2.28679816252814,-2.28227446379223,-2.2752241378696,-2.25460537193083,
-2.15520087420387,-2.14118020174492,-2.13190379206863,-2.12837873404686,
-2.12594627243598,-2.12371947728022,-2.12061261366701,-2.11248935071206,
-2.0628865616765,-2.05184291245054,-2.03165746075049,-1.98115202486522,
-1.97295607823159,-1.96770379425843,-1.96350320435912,-1.95873350139782,
-1.95055869366086,-1.91417959380968,-1.86556923818777,-1.84083175773657,
-1.81296855049339,-1.8081940458159,-1.80520683283672,-1.80285246102468,
-1.80005713013371,-1.79486026441714,-1.76326575464596,-1.69715013019003,
-1.65800113698883,-1.64945192898591,-1.64455037798679,-1.64040093780557,
-1.63534023612804,-1.62580017436166,-1.61380059407552,-1.58648490115453,
-1.54466786480509,-1.49516457585576,-1.48703173834883,-1.48392355454095,
-1.48169642532567,-1.47926424364828,-1.4757407321054,-1.46647480103462,
-1.45247710770272,-1.37017729781545),.UNSPECIFIED.);
#1375=B_SPLINE_CURVE_WITH_KNOTS('',3,(#32745,#32746,#32747,#32748,#32749,
#32750,#32751,#32752,#32753,#32754,#32755,#32756,#32757,#32758,#32759,#32760,
#32761,#32762,#32763,#32764,#32765,#32766,#32767,#32768,#32769,#32770,#32771,
#32772,#32773,#32774,#32775,#32776,#32777,#32778,#32779,#32780,#32781,#32782,
#32783,#32784,#32785,#32786,#32787,#32788,#32789,#32790,#32791,#32792,#32793,
#32794,#32795,#32796,#32797,#32798,#32799,#32800,#32801,#32802,#32803,#32804,
#32805,#32806,#32807,#32808,#32809,#32810,#32811,#32812,#32813,#32814,#32815,
#32816,#32817,#32818,#32819,#32820,#32821,#32822,#32823,#32824,#32825,#32826,
#32827,#32828,#32829,#32830,#32831,#32832,#32833,#32834,#32835,#32836,#32837,
#32838),.UNSPECIFIED.,.F.,.F.,(4,2,2,2,2,2,2,2,2,2,2,2,2,2,2,2,2,2,2,2,
2,2,2,2,2,2,2,2,2,2,2,2,2,2,2,2,2,2,2,2,2,2,2,2,2,2,4),(-0.662096941273505,
-0.644012719739959,-0.624813906700673,-0.617946465357201,-0.61345872401671,
-0.609168813828691,-0.603294615271159,-0.589416215840541,-0.569974529301255,
-0.512373160929998,-0.488520616481295,-0.460872434565717,-0.456103611975906,
-0.453116473389265,-0.450759955505912,-0.447959352362998,-0.442744501743739,
-0.410724261387381,-0.342088399887239,-0.305684066271292,-0.297260779481479,
-0.29238538676688,-0.288365535647978,-0.288284500126682,-0.288213905080228,
-0.288152183486406,-0.288098050919491,-0.288050444656379,-0.287954023183898,
-0.287859928484098,-0.287767993288569,-0.287678062119022,-0.287589990493134,
-0.28267224182747,-0.277034907874753,-0.267897316736875,-0.24950233237944,
-0.195245063880915,-0.143014950278401,-0.134905540056361,-0.131798965530057,
-0.12957116488514,-0.127136232799798,-0.1236049776553,-0.114296766641828,
-0.100215253267655,-0.000985697035008145),.UNSPECIFIED.);
#1376=B_SPLINE_CURVE_WITH_KNOTS('',3,(#32839,#32840,#32841,#32842,#32843,
#32844,#32845,#32846,#32847,#32848,#32849,#32850,#32851,#32852,#32853,#32854,
#32855,#32856,#32857,#32858,#32859,#32860,#32861,#32862,#32863,#32864,#32865,
#32866,#32867,#32868,#32869,#32870,#32871,#32872,#32873,#32874,#32875,#32876,
#32877,#32878,#32879,#32880,#32881,#32882,#32883,#32884,#32885,#32886,#32887,
#32888,#32889,#32890,#32891,#32892,#32893,#32894,#32895,#32896,#32897,#32898,
#32899,#32900,#32901,#32902,#32903,#32904,#32905,#32906,#32907,#32908,#32909,
#32910,#32911,#32912,#32913,#32914,#32915,#32916,#32917,#32918,#32919,#32920,
#32921,#32922,#32923,#32924,#32925,#32926,#32927,#32928,#32929,#32930,#32931,
#32932,#32933,#32934,#32935,#32936,#32937,#32938,#32939,#32940,#32941,#32942,
#32943,#32944,#32945,#32946,#32947,#32948,#32949,#32950,#32951,#32952,#32953,
#32954,#32955,#32956,#32957,#32958,#32959,#32960,#32961,#32962,#32963,#32964,
#32965,#32966,#32967,#32968,#32969,#32970,#32971,#32972,#32973,#32974,#32975,
#32976,#32977,#32978,#32979,#32980,#32981,#32982,#32983,#32984,#32985,#32986,
#32987,#32988,#32989,#32990,#32991,#32992),.UNSPECIFIED.,.F.,.F.,(4,2,2,
2,2,2,2,2,2,2,2,2,2,2,2,2,2,2,2,2,2,2,2,2,2,2,2,2,2,2,2,2,2,2,2,2,2,2,2,
2,2,2,2,2,2,2,2,2,2,2,2,2,2,2,2,2,2,2,2,2,2,2,2,2,2,2,2,2,2,2,2,2,2,2,2,
2,4),(-4.06157145021908,-4.04807440817928,-4.03856467987825,-4.03393873005346,
-4.03000157592306,-4.02604097088093,-4.02081706246017,-4.0127177091575,
-3.98635579660403,-3.93397204242227,-3.87725700878007,-3.87157254187659,
-3.86867490169071,-3.86655357980012,-3.86378019163222,-3.85882924332806,
-3.83611505747223,-3.82812448825048,-3.74575260748455,-3.72826727557778,
-3.71944848640976,-3.71205572037451,-3.70862621689302,-3.70451682093695,
-3.6996433166824,-3.69122350406628,-3.65476818366308,-3.58656708036991,
-3.5646363935611,-3.55186345142934,-3.54788547798063,-3.54535623137956,
-3.54294778829835,-3.53942598139824,-3.53082103944866,-3.43334018119189,
-3.39825062761908,-3.39015482394934,-3.38540143114383,-3.38119710041741,
-3.37591602986257,-3.36762759654677,-3.3100044839404,-3.25400106117824,
-3.23104430626754,-3.22624029043099,-3.22352897176375,-3.22116286531749,
-3.21810376350195,-3.21142587089775,-3.20983109897739,-3.14421900669202,
-3.09930666832812,-3.08279270303488,-3.07054387065534,-3.06495503698883,
-3.06071316305695,-3.05668515368407,-3.04986715839868,-3.03100524868918,
-2.92951427869627,-2.91541286568839,-2.90609619336183,-2.90256407293655,
-2.90012931035266,-2.89790234827737,-2.89479773397084,-2.88669902542398,
-2.83637454939601,-2.7894259719955,-2.75364633096651,-2.74550579395821,
-2.7407419736787,-2.73653799902376,-2.73127009425987,-2.72302728728776,
-2.69274389685463),.UNSPECIFIED.);
#1377=B_SPLINE_CURVE_WITH_KNOTS('',3,(#32998,#32999,#33000,#33001,#33002,
#33003,#33004,#33005,#33006,#33007,#33008,#33009,#33010,#33011,#33012,#33013,
#33014,#33015,#33016,#33017,#33018,#33019,#33020,#33021,#33022,#33023,#33024,
#33025,#33026,#33027,#33028,#33029,#33030,#33031,#33032,#33033,#33034,#33035,
#33036,#33037,#33038,#33039,#33040,#33041,#33042,#33043,#33044,#33045,#33046,
#33047,#33048,#33049,#33050,#33051,#33052,#33053,#33054,#33055,#33056,#33057,
#33058,#33059,#33060,#33061,#33062,#33063,#33064,#33065,#33066,#33067,#33068,
#33069,#33070,#33071,#33072,#33073,#33074,#33075,#33076,#33077,#33078,#33079,
#33080,#33081,#33082,#33083,#33084,#33085,#33086,#33087,#33088,#33089,#33090,
#33091,#33092,#33093,#33094,#33095,#33096,#33097,#33098,#33099,#33100,#33101,
#33102,#33103,#33104,#33105,#33106,#33107,#33108,#33109,#33110,#33111,#33112,
#33113,#33114,#33115,#33116,#33117,#33118,#33119,#33120,#33121,#33122,#33123,
#33124,#33125,#33126,#33127,#33128,#33129,#33130,#33131,#33132,#33133,#33134,
#33135,#33136,#33137,#33138,#33139,#33140,#33141,#33142,#33143,#33144,#33145,
#33146,#33147,#33148,#33149),.UNSPECIFIED.,.F.,.F.,(4,2,2,2,2,2,2,2,2,2,
2,2,2,2,2,2,2,2,2,2,2,2,2,2,2,2,2,2,2,2,2,2,2,2,2,2,2,2,2,2,2,2,2,2,2,2,
2,2,2,2,2,2,2,2,2,2,2,2,2,2,2,2,2,2,2,2,2,2,2,2,2,2,2,2,2,4),(-1.36994781431221,
-1.35403913083624,-1.30344451495222,-1.29534465922271,-1.29224063884764,
-1.29001441570313,-1.28758086695492,-1.284051378108,-1.27474675702159,-1.26067054126231,
-1.15978907963419,-1.14042544509649,-1.13353898820462,-1.12905010352677,
-1.12476737954213,-1.11891624827375,-1.10515593004192,-1.08592797343983,
-1.0295047467755,-1.00849221602317,-0.995577372928076,-0.975607063867324,
-0.970839979704906,-0.968109192655276,-0.965984214333597,-0.963035164179288,
-0.957092937533464,-0.900753006527331,-0.871047715508243,-0.822183027676799,
-0.814028034181265,-0.808788214836695,-0.804588745105528,-0.799810765179259,
-0.79159769912195,-0.754575788575409,-0.709524470366712,-0.658574742817765,
-0.650476594600359,-0.647373049335334,-0.645147122086622,-0.642713844579556,
-0.639184662296964,-0.629880349919068,-0.615804162916471,-0.51489121218588,
-0.495565690712209,-0.48868503262247,-0.484197755986418,-0.479914982646323,
-0.474061270508087,-0.460282955098616,-0.441021101492656,-0.384405622040821,
-0.336076920641187,-0.327990508575039,-0.324613060896587,-0.322232382556755,
-0.320035548214643,-0.317527490258593,-0.310319907611356,-0.27831689190842,
-0.203602816193235,-0.175281078771535,-0.167359374787102,-0.162645440414172,
-0.158858100496402,-0.153726603826024,-0.143840700829879,-0.131287186479607,
-0.102074471247827,-0.0455501577320752,-0.0103273183728019,-0.00448290106007735,
-0.00200870709752073,-0.000951636744030443),.UNSPECIFIED.);
#1378=B_SPLINE_CURVE_WITH_KNOTS('',3,(#33150,#33151,#33152,#33153,#33154,
#33155,#33156,#33157,#33158,#33159,#33160,#33161,#33162,#33163,#33164,#33165,
#33166,#33167,#33168,#33169,#33170,#33171,#33172,#33173,#33174,#33175,#33176,
#33177,#33178,#33179,#33180,#33181,#33182,#33183,#33184,#33185,#33186,#33187,
#33188,#33189,#33190,#33191,#33192,#33193,#33194,#33195,#33196,#33197,#33198,
#33199,#33200,#33201,#33202,#33203,#33204,#33205,#33206,#33207,#33208,#33209,
#33210,#33211,#33212,#33213,#33214,#33215,#33216,#33217,#33218,#33219,#33220,
#33221,#33222,#33223,#33224,#33225,#33226,#33227,#33228,#33229,#33230,#33231),
 .UNSPECIFIED.,.F.,.F.,(4,2,2,2,2,2,2,2,2,2,2,2,2,2,2,2,2,2,2,2,2,2,2,2,
2,2,2,2,2,2,2,2,2,2,2,2,2,2,2,2,4),(-4.06098341928092,-4.06080310437317,
-4.05935516277898,-4.05671553698414,-4.05219170774946,-4.03466221784105,
-4.02168389330639,-3.95943259813033,-3.9294978819508,-3.91673927325081,
-3.90672647937867,-3.90157048021314,-3.89737939171005,-3.89254604393623,
-3.88428972131288,-3.84994246621341,-3.78067236244368,-3.74986832349323,
-3.74279775147556,-3.74030418116452,-3.73810805690436,-3.73577611157493,
-3.73239875285325,-3.7243079361267,-3.67421012083181,-3.62711858962269,
-3.59129729265715,-3.5831601040997,-3.57840024782517,-3.57420102377141,
-3.56894077754901,-3.56071341638611,-3.4967801651768,-3.43164404785125,
-3.42167540578113,-3.41805158700942,-3.41560011089201,-3.4133942115017,
-3.41036560161198,-3.40273282390601,-3.40019978283383),.UNSPECIFIED.);
#1379=B_SPLINE_CURVE_WITH_KNOTS('',3,(#33232,#33233,#33234,#33235,#33236,
#33237,#33238,#33239,#33240,#33241,#33242,#33243,#33244,#33245,#33246,#33247,
#33248,#33249,#33250,#33251,#33252,#33253,#33254,#33255,#33256,#33257,#33258,
#33259,#33260,#33261,#33262,#33263,#33264,#33265,#33266,#33267,#33268,#33269,
#33270,#33271,#33272,#33273,#33274,#33275,#33276,#33277,#33278,#33279,#33280,
#33281,#33282,#33283,#33284,#33285,#33286,#33287,#33288,#33289,#33290,#33291,
#33292,#33293,#33294,#33295,#33296,#33297,#33298,#33299,#33300,#33301,#33302,
#33303,#33304,#33305,#33306,#33307,#33308,#33309,#33310,#33311,#33312,#33313,
#33314,#33315,#33316,#33317,#33318,#33319,#33320,#33321,#33322,#33323,#33324,
#33325,#33326,#33327,#33328,#33329,#33330,#33331,#33332,#33333,#33334,#33335,
#33336,#33337,#33338,#33339,#33340,#33341,#33342,#33343,#33344,#33345,#33346,
#33347,#33348,#33349,#33350,#33351,#33352,#33353,#33354,#33355,#33356,#33357,
#33358,#33359,#33360,#33361,#33362,#33363,#33364,#33365,#33366,#33367,#33368,
#33369,#33370,#33371,#33372,#33373,#33374,#33375,#33376,#33377,#33378,#33379,
#33380,#33381,#33382,#33383,#33384,#33385,#33386,#33387,#33388,#33389,#33390,
#33391,#33392,#33393,#33394,#33395,#33396,#33397,#33398,#33399,#33400,#33401,
#33402,#33403,#33404,#33405,#33406,#33407,#33408,#33409,#33410,#33411,#33412,
#33413,#33414,#33415,#33416,#33417,#33418,#33419,#33420,#33421,#33422,#33423,
#33424,#33425,#33426,#33427,#33428,#33429,#33430,#33431,#33432,#33433,#33434,
#33435),.UNSPECIFIED.,.F.,.F.,(4,2,2,2,2,2,2,2,2,2,2,2,2,2,2,2,2,2,2,2,
2,2,2,2,2,2,2,2,2,2,2,2,2,2,2,2,2,2,2,2,2,2,2,2,2,2,2,2,2,2,2,2,2,2,2,2,
2,2,2,2,2,2,2,2,2,2,2,2,2,2,2,2,2,2,2,2,2,2,2,2,2,2,2,2,2,2,2,2,2,2,2,2,
2,2,2,2,2,2,2,2,2,4),(-2.69274389685463,-2.65996324899456,-2.5940083245505,
-2.58398511534276,-2.58035127739488,-2.57789588111239,-2.57568859799975,
-2.57266070754016,-2.5650433537799,-2.49977345661444,-2.45461787405291,
-2.43804912217385,-2.42576824498821,-2.42017276544664,-2.41592906755699,
-2.41190171986369,-2.40509070832018,-2.3862860780695,-2.28469466397845,
-2.27058696871724,-2.26126662798916,-2.25773342786145,-2.25529802074957,
-2.25307056346958,-2.249965360392,-2.24186588944671,-2.1913523066016,-2.14701024489156,
-2.10902042255395,-2.10074745671393,-2.09595409934006,-2.09175264908689,
-2.08652540626277,-2.07841887302653,-2.03121996720006,-1.95853249084424,
-1.94105335883462,-1.93643514861003,-1.93376367154131,-1.93138732723421,
-1.92820172854944,-1.92101776454692,-1.88925390955357,-1.81583422100394,
-1.78610184135241,-1.77807670352973,-1.77333719074546,-1.76954917635182,
-1.7644426491467,-1.75469352519467,-1.69098145621153,-1.62333472717303,
-1.6158904626649,-1.61289153189135,-1.61069103901612,-1.60822586071836,
-1.60454749758677,-1.5942058307455,-1.57794603520031,-1.52900603173646,
-1.46565346051885,-1.45740777443098,-1.4521380063163,-1.44793256000442,
-1.44316708803954,-1.43502378360481,-1.39923642008227,-1.35228919612668,
-1.30185436566104,-1.29375156543399,-1.29064560089792,-1.28841776736352,
-1.28598212442745,-1.28244889138968,-1.2731301027863,-1.25902781619956,
-1.15751015588664,-1.13867014178734,-1.13185348835024,-1.12782460480089,
-1.12358057710361,-1.11798685569063,-1.10571894011434,-1.08917192751295,
-1.04412096424067,-0.978594791679027,-0.970986860739619,-0.967960196775019,
-0.96575293080583,-0.963296487188248,-0.959659276591147,-0.949614993131925,
-0.883328351109479,-0.820657355393565,-0.812412410319363,-0.807143198990509,
-0.802938250023272,-0.798173398399364,-0.790031295670248,-0.754251857247748,
-0.707320128128854,-0.662256880685031),.UNSPECIFIED.);
#1380=B_SPLINE_CURVE_WITH_KNOTS('',3,(#33440,#33441,#33442,#33443,#33444,
#33445,#33446,#33447,#33448,#33449,#33450,#33451,#33452,#33453,#33454,#33455,
#33456,#33457,#33458,#33459,#33460,#33461,#33462,#33463,#33464,#33465,#33466,
#33467,#33468,#33469,#33470,#33471,#33472,#33473,#33474,#33475,#33476,#33477,
#33478,#33479,#33480,#33481,#33482,#33483,#33484,#33485,#33486,#33487,#33488,
#33489,#33490,#33491,#33492,#33493,#33494,#33495,#33496,#33497,#33498,#33499,
#33500,#33501,#33502,#33503,#33504,#33505,#33506,#33507,#33508,#33509,#33510,
#33511,#33512,#33513,#33514,#33515,#33516,#33517,#33518,#33519,#33520,#33521,
#33522,#33523,#33524,#33525,#33526,#33527,#33528,#33529,#33530,#33531,#33532,
#33533,#33534,#33535,#33536,#33537,#33538,#33539,#33540,#33541,#33542,#33543,
#33544,#33545,#33546,#33547,#33548,#33549,#33550,#33551,#33552,#33553,#33554,
#33555,#33556,#33557,#33558,#33559,#33560,#33561,#33562,#33563,#33564,#33565,
#33566,#33567,#33568,#33569,#33570,#33571,#33572,#33573,#33574,#33575,#33576,
#33577,#33578,#33579,#33580,#33581,#33582,#33583,#33584,#33585,#33586,#33587,
#33588,#33589,#33590,#33591,#33592,#33593,#33594,#33595,#33596,#33597,#33598,
#33599,#33600,#33601,#33602,#33603,#33604,#33605,#33606,#33607,#33608,#33609,
#33610,#33611,#33612,#33613,#33614,#33615,#33616,#33617,#33618,#33619,#33620,
#33621,#33622,#33623,#33624,#33625,#33626,#33627,#33628,#33629,#33630,#33631,
#33632,#33633,#33634,#33635,#33636,#33637,#33638,#33639,#33640,#33641,#33642,
#33643,#33644,#33645,#33646,#33647,#33648,#33649,#33650,#33651,#33652,#33653,
#33654,#33655,#33656,#33657),.UNSPECIFIED.,.F.,.F.,(4,2,2,2,2,2,2,2,2,2,
2,2,2,2,2,2,2,2,2,2,2,2,2,2,2,2,2,2,2,2,2,2,2,2,2,2,2,2,2,2,2,2,2,2,2,2,
2,2,2,2,2,2,2,2,2,2,2,2,2,2,2,2,2,2,2,2,2,2,2,2,2,2,2,2,2,2,2,2,2,2,2,2,
2,2,2,2,2,2,2,2,2,2,2,2,2,2,2,2,2,2,2,2,2,2,2,2,2,2,4),(-3.40027864395219,
-3.39526694442771,-3.38941664528869,-3.38513479929102,-3.38064707582144,
-3.37376289130956,-3.35440901647098,-3.25349185689639,-3.23941222672951,
-3.2301071528882,-3.22657797302984,-3.2241448060387,-3.22191905698823,-3.21881588799011,
-3.21071925123346,-3.16005988842744,-3.1133230111501,-3.07762309782326,
-3.06949051735682,-3.06473019178421,-3.06052864131234,-3.05526294501151,
-3.04702208958492,-2.98360963409326,-2.93459138745507,-2.9104066296905,
-2.90553506137354,-2.90280965241121,-2.90044706811189,-2.89741268022228,
-2.89237057074954,-2.85396102272484,-2.79740634168158,-2.75584017368339,
-2.74738372280542,-2.7425529794996,-2.73835898118844,-2.73319279679595,
-2.72527935641716,-2.68323185626629,-2.61954662882662,-2.59861448065653,
-2.59029328708264,-2.5840541974567,-2.58104653895082,-2.57869078990821,
-2.57591114724268,-2.57092920110732,-2.54770122314852,-2.54103958949081,
-2.51769360016757,-2.46110972276335,-2.44185341715776,-2.42807640219829,
-2.42222239734796,-2.41793908721741,-2.41345095531639,-2.40656840499489,
-2.38723392729998,-2.28626169830717,-2.27217738370819,-2.26286941054893,
-2.25933925954978,-2.25690546361179,-2.25467917162272,-2.25157528803708,
-2.24347710381067,-2.19253249529662,-2.1474855412448,-2.11049101346007,
-2.10227852593253,-2.09750004571732,-2.09329963031623,-2.08805796677039,
-2.07989874173682,-2.03094988061131,-1.97766068675707,-1.94419732416433,
-1.9392284989376,-1.93618286386817,-1.933823656949,-1.93107046631797,-1.92607223916869,
-1.899377481294,-1.81096924619372,-1.78660651889419,-1.77911620346404,-1.77449584112607,
-1.77026468109079,-1.76474619788352,-1.75287763519025,-1.70446713282638,
-1.64982835813692,-1.6213852828933,-1.61658671874534,-1.61359207313376,
-1.61123695707861,-1.60844677975401,-1.60327514517467,-1.57239511476165,
-1.5285964046287,-1.46723152820404,-1.45899225371714,-1.45372656266826,
-1.44952440599155,-1.44476273927614,-1.43662624933331,-1.40088236390028,
-1.36994781431221),.UNSPECIFIED.);
#1381=B_SPLINE_CURVE_WITH_KNOTS('',3,(#33659,#33660,#33661,#33662,#33663,
#33664,#33665,#33666,#33667,#33668,#33669,#33670,#33671,#33672,#33673,#33674,
#33675,#33676,#33677,#33678,#33679,#33680,#33681,#33682,#33683,#33684,#33685,
#33686,#33687,#33688,#33689,#33690,#33691,#33692,#33693,#33694,#33695,#33696,
#33697,#33698,#33699,#33700,#33701,#33702,#33703,#33704,#33705,#33706,#33707,
#33708,#33709,#33710,#33711,#33712,#33713,#33714,#33715,#33716,#33717,#33718,
#33719,#33720,#33721,#33722,#33723,#33724,#33725,#33726,#33727,#33728,#33729,
#33730,#33731,#33732,#33733,#33734,#33735,#33736),.UNSPECIFIED.,.F.,.F.,
(4,2,2,2,2,2,2,2,2,2,2,2,2,2,2,2,2,2,2,2,2,2,2,2,2,2,2,2,2,2,2,2,2,2,2,
2,2,2,4),(-0.662256880685031,-0.656877296145055,-0.648775583122173,-0.645670006523397,
-0.643442443997101,-0.641007089033966,-0.637474259638706,-0.628156454261886,
-0.614055584043697,-0.512542794514352,-0.49371098281102,-0.486895979214415,
-0.48286773840294,-0.47862414602344,-0.473030591614327,-0.46076136733263,
-0.444211480313638,-0.399143680132143,-0.333564903143002,-0.326020670736594,
-0.322739142773218,-0.320375640873755,-0.318176010640031,-0.314383106592926,
-0.303164557881548,-0.284950987202906,-0.191332929247415,-0.171536752245391,
-0.164589855766057,-0.160086291468646,-0.155807397011775,-0.149989534546236,
-0.136438317209894,-0.117596386639476,-0.065955914197476,-0.00962864573827704,
-0.00363211110775064,-0.00165261963449196,-0.000951735584449904),
 .UNSPECIFIED.);
#1382=B_SPLINE_CURVE_WITH_KNOTS('',3,(#33737,#33738,#33739,#33740,#33741,
#33742,#33743,#33744,#33745,#33746,#33747,#33748,#33749,#33750,#33751,#33752,
#33753,#33754,#33755,#33756,#33757,#33758,#33759,#33760,#33761,#33762,#33763,
#33764,#33765,#33766,#33767,#33768,#33769,#33770,#33771,#33772,#33773,#33774,
#33775,#33776,#33777,#33778,#33779,#33780,#33781,#33782,#33783,#33784,#33785,
#33786,#33787,#33788,#33789,#33790,#33791,#33792,#33793,#33794,#33795,#33796,
#33797,#33798,#33799,#33800,#33801,#33802,#33803,#33804,#33805,#33806,#33807,
#33808,#33809,#33810,#33811,#33812,#33813,#33814,#33815,#33816,#33817,#33818,
#33819,#33820,#33821,#33822,#33823,#33824,#33825,#33826,#33827,#33828,#33829,
#33830,#33831,#33832,#33833,#33834,#33835,#33836,#33837,#33838,#33839,#33840,
#33841,#33842,#33843,#33844,#33845,#33846,#33847,#33848,#33849,#33850,#33851,
#33852,#33853,#33854,#33855,#33856,#33857,#33858,#33859,#33860,#33861,#33862,
#33863,#33864,#33865,#33866,#33867,#33868,#33869,#33870,#33871,#33872,#33873,
#33874,#33875,#33876,#33877,#33878,#33879,#33880,#33881,#33882,#33883,#33884,
#33885,#33886,#33887,#33888,#33889,#33890,#33891,#33892,#33893,#33894),
 .UNSPECIFIED.,.F.,.F.,(4,2,2,2,2,2,2,2,2,2,2,2,2,2,2,2,2,2,2,2,2,2,2,2,
2,2,2,2,2,2,2,2,2,2,2,2,2,2,2,2,2,2,2,2,2,2,2,2,2,2,2,2,2,2,2,2,2,2,2,2,
2,2,2,2,2,2,2,2,2,2,2,2,2,2,2,2,2,2,4),(-4.06163372264747,-4.06090083217341,
-4.05900435491866,-4.05659198049401,-4.05306580980933,-4.04400200753387,
-4.03568916741852,-3.98543879491345,-3.93918649778018,-3.92066637708922,
-3.90729110492638,-3.90150374185163,-3.89723050404575,-3.89325829342407,
-3.8878019798035,-3.87382110036059,-3.79357017365643,-3.76076124325672,
-3.74964330261204,-3.74184665490773,-3.73927930858579,-3.73682194472232,
-3.73450029600026,-3.73112184376486,-3.7230361537368,-3.67475064583821,
-3.61817718020949,-3.59892315249405,-3.58514643440645,-3.57929093241746,
-3.57500586756126,-3.57051526509307,-3.56362757747713,-3.54426861783956,
-3.44337221043695,-3.42929223497135,-3.41998573316167,-3.41645485421019,
-3.41402012252149,-3.41179254465429,-3.40868620732549,-3.40057653174074,
-3.35066617553326,-3.30342367805876,-3.26753425095649,-3.25938624692227,
-3.25462046029077,-3.25041620156123,-3.24514986418576,-3.23691327795004,
-3.17201045523559,-3.12129236130429,-3.1070474138008,-3.09766048185232,
-3.09411767594483,-3.09168055618969,-3.08945543886151,-3.08635859659279,
-3.07831743718965,-3.02270855622954,-2.97097056435548,-2.95305070559221,
-2.94000698244206,-2.93427582855313,-2.93001092255537,-2.92547593294475,
-2.91838505515609,-2.89748932659936,-2.88014702052472,-2.81136674876867,
-2.77857350240568,-2.77333289368799,-2.77052708218261,-2.76817160209282,
-2.76519263870322,-2.7604492421632,-2.73338088581184,-2.70810953216271,
-2.69294723752461),.UNSPECIFIED.);
#1383=B_SPLINE_CURVE_WITH_KNOTS('',3,(#33900,#33901,#33902,#33903,#33904,
#33905,#33906,#33907,#33908,#33909,#33910,#33911,#33912,#33913,#33914,#33915,
#33916,#33917,#33918,#33919,#33920,#33921,#33922,#33923,#33924,#33925,#33926,
#33927,#33928,#33929,#33930,#33931,#33932,#33933,#33934,#33935,#33936,#33937,
#33938,#33939,#33940,#33941,#33942,#33943,#33944,#33945,#33946,#33947,#33948,
#33949,#33950,#33951,#33952,#33953,#33954,#33955,#33956,#33957,#33958,#33959,
#33960,#33961,#33962,#33963,#33964,#33965,#33966,#33967,#33968,#33969,#33970,
#33971,#33972,#33973,#33974,#33975,#33976,#33977,#33978,#33979,#33980,#33981,
#33982,#33983,#33984,#33985,#33986,#33987,#33988,#33989,#33990,#33991,#33992,
#33993,#33994,#33995,#33996,#33997,#33998,#33999,#34000,#34001,#34002,#34003,
#34004,#34005,#34006,#34007,#34008,#34009,#34010,#34011,#34012,#34013,#34014,
#34015,#34016,#34017,#34018,#34019,#34020,#34021,#34022,#34023,#34024,#34025,
#34026,#34027,#34028,#34029,#34030,#34031,#34032,#34033,#34034,#34035,#34036,
#34037,#34038,#34039,#34040,#34041),.UNSPECIFIED.,.F.,.F.,(4,2,2,2,2,2,
2,2,2,2,2,2,2,2,2,2,2,2,2,2,2,2,2,2,2,2,2,2,2,2,2,2,2,2,2,2,2,2,2,2,2,2,
2,2,2,2,2,2,2,2,2,2,2,2,2,2,2,2,2,2,2,2,2,2,2,2,2,2,2,2,4),(-1.36980481141947,
-1.32341652796323,-1.27554671181702,-1.26742186076528,-1.2621910509795,
-1.25799212879625,-1.25320754541437,-1.24496482175383,-1.20743934642901,
-1.16273276497357,-1.1119896360613,-1.10389063917951,-1.10078687684696,
-1.0985608209876,-1.09612743440691,-1.09259814632891,-1.08329385649739,
-1.06921796811361,-0.968326292839698,-0.948978200079611,-0.942094196417019,
-0.937606050009271,-0.933323402980211,-0.927471381383577,-0.913704248453021,
-0.894463308978411,-0.837965362967141,-0.815715503893684,-0.806691117916107,
-0.784452820163578,-0.779530684541559,-0.776764726520455,-0.774407813870399,
-0.771382242225817,-0.765049905095009,-0.756568868566862,-0.735032763017293,
-0.668117090842425,-0.6299509699465,-0.621453761635813,-0.616564217155136,
-0.612374462419738,-0.607282778632391,-0.597591800752157,-0.535403448686576,
-0.465872499601115,-0.458460244996091,-0.45555576035116,-0.453162684317778,
-0.450611210514127,-0.446528747710044,-0.432781060465283,-0.408343299636457,
-0.328722171973697,-0.305241944957634,-0.297850193116277,-0.293252005429176,
-0.289185204219945,-0.283730560321841,-0.277790856802232,-0.267906981290785,
-0.247311259963206,-0.182682624183383,-0.140768332805188,-0.135193403957654,
-0.13228276483854,-0.129931615999683,-0.127070746644813,-0.121561146140149,
-0.0772847850799816,-0.000952358992618726),.UNSPECIFIED.);
#1384=B_SPLINE_CURVE_WITH_KNOTS('',3,(#34042,#34043,#34044,#34045,#34046,
#34047,#34048,#34049,#34050,#34051,#34052,#34053,#34054,#34055,#34056,#34057,
#34058,#34059,#34060,#34061,#34062,#34063,#34064,#34065,#34066,#34067,#34068,
#34069,#34070,#34071,#34072,#34073,#34074,#34075,#34076,#34077,#34078,#34079,
#34080,#34081,#34082,#34083,#34084,#34085,#34086,#34087,#34088,#34089,#34090,
#34091,#34092,#34093,#34094,#34095,#34096,#34097,#34098,#34099,#34100,#34101,
#34102,#34103,#34104,#34105,#34106,#34107,#34108,#34109,#34110,#34111,#34112,
#34113,#34114,#34115,#34116,#34117,#34118,#34119),.UNSPECIFIED.,.F.,.F.,
(4,2,2,2,2,2,2,2,2,2,2,2,2,2,2,2,2,2,2,2,2,2,2,2,2,2,2,2,2,2,2,2,2,2,2,
2,2,2,4),(-4.06145513647978,-4.0422638812803,-4.03712630964723,-4.03307460276732,
-4.02895028033439,-4.024215669444,-4.01619757626936,-3.98971687449884,-3.90906896261304,
-3.87808367814854,-3.87290930175311,-3.87011910938599,-3.86776485288048,
-3.86477243364192,-3.8599796077253,-3.83164267722664,-3.74766161698994,
-3.73003418075558,-3.72116690810042,-3.71374178296504,-3.71032224720732,
-3.70621477598371,-3.70136056789861,-3.6930168007416,-3.65776196781635,
-3.58879107135689,-3.56646281699231,-3.55777612704599,-3.55132561329452,
-3.54827763231599,-3.5459191678788,-3.54316981152524,-3.53831967340618,
-3.51714447982317,-3.50633181035696,-3.48468857206439,-3.42825403950671,
-3.40902715140468,-3.40027864395219),.UNSPECIFIED.);
#1385=B_SPLINE_CURVE_WITH_KNOTS('',3,(#34120,#34121,#34122,#34123,#34124,
#34125,#34126,#34127,#34128,#34129,#34130,#34131,#34132,#34133,#34134,#34135,
#34136,#34137,#34138,#34139,#34140,#34141,#34142,#34143,#34144,#34145,#34146,
#34147,#34148,#34149,#34150,#34151,#34152,#34153,#34154,#34155,#34156,#34157,
#34158,#34159,#34160,#34161,#34162,#34163,#34164,#34165,#34166,#34167,#34168,
#34169,#34170,#34171,#34172,#34173,#34174,#34175,#34176,#34177,#34178,#34179,
#34180,#34181,#34182,#34183,#34184,#34185,#34186,#34187,#34188,#34189,#34190,
#34191,#34192,#34193,#34194,#34195,#34196,#34197,#34198,#34199,#34200,#34201,
#34202,#34203,#34204,#34205,#34206,#34207,#34208,#34209,#34210,#34211,#34212,
#34213,#34214,#34215,#34216,#34217,#34218,#34219,#34220,#34221,#34222,#34223,
#34224,#34225,#34226,#34227,#34228,#34229,#34230,#34231,#34232,#34233,#34234,
#34235,#34236,#34237,#34238,#34239,#34240,#34241,#34242,#34243,#34244,#34245,
#34246,#34247,#34248,#34249,#34250,#34251,#34252,#34253,#34254,#34255,#34256,
#34257,#34258,#34259,#34260,#34261,#34262,#34263,#34264,#34265,#34266,#34267,
#34268,#34269,#34270,#34271,#34272,#34273,#34274,#34275,#34276,#34277,#34278,
#34279,#34280,#34281,#34282,#34283,#34284,#34285,#34286,#34287,#34288,#34289,
#34290,#34291,#34292,#34293,#34294,#34295,#34296,#34297,#34298,#34299,#34300,
#34301,#34302,#34303,#34304,#34305,#34306,#34307,#34308,#34309,#34310,#34311,
#34312,#34313,#34314,#34315,#34316,#34317,#34318,#34319,#34320,#34321,#34322,
#34323,#34324,#34325,#34326,#34327,#34328,#34329,#34330,#34331,#34332,#34333,
#34334,#34335,#34336,#34337,#34338,#34339,#34340,#34341,#34342,#34343,#34344,
#34345),.UNSPECIFIED.,.F.,.F.,(4,2,2,2,2,2,2,2,2,2,2,2,2,2,2,2,2,2,2,2,
2,2,2,2,2,2,2,2,2,2,2,2,2,2,2,2,2,2,2,2,2,2,2,2,2,2,2,2,2,2,2,2,2,2,2,2,
2,2,2,2,2,2,2,2,2,2,2,2,2,2,2,2,2,2,2,2,2,2,2,2,2,2,2,2,2,2,2,2,2,2,2,2,
2,2,2,2,2,2,2,2,2,2,2,2,2,2,2,2,2,2,2,2,4),(-2.69294723752461,-2.65114166127505,
-2.63181396086124,-2.61799640926919,-2.61213315788334,-2.60784590043303,
-2.60335613546443,-2.59647601992327,-2.57717949710199,-2.47617437505175,
-2.46208757005142,-2.45277710062453,-2.44924507369218,-2.44680966336363,
-2.44458155476218,-2.44147459533425,-2.43336418601692,-2.38157162990355,
-2.37298842654651,-2.32480243453079,-2.30758873872382,-2.29494035023141,
-2.28927783393323,-2.28502293341102,-2.28101405079215,-2.27430449711245,
-2.25622315165895,-2.16995516693249,-2.13684558241765,-2.12951271702238,
-2.12630037498813,-2.12392005477092,-2.12126171208211,-2.11670430902634,
-2.09996784983596,-2.08665881394654,-2.03183369741423,-1.97954074051042,
-1.97130879662538,-1.9660428950167,-1.96183739832574,-1.95706850714249,
-1.94891095631621,-1.91290303137255,-1.86535722859543,-1.81579391890578,
-1.80765968408705,-1.8045492720663,-1.80232012024329,-1.79988521408916,
-1.79635666691738,-1.78707100068286,-1.77303702667756,-1.67331007621292,
-1.65298228369763,-1.64596485836122,-1.64144513344539,-1.63717202275139,
-1.63139494962487,-1.61808965204889,-1.59969713392372,-1.54545706187921,
-1.49319291279325,-1.48508401720847,-1.48197723602652,-1.47974919675262,
-1.47731377152151,-1.4737815900337,-1.46446980817128,-1.45038184132571,
-1.34924079925545,-1.33009444563955,-1.32323508400709,-1.31919800705343,
-1.3149576750696,-1.30938945997497,-1.29726169630753,-1.24669001698659,
-1.22062722971483,-1.17066707417821,-1.16255486676606,-1.15944791094389,
-1.15722001831758,-1.15478506997232,-1.15125410628924,-1.14194855991097,
-1.12787268113652,-1.02701120747538,-1.00765021694377,-1.00076162194502,
-0.996270360425195,-0.991984614187713,-0.986128100508921,-0.972348724095114,
-0.953088506286536,-0.896494914806161,-0.873040381868709,-0.865828054025307,
-0.843168610135076,-0.838220322747817,-0.835447281227641,-0.833089210539276,
-0.830068271402717,-0.823766420254556,-0.815339323042691,-0.79401332656967,
-0.728081236908415,-0.688745099378829,-0.680183173896067,-0.675276899599574,
-0.671124902893915,-0.666062812089729,-0.662308805568785),.UNSPECIFIED.);
#1386=B_SPLINE_CURVE_WITH_KNOTS('',3,(#34350,#34351,#34352,#34353,#34354,
#34355,#34356,#34357,#34358,#34359,#34360,#34361,#34362,#34363,#34364,#34365,
#34366,#34367,#34368,#34369,#34370,#34371,#34372,#34373,#34374,#34375,#34376,
#34377,#34378,#34379,#34380,#34381,#34382,#34383,#34384,#34385,#34386,#34387,
#34388,#34389,#34390,#34391,#34392,#34393,#34394,#34395,#34396,#34397,#34398,
#34399,#34400,#34401,#34402,#34403,#34404,#34405,#34406,#34407,#34408,#34409,
#34410,#34411,#34412,#34413,#34414,#34415,#34416,#34417,#34418,#34419,#34420,
#34421,#34422,#34423,#34424,#34425,#34426,#34427,#34428,#34429,#34430,#34431,
#34432,#34433,#34434,#34435,#34436,#34437,#34438,#34439,#34440,#34441,#34442,
#34443,#34444,#34445,#34446,#34447,#34448,#34449,#34450,#34451,#34452,#34453,
#34454,#34455,#34456,#34457,#34458,#34459,#34460,#34461,#34462,#34463,#34464,
#34465,#34466,#34467,#34468,#34469,#34470,#34471,#34472,#34473,#34474,#34475,
#34476,#34477,#34478,#34479,#34480,#34481,#34482,#34483,#34484,#34485,#34486,
#34487,#34488,#34489,#34490,#34491,#34492,#34493,#34494,#34495,#34496,#34497,
#34498,#34499,#34500,#34501,#34502,#34503,#34504,#34505,#34506,#34507,#34508,
#34509,#34510,#34511,#34512,#34513,#34514,#34515,#34516,#34517,#34518,#34519,
#34520,#34521,#34522,#34523,#34524,#34525,#34526,#34527,#34528,#34529,#34530,
#34531,#34532,#34533,#34534,#34535,#34536,#34537,#34538,#34539,#34540,#34541,
#34542,#34543,#34544,#34545,#34546,#34547,#34548,#34549,#34550,#34551,#34552,
#34553,#34554,#34555,#34556,#34557,#34558,#34559,#34560,#34561,#34562,#34563,
#34564,#34565),.UNSPECIFIED.,.F.,.F.,(4,2,2,2,2,2,2,2,2,2,2,2,2,2,2,2,2,
2,2,2,2,2,2,2,2,2,2,2,2,2,2,2,2,2,2,2,2,2,2,2,2,2,2,2,2,2,2,2,2,2,2,2,2,
2,2,2,2,2,2,2,2,2,2,2,2,2,2,2,2,2,2,2,2,2,2,2,2,2,2,2,2,2,2,2,2,2,2,2,2,
2,2,2,2,2,2,2,2,2,2,2,2,2,2,2,2,2,2,4),(-3.40037133238205,-3.3958593199486,
-3.36461546646417,-3.35943142736421,-3.35663906111019,-3.35428480070634,
-3.35129470908302,-3.34650999012586,-3.31837920720899,-3.23419825261601,
-3.21655274783487,-3.2036644360115,-3.19796339735095,-3.19370627167876,
-3.18916588739566,-3.1820379692777,-3.16081370545087,-3.06213476930674,
-3.04814411461567,-3.03888249310273,-3.03535972342486,-3.03292778189279,
-3.03070060100281,-3.0275920900534,-3.019455869361,-2.97008671586442,-2.89623041871921,
-2.88180790630273,-2.87584804982145,-2.87154627579255,-2.8676157056339,
-2.86232064216408,-2.85195609985107,-2.77070955610631,-2.72112689413215,
-2.71503129612839,-2.71205177402978,-2.70992356231367,-2.70721432005216,
-2.70254137908967,-2.68371305149385,-2.59157465470434,-2.57258995275449,
-2.5589611656633,-2.55313250144345,-2.54885396683467,-2.5443583614553,-2.53743917911911,
-2.51783342132499,-2.41720738501874,-2.40313773446656,-2.39383723351361,
-2.39030846532504,-2.38787516400173,-2.38564895831586,-2.38254471582826,
-2.37444200018048,-2.32258548975452,-2.26808310769906,-2.24964664370148,
-2.23631799341665,-2.2305396995894,-2.22626907552939,-2.22175513490086,
-2.21475326426898,-2.19452066729164,-2.1108810785795,-2.07484271013731,
-2.06950656862376,-2.06668153128964,-2.06432862136666,-2.06137659699598,
-2.05671950955988,-2.03127784426511,-1.95202516198594,-1.91905425562225,
-1.91088583218888,-1.90607042791539,-1.90187447426128,-1.89668623178858,
-1.88652523567147,-1.87352770166731,-1.84275512796906,-1.77770978290299,
-1.75210906098205,-1.74744428462096,-1.74448998382192,-1.74213703485185,
-1.73931406332338,-1.73398756143383,-1.69828432680799,-1.61866415959717,
-1.59497847791425,-1.58756282683782,-1.5829589000224,-1.57872303241422,
-1.57316971161573,-1.56111123827875,-1.51110459863466,-1.46986828877692,
-1.43039794495249,-1.42533913716731,-1.42229975558202,-1.41993645468558,
-1.41721389594947,-1.41235617664627,-1.38842975984289,-1.36980481141947),
 .UNSPECIFIED.);
#1387=B_SPLINE_CURVE_WITH_KNOTS('',3,(#34567,#34568,#34569,#34570,#34571,
#34572,#34573,#34574,#34575,#34576,#34577,#34578,#34579,#34580,#34581,#34582,
#34583,#34584,#34585,#34586,#34587,#34588,#34589,#34590,#34591,#34592,#34593,
#34594,#34595,#34596,#34597,#34598,#34599,#34600,#34601,#34602,#34603,#34604,
#34605,#34606,#34607,#34608,#34609,#34610,#34611,#34612,#34613,#34614,#34615,
#34616,#34617,#34618,#34619,#34620,#34621,#34622,#34623,#34624,#34625,#34626,
#34627,#34628,#34629,#34630,#34631,#34632,#34633,#34634,#34635,#34636,#34637,
#34638,#34639,#34640,#34641,#34642),.UNSPECIFIED.,.F.,.F.,(4,2,2,2,2,2,
2,2,2,2,2,2,2,2,2,2,2,2,2,2,2,2,2,2,2,2,2,2,2,2,2,2,2,2,2,2,2,4),(-0.662308805568785,
-0.656525263118195,-0.586929482800625,-0.525386354673078,-0.517571766729085,
-0.514510554571795,-0.512294682743695,-0.509848358376822,-0.506259578976813,
-0.496556046832651,-0.435653921453166,-0.372625495080247,-0.360019643289771,
-0.354426724262138,-0.350168227778875,-0.349648983064658,-0.345057398224343,
-0.340228047237268,-0.333051091433346,-0.320033327103222,-0.289193350981699,
-0.221973600570761,-0.198484353892505,-0.193484794861598,-0.190700046208865,
-0.188342919706885,-0.185337144945508,-0.179114016182033,-0.170822245801388,
-0.150006585591807,-0.0660721055234023,-0.0417239069242697,-0.0342311404955614,
-0.0296087078489306,-0.0255413886337936,-0.021440687782664,-0.016153695933201,
-0.000950919900370663),.UNSPECIFIED.);
#1388=B_SPLINE_CURVE_WITH_KNOTS('',3,(#34643,#34644,#34645,#34646,#34647,
#34648,#34649,#34650,#34651,#34652,#34653,#34654,#34655,#34656,#34657,#34658,
#34659,#34660,#34661,#34662,#34663,#34664,#34665,#34666,#34667,#34668,#34669,
#34670,#34671,#34672,#34673,#34674,#34675,#34676,#34677,#34678,#34679,#34680,
#34681,#34682,#34683,#34684,#34685,#34686,#34687,#34688,#34689,#34690,#34691,
#34692,#34693,#34694,#34695,#34696,#34697,#34698,#34699,#34700,#34701,#34702,
#34703,#34704,#34705,#34706,#34707,#34708,#34709,#34710,#34711,#34712,#34713,
#34714,#34715,#34716,#34717,#34718,#34719,#34720,#34721,#34722,#34723,#34724,
#34725,#34726,#34727,#34728,#34729,#34730,#34731,#34732,#34733,#34734,#34735,
#34736,#34737,#34738,#34739,#34740,#34741,#34742,#34743,#34744,#34745,#34746,
#34747,#34748,#34749,#34750,#34751,#34752,#34753,#34754,#34755,#34756,#34757,
#34758,#34759,#34760,#34761,#34762,#34763,#34764,#34765,#34766,#34767,#34768,
#34769,#34770,#34771,#34772,#34773,#34774,#34775,#34776,#34777,#34778,#34779,
#34780),.UNSPECIFIED.,.F.,.F.,(4,2,2,2,2,2,2,2,2,2,2,2,2,2,2,2,2,2,2,2,
2,2,2,2,2,2,2,2,2,2,2,2,2,2,2,2,2,2,2,2,2,2,2,2,2,2,2,2,2,2,2,2,2,2,2,2,
2,2,2,2,2,2,2,2,2,2,2,2,4),(-4.06059553295812,-3.95888332605128,-3.93524837446757,
-3.93040575401771,-3.92768599130884,-3.9253213196809,-3.92227524286053,
-3.91719504024668,-3.87604943766431,-3.81089170722431,-3.79021971726244,
-3.78030903390612,-3.77435754711254,-3.76892484895596,-3.76485148118313,
-3.76082383198741,-3.75400802355856,-3.73516237649858,-3.63364989820849,
-3.61954751977705,-3.61023032757608,-3.60669808252017,-3.60426325835415,
-3.60203627375543,-3.59893165064515,-3.59083310374198,-3.5404802435321,
-3.49355026739594,-3.45777721116723,-3.4496370066841,-3.44487322144071,
-3.44066918150538,-3.43540106762591,-3.42715768475613,-3.36386456999922,
-3.31186737826032,-3.29744028523237,-3.28796528639471,-3.28440978594458,
-3.28197032439139,-3.27974813701758,-3.27666196438192,-3.26869178579942,
-3.21093535955183,-3.18768781178593,-3.14124329271754,-3.12961283582514,
-3.12413720850642,-3.11991011376656,-3.11526540704156,-3.10767013904823,
-3.0824281790699,-3.01283257539637,-2.96930448439377,-2.96380394537079,
-2.96094378331988,-2.95859093184779,-2.95567520464474,-2.95008214425666,
-2.90249776912101,-2.86138340768888,-2.81825850899877,-2.80704977295758,
-2.8016538299286,-2.79743629801213,-2.79274908381092,-2.7849605057298,-2.75779268177983,
-2.69191355936612),.UNSPECIFIED.);
#1389=B_SPLINE_CURVE_WITH_KNOTS('',3,(#34786,#34787,#34788,#34789,#34790,
#34791,#34792,#34793,#34794,#34795,#34796,#34797,#34798,#34799,#34800,#34801,
#34802,#34803,#34804,#34805,#34806,#34807,#34808,#34809,#34810,#34811,#34812,
#34813,#34814,#34815,#34816,#34817,#34818,#34819,#34820,#34821,#34822,#34823,
#34824,#34825,#34826,#34827,#34828,#34829,#34830,#34831,#34832,#34833,#34834,
#34835,#34836,#34837,#34838,#34839,#34840,#34841,#34842,#34843,#34844,#34845,
#34846,#34847,#34848,#34849,#34850,#34851,#34852,#34853,#34854,#34855,#34856,
#34857,#34858,#34859,#34860,#34861,#34862,#34863,#34864,#34865,#34866,#34867,
#34868,#34869,#34870,#34871,#34872,#34873,#34874,#34875,#34876,#34877,#34878,
#34879,#34880,#34881,#34882,#34883,#34884,#34885,#34886,#34887,#34888,#34889,
#34890,#34891,#34892,#34893,#34894,#34895,#34896,#34897,#34898,#34899,#34900,
#34901,#34902,#34903,#34904,#34905,#34906,#34907,#34908,#34909,#34910,#34911,
#34912,#34913,#34914,#34915,#34916,#34917,#34918,#34919,#34920,#34921,#34922,
#34923,#34924,#34925,#34926,#34927,#34928,#34929),.UNSPECIFIED.,.F.,.F.,
(4,2,2,2,2,2,2,2,2,2,2,2,2,2,2,2,2,2,2,2,2,2,2,2,2,2,2,2,2,2,2,2,2,2,2,
2,2,2,2,2,2,2,2,2,2,2,2,2,2,2,2,2,2,2,2,2,2,2,2,2,2,2,2,2,2,2,2,2,2,2,2,
4),(-1.37014057674011,-1.37000038523809,-1.3193807857946,-1.29516072778694,
-1.28794739647049,-1.23944085044802,-1.23437673038055,-1.23133618776153,
-1.22897325908904,-1.22625261996907,-1.22140184539273,-1.19758604490048,
-1.13325547782832,-1.08466057967899,-1.0765147763891,-1.07127828277985,
-1.06707981996203,-1.06230119291961,-1.05408248317551,-1.01694453485038,
-0.971984850747004,-0.921098890522783,-0.913002195714879,-0.90989923696995,
-0.907673737784872,-0.905240936806457,-0.901712459963499,-0.892410089673449,
-0.878336912946387,-0.777450761854404,-0.758123107234341,-0.751242968602848,
-0.746756388476347,-0.742474540756264,-0.736622507855895,-0.722850111069251,
-0.703597973752917,-0.647026385171577,-0.598686011205405,-0.59058047704131,
-0.587476560923835,-0.585250979534515,-0.58281879237831,-0.579292375241125,
-0.570002155326508,-0.555953252340658,-0.455662334292326,-0.43585605009363,
-0.428911959908986,-0.424412009479871,-0.420137880887261,-0.414328645049147,
-0.400807926092358,-0.382016788533066,-0.280500189735869,-0.269127490375588,
-0.265186292790822,-0.262916720224567,-0.260516802362791,-0.25736183148815,
-0.250124370569427,-0.239787858198167,-0.210597176892684,-0.173489617417905,
-0.11762813045963,-0.109369838681646,-0.104099278939646,-0.0998978703794037,
-0.0951420049269887,-0.0870277655722719,-0.0772405797427724,-0.000952140262247388),
 .UNSPECIFIED.);
#1390=B_SPLINE_CURVE_WITH_KNOTS('',3,(#34930,#34931,#34932,#34933,#34934,
#34935,#34936,#34937,#34938,#34939,#34940,#34941,#34942,#34943,#34944,#34945,
#34946,#34947,#34948,#34949,#34950,#34951,#34952,#34953,#34954,#34955,#34956,
#34957,#34958,#34959,#34960,#34961,#34962,#34963,#34964,#34965,#34966,#34967,
#34968,#34969,#34970,#34971,#34972,#34973,#34974,#34975,#34976,#34977,#34978,
#34979,#34980,#34981,#34982,#34983,#34984,#34985,#34986,#34987,#34988,#34989,
#34990,#34991,#34992,#34993,#34994,#34995,#34996,#34997,#34998,#34999,#35000,
#35001,#35002,#35003,#35004,#35005),.UNSPECIFIED.,.F.,.F.,(4,2,2,2,2,2,
2,2,2,2,2,2,2,2,2,2,2,2,2,2,2,2,2,2,2,2,2,2,2,2,2,2,2,2,2,2,2,4),(-4.06103572343788,
-4.01111266036306,-4.00663360504596,-4.00374863469166,-4.00102817468496,
-3.99866538066405,-3.99562502280188,-3.99056125606958,-3.95060498761795,
-3.91948798465717,-3.89209660458075,-3.85648947981115,-3.84666528987173,
-3.84154653290425,-3.83735595568599,-3.83248973437651,-3.82409407820223,
-3.78771106943414,-3.72495828224382,-3.69921592901282,-3.68967868648822,
-3.68281122484818,-3.67968765308805,-3.67731308089062,-3.6746474636272,
-3.67004803658893,-3.6527550430313,-3.64006081604174,-3.61770346282282,
-3.5797117837695,-3.53230129714135,-3.52359491254894,-3.51871081598452,
-3.51494140355726,-3.51002247526951,-3.50139420653846,-3.46063952180805,
-3.40037133238205),.UNSPECIFIED.);
#1391=B_SPLINE_CURVE_WITH_KNOTS('',3,(#35006,#35007,#35008,#35009,#35010,
#35011,#35012,#35013,#35014,#35015,#35016,#35017,#35018,#35019,#35020,#35021,
#35022,#35023,#35024,#35025,#35026,#35027,#35028,#35029,#35030,#35031,#35032,
#35033,#35034,#35035,#35036,#35037,#35038,#35039,#35040,#35041,#35042,#35043,
#35044,#35045,#35046,#35047,#35048,#35049,#35050,#35051,#35052,#35053,#35054,
#35055,#35056,#35057,#35058,#35059,#35060,#35061,#35062,#35063,#35064,#35065,
#35066,#35067,#35068,#35069,#35070,#35071,#35072,#35073,#35074,#35075,#35076,
#35077,#35078,#35079,#35080,#35081,#35082,#35083,#35084,#35085,#35086,#35087,
#35088,#35089,#35090,#35091,#35092,#35093,#35094,#35095,#35096,#35097,#35098,
#35099,#35100,#35101,#35102,#35103,#35104,#35105,#35106,#35107,#35108,#35109,
#35110,#35111,#35112,#35113,#35114,#35115,#35116,#35117,#35118,#35119,#35120,
#35121,#35122,#35123,#35124,#35125,#35126,#35127,#35128,#35129,#35130,#35131,
#35132,#35133,#35134,#35135,#35136,#35137,#35138,#35139,#35140,#35141,#35142,
#35143,#35144,#35145,#35146,#35147,#35148,#35149,#35150,#35151,#35152,#35153,
#35154,#35155,#35156,#35157,#35158,#35159,#35160,#35161,#35162,#35163,#35164,
#35165,#35166,#35167,#35168,#35169,#35170,#35171,#35172,#35173,#35174,#35175,
#35176,#35177,#35178,#35179,#35180,#35181,#35182,#35183,#35184,#35185,#35186,
#35187,#35188,#35189,#35190,#35191,#35192,#35193,#35194,#35195,#35196,#35197,
#35198,#35199,#35200,#35201,#35202,#35203,#35204,#35205,#35206,#35207,#35208,
#35209,#35210,#35211,#35212,#35213,#35214,#35215,#35216,#35217,#35218,#35219,
#35220,#35221,#35222,#35223,#35224,#35225,#35226,#35227),.UNSPECIFIED.,
 .F.,.F.,(4,2,2,2,2,2,2,2,2,2,2,2,2,2,2,2,2,2,2,2,2,2,2,2,2,2,2,2,2,2,2,
2,2,2,2,2,2,2,2,2,2,2,2,2,2,2,2,2,2,2,2,2,2,2,2,2,2,2,2,2,2,2,2,2,2,2,2,
2,2,2,2,2,2,2,2,2,2,2,2,2,2,2,2,2,2,2,2,2,2,2,2,2,2,2,2,2,2,2,2,2,2,2,2,
2,2,2,2,2,2,2,4),(-2.69191355936612,-2.68184878374859,-2.64962750863557,
-2.6423934893288,-2.63919927472136,-2.63682209906018,-2.6341558565772,-2.62956020432886,
-2.61234432288922,-2.60098330413407,-2.57591806016906,-2.52723694506063,
-2.49083173187507,-2.48265195503412,-2.47787911405952,-2.47367556933407,
-2.4684192931653,-2.46021634347588,-2.40956999335524,-2.34700678403509,
-2.32346880895875,-2.31863028669715,-2.31591079164253,-2.31354501199639,
-2.31049580633884,-2.30540686246707,-2.26354995187619,-2.25253134760833,
-2.20458580732447,-2.16844021601739,-2.16027583885786,-2.15550616301101,
-2.15130190097621,-2.14604009487562,-2.13781946487149,-2.07571383695125,
-2.03064006336576,-2.0172676511193,-2.00058561198714,-1.99603367598981,
-1.99337692070661,-1.99099685029287,-1.98778329614877,-1.98044105258042,
-1.94724040026906,-1.85898861116881,-1.84253512974541,-1.83607419011304,
-1.83211250147999,-1.82782980143794,-1.82199251772878,-1.80832941595,-1.78928348067018,
-1.71356839938967,-1.67979596935156,-1.67481446707291,-1.67176421796371,
-1.6694034362481,-1.66665058441141,-1.66165818261176,-1.63512630614493,
-1.54858834939047,-1.52257507285416,-1.51490265947789,-1.51024077814487,
-1.50601742010814,-1.50057394912769,-1.48911607922425,-1.44404879580986,
-1.38460954364073,-1.35696735814146,-1.35219985850398,-1.34921368769467,
-1.34685785045237,-1.34405792536757,-1.33884490053971,-1.30685847525199,
-1.23957586650359,-1.20188800449964,-1.19341244981074,-1.18852555077207,
-1.18433224302438,-1.17922894686774,-1.16949301778481,-1.10613369689557,
-1.03807709736447,-1.03067441271345,-1.02768293077643,-1.02526607947621,
-1.0227474627466,-1.01881996720616,-1.00649400665832,-0.985670887700816,
-0.941849897092128,-0.880505614273177,-0.872254895929421,-0.866984078665993,
-0.862779174994307,-0.858015794923948,-0.849879749482219,-0.814192933173186,
-0.767509422180126,-0.716720398314151,-0.708620216122763,-0.705514949368648,
-0.703287539502368,-0.700852270274692,-0.697319430457627,-0.688000821502116,
-0.673898053427717,-0.661876260241505),.UNSPECIFIED.);
#1392=B_SPLINE_CURVE_WITH_KNOTS('',3,(#35232,#35233,#35234,#35235,#35236,
#35237,#35238,#35239,#35240,#35241,#35242,#35243,#35244,#35245,#35246,#35247,
#35248,#35249,#35250,#35251,#35252,#35253,#35254,#35255,#35256,#35257,#35258,
#35259,#35260,#35261,#35262,#35263,#35264,#35265,#35266,#35267,#35268,#35269,
#35270,#35271,#35272,#35273,#35274,#35275,#35276,#35277,#35278,#35279,#35280,
#35281,#35282,#35283,#35284,#35285,#35286,#35287,#35288,#35289,#35290,#35291,
#35292,#35293,#35294,#35295,#35296,#35297,#35298,#35299,#35300,#35301,#35302,
#35303,#35304,#35305,#35306,#35307,#35308,#35309,#35310,#35311,#35312,#35313,
#35314,#35315,#35316,#35317,#35318,#35319,#35320,#35321,#35322,#35323,#35324,
#35325,#35326,#35327,#35328,#35329,#35330,#35331,#35332,#35333,#35334,#35335,
#35336,#35337,#35338,#35339,#35340,#35341,#35342,#35343,#35344,#35345,#35346,
#35347,#35348,#35349,#35350,#35351,#35352,#35353,#35354,#35355,#35356,#35357,
#35358,#35359,#35360,#35361,#35362,#35363,#35364,#35365,#35366,#35367,#35368,
#35369,#35370,#35371,#35372,#35373,#35374,#35375,#35376,#35377,#35378,#35379,
#35380,#35381,#35382,#35383,#35384,#35385,#35386,#35387,#35388,#35389,#35390,
#35391,#35392,#35393,#35394,#35395,#35396,#35397,#35398,#35399,#35400,#35401,
#35402,#35403,#35404,#35405,#35406,#35407,#35408,#35409,#35410,#35411,#35412,
#35413,#35414,#35415,#35416,#35417,#35418,#35419,#35420,#35421,#35422,#35423,
#35424,#35425,#35426,#35427,#35428,#35429,#35430,#35431,#35432,#35433,#35434,
#35435,#35436,#35437,#35438,#35439,#35440,#35441,#35442,#35443,#35444,#35445,
#35446,#35447,#35448,#35449,#35450,#35451),.UNSPECIFIED.,.F.,.F.,(4,2,2,
2,2,2,2,2,2,2,2,2,2,2,2,2,2,2,2,2,2,2,2,2,2,2,2,2,2,2,2,2,2,2,2,2,2,2,2,
2,2,2,2,2,2,2,2,2,2,2,2,2,2,2,2,2,2,2,2,2,2,2,2,2,2,2,2,2,2,2,2,2,2,2,2,
2,2,2,2,2,2,2,2,2,2,2,2,2,2,2,2,2,2,2,2,2,2,2,2,2,2,2,2,2,2,2,2,2,2,4),
(-3.40033477739996,-3.36451418220255,-3.33850355115555,-3.33111351743207,
-3.32651564670777,-3.32227874675779,-3.31680827106374,-3.30487416089585,
-3.22773898162582,-3.1900469364208,-3.1779632482735,-3.16966070836856,-3.16628663904097,
-3.16388241527472,-3.16161871469554,-3.15770866018037,-3.14656464589143,
-3.08084765441228,-3.03933910296471,-3.01564263934699,-3.00848007315647,
-3.00393170810425,-2.99967690825306,-2.99409202163094,-2.98151862627548,
-2.92133643796569,-2.85769459535463,-2.84781615646045,-2.84420395718218,
-2.84175404779108,-2.83954465736003,-2.8365049872345,-2.82881132234366,
-2.76535631732625,-2.69747729850175,-2.68798195818182,-2.6829306540106,
-2.67878167373204,-2.67387214990161,-2.66528724282318,-2.62543708055649,
-2.55987084501661,-2.5284221931878,-2.52323029540692,-2.5204360395077,-2.51808159580471,
-2.51509306688751,-2.51031421349815,-2.48233870089724,-2.45774467888692,
-2.4178293170681,-2.38844757720453,-2.37584418266547,-2.3659262246695,-2.36078758776022,
-2.35659508371772,-2.35174273491474,-2.34341105506712,-2.30803325116887,
-2.23907837074787,-2.20615423957555,-2.20091164713636,-2.19810650158538,
-2.19575265274773,-2.19277726726955,-2.18804246373164,-2.16113197020524,
-2.13615846063419,-2.07881470212002,-2.05942088174506,-2.0455690874852,
-2.03970235134988,-2.03541660506637,-2.03146508881164,-2.02505016896687,
-2.0075942793239,-1.98108989651934,-1.93815233230172,-1.88842594322002,
-1.88030431591139,-1.87719744081582,-1.87497052391221,-1.8725377919158,
-1.86901210387502,-1.85973251796886,-1.84570732505606,-1.74611642997218,
-1.72568507524278,-1.71865819485597,-1.71413920400873,-1.70987168243653,
-1.70410980422073,-1.6908745101837,-1.67260435650092,-1.61900483391207,
-1.56587908927099,-1.55778575098311,-1.5546829209477,-1.5524572234158,-1.55002386706463,
-1.54649402176984,-1.5371848040134,-1.52309842385622,-1.42191052763166,
-1.40281271601991,-1.39596380719189,-1.39193125184546,-1.38769452300188,
-1.38212917220927,-1.37014057674011),.UNSPECIFIED.);
#1393=B_SPLINE_CURVE_WITH_KNOTS('',3,(#35453,#35454,#35455,#35456,#35457,
#35458,#35459,#35460,#35461,#35462,#35463,#35464,#35465,#35466,#35467,#35468,
#35469,#35470,#35471,#35472,#35473,#35474,#35475,#35476,#35477,#35478,#35479,
#35480,#35481,#35482,#35483,#35484,#35485,#35486,#35487,#35488,#35489,#35490,
#35491,#35492,#35493,#35494,#35495,#35496,#35497,#35498,#35499,#35500,#35501,
#35502,#35503,#35504,#35505,#35506,#35507,#35508,#35509,#35510,#35511,#35512,
#35513,#35514,#35515,#35516,#35517,#35518,#35519,#35520,#35521,#35522),
 .UNSPECIFIED.,.F.,.F.,(4,2,2,2,2,2,2,2,2,2,2,2,2,2,2,2,2,2,2,2,2,2,2,2,
2,2,2,2,2,2,2,2,2,2,4),(-0.661876260241505,-0.572320924024388,-0.553546536125019,
-0.546739796163848,-0.542713278014369,-0.538469198202907,-0.5328711239966,
-0.520575991442001,-0.503980548303871,-0.458702214209073,-0.393461964550517,
-0.385869562379819,-0.382858738152879,-0.380655689035602,-0.378195099557297,
-0.37464115581892,-0.364986332431045,-0.30404935934828,-0.240988525311571,
-0.229681154669253,-0.223539690090359,-0.219245040381863,-0.214841833708473,
-0.2083721085236,-0.190531876219844,-0.141603338064727,-0.106446414563869,
-0.0678662765952388,-0.0628192245705687,-0.0597824591305558,-0.0574183589611437,
-0.0551959211726501,-0.0524918835236233,-0.0484568488096544,-0.000950994778662939),
 .UNSPECIFIED.);
#1394=B_SPLINE_CURVE_WITH_KNOTS('',3,(#35523,#35524,#35525,#35526,#35527,
#35528,#35529,#35530,#35531,#35532,#35533,#35534,#35535,#35536,#35537,#35538,
#35539,#35540,#35541,#35542,#35543,#35544,#35545,#35546,#35547,#35548,#35549,
#35550,#35551,#35552,#35553,#35554,#35555,#35556,#35557,#35558,#35559,#35560,
#35561,#35562,#35563,#35564,#35565,#35566,#35567,#35568,#35569,#35570,#35571,
#35572,#35573,#35574,#35575,#35576,#35577,#35578,#35579,#35580,#35581,#35582,
#35583,#35584,#35585,#35586,#35587,#35588,#35589,#35590,#35591,#35592,#35593,
#35594,#35595,#35596,#35597,#35598,#35599,#35600,#35601,#35602,#35603,#35604,
#35605,#35606,#35607,#35608,#35609,#35610,#35611,#35612,#35613,#35614,#35615,
#35616,#35617,#35618,#35619,#35620,#35621,#35622,#35623,#35624,#35625,#35626,
#35627,#35628,#35629,#35630,#35631,#35632,#35633,#35634,#35635,#35636,#35637,
#35638,#35639,#35640,#35641,#35642,#35643,#35644,#35645,#35646,#35647,#35648,
#35649,#35650,#35651,#35652,#35653,#35654,#35655,#35656,#35657,#35658,#35659,
#35660,#35661,#35662),.UNSPECIFIED.,.F.,.F.,(4,2,2,2,2,2,2,2,2,2,2,2,2,
2,2,2,2,2,2,2,2,2,2,2,2,2,2,2,2,2,2,2,2,2,2,2,2,2,2,2,2,2,2,2,2,2,2,2,2,
2,2,2,2,2,2,2,2,2,2,2,2,2,2,2,2,2,2,2,2,4),(-4.06190321821732,-3.99422219017382,
-3.97055969618172,-3.96339910922043,-3.95885005861324,-3.95459322681607,
-3.94900360402586,-3.93641013908849,-3.8748315541624,-3.82586292660814,
-3.81187828161991,-3.80272526927325,-3.79927138958828,-3.79681032664915,
-3.79460892351872,-3.7916029889917,-3.78411212354339,-3.71793194295498,
-3.6733174284296,-3.65686896625554,-3.64465770667096,-3.6390757450808,-3.63483492100245,
-3.63080480393728,-3.62397561334912,-3.60503312976436,-3.50364423680699,
-3.48954690802705,-3.48023227199527,-3.47670048658262,-3.47426581837415,
-3.47203884804385,-3.46893407685902,-3.46083389013004,-3.41047959829797,
-3.36355562486356,-3.32778547468295,-3.31964567368704,-3.31488208908652,
-3.31067820477749,-3.30541025749043,-3.29716707957948,-3.23382824406505,
-3.16813114773904,-3.15812373709248,-3.15449216483051,-3.15203728119064,
-3.14982966319807,-3.14680030871249,-3.13917403202114,-3.07407371279547,
-3.02880893743353,-3.01221655438943,-2.99992222681121,-2.99432438848688,
-2.990080422085,-2.9860539490331,-2.97924718064494,-2.96047213070521,-2.85884726887721,
-2.84473855296375,-2.83541776800587,-2.83188454890107,-2.82944917580603,
-2.82722178686823,-2.82411672792176,-2.81601799617708,-2.76521927448344,
-2.72039759015022,-2.69283977885968),.UNSPECIFIED.);
#1395=B_SPLINE_CURVE_WITH_KNOTS('',3,(#35668,#35669,#35670,#35671,#35672,
#35673,#35674,#35675,#35676,#35677,#35678,#35679,#35680,#35681,#35682,#35683,
#35684,#35685,#35686,#35687,#35688,#35689,#35690,#35691,#35692,#35693,#35694,
#35695,#35696,#35697,#35698,#35699,#35700,#35701,#35702,#35703,#35704,#35705,
#35706,#35707,#35708,#35709,#35710,#35711,#35712,#35713,#35714,#35715,#35716,
#35717,#35718,#35719,#35720,#35721,#35722,#35723,#35724,#35725,#35726,#35727,
#35728,#35729,#35730,#35731,#35732,#35733,#35734,#35735,#35736,#35737,#35738,
#35739,#35740,#35741,#35742,#35743,#35744,#35745,#35746,#35747,#35748,#35749,
#35750,#35751,#35752,#35753,#35754,#35755,#35756,#35757,#35758,#35759,#35760,
#35761,#35762,#35763,#35764,#35765,#35766,#35767,#35768,#35769,#35770,#35771,
#35772,#35773,#35774,#35775,#35776,#35777,#35778,#35779,#35780,#35781,#35782,
#35783,#35784,#35785,#35786,#35787,#35788,#35789,#35790,#35791,#35792,#35793,
#35794,#35795,#35796,#35797,#35798,#35799,#35800,#35801,#35802,#35803,#35804,
#35805,#35806,#35807,#35808,#35809,#35810,#35811,#35812,#35813,#35814,#35815,
#35816,#35817,#35818,#35819),.UNSPECIFIED.,.F.,.F.,(4,2,2,2,2,2,2,2,2,2,
2,2,2,2,2,2,2,2,2,2,2,2,2,2,2,2,2,2,2,2,2,2,2,2,2,2,2,2,2,2,2,2,2,2,2,2,
2,2,2,2,2,2,2,2,2,2,2,2,2,2,2,2,2,2,2,2,2,2,2,2,2,2,2,2,2,4),(-1.36941396256219,
-1.36567125877387,-1.36256519446724,-1.3603385606735,-1.35790579117546,
-1.35437947282384,-1.3450949253861,-1.33105934135082,-1.23119524877981,
-1.2109976269388,-1.20400105397277,-1.1994887562077,-1.19521841603027,-1.18943853237784,
-1.17609730223273,-1.15763496963987,-1.10298764942891,-1.09179077007889,
-1.04736457836952,-1.04177860583558,-1.03886563031094,-1.03651450757192,
-1.0336559940036,-1.02815750410302,-0.984557784383335,-0.914759998588243,
-0.889775031193937,-0.882217711290876,-0.877583393414395,-0.873357408829341,
-0.867871374442199,-0.856173209670865,-0.809150724069344,-0.761825987984907,
-0.724874978609838,-0.719855993301959,-0.716828534531096,-0.714466915061892,
-0.711737384530986,-0.706846024282249,-0.682280119155158,-0.633661570419317,
-0.570348738278909,-0.562109401936436,-0.556844416364295,-0.552643297270848,
-0.547883314433281,-0.539750969759379,-0.504048928642275,-0.457305903810248,
-0.406599904726469,-0.398502409888869,-0.395399233446972,-0.393173600361015,
-0.39074067891769,-0.387554196341755,-0.37943853462475,-0.367584231869073,
-0.331091999866335,-0.264847340178948,-0.24414433185155,-0.237073252008063,
-0.232544979681656,-0.228282230844111,-0.22254764351051,-0.21017947980432,
-0.166197233753262,-0.128329136877823,-0.0803772908676197,-0.074784322698507,
-0.0718699129930306,-0.0695188657834898,-0.0666619408875339,-0.063582754698667,
-0.0586294751953665,-0.000951400989500799),.UNSPECIFIED.);
#1396=B_SPLINE_CURVE_WITH_KNOTS('',3,(#35820,#35821,#35822,#35823,#35824,
#35825,#35826,#35827,#35828,#35829,#35830,#35831,#35832,#35833,#35834,#35835,
#35836,#35837,#35838,#35839,#35840,#35841,#35842,#35843,#35844,#35845,#35846,
#35847,#35848,#35849,#35850,#35851,#35852,#35853,#35854,#35855,#35856,#35857,
#35858,#35859,#35860,#35861,#35862,#35863,#35864,#35865,#35866,#35867,#35868,
#35869,#35870,#35871,#35872,#35873,#35874,#35875,#35876,#35877,#35878,#35879,
#35880,#35881,#35882,#35883,#35884,#35885,#35886,#35887,#35888,#35889),
 .UNSPECIFIED.,.F.,.F.,(4,2,2,2,2,2,2,2,2,2,2,2,2,2,2,2,2,2,2,2,2,2,2,2,
2,2,2,2,2,2,2,2,2,2,4),(-4.06178433014842,-4.00353083390514,-3.98468044596785,
-3.97655881826495,-3.97180080007593,-3.96759880296338,-3.96232925015822,
-3.95407588946756,-3.8991026474051,-3.85978061779031,-3.81936128801146,
-3.81347417331262,-3.81048213195841,-3.80812750190857,-3.80533605518293,
-3.80030150671206,-3.77615673484903,-3.69579946579093,-3.66229614839818,
-3.65416274448491,-3.64940234866229,-3.64520098502292,-3.63993585289152,
-3.6316965273176,-3.56800979274994,-3.51680918182206,-3.50211987978418,
-3.49251965507249,-3.48894732612245,-3.48650560963042,-3.48428877922437,
-3.48121973697877,-3.47335055387537,-3.41284908074069,-3.40033477739996),
 .UNSPECIFIED.);
#1397=B_SPLINE_CURVE_WITH_KNOTS('',3,(#35890,#35891,#35892,#35893,#35894,
#35895,#35896,#35897,#35898,#35899,#35900,#35901,#35902,#35903,#35904,#35905,
#35906,#35907,#35908,#35909,#35910,#35911,#35912,#35913,#35914,#35915,#35916,
#35917,#35918,#35919,#35920,#35921,#35922,#35923,#35924,#35925,#35926,#35927,
#35928,#35929,#35930,#35931,#35932,#35933,#35934,#35935,#35936,#35937,#35938,
#35939,#35940,#35941,#35942,#35943,#35944,#35945,#35946,#35947,#35948,#35949,
#35950,#35951,#35952,#35953,#35954,#35955,#35956,#35957,#35958,#35959,#35960,
#35961,#35962,#35963,#35964,#35965,#35966,#35967,#35968,#35969,#35970,#35971,
#35972,#35973,#35974,#35975,#35976,#35977,#35978,#35979,#35980,#35981,#35982,
#35983,#35984,#35985,#35986,#35987,#35988,#35989,#35990,#35991,#35992,#35993,
#35994,#35995,#35996,#35997,#35998,#35999,#36000,#36001,#36002,#36003,#36004,
#36005,#36006,#36007,#36008,#36009,#36010,#36011,#36012,#36013,#36014,#36015,
#36016,#36017,#36018,#36019,#36020,#36021,#36022,#36023,#36024,#36025,#36026,
#36027,#36028,#36029,#36030,#36031,#36032,#36033,#36034,#36035,#36036,#36037,
#36038,#36039,#36040,#36041,#36042,#36043,#36044,#36045,#36046,#36047,#36048,
#36049,#36050,#36051,#36052,#36053,#36054,#36055,#36056,#36057,#36058,#36059,
#36060,#36061,#36062,#36063,#36064,#36065,#36066,#36067,#36068,#36069,#36070,
#36071,#36072,#36073,#36074,#36075,#36076,#36077,#36078,#36079,#36080,#36081,
#36082,#36083,#36084,#36085,#36086,#36087,#36088,#36089,#36090,#36091,#36092,
#36093,#36094,#36095,#36096,#36097,#36098,#36099,#36100,#36101,#36102,#36103,
#36104,#36105),.UNSPECIFIED.,.F.,.F.,(4,2,2,2,2,2,2,2,2,2,2,2,2,2,2,2,2,
2,2,2,2,2,2,2,2,2,2,2,2,2,2,2,2,2,2,2,2,2,2,2,2,2,2,2,2,2,2,2,2,2,2,2,2,
2,2,2,2,2,2,2,2,2,2,2,2,2,2,2,2,2,2,2,2,2,2,2,2,2,2,2,2,2,2,2,2,2,2,2,2,
2,2,2,2,2,2,2,2,2,2,2,2,2,2,2,2,2,2,4),(-2.69283977885968,-2.68310143069254,
-2.67486842657118,-2.67008382205593,-2.66588145365924,-2.66064181106887,
-2.65249425890529,-2.6040282498421,-2.5395143715343,-2.51566065414712,-2.51080437591683,
-2.50808091287636,-2.50571563196259,-2.50267207434551,-2.49760289340965,
-2.4493558749743,-2.38969344019534,-2.35975336139693,-2.35202110529889,
-2.3473457218264,-2.34312475982452,-2.33770483192546,-2.32637338422226,
-2.24360973717306,-2.19520167284159,-2.1891354034682,-2.18616010202923,
-2.18403074095888,-2.18131416729415,-2.1766156201239,-2.15758405085398,
-2.13962149982905,-2.08910379444174,-2.05589198032722,-2.04222192887267,
-2.03164773590248,-2.02637447863243,-2.02216869983366,-2.01740547459455,
-2.00927255057752,-1.97365243170672,-1.92715710254637,-1.87608125906569,
-1.86797966132223,-1.86487384958149,-1.86264604821053,-1.8602103502604,
-1.85667688735662,-1.84735662834868,-1.83325135735085,-1.73165577321704,
-1.71287855813683,-1.70607068749421,-1.70204347380289,-1.69779864143056,
-1.69219954182274,-1.67990202192771,-1.66330326673895,-1.61801516288957,
-1.55285138063636,-1.54522308403937,-1.5421929733796,-1.53998483256562,
-1.5375293792845,-1.53389700427618,-1.52388744873649,-1.45817510242357,
-1.39488300134366,-1.38663835196857,-1.38136921780606,-1.37716425918247,
-1.37239932032969,-1.36425687814767,-1.3284723920359,-1.28152717622446,
-1.23110305766583,-1.2230011511352,-1.21989553930169,-1.21766796129195,
-1.2152326006997,-1.21169978210103,-1.2023821144702,-1.18828154869582,-1.08677807519096,
-1.06793823194321,-1.06112208448301,-1.0570936119629,-1.0528500986747,-1.04725719223619,
-1.03499162792078,-1.01844816000191,-0.973409877764712,-0.907879741590399,
-0.900273377247643,-0.897247178914939,-0.895040196902427,-0.892584002742436,
-0.888947046875392,-0.878902737495788,-0.812604056616784,-0.749961830993934,
-0.741717683855692,-0.736449034312483,-0.732244566690971,-0.727480295875256,
-0.719339273909858,-0.683566234576041,-0.662425644205117),.UNSPECIFIED.);
#1398=B_SPLINE_CURVE_WITH_KNOTS('',3,(#36110,#36111,#36112,#36113,#36114,
#36115,#36116,#36117,#36118,#36119,#36120,#36121,#36122,#36123,#36124,#36125,
#36126,#36127,#36128,#36129,#36130,#36131,#36132,#36133,#36134,#36135,#36136,
#36137,#36138,#36139,#36140,#36141,#36142,#36143,#36144,#36145,#36146,#36147,
#36148,#36149,#36150,#36151,#36152,#36153,#36154,#36155,#36156,#36157,#36158,
#36159,#36160,#36161,#36162,#36163,#36164,#36165,#36166,#36167,#36168,#36169,
#36170,#36171,#36172,#36173,#36174,#36175,#36176,#36177,#36178,#36179,#36180,
#36181,#36182,#36183,#36184,#36185,#36186,#36187,#36188,#36189,#36190,#36191,
#36192,#36193,#36194,#36195,#36196,#36197,#36198,#36199,#36200,#36201,#36202,
#36203,#36204,#36205,#36206,#36207,#36208,#36209,#36210,#36211,#36212,#36213,
#36214,#36215,#36216,#36217,#36218,#36219,#36220,#36221,#36222,#36223,#36224,
#36225,#36226,#36227,#36228,#36229,#36230,#36231,#36232,#36233,#36234,#36235,
#36236,#36237,#36238,#36239,#36240,#36241,#36242,#36243,#36244,#36245,#36246,
#36247,#36248,#36249,#36250,#36251,#36252,#36253,#36254,#36255,#36256,#36257,
#36258,#36259,#36260,#36261,#36262,#36263,#36264,#36265,#36266,#36267,#36268,
#36269,#36270,#36271,#36272,#36273,#36274,#36275,#36276,#36277,#36278,#36279,
#36280,#36281,#36282,#36283,#36284,#36285,#36286,#36287,#36288,#36289,#36290,
#36291,#36292,#36293,#36294,#36295,#36296,#36297,#36298,#36299,#36300,#36301,
#36302,#36303,#36304,#36305,#36306,#36307,#36308,#36309,#36310,#36311,#36312,
#36313,#36314,#36315,#36316,#36317,#36318,#36319),.UNSPECIFIED.,.F.,.F.,
(4,2,2,2,2,2,2,2,2,2,2,2,2,2,2,2,2,2,2,2,2,2,2,2,2,2,2,2,2,2,2,2,2,2,2,
2,2,2,2,2,2,2,2,2,2,2,2,2,2,2,2,2,2,2,2,2,2,2,2,2,2,2,2,2,2,2,2,2,2,2,2,
2,2,2,2,2,2,2,2,2,2,2,2,2,2,2,2,2,2,2,2,2,2,2,2,2,2,2,2,2,2,2,2,2,4),(-3.39960000691215,
-3.33661693680887,-3.3142928808857,-3.30560723188051,-3.29915729582697,
-3.2961093980794,-3.29375090991268,-3.29100142371395,-3.28615082295111,
-3.26496947575705,-3.25416660749216,-3.23251988293263,-3.17608430484181,
-3.15685709260627,-3.14309666001341,-3.13724627010666,-3.13296435954881,
-3.12847657010988,-3.12159228779436,-3.10223816022417,-3.00131944827361,
-2.98723960602559,-2.97793439231517,-2.97440515961066,-2.97197195623666,
-2.96974617394638,-2.96664295867037,-2.95854620163059,-2.90788557194195,
-2.86114835624393,-2.8254480425375,-2.81731534880772,-2.81255495389357,
-2.80835334038212,-2.80308756264278,-2.79484657498922,-2.7314242037378,
-2.68239056820158,-2.65822699640528,-2.65335651752462,-2.65063132008687,
-2.64826865929297,-2.64523384456385,-2.64019035151028,-2.60169561165248,
-2.54520155261438,-2.50365827903236,-2.49520284548529,-2.49037227682619,
-2.48617819428788,-2.48101160443384,-2.47309697379004,-2.4310204446325,
-2.36735883503205,-2.34643030917835,-2.33811003920562,-2.33187146730801,
-2.32886388262667,-2.32650810661212,-2.32372833246878,-2.31874591420167,
-2.29551083041115,-2.28868716086997,-2.20576401138959,-2.17929626884315,
-2.17186382105886,-2.167256605541,-2.16302247569691,-2.15757147253651,-2.14574457603877,
-2.06746694291484,-2.03050865497506,-2.01293960044915,-2.00831633811327,
-2.00564515046474,-2.00327137529979,-2.00009250817752,-1.99293723153902,
-1.96140636985788,-1.88905560082353,-1.85817426367366,-1.85005470192525,
-1.84529711113054,-1.84151527335835,-1.83644369989881,-1.82685128082296,
-1.7617196743932,-1.69540592252158,-1.68785209541015,-1.6848358925001,-1.68263233707729,
-1.68017540007131,-1.67652964620229,-1.6664120220225,-1.59884968159553,
-1.53751150784998,-1.52928601230348,-1.52402473995314,-1.51982331107646,
-1.51505946926798,-1.50691176652551,-1.4709780109223,-1.42361220764589,
-1.37378757915261,-1.36941396256219),.UNSPECIFIED.);
#1399=B_SPLINE_CURVE_WITH_KNOTS('',3,(#36321,#36322,#36323,#36324,#36325,
#36326,#36327,#36328,#36329,#36330,#36331,#36332,#36333,#36334,#36335,#36336,
#36337,#36338,#36339,#36340,#36341,#36342,#36343,#36344,#36345,#36346,#36347,
#36348,#36349,#36350,#36351,#36352,#36353,#36354,#36355,#36356,#36357,#36358,
#36359,#36360,#36361,#36362,#36363,#36364,#36365,#36366,#36367,#36368,#36369,
#36370,#36371,#36372,#36373,#36374,#36375,#36376,#36377,#36378,#36379,#36380,
#36381,#36382,#36383,#36384,#36385,#36386,#36387,#36388,#36389,#36390,#36391,
#36392),.UNSPECIFIED.,.F.,.F.,(4,2,2,2,2,2,2,2,2,2,2,2,2,2,2,2,2,2,2,2,
2,2,2,2,2,2,2,2,2,2,2,2,2,2,2,4),(-0.662425644205117,-0.636646086239023,
-0.586200282206748,-0.57809957168942,-0.574994362812132,-0.572767059893278,
-0.570331983817414,-0.566799550956724,-0.557482745293484,-0.543383347437845,
-0.441878150370085,-0.42305186539602,-0.416238118177119,-0.412210432428839,
-0.407967288359352,-0.40237409530578,-0.39041027985277,-0.374215799653739,
-0.330748238142239,-0.271760255898399,-0.257447218428823,-0.253141796922812,
-0.250539963589588,-0.248141685587373,-0.244808513593056,-0.237056905795168,
-0.197264095533609,-0.158093467926337,-0.105173906541785,-0.0969374812351964,
-0.0916714046660101,-0.0874674846711437,-0.0827022211851563,-0.077743904539085,
-0.0702532742700582,-0.000951723655427596),.UNSPECIFIED.);
#1400=B_SPLINE_CURVE_WITH_KNOTS('',3,(#36393,#36394,#36395,#36396,#36397,
#36398,#36399,#36400,#36401,#36402,#36403,#36404,#36405,#36406,#36407,#36408,
#36409,#36410,#36411,#36412,#36413,#36414,#36415,#36416,#36417,#36418,#36419,
#36420,#36421,#36422,#36423,#36424,#36425,#36426,#36427,#36428,#36429,#36430,
#36431,#36432,#36433,#36434,#36435,#36436,#36437,#36438,#36439,#36440,#36441,
#36442,#36443,#36444,#36445,#36446,#36447,#36448,#36449,#36450,#36451,#36452,
#36453,#36454,#36455,#36456,#36457,#36458,#36459,#36460,#36461,#36462,#36463,
#36464,#36465,#36466,#36467,#36468,#36469,#36470,#36471,#36472,#36473,#36474,
#36475,#36476,#36477,#36478,#36479,#36480,#36481,#36482,#36483,#36484,#36485,
#36486,#36487,#36488,#36489,#36490,#36491,#36492,#36493,#36494,#36495,#36496,
#36497,#36498,#36499,#36500,#36501,#36502,#36503,#36504,#36505,#36506,#36507,
#36508,#36509,#36510,#36511,#36512,#36513,#36514,#36515,#36516,#36517,#36518,
#36519,#36520,#36521,#36522,#36523,#36524,#36525,#36526,#36527,#36528,#36529,
#36530,#36531,#36532,#36533,#36534,#36535,#36536,#36537,#36538,#36539,#36540,
#36541,#36542,#36543,#36544,#36545,#36546),.UNSPECIFIED.,.F.,.F.,(4,2,2,
2,2,2,2,2,2,2,2,2,2,2,2,2,2,2,2,2,2,2,2,2,2,2,2,2,2,2,2,2,2,2,2,2,2,2,2,
2,2,2,2,2,2,2,2,2,2,2,2,2,2,2,2,2,2,2,2,2,2,2,2,2,2,2,2,2,2,2,2,2,2,2,2,
2,4),(-4.06102231635032,-3.99984654277032,-3.99488213931563,-3.99179793324655,
-3.98893724184584,-3.98658502286122,-3.98367140336896,-3.97808606014687,
-3.93457442605208,-3.92520848652895,-3.87174543846425,-3.84056175286585,
-3.83301976862949,-3.82825225104584,-3.82404958784693,-3.81878938121044,
-3.81057046516069,-3.74643132923399,-3.68145184229221,-3.67155023920359,
-3.66789780401313,-3.66543884569562,-3.66323530268854,-3.66022135328246,
-3.65268451295887,-3.58709723877599,-3.54210005530019,-3.52556699324923,
-3.51330699947153,-3.50771586185343,-3.50347336616354,-3.49944560441746,
-3.49263008229106,-3.4737883170242,-3.37226339002447,-3.35815990962468,
-3.34884202964806,-3.34530955014946,-3.3428745726869,-3.34064745450078,
-3.33754265381698,-3.32944370831833,-3.27907667702283,-3.23215156020394,
-3.19637915159503,-3.18823862251983,-3.18347458235237,-3.17927027819029,
-3.1740017811646,-3.16575769674041,-3.10235625132791,-3.05358296288273,
-3.02918520800431,-3.02430005090086,-3.02157058657536,-3.01920674510929,
-3.01617344194689,-3.0111385788302,-2.9747265282584,-2.95834211199055,-2.95366994721698,
-2.90039135989145,-2.88217927767047,-2.86897325352961,-2.86321400268094,
-2.85894452956393,-2.85441982913439,-2.84737646240552,-2.82683952173272,
-2.72733600554875,-2.71330887148643,-2.70402772734729,-2.70050019797248,
-2.69806578875981,-2.69583691796467,-2.69272669724805,-2.69249692795472),
 .UNSPECIFIED.);
#1401=B_SPLINE_CURVE_WITH_KNOTS('',3,(#36552,#36553,#36554,#36555,#36556,
#36557,#36558,#36559,#36560,#36561,#36562,#36563,#36564,#36565,#36566,#36567,
#36568,#36569,#36570,#36571,#36572,#36573,#36574,#36575,#36576,#36577,#36578,
#36579,#36580,#36581,#36582,#36583,#36584,#36585,#36586,#36587,#36588,#36589,
#36590,#36591,#36592,#36593,#36594,#36595,#36596,#36597,#36598,#36599,#36600,
#36601,#36602,#36603,#36604,#36605,#36606,#36607,#36608,#36609,#36610,#36611,
#36612,#36613,#36614,#36615,#36616,#36617,#36618,#36619,#36620,#36621,#36622,
#36623,#36624,#36625,#36626,#36627,#36628,#36629,#36630,#36631,#36632,#36633,
#36634,#36635,#36636,#36637,#36638,#36639,#36640,#36641,#36642,#36643,#36644,
#36645,#36646,#36647,#36648,#36649,#36650,#36651,#36652,#36653,#36654,#36655,
#36656,#36657,#36658,#36659,#36660,#36661,#36662,#36663,#36664,#36665,#36666,
#36667,#36668,#36669,#36670,#36671,#36672,#36673,#36674,#36675,#36676,#36677,
#36678,#36679,#36680,#36681,#36682,#36683,#36684,#36685,#36686,#36687,#36688,
#36689,#36690,#36691,#36692,#36693,#36694,#36695,#36696,#36697,#36698,#36699,
#36700,#36701,#36702,#36703,#36704,#36705,#36706,#36707,#36708,#36709,#36710,
#36711,#36712,#36713,#36714,#36715,#36716,#36717,#36718,#36719,#36720,#36721,
#36722,#36723,#36724,#36725),.UNSPECIFIED.,.F.,.F.,(4,2,2,2,2,2,2,2,2,2,
2,2,2,2,2,2,2,2,2,2,2,2,2,2,2,2,2,2,2,2,2,2,2,2,2,2,2,2,2,2,2,2,2,2,2,2,
2,2,2,2,2,2,2,2,2,2,2,2,2,2,2,2,2,2,2,2,2,2,2,2,2,2,2,2,2,2,2,2,2,2,2,2,
2,2,2,2,4),(-1.37005450945405,-1.34532621637229,-1.33713923164383,-1.33232026557117,
-1.32812570734539,-1.32294498136244,-1.31281765532065,-1.29987401033403,
-1.26928992458156,-1.20206482037715,-1.17821101179695,-1.17319296306083,
-1.17040532583634,-1.1680505098258,-1.16505391182974,-1.15887071436178,
-1.15064570957225,-1.13007348947339,-1.08598777703611,-1.02457146896735,
-1.01630014534599,-1.01102529844781,-1.00682303191568,-1.00206892750175,
-0.993964483367067,-0.958713306787006,-0.880707316432008,-0.855908346951102,
-0.851282959328518,-0.848340825524222,-0.845988681119941,-0.843155996676435,
-0.837782093555426,-0.800253821588666,-0.708523382461591,-0.695465084735774,
-0.690164237118537,-0.68623233293887,-0.68193198504365,-0.675979463883206,
-0.6616016853154,-0.595660687726437,-0.538046690996075,-0.530068087303279,
-0.526981782969047,-0.524760459911294,-0.522323132495924,-0.518772896389182,
-0.509324672644679,-0.494952274417858,-0.443322279105811,-0.379613187328578,
-0.37137298922778,-0.366107520218591,-0.361906058200078,-0.361830426505256,
-0.361734239613267,-0.361644584105557,-0.361561007518534,-0.361483088629685,
-0.361410435510148,-0.3613426834948,-0.361279493610346,-0.361220550913095,
-0.361165562721758,-0.356243218535335,-0.347125963575631,-0.33567329088123,
-0.310169957347652,-0.266182492209392,-0.215863696728321,-0.207763295774833,
-0.204659574677154,-0.202433693118009,-0.200000665598389,-0.196472178444829,
-0.187171611170168,-0.17310276781771,-0.0897815607022127,-0.0611334789419045,
-0.0495574015475814,-0.0441528060359751,-0.0399254794858704,-0.0359973851921187,
-0.0314509504551579,-0.024966113326458,-0.000950797002019388),
 .UNSPECIFIED.);
#1402=B_SPLINE_CURVE_WITH_KNOTS('',3,(#36726,#36727,#36728,#36729,#36730,
#36731,#36732,#36733,#36734,#36735,#36736,#36737,#36738,#36739,#36740,#36741,
#36742,#36743,#36744,#36745,#36746,#36747,#36748,#36749,#36750,#36751,#36752,
#36753,#36754,#36755,#36756,#36757,#36758,#36759,#36760,#36761,#36762,#36763,
#36764,#36765,#36766,#36767,#36768,#36769,#36770,#36771,#36772,#36773,#36774,
#36775,#36776,#36777,#36778,#36779,#36780,#36781,#36782,#36783,#36784,#36785,
#36786,#36787,#36788,#36789,#36790,#36791,#36792,#36793,#36794,#36795,#36796,
#36797,#36798,#36799,#36800,#36801),.UNSPECIFIED.,.F.,.F.,(4,2,2,2,2,2,
2,2,2,2,2,2,2,2,2,2,2,2,2,2,2,2,2,2,2,2,2,2,2,2,2,2,2,2,2,2,2,4),(-4.06037931501153,
-4.03713134392637,-3.95731390874865,-3.94945838041092,-3.94349344013245,
-3.9405402969288,-3.93841537819424,-3.93568880182403,-3.93093836106775,
-3.91118179479392,-3.82613353629426,-3.80372395300647,-3.79324505698843,
-3.78478041867085,-3.78003159381997,-3.77625268497845,-3.7713815870264,
-3.76296258787298,-3.72614114840973,-3.65737449341879,-3.62584161603421,
-3.620647892452,-3.61785373164648,-3.61550001578828,-3.61251323535657,-3.60773872180304,
-3.57984380918808,-3.55519470999195,-3.51532795491119,-3.48592089729895,
-3.47331143608953,-3.46339031266757,-3.45825191932105,-3.45406054465984,
-3.44921054563837,-3.44088548311329,-3.40558404251273,-3.39960000691215),
 .UNSPECIFIED.);
#1403=B_SPLINE_CURVE_WITH_KNOTS('',3,(#36802,#36803,#36804,#36805,#36806,
#36807,#36808,#36809,#36810,#36811,#36812,#36813,#36814,#36815,#36816,#36817,
#36818,#36819,#36820,#36821,#36822,#36823,#36824,#36825,#36826,#36827,#36828,
#36829,#36830,#36831,#36832,#36833,#36834,#36835,#36836,#36837,#36838,#36839,
#36840,#36841,#36842,#36843,#36844,#36845,#36846,#36847,#36848,#36849,#36850,
#36851,#36852,#36853,#36854,#36855,#36856,#36857,#36858,#36859,#36860,#36861,
#36862,#36863,#36864,#36865,#36866,#36867,#36868,#36869,#36870,#36871,#36872,
#36873,#36874,#36875,#36876,#36877,#36878,#36879,#36880,#36881,#36882,#36883,
#36884,#36885,#36886,#36887,#36888,#36889,#36890,#36891,#36892,#36893,#36894,
#36895,#36896,#36897,#36898,#36899,#36900,#36901,#36902,#36903,#36904,#36905,
#36906,#36907,#36908,#36909,#36910,#36911,#36912,#36913,#36914,#36915,#36916,
#36917,#36918,#36919,#36920,#36921,#36922,#36923,#36924,#36925,#36926,#36927,
#36928,#36929,#36930,#36931,#36932,#36933,#36934,#36935,#36936,#36937,#36938,
#36939,#36940,#36941,#36942,#36943,#36944,#36945,#36946,#36947,#36948,#36949,
#36950,#36951,#36952,#36953,#36954,#36955,#36956,#36957,#36958,#36959,#36960,
#36961,#36962,#36963,#36964,#36965,#36966,#36967,#36968,#36969,#36970,#36971,
#36972,#36973,#36974,#36975,#36976,#36977,#36978,#36979,#36980,#36981,#36982,
#36983,#36984,#36985,#36986,#36987,#36988,#36989,#36990,#36991,#36992,#36993,
#36994,#36995,#36996,#36997,#36998,#36999,#37000,#37001,#37002,#37003,#37004,
#37005,#37006,#37007,#37008,#37009),.UNSPECIFIED.,.F.,.F.,(4,2,2,2,2,2,
2,2,2,2,2,2,2,2,2,2,2,2,2,2,2,2,2,2,2,2,2,2,2,2,2,2,2,2,2,2,2,2,2,2,2,2,
2,2,2,2,2,2,2,2,2,2,2,2,2,2,2,2,2,2,2,2,2,2,2,2,2,2,2,2,2,2,2,2,2,2,2,2,
2,2,2,2,2,2,2,2,2,2,2,2,2,2,2,2,2,2,2,2,2,2,2,2,2,4),(-2.69249692795472,
-2.68459093233267,-2.63515909771338,-2.58837220213187,-2.55164942171319,
-2.54344969242352,-2.53867206666938,-2.53446842243638,-2.52921744488154,
-2.52103332506659,-2.47126740043804,-2.40790937824799,-2.38423941725221,
-2.37939300265136,-2.37667154262279,-2.37430568066648,-2.37125843245205,
-2.36617702466281,-2.31773708286663,-2.25823142450575,-2.22833085242378,
-2.22060126670146,-2.2159262141567,-2.21170473055825,-2.20628298792448,
-2.19494346244823,-2.11223027743305,-2.07799843616651,-2.06658677552773,
-2.05863353468367,-2.05531486767034,-2.0529182867092,-2.05030892016354,
-2.04597247311814,-2.03138587281004,-2.00391643861213,-1.972801849453,-1.91378450770349,
-1.90249031972551,-1.89635132693382,-1.89205608642049,-1.88765032697998,
-1.8811732125416,-1.86328866805201,-1.83588055387273,-1.77991740534245,
-1.74064312546832,-1.73558407782977,-1.7325432628246,-1.73017800414899,
-1.72745206350877,-1.72258550096841,-1.69855052211789,-1.63286880872178,
-1.58573116456729,-1.57762608914586,-1.57239888643464,-1.56819691607482,
-1.563402364319,-1.55512582175939,-1.51709213364138,-1.47273310345262,-1.42219760341824,
-1.41409521649996,-1.41098925293292,-1.40876138053682,-1.40632564906188,
-1.40279221090839,-1.39347243974879,-1.37936827826183,-1.27780829597349,
-1.25899990412908,-1.25218756727365,-1.24815943679293,-1.2439148938867,
-1.23831829085251,-1.22603497861429,-1.20946118366649,-1.16428836586456,
-1.09894566963456,-1.0913268228559,-1.08829826757187,-1.08609048620274,
-1.0836345049018,-1.07999975676878,-1.06997356739294,-1.00398933779334,
-0.940986605027574,-0.932742360363799,-0.927473285996992,-0.923268248386676,
-0.918503084326639,-0.910359918571633,-0.874565922479762,-0.827595996138246,
-0.777204540087443,-0.769102126788519,-0.765996400703885,-0.76376876082003,
-0.761333355968919,-0.757800512051332,-0.748483001564767,-0.73438287028182,
-0.661987786041638),.UNSPECIFIED.);
#1404=B_SPLINE_CURVE_WITH_KNOTS('',3,(#37014,#37015,#37016,#37017,#37018,
#37019,#37020,#37021,#37022,#37023,#37024,#37025,#37026,#37027,#37028,#37029,
#37030,#37031,#37032,#37033,#37034,#37035,#37036,#37037,#37038,#37039,#37040,
#37041,#37042,#37043,#37044,#37045,#37046,#37047,#37048,#37049,#37050,#37051,
#37052,#37053,#37054,#37055,#37056,#37057,#37058,#37059,#37060,#37061,#37062,
#37063,#37064,#37065,#37066,#37067,#37068,#37069,#37070,#37071,#37072,#37073,
#37074,#37075,#37076,#37077,#37078,#37079,#37080,#37081,#37082,#37083,#37084,
#37085,#37086,#37087,#37088,#37089,#37090,#37091,#37092,#37093,#37094,#37095,
#37096,#37097,#37098,#37099,#37100,#37101,#37102,#37103,#37104,#37105,#37106,
#37107,#37108,#37109,#37110,#37111,#37112,#37113,#37114,#37115,#37116,#37117,
#37118,#37119,#37120,#37121,#37122,#37123,#37124,#37125,#37126,#37127,#37128,
#37129,#37130,#37131,#37132,#37133,#37134,#37135,#37136,#37137,#37138,#37139,
#37140,#37141,#37142,#37143,#37144,#37145,#37146,#37147,#37148,#37149,#37150,
#37151,#37152,#37153,#37154,#37155,#37156,#37157,#37158,#37159,#37160,#37161,
#37162,#37163,#37164,#37165,#37166,#37167,#37168,#37169,#37170,#37171,#37172,
#37173,#37174,#37175,#37176,#37177,#37178,#37179,#37180,#37181,#37182,#37183,
#37184,#37185,#37186,#37187,#37188,#37189,#37190,#37191,#37192,#37193,#37194,
#37195,#37196,#37197,#37198,#37199,#37200,#37201,#37202,#37203,#37204,#37205,
#37206,#37207,#37208,#37209,#37210,#37211,#37212,#37213,#37214,#37215,#37216,
#37217,#37218,#37219,#37220,#37221),.UNSPECIFIED.,.F.,.F.,(4,2,2,2,2,2,
2,2,2,2,2,2,2,2,2,2,2,2,2,2,2,2,2,2,2,2,2,2,2,2,2,2,2,2,2,2,2,2,2,2,2,2,
2,2,2,2,2,2,2,2,2,2,2,2,2,2,2,2,2,2,2,2,2,2,2,2,2,2,2,2,2,2,2,2,2,2,2,2,
2,2,2,2,2,2,2,2,2,2,2,2,2,2,2,2,2,2,2,2,2,2,2,2,2,4),(-3.39962297301684,
-3.36254556477445,-3.32072301844083,-3.29347869106837,-3.27567482207821,
-3.26921424206043,-3.26481617221012,-3.26052572943178,-3.25438894653677,
-3.24308683145512,-3.17988975229796,-3.11904416732163,-3.10934880158451,
-3.10576352134441,-3.10331977385038,-3.10110645706124,-3.09804918492491,
-3.09024676665842,-3.02863069917918,-2.98106685553121,-2.95530619399558,
-2.94794130934146,-2.94334993988734,-2.9391128758676,-2.93363353432495,
-2.92164445962634,-2.84520787721698,-2.80708853396324,-2.79492639969945,
-2.78658405862663,-2.78320425941076,-2.78079964063717,-2.77853860760316,
-2.77463951255915,-2.76356827913853,-2.69781168589542,-2.65629825922005,
-2.63260298758734,-2.62544214508508,-2.62089517099366,-2.61664187847665,
-2.61105926946479,-2.59849230856507,-2.53879210225177,-2.48827303273349,
-2.47406131856074,-2.46469268210081,-2.4611548230828,-2.45872051950451,
-2.45649758938201,-2.45340338861596,-2.44536640765803,-2.39011735306177,
-2.33813149686875,-2.32016913092668,-2.30710450494831,-2.30137332323,-2.29711195103899,
-2.29258406501828,-2.28551135490787,-2.26475221618176,-2.16555217997405,
-2.15154194960709,-2.14227117344821,-2.13874741981798,-2.13631559133994,
-2.13408914718258,-2.13098249433349,-2.12285760583724,-2.0733265984331,
-2.03143661235886,-1.99089206067141,-1.98227443814986,-1.97735798574691,
-1.97358860900375,-1.96870232246343,-1.9599853945579,-1.91229942031345,
-1.83963590909024,-1.82215253682837,-1.81753690586894,-1.81486762544469,
-1.81249379048798,-1.80931246762411,-1.80214201042114,-1.77047150897854,
-1.6974605967261,-1.66729892104302,-1.65924545584733,-1.65450269862606,
-1.65071954550933,-1.64562927190657,-1.63594431095098,-1.57391579865678,
-1.50419093890524,-1.49689546053836,-1.49396117962422,-1.49156066965804,
-1.48902238128798,-1.48499923819309,-1.47180573113252,-1.4488109685451,
-1.37859646924867,-1.37005450945405),.UNSPECIFIED.);
#1405=B_SPLINE_CURVE_WITH_KNOTS('',3,(#37223,#37224,#37225,#37226,#37227,
#37228,#37229,#37230,#37231,#37232,#37233,#37234,#37235,#37236,#37237,#37238,
#37239,#37240,#37241,#37242,#37243,#37244,#37245,#37246,#37247,#37248,#37249,
#37250,#37251,#37252,#37253,#37254,#37255,#37256,#37257,#37258,#37259,#37260,
#37261,#37262,#37263,#37264,#37265,#37266,#37267,#37268,#37269,#37270,#37271,
#37272,#37273,#37274,#37275,#37276,#37277,#37278,#37279,#37280,#37281,#37282,
#37283,#37284,#37285,#37286,#37287,#37288,#37289,#37290,#37291,#37292,#37293,
#37294),.UNSPECIFIED.,.F.,.F.,(4,2,2,2,2,2,2,2,2,2,2,2,2,2,2,2,2,2,2,2,
2,2,2,2,2,2,2,2,2,2,2,2,2,2,2,4),(-0.661987786041638,-0.632897110421259,
-0.614040566443078,-0.607221985882824,-0.603192984919947,-0.598949576198417,
-0.593357919662498,-0.581099672443385,-0.564569101935066,-0.519590495412795,
-0.453965140633778,-0.446340790788293,-0.443324194282382,-0.441119588982708,
-0.438660474599158,-0.435009603795102,-0.424865358513279,-0.356883746135923,
-0.296098466928258,-0.287829692657471,-0.282553534244782,-0.278348307112415,
-0.273780766042135,-0.266116711546224,-0.256841741124321,-0.23804840711835,
-0.191699409280118,-0.131992292795311,-0.124097183296083,-0.121022524607124,
-0.118803138273764,-0.116360268149262,-0.112788916626733,-0.103206866529573,
-0.0885601570869462,-0.000952451209969257),.UNSPECIFIED.);
#1406=B_SPLINE_CURVE_WITH_KNOTS('',3,(#37295,#37296,#37297,#37298,#37299,
#37300,#37301,#37302,#37303,#37304,#37305,#37306,#37307,#37308,#37309,#37310,
#37311,#37312,#37313,#37314,#37315,#37316,#37317,#37318,#37319,#37320,#37321,
#37322,#37323,#37324,#37325,#37326,#37327,#37328,#37329,#37330,#37331,#37332,
#37333,#37334,#37335,#37336,#37337,#37338,#37339,#37340,#37341,#37342,#37343,
#37344,#37345,#37346,#37347,#37348,#37349,#37350,#37351,#37352,#37353,#37354,
#37355,#37356,#37357,#37358,#37359,#37360,#37361,#37362,#37363,#37364,#37365,
#37366,#37367,#37368,#37369,#37370,#37371,#37372,#37373,#37374,#37375,#37376,
#37377,#37378,#37379,#37380,#37381,#37382,#37383,#37384,#37385,#37386,#37387,
#37388,#37389,#37390,#37391,#37392,#37393,#37394,#37395,#37396,#37397,#37398,
#37399,#37400,#37401,#37402,#37403,#37404,#37405,#37406,#37407,#37408,#37409,
#37410,#37411,#37412,#37413,#37414,#37415,#37416,#37417,#37418,#37419,#37420,
#37421,#37422,#37423,#37424,#37425,#37426,#37427,#37428,#37429,#37430,#37431,
#37432,#37433,#37434,#37435,#37436,#37437,#37438,#37439,#37440,#37441,#37442,
#37443,#37444,#37445,#37446,#37447,#37448,#37449,#37450,#37451,#37452,#37453,
#37454,#37455,#37456,#37457,#37458,#37459,#37460,#37461,#37462,#37463,#37464,
#37465,#37466,#37467,#37468,#37469,#37470,#37471,#37472,#37473,#37474,#37475,
#37476,#37477,#37478,#37479,#37480),.UNSPECIFIED.,.F.,.F.,(4,2,2,2,2,2,
2,2,2,2,2,2,2,2,2,2,2,2,2,2,2,2,2,2,2,2,2,2,2,2,2,2,2,2,2,2,2,2,2,2,2,2,
2,2,2,2,2,2,2,2,2,2,2,2,2,2,2,2,2,2,2,2,2,2,2,2,2,2,2,2,2,2,2,2,2,2,2,2,
2,2,2,2,2,2,2,2,2,2,2,2,2,2,4),(-4.06207904828509,-4.04335695901034,-4.03155435033365,
-4.02608365069201,-4.0219218175068,-4.01791141510869,-4.01394354042528,
-4.00850443728747,-3.99463044250151,-3.96608070517844,-3.89310104584232,
-3.86601034442442,-3.86099291220808,-3.85823514776986,-3.85587573543404,
-3.85283451797909,-3.84788198942486,-3.81491326836232,-3.75421374358963,
-3.72578939275626,-3.71346186154221,-3.70379230963457,-3.69873314731702,
-3.69869522502636,-3.6986546351422,-3.6986111838906,-3.69856466246732,-3.69851484612974,
-3.69846149306318,-3.69840434232486,-3.69834311325685,-3.69827750334002,
-3.69820718652685,-3.69813181158868,-3.6980510004978,-3.69796434609788,
-3.69787140995314,-3.69781505718549,-3.69773644016462,-3.69353198144047,
-3.68825632802986,-3.67998736883403,-3.61926074070865,-3.55119032798046,
-3.54104165664174,-3.53739052654311,-3.5349316449013,-3.53272755204159,
-3.52971206670863,-3.52209023410478,-3.45649531650488,-3.41155530731917,
-3.39503398588419,-3.38278039276131,-3.37719003027038,-3.37294725561798,
-3.36891858385026,-3.36209993976592,-3.34323928535951,-3.24172331990386,
-3.22761900245592,-3.21830043576989,-3.2147676086336,-3.21233236397536,
-3.21010497941178,-3.20699977860134,-3.19889957488055,-3.14856130035586,
-3.10160667699447,-3.06582130039698,-3.05767929049224,-3.05291458603546,
-3.04870981787668,-3.04344090148969,-3.03519647853824,-2.97208043733708,
-2.90614951617144,-2.89612661681516,-2.89249240376657,-2.890036610716,-2.88782885383535,
-2.88480017315056,-2.87718009769879,-2.81192046776632,-2.76674133957567,
-2.75016616702003,-2.73788108055799,-2.73228419398127,-2.72803963516158,
-2.72401162364716,-2.71719986457004,-2.69839559582656,-2.69307182648613),
 .UNSPECIFIED.);
#1407=B_SPLINE_CURVE_WITH_KNOTS('',3,(#37486,#37487,#37488,#37489,#37490,
#37491,#37492,#37493,#37494,#37495,#37496,#37497,#37498,#37499,#37500,#37501,
#37502,#37503,#37504,#37505,#37506,#37507,#37508,#37509,#37510,#37511,#37512,
#37513,#37514,#37515,#37516,#37517,#37518,#37519,#37520,#37521,#37522,#37523,
#37524,#37525,#37526,#37527,#37528,#37529,#37530,#37531,#37532,#37533,#37534,
#37535,#37536,#37537,#37538,#37539,#37540,#37541,#37542,#37543,#37544,#37545,
#37546,#37547,#37548,#37549,#37550,#37551,#37552,#37553,#37554,#37555,#37556,
#37557,#37558,#37559,#37560,#37561,#37562,#37563,#37564,#37565,#37566,#37567,
#37568,#37569,#37570,#37571,#37572,#37573,#37574,#37575,#37576,#37577,#37578,
#37579,#37580,#37581,#37582,#37583,#37584,#37585,#37586,#37587,#37588,#37589,
#37590,#37591,#37592,#37593,#37594,#37595,#37596,#37597,#37598,#37599,#37600,
#37601,#37602,#37603,#37604,#37605,#37606,#37607,#37608,#37609,#37610,#37611,
#37612,#37613,#37614,#37615,#37616,#37617,#37618,#37619,#37620,#37621,#37622,
#37623,#37624,#37625,#37626,#37627,#37628,#37629,#37630,#37631,#37632,#37633,
#37634,#37635,#37636,#37637,#37638,#37639,#37640,#37641,#37642,#37643,#37644,
#37645),.UNSPECIFIED.,.F.,.F.,(4,2,2,2,2,2,2,2,2,2,2,2,2,2,2,2,2,2,2,2,
2,2,2,2,2,2,2,2,2,2,2,2,2,2,2,2,2,2,2,2,2,2,2,2,2,2,2,2,2,2,2,2,2,2,2,2,
2,2,2,2,2,2,2,2,2,2,2,2,2,2,2,2,2,2,2,2,2,2,2,4),(-1.36964948262408,-1.36420575719923,
-1.31373938642615,-1.30563991170215,-1.30253617806612,-1.3003101957542,
-1.29787695125363,-1.29434797180143,-1.28504508540802,-1.27097183769727,
-1.17013647399185,-1.15074707674252,-1.14385753627168,-1.13936834407756,
-1.13508656652235,-1.12923869397388,-1.11549534952302,-1.09629792665995,
-1.04003613625122,-1.02265040999473,-1.00463911117486,-0.985775164097792,
-0.981099564622399,-0.97838992926173,-0.976262099322461,-0.973284046195613,
-0.967194734440265,-0.917806706620069,-0.83639379839076,-0.826054390504639,
-0.820765916607833,-0.816837263675266,-0.812534679784094,-0.806568342231466,
-0.79210328442518,-0.751715343780525,-0.692487899331927,-0.664393789784042,
-0.659610476428317,-0.656620885469368,-0.654266748829769,-0.651474190879136,
-0.646288952339892,-0.615000597564471,-0.55000447140555,-0.509556781388679,
-0.500943832934489,-0.496028426132366,-0.491880314755915,-0.486837199474777,
-0.47737899579729,-0.465508878397657,-0.438625116846288,-0.396105043731741,
-0.346586726813181,-0.338492542657269,-0.335387574328687,-0.333161556135635,
-0.330778111812376,-0.32736466708586,-0.323429038475711,-0.316314861802805,
-0.299669014160669,-0.263766348410505,-0.193081405809607,-0.180731695711628,
-0.175186914976504,-0.170939079395929,-0.166375158177965,-0.159138933429679,
-0.134712397102432,-0.0911359770498033,-0.0296845051681231,-0.0174708888496529,
-0.0134213869570827,-0.0108774332789702,-0.00864748008808993,-0.0062496972863311,
-0.00349027148950385,-0.000951110743857238),.UNSPECIFIED.);
#1408=B_SPLINE_CURVE_WITH_KNOTS('',3,(#37646,#37647,#37648,#37649,#37650,
#37651,#37652,#37653,#37654,#37655,#37656,#37657,#37658,#37659,#37660,#37661,
#37662,#37663,#37664,#37665,#37666,#37667,#37668,#37669,#37670,#37671,#37672,
#37673,#37674,#37675,#37676,#37677,#37678,#37679,#37680,#37681,#37682,#37683,
#37684,#37685,#37686,#37687,#37688,#37689,#37690,#37691,#37692,#37693,#37694,
#37695,#37696,#37697,#37698,#37699,#37700,#37701,#37702,#37703,#37704,#37705,
#37706,#37707,#37708,#37709,#37710,#37711,#37712,#37713,#37714,#37715,#37716,
#37717,#37718,#37719),.UNSPECIFIED.,.F.,.F.,(4,2,2,2,2,2,2,2,2,2,2,2,2,
2,2,2,2,2,2,2,2,2,2,2,2,2,2,2,2,2,2,2,2,2,2,2,4),(-4.0605476020252,-4.04893185698267,
-4.00169615318516,-3.94952623524974,-3.9315311539863,-3.91844928136004,
-3.91271617726025,-3.90845552214372,-3.90447533819932,-3.89789429569454,
-3.88064323577898,-3.80375160388145,-3.75755716514169,-3.75361179825645,
-3.75018921449901,-3.74781264486562,-3.74559021929055,-3.74249657970057,
-3.73446780727046,-3.67905536969102,-3.62721013703199,-3.60927676923934,
-3.59622905890309,-3.59050169194357,-3.58624178192483,-3.58171417015119,
-3.57463922166177,-3.5538326711896,-3.45471519262012,-3.44071084546643,
-3.43144356007159,-3.42792086920845,-3.42548969043545,-3.42326377419266,
-3.42015777027404,-3.41203389864517,-3.39962297301684),.UNSPECIFIED.);
#1409=B_SPLINE_CURVE_WITH_KNOTS('',3,(#37720,#37721,#37722,#37723,#37724,
#37725,#37726,#37727,#37728,#37729,#37730,#37731,#37732,#37733,#37734,#37735,
#37736,#37737,#37738,#37739,#37740,#37741,#37742,#37743,#37744,#37745,#37746,
#37747,#37748,#37749,#37750,#37751,#37752,#37753,#37754,#37755,#37756,#37757,
#37758,#37759,#37760,#37761,#37762,#37763,#37764,#37765,#37766,#37767,#37768,
#37769,#37770,#37771,#37772,#37773,#37774,#37775,#37776,#37777,#37778,#37779,
#37780,#37781,#37782,#37783,#37784,#37785,#37786,#37787,#37788,#37789,#37790,
#37791,#37792,#37793,#37794,#37795,#37796,#37797,#37798,#37799,#37800,#37801,
#37802,#37803,#37804,#37805,#37806,#37807,#37808,#37809,#37810,#37811,#37812,
#37813,#37814,#37815,#37816,#37817,#37818,#37819,#37820,#37821,#37822,#37823,
#37824,#37825,#37826,#37827,#37828,#37829,#37830,#37831,#37832,#37833,#37834,
#37835,#37836,#37837,#37838,#37839,#37840,#37841,#37842,#37843,#37844,#37845,
#37846,#37847,#37848,#37849,#37850,#37851,#37852,#37853,#37854,#37855,#37856,
#37857,#37858,#37859,#37860,#37861,#37862,#37863,#37864,#37865,#37866,#37867,
#37868,#37869,#37870,#37871,#37872,#37873,#37874,#37875,#37876,#37877,#37878,
#37879,#37880,#37881,#37882,#37883,#37884,#37885,#37886,#37887,#37888,#37889,
#37890,#37891,#37892,#37893,#37894,#37895,#37896,#37897,#37898,#37899,#37900,
#37901,#37902,#37903,#37904,#37905,#37906,#37907,#37908,#37909,#37910,#37911,
#37912,#37913,#37914,#37915,#37916,#37917,#37918,#37919,#37920,#37921,#37922,
#37923),.UNSPECIFIED.,.F.,.F.,(4,2,2,2,2,2,2,2,2,2,2,2,2,2,2,2,2,2,2,2,
2,2,2,2,2,2,2,2,2,2,2,2,2,2,2,2,2,2,2,2,2,2,2,2,2,2,2,2,2,2,2,2,2,2,2,2,
2,2,2,2,2,2,2,2,2,2,2,2,2,2,2,2,2,2,2,2,2,2,2,2,2,2,2,2,2,2,2,2,2,2,2,2,
2,2,2,2,2,2,2,2,2,4),(-2.69307182648613,-2.59678002806464,-2.58266946313718,
-2.57334725562269,-2.569813366031,-2.56737748934965,-2.56514960677407,-2.56204381643266,
-2.55394285519653,-2.50340127643883,-2.45901947268785,-2.42106724034895,
-2.41279522962788,-2.4080015048615,-2.40379918536693,-2.39857014609783,
-2.39045944742972,-2.34317483864599,-2.27756504992639,-2.26146548893328,
-2.25119836077135,-2.24752990330896,-2.24506662511959,-2.24286418087539,
-2.23985801201697,-2.2323725839028,-2.16521383732554,-2.10113978677428,
-2.09137795350005,-2.08626839051568,-2.08207360121999,-2.07718914135381,
-2.06872832706745,-2.03135729068771,-1.98690299309149,-1.93631034627506,
-1.92820778362807,-1.92510170193445,-1.92287373204588,-1.92043787912758,
-1.91690424010372,-1.90758379683909,-1.8934784932247,-1.79190099462884,
-1.77310207273381,-1.7662908676212,-1.76226282620248,-1.75801795483589,
-1.75242020759388,-1.74013145100486,-1.72354836545171,-1.67833437320218,
-1.6130483248699,-1.60542581298646,-1.60239655728856,-1.60018853168595,
-1.59773259794555,-1.59409846804345,-1.58407745912395,-1.51818340250931,
-1.45507731043981,-1.44683253627665,-1.44156317159162,-1.43735793293797,
-1.43259257388242,-1.42444915684274,-1.38865558763836,-1.34168918208293,
-1.29128717680384,-1.28318446727812,-1.28007860696762,-1.27785086561257,
-1.27541534378155,-1.27188232012847,-1.26256427773527,-1.24846329069005,
-1.14696760288368,-1.12811438028997,-1.12129606883338,-1.11726699197672,
-1.1130233325632,-1.10743105848492,-1.09517027589864,-1.07863550441089,
-1.0336391276528,-0.968034913835258,-0.960432226511016,-0.957406528672747,
-0.955199571846554,-0.952742997986923,-0.949104779338261,-0.939052522610395,
-0.872628682698347,-0.810114881309919,-0.801868716541581,-0.796599263253016,
-0.792394463622042,-0.787630147865629,-0.77948987582087,-0.743735562380239,
-0.696869721637699,-0.662302199137575),.UNSPECIFIED.);
#1410=B_SPLINE_CURVE_WITH_KNOTS('',3,(#37928,#37929,#37930,#37931,#37932,
#37933,#37934,#37935,#37936,#37937,#37938,#37939,#37940,#37941,#37942,#37943,
#37944,#37945,#37946,#37947,#37948,#37949,#37950,#37951,#37952,#37953,#37954,
#37955,#37956,#37957,#37958,#37959,#37960,#37961,#37962,#37963,#37964,#37965,
#37966,#37967,#37968,#37969,#37970,#37971,#37972,#37973,#37974,#37975,#37976,
#37977,#37978,#37979,#37980,#37981,#37982,#37983,#37984,#37985,#37986,#37987,
#37988,#37989,#37990,#37991,#37992,#37993,#37994,#37995,#37996,#37997,#37998,
#37999,#38000,#38001,#38002,#38003,#38004,#38005,#38006,#38007,#38008,#38009,
#38010,#38011,#38012,#38013,#38014,#38015,#38016,#38017,#38018,#38019,#38020,
#38021,#38022,#38023,#38024,#38025,#38026,#38027,#38028,#38029,#38030,#38031,
#38032,#38033,#38034,#38035,#38036,#38037,#38038,#38039,#38040,#38041,#38042,
#38043,#38044,#38045,#38046,#38047,#38048,#38049,#38050,#38051,#38052,#38053,
#38054,#38055,#38056,#38057,#38058,#38059,#38060,#38061,#38062,#38063,#38064,
#38065,#38066,#38067,#38068,#38069,#38070,#38071,#38072,#38073,#38074,#38075,
#38076,#38077,#38078,#38079,#38080,#38081,#38082,#38083,#38084,#38085,#38086,
#38087,#38088,#38089,#38090,#38091,#38092,#38093,#38094,#38095,#38096,#38097,
#38098,#38099,#38100,#38101,#38102,#38103,#38104,#38105,#38106,#38107,#38108,
#38109,#38110,#38111,#38112,#38113,#38114,#38115,#38116,#38117,#38118,#38119,
#38120,#38121,#38122,#38123,#38124,#38125,#38126,#38127,#38128,#38129,#38130,
#38131,#38132,#38133,#38134,#38135,#38136,#38137,#38138,#38139),
 .UNSPECIFIED.,.F.,.F.,(4,2,2,2,2,2,2,2,2,2,2,2,2,2,2,2,2,2,2,2,2,2,2,2,
2,2,2,2,2,2,2,2,2,2,2,2,2,2,2,2,2,2,2,2,2,2,2,2,2,2,2,2,2,2,2,2,2,2,2,2,
2,2,2,2,2,2,2,2,2,2,2,2,2,2,2,2,2,2,2,2,2,2,2,2,2,2,2,2,2,2,2,2,2,2,2,2,
2,2,2,2,2,2,2,2,2,4),(-3.40003668949591,-3.3995458848467,-3.39528527315639,
-3.39075245278261,-3.38366004357326,-3.36273876788145,-3.26370009059015,
-3.24969421010163,-3.24042502501189,-3.23690103093427,-3.23446876842328,
-3.23224171261896,-3.22913392549394,-3.22100388915922,-3.17152048036574,
-3.12972758070188,-3.10242382901365,-3.08458973630762,-3.07812312006481,
-3.07372235011673,-3.06943035477724,-3.0632932414306,-3.05199544150283,
-2.99276379930217,-2.92819107591619,-2.91825389770932,-2.91463324653464,
-2.91218146623128,-2.90997339186421,-2.90693936812978,-2.89928021172689,
-2.8348787642099,-2.76792362484592,-2.75840448877016,-2.75334798478054,
-2.74919849754337,-2.74429279737192,-2.73572589250554,-2.69624422550159,
-2.63035838598052,-2.59882071801677,-2.59362532397676,-2.59083018590394,
-2.58847559960342,-2.5854876544926,-2.58071116661063,-2.55280070022704,
-2.52814702580471,-2.48826285625832,-2.45884746177747,-2.44623407221293,
-2.43630973931055,-2.4311695447881,-2.42697663228464,-2.42212477688976,
-2.41379633749472,-2.37847701853485,-2.30948681861726,-2.28715667571151,
-2.27422473114767,-2.27022972316123,-2.26769724939391,-2.26529218741406,
-2.26178534916213,-2.25326809873307,-2.15561271362714,-2.12050098085331,
-2.11240493649938,-2.10765232656296,-2.10344929146873,-2.0981706978445,
-2.08988794708771,-2.0305762787369,-1.96909202288149,-1.95270723530454,
-1.94817796170537,-1.94552735579411,-1.94314776525696,-1.93992813661065,
-1.93254383024007,-1.89893616989502,-1.80963848703443,-1.79427863373091,
-1.78799735292232,-1.78407026315965,-1.7797647421768,-1.77378570056311,
-1.75924615368478,-1.7147295415267,-1.66007153772704,-1.63164134458179,
-1.62684372795832,-1.62384954908988,-1.62149471665725,-1.61870477685022,
-1.61353332752726,-1.58264545923712,-1.53886030864452,-1.47750226953663,
-1.46926611785044,-1.46400169680184,-1.459800091111,-1.45503855337675,-1.44690104724737,
-1.41112960658645,-1.36964948262408),.UNSPECIFIED.);
#1411=B_SPLINE_CURVE_WITH_KNOTS('',3,(#38141,#38142,#38143,#38144,#38145,
#38146,#38147,#38148,#38149,#38150,#38151,#38152,#38153,#38154,#38155,#38156,
#38157,#38158,#38159,#38160,#38161,#38162,#38163,#38164,#38165,#38166,#38167,
#38168,#38169,#38170,#38171,#38172,#38173,#38174,#38175,#38176,#38177,#38178,
#38179,#38180,#38181,#38182,#38183,#38184,#38185,#38186,#38187,#38188,#38189,
#38190,#38191,#38192,#38193,#38194,#38195,#38196,#38197,#38198,#38199,#38200,
#38201,#38202,#38203,#38204,#38205,#38206,#38207,#38208,#38209,#38210,#38211,
#38212,#38213,#38214),.UNSPECIFIED.,.F.,.F.,(4,2,2,2,2,2,2,2,2,2,2,2,2,
2,2,2,2,2,2,2,2,2,2,2,2,2,2,2,2,2,2,2,2,2,2,2,4),(-0.662302199137575,-0.646338159767163,
-0.638237608602623,-0.635132282033017,-0.63290484978247,-0.630469579986745,
-0.626936779097043,-0.617618501748615,-0.603516436636057,-0.501959334207145,
-0.483168188665671,-0.476359077337931,-0.47233209144975,-0.468088199426295,
-0.462491519640081,-0.450204182259338,-0.433622399054046,-0.388406958720866,
-0.323067079767071,-0.315505862035146,-0.312487403021977,-0.310282438431202,
-0.307882418521396,-0.304354543721482,-0.300257642284619,-0.292722491547411,
-0.274652453728868,-0.183800054015231,-0.161638257143985,-0.154396326524713,
-0.149828921725321,-0.145577880217575,-0.139932183040148,-0.127371101476896,
-0.110307971961426,-0.0628349439114606,-0.000952237661129041),
 .UNSPECIFIED.);
#1412=B_SPLINE_CURVE_WITH_KNOTS('',3,(#38215,#38216,#38217,#38218,#38219,
#38220,#38221,#38222,#38223,#38224,#38225,#38226,#38227,#38228,#38229,#38230,
#38231,#38232,#38233,#38234,#38235,#38236,#38237,#38238,#38239,#38240,#38241,
#38242,#38243,#38244,#38245,#38246,#38247,#38248,#38249,#38250,#38251,#38252,
#38253,#38254,#38255,#38256,#38257,#38258,#38259,#38260,#38261,#38262,#38263,
#38264,#38265,#38266,#38267,#38268,#38269,#38270,#38271,#38272,#38273,#38274,
#38275,#38276,#38277,#38278,#38279,#38280,#38281,#38282,#38283,#38284,#38285,
#38286,#38287,#38288,#38289,#38290,#38291,#38292,#38293,#38294,#38295,#38296,
#38297,#38298,#38299,#38300,#38301,#38302,#38303,#38304,#38305,#38306,#38307,
#38308,#38309,#38310,#38311,#38312,#38313,#38314,#38315,#38316,#38317,#38318,
#38319,#38320,#38321,#38322,#38323,#38324,#38325,#38326,#38327,#38328,#38329,
#38330,#38331,#38332,#38333,#38334,#38335,#38336,#38337,#38338,#38339,#38340,
#38341,#38342,#38343,#38344,#38345,#38346,#38347,#38348,#38349,#38350,#38351,
#38352,#38353,#38354,#38355,#38356,#38357,#38358,#38359,#38360,#38361,#38362,
#38363,#38364,#38365,#38366),.UNSPECIFIED.,.F.,.F.,(4,2,2,2,2,2,2,2,2,2,
2,2,2,2,2,2,2,2,2,2,2,2,2,2,2,2,2,2,2,2,2,2,2,2,2,2,2,2,2,2,2,2,2,2,2,2,
2,2,2,2,2,2,2,2,2,2,2,2,2,2,2,2,2,2,2,2,2,2,2,2,2,2,2,2,2,4),(-4.06185261524568,
-4.05708505957242,-4.05285548409638,-4.05048801339724,-4.04823074791862,
-4.04563329060578,-4.04134734048006,-4.02716467492896,-3.93797472700334,
-3.9019124917828,-3.89375527840498,-3.88898819998056,-3.88478527056778,
-3.87952386631328,-3.87130138877667,-3.8091722107146,-3.7650108488942,-3.74487644788151,
-3.73676904555361,-3.73245803578029,-3.72964128156967,-3.72701440386011,
-3.72474687911975,-3.72171150001949,-3.71666839048799,-3.67821588273949,
-3.63749521856553,-3.58627285361472,-3.57407082775049,-3.56849012007095,
-3.56424904401895,-3.56021778922336,-3.55338446127771,-3.53441611565386,
-3.43304323888024,-3.41894522220792,-3.40962994361556,-3.40609779174135,
-3.40366283211739,-3.40143556427606,-3.39833033781048,-3.39022866052372,
-3.34004250345076,-3.29298931647877,-3.25716937035706,-3.24902573699305,
-3.24426094051343,-3.24005660939871,-3.23478892769658,-3.22654778293989,
-3.16433734774897,-3.09757330317497,-3.08750079468223,-3.08385986502947,
-3.0814028314911,-3.07919651201705,-3.07617304807871,-3.06858515033518,
-3.00281982176751,-2.95797595212944,-2.94147464976351,-2.9292320842113,
-2.92364319671007,-2.9194001018845,-2.91537005439773,-2.90854645208976,
-2.8896550141435,-2.78815743119671,-2.77405220546355,-2.76473281612469,
-2.76119953177653,-2.75876392605747,-2.75653617463109,-2.75343041447236,
-2.7453283942911,-2.69294542034399),.UNSPECIFIED.);
#1413=B_SPLINE_CURVE_WITH_KNOTS('',3,(#38372,#38373,#38374,#38375,#38376,
#38377,#38378,#38379,#38380,#38381,#38382,#38383,#38384,#38385,#38386,#38387,
#38388,#38389,#38390,#38391,#38392,#38393,#38394,#38395,#38396,#38397,#38398,
#38399,#38400,#38401,#38402,#38403,#38404,#38405,#38406,#38407,#38408,#38409,
#38410,#38411,#38412,#38413,#38414,#38415,#38416,#38417,#38418,#38419,#38420,
#38421,#38422,#38423,#38424,#38425,#38426,#38427,#38428,#38429,#38430,#38431,
#38432,#38433,#38434,#38435,#38436,#38437,#38438,#38439,#38440,#38441,#38442,
#38443,#38444,#38445,#38446,#38447,#38448,#38449,#38450,#38451,#38452,#38453,
#38454,#38455,#38456,#38457,#38458,#38459,#38460,#38461,#38462,#38463,#38464,
#38465,#38466,#38467,#38468,#38469,#38470,#38471,#38472,#38473,#38474,#38475,
#38476,#38477,#38478,#38479,#38480,#38481,#38482,#38483,#38484,#38485,#38486,
#38487,#38488,#38489,#38490,#38491,#38492,#38493,#38494,#38495,#38496,#38497,
#38498,#38499,#38500,#38501,#38502,#38503,#38504,#38505,#38506,#38507,#38508,
#38509,#38510,#38511,#38512,#38513,#38514,#38515,#38516,#38517,#38518,#38519,
#38520,#38521,#38522,#38523,#38524,#38525,#38526,#38527,#38528,#38529,#38530,
#38531,#38532,#38533,#38534,#38535,#38536,#38537,#38538,#38539,#38540,#38541),
 .UNSPECIFIED.,.F.,.F.,(4,2,2,2,2,2,2,2,2,2,2,2,2,2,2,2,2,2,2,2,2,2,2,2,
2,2,2,2,2,2,2,2,2,2,2,2,2,2,2,2,2,2,2,2,2,2,2,2,2,2,2,2,2,2,2,2,2,2,2,2,
2,2,2,2,2,2,2,2,2,2,2,2,2,2,2,2,2,2,2,2,2,2,2,2,4),(-1.36962177122299,-1.32182238407877,
-1.2850684154456,-1.2766479916492,-1.27177604658522,-1.2675856555344,-1.26247354222409,
-1.25268228975713,-1.18750292975858,-1.12163581844339,-1.11402897599387,
-1.11101678020998,-1.10881444934637,-1.10635682666759,-1.10270651555574,
-1.09255341807395,-1.02436884386449,-0.963808535367563,-0.955538417418492,
-0.950264073430916,-0.946062038647845,-0.941308016168192,-0.933203263951293,
-0.897942597175451,-0.821877560973487,-0.795334998583643,-0.790618255399449,
-0.787648544140803,-0.785295299188886,-0.782486233010396,-0.777224052104454,
-0.743663907147497,-0.674576387054659,-0.639984306066628,-0.631708228834379,
-0.626868871275764,-0.622675920731407,-0.61752189843231,-0.607526714675422,
-0.594797198581604,-0.564970564067933,-0.510393274605143,-0.47354531156842,
-0.468527411580614,-0.465500213898569,-0.463138548690593,-0.460408672452058,
-0.455515993119272,-0.430927490760664,-0.361423714917032,-0.318448951647306,
-0.310499590705437,-0.305322707088563,-0.301231227374083,-0.30105429487929,
-0.300902520899787,-0.300771061449599,-0.300656266565702,-0.30055532642677,
-0.300466037865446,-0.300386646236463,-0.300315734701143,-0.300252145090754,
-0.300194920288565,-0.300143261810963,-0.300096497688419,-0.299999268182783,
-0.299903724084309,-0.299809713955632,-0.299717096139761,-0.294358139630899,
-0.288464823804344,-0.278695201476487,-0.232408053373161,-0.185644132521259,
-0.167449926824457,-0.149619423537348,-0.144974576360588,-0.142298868733295,
-0.139926618290346,-0.136757270754286,-0.129653568615952,-0.0985749262887441,
-0.0571044553074189,-0.000952159825757125),.UNSPECIFIED.);
#1414=B_SPLINE_CURVE_WITH_KNOTS('',3,(#38542,#38543,#38544,#38545,#38546,
#38547,#38548,#38549,#38550,#38551,#38552,#38553,#38554,#38555,#38556,#38557,
#38558,#38559,#38560,#38561,#38562,#38563,#38564,#38565,#38566,#38567,#38568,
#38569,#38570,#38571,#38572,#38573,#38574,#38575,#38576,#38577,#38578,#38579,
#38580,#38581,#38582,#38583,#38584,#38585,#38586,#38587,#38588,#38589,#38590,
#38591,#38592,#38593,#38594,#38595,#38596,#38597,#38598,#38599,#38600,#38601,
#38602,#38603,#38604,#38605,#38606,#38607,#38608,#38609,#38610,#38611,#38612,
#38613,#38614,#38615,#38616,#38617,#38618,#38619,#38620,#38621),
 .UNSPECIFIED.,.F.,.F.,(4,2,2,2,2,2,2,2,2,2,2,2,2,2,2,2,2,2,2,2,2,2,2,2,
2,2,2,2,2,2,2,2,2,2,2,2,2,2,2,4),(-4.06117045119648,-4.05432040146447,-4.04820732500887,
-4.04405540252273,-4.04004268008692,-4.03552792660978,-4.02851751083157,
-4.00815949447454,-3.91997642877976,-3.89864540712678,-3.89021892851807,
-3.88391880491664,-3.88089961445068,-3.87854339025131,-3.87577320438849,
-3.87083180211565,-3.8482717028776,-3.79138267103709,-3.75309717597981,
-3.73812484563565,-3.7302141293804,-3.7234391480088,-3.71902805471729,-3.71489490299815,
-3.70930676310575,-3.69671262406839,-3.63713135686164,-3.58652338952762,
-3.57229722549555,-3.5629210126716,-3.55938155573755,-3.55694654878127,
-3.55472329147679,-3.55162904644104,-3.54359479034715,-3.48756188402932,
-3.43613156191842,-3.41827444551578,-3.40526776157587,-3.40003668949591),
 .UNSPECIFIED.);
#1415=B_SPLINE_CURVE_WITH_KNOTS('',3,(#38622,#38623,#38624,#38625,#38626,
#38627,#38628,#38629,#38630,#38631,#38632,#38633,#38634,#38635,#38636,#38637,
#38638,#38639,#38640,#38641,#38642,#38643,#38644,#38645,#38646,#38647,#38648,
#38649,#38650,#38651,#38652,#38653,#38654,#38655,#38656,#38657,#38658,#38659,
#38660,#38661,#38662,#38663,#38664,#38665,#38666,#38667,#38668,#38669,#38670,
#38671,#38672,#38673,#38674,#38675,#38676,#38677,#38678,#38679,#38680,#38681,
#38682,#38683,#38684,#38685,#38686,#38687,#38688,#38689,#38690,#38691,#38692,
#38693,#38694,#38695,#38696,#38697,#38698,#38699,#38700,#38701,#38702,#38703,
#38704,#38705,#38706,#38707,#38708,#38709,#38710,#38711,#38712,#38713,#38714,
#38715,#38716,#38717,#38718,#38719,#38720,#38721,#38722,#38723,#38724,#38725,
#38726,#38727,#38728,#38729,#38730,#38731,#38732,#38733,#38734,#38735,#38736,
#38737,#38738,#38739,#38740,#38741,#38742,#38743,#38744,#38745,#38746,#38747,
#38748,#38749,#38750,#38751,#38752,#38753,#38754,#38755,#38756,#38757,#38758,
#38759,#38760,#38761,#38762,#38763,#38764,#38765,#38766,#38767,#38768,#38769,
#38770,#38771,#38772,#38773,#38774,#38775,#38776,#38777,#38778,#38779,#38780,
#38781,#38782,#38783,#38784,#38785,#38786,#38787,#38788,#38789,#38790,#38791,
#38792,#38793,#38794,#38795,#38796,#38797,#38798,#38799,#38800,#38801,#38802,
#38803,#38804,#38805,#38806,#38807,#38808,#38809,#38810,#38811,#38812,#38813,
#38814,#38815,#38816,#38817,#38818,#38819,#38820,#38821,#38822,#38823,#38824,
#38825,#38826,#38827,#38828,#38829,#38830,#38831,#38832,#38833),
 .UNSPECIFIED.,.F.,.F.,(4,2,2,2,2,2,2,2,2,2,2,2,2,2,2,2,2,2,2,2,2,2,2,2,
2,2,2,2,2,2,2,2,2,2,2,2,2,2,2,2,2,2,2,2,2,2,2,2,2,2,2,2,2,2,2,2,2,2,2,2,
2,2,2,2,2,2,2,2,2,2,2,2,2,2,2,2,2,2,2,2,2,2,2,2,2,2,2,2,2,2,2,2,2,2,2,2,
2,2,2,2,2,2,2,2,2,4),(-2.69294542034399,-2.6928928505863,-2.63882773344267,
-2.62046805321308,-2.60717972549637,-2.60140556837181,-2.59713292897633,
-2.5926121473132,-2.58558988602039,-2.56522502157542,-2.48174327500305,
-2.44571414558974,-2.44037515616131,-2.43754814321433,-2.43519327223398,
-2.43223823580005,-2.42757530572775,-2.40206255512511,-2.33428226751476,
-2.30522795517801,-2.292715775396,-2.2828527242158,-2.27772241827823,-2.27352666660196,
-2.26865922006533,-2.26027326705638,-2.22412977976389,-2.15563720238791,
-2.13358950146674,-2.12076754597086,-2.11678269506573,-2.11425104527045,
-2.11184193069927,-2.1083216841153,-2.10165930919544,-2.03189129800188,
-1.9690142415646,-1.96076853474069,-1.95549855236157,-1.95129280698205,
-1.94652685895233,-1.9383823986052,-1.90258355541477,-1.85560889915667,
-1.80520447788957,-1.79710075146804,-1.79399451054906,-1.79176649850709,
-1.7893306834325,-1.78579723886,-1.77647811203658,-1.76237550650481,-1.66086984352645,
-1.64201247297892,-1.63519307551586,-1.63116346129063,-1.62691931175715,
-1.62132651941167,-1.60906512556103,-1.59252987716967,-1.54753501965914,
-1.48191211377001,-1.47430916637186,-1.47128321412731,-1.46907601844971,
-1.46661911477013,-1.4629802977569,-1.45292568784383,-1.38647487275192,
-1.32397558480673,-1.31572756343887,-1.31045721288047,-1.3062518814333,
-1.30148716026879,-1.29334668752886,-1.25760066767841,-1.2107633559977,
-1.1601774920642,-1.15207589395443,-1.14897018257566,-1.14674247846021,
-1.1443069162732,-1.14077369925754,-1.13145437067886,-1.11735075537655,
-1.01578551736578,-0.996988724428408,-0.990178316015324,-0.98615075214909,
-0.981906388702902,-0.976309319099813,-0.964022082492951,-0.947441069525992,
-0.902232903132334,-0.83695398650396,-0.829332420207833,-0.826303532047379,
-0.824095771446446,-0.821640128979283,-0.818006424100635,-0.807986549320123,
-0.742099339856279,-0.679001869411645,-0.670758081219974,-0.665489345942252,
-0.662282742015645),.UNSPECIFIED.);
#1416=B_SPLINE_CURVE_WITH_KNOTS('',3,(#38838,#38839,#38840,#38841,#38842,
#38843,#38844,#38845,#38846,#38847,#38848,#38849,#38850,#38851,#38852,#38853,
#38854,#38855,#38856,#38857,#38858,#38859,#38860,#38861,#38862,#38863,#38864,
#38865,#38866,#38867,#38868,#38869,#38870,#38871,#38872,#38873,#38874,#38875,
#38876,#38877,#38878,#38879,#38880,#38881,#38882,#38883,#38884,#38885,#38886,
#38887,#38888,#38889,#38890,#38891,#38892,#38893,#38894,#38895,#38896,#38897,
#38898,#38899,#38900,#38901,#38902,#38903,#38904,#38905,#38906,#38907,#38908,
#38909,#38910,#38911,#38912,#38913,#38914,#38915,#38916,#38917,#38918,#38919,
#38920,#38921,#38922,#38923,#38924,#38925,#38926,#38927,#38928,#38929,#38930,
#38931,#38932,#38933,#38934,#38935,#38936,#38937,#38938,#38939,#38940,#38941,
#38942,#38943,#38944,#38945,#38946,#38947,#38948,#38949,#38950,#38951,#38952,
#38953,#38954,#38955,#38956,#38957,#38958,#38959,#38960,#38961,#38962,#38963,
#38964,#38965,#38966,#38967,#38968,#38969,#38970,#38971,#38972,#38973,#38974,
#38975,#38976,#38977,#38978,#38979,#38980,#38981,#38982,#38983,#38984,#38985,
#38986,#38987,#38988,#38989,#38990,#38991,#38992,#38993,#38994,#38995,#38996,
#38997,#38998,#38999,#39000,#39001,#39002,#39003,#39004,#39005,#39006,#39007,
#39008,#39009,#39010,#39011,#39012,#39013,#39014,#39015,#39016,#39017,#39018,
#39019,#39020,#39021,#39022,#39023,#39024,#39025,#39026,#39027,#39028,#39029,
#39030,#39031,#39032,#39033,#39034,#39035,#39036,#39037,#39038,#39039,#39040,
#39041,#39042,#39043,#39044,#39045,#39046,#39047,#39048,#39049,#39050,#39051,
#39052,#39053,#39054,#39055,#39056,#39057,#39058,#39059),.UNSPECIFIED.,
 .F.,.F.,(4,2,2,2,2,2,2,2,2,2,2,2,2,2,2,2,2,2,2,2,2,2,2,2,2,2,2,2,2,2,2,
2,2,2,2,2,2,2,2,2,2,2,2,2,2,2,2,2,2,2,2,2,2,2,2,2,2,2,2,2,2,2,2,2,2,2,2,
2,2,2,2,2,2,2,2,2,2,2,2,2,2,2,2,2,2,2,2,2,2,2,2,2,2,2,2,2,2,2,2,2,2,2,2,
2,2,2,2,2,2,2,4),(-3.3994167761936,-3.39442164906984,-3.38034416848886,
-3.37104051307309,-3.36751186976563,-3.36507907224068,-3.36285366078891,
-3.35975096200867,-3.35165554862964,-3.30100762950804,-3.25427519164643,
-3.21857971483864,-3.21044830756437,-3.20568869112948,-3.20148778011025,
-3.19622290320236,-3.1879833653753,-3.1246250833392,-3.07594174580726,-3.05142103747698,
-3.04653208060429,-3.04380315307592,-3.04144155771395,-3.03841353784895,
-3.03339243686023,-2.99626609088144,-2.93884108569202,-2.89687999990697,
-2.88840549223081,-2.88357130827243,-2.87937830325598,-2.87421842624741,
-2.86632422209368,-2.8248786322846,-2.76069798320331,-2.73968637964977,
-2.73134446192148,-2.72509350438527,-2.72208381098282,-2.71972824334746,
-2.71695089919474,-2.711978011135,-2.68889421130294,-2.68210448756076,-2.65873907925416,
-2.60216153431056,-2.5829077543951,-2.56913261967478,-2.56327947306876,
-2.55899681241839,-2.55450938046214,-2.54762794246094,-2.52829684464235,
-2.4435946728105,-2.41902560223549,-2.40522957091918,-2.40114204502221,
-2.39858947688626,-2.39619704579261,-2.39329511321307,-2.38589880449259,
-2.3149433806828,-2.25319040220295,-2.24410459153482,-2.23913933008357,
-2.23536589931028,-2.23052292613989,-2.22223111821802,-2.18743592920801,
-2.11829660317755,-2.08494018612046,-2.07968405892186,-2.07687622296797,
-2.0745228139862,-2.07155139976785,-2.06682923127756,-2.04025420278267,
-2.03098288674323,-1.95130234511404,-1.9276865466937,-1.92027949207753,
-1.91567792578148,-1.91144223800245,-1.90588624872804,-1.89381024758399,
-1.84364606886248,-1.80572011082791,-1.76320794821286,-1.75762814515457,
-1.75471648680764,-1.75236536664811,-1.74950556751446,-1.74400095954611,
-1.70003078407794,-1.62925045805596,-1.60538371161242,-1.59794881307469,
-1.59334125865426,-1.58910760413258,-1.58356525366598,-1.571563048529,-1.52202261712466,
-1.47429685932129,-1.44063945666054,-1.43566504155081,-1.43265060561563,
-1.43029030101327,-1.42755186631513,-1.42261945334926,-1.39725725750434,
-1.36962177122299),.UNSPECIFIED.);
#1417=B_SPLINE_CURVE_WITH_KNOTS('',3,(#39061,#39062,#39063,#39064,#39065,
#39066,#39067,#39068,#39069,#39070,#39071,#39072,#39073,#39074,#39075,#39076,
#39077,#39078,#39079,#39080,#39081,#39082,#39083,#39084,#39085,#39086,#39087,
#39088,#39089,#39090,#39091,#39092,#39093,#39094,#39095,#39096,#39097,#39098,
#39099,#39100,#39101,#39102,#39103,#39104,#39105,#39106,#39107,#39108,#39109,
#39110,#39111,#39112,#39113,#39114,#39115,#39116,#39117,#39118,#39119,#39120,
#39121,#39122,#39123,#39124,#39125,#39126,#39127,#39128,#39129,#39130,#39131,
#39132,#39133,#39134,#39135,#39136,#39137,#39138,#39139,#39140),
 .UNSPECIFIED.,.F.,.F.,(4,2,2,2,2,2,2,2,2,2,2,2,2,2,2,2,2,2,2,2,2,2,2,2,
2,2,2,2,2,2,2,2,2,2,2,2,2,2,2,4),(-0.662282742015645,-0.661284609116616,
-0.65651981822441,-0.648377370840048,-0.612588039983296,-0.565627149997621,
-0.515231285197535,-0.507129541221009,-0.504024051326852,-0.501796575742074,
-0.499361344563022,-0.495828742688839,-0.486511813576414,-0.472412512024089,
-0.370929012965544,-0.352077976412442,-0.345260469629144,-0.34123187182051,
-0.337073255615075,-0.331647011656286,-0.325655356851237,-0.315646278901475,
-0.26372876092633,-0.200490038387841,-0.186388137487069,-0.182106016680302,
-0.179509202537946,-0.177108491527682,-0.17376192644085,-0.165636438546779,
-0.153896725804903,-0.118005807928824,-0.048596137079172,-0.0297128719064544,
-0.0228966503970393,-0.0188682031481931,-0.0148170287410706,-0.0107010941196923,
-0.00592907222480298,-0.000951129530177771),.UNSPECIFIED.);
#1418=B_SPLINE_CURVE_WITH_KNOTS('',3,(#39141,#39142,#39143,#39144,#39145,
#39146,#39147,#39148,#39149,#39150,#39151,#39152,#39153,#39154,#39155,#39156,
#39157,#39158,#39159,#39160,#39161,#39162,#39163,#39164,#39165,#39166,#39167,
#39168,#39169,#39170,#39171,#39172,#39173,#39174,#39175,#39176,#39177,#39178,
#39179,#39180,#39181,#39182,#39183,#39184,#39185,#39186,#39187,#39188,#39189,
#39190,#39191,#39192,#39193,#39194,#39195,#39196,#39197,#39198,#39199,#39200,
#39201,#39202,#39203,#39204,#39205,#39206,#39207,#39208,#39209,#39210,#39211,
#39212,#39213,#39214,#39215,#39216,#39217,#39218,#39219,#39220,#39221,#39222,
#39223,#39224,#39225,#39226,#39227,#39228,#39229,#39230,#39231,#39232,#39233,
#39234,#39235,#39236,#39237,#39238,#39239,#39240,#39241,#39242,#39243,#39244,
#39245,#39246,#39247,#39248,#39249,#39250,#39251,#39252,#39253,#39254,#39255,
#39256,#39257,#39258,#39259,#39260,#39261,#39262,#39263,#39264,#39265,#39266,
#39267,#39268,#39269,#39270,#39271,#39272,#39273,#39274,#39275,#39276,#39277,
#39278,#39279,#39280,#39281,#39282,#39283,#39284,#39285,#39286,#39287,#39288,
#39289,#39290,#39291,#39292,#39293,#39294),.UNSPECIFIED.,.F.,.F.,(4,2,2,
2,2,2,2,2,2,2,2,2,2,2,2,2,2,2,2,2,2,2,2,2,2,2,2,2,2,2,2,2,2,2,2,2,2,2,2,
2,2,2,2,2,2,2,2,2,2,2,2,2,2,2,2,2,2,2,2,2,2,2,2,2,2,2,2,2,2,2,2,2,2,2,2,
2,4),(-4.06127466498446,-4.04616684401087,-3.97047454395635,-3.92646874790103,
-3.92095911744303,-3.91809662598807,-3.91574320000556,-3.91282842395056,
-3.90724180230987,-3.86413442467703,-3.77982965630429,-3.77006485643972,
-3.76417165612202,-3.75889284262175,-3.75879592892169,-3.75869792845998,
-3.758654605828,-3.75860797743966,-3.75855767045854,-3.75850325201899,-3.75844421720845,
-3.75837997161098,-3.75435690992838,-3.74963528309801,-3.74169176430377,
-3.71296338618885,-3.63854116380484,-3.60362267173816,-3.59831544269605,
-3.59549528337143,-3.59314029656281,-3.59017777113489,-3.58548961148469,
-3.55943638261745,-3.47326493020888,-3.44636455324335,-3.43888884462978,
-3.43426964561768,-3.4300343110146,-3.42459533483568,-3.41284898050076,
-3.33373121445113,-3.29730506176416,-3.28546030294407,-3.27728027233682,
-3.27392436257466,-3.27152169357215,-3.26924992532191,-3.26530565289905,
-3.25392851460564,-3.18841759114668,-3.12778225177244,-3.118141613754,-3.11305756918907,
-3.10927184186816,-3.1045164260944,-3.09641799433392,-3.06572996883521,
-3.06035001451274,-2.99145755281917,-2.96916959972103,-2.96049080410266,
-2.95404345584398,-2.95099413708534,-2.94863328774185,-2.94587944319076,
-2.94101734350758,-2.91971424325242,-2.85128718887266,-2.80376883539671,
-2.79505251290309,-2.79016335172717,-2.78639023046136,-2.78146670796622,
-2.77283088029294,-2.73203329550979,-2.69212785249457),.UNSPECIFIED.);
#1419=B_SPLINE_CURVE_WITH_KNOTS('',3,(#39300,#39301,#39302,#39303,#39304,
#39305,#39306,#39307,#39308,#39309,#39310,#39311,#39312,#39313,#39314,#39315,
#39316,#39317,#39318,#39319,#39320,#39321,#39322,#39323,#39324,#39325,#39326,
#39327,#39328,#39329,#39330,#39331,#39332,#39333,#39334,#39335,#39336,#39337,
#39338,#39339,#39340,#39341,#39342,#39343,#39344,#39345,#39346,#39347,#39348,
#39349,#39350,#39351,#39352,#39353,#39354,#39355,#39356,#39357,#39358,#39359,
#39360,#39361,#39362,#39363,#39364,#39365,#39366,#39367,#39368,#39369,#39370,
#39371,#39372,#39373,#39374,#39375,#39376,#39377,#39378,#39379,#39380,#39381,
#39382,#39383,#39384,#39385,#39386,#39387,#39388,#39389,#39390,#39391,#39392,
#39393,#39394,#39395,#39396,#39397,#39398,#39399,#39400,#39401,#39402,#39403,
#39404,#39405,#39406,#39407,#39408,#39409,#39410,#39411,#39412,#39413,#39414,
#39415,#39416,#39417,#39418,#39419,#39420,#39421,#39422,#39423,#39424,#39425,
#39426,#39427,#39428,#39429,#39430,#39431,#39432,#39433,#39434,#39435,#39436,
#39437,#39438,#39439,#39440,#39441),.UNSPECIFIED.,.F.,.F.,(4,2,2,2,2,2,
2,2,2,2,2,2,2,2,2,2,2,2,2,2,2,2,2,2,2,2,2,2,2,2,2,2,2,2,2,2,2,2,2,2,2,2,
2,2,2,2,2,2,2,2,2,2,2,2,2,2,2,2,2,2,2,2,2,2,2,2,2,2,2,2,4),(-1.36995468810373,
-1.34524430130784,-1.30338042112438,-1.25385409901805,-1.24572391017952,
-1.24261634850845,-1.24038956640011,-1.23795771106143,-1.2344345040908,
-1.22516837960924,-1.21116959496001,-1.11217702182287,-1.09127186798715,
-1.08418208159927,-1.07965014794946,-1.07538981055964,-1.06966744815885,
-1.05665596467422,-1.03878767222862,-0.987297698675521,-0.931292979870644,
-0.92325532097066,-0.920160706027039,-0.917937472027335,-0.915502804041723,
-0.911964383517623,-0.902593932000619,-0.888380813959507,-0.837850616048762,
-0.778210893282045,-0.765644694319501,-0.760061724111958,-0.755807864754708,
-0.751260004683357,-0.744097182129189,-0.720390424635643,-0.678844055005731,
-0.613122878452704,-0.601988986900391,-0.59808069870273,-0.595817581080475,
-0.593413586299495,-0.590039224463397,-0.581732840347395,-0.569642362709692,
-0.531908990025203,-0.454926668424072,-0.442986909024379,-0.437515928056792,
-0.433279479621659,-0.42868294282424,-0.421296924545675,-0.395322131364976,
-0.347091034762141,-0.286363529461873,-0.278517086967082,-0.275452013475459,
-0.273236391064645,-0.270794024627438,-0.267423759764045,-0.258770103617987,
-0.245807996088087,-0.203212882845492,-0.133253784209077,-0.120872881083716,
-0.115322564978666,-0.111073861709748,-0.106512302107184,-0.0992868843734209,
-0.0749678591588764,-0.000952473517230175),.UNSPECIFIED.);
#1420=B_SPLINE_CURVE_WITH_KNOTS('',3,(#39442,#39443,#39444,#39445,#39446,
#39447,#39448,#39449,#39450,#39451,#39452,#39453,#39454,#39455,#39456,#39457,
#39458,#39459,#39460,#39461,#39462,#39463,#39464,#39465,#39466,#39467,#39468,
#39469,#39470,#39471,#39472,#39473,#39474,#39475,#39476,#39477,#39478,#39479,
#39480,#39481,#39482,#39483,#39484,#39485,#39486,#39487,#39488,#39489,#39490,
#39491,#39492,#39493,#39494,#39495,#39496,#39497,#39498,#39499,#39500,#39501,
#39502,#39503,#39504,#39505,#39506,#39507,#39508,#39509,#39510,#39511,#39512,
#39513),.UNSPECIFIED.,.F.,.F.,(4,2,2,2,2,2,2,2,2,2,2,2,2,2,2,2,2,2,2,2,
2,2,2,2,2,2,2,2,2,2,2,2,2,2,2,4),(-4.06017442960531,-4.0198490772075,-4.01576004008251,
-4.01303507719492,-4.01080972136062,-4.00845177097557,-4.00540465693538,
-4.00042736929215,-3.96665499648457,-3.92853463158271,-3.88846571308708,
-3.86195146965499,-3.85451667113691,-3.8499100745933,-3.84567789720946,
-3.84023133589455,-3.82842189084888,-3.75004256126864,-3.71318209887599,
-3.70125809957024,-3.69309095727252,-3.68990865565758,-3.68747609677886,
-3.68525131261838,-3.68215002334286,-3.67406227250093,-3.62558125273539,
-3.56915683250162,-3.54993314420651,-3.53617517860012,-3.53032579293961,
-3.52604460119274,-3.52155755050054,-3.5146743720624,-3.49532315562753,
-3.3994167761936),.UNSPECIFIED.);
#1421=B_SPLINE_CURVE_WITH_KNOTS('',3,(#39514,#39515,#39516,#39517,#39518,
#39519,#39520,#39521,#39522,#39523,#39524,#39525,#39526,#39527,#39528,#39529,
#39530,#39531,#39532,#39533,#39534,#39535,#39536,#39537,#39538,#39539,#39540,
#39541,#39542,#39543,#39544,#39545,#39546,#39547,#39548,#39549,#39550,#39551,
#39552,#39553,#39554,#39555,#39556,#39557,#39558,#39559,#39560,#39561,#39562,
#39563,#39564,#39565,#39566,#39567,#39568,#39569,#39570,#39571,#39572,#39573,
#39574,#39575,#39576,#39577,#39578,#39579,#39580,#39581,#39582,#39583,#39584,
#39585,#39586,#39587,#39588,#39589,#39590,#39591,#39592,#39593,#39594,#39595,
#39596,#39597,#39598,#39599,#39600,#39601,#39602,#39603,#39604,#39605,#39606,
#39607,#39608,#39609,#39610,#39611,#39612,#39613,#39614,#39615,#39616,#39617,
#39618,#39619,#39620,#39621,#39622,#39623,#39624,#39625,#39626,#39627,#39628,
#39629,#39630,#39631,#39632,#39633,#39634,#39635,#39636,#39637,#39638,#39639,
#39640,#39641,#39642,#39643,#39644,#39645,#39646,#39647,#39648,#39649,#39650,
#39651,#39652,#39653,#39654,#39655,#39656,#39657,#39658,#39659,#39660,#39661,
#39662,#39663,#39664,#39665,#39666,#39667,#39668,#39669,#39670,#39671,#39672,
#39673,#39674,#39675,#39676,#39677,#39678,#39679,#39680,#39681,#39682,#39683,
#39684,#39685,#39686,#39687,#39688,#39689,#39690,#39691,#39692,#39693,#39694,
#39695,#39696,#39697,#39698,#39699,#39700,#39701,#39702,#39703,#39704,#39705,
#39706,#39707,#39708,#39709,#39710,#39711,#39712,#39713,#39714,#39715,#39716,
#39717,#39718,#39719,#39720,#39721,#39722,#39723,#39724,#39725,#39726,#39727,
#39728,#39729,#39730,#39731,#39732,#39733),.UNSPECIFIED.,.F.,.F.,(4,2,2,
2,2,2,2,2,2,2,2,2,2,2,2,2,2,2,2,2,2,2,2,2,2,2,2,2,2,2,2,2,2,2,2,2,2,2,2,
2,2,2,2,2,2,2,2,2,2,2,2,2,2,2,2,2,2,2,2,2,2,2,2,2,2,2,2,2,2,2,2,2,2,2,2,
2,2,2,2,2,2,2,2,2,2,2,2,2,2,2,2,2,2,2,2,2,2,2,2,2,2,2,2,2,2,2,2,2,2,4),
(-2.69212785249457,-2.66727989701356,-2.64616552319342,-2.63372095713774,
-2.62977944367602,-2.62725759520586,-2.62484259551211,-2.62185868194171,
-2.61450067773853,-2.54603231520456,-2.50284379339667,-2.47854511713085,
-2.47131710508253,-2.46675188238764,-2.46249832932244,-2.45693955784036,
-2.44453044219312,-2.37500383879394,-2.33825943763338,-2.31314383103301,
-2.30822044203222,-2.3054823403991,-2.30311924247648,-2.30004646120218,
-2.29498940071131,-2.25579361013186,-2.19982510615917,-2.17242202643007,
-2.15453852058383,-2.14806190019371,-2.14365648324377,-2.13936157699765,
-2.13322307101615,-2.12192964601337,-2.05693899247034,-2.03067445315504,
-1.99189091181378,-1.98683951417776,-1.98380104542996,-1.98143619355091,
-1.97870906071893,-1.97383643370548,-1.94968474053626,-1.9006716669888,
-1.83727555436632,-1.82903016521644,-1.8237605959357,-1.81955531407384,
-1.81479003463521,-1.80664707460547,-1.77086151125462,-1.72391719760335,
-1.67348284724176,-1.6653803786339,-1.66227453779059,-1.6600467921085,-1.65761124425224,
-1.65407814741565,-1.64475970803118,-1.63065794107718,-1.52914335636685,
-1.51030482618826,-1.50348854456057,-1.49945983912708,-1.49521596877495,
-1.48962240378856,-1.47735462145513,-1.46080764957954,-1.41575566780296,
-1.350236371517,-1.34262848338344,-1.33960189497708,-1.33739470476851,-1.33493837029946,
-1.33130136381787,-1.32125791442368,-1.25498117251233,-1.19230467414953,
-1.18406010712324,-1.17879111925732,-1.17458633706122,-1.16982166203015,
-1.16167983015368,-1.12590100516029,-1.07896896824866,-1.02853118431582,
-1.0204297653349,-1.0173243075528,-1.01509683178548,-1.0126615735444,-1.00912888745757,
-0.99981147730133,-0.985711220417281,-0.884203988641315,-0.865371640796756,
-0.858556726509011,-0.854528609945143,-0.850285200428662,-0.844691974525185,
-0.832423830999553,-0.815875640377666,-0.770814398639095,-0.705325544789426,
-0.697717230149788,-0.694690778709533,-0.69248379655605,-0.690027823549075,
-0.686391575204932,-0.676351637263147,-0.661760008706104),.UNSPECIFIED.);
#1422=B_SPLINE_CURVE_WITH_KNOTS('',3,(#39738,#39739,#39740,#39741,#39742,
#39743,#39744,#39745,#39746,#39747,#39748,#39749,#39750,#39751,#39752,#39753,
#39754,#39755,#39756,#39757,#39758,#39759,#39760,#39761,#39762,#39763,#39764,
#39765,#39766,#39767,#39768,#39769,#39770,#39771,#39772,#39773,#39774,#39775,
#39776,#39777,#39778,#39779,#39780,#39781,#39782,#39783,#39784,#39785,#39786,
#39787,#39788,#39789,#39790,#39791,#39792,#39793,#39794,#39795,#39796,#39797,
#39798,#39799,#39800,#39801,#39802,#39803,#39804,#39805,#39806,#39807,#39808,
#39809,#39810,#39811,#39812,#39813,#39814,#39815,#39816,#39817,#39818,#39819,
#39820,#39821,#39822,#39823,#39824,#39825,#39826,#39827,#39828,#39829,#39830,
#39831,#39832,#39833,#39834,#39835,#39836,#39837,#39838,#39839,#39840,#39841,
#39842,#39843,#39844,#39845,#39846,#39847,#39848,#39849,#39850,#39851,#39852,
#39853,#39854,#39855,#39856,#39857,#39858,#39859,#39860,#39861,#39862,#39863,
#39864,#39865,#39866,#39867,#39868,#39869,#39870,#39871,#39872,#39873,#39874,
#39875,#39876,#39877,#39878,#39879,#39880,#39881,#39882,#39883,#39884,#39885,
#39886,#39887,#39888,#39889,#39890,#39891,#39892,#39893,#39894,#39895,#39896,
#39897,#39898,#39899,#39900,#39901,#39902,#39903,#39904,#39905,#39906,#39907,
#39908,#39909,#39910,#39911,#39912,#39913,#39914,#39915,#39916,#39917,#39918,
#39919,#39920,#39921,#39922,#39923,#39924,#39925,#39926,#39927,#39928,#39929,
#39930,#39931,#39932,#39933,#39934,#39935,#39936,#39937,#39938,#39939,#39940,
#39941,#39942,#39943,#39944,#39945,#39946,#39947,#39948,#39949,#39950,#39951,
#39952,#39953,#39954,#39955,#39956,#39957),.UNSPECIFIED.,.F.,.F.,(4,2,2,
2,2,2,2,2,2,2,2,2,2,2,2,2,2,2,2,2,2,2,2,2,2,2,2,2,2,2,2,2,2,2,2,2,2,2,2,
2,2,2,2,2,2,2,2,2,2,2,2,2,2,2,2,2,2,2,2,2,2,2,2,2,2,2,2,2,2,2,2,2,2,2,2,
2,2,2,2,2,2,2,2,2,2,2,2,2,2,2,2,2,2,2,2,2,2,2,2,2,2,2,2,2,2,2,2,2,2,4),
(-3.39979696556878,-3.37744498003102,-3.35861069348364,-3.34506488607214,
-3.33925101834471,-3.33497572703817,-3.33047659469462,-3.32353791987474,
-3.30377703941068,-3.20336296062979,-3.1893038016249,-3.1800090189603,-3.17648164754876,
-3.17404907872227,-3.17182346681411,-3.16871981388899,-3.16061696066295,
-3.10944787344756,-3.06308853098223,-3.02753177484141,-3.01940923573579,
-3.01465168317684,-3.01045070617049,-3.00518324573007,-2.99693477155237,
-2.93449580024307,-2.88962321048857,-2.87016843940872,-2.86224791829032,
-2.85624444755682,-2.85328359261279,-2.85115778200827,-2.84843645517322,
-2.84370964478586,-2.8242719558361,-2.7538353115502,-2.70624824039539,-2.6975353643801,
-2.69264991645845,-2.68888051255544,-2.68396308752625,-2.67534130214054,
-2.63471849325497,-2.56983245064334,-2.54870031757402,-2.54032646183851,
-2.5340569291915,-2.53104364118136,-2.52868785079088,-2.525913290932,-2.52095247404733,
-2.49804446124985,-2.49045724666118,-2.41808443213978,-2.3828173360825,
-2.37471294879723,-2.36995929428552,-2.36575767290137,-2.3604839659525,
-2.35221500590998,-2.29146659305402,-2.22340567794163,-2.21325993987489,
-2.209610785242,-2.20715353032138,-2.20495120965328,-2.20193864029987,-2.19440381423585,
-2.12792641458797,-2.06332607291784,-2.05355455227567,-2.0484466399312,
-2.04425662675977,-2.03938164796086,-2.03094725223126,-1.98767674593242,
-1.92449564771755,-1.91604688421022,-1.89350712134465,-1.88856683422172,
-1.88579692471071,-1.88344068060331,-1.88042116817684,-1.87411935219238,
-1.86569068148351,-1.84435244283121,-1.77833452202546,-1.73908965257323,
-1.73053662282668,-1.7256347024537,-1.72148600367427,-1.71642750066372,
-1.70689555623615,-1.63742854782449,-1.57574003668981,-1.56793526700877,
-1.56487709104276,-1.56266313280061,-1.56021867685184,-1.55663236314167,
-1.54693406861035,-1.48606811636443,-1.42291761599845,-1.41161389175017,
-1.40547567573514,-1.40118399664856,-1.39678445801982,-1.39032135314762,
-1.37250837721402,-1.36995468810373),.UNSPECIFIED.);
#1423=B_SPLINE_CURVE_WITH_KNOTS('',3,(#39959,#39960,#39961,#39962,#39963,
#39964,#39965,#39966,#39967,#39968,#39969,#39970,#39971,#39972,#39973,#39974,
#39975,#39976,#39977,#39978,#39979,#39980,#39981,#39982,#39983,#39984,#39985,
#39986,#39987,#39988,#39989,#39990,#39991,#39992,#39993,#39994,#39995,#39996,
#39997,#39998,#39999,#40000,#40001,#40002,#40003,#40004,#40005,#40006,#40007,
#40008,#40009,#40010,#40011,#40012,#40013,#40014,#40015,#40016,#40017,#40018,
#40019,#40020,#40021,#40022,#40023,#40024,#40025,#40026,#40027,#40028,#40029,
#40030,#40031,#40032),.UNSPECIFIED.,.F.,.F.,(4,2,2,2,2,2,2,2,2,2,2,2,2,
2,2,2,2,2,2,2,2,2,2,2,2,2,2,2,2,2,2,2,2,2,2,2,4),(-0.661760008706104,-0.610121130832886,
-0.547410337844604,-0.539167014544015,-0.533898736112226,-0.529694465651339,
-0.52493031223833,-0.516789226305753,-0.481010963551039,-0.434074418664113,
-0.383656778907406,-0.375556494041579,-0.372451430796078,-0.370224228012008,
-0.367789255423349,-0.36460524451549,-0.356427678910649,-0.344491835723892,
-0.30758588596065,-0.229322918807091,-0.217499950920666,-0.212047622492467,
-0.207811085975501,-0.2031998322688,-0.195757626531973,-0.169216353237172,
-0.127576692493981,-0.0880856711935334,-0.0775501452560537,-0.0561640576798613,
-0.0512972048177857,-0.0485427053965044,-0.0461826211105746,-0.0438770898741965,
-0.0408775438910002,-0.0361210025104908,-0.000950734522379934),
 .UNSPECIFIED.);
#1424=B_SPLINE_CURVE_WITH_KNOTS('',3,(#40033,#40034,#40035,#40036,#40037,
#40038,#40039,#40040,#40041,#40042,#40043,#40044,#40045,#40046,#40047,#40048,
#40049,#40050,#40051,#40052,#40053,#40054,#40055,#40056,#40057,#40058,#40059,
#40060,#40061,#40062,#40063,#40064,#40065,#40066,#40067,#40068,#40069,#40070,
#40071,#40072,#40073,#40074,#40075,#40076,#40077,#40078,#40079,#40080,#40081,
#40082,#40083,#40084,#40085,#40086,#40087,#40088,#40089,#40090,#40091,#40092,
#40093,#40094,#40095,#40096,#40097,#40098,#40099,#40100,#40101,#40102,#40103,
#40104,#40105,#40106,#40107,#40108,#40109,#40110,#40111,#40112,#40113,#40114,
#40115,#40116,#40117,#40118,#40119,#40120,#40121,#40122,#40123,#40124,#40125,
#40126,#40127,#40128,#40129,#40130,#40131,#40132,#40133,#40134,#40135,#40136,
#40137,#40138,#40139,#40140,#40141,#40142,#40143,#40144,#40145,#40146,#40147,
#40148,#40149,#40150,#40151,#40152,#40153,#40154,#40155,#40156,#40157,#40158,
#40159,#40160,#40161,#40162,#40163,#40164,#40165,#40166,#40167,#40168,#40169,
#40170,#40171,#40172,#40173,#40174,#40175,#40176,#40177),.UNSPECIFIED.,
 .F.,.F.,(4,3,3,3,3,3,3,3,3,3,3,3,3,3,3,3,3,3,3,3,3,3,3,3,3,3,3,3,3,3,3,
3,3,3,3,3,3,3,3,3,3,3,3,3,3,3,3,3,4),(122.522113490244,122.613744298623,
122.708839823948,122.80029837443,122.891723140004,122.983140229123,123.074575737944,
123.166108241455,123.257698561075,123.349426790597,123.374508501224,123.467603526403,
123.560572888272,123.653444189759,123.746248050553,123.839017024604,123.931775909089,
124.024549486236,124.117422017638,124.210346529202,124.303425262594,124.372359342951,
124.465454390665,124.558423775412,124.651295100083,124.744098984424,124.836867982237,
124.929626890668,125.022400491916,125.115273047508,125.208197583347,125.301276340902,
125.370210184679,125.46330507077,125.556274293555,125.649145456144,125.741949178877,
125.834718015426,125.927476763126,126.020250204364,126.113122602046,126.2060469809,
126.299125584598,126.368061026406,126.465860047437,126.558813461684,126.651680825063,
126.744477529307,126.759257110528),.UNSPECIFIED.);
#1425=B_SPLINE_CURVE_WITH_KNOTS('',3,(#40183,#40184,#40185,#40186,#40187,
#40188,#40189,#40190,#40191,#40192,#40193,#40194,#40195,#40196,#40197,#40198,
#40199,#40200,#40201,#40202,#40203,#40204,#40205,#40206,#40207,#40208,#40209,
#40210,#40211,#40212,#40213,#40214,#40215,#40216,#40217,#40218,#40219,#40220,
#40221,#40222,#40223,#40224,#40225,#40226,#40227,#40228,#40229,#40230,#40231,
#40232,#40233,#40234,#40235,#40236,#40237,#40238,#40239,#40240,#40241,#40242,
#40243,#40244,#40245,#40246,#40247,#40248,#40249,#40250,#40251,#40252,#40253,
#40254,#40255,#40256,#40257,#40258,#40259,#40260,#40261,#40262,#40263,#40264,
#40265,#40266,#40267,#40268,#40269,#40270,#40271,#40272,#40273,#40274,#40275,
#40276,#40277,#40278,#40279,#40280,#40281,#40282,#40283,#40284,#40285,#40286,
#40287,#40288,#40289,#40290,#40291,#40292,#40293,#40294,#40295,#40296,#40297,
#40298,#40299,#40300,#40301,#40302,#40303,#40304,#40305,#40306,#40307,#40308,
#40309,#40310,#40311,#40312,#40313,#40314,#40315,#40316,#40317,#40318,#40319,
#40320,#40321),.UNSPECIFIED.,.F.,.F.,(4,3,3,3,3,3,3,3,3,3,3,3,3,3,3,3,3,
3,3,3,3,3,3,3,3,3,3,3,3,3,3,3,3,3,3,3,3,3,3,3,3,3,3,3,3,3,4),(128.805298797437,
128.929991698155,129.054684598874,129.147795384353,129.240780462687,129.333667417213,
129.426486773064,129.519271140378,129.61204529876,129.704834012771,129.797721376801,
129.890660574789,129.98375360517,130.052535440601,130.1456368389,130.238612757127,
130.331490787099,130.424301604411,130.517077672376,130.60984377884,130.702624696804,
130.795504705468,130.888436781627,130.981523141936,131.050386282328,131.143399346805,
131.236286529022,131.329075539228,131.421797275338,131.514484251581,131.607161359868,
131.699853477369,131.792645539447,131.885490005879,131.97849021635,132.048237124056,
132.141489610871,132.234616088049,132.327643956439,132.420602734125,132.513525642518,
132.606437297571,132.699362299286,132.792382237166,132.885452744539,132.978671062894,
133.042160362488),.UNSPECIFIED.);
#1426=B_SPLINE_CURVE_WITH_KNOTS('',3,(#40322,#40323,#40324,#40325,#40326,
#40327,#40328,#40329,#40330,#40331,#40332,#40333,#40334,#40335,#40336,#40337,
#40338,#40339,#40340,#40341,#40342,#40343,#40344,#40345,#40346,#40347,#40348,
#40349,#40350,#40351,#40352,#40353,#40354,#40355,#40356,#40357,#40358,#40359,
#40360,#40361,#40362,#40363,#40364,#40365,#40366,#40367,#40368,#40369,#40370,
#40371,#40372,#40373,#40374,#40375,#40376,#40377,#40378,#40379,#40380,#40381,
#40382,#40383,#40384,#40385,#40386,#40387,#40388,#40389,#40390,#40391),
 .UNSPECIFIED.,.F.,.F.,(4,2,2,2,2,2,2,2,2,2,2,2,2,2,2,2,2,2,2,2,2,2,2,2,
2,2,2,2,2,2,2,2,2,2,4),(-4.06123088005783,-3.99915769086102,-3.99163726706931,
-3.9866691328777,-3.98189860315967,-3.97770198514831,-3.97246090317619,
-3.96429462822665,-3.91489664695743,-3.8740430317043,-3.82926394557993,
-3.82346359017865,-3.8204904331031,-3.81836400142996,-3.81565282686222,
-3.81097009832807,-3.79201981736089,-3.72967739114034,-3.69232097445996,
-3.67025118650308,-3.66342445538446,-3.65886388830599,-3.65461386369307,
-3.64905857058841,-3.63665255117785,-3.56678567827841,-3.52412808003807,
-3.51115468488872,-3.50239817690508,-3.49895195972588,-3.49653452214352,
-3.49428973781681,-3.49047539651302,-3.48002372339966,-3.39979696556878),
 .UNSPECIFIED.);
#1427=B_SPLINE_CURVE_WITH_KNOTS('',3,(#40393,#40394,#40395,#40396,#40397,
#40398,#40399,#40400,#40401,#40402,#40403,#40404,#40405,#40406,#40407,#40408,
#40409,#40410,#40411,#40412,#40413,#40414,#40415,#40416,#40417,#40418,#40419,
#40420,#40421,#40422,#40423,#40424,#40425,#40426,#40427,#40428,#40429,#40430,
#40431,#40432,#40433,#40434,#40435,#40436,#40437,#40438,#40439,#40440,#40441,
#40442,#40443,#40444,#40445,#40446,#40447,#40448,#40449,#40450,#40451,#40452,
#40453,#40454,#40455,#40456,#40457,#40458,#40459,#40460,#40461,#40462),
 .UNSPECIFIED.,.F.,.F.,(4,3,3,3,3,3,3,3,3,3,3,3,3,3,3,3,3,3,3,3,3,3,3,4),
(126.759257110528,126.852022037374,126.944782070836,127.037561992392,127.130443687958,
127.223382033601,127.316468841556,127.365911868133,127.459007116446,127.551976703792,
127.644848232775,127.737652323135,127.830421527947,127.923180644104,128.015954453555,
128.108827216787,128.201751960273,128.294830923321,128.363762709861,128.464552334364,
128.564983981233,128.665188037793,128.765060809243,128.805298796957),
 .UNSPECIFIED.);
#1428=B_SPLINE_CURVE_WITH_KNOTS('',3,(#40463,#40464,#40465,#40466,#40467,
#40468,#40469,#40470,#40471,#40472,#40473,#40474,#40475,#40476,#40477,#40478,
#40479,#40480,#40481,#40482,#40483,#40484,#40485,#40486,#40487,#40488,#40489,
#40490,#40491,#40492,#40493,#40494,#40495,#40496,#40497,#40498,#40499,#40500,
#40501,#40502,#40503,#40504,#40505,#40506,#40507,#40508,#40509,#40510,#40511,
#40512,#40513,#40514,#40515,#40516,#40517,#40518,#40519,#40520,#40521,#40522,
#40523,#40524,#40525,#40526,#40527,#40528,#40529,#40530,#40531,#40532,#40533,
#40534,#40535,#40536,#40537,#40538,#40539,#40540,#40541,#40542,#40543,#40544,
#40545,#40546,#40547,#40548,#40549,#40550,#40551,#40552,#40553,#40554,#40555,
#40556,#40557,#40558,#40559,#40560,#40561,#40562,#40563,#40564,#40565,#40566,
#40567,#40568,#40569,#40570,#40571,#40572,#40573,#40574,#40575,#40576,#40577,
#40578,#40579,#40580,#40581,#40582,#40583,#40584,#40585,#40586,#40587,#40588,
#40589,#40590,#40591,#40592,#40593,#40594,#40595,#40596,#40597,#40598,#40599,
#40600,#40601,#40602,#40603,#40604,#40605,#40606,#40607,#40608,#40609,#40610,
#40611,#40612,#40613,#40614,#40615,#40616),.UNSPECIFIED.,.F.,.F.,(4,2,2,
2,2,2,2,2,2,2,2,2,2,2,2,2,2,2,2,2,2,2,2,2,2,2,2,2,2,2,2,2,2,2,2,2,2,2,2,
2,2,2,2,2,2,2,2,2,2,2,2,2,2,2,2,2,2,2,2,2,2,2,2,2,2,2,2,2,2,2,2,2,2,2,2,
2,4),(1.36986813415593,1.41472412899457,1.42275371239178,1.42795815610329,
1.43215877399454,1.43697033725174,1.44532395773671,1.48475914832888,1.52808382678746,
1.57801766436043,1.58612816311396,1.58923460129861,1.59146233481792,1.59389580161617,
1.59742468867269,1.60672622206272,1.6207984267892,1.72155555163549,1.74101734255056,
1.74791649473522,1.75240742967011,1.75668758292653,1.76252803921264,1.77622949526211,
1.79534798025403,1.85118653392302,1.90046295084852,1.9085642526298,1.91166770971675,
1.91389316434396,1.91632694364819,1.91985632325798,1.92915698817388,1.94322649609053,
2.04392923303818,2.0634197220064,2.07032502908901,2.07481897653573,2.07910132519409,
2.08494378225342,2.09864589391576,2.11776428319321,2.17361744968784,2.2227639792405,
2.23086297872011,2.2339673672784,2.23619412675541,2.23862823951232,2.24215940538797,
2.25147388409074,2.26557238030009,2.36708984579862,2.3858867721409,2.39269421668486,
2.39671926778274,2.40087591432703,2.40630177308218,2.41229410913678,2.42230748761514,
2.47503917517413,2.5400265506722,2.55193121460002,2.55594425558728,2.55822838368599,
2.5606209119779,2.56392618471981,2.57181141164477,2.5830980277763,2.61673606462629,
2.68844376519829,2.70788382372786,2.71477326901278,2.71926253432093,2.72326380519083,
2.72743373181106,2.73269205327641,2.73843249748408),.UNSPECIFIED.);
#1429=B_SPLINE_CURVE_WITH_KNOTS('',3,(#40620,#40621,#40622,#40623,#40624,
#40625,#40626,#40627,#40628,#40629,#40630,#40631,#40632,#40633,#40634,#40635,
#40636,#40637,#40638,#40639,#40640,#40641,#40642,#40643,#40644,#40645,#40646,
#40647,#40648,#40649,#40650,#40651,#40652,#40653,#40654,#40655,#40656,#40657,
#40658,#40659,#40660,#40661,#40662,#40663,#40664,#40665,#40666,#40667,#40668,
#40669,#40670,#40671,#40672,#40673,#40674,#40675,#40676,#40677,#40678,#40679,
#40680,#40681,#40682,#40683,#40684,#40685,#40686,#40687,#40688,#40689,#40690,
#40691,#40692),.UNSPECIFIED.,.F.,.F.,(4,3,3,3,3,3,3,3,3,3,3,3,3,3,3,3,3,
3,3,3,3,3,3,3,4),(-4.09274904019424,-3.99140336690961,-3.90268063202685,
-3.81407250519492,-3.72555538516043,-3.63405502766315,-3.5456414745384,
-3.45724216684168,-3.36883591664657,-3.28040153632723,-3.19186974100238,
-3.10327972302285,-3.01456344360957,-2.99355252518221,-2.90585728432194,
-2.81827426436052,-2.73077877361514,-2.64334382474895,-2.55593995423922,
-2.46854499256392,-2.38113678182524,-2.29364202365736,-2.20610056041848,
-2.11842612027813,-2.06158267649742),.UNSPECIFIED.);
#1430=B_SPLINE_CURVE_WITH_KNOTS('',3,(#40696,#40697,#40698,#40699,#40700),
 .UNSPECIFIED.,.F.,.F.,(4,1,4),(0.,0.997850841727403,1.11004521091123),
 .UNSPECIFIED.);
#1431=B_SPLINE_CURVE_WITH_KNOTS('',3,(#40702,#40703,#40704,#40705,#40706,
#40707,#40708,#40709,#40710,#40711,#40712,#40713,#40714,#40715,#40716,#40717,
#40718,#40719,#40720,#40721,#40722,#40723,#40724,#40725,#40726,#40727,#40728,
#40729,#40730,#40731,#40732,#40733,#40734,#40735,#40736,#40737,#40738,#40739,
#40740,#40741,#40742,#40743,#40744,#40745,#40746,#40747,#40748,#40749,#40750,
#40751,#40752,#40753,#40754,#40755,#40756,#40757,#40758,#40759,#40760,#40761,
#40762,#40763,#40764,#40765,#40766,#40767,#40768,#40769,#40770,#40771,#40772,
#40773,#40774,#40775,#40776,#40777,#40778,#40779,#40780,#40781,#40782,#40783,
#40784,#40785,#40786,#40787,#40788,#40789,#40790,#40791,#40792,#40793,#40794,
#40795,#40796,#40797,#40798,#40799,#40800,#40801,#40802,#40803,#40804,#40805,
#40806,#40807,#40808,#40809,#40810,#40811,#40812,#40813,#40814,#40815,#40816,
#40817,#40818,#40819,#40820,#40821,#40822,#40823,#40824,#40825,#40826,#40827,
#40828,#40829,#40830,#40831,#40832,#40833,#40834,#40835,#40836,#40837,#40838,
#40839,#40840,#40841,#40842,#40843,#40844,#40845,#40846,#40847,#40848,#40849,
#40850,#40851,#40852,#40853,#40854,#40855,#40856,#40857,#40858,#40859,#40860,
#40861,#40862,#40863,#40864,#40865,#40866,#40867,#40868,#40869,#40870,#40871,
#40872,#40873,#40874,#40875,#40876,#40877,#40878,#40879,#40880,#40881,#40882,
#40883,#40884,#40885,#40886,#40887,#40888,#40889,#40890,#40891,#40892,#40893,
#40894,#40895,#40896,#40897,#40898,#40899,#40900,#40901,#40902,#40903,#40904,
#40905,#40906,#40907,#40908,#40909,#40910,#40911,#40912,#40913,#40914,#40915,
#40916,#40917,#40918,#40919,#40920,#40921,#40922,#40923,#40924,#40925,#40926,
#40927,#40928,#40929,#40930),.UNSPECIFIED.,.F.,.F.,(4,3,3,3,3,3,3,3,3,3,
3,3,3,3,3,3,3,3,3,3,3,3,3,3,3,3,3,3,3,3,3,3,3,3,3,3,3,3,3,3,3,3,3,3,3,3,
3,3,3,3,3,3,3,3,3,3,3,3,3,3,3,3,3,3,3,3,3,3,3,3,3,3,3,3,3,3,4),(1.11004521091123,
1.19681857962916,1.28348712019175,1.37251394059963,1.45905369666318,1.54557153490185,
1.63209020527474,1.72299307481976,1.80963167118428,1.89632823527782,1.98314923320001,
1.99570168345481,2.08428836921591,2.17275930675744,2.26113826477258,2.35269004732378,
2.44096386095791,2.52922308261749,2.61748904579692,2.70578308363948,2.79417514450019,
2.88262561661478,2.97120367664702,2.99355252518221,3.08226159218255,3.17085866821476,
3.25936734373045,3.35087184662785,3.43928348434477,3.52768329462181,3.61609246484359,
3.7045321838872,3.79307286406892,3.88167384880736,3.97040404053157,3.99140336690961,
4.07990226017908,4.16828588762427,4.25657812029096,4.34816263133422,4.43635174131991,
4.52452715507421,4.61271029903408,4.70092260011546,4.7892349478161,4.87760678960562,
4.96610841543857,4.98925420863701,5.07783461717695,5.1663006090823,5.25467595129453,
5.34622958867827,5.43450314168811,5.52276334774254,5.61103154350697,5.69932906623069,
5.78772645777222,5.8761833444269,5.96476936069165,5.98710505036441,6.07569171207561,
6.16416426366233,6.25254646262046,6.34409764130438,6.43237875249101,6.52064676413912,
6.60892300557215,6.69722880686894,6.78563478230987,6.87410044159731,6.96269544049623,
6.98495589209181,7.08702454854288,7.18451386528577,7.28173097504692,7.37854662647687,
7.3932305178961),.UNSPECIFIED.);
#1432=B_SPLINE_CURVE_WITH_KNOTS('',3,(#40932,#40933,#40934,#40935,#40936,
#40937,#40938,#40939,#40940,#40941,#40942,#40943,#40944,#40945,#40946,#40947,
#40948,#40949,#40950,#40951,#40952,#40953,#40954,#40955,#40956,#40957,#40958,
#40959,#40960,#40961,#40962,#40963,#40964,#40965,#40966,#40967,#40968,#40969,
#40970,#40971,#40972,#40973,#40974,#40975,#40976,#40977,#40978,#40979,#40980,
#40981,#40982,#40983,#40984,#40985,#40986,#40987,#40988,#40989,#40990,#40991,
#40992,#40993,#40994,#40995,#40996,#40997,#40998,#40999,#41000,#41001,#41002,
#41003,#41004,#41005,#41006,#41007,#41008,#41009,#41010,#41011,#41012,#41013,
#41014,#41015,#41016,#41017,#41018,#41019,#41020,#41021,#41022,#41023,#41024,
#41025,#41026,#41027,#41028,#41029,#41030,#41031,#41032,#41033,#41034,#41035,
#41036,#41037,#41038,#41039,#41040,#41041,#41042,#41043,#41044,#41045,#41046,
#41047,#41048,#41049,#41050,#41051,#41052,#41053,#41054,#41055,#41056,#41057,
#41058,#41059,#41060,#41061,#41062,#41063,#41064,#41065,#41066,#41067,#41068,
#41069,#41070,#41071,#41072,#41073,#41074,#41075,#41076,#41077,#41078,#41079,
#41080,#41081,#41082,#41083,#41084,#41085,#41086,#41087,#41088,#41089,#41090,
#41091,#41092,#41093,#41094,#41095,#41096,#41097,#41098,#41099,#41100,#41101,
#41102,#41103,#41104,#41105,#41106,#41107,#41108,#41109,#41110,#41111,#41112,
#41113,#41114,#41115,#41116,#41117,#41118,#41119,#41120,#41121,#41122,#41123,
#41124,#41125,#41126,#41127,#41128,#41129,#41130,#41131,#41132,#41133,#41134,
#41135,#41136,#41137,#41138,#41139,#41140,#41141,#41142,#41143,#41144,#41145,
#41146,#41147,#41148,#41149,#41150,#41151,#41152,#41153,#41154,#41155,#41156,
#41157),.UNSPECIFIED.,.F.,.F.,(4,3,3,3,3,3,3,3,3,3,3,3,3,3,3,3,3,3,3,3,
3,3,3,3,3,3,3,3,3,3,3,3,3,3,3,3,3,3,3,3,3,3,3,3,3,3,3,3,3,3,3,3,3,3,3,3,
3,3,3,3,3,3,3,3,3,3,3,3,3,3,3,3,3,3,3,4),(7.39323051809082,7.48288036686472,
7.57256220481202,7.66229492622905,7.75216069815711,7.84209994754193,7.9322010208113,
7.98280673381922,8.07138131775184,8.15984154810557,8.24821119867417,8.33976699578323,
8.42803507032422,8.51628988674049,8.60455278803785,8.69284511788348,8.7812374945029,
8.86968946404034,8.95827074499974,8.98065757554662,9.06923201113828,9.15769211569553,
9.24606166307021,9.33761750734569,9.42588553618497,9.51414032834517,9.60240322696447,
9.69069557585812,9.77908800384221,9.86754004367646,9.9561214222471,9.97850841727402,
10.067080560139,10.1555383329379,10.2439055125692,10.3354622308732,10.4237278170777,
10.5119801430473,10.6002405544998,10.688530397817,10.7769203054923,10.8653698133419,
10.9539486622742,10.9763592590014,11.0649326354006,11.1533916568987,11.2417600987877,
11.3333163490303,11.4215832232792,11.5098368446218,11.5980985573963,11.6863897066082,
11.7747809203645,11.8632317359969,11.951811885131,11.9742101007288,12.0627833654436,
12.1512422764058,12.2396106090393,12.3311669007164,12.4194336696461,12.5076871873168,
12.5959487981883,12.6842398473887,12.7726309644632,12.86108168524,12.9496617429377,
12.9720609424562,13.060105302808,13.1479581989514,13.2357263478001,13.3234317718887,
13.4116777852341,13.4993383649874,13.5878770951289,13.6764158252704),
 .UNSPECIFIED.);
#1433=B_SPLINE_CURVE_WITH_KNOTS('',3,(#41159,#41160,#41161,#41162,#41163,
#41164,#41165,#41166,#41167,#41168,#41169,#41170,#41171,#41172,#41173,#41174,
#41175,#41176,#41177,#41178,#41179,#41180,#41181,#41182,#41183,#41184,#41185,
#41186,#41187,#41188,#41189,#41190,#41191,#41192,#41193,#41194,#41195,#41196,
#41197,#41198,#41199,#41200,#41201,#41202,#41203,#41204,#41205,#41206,#41207,
#41208,#41209,#41210,#41211,#41212,#41213,#41214,#41215,#41216,#41217,#41218,
#41219,#41220,#41221,#41222,#41223,#41224,#41225,#41226,#41227,#41228,#41229,
#41230,#41231,#41232,#41233,#41234,#41235,#41236,#41237,#41238,#41239,#41240,
#41241,#41242,#41243,#41244,#41245,#41246,#41247,#41248,#41249,#41250,#41251,
#41252,#41253,#41254,#41255,#41256,#41257,#41258,#41259,#41260,#41261,#41262,
#41263,#41264,#41265,#41266,#41267,#41268,#41269,#41270,#41271,#41272,#41273,
#41274,#41275,#41276,#41277,#41278,#41279,#41280,#41281,#41282,#41283,#41284,
#41285,#41286,#41287,#41288,#41289,#41290,#41291,#41292,#41293,#41294,#41295,
#41296,#41297,#41298,#41299,#41300,#41301,#41302,#41303,#41304,#41305,#41306,
#41307,#41308,#41309,#41310,#41311,#41312,#41313,#41314,#41315,#41316,#41317,
#41318,#41319,#41320,#41321,#41322,#41323,#41324,#41325,#41326,#41327,#41328,
#41329,#41330,#41331,#41332,#41333,#41334,#41335,#41336,#41337,#41338,#41339,
#41340,#41341,#41342,#41343,#41344,#41345,#41346,#41347,#41348,#41349,#41350,
#41351,#41352,#41353,#41354,#41355,#41356,#41357,#41358,#41359,#41360,#41361,
#41362,#41363,#41364,#41365,#41366,#41367,#41368,#41369,#41370,#41371,#41372,
#41373,#41374,#41375,#41376,#41377,#41378,#41379,#41380,#41381,#41382,#41383,
#41384,#41385,#41386,#41387),.UNSPECIFIED.,.F.,.F.,(4,3,3,3,3,3,3,3,3,3,
3,3,3,3,3,3,3,3,3,3,3,3,3,3,3,3,3,3,3,3,3,3,3,3,3,3,3,3,3,3,3,3,3,3,3,3,
3,3,3,3,3,3,3,3,3,3,3,3,3,3,3,3,3,3,3,3,3,3,3,3,3,3,3,3,3,3,4),(13.6764158254185,
13.7833994164136,13.8918858024763,13.9699117841836,14.0584849658365,14.1469437914998,
14.2353120367115,14.3268683603615,14.4151350371095,14.5033884609907,14.5916499765596,
14.6799409290381,14.7683319477645,14.8567825691239,14.9453625265971,14.967762625911,
15.0563357846373,15.1447945873451,15.2331628096013,15.324719141856,15.4129857957979,
15.5012391969687,15.5895006899479,15.677791619983,15.7661826165984,15.8546332160138,
15.943213151958,15.9656134676384,16.0541866044928,16.1426453849034,16.2310135844665,
16.3225699250789,16.410836555482,16.4990899328407,16.5873514017595,16.6756423075101,
16.7640332796304,16.8524838543977,16.941063765659,16.9634643093658,17.0520374629929,
17.1404962604055,17.2288644771775,17.320420811417,17.4086874594366,17.4969408545324,
17.58520234129,17.6734932649627,17.7618842550379,17.8503348478012,17.9389147769802,
17.9613151510932,18.0498883010376,18.1383470947465,18.2267153077987,18.3182716434264,
18.4065382877099,18.49479167907,18.5830531620966,18.6713440820469,18.7597350684314,
18.8481856575184,18.9367655830698,18.9591659928206,19.0477391407883,19.1361979324781,
19.2245661434715,19.316122479856,19.4043891219944,19.4926425111812,19.5809039920083,
19.6691949097351,19.7575858938721,19.8460364806943,19.9346164039739,19.957016834548,
19.95960113245),.UNSPECIFIED.);
#1434=B_SPLINE_CURVE_WITH_KNOTS('',3,(#41389,#41390,#41391,#41392,#41393,
#41394,#41395,#41396,#41397,#41398,#41399,#41400,#41401,#41402,#41403,#41404,
#41405,#41406,#41407,#41408,#41409,#41410,#41411,#41412,#41413,#41414,#41415,
#41416,#41417,#41418,#41419,#41420,#41421,#41422,#41423,#41424,#41425,#41426,
#41427,#41428,#41429,#41430,#41431,#41432,#41433,#41434,#41435,#41436,#41437,
#41438,#41439,#41440,#41441,#41442,#41443,#41444,#41445,#41446,#41447,#41448,
#41449,#41450,#41451,#41452,#41453,#41454,#41455,#41456,#41457,#41458,#41459,
#41460,#41461,#41462,#41463,#41464,#41465,#41466,#41467,#41468,#41469,#41470,
#41471,#41472,#41473,#41474,#41475,#41476,#41477,#41478,#41479,#41480,#41481,
#41482,#41483,#41484,#41485,#41486,#41487,#41488,#41489,#41490,#41491,#41492,
#41493,#41494,#41495,#41496,#41497,#41498,#41499,#41500,#41501,#41502,#41503,
#41504,#41505,#41506,#41507,#41508,#41509,#41510,#41511,#41512,#41513,#41514,
#41515,#41516,#41517,#41518,#41519,#41520,#41521,#41522,#41523,#41524,#41525,
#41526,#41527,#41528,#41529,#41530,#41531,#41532,#41533,#41534,#41535,#41536,
#41537,#41538,#41539,#41540,#41541,#41542,#41543,#41544,#41545,#41546,#41547,
#41548,#41549,#41550,#41551,#41552,#41553,#41554,#41555,#41556,#41557,#41558,
#41559,#41560,#41561,#41562,#41563,#41564,#41565,#41566,#41567,#41568,#41569,
#41570,#41571,#41572,#41573,#41574,#41575,#41576,#41577,#41578,#41579,#41580,
#41581,#41582,#41583,#41584,#41585,#41586,#41587,#41588,#41589,#41590,#41591,
#41592,#41593,#41594,#41595,#41596,#41597,#41598,#41599,#41600,#41601,#41602,
#41603,#41604,#41605,#41606,#41607,#41608,#41609,#41610,#41611,#41612,#41613,
#41614),.UNSPECIFIED.,.F.,.F.,(4,3,3,3,3,3,3,3,3,3,3,3,3,3,3,3,3,3,3,3,
3,3,3,3,3,3,3,3,3,3,3,3,3,3,3,3,3,3,3,3,3,3,3,3,3,3,3,3,3,3,3,3,3,3,3,3,
3,3,3,3,3,3,3,3,3,3,3,3,3,3,3,3,3,3,3,4),(19.9596011325877,20.0481329717931,
20.1365504859385,20.2248775009963,20.3161262729062,20.404352141197,20.4925649061808,
20.5807859574653,20.6690366855045,20.7573874921075,20.8457982021158,20.9343376898428,
20.9548676762755,21.043440825605,21.1318996186796,21.2202678310788,21.3118241669443,
21.4000908105316,21.4883442011809,21.5766056834827,21.6648966026947,21.753287588325,
21.8417381766471,21.9303181014248,21.9527185180029,22.0412916671691,22.1297504600762,
22.2181186723037,22.3096750082321,22.3979416516396,22.4861950421065,22.574456524223,
22.6627474432473,22.7511384286871,22.839589016817,22.9281689414009,22.9505693597303,
23.0391425091049,23.1276013022237,23.2159695146662,23.3075258505151,23.3957924941428,
23.4840458848314,23.5723073671713,23.6605982864196,23.7489892720849,23.8374398604412,
23.926019785251,23.9484202014577,24.0369933507614,24.125452143808,24.2138203561779,
24.3053766920538,24.3936433356082,24.4818967262232,24.5701582084893,24.6584491276642,
24.7468401132559,24.8352907015382,24.9238706262749,24.9462710431851,25.0348441924774,
25.1233029855122,25.2116711978705,25.3032275337507,25.3914941772924,25.4797475678944,
25.5680090501472,25.6562999693086,25.7446909548863,25.8331415431545,25.9217214678769,
25.9441218849125,26.0521117084359,26.1587324100376,26.2427864394712),
 .UNSPECIFIED.);
#1435=B_SPLINE_CURVE_WITH_KNOTS('',3,(#41616,#41617,#41618,#41619,#41620,
#41621,#41622,#41623,#41624,#41625,#41626,#41627,#41628,#41629,#41630,#41631,
#41632,#41633,#41634,#41635,#41636,#41637,#41638,#41639,#41640,#41641,#41642,
#41643,#41644,#41645,#41646,#41647,#41648,#41649,#41650,#41651,#41652,#41653,
#41654,#41655,#41656,#41657,#41658,#41659,#41660,#41661,#41662,#41663,#41664,
#41665,#41666,#41667,#41668,#41669,#41670,#41671,#41672,#41673,#41674,#41675,
#41676,#41677,#41678,#41679,#41680,#41681,#41682,#41683,#41684,#41685,#41686,
#41687,#41688,#41689,#41690,#41691,#41692,#41693,#41694,#41695,#41696,#41697,
#41698,#41699,#41700,#41701,#41702,#41703,#41704,#41705,#41706,#41707,#41708,
#41709,#41710,#41711,#41712,#41713,#41714,#41715,#41716,#41717,#41718,#41719,
#41720,#41721,#41722,#41723,#41724,#41725,#41726,#41727,#41728,#41729,#41730,
#41731,#41732,#41733,#41734,#41735,#41736,#41737,#41738,#41739,#41740,#41741,
#41742,#41743,#41744,#41745,#41746,#41747,#41748,#41749,#41750,#41751,#41752,
#41753,#41754,#41755,#41756,#41757,#41758,#41759,#41760,#41761,#41762,#41763,
#41764,#41765,#41766,#41767,#41768,#41769,#41770,#41771,#41772,#41773,#41774,
#41775,#41776,#41777,#41778,#41779,#41780,#41781,#41782,#41783,#41784,#41785,
#41786,#41787,#41788,#41789,#41790,#41791,#41792,#41793,#41794,#41795,#41796,
#41797,#41798,#41799,#41800,#41801,#41802,#41803,#41804,#41805,#41806,#41807,
#41808,#41809,#41810,#41811,#41812,#41813,#41814,#41815,#41816,#41817,#41818,
#41819,#41820,#41821,#41822,#41823,#41824,#41825,#41826,#41827,#41828,#41829,
#41830,#41831,#41832,#41833,#41834,#41835,#41836,#41837,#41838,#41839,#41840,
#41841),.UNSPECIFIED.,.F.,.F.,(4,3,3,3,3,3,3,3,3,3,3,3,3,3,3,3,3,3,3,3,
3,3,3,3,3,3,3,3,3,3,3,3,3,3,3,3,3,3,3,3,3,3,3,3,3,3,3,3,3,3,3,3,3,3,3,3,
3,3,3,3,3,3,3,3,3,3,3,3,3,3,3,3,3,3,3,4),(26.2427864396296,26.3305471278199,
26.4182777501481,26.5060001655125,26.5937362218,26.6815653163576,26.7694406835887,
26.8574653064194,26.9419727266399,27.0305458759455,27.1190046689943,27.2073728813658,
27.298929217241,27.387195860797,27.4754492514135,27.5637107336809,27.6520016528573,
27.7403926384499,27.8288432267331,27.9174231514704,27.9398235683673,28.0283967176725,
28.1168555107208,28.2052237230921,28.2967800589675,28.3850467025228,28.4733000931386,
28.561561575405,28.6498524945803,28.7382434801722,28.826694068455,28.9152739931916,
28.9376744100947,29.0262475594023,29.114706352453,29.2030745648264,29.2946309007009,
29.3828975442588,29.4711509348772,29.5594124171467,29.6477033363247,29.7360943219193,
29.824544910205,29.9131248349443,29.9355252518221,30.0240984011285,30.1125571941781,
30.2009254065503,30.2924817424252,30.3807483859818,30.469001776599,30.5572632588673,
30.645554178044,30.7339451636374,30.8223957519215,30.9109756766594,30.9333760935495,
31.021949242856,31.1104080359057,31.1987762482784,31.2903325841532,31.37859922771,
31.4668526183273,31.5551141005953,31.6434050197721,31.7317960053654,31.8202465936495,
31.9088265183877,31.9312269352769,32.0211983969395,32.1110439823456,32.2007831067229,
32.2904186784366,32.3799933630522,32.4695266106531,32.5259717468092),
 .UNSPECIFIED.);
#1436=B_SPLINE_CURVE_WITH_KNOTS('',3,(#41843,#41844,#41845,#41846,#41847,
#41848,#41849,#41850,#41851,#41852,#41853,#41854,#41855,#41856,#41857,#41858,
#41859,#41860,#41861,#41862,#41863,#41864,#41865,#41866,#41867,#41868,#41869,
#41870,#41871,#41872,#41873,#41874,#41875,#41876,#41877,#41878,#41879,#41880,
#41881,#41882,#41883,#41884,#41885,#41886,#41887,#41888,#41889,#41890,#41891,
#41892,#41893,#41894,#41895,#41896,#41897,#41898,#41899,#41900,#41901,#41902,
#41903,#41904,#41905,#41906,#41907,#41908,#41909,#41910,#41911,#41912,#41913,
#41914,#41915,#41916,#41917,#41918,#41919,#41920,#41921,#41922,#41923,#41924,
#41925,#41926,#41927,#41928,#41929,#41930,#41931,#41932,#41933,#41934,#41935,
#41936,#41937,#41938,#41939,#41940,#41941,#41942,#41943,#41944,#41945,#41946,
#41947,#41948,#41949,#41950,#41951,#41952,#41953,#41954,#41955,#41956,#41957,
#41958,#41959,#41960,#41961,#41962,#41963,#41964,#41965,#41966,#41967,#41968,
#41969,#41970,#41971,#41972,#41973,#41974,#41975,#41976,#41977,#41978,#41979,
#41980,#41981,#41982,#41983,#41984,#41985,#41986,#41987,#41988,#41989,#41990,
#41991,#41992,#41993,#41994,#41995,#41996,#41997,#41998,#41999,#42000,#42001,
#42002,#42003,#42004,#42005,#42006,#42007,#42008,#42009,#42010,#42011,#42012,
#42013,#42014,#42015,#42016,#42017,#42018,#42019,#42020,#42021,#42022,#42023,
#42024,#42025,#42026,#42027,#42028,#42029,#42030,#42031,#42032,#42033,#42034,
#42035,#42036,#42037,#42038,#42039,#42040,#42041,#42042,#42043,#42044,#42045,
#42046,#42047,#42048,#42049,#42050,#42051,#42052,#42053,#42054,#42055,#42056,
#42057,#42058,#42059,#42060,#42061,#42062,#42063,#42064,#42065,#42066,#42067,
#42068),.UNSPECIFIED.,.F.,.F.,(4,3,3,3,3,3,3,3,3,3,3,3,3,3,3,3,3,3,3,3,
3,3,3,3,3,3,3,3,3,3,3,3,3,3,3,3,3,3,3,3,3,3,3,3,3,3,3,3,3,3,3,3,3,3,3,3,
3,3,3,3,3,3,3,3,3,3,3,3,3,3,3,3,3,3,3,4),(32.5259717470101,32.6267482545086,
32.7244046859025,32.8267412314534,32.9290777770043,33.0176509263108,33.1061097193606,
33.1944779317332,33.286034267608,33.3743009111648,33.462554301782,33.5508157840503,
33.6391067032275,33.727497688821,33.8159482771052,33.9045282018435,33.9269286187317,
34.0155017680383,34.103960561088,34.1923287734605,34.2838851093353,34.3721517528922,
34.4604051435095,34.5486666257778,34.636957544955,34.7253485305484,34.8137991188327,
34.9023790435709,34.9247794604591,35.0133526097657,35.1018114028155,35.1901796151881,
35.2817359510629,35.3700025946197,35.458255985237,35.5465174675054,35.6348083866826,
35.7231993722761,35.8116499605603,35.9002298852985,35.9226303021865,36.0112034514932,
36.0996622445429,36.1880304569156,36.2795867927904,36.3678534363472,36.4561068269646,
36.544368309233,36.6326592284102,36.7210502140037,36.809500802288,36.8980807270263,
36.9204811439139,37.0090542932204,37.0975130862701,37.1858812986425,37.2774376345174,
37.3657042780741,37.4539576686913,37.5422191509596,37.6305100701367,37.7189010557301,
37.8073516440141,37.8959315687522,37.9183319856413,38.0057567402234,38.0930680815749,
38.1825792030973,38.269738045413,38.3568657274577,38.4439846320742,38.5352777374942,
38.6224901904441,38.7097513439552,38.7971229178579,38.8091570537541),
 .UNSPECIFIED.);
#1437=B_SPLINE_CURVE_WITH_KNOTS('',3,(#42070,#42071,#42072,#42073,#42074,
#42075,#42076,#42077,#42078,#42079,#42080,#42081,#42082,#42083,#42084,#42085,
#42086,#42087,#42088,#42089,#42090,#42091,#42092,#42093,#42094,#42095,#42096,
#42097,#42098,#42099,#42100,#42101,#42102,#42103,#42104,#42105,#42106,#42107,
#42108,#42109,#42110,#42111,#42112,#42113,#42114,#42115,#42116,#42117,#42118,
#42119,#42120,#42121,#42122,#42123,#42124,#42125,#42126,#42127,#42128,#42129,
#42130,#42131,#42132,#42133,#42134,#42135,#42136,#42137,#42138,#42139,#42140,
#42141,#42142,#42143,#42144,#42145,#42146,#42147,#42148,#42149,#42150,#42151,
#42152,#42153,#42154,#42155,#42156,#42157,#42158,#42159,#42160,#42161,#42162,
#42163,#42164,#42165,#42166,#42167,#42168,#42169,#42170,#42171,#42172,#42173,
#42174,#42175,#42176,#42177,#42178,#42179,#42180,#42181,#42182,#42183,#42184,
#42185,#42186,#42187,#42188,#42189,#42190,#42191,#42192,#42193,#42194,#42195,
#42196,#42197,#42198,#42199,#42200,#42201,#42202,#42203,#42204,#42205,#42206,
#42207,#42208,#42209,#42210,#42211,#42212,#42213,#42214,#42215,#42216,#42217,
#42218,#42219,#42220,#42221,#42222,#42223,#42224,#42225,#42226,#42227,#42228,
#42229,#42230,#42231,#42232,#42233,#42234,#42235,#42236,#42237,#42238,#42239,
#42240,#42241,#42242,#42243,#42244,#42245,#42246,#42247,#42248,#42249,#42250,
#42251,#42252,#42253,#42254,#42255,#42256,#42257,#42258,#42259,#42260,#42261,
#42262,#42263,#42264,#42265,#42266,#42267,#42268,#42269,#42270,#42271,#42272,
#42273,#42274,#42275,#42276,#42277,#42278,#42279,#42280,#42281,#42282,#42283,
#42284,#42285,#42286,#42287,#42288,#42289,#42290,#42291,#42292,#42293,#42294,
#42295),.UNSPECIFIED.,.F.,.F.,(4,3,3,3,3,3,3,3,3,3,3,3,3,3,3,3,3,3,3,3,
3,3,3,3,3,3,3,3,3,3,3,3,3,3,3,3,3,3,3,3,3,3,3,3,3,3,3,3,3,3,3,3,3,3,3,3,
3,3,3,3,3,3,3,3,3,3,3,3,3,3,3,3,3,3,3,4),(38.8091570539888,38.9161828273687,
39.0047559766753,39.0932147697253,39.181582982098,39.2731393179728,39.3614059615296,
39.4496593521471,39.5379208344155,39.6262117535927,39.7146027391863,39.8030533274705,
39.8916332522088,39.9140336690961,40.0026068184029,40.0910656114527,40.1794338238255,
40.2709901597002,40.3592568032572,40.4475101938747,40.5357716761431,40.6240625953204,
40.712453580914,40.8009041691985,40.8894840939368,40.9118845108235,41.00045766013,
41.0889164531796,41.177284665552,41.2688410014269,41.3571076449836,41.4453610356008,
41.533622517869,41.6219134370461,41.7103044226395,41.7987550109236,41.8873349356617,
41.9097353525509,41.9983085018575,42.0867672949072,42.1751355072797,42.2666918431545,
42.3549584867113,42.4432118773286,42.5314733595969,42.6197642787741,42.7081552643675,
42.7966058526517,42.8851857773899,42.9075861942783,42.9961593435851,43.0846181366349,
43.1729863490076,43.2645426848824,43.3528093284394,43.4410627190568,43.5293242013252,
43.6176151205024,43.7060061060961,43.7944566943805,43.8830366191189,43.9054370360057,
43.9940101853122,44.0824689783619,44.1708371907343,44.2623935266091,44.3506601701658,
44.438913560783,44.5271750430515,44.6154659622283,44.7038569478217,44.7923075361057,
44.8808874608438,44.9032878777331,45.0337718756005,45.0923423611683),
 .UNSPECIFIED.);
#1438=B_SPLINE_CURVE_WITH_KNOTS('',3,(#42297,#42298,#42299,#42300,#42301,
#42302,#42303,#42304,#42305,#42306,#42307,#42308,#42309,#42310,#42311,#42312,
#42313,#42314,#42315,#42316,#42317,#42318,#42319,#42320,#42321,#42322,#42323,
#42324,#42325,#42326,#42327,#42328,#42329,#42330,#42331,#42332,#42333,#42334,
#42335,#42336,#42337,#42338,#42339,#42340,#42341,#42342,#42343,#42344,#42345,
#42346,#42347,#42348,#42349,#42350,#42351,#42352,#42353,#42354,#42355,#42356,
#42357,#42358,#42359,#42360,#42361,#42362,#42363,#42364,#42365,#42366,#42367,
#42368,#42369,#42370,#42371,#42372,#42373,#42374,#42375,#42376,#42377,#42378,
#42379,#42380,#42381,#42382,#42383,#42384,#42385,#42386,#42387,#42388,#42389,
#42390,#42391,#42392,#42393,#42394,#42395,#42396,#42397,#42398,#42399,#42400,
#42401,#42402,#42403,#42404,#42405,#42406,#42407,#42408,#42409,#42410,#42411,
#42412,#42413,#42414,#42415,#42416,#42417,#42418,#42419,#42420,#42421,#42422,
#42423,#42424,#42425,#42426,#42427,#42428,#42429,#42430,#42431,#42432,#42433,
#42434,#42435,#42436,#42437,#42438,#42439,#42440,#42441,#42442,#42443,#42444,
#42445,#42446,#42447,#42448,#42449,#42450,#42451,#42452,#42453,#42454,#42455,
#42456,#42457,#42458,#42459,#42460,#42461,#42462,#42463,#42464,#42465,#42466,
#42467,#42468,#42469,#42470,#42471,#42472,#42473,#42474,#42475,#42476,#42477,
#42478,#42479,#42480,#42481,#42482,#42483,#42484,#42485,#42486,#42487,#42488,
#42489,#42490,#42491,#42492,#42493,#42494,#42495,#42496,#42497,#42498,#42499,
#42500,#42501,#42502,#42503,#42504,#42505,#42506,#42507,#42508,#42509,#42510,
#42511,#42512,#42513,#42514,#42515,#42516,#42517,#42518,#42519,#42520,#42521,
#42522,#42523,#42524,#42525),.UNSPECIFIED.,.F.,.F.,(4,3,3,3,3,3,3,3,3,3,
3,3,3,3,3,3,3,3,3,3,3,3,3,3,3,3,3,3,3,3,3,3,3,3,3,3,3,3,3,3,3,3,3,3,3,3,
3,3,3,3,3,3,3,3,3,3,3,3,3,3,3,3,3,3,3,3,3,3,3,3,3,3,3,3,3,3,4),(45.0923423614058,
45.1794682863814,45.2696770905163,45.3566731775864,45.4436469087234,45.5306207667714,
45.6176172314561,45.7047067004475,45.7918517845714,45.8791228652891,45.9011387194605,
45.989711868767,46.0781706618167,46.1665388741891,46.258095210064,46.3463618536207,
46.434615244238,46.5228767265062,46.6111676456835,46.6995586312769,46.7880092195609,
46.8765891442992,46.8989895611879,46.9875627104945,47.0760215035442,47.164389715917,
47.2559460517918,47.3442126953487,47.432466085966,47.5207275682341,47.6090184874112,
47.6974094730047,47.785860061289,47.8744399860272,47.8968404029153,47.9854135522218,
48.0738723452715,48.162240557644,48.2537968935189,48.3420635370757,48.4303169276929,
48.5185784099612,48.6068693291381,48.6952603147317,48.7837109030158,48.8722908277539,
48.8946912446427,48.9832643939494,49.0717231869992,49.1600913993721,49.2516477352468,
49.3399143788038,49.4281677694212,49.5164292516896,49.6047201708667,49.6931111564602,
49.7815617447447,49.8701416694831,49.8925420863701,49.9811152356767,50.069574028726,
50.1579422410982,50.2494985769732,50.3377652205299,50.4260186111471,50.5142800934155,
50.6025710125928,50.6909619981861,50.7794125864703,50.8679925112085,50.8903929280975,
50.9841089426365,51.0819636240283,51.175258107441,51.2684075657143,51.3613757125319,
51.3755276682037),.UNSPECIFIED.);
#1439=B_SPLINE_CURVE_WITH_KNOTS('',3,(#42527,#42528,#42529,#42530,#42531,
#42532,#42533,#42534,#42535,#42536,#42537,#42538,#42539,#42540,#42541,#42542,
#42543,#42544,#42545,#42546,#42547,#42548,#42549,#42550,#42551,#42552,#42553,
#42554,#42555,#42556,#42557,#42558,#42559,#42560,#42561,#42562,#42563,#42564,
#42565,#42566,#42567,#42568,#42569,#42570,#42571,#42572,#42573,#42574,#42575,
#42576,#42577,#42578,#42579,#42580,#42581,#42582,#42583,#42584,#42585,#42586,
#42587,#42588,#42589,#42590,#42591,#42592,#42593,#42594,#42595,#42596,#42597,
#42598,#42599,#42600,#42601,#42602,#42603,#42604,#42605,#42606,#42607,#42608,
#42609,#42610,#42611,#42612,#42613,#42614,#42615,#42616,#42617,#42618,#42619,
#42620,#42621,#42622,#42623,#42624,#42625,#42626,#42627,#42628,#42629,#42630,
#42631,#42632,#42633,#42634,#42635,#42636,#42637,#42638,#42639,#42640,#42641,
#42642,#42643,#42644,#42645,#42646,#42647,#42648,#42649,#42650,#42651,#42652,
#42653,#42654,#42655,#42656,#42657,#42658,#42659,#42660,#42661,#42662,#42663,
#42664,#42665,#42666,#42667,#42668,#42669,#42670,#42671,#42672,#42673,#42674,
#42675,#42676,#42677,#42678,#42679,#42680,#42681,#42682,#42683,#42684,#42685,
#42686,#42687,#42688,#42689,#42690,#42691,#42692,#42693,#42694,#42695,#42696,
#42697,#42698,#42699,#42700,#42701,#42702,#42703,#42704,#42705,#42706,#42707,
#42708,#42709,#42710,#42711,#42712,#42713,#42714,#42715,#42716,#42717,#42718,
#42719,#42720,#42721,#42722,#42723,#42724,#42725,#42726,#42727,#42728,#42729,
#42730,#42731,#42732,#42733,#42734,#42735,#42736,#42737,#42738,#42739,#42740,
#42741,#42742,#42743,#42744,#42745,#42746,#42747,#42748,#42749,#42750,#42751,
#42752),.UNSPECIFIED.,.F.,.F.,(4,3,3,3,3,3,3,3,3,3,3,3,3,3,3,3,3,3,3,3,
3,3,3,3,3,3,3,3,3,3,3,3,3,3,3,3,3,3,3,3,3,3,3,3,3,3,3,3,3,3,3,3,3,3,3,3,
3,3,3,3,3,3,3,3,3,3,3,3,3,3,3,3,3,3,3,4),(51.3755276683479,51.4674551182633,
51.5594915131789,51.6517320877935,51.7440828937281,51.8366378040773,51.8882437698249,
51.9768169191314,52.065275712181,52.1536439245534,52.2452002604282,52.3334669039849,
52.421720294602,52.5099817768701,52.598272696047,52.6866636816403,52.7751142699245,
52.8636941946625,52.8860946115523,52.974667760859,53.063126553909,53.1514947662817,
53.2430511021564,53.3313177457134,53.4195711363307,53.5078326185991,53.5961235377762,
53.6845145233698,53.7729651116538,53.8615450363921,53.8839454532797,53.9725186025863,
54.0609773956361,54.1493456080088,54.2409019438836,54.3291685874404,54.4174219780577,
54.5056834603261,54.593974379503,54.6823653650966,54.7708159533807,54.8593958781189,
54.8817962950071,54.9703694443136,55.0588282373631,55.1471964497356,55.2387527856105,
55.3270194291673,55.4152728197845,55.5035343020528,55.5918252212297,55.680216206823,
55.7686667951072,55.8572467198455,55.8796471367346,55.9682202860413,56.0566790790914,
56.1450472914638,56.2366036273385,56.3248702708955,56.4131236615128,56.5013851437812,
56.5896760629585,56.6780670485522,56.7665176368358,56.855097561574,56.877497978462,
56.9648624461651,57.0520884991052,57.1392356291957,57.226326359989,57.3133831580095,
57.4004603167845,57.4875438192554,57.5747123789959,57.6587129753234),
 .UNSPECIFIED.);
#1440=B_SPLINE_CURVE_WITH_KNOTS('',3,(#42754,#42755,#42756,#42757,#42758,
#42759,#42760,#42761,#42762,#42763,#42764,#42765,#42766,#42767,#42768,#42769,
#42770,#42771,#42772,#42773,#42774,#42775,#42776,#42777,#42778,#42779,#42780,
#42781,#42782,#42783,#42784,#42785,#42786,#42787,#42788,#42789,#42790,#42791,
#42792,#42793,#42794,#42795,#42796,#42797,#42798,#42799,#42800,#42801,#42802,
#42803,#42804,#42805,#42806,#42807,#42808,#42809,#42810,#42811,#42812,#42813,
#42814,#42815,#42816,#42817,#42818,#42819,#42820,#42821,#42822,#42823,#42824,
#42825,#42826,#42827,#42828,#42829,#42830,#42831,#42832,#42833,#42834,#42835,
#42836,#42837,#42838,#42839,#42840,#42841,#42842,#42843,#42844,#42845,#42846,
#42847,#42848,#42849,#42850,#42851,#42852,#42853,#42854,#42855,#42856,#42857,
#42858,#42859,#42860,#42861,#42862,#42863,#42864,#42865,#42866,#42867,#42868,
#42869,#42870,#42871,#42872,#42873,#42874,#42875,#42876,#42877,#42878,#42879,
#42880,#42881,#42882,#42883,#42884,#42885,#42886,#42887,#42888,#42889,#42890,
#42891,#42892,#42893,#42894,#42895,#42896,#42897,#42898,#42899,#42900,#42901,
#42902,#42903,#42904,#42905,#42906,#42907,#42908,#42909,#42910,#42911,#42912,
#42913,#42914,#42915,#42916,#42917,#42918,#42919,#42920,#42921,#42922,#42923,
#42924,#42925,#42926,#42927,#42928,#42929,#42930,#42931,#42932,#42933,#42934,
#42935,#42936,#42937,#42938,#42939,#42940,#42941,#42942,#42943,#42944,#42945,
#42946,#42947,#42948,#42949,#42950,#42951,#42952,#42953,#42954,#42955,#42956,
#42957,#42958,#42959,#42960,#42961,#42962,#42963,#42964,#42965,#42966,#42967,
#42968,#42969,#42970,#42971,#42972,#42973,#42974,#42975,#42976,#42977,#42978,
#42979),.UNSPECIFIED.,.F.,.F.,(4,3,3,3,3,3,3,3,3,3,3,3,3,3,3,3,3,3,3,3,
3,3,3,3,3,3,3,3,3,3,3,3,3,3,3,3,3,3,3,3,3,3,3,3,3,3,3,3,3,3,3,3,3,3,3,3,
3,3,3,3,3,3,3,3,3,3,3,3,3,3,3,3,3,3,3,4),(57.6587129755275,57.7806561529807,
57.8753488201894,57.963921969496,58.0523807625458,58.1407489749183,58.2323053107931,
58.32057195435,58.4088253449673,58.4970868272357,58.585377746413,58.6737687320065,
58.7622193202907,58.8507992450289,58.8731996619168,58.9617728112232,59.0502316042727,
59.1385998166451,59.23015615252,59.3184227960766,59.4066761866937,59.4949376689618,
59.5832285881387,59.671619573732,59.7600701620161,59.8486500867541,59.8710505036442,
59.9596236529509,60.0480824460007,60.1364506583733,60.2280069942481,60.316273637805,
60.4045270284224,60.4927885106908,60.581079429868,60.6694704154616,60.7579210037459,
60.8465009284842,60.8689013453716,60.9574744946783,61.0459332877281,61.1343015001007,
61.2258578359755,61.3141244795324,61.4023778701499,61.4906393524183,61.5789302715955,
61.6673212571891,61.7557718454734,61.8443517702117,61.866752187099,61.9553253364055,
62.0437841294551,62.1321523418276,62.2237086777024,62.3119753212591,62.4002287118763,
62.4884901941445,62.5767811133215,62.6651720989148,62.7536226871989,62.842202611937,
62.8646030288264,62.953176178133,63.0416349711828,63.1300031835554,63.2215595194302,
63.3098261629871,63.3980795536044,63.4863410358728,63.57463195505,63.6630229406436,
63.7514735289279,63.8400534536661,63.8624538705538,63.9418982827071),
 .UNSPECIFIED.);
#1441=B_SPLINE_CURVE_WITH_KNOTS('',3,(#42981,#42982,#42983,#42984,#42985,
#42986,#42987,#42988,#42989,#42990,#42991,#42992,#42993,#42994,#42995,#42996,
#42997,#42998,#42999,#43000,#43001,#43002,#43003,#43004,#43005,#43006,#43007,
#43008,#43009,#43010,#43011,#43012,#43013,#43014,#43015,#43016,#43017,#43018,
#43019,#43020,#43021,#43022,#43023,#43024,#43025,#43026,#43027,#43028,#43029,
#43030,#43031,#43032,#43033,#43034,#43035,#43036,#43037,#43038,#43039,#43040,
#43041,#43042,#43043,#43044,#43045,#43046,#43047,#43048,#43049,#43050,#43051,
#43052,#43053,#43054,#43055,#43056,#43057,#43058,#43059,#43060,#43061,#43062,
#43063,#43064,#43065,#43066,#43067,#43068,#43069,#43070,#43071,#43072,#43073,
#43074,#43075,#43076,#43077,#43078,#43079,#43080,#43081,#43082,#43083,#43084,
#43085,#43086,#43087,#43088,#43089,#43090,#43091,#43092,#43093,#43094,#43095,
#43096,#43097,#43098,#43099,#43100,#43101,#43102,#43103,#43104,#43105,#43106,
#43107,#43108,#43109,#43110,#43111,#43112,#43113,#43114,#43115,#43116,#43117,
#43118,#43119,#43120,#43121,#43122,#43123,#43124,#43125,#43126,#43127,#43128,
#43129,#43130,#43131,#43132,#43133,#43134,#43135,#43136,#43137,#43138,#43139,
#43140,#43141,#43142,#43143,#43144,#43145,#43146,#43147,#43148,#43149,#43150,
#43151,#43152,#43153,#43154,#43155,#43156,#43157,#43158,#43159,#43160,#43161,
#43162,#43163,#43164,#43165,#43166,#43167,#43168,#43169,#43170,#43171,#43172,
#43173,#43174,#43175,#43176,#43177,#43178,#43179,#43180,#43181,#43182,#43183,
#43184,#43185,#43186,#43187,#43188,#43189,#43190,#43191,#43192,#43193,#43194,
#43195,#43196,#43197,#43198,#43199,#43200,#43201,#43202,#43203,#43204,#43205,
#43206),.UNSPECIFIED.,.F.,.F.,(4,3,3,3,3,3,3,3,3,3,3,3,3,3,3,3,3,3,3,3,
3,3,3,3,3,3,3,3,3,3,3,3,3,3,3,3,3,3,3,3,3,3,3,3,3,3,3,3,3,3,3,3,3,3,3,3,
3,3,3,3,3,3,3,3,3,3,3,3,3,3,3,3,3,3,3,4),(63.9418982829247,64.0294781425003,
64.1169515893512,64.2043433733613,64.2916830535804,64.3789971694347,64.4663079591173,
64.5536376539925,64.6410595742652,64.7285333074612,64.816140164755,64.8603047122812,
64.9488778615877,65.0373366546372,65.1257048670097,65.2172612028846,65.3055278464413,
65.3937812370584,65.4820427193266,65.5703336385034,65.6587246240968,65.747175212381,
65.8357551371191,65.8581555540086,65.9467287033153,66.0351874963652,66.1235557087377,
66.2151120446125,66.3033786881694,66.3916320787869,66.4798935610554,66.5681844802327,
66.6565754658264,66.7450260541106,66.8336059788487,66.856006395736,66.9445795450427,
67.0330383380923,67.1214065504652,67.21296288634,67.3012295298969,67.3894829205143,
67.4777444027824,67.5660353219593,67.6544263075529,67.7428768958373,67.8314568205756,
67.8538572374634,67.9424303867701,68.0308891798198,68.1192573921924,68.2108137280672,
68.299080371624,68.3873337622413,68.4755952445098,68.5638861636865,68.65227714928,
68.740727737564,68.8293076623022,68.8517080791908,68.9402812284974,69.0287400215473,
69.1171082339198,69.2086645697946,69.2969312133513,69.3851846039687,69.4734460862368,
69.5617370054135,69.6501279910071,69.7385785792912,69.8271585040295,69.8495589209182,
69.9496992033075,70.0495090652108,70.1487062366456,70.2250835896641),
 .UNSPECIFIED.);
#1442=B_SPLINE_CURVE_WITH_KNOTS('',3,(#43208,#43209,#43210,#43211,#43212,
#43213,#43214,#43215,#43216,#43217,#43218,#43219,#43220,#43221,#43222,#43223,
#43224,#43225,#43226,#43227,#43228,#43229,#43230,#43231,#43232,#43233,#43234,
#43235,#43236,#43237,#43238,#43239,#43240,#43241,#43242,#43243,#43244,#43245,
#43246,#43247,#43248,#43249,#43250,#43251,#43252,#43253,#43254,#43255,#43256,
#43257,#43258,#43259,#43260,#43261,#43262,#43263,#43264,#43265,#43266,#43267,
#43268,#43269,#43270,#43271,#43272,#43273,#43274,#43275,#43276,#43277,#43278,
#43279,#43280,#43281,#43282,#43283,#43284,#43285,#43286,#43287,#43288,#43289,
#43290,#43291,#43292,#43293,#43294,#43295,#43296,#43297,#43298,#43299,#43300,
#43301,#43302,#43303,#43304,#43305,#43306,#43307,#43308,#43309,#43310,#43311,
#43312,#43313,#43314,#43315,#43316,#43317,#43318,#43319,#43320,#43321,#43322,
#43323,#43324,#43325,#43326,#43327,#43328,#43329,#43330,#43331,#43332,#43333,
#43334,#43335,#43336,#43337,#43338,#43339,#43340,#43341,#43342,#43343,#43344,
#43345,#43346,#43347,#43348,#43349,#43350,#43351,#43352,#43353,#43354,#43355,
#43356,#43357,#43358,#43359,#43360,#43361,#43362,#43363,#43364,#43365,#43366,
#43367,#43368,#43369,#43370,#43371,#43372,#43373,#43374,#43375,#43376,#43377,
#43378,#43379,#43380,#43381,#43382,#43383,#43384,#43385,#43386,#43387,#43388,
#43389,#43390,#43391,#43392,#43393,#43394,#43395,#43396,#43397,#43398,#43399,
#43400,#43401,#43402,#43403,#43404,#43405,#43406,#43407,#43408,#43409,#43410,
#43411,#43412,#43413,#43414,#43415,#43416,#43417,#43418,#43419,#43420,#43421,
#43422,#43423,#43424,#43425,#43426,#43427,#43428,#43429,#43430,#43431,#43432,
#43433),.UNSPECIFIED.,.F.,.F.,(4,3,3,3,3,3,3,3,3,3,3,3,3,3,3,3,3,3,3,3,
3,3,3,3,3,3,3,3,3,3,3,3,3,3,3,3,3,3,3,3,3,3,3,3,3,3,3,3,3,3,3,3,3,3,3,3,
3,3,3,3,3,3,3,3,3,3,3,3,3,3,3,3,3,3,3,4),(70.2250835898867,70.3140257139893,
70.4029773741118,70.4919588141696,70.5810544107307,70.6702073895624,70.7595248544884,
70.8474097626456,70.9359829119522,71.0244417050017,71.1128099173742,71.2043662532491,
71.2926328968058,71.380886287423,71.4691477696913,71.5574386888683,71.6458296744617,
71.734280262746,71.8228601874841,71.845260604373,71.9338337536797,72.0222925467294,
72.1106607591019,72.2022170949767,72.2904837385336,72.378737129151,72.4669986114194,
72.5552895305965,72.6436805161901,72.7321311044744,72.8207110292126,72.8431114461004,
72.931684595407,73.0201433884568,73.1085116008291,73.2000679367039,73.2883345802607,
73.3765879708781,73.4648494531464,73.5531403723234,73.6415313579169,73.7299819462011,
73.8185618709393,73.8409622878278,73.9295354371343,74.0179942301839,74.1063624425564,
74.1979187784313,74.2861854219881,74.3744388126054,74.4627002948738,74.550991214051,
74.6393821996444,74.7278327879286,74.8164127126668,74.8388131295552,74.9273862788618,
75.0158450719114,75.1042132842842,75.195769620159,75.2840362637158,75.3722896543332,
75.4605511366013,75.5488420557784,75.6372330413719,75.7256836296563,75.8142635543946,
75.8366639712826,75.9250774885633,76.0133803059622,76.1015940720834,76.1897403602781,
76.2778480053841,76.3659320489736,76.4540370202493,76.5082688970663),
 .UNSPECIFIED.);
#1443=B_SPLINE_CURVE_WITH_KNOTS('',3,(#43435,#43436,#43437,#43438,#43439,
#43440,#43441,#43442,#43443,#43444,#43445,#43446,#43447,#43448,#43449,#43450,
#43451,#43452,#43453,#43454,#43455,#43456,#43457,#43458,#43459,#43460,#43461,
#43462,#43463,#43464,#43465,#43466,#43467,#43468,#43469,#43470,#43471,#43472,
#43473,#43474,#43475,#43476,#43477,#43478,#43479,#43480,#43481,#43482,#43483,
#43484,#43485,#43486,#43487,#43488,#43489,#43490,#43491,#43492,#43493,#43494,
#43495,#43496,#43497,#43498,#43499,#43500,#43501,#43502,#43503,#43504,#43505,
#43506,#43507,#43508,#43509,#43510,#43511,#43512,#43513,#43514,#43515,#43516,
#43517,#43518,#43519,#43520,#43521,#43522,#43523,#43524,#43525,#43526,#43527,
#43528,#43529,#43530,#43531,#43532,#43533,#43534,#43535,#43536,#43537,#43538,
#43539,#43540,#43541,#43542,#43543,#43544,#43545,#43546,#43547,#43548,#43549,
#43550,#43551,#43552,#43553,#43554,#43555,#43556,#43557,#43558,#43559,#43560,
#43561,#43562,#43563,#43564,#43565,#43566,#43567,#43568,#43569,#43570,#43571,
#43572,#43573,#43574,#43575,#43576,#43577,#43578,#43579,#43580,#43581,#43582,
#43583,#43584,#43585,#43586,#43587,#43588,#43589,#43590,#43591,#43592,#43593,
#43594,#43595,#43596,#43597,#43598,#43599,#43600,#43601,#43602,#43603,#43604,
#43605,#43606,#43607,#43608,#43609,#43610,#43611,#43612,#43613,#43614,#43615,
#43616,#43617,#43618,#43619,#43620,#43621,#43622,#43623,#43624,#43625,#43626,
#43627,#43628,#43629,#43630,#43631,#43632,#43633,#43634,#43635,#43636,#43637,
#43638,#43639,#43640,#43641,#43642,#43643,#43644,#43645,#43646,#43647,#43648,
#43649,#43650,#43651,#43652,#43653,#43654,#43655,#43656,#43657,#43658,#43659,
#43660),.UNSPECIFIED.,.F.,.F.,(4,3,3,3,3,3,3,3,3,3,3,3,3,3,3,3,3,3,3,3,
3,3,3,3,3,3,3,3,3,3,3,3,3,3,3,3,3,3,3,3,3,3,3,3,3,3,3,3,3,3,3,3,3,3,3,3,
3,3,3,3,3,3,3,3,3,3,3,3,3,3,3,3,3,3,3,4),(76.5082688972673,76.6116784352087,
76.7157763021011,76.8206168958636,76.83451481301,76.9230879623167,77.0115467553667,
77.0999149677394,77.1914713036142,77.2797379471712,77.3679913377887,77.4562528200573,
77.5445437392345,77.6329347248282,77.7213853131125,77.8099652378508,77.8323656547374,
77.9209388040438,78.0093975970933,78.0977658094656,78.1893221453405,78.2775887888971,
78.3658421795142,78.4541036617823,78.5423945809592,78.6307855665524,78.7192361548364,
78.8078160795743,78.8302164964648,78.9187896457715,79.0072484388213,79.095616651194,
79.1871729870687,79.2754396306256,79.3636930212431,79.4519545035115,79.5402454226887,
79.6286364082823,79.7170869965666,79.8056669213049,79.8280673381922,79.9166404874989,
80.0050992805487,80.0934674929213,80.1850238287961,80.273290472353,80.3615438629704,
80.4498053452388,80.5380962644162,80.6264872500097,80.714937838294,80.8035177630323,
80.8259181799196,80.9144913292261,81.0029501222757,81.0913183346482,81.182874670523,
81.2711413140798,81.359394704697,81.4476561869652,81.5359471061422,81.6243380917357,
81.7127886800199,81.801368604758,81.823769021647,81.9119038818887,81.9999246913006,
82.0878557266216,82.1758055362963,82.2636390313494,82.3514605650463,82.4392919270503,
82.5273324962926,82.6152945515581,82.7034023713968,82.7914542040193),
 .UNSPECIFIED.);
#1444=B_SPLINE_CURVE_WITH_KNOTS('',3,(#43662,#43663,#43664,#43665,#43666,
#43667,#43668,#43669,#43670,#43671,#43672,#43673,#43674,#43675,#43676,#43677,
#43678,#43679,#43680,#43681,#43682,#43683,#43684,#43685,#43686,#43687,#43688,
#43689,#43690,#43691,#43692,#43693,#43694,#43695,#43696,#43697,#43698,#43699,
#43700,#43701,#43702,#43703,#43704,#43705,#43706,#43707,#43708,#43709,#43710,
#43711,#43712,#43713,#43714,#43715,#43716,#43717,#43718,#43719,#43720,#43721,
#43722,#43723,#43724,#43725,#43726,#43727,#43728,#43729,#43730,#43731,#43732,
#43733,#43734,#43735,#43736,#43737,#43738,#43739,#43740,#43741,#43742,#43743,
#43744,#43745,#43746,#43747,#43748,#43749,#43750,#43751,#43752,#43753,#43754,
#43755,#43756,#43757,#43758,#43759,#43760,#43761,#43762,#43763,#43764,#43765,
#43766,#43767,#43768,#43769,#43770,#43771,#43772,#43773,#43774,#43775,#43776,
#43777,#43778,#43779,#43780,#43781,#43782,#43783,#43784,#43785,#43786,#43787,
#43788,#43789,#43790,#43791,#43792,#43793,#43794,#43795,#43796,#43797,#43798,
#43799,#43800,#43801,#43802,#43803,#43804,#43805,#43806,#43807,#43808,#43809,
#43810,#43811,#43812,#43813,#43814,#43815,#43816,#43817,#43818,#43819,#43820,
#43821,#43822,#43823,#43824,#43825,#43826,#43827,#43828,#43829,#43830,#43831,
#43832,#43833,#43834,#43835,#43836,#43837,#43838,#43839,#43840,#43841,#43842,
#43843,#43844,#43845,#43846,#43847,#43848,#43849,#43850,#43851,#43852,#43853,
#43854,#43855,#43856,#43857,#43858,#43859,#43860,#43861,#43862,#43863,#43864,
#43865,#43866,#43867,#43868,#43869,#43870,#43871,#43872,#43873,#43874,#43875,
#43876,#43877,#43878,#43879,#43880,#43881,#43882,#43883,#43884,#43885,#43886,
#43887,#43888,#43889,#43890),.UNSPECIFIED.,.F.,.F.,(4,3,3,3,3,3,3,3,3,3,
3,3,3,3,3,3,3,3,3,3,3,3,3,3,3,3,3,3,3,3,3,3,3,3,3,3,3,3,3,3,3,3,3,3,3,3,
3,3,3,3,3,3,3,3,3,3,3,3,3,3,3,3,3,3,3,3,3,3,3,3,3,3,3,3,3,3,4),(82.7914542042459,
82.8216198633744,82.910193012681,82.9986518057306,83.0870200181033,83.1785763539781,
83.2668429975349,83.3550963881522,83.4433578704206,83.5316487895977,83.6200397751912,
83.7084903634754,83.7970702882137,83.8194707051018,83.9080438544085,83.9965026474585,
84.0848708598313,84.1764271957061,84.2646938392631,84.3529472298806,84.4412087121492,
84.5294996313266,84.6178906169202,84.7063412052046,84.794921129943,84.8173215468292,
84.9058946961358,84.9943534891854,85.082721701558,85.1742780374328,85.2625446809896,
85.3507980716068,85.4390595538751,85.5273504730522,85.6157414586456,85.7041920469298,
85.792771971668,85.8151723885566,85.9037455378633,85.9922043309131,86.0805725432857,
86.1721288791605,86.2603955227174,86.3486489133348,86.4369103956032,86.5252013147804,
86.613592300374,86.7020428886583,86.7906228133966,86.813023230284,86.9015963795905,
86.9900551726401,87.0784233850126,87.1699797208875,87.2582463644442,87.3464997550614,
87.4347612373296,87.5230521565066,87.6114431421,87.699893730384,87.7884736551221,
87.8108740720114,87.8994472213181,87.9879060143678,88.0762742267405,88.1678305626153,
88.2560972061722,88.3443505967895,88.4326120790578,88.5209029982349,88.6092939838285,
88.6977445721128,88.7863244968511,88.8087249137388,88.9216441128936,89.0325337049006,
89.0746395112596),.UNSPECIFIED.);
#1445=B_SPLINE_CURVE_WITH_KNOTS('',3,(#43892,#43893,#43894,#43895,#43896,
#43897,#43898,#43899,#43900,#43901,#43902,#43903,#43904,#43905,#43906,#43907,
#43908,#43909,#43910,#43911,#43912,#43913,#43914,#43915,#43916,#43917,#43918,
#43919,#43920,#43921,#43922,#43923,#43924,#43925,#43926,#43927,#43928,#43929,
#43930,#43931,#43932,#43933,#43934,#43935,#43936,#43937,#43938,#43939,#43940,
#43941,#43942,#43943,#43944,#43945,#43946,#43947,#43948,#43949,#43950,#43951,
#43952,#43953,#43954,#43955,#43956,#43957,#43958,#43959,#43960,#43961,#43962,
#43963,#43964,#43965,#43966,#43967,#43968,#43969,#43970,#43971,#43972,#43973,
#43974,#43975,#43976,#43977,#43978,#43979,#43980,#43981,#43982,#43983,#43984,
#43985,#43986,#43987,#43988,#43989,#43990,#43991,#43992,#43993,#43994,#43995,
#43996,#43997,#43998,#43999,#44000,#44001,#44002,#44003,#44004,#44005,#44006,
#44007,#44008,#44009,#44010,#44011,#44012,#44013,#44014,#44015,#44016,#44017,
#44018,#44019,#44020,#44021,#44022,#44023,#44024,#44025,#44026,#44027,#44028,
#44029,#44030,#44031,#44032,#44033,#44034,#44035,#44036,#44037,#44038,#44039,
#44040,#44041,#44042,#44043,#44044,#44045,#44046,#44047,#44048,#44049,#44050,
#44051,#44052,#44053,#44054,#44055,#44056,#44057,#44058,#44059,#44060,#44061,
#44062,#44063,#44064,#44065,#44066,#44067,#44068,#44069,#44070,#44071,#44072,
#44073,#44074,#44075,#44076,#44077,#44078,#44079,#44080,#44081,#44082,#44083,
#44084,#44085,#44086,#44087,#44088,#44089,#44090,#44091,#44092,#44093,#44094,
#44095,#44096,#44097,#44098,#44099,#44100,#44101,#44102,#44103,#44104,#44105,
#44106,#44107,#44108,#44109,#44110,#44111,#44112,#44113,#44114,#44115,#44116,
#44117,#44118,#44119,#44120),.UNSPECIFIED.,.F.,.F.,(4,3,3,3,3,3,3,3,3,3,
3,3,3,3,3,3,3,3,3,3,3,3,3,3,3,3,3,3,3,3,3,3,3,3,3,3,3,3,3,3,3,3,3,3,3,3,
3,3,3,3,3,3,3,3,3,3,3,3,3,3,3,3,3,3,3,3,3,3,3,3,3,3,3,3,3,3,4),(89.0746395114255,
89.1661315419306,89.2535335418103,89.3409155597642,89.4282997621432,89.5157083129216,
89.6032130314673,89.6907742923472,89.7784657067371,89.8065757554662,89.895148904773,
89.9836076978229,90.0719759101956,90.1635322460703,90.2517988896274,90.3400522802448,
90.428313762513,90.5166046816903,90.604995667284,90.6934462555685,90.7820261803069,
90.8044265971937,90.8929997465002,90.9814585395498,91.0698267519223,91.1613830877972,
91.249649731354,91.3379031219712,91.4261646042394,91.5144555234168,91.6028465090102,
91.6912970972945,91.7798770220327,91.8022774389211,91.8908505882277,91.9793093812776,
92.0676775936504,92.1592339295251,92.247500573082,92.3357539636995,92.4240154459681,
92.5123063651456,92.6006973507392,92.6891479390233,92.7777278637613,92.8001282806484,
92.8887014299549,92.9771602230045,93.0655284353775,93.1570847712523,93.2453514148092,
93.3336048054265,93.4218662876948,93.5101572068716,93.5985481924652,93.6869987807492,
93.7755787054873,93.7979791223758,93.8865522716825,93.9750110647324,94.0633792771048,
94.1549356129796,94.2432022565365,94.3314556471538,94.4197171294219,94.5080080485987,
94.5963990341921,94.6848496224764,94.7734295472146,94.7958299641032,94.8867065999349,
94.9774468352194,95.0725413310658,95.1630320672434,95.2534488825731,95.3437980500459,
95.3578248186051),.UNSPECIFIED.);
#1446=B_SPLINE_CURVE_WITH_KNOTS('',3,(#44122,#44123,#44124,#44125,#44126,
#44127,#44128,#44129,#44130,#44131,#44132,#44133,#44134,#44135,#44136,#44137,
#44138,#44139,#44140,#44141,#44142,#44143,#44144,#44145,#44146,#44147,#44148,
#44149,#44150,#44151,#44152,#44153,#44154,#44155,#44156,#44157,#44158,#44159,
#44160,#44161,#44162,#44163,#44164,#44165,#44166,#44167,#44168,#44169,#44170,
#44171,#44172,#44173,#44174,#44175,#44176,#44177,#44178,#44179,#44180,#44181,
#44182,#44183,#44184,#44185,#44186,#44187,#44188,#44189,#44190,#44191,#44192,
#44193,#44194,#44195,#44196,#44197,#44198,#44199,#44200,#44201,#44202,#44203,
#44204,#44205,#44206,#44207,#44208,#44209,#44210,#44211,#44212,#44213,#44214,
#44215,#44216,#44217,#44218,#44219,#44220,#44221,#44222,#44223,#44224,#44225,
#44226,#44227,#44228,#44229,#44230,#44231,#44232,#44233,#44234,#44235,#44236,
#44237,#44238,#44239,#44240,#44241,#44242,#44243,#44244,#44245,#44246,#44247,
#44248,#44249,#44250,#44251,#44252,#44253,#44254,#44255,#44256,#44257,#44258,
#44259,#44260,#44261,#44262,#44263,#44264,#44265,#44266,#44267,#44268,#44269,
#44270,#44271,#44272,#44273,#44274,#44275,#44276,#44277,#44278,#44279,#44280,
#44281,#44282,#44283,#44284,#44285,#44286,#44287,#44288,#44289,#44290,#44291,
#44292,#44293,#44294,#44295,#44296,#44297,#44298,#44299,#44300,#44301,#44302,
#44303,#44304,#44305,#44306,#44307,#44308,#44309,#44310,#44311,#44312,#44313,
#44314,#44315,#44316,#44317,#44318,#44319,#44320,#44321,#44322,#44323,#44324,
#44325,#44326,#44327,#44328,#44329,#44330,#44331,#44332,#44333,#44334,#44335,
#44336,#44337,#44338,#44339,#44340,#44341,#44342,#44343,#44344,#44345,#44346,
#44347),.UNSPECIFIED.,.F.,.F.,(4,3,3,3,3,3,3,3,3,3,3,3,3,3,3,3,3,3,3,3,
3,3,3,3,3,3,3,3,3,3,3,3,3,3,3,3,3,3,3,3,3,3,3,3,3,3,3,3,3,3,3,3,3,3,3,3,
3,3,3,3,3,3,3,3,3,3,3,3,3,3,3,3,3,3,3,4),(95.3578248187554,95.4530925370813,
95.5487521534953,95.6446140067219,95.7407816715538,95.7936808058306,95.8822539551371,
95.9707127481868,96.0590809605592,96.1506372964341,96.2389039399908,96.3271573306081,
96.4154188128763,96.5037097320534,96.5921007176468,96.680551305931,96.7691312306691,
96.791531647558,96.8801047968644,96.968563589914,97.0569318022864,97.1484881381613,
97.2367547817179,97.325008172335,97.4132696546032,97.5015605737801,97.5899515593734,
97.6784021476575,97.7669820723955,97.7893824892855,97.8779556385931,97.9664144316439,
98.0547826440175,98.1463389798919,98.2346056234498,98.3228590140681,98.4111204963375,
98.4994114155156,98.5878024011101,98.6762529893954,98.7648329141346,98.7872333310129,
98.8758064803179,98.9642652733661,99.0526334857372,99.1441898216126,99.2324564651679,
99.3207098557838,99.4089713380506,99.4972622572263,99.5856532428184,99.6741038311011,
99.762683755838,99.7850841727403,99.8736573220461,99.962116115095,100.050484327467,
100.142040663342,100.230307306898,100.318560697514,100.406822179782,100.495113098958,
100.58350408455,100.671954672834,100.760534597571,100.782935014468,100.870225958326,
100.957403438561,101.044482974272,101.131508277622,101.218501858615,101.305486194025,
101.392527562315,101.479596613056,101.566780277413,101.641010125573),
 .UNSPECIFIED.);
#1447=B_SPLINE_CURVE_WITH_KNOTS('',3,(#44349,#44350,#44351,#44352,#44353,
#44354,#44355,#44356,#44357,#44358,#44359,#44360,#44361,#44362,#44363,#44364,
#44365,#44366,#44367,#44368,#44369,#44370,#44371,#44372,#44373,#44374,#44375,
#44376,#44377,#44378,#44379,#44380,#44381,#44382,#44383,#44384,#44385,#44386,
#44387,#44388,#44389,#44390,#44391,#44392,#44393,#44394,#44395,#44396,#44397,
#44398,#44399,#44400,#44401,#44402,#44403,#44404,#44405,#44406,#44407,#44408,
#44409,#44410,#44411,#44412,#44413,#44414,#44415,#44416,#44417,#44418,#44419,
#44420,#44421,#44422,#44423,#44424,#44425,#44426,#44427,#44428,#44429,#44430,
#44431,#44432,#44433,#44434,#44435,#44436,#44437,#44438,#44439,#44440,#44441,
#44442,#44443,#44444,#44445,#44446,#44447,#44448,#44449,#44450,#44451,#44452,
#44453,#44454,#44455,#44456,#44457,#44458,#44459,#44460,#44461,#44462,#44463,
#44464,#44465,#44466,#44467,#44468,#44469,#44470,#44471,#44472,#44473,#44474,
#44475,#44476,#44477,#44478,#44479,#44480,#44481,#44482,#44483,#44484,#44485,
#44486,#44487,#44488,#44489,#44490,#44491,#44492,#44493,#44494,#44495,#44496,
#44497,#44498,#44499,#44500,#44501,#44502,#44503,#44504,#44505,#44506,#44507,
#44508,#44509,#44510,#44511,#44512,#44513,#44514,#44515,#44516,#44517,#44518,
#44519,#44520,#44521,#44522,#44523,#44524,#44525,#44526,#44527,#44528,#44529,
#44530,#44531,#44532,#44533,#44534,#44535,#44536,#44537,#44538,#44539,#44540,
#44541,#44542,#44543,#44544,#44545,#44546,#44547,#44548,#44549,#44550,#44551,
#44552,#44553,#44554,#44555,#44556,#44557,#44558,#44559,#44560,#44561,#44562,
#44563,#44564,#44565,#44566,#44567,#44568,#44569,#44570,#44571,#44572,#44573,
#44574),.UNSPECIFIED.,.F.,.F.,(4,3,3,3,3,3,3,3,3,3,3,3,3,3,3,3,3,3,3,3,
3,3,3,3,3,3,3,3,3,3,3,3,3,3,3,3,3,3,3,3,3,3,3,3,3,3,3,3,3,3,3,3,3,3,3,3,
3,3,3,3,3,3,3,3,3,3,3,3,3,3,3,3,3,3,3,4),(101.641010125785,101.780785856195,
101.869359005486,101.957817798521,102.046186010879,102.137742346759,102.226008990301,
102.314262380904,102.402523863157,102.49081478232,102.579205767899,102.667656356169,
102.756236280894,102.778636697922,102.867209847227,102.955668640276,103.044036852647,
103.135593188522,103.223859832077,103.312113222692,103.400374704959,103.488665624134,
103.577056609725,103.665507198006,103.754087122742,103.77648753965,103.865060689027,
103.953519482148,104.041887694592,104.13344403044,104.221710674068,104.309964064756,
104.398225547095,104.486516466342,104.574907452005,104.663358040359,104.751937965165,
104.774338381377,104.86291153053,104.951370323427,105.039738535647,105.131294871579,
105.219561514985,105.307814905453,105.396076387572,105.484367306602,105.57275829205,
105.661208880191,105.749788804788,105.772189223105,105.860762372451,105.949221165538,
106.037589377947,106.129145713808,106.217412357397,106.305665748046,106.393927230345,
106.48221814955,106.57060913517,106.659059723479,106.74763964824,106.770040064832,
106.85861321471,106.947072008333,107.03544022128,107.12699655694,107.215263201072,
107.303516592264,107.391778075105,107.480068994853,107.568459981011,107.656910569858,
107.745490495149,107.767890906559,107.913755939669,107.924195432964),
 .UNSPECIFIED.);
#1448=B_SPLINE_CURVE_WITH_KNOTS('',3,(#44576,#44577,#44578,#44579,#44580,
#44581,#44582,#44583,#44584,#44585,#44586,#44587,#44588,#44589,#44590,#44591,
#44592,#44593,#44594,#44595,#44596,#44597,#44598,#44599,#44600,#44601,#44602,
#44603,#44604,#44605,#44606,#44607,#44608,#44609,#44610,#44611,#44612,#44613,
#44614,#44615,#44616,#44617,#44618,#44619,#44620,#44621,#44622,#44623,#44624,
#44625,#44626,#44627,#44628,#44629,#44630,#44631,#44632,#44633,#44634,#44635,
#44636,#44637,#44638,#44639,#44640,#44641,#44642,#44643,#44644,#44645,#44646,
#44647,#44648,#44649,#44650,#44651,#44652,#44653,#44654,#44655,#44656,#44657,
#44658,#44659,#44660,#44661,#44662,#44663,#44664,#44665,#44666,#44667,#44668,
#44669,#44670,#44671,#44672,#44673,#44674,#44675,#44676,#44677,#44678,#44679,
#44680,#44681,#44682,#44683,#44684,#44685,#44686,#44687,#44688,#44689,#44690,
#44691,#44692,#44693,#44694,#44695,#44696,#44697,#44698,#44699,#44700,#44701,
#44702,#44703,#44704,#44705,#44706,#44707,#44708,#44709,#44710,#44711,#44712,
#44713,#44714,#44715,#44716,#44717,#44718,#44719,#44720,#44721,#44722,#44723,
#44724,#44725,#44726,#44727,#44728,#44729,#44730,#44731,#44732,#44733,#44734,
#44735,#44736,#44737,#44738,#44739,#44740,#44741,#44742,#44743,#44744,#44745,
#44746,#44747,#44748,#44749,#44750,#44751,#44752,#44753,#44754,#44755,#44756,
#44757,#44758,#44759,#44760,#44761,#44762,#44763,#44764,#44765,#44766,#44767,
#44768,#44769,#44770,#44771,#44772,#44773,#44774,#44775,#44776,#44777,#44778,
#44779,#44780,#44781,#44782,#44783,#44784,#44785,#44786,#44787,#44788,#44789,
#44790,#44791,#44792,#44793,#44794,#44795,#44796,#44797,#44798,#44799,#44800,
#44801),.UNSPECIFIED.,.F.,.F.,(4,3,3,3,3,3,3,3,3,3,3,3,3,3,3,3,3,3,3,3,
3,3,3,3,3,3,3,3,3,3,3,3,3,3,3,3,3,3,3,3,3,3,3,3,3,3,3,3,3,3,3,3,3,3,3,3,
3,3,3,3,3,3,3,3,3,3,3,3,3,3,3,3,3,3,3,4),(107.92419543315,108.01134635584,
108.098408190689,108.185408317907,108.272376689573,108.359335804232,108.44630814868,
108.533368394491,108.620475838792,108.70771891813,108.765741748287,108.854314898402,
108.942773692249,109.031141905407,109.122698240983,109.21096488529,109.299218276644,
109.387479759634,109.475770679517,109.564161665791,109.65261225474,109.741192180117,
109.763592590014,109.852165743744,109.940624541239,110.028992758074,110.120549092283,
110.208815740317,110.29706913541,110.385330622146,110.473621545779,110.562012535788,
110.650463128471,110.739043057546,110.761443431742,110.85001656763,110.938475347259,
111.026843546225,111.11839988713,111.206666517397,111.294919894789,111.383181363912,
111.471472270038,111.559863242783,111.648313818323,111.736893730565,111.759294273469,
111.847867433928,111.936326238037,112.024694461365,112.116250793094,112.204517447281,
112.292770848391,112.381032341004,112.469323270367,112.557714265861,112.646164863892,
112.734744798077,112.757145115197,112.845718297108,112.93417712298,113.022545368351,
113.114101691923,113.202368368707,113.290621792579,113.378883308092,113.467174260469,
113.555565279028,113.64401590018,113.732595857391,113.754995956924,113.850302064542,
113.945297709924,114.040103513436,114.134621615787,114.207380739913),
 .UNSPECIFIED.);
#1449=B_SPLINE_CURVE_WITH_KNOTS('',3,(#44803,#44804,#44805,#44806,#44807,
#44808,#44809,#44810,#44811,#44812,#44813,#44814,#44815,#44816,#44817,#44818,
#44819,#44820,#44821,#44822,#44823,#44824,#44825,#44826,#44827,#44828,#44829,
#44830,#44831,#44832,#44833,#44834,#44835,#44836,#44837,#44838,#44839,#44840,
#44841,#44842,#44843,#44844,#44845,#44846,#44847,#44848,#44849,#44850,#44851,
#44852,#44853,#44854,#44855,#44856,#44857,#44858,#44859,#44860,#44861,#44862,
#44863,#44864,#44865,#44866,#44867,#44868,#44869,#44870,#44871,#44872,#44873,
#44874,#44875,#44876,#44877,#44878,#44879,#44880,#44881,#44882,#44883,#44884,
#44885,#44886,#44887,#44888,#44889,#44890,#44891,#44892,#44893,#44894,#44895,
#44896,#44897,#44898,#44899,#44900,#44901,#44902,#44903,#44904,#44905,#44906,
#44907,#44908,#44909,#44910,#44911,#44912,#44913,#44914,#44915,#44916,#44917,
#44918,#44919,#44920,#44921,#44922,#44923,#44924,#44925,#44926,#44927,#44928,
#44929,#44930,#44931,#44932,#44933,#44934,#44935,#44936,#44937,#44938,#44939,
#44940,#44941,#44942,#44943,#44944,#44945,#44946,#44947,#44948,#44949,#44950,
#44951,#44952,#44953,#44954,#44955,#44956,#44957,#44958,#44959,#44960,#44961,
#44962,#44963,#44964,#44965,#44966,#44967,#44968,#44969,#44970,#44971,#44972,
#44973,#44974,#44975,#44976,#44977,#44978,#44979,#44980,#44981,#44982,#44983,
#44984,#44985,#44986,#44987,#44988,#44989,#44990,#44991,#44992,#44993,#44994,
#44995,#44996,#44997,#44998,#44999,#45000,#45001,#45002,#45003,#45004,#45005,
#45006,#45007,#45008,#45009,#45010,#45011,#45012,#45013,#45014,#45015,#45016,
#45017,#45018,#45019,#45020,#45021,#45022,#45023,#45024,#45025,#45026,#45027,
#45028),.UNSPECIFIED.,.F.,.F.,(4,3,3,3,3,3,3,3,3,3,3,3,3,3,3,3,3,3,3,3,
3,3,3,3,3,3,3,3,3,3,3,3,3,3,3,3,3,3,3,3,3,3,3,3,3,3,3,3,3,3,3,3,3,3,3,3,
3,3,3,3,3,3,3,3,3,3,3,3,3,3,3,3,3,3,3,4),(114.207380740144,114.29822902319,
114.389148151898,114.480233973373,114.571404209436,114.662772777588,114.752846798651,
114.841420080294,114.929879004949,115.018247348053,115.109803634594,115.198070405915,
115.286323922988,115.374585530273,115.462876572899,115.551267679009,115.639718386248,
115.728298426754,115.750697640379,115.83927101322,115.92773003184,116.016098471528,
116.10765472285,116.195921596597,116.284175218065,116.372436931593,116.460728082187,
116.549119298247,116.637570116725,116.726150269473,116.748548482106,116.837120560223,
116.925578280648,117.013945420227,117.105502158178,117.193767735238,117.282020063494,
117.370280488661,117.458570357127,117.546960306742,117.635409866374,117.723988781068,
117.746399323834,117.834973920296,117.923434154979,118.011803801864,118.103359597326,
118.191627648883,118.27988243536,118.368145299902,118.456437586308,118.544829910087,
118.63328182126,118.721863036437,118.744250165561,118.832824666255,118.921284829279,
119.009654428358,119.101210250725,119.189478313511,119.277733132867,119.365996051797,
119.454288413975,119.542680844513,119.631132880622,119.719714246125,119.742101007288,
119.829657712105,119.917073105115,120.004407658741,120.091683759538,120.17892373707,
120.266174310352,120.353429477391,120.44074933614,120.490566047323),
 .UNSPECIFIED.);
#1450=B_SPLINE_CURVE_WITH_KNOTS('',3,(#45030,#45031,#45032,#45033,#45034,
#45035,#45036,#45037,#45038,#45039,#45040,#45041,#45042,#45043,#45044,#45045,
#45046,#45047,#45048,#45049,#45050,#45051,#45052,#45053,#45054,#45055,#45056,
#45057,#45058,#45059,#45060,#45061,#45062,#45063,#45064,#45065,#45066,#45067,
#45068,#45069,#45070,#45071,#45072,#45073,#45074,#45075,#45076,#45077,#45078,
#45079,#45080,#45081,#45082,#45083,#45084,#45085,#45086,#45087,#45088,#45089,
#45090,#45091,#45092,#45093,#45094,#45095,#45096,#45097,#45098,#45099,#45100,
#45101,#45102,#45103,#45104,#45105,#45106,#45107,#45108,#45109,#45110,#45111,
#45112,#45113,#45114,#45115,#45116,#45117,#45118,#45119,#45120,#45121,#45122,
#45123,#45124,#45125,#45126,#45127,#45128,#45129,#45130,#45131,#45132,#45133,
#45134,#45135,#45136,#45137,#45138,#45139,#45140,#45141,#45142,#45143,#45144,
#45145,#45146,#45147,#45148,#45149,#45150,#45151,#45152,#45153,#45154,#45155,
#45156,#45157,#45158,#45159,#45160,#45161,#45162,#45163,#45164,#45165,#45166,
#45167,#45168,#45169,#45170,#45171,#45172,#45173,#45174,#45175,#45176,#45177,
#45178,#45179,#45180,#45181,#45182,#45183,#45184,#45185,#45186,#45187,#45188,
#45189,#45190,#45191,#45192,#45193,#45194,#45195,#45196,#45197,#45198,#45199,
#45200,#45201,#45202,#45203,#45204,#45205,#45206,#45207,#45208,#45209,#45210,
#45211,#45212,#45213,#45214,#45215,#45216),.UNSPECIFIED.,.F.,.F.,(4,3,3,
3,3,3,3,3,3,3,3,3,3,3,3,3,3,3,3,3,3,3,3,3,3,3,3,3,3,3,3,3,3,3,3,3,3,3,3,
3,3,3,3,3,3,3,3,3,3,3,3,3,3,3,3,3,3,3,3,3,3,3,4),(120.490566047475,120.603855612386,
120.71971094167,120.739951849016,120.828540004253,120.917013763895,121.005396886632,
121.096947612146,121.185228934143,121.273496892886,121.361772817757,121.450078038697,
121.538483046463,121.626947510997,121.71554099275,121.737802690743,121.826381914761,
121.914846948535,122.003221558057,122.094775554858,122.183048940626,122.271309188573,
122.359577635319,122.447875618222,122.536273777125,122.624731611222,122.71331883065,
122.735653532471,122.824148713268,122.912529337165,123.000819272197,123.092404909948,
123.180593494166,123.268769036965,123.356952964635,123.44516670444,123.533481453563,
123.621856260651,123.710361654286,123.733504374198,123.822227114771,123.910835247245,
123.999352372869,124.090852728251,124.179266286799,124.26766559985,124.356071855323,
124.444506240839,124.533038041216,124.621628064168,124.710344348404,124.731355215925,
124.81905048528,124.90663353371,124.994129052871,125.081564029985,125.168967928638,
125.256362918329,125.343771156934,125.431265942597,125.518807433168,125.606481900134,
125.663325063941),.UNSPECIFIED.);
#1451=B_SPLINE_CURVE_WITH_KNOTS('',3,(#45220,#45221,#45222,#45223,#45224,
#45225,#45226,#45227),.UNSPECIFIED.,.F.,.F.,(4,1,1,1,1,4),(-127.724907741108,
-126.72705689938,-125.729206057653,-124.731355215925,-123.733504374198,
-123.473272362321),.UNSPECIFIED.);
#1452=B_SPLINE_CURVE_WITH_KNOTS('',3,(#45229,#45230,#45231,#45232,#45233,
#45234,#45235,#45236,#45237,#45238,#45239,#45240,#45241,#45242,#45243,#45244,
#45245,#45246,#45247,#45248,#45249,#45250,#45251,#45252,#45253,#45254,#45255,
#45256,#45257,#45258,#45259,#45260,#45261,#45262,#45263,#45264,#45265,#45266,
#45267,#45268,#45269,#45270,#45271,#45272,#45273,#45274,#45275,#45276,#45277,
#45278,#45279,#45280,#45281,#45282,#45283,#45284,#45285,#45286,#45287,#45288,
#45289,#45290,#45291,#45292,#45293,#45294,#45295,#45296,#45297,#45298,#45299,
#45300,#45301,#45302,#45303,#45304,#45305,#45306,#45307,#45308,#45309,#45310,
#45311,#45312,#45313,#45314,#45315,#45316,#45317,#45318,#45319,#45320,#45321,
#45322,#45323,#45324,#45325,#45326,#45327,#45328,#45329,#45330,#45331,#45332,
#45333,#45334,#45335,#45336,#45337,#45338,#45339,#45340,#45341,#45342,#45343,
#45344,#45345,#45346,#45347,#45348,#45349,#45350,#45351,#45352,#45353,#45354,
#45355,#45356,#45357,#45358,#45359,#45360,#45361,#45362,#45363,#45364,#45365,
#45366,#45367,#45368,#45369,#45370,#45371,#45372,#45373,#45374,#45375,#45376,
#45377,#45378,#45379,#45380,#45381,#45382,#45383,#45384,#45385,#45386,#45387,
#45388,#45389,#45390,#45391,#45392,#45393,#45394,#45395,#45396,#45397,#45398,
#45399,#45400,#45401,#45402,#45403,#45404,#45405,#45406,#45407,#45408,#45409,
#45410,#45411,#45412,#45413,#45414,#45415,#45416,#45417,#45418,#45419,#45420,
#45421,#45422,#45423,#45424,#45425,#45426,#45427,#45428,#45429,#45430,#45431,
#45432,#45433,#45434,#45435,#45436,#45437,#45438,#45439,#45440,#45441,#45442,
#45443,#45444,#45445,#45446,#45447,#45448,#45449,#45450,#45451,#45452,#45453,
#45454),.UNSPECIFIED.,.F.,.F.,(4,3,3,3,3,3,3,3,3,3,3,3,3,3,3,3,3,3,3,3,
3,3,3,3,3,3,3,3,3,3,3,3,3,3,3,3,3,3,3,3,3,3,3,3,3,3,3,3,3,3,3,3,3,3,3,3,
3,3,3,3,3,3,3,3,3,3,3,3,3,3,3,3,3,3,3,4),(-123.473269876606,-123.38591924059,
-123.298617101219,-123.211338154408,-123.124060152026,-123.036760850702,
-122.949367056308,-122.861919316573,-122.774338602659,-122.735653532471,
-122.647073127485,-122.558607139165,-122.470231800566,-122.378678161838,
-122.290404612489,-122.202144410105,-122.113876218018,-122.025578698975,
-121.9371813111,-121.848724428107,-121.760138415471,-121.737802690743,-121.649216030073,
-121.560743479549,-121.472361281677,-121.380810102595,-121.292528992542,
-121.204260982044,-121.115984741777,-121.027678941658,-120.939272967411,
-120.850807309327,-120.762212311637,-120.739951849016,-120.6513874492,-120.562937519873,
-120.474578274038,-120.383018615694,-120.294761138282,-120.206516971966,
-120.118264762376,-120.029983154502,-119.941601490546,-119.853160241319,
-119.764589609245,-119.742101007288,-119.65352642391,-119.565066194115,
-119.47669654411,-119.385140746791,-119.29687267282,-119.208617856976,-119.120354956251,
-119.032062626978,-118.943670250929,-118.855218281961,-118.766637001566,
-118.744250165561,-118.65567573012,-118.567215625718,-118.478846078501,
-118.387290234168,-118.299022205494,-118.210767413502,-118.122504515054,
-118.034212166333,-117.945819738524,-117.857367698867,-117.768786320475,
-117.746399323834,-117.655350362726,-117.564439993407,-117.470851137412,
-117.380195982519,-117.285140275973,-117.190084569427),.UNSPECIFIED.);
#1453=B_SPLINE_CURVE_WITH_KNOTS('',3,(#45456,#45457,#45458,#45459,#45460,
#45461,#45462,#45463,#45464,#45465,#45466,#45467,#45468,#45469,#45470,#45471,
#45472,#45473,#45474,#45475,#45476,#45477,#45478,#45479,#45480,#45481,#45482,
#45483,#45484,#45485,#45486,#45487,#45488,#45489,#45490,#45491,#45492,#45493,
#45494,#45495,#45496,#45497,#45498,#45499,#45500,#45501,#45502,#45503,#45504,
#45505,#45506,#45507,#45508,#45509,#45510,#45511,#45512,#45513,#45514,#45515,
#45516,#45517,#45518,#45519,#45520,#45521,#45522,#45523,#45524,#45525,#45526,
#45527,#45528,#45529,#45530,#45531,#45532,#45533,#45534,#45535,#45536,#45537,
#45538,#45539,#45540,#45541,#45542,#45543,#45544,#45545,#45546,#45547,#45548,
#45549,#45550,#45551,#45552,#45553,#45554,#45555,#45556,#45557,#45558,#45559,
#45560,#45561,#45562,#45563,#45564,#45565,#45566,#45567,#45568,#45569,#45570,
#45571,#45572,#45573,#45574,#45575,#45576,#45577,#45578,#45579,#45580,#45581,
#45582,#45583,#45584,#45585,#45586,#45587,#45588,#45589,#45590,#45591,#45592,
#45593,#45594,#45595,#45596,#45597,#45598,#45599,#45600,#45601,#45602,#45603,
#45604,#45605,#45606,#45607,#45608,#45609,#45610,#45611,#45612,#45613,#45614,
#45615,#45616,#45617,#45618,#45619,#45620,#45621,#45622,#45623,#45624,#45625,
#45626,#45627,#45628,#45629,#45630,#45631,#45632,#45633,#45634,#45635,#45636,
#45637,#45638,#45639,#45640,#45641,#45642,#45643,#45644,#45645,#45646,#45647,
#45648,#45649,#45650,#45651,#45652,#45653,#45654,#45655,#45656,#45657,#45658,
#45659,#45660,#45661,#45662,#45663,#45664,#45665,#45666,#45667,#45668,#45669,
#45670,#45671,#45672,#45673,#45674,#45675,#45676,#45677,#45678,#45679,#45680,
#45681),.UNSPECIFIED.,.F.,.F.,(4,3,3,3,3,3,3,3,3,3,3,3,3,3,3,3,3,3,3,3,
3,3,3,3,3,3,3,3,3,3,3,3,3,3,3,3,3,3,3,3,3,3,3,3,3,3,3,3,3,3,3,3,3,3,3,3,
3,3,3,3,3,3,3,3,3,3,3,3,3,3,3,3,3,3,3,4),(-117.190084569288,-117.095110346029,
-116.99976205911,-116.904221663067,-116.808380876812,-116.748548482106,
-116.659975105794,-116.571516084384,-116.483147642584,-116.391591392309,
-116.30332451815,-116.215070896898,-116.126809184213,-116.038518035092,
-115.950126821426,-115.861676005884,-115.773095856839,-115.750697640379,
-115.662124375681,-115.573665464735,-115.485297132119,-115.393740840436,
-115.305474071525,-115.217220553873,-115.128958943021,-115.04066789384,
-114.952276776786,-114.863826056029,-114.775245998352,-114.752846798651,
-114.664273762505,-114.57581508424,-114.487446988128,-114.395890609228,
-114.307624084878,-114.219370814354,-114.131109452938,-114.042818655246,
-113.954427791465,-113.865977325332,-113.777397522303,-113.754995956924,
-113.666422775285,-113.577963949636,-113.489595704438,-113.398039380783,
-113.309772704049,-113.221519280182,-113.133257764627,-113.044966812163,
-112.956575793451,-112.868125172106,-112.779545214647,-112.757145115197,
-112.668571956472,-112.580113153765,-112.491744931509,-112.400188599254,
-112.311921945313,-112.223668544144,-112.135407051166,-112.047116121132,
-111.958725124518,-111.870274525103,-111.78169458916,-111.759294273469,
-111.672016516612,-111.584852262681,-111.497786145448,-111.410774318335,
-111.323794262059,-111.236823490763,-111.149796935836,-111.062742663134,
-110.975577012017,-110.906899262451),.UNSPECIFIED.);
#1454=B_SPLINE_CURVE_WITH_KNOTS('',3,(#45683,#45684,#45685,#45686,#45687,
#45688,#45689,#45690,#45691,#45692,#45693,#45694,#45695,#45696,#45697,#45698,
#45699,#45700,#45701,#45702,#45703,#45704,#45705,#45706,#45707,#45708,#45709,
#45710,#45711,#45712,#45713,#45714,#45715,#45716,#45717,#45718,#45719,#45720,
#45721,#45722,#45723,#45724,#45725,#45726,#45727,#45728,#45729,#45730,#45731,
#45732,#45733,#45734,#45735,#45736,#45737,#45738,#45739,#45740,#45741,#45742,
#45743,#45744,#45745,#45746,#45747,#45748,#45749,#45750,#45751,#45752,#45753,
#45754,#45755,#45756,#45757,#45758,#45759,#45760,#45761,#45762,#45763,#45764,
#45765,#45766,#45767,#45768,#45769,#45770,#45771,#45772,#45773,#45774,#45775,
#45776,#45777,#45778,#45779,#45780,#45781,#45782,#45783,#45784,#45785,#45786,
#45787,#45788,#45789,#45790,#45791,#45792,#45793,#45794,#45795,#45796,#45797,
#45798,#45799,#45800,#45801,#45802,#45803,#45804,#45805,#45806,#45807,#45808,
#45809,#45810,#45811,#45812,#45813,#45814,#45815,#45816,#45817,#45818,#45819,
#45820,#45821,#45822,#45823,#45824,#45825,#45826,#45827,#45828,#45829,#45830,
#45831,#45832,#45833,#45834,#45835,#45836,#45837,#45838,#45839,#45840,#45841,
#45842,#45843,#45844,#45845,#45846,#45847,#45848,#45849,#45850,#45851,#45852,
#45853,#45854,#45855,#45856,#45857,#45858,#45859,#45860,#45861,#45862,#45863,
#45864,#45865,#45866,#45867,#45868,#45869,#45870,#45871,#45872,#45873,#45874,
#45875,#45876,#45877,#45878,#45879,#45880,#45881,#45882,#45883,#45884,#45885,
#45886,#45887,#45888,#45889,#45890,#45891,#45892,#45893,#45894,#45895,#45896,
#45897,#45898,#45899,#45900,#45901,#45902,#45903,#45904,#45905),
 .UNSPECIFIED.,.F.,.F.,(4,3,3,3,3,3,3,3,3,3,3,3,3,3,3,3,3,3,3,3,3,3,3,3,
3,3,3,3,3,3,3,3,3,3,3,3,3,3,3,3,3,3,3,3,3,3,3,3,3,3,3,3,3,3,3,3,3,3,3,3,
3,3,3,3,3,3,3,3,3,3,3,3,3,3,4),(-110.906899262247,-110.761443431742,-110.672870278115,
-110.584411480703,-110.496043263931,-110.404486929691,-110.316220281672,
-110.227966886576,-110.139705399819,-110.051414476147,-109.963023486072,
-109.874572893308,-109.78599296413,-109.763592590014,-109.67501944007,-109.586560646362,
-109.498192433311,-109.406636097683,-109.3183694534,-109.23011606204,-109.141854579015,
-109.053563659065,-108.965172672681,-108.876722083595,-108.788142158044,
-108.765741748287,-108.677168600319,-108.588709808628,-108.500341597634,
-108.40878526125,-108.320518619111,-108.232265229923,-108.144003749096,
-108.055712831368,-107.967321847231,-107.878871260408,-107.790291337127,
-107.767890906559,-107.679317756701,-107.590858963093,-107.502490750157,
-107.410934414492,-107.322667770362,-107.23441437917,-107.146152896324,
-107.057861976568,-106.969470990397,-106.881020401535,-106.792440476223,
-106.770040064832,-106.681466915503,-106.593008122429,-106.50463991003,
-106.413083574164,-106.324816930577,-106.236563539929,-106.148302057627,
-106.060011138416,-105.971620152786,-105.883169564464,-105.794589639687,
-105.772189223105,-105.683616073939,-105.595157281031,-105.506789068803,
-105.415232732875,-105.326966089467,-105.238712699,-105.150451216883,-105.062160297859,
-104.973769312418,-104.885318724288,-104.796738799704,-104.774338381377,
-104.623713955068),.UNSPECIFIED.);
#1455=B_SPLINE_CURVE_WITH_KNOTS('',3,(#45907,#45908,#45909,#45910,#45911,
#45912,#45913,#45914,#45915,#45916,#45917,#45918,#45919,#45920,#45921,#45922,
#45923,#45924,#45925,#45926,#45927,#45928,#45929,#45930,#45931,#45932,#45933,
#45934,#45935,#45936,#45937,#45938,#45939,#45940,#45941,#45942,#45943,#45944,
#45945,#45946,#45947,#45948,#45949,#45950,#45951,#45952,#45953,#45954,#45955,
#45956,#45957,#45958,#45959,#45960,#45961,#45962,#45963,#45964,#45965,#45966,
#45967,#45968,#45969,#45970,#45971,#45972,#45973,#45974,#45975,#45976,#45977,
#45978,#45979,#45980,#45981,#45982,#45983,#45984,#45985,#45986,#45987,#45988,
#45989,#45990,#45991,#45992,#45993,#45994,#45995,#45996,#45997,#45998,#45999,
#46000,#46001,#46002,#46003,#46004,#46005,#46006,#46007,#46008,#46009,#46010,
#46011,#46012,#46013,#46014,#46015,#46016,#46017,#46018,#46019,#46020,#46021,
#46022,#46023,#46024,#46025,#46026,#46027,#46028,#46029,#46030,#46031,#46032,
#46033,#46034,#46035,#46036,#46037,#46038,#46039,#46040,#46041,#46042,#46043,
#46044,#46045,#46046,#46047,#46048,#46049,#46050,#46051,#46052,#46053,#46054,
#46055,#46056,#46057,#46058,#46059,#46060,#46061,#46062,#46063,#46064,#46065,
#46066,#46067,#46068,#46069,#46070,#46071,#46072,#46073,#46074,#46075,#46076,
#46077,#46078,#46079,#46080,#46081,#46082,#46083,#46084,#46085,#46086,#46087,
#46088,#46089,#46090,#46091,#46092,#46093,#46094,#46095,#46096,#46097,#46098,
#46099,#46100,#46101,#46102,#46103,#46104,#46105,#46106,#46107,#46108,#46109,
#46110,#46111,#46112,#46113,#46114,#46115,#46116,#46117,#46118,#46119,#46120,
#46121,#46122,#46123,#46124,#46125,#46126,#46127,#46128,#46129,#46130,#46131,
#46132),.UNSPECIFIED.,.F.,.F.,(4,3,3,3,3,3,3,3,3,3,3,3,3,3,3,3,3,3,3,3,
3,3,3,3,3,3,3,3,3,3,3,3,3,3,3,3,3,3,3,3,3,3,3,3,3,3,3,3,3,3,3,3,3,3,3,3,
3,3,3,3,3,3,3,3,3,3,3,3,3,3,3,3,3,3,3,4),(-104.623713954873,-104.536549056533,
-104.449474776175,-104.362464266208,-104.275486898148,-104.188520177306,
-104.101541622016,-104.014475919247,-103.927364282644,-103.840115392771,
-103.77648753965,-103.687914390346,-103.599455597299,-103.511087384929,
-103.419531049053,-103.331264405498,-103.243011014883,-103.154749532617,
-103.066458613441,-102.978067627849,-102.889617039567,-102.80103711483,
-102.778636697922,-102.69006354863,-102.601604755595,-102.513236543237,
-102.421680207357,-102.333413563815,-102.245160173213,-102.156898690961,
-102.0686077718,-101.980216786222,-101.891766197954,-101.803186273231,-101.780785856195,
-101.69221270688,-101.603753913822,-101.515385701442,-101.42382936557,-101.335562722005,
-101.247309331379,-101.159047849102,-101.070756929917,-100.982365944315,
-100.893915356022,-100.805335431276,-100.782935014468,-100.694361865162,
-100.605903072113,-100.517534859742,-100.425978523867,-100.337711880311,
-100.249458489695,-100.161197007427,-100.072906088251,-99.9845151026583,
-99.8960645143748,-99.8074845896374,-99.7850841727403,-99.6965110234348,
-99.6080522303865,-99.5196840180148,-99.4281276821396,-99.3398610385841,
-99.251607647968,-99.1633461657009,-99.0750552465254,-98.9866642609333,
-98.8982136726508,-98.809633747914,-98.7872333310129,-98.6916230320358,
-98.5963332393344,-98.501241351583,-98.4064500985313,-98.340528648016),
 .UNSPECIFIED.);
#1456=B_SPLINE_CURVE_WITH_KNOTS('',3,(#46134,#46135,#46136,#46137,#46138,
#46139,#46140,#46141,#46142,#46143,#46144,#46145,#46146,#46147,#46148,#46149,
#46150,#46151,#46152,#46153,#46154,#46155,#46156,#46157,#46158,#46159,#46160,
#46161,#46162,#46163,#46164,#46165,#46166,#46167,#46168,#46169,#46170,#46171,
#46172,#46173,#46174,#46175,#46176,#46177,#46178,#46179,#46180,#46181,#46182,
#46183,#46184,#46185,#46186,#46187,#46188,#46189,#46190,#46191,#46192,#46193,
#46194,#46195,#46196,#46197,#46198,#46199,#46200,#46201,#46202,#46203,#46204,
#46205,#46206,#46207,#46208,#46209,#46210,#46211,#46212,#46213,#46214,#46215,
#46216,#46217,#46218,#46219,#46220,#46221,#46222,#46223,#46224,#46225,#46226,
#46227,#46228,#46229,#46230,#46231,#46232,#46233,#46234,#46235,#46236,#46237,
#46238,#46239,#46240,#46241,#46242,#46243,#46244,#46245,#46246,#46247,#46248,
#46249,#46250,#46251,#46252,#46253,#46254,#46255,#46256,#46257,#46258,#46259,
#46260,#46261,#46262,#46263,#46264,#46265,#46266,#46267,#46268,#46269,#46270,
#46271,#46272,#46273,#46274,#46275,#46276,#46277,#46278,#46279,#46280,#46281,
#46282,#46283,#46284,#46285,#46286,#46287,#46288,#46289,#46290,#46291,#46292,
#46293,#46294,#46295,#46296,#46297,#46298,#46299,#46300,#46301,#46302,#46303,
#46304,#46305,#46306,#46307,#46308,#46309,#46310,#46311,#46312,#46313,#46314,
#46315,#46316,#46317,#46318,#46319,#46320,#46321,#46322,#46323,#46324,#46325,
#46326,#46327,#46328,#46329,#46330,#46331,#46332,#46333,#46334,#46335,#46336,
#46337,#46338,#46339,#46340,#46341,#46342,#46343,#46344,#46345,#46346,#46347,
#46348,#46349,#46350,#46351,#46352,#46353,#46354,#46355,#46356,#46357,#46358,
#46359),.UNSPECIFIED.,.F.,.F.,(4,3,3,3,3,3,3,3,3,3,3,3,3,3,3,3,3,3,3,3,
3,3,3,3,3,3,3,3,3,3,3,3,3,3,3,3,3,3,3,3,3,3,3,3,3,3,3,3,3,3,3,3,3,3,3,3,
3,3,3,3,3,3,3,3,3,3,3,3,3,3,3,3,3,3,3,4),(-98.3405286478881,-98.2498497411809,
-98.1591056839463,-98.0666748852811,-97.9756879240618,-97.8825352066736,
-97.7893824892855,-97.7008093399791,-97.6123505469294,-97.5239823345569,
-97.432425998682,-97.3441593551254,-97.2559059645082,-97.1676444822402,
-97.0793535630634,-96.99096257747,-96.9025119891859,-96.8139320644476,-96.791531647558,
-96.7029584982515,-96.6144997052018,-96.526131492829,-96.4345751569543,
-96.3463085133976,-96.2580551227804,-96.1697936405121,-96.0815027213353,
-95.9931117357419,-95.9046611474578,-95.8160812227196,-95.7936808058307,
-95.705107656524,-95.6166488634743,-95.5282806511014,-95.4367243152267,
-95.3484576716697,-95.2602042810523,-95.1719427987839,-95.0836518796068,
-94.9952608940133,-94.9068103057289,-94.8182303809906,-94.7958299641032,
-94.7072568147966,-94.618798021747,-94.5304298093744,-94.4388734734996,
-94.3506068299428,-94.2623534393254,-94.1740919570567,-94.0858010378792,
-93.9974100522856,-93.9089594640012,-93.820379539263,-93.7979791223758,
-93.7094059730693,-93.6209471800196,-93.5325789676472,-93.4410226317723,
-93.3527559882155,-93.2645025975981,-93.1762411153299,-93.0879501961525,
-92.9995592105589,-92.911108622275,-92.8225286975367,-92.8001282806485,
-92.7125191503955,-92.6250518999664,-92.5376658860685,-92.4503387614408,
-92.3630482356725,-92.2757489183866,-92.1884454166725,-92.1010806652874,
-92.0573433407085),.UNSPECIFIED.);
#1457=B_SPLINE_CURVE_WITH_KNOTS('',3,(#46361,#46362,#46363,#46364,#46365,
#46366,#46367,#46368,#46369,#46370,#46371,#46372,#46373,#46374,#46375,#46376,
#46377,#46378,#46379,#46380,#46381,#46382,#46383,#46384,#46385,#46386,#46387,
#46388,#46389,#46390,#46391,#46392,#46393,#46394,#46395,#46396,#46397,#46398,
#46399,#46400,#46401,#46402,#46403,#46404,#46405,#46406,#46407,#46408,#46409,
#46410,#46411,#46412,#46413,#46414,#46415,#46416,#46417,#46418,#46419,#46420,
#46421,#46422,#46423,#46424,#46425,#46426,#46427,#46428,#46429,#46430,#46431,
#46432,#46433,#46434,#46435,#46436,#46437,#46438,#46439,#46440,#46441,#46442,
#46443,#46444,#46445,#46446,#46447,#46448,#46449,#46450,#46451,#46452,#46453,
#46454,#46455,#46456,#46457,#46458,#46459,#46460,#46461,#46462,#46463,#46464,
#46465,#46466,#46467,#46468,#46469,#46470,#46471,#46472,#46473,#46474,#46475,
#46476,#46477,#46478,#46479,#46480,#46481,#46482,#46483,#46484,#46485,#46486,
#46487,#46488,#46489,#46490,#46491,#46492,#46493,#46494,#46495,#46496,#46497,
#46498,#46499,#46500,#46501,#46502,#46503,#46504,#46505,#46506,#46507,#46508,
#46509,#46510,#46511,#46512,#46513,#46514,#46515,#46516,#46517,#46518,#46519,
#46520,#46521,#46522,#46523,#46524,#46525,#46526,#46527,#46528,#46529,#46530,
#46531,#46532,#46533,#46534,#46535,#46536,#46537,#46538,#46539,#46540,#46541,
#46542,#46543,#46544,#46545,#46546,#46547,#46548,#46549,#46550,#46551,#46552,
#46553,#46554,#46555,#46556,#46557,#46558,#46559,#46560,#46561,#46562,#46563,
#46564,#46565,#46566,#46567,#46568,#46569,#46570,#46571,#46572,#46573,#46574,
#46575,#46576,#46577,#46578,#46579,#46580,#46581,#46582,#46583,#46584,#46585,
#46586,#46587,#46588,#46589),.UNSPECIFIED.,.F.,.F.,(4,3,3,3,3,3,3,3,3,3,
3,3,3,3,3,3,3,3,3,3,3,3,3,3,3,3,3,3,3,3,3,3,3,3,3,3,3,3,3,3,3,3,3,3,3,3,
3,3,3,3,3,3,3,3,3,3,3,3,3,3,3,3,3,3,3,3,3,3,3,3,3,3,3,3,3,3,4),(-92.057343340495,
-91.9449587259192,-91.8301949929713,-91.8022774389211,-91.7137042896145,
-91.6252454965649,-91.5368772841923,-91.4453209483174,-91.3570543047606,
-91.2688009141433,-91.180539431875,-91.0922485126981,-91.0038575271046,
-90.9154069388204,-90.8268270140822,-90.8044265971936,-90.7158534478869,
-90.627394654837,-90.5390264424644,-90.4474701065896,-90.3592034630327,
-90.2709500724152,-90.1826885901467,-90.0943976709694,-90.0060066853758,
-89.9175560970915,-89.8289761723532,-89.8065757554662,-89.7180026061597,
-89.6295438131101,-89.5411756007375,-89.4496192648627,-89.361352621306,
-89.2730992306887,-89.1848377484205,-89.0965468292434,-89.00815584365,-88.9197052553658,
-88.8311253306277,-88.8087249137388,-88.7201517644322,-88.6316929713824,
-88.5433247590098,-88.451768423135,-88.3635017795781,-88.2752483889608,
-88.1869869066924,-88.0986959875153,-88.0103050019217,-87.9218544136375,
-87.8332744888993,-87.8108740720114,-87.7223009227048,-87.633842129655,
-87.5454739172825,-87.4539175814076,-87.3656509378508,-87.2773975472334,
-87.1891360649651,-87.1008451457881,-87.0124541601946,-86.9240035719103,
-86.8354236471721,-86.813023230284,-86.7244500809775,-86.6359912879278,
-86.5476230755552,-86.4560667396804,-86.3678000961236,-86.2795467055064,
-86.1912852232381,-86.102994304061,-86.0146033184676,-85.9261527301834,
-85.8375728054453,-85.8151723885566,-85.7741580335289),.UNSPECIFIED.);
#1458=B_SPLINE_CURVE_WITH_KNOTS('',3,(#46591,#46592,#46593,#46594,#46595,
#46596,#46597,#46598,#46599,#46600,#46601,#46602,#46603,#46604,#46605,#46606,
#46607,#46608,#46609,#46610,#46611,#46612,#46613,#46614,#46615,#46616,#46617,
#46618,#46619,#46620,#46621,#46622,#46623,#46624,#46625,#46626,#46627,#46628,
#46629,#46630,#46631,#46632,#46633,#46634,#46635,#46636,#46637,#46638,#46639,
#46640,#46641,#46642,#46643,#46644,#46645,#46646,#46647,#46648,#46649,#46650,
#46651,#46652,#46653,#46654,#46655,#46656,#46657,#46658,#46659,#46660,#46661,
#46662,#46663,#46664,#46665,#46666,#46667,#46668,#46669,#46670,#46671,#46672,
#46673,#46674,#46675,#46676,#46677,#46678,#46679,#46680,#46681,#46682,#46683,
#46684,#46685,#46686,#46687,#46688,#46689,#46690,#46691,#46692,#46693,#46694,
#46695,#46696,#46697,#46698,#46699,#46700,#46701,#46702,#46703,#46704,#46705,
#46706,#46707,#46708,#46709,#46710,#46711,#46712,#46713,#46714,#46715,#46716,
#46717,#46718,#46719,#46720,#46721,#46722,#46723,#46724,#46725,#46726,#46727,
#46728,#46729,#46730,#46731,#46732,#46733,#46734,#46735,#46736,#46737,#46738,
#46739,#46740,#46741,#46742,#46743,#46744,#46745,#46746,#46747,#46748,#46749,
#46750,#46751,#46752,#46753,#46754,#46755,#46756,#46757,#46758,#46759,#46760,
#46761,#46762,#46763,#46764,#46765,#46766,#46767,#46768,#46769,#46770,#46771,
#46772,#46773,#46774,#46775,#46776,#46777,#46778,#46779,#46780,#46781,#46782,
#46783,#46784,#46785,#46786,#46787,#46788,#46789,#46790,#46791,#46792,#46793,
#46794,#46795,#46796,#46797,#46798,#46799,#46800,#46801,#46802,#46803,#46804,
#46805,#46806,#46807,#46808,#46809,#46810,#46811,#46812,#46813,#46814,#46815,
#46816),.UNSPECIFIED.,.F.,.F.,(4,3,3,3,3,3,3,3,3,3,3,3,3,3,3,3,3,3,3,3,
3,3,3,3,3,3,3,3,3,3,3,3,3,3,3,3,3,3,3,3,3,3,3,3,3,3,3,3,3,3,3,3,3,3,3,3,
3,3,3,3,3,3,3,3,3,3,3,3,3,3,3,3,3,3,3,4),(-85.7741580333869,-85.6861685578636,
-85.5982909458262,-85.5105007898011,-85.4227708640778,-85.3350723553463,
-85.247383339102,-85.1596819028892,-85.0718905841978,-84.9840538824836,
-84.8960730339901,-84.8173215468292,-84.7287483975225,-84.6402896044727,
-84.5519213921003,-84.4603650562255,-84.3720984126686,-84.2838450220513,
-84.1955835397829,-84.1072926206058,-84.0189016350122,-83.930451046728,
-83.8418711219897,-83.8194707051018,-83.7308975557953,-83.6424387627455,
-83.5540705503729,-83.4625142144981,-83.3742475709413,-83.285994180324,
-83.1977326980555,-83.1094417788783,-83.0210507932848,-82.9326002050006,
-82.8440202802623,-82.8216198633744,-82.7330467140678,-82.644587921018,
-82.556219708645,-82.4646633727702,-82.3763967292134,-82.288143338596,-82.1998818563276,
-82.1115909371499,-82.0231999515564,-81.9347493632724,-81.846169438534,
-81.823769021647,-81.7351958723405,-81.6467370792908,-81.5583688669186,
-81.4668125310437,-81.3785458874869,-81.2902924968697,-81.2020310146015,
-81.1137400954241,-81.0253491098307,-80.9368985215465,-80.8483185968085,
-80.8259181799196,-80.7373450306132,-80.6488862375634,-80.5605180251908,
-80.468961689316,-80.3806950457592,-80.2924416551418,-80.2041801728737,
-80.115889253696,-80.0274982681023,-79.9390476798177,-79.8504677550797,
-79.8280673381922,-79.7244964726417,-79.6214093916813,-79.5191863692498,
-79.4909727265609),.UNSPECIFIED.);
#1459=B_SPLINE_CURVE_WITH_KNOTS('',3,(#46818,#46819,#46820,#46821,#46822,
#46823,#46824,#46825,#46826,#46827,#46828,#46829,#46830,#46831,#46832,#46833,
#46834,#46835,#46836,#46837,#46838,#46839,#46840,#46841,#46842,#46843,#46844,
#46845,#46846,#46847,#46848,#46849,#46850,#46851,#46852,#46853,#46854,#46855,
#46856,#46857,#46858,#46859,#46860,#46861,#46862,#46863,#46864,#46865,#46866,
#46867,#46868,#46869,#46870,#46871,#46872,#46873,#46874,#46875,#46876,#46877,
#46878,#46879,#46880,#46881,#46882,#46883,#46884,#46885,#46886,#46887,#46888,
#46889,#46890,#46891,#46892,#46893,#46894,#46895,#46896,#46897,#46898,#46899,
#46900,#46901,#46902,#46903,#46904,#46905,#46906,#46907,#46908,#46909,#46910,
#46911,#46912,#46913,#46914,#46915,#46916,#46917,#46918,#46919,#46920,#46921,
#46922,#46923,#46924,#46925,#46926,#46927,#46928,#46929,#46930,#46931,#46932,
#46933,#46934,#46935,#46936,#46937,#46938,#46939,#46940,#46941,#46942,#46943,
#46944,#46945,#46946,#46947,#46948,#46949,#46950,#46951,#46952,#46953,#46954,
#46955,#46956,#46957,#46958,#46959,#46960,#46961,#46962,#46963,#46964,#46965,
#46966,#46967,#46968,#46969,#46970,#46971,#46972,#46973,#46974,#46975,#46976,
#46977,#46978,#46979,#46980,#46981,#46982,#46983,#46984,#46985,#46986,#46987,
#46988,#46989,#46990,#46991,#46992,#46993,#46994,#46995,#46996,#46997,#46998,
#46999,#47000,#47001,#47002,#47003,#47004,#47005,#47006,#47007,#47008,#47009,
#47010,#47011,#47012,#47013,#47014,#47015,#47016,#47017,#47018,#47019,#47020,
#47021,#47022,#47023,#47024,#47025,#47026,#47027,#47028,#47029,#47030,#47031,
#47032,#47033,#47034,#47035,#47036,#47037,#47038,#47039,#47040,#47041,#47042,
#47043),.UNSPECIFIED.,.F.,.F.,(4,3,3,3,3,3,3,3,3,3,3,3,3,3,3,3,3,3,3,3,
3,3,3,3,3,3,3,3,3,3,3,3,3,3,3,3,3,3,3,3,3,3,3,3,3,3,3,3,3,3,3,3,3,3,3,3,
3,3,3,3,3,3,3,3,3,3,3,3,3,3,3,3,3,3,3,4),(-79.4909727263493,-79.4027030535825,
-79.3144454917003,-79.2261787933954,-79.1378817098842,-79.0494784849834,
-78.9610151902706,-78.8724102190024,-78.8302164964648,-78.7416433471584,
-78.6531845541089,-78.5648163417366,-78.4732600058617,-78.3849933623051,
-78.296739971688,-78.2084784894198,-78.1201875702428,-78.0317965846497,
-77.9433459963656,-77.8547660716276,-77.8323656547374,-77.7437925054306,
-77.6553337123805,-77.5669655000076,-77.4754091641329,-77.3871425205758,
-77.2988891299583,-77.2106276476894,-77.1223367285122,-77.0339457429185,
-76.945495154634,-76.8569152298955,-76.83451481301,-76.7459416637034,-76.6574828706539,
-76.5691146582814,-76.4775583224066,-76.3892916788497,-76.3010382882324,
-76.2127768059642,-76.1244858867866,-76.0360949011931,-75.9476443129089,
-75.8590643881708,-75.8366639712826,-75.7480908219762,-75.6596320289267,
-75.571263816554,-75.4797074806792,-75.3914408371224,-75.3031874465053,
-75.2149259642374,-75.1266350450602,-75.0382440594668,-74.9497934711824,
-74.8612135464444,-74.8388131295552,-74.7502399802486,-74.6617811871987,
-74.573412974826,-74.4818566389512,-74.3935899953943,-74.3053366047771,
-74.2170751225086,-74.1287842033319,-74.0403932177383,-73.9519426294544,
-73.8633627047159,-73.8409622878278,-73.751861812671,-73.6628783053689,
-73.573990958071,-73.4824400733457,-73.3936855521488,-73.3007364856592,
-73.2077874191697),.UNSPECIFIED.);
#1460=B_SPLINE_CURVE_WITH_KNOTS('',3,(#47045,#47046,#47047,#47048,#47049,
#47050,#47051,#47052,#47053,#47054,#47055,#47056,#47057,#47058,#47059,#47060,
#47061,#47062,#47063,#47064,#47065,#47066,#47067,#47068,#47069,#47070,#47071,
#47072,#47073,#47074,#47075,#47076,#47077,#47078,#47079,#47080,#47081,#47082,
#47083,#47084,#47085,#47086,#47087,#47088,#47089,#47090,#47091,#47092,#47093,
#47094,#47095,#47096,#47097,#47098,#47099,#47100,#47101,#47102,#47103,#47104,
#47105,#47106,#47107,#47108,#47109,#47110,#47111,#47112,#47113,#47114,#47115,
#47116,#47117,#47118,#47119,#47120,#47121,#47122,#47123,#47124,#47125,#47126,
#47127,#47128,#47129,#47130,#47131,#47132,#47133,#47134,#47135,#47136,#47137,
#47138,#47139,#47140,#47141,#47142,#47143,#47144,#47145,#47146,#47147,#47148,
#47149,#47150,#47151,#47152,#47153,#47154,#47155,#47156,#47157,#47158,#47159,
#47160,#47161,#47162,#47163,#47164,#47165,#47166,#47167,#47168,#47169,#47170,
#47171,#47172,#47173,#47174,#47175,#47176,#47177,#47178,#47179,#47180,#47181,
#47182,#47183,#47184,#47185,#47186,#47187,#47188,#47189,#47190,#47191,#47192,
#47193,#47194,#47195,#47196,#47197,#47198,#47199,#47200,#47201,#47202,#47203,
#47204,#47205,#47206,#47207,#47208,#47209,#47210,#47211,#47212,#47213,#47214,
#47215,#47216,#47217,#47218,#47219,#47220,#47221,#47222,#47223,#47224,#47225,
#47226,#47227,#47228,#47229,#47230,#47231,#47232,#47233,#47234,#47235,#47236,
#47237,#47238,#47239,#47240,#47241,#47242,#47243,#47244,#47245,#47246,#47247,
#47248,#47249,#47250,#47251,#47252,#47253,#47254,#47255,#47256,#47257,#47258,
#47259,#47260,#47261,#47262,#47263,#47264,#47265,#47266,#47267,#47268,#47269,
#47270),.UNSPECIFIED.,.F.,.F.,(4,3,3,3,3,3,3,3,3,3,3,3,3,3,3,3,3,3,3,3,
3,3,3,3,3,3,3,3,3,3,3,3,3,3,3,3,3,3,3,3,3,3,3,3,3,3,3,3,3,3,3,3,3,3,3,3,
3,3,3,3,3,3,3,3,3,3,3,3,3,3,3,3,3,3,3,4),(-73.2077874189448,-73.107736006707,
-73.0072421038471,-72.9061731673785,-72.8431114461004,-72.7545382967941,
-72.6660795037445,-72.5777112913722,-72.4861549554973,-72.3978883119406,
-72.3096349213235,-72.2213734390554,-72.1330825198784,-72.0446915342851,
-71.9562409460012,-71.8676610212632,-71.845260604373,-71.7566874550661,
-71.668228662016,-71.5798604496431,-71.4883041137684,-71.4000374702112,
-71.3117840795936,-71.2235225973249,-71.1352316781473,-71.0468406925535,
-70.9583901042689,-70.8698101795304,-70.8474097626456,-70.7588366133391,
-70.6703778202896,-70.5820096079171,-70.4904532720422,-70.4021866284856,
-70.3139332378684,-70.2256717556002,-70.1373808364232,-70.0489898508298,
-69.9605392625457,-69.8719593378077,-69.8495589209182,-69.7609857716116,
-69.6725269785619,-69.5841587661894,-69.4926024303146,-69.4043357867578,
-69.3160823961405,-69.2278209138722,-69.1395299946951,-69.0511390091016,
-68.9626884208175,-68.8741084960793,-68.8517080791908,-68.7631349298841,
-68.6746761368343,-68.5863079244616,-68.4947515885868,-68.4064849450298,
-68.3182315544124,-68.229970072144,-68.1416791529668,-68.0532881673732,
-67.9648375790888,-67.8762576543504,-67.8538572374634,-67.766148257947,
-67.6785529256838,-67.5910465431623,-67.5036029660178,-67.4161918075192,
-67.3287908976867,-67.2413780793301,-67.153881432156,-67.0663392072975,
-66.978667484412,-66.9246021121963),.UNSPECIFIED.);
#1461=B_SPLINE_CURVE_WITH_KNOTS('',3,(#47272,#47273,#47274,#47275,#47276,
#47277,#47278,#47279,#47280,#47281,#47282,#47283,#47284,#47285,#47286,#47287,
#47288,#47289,#47290,#47291,#47292,#47293,#47294,#47295,#47296,#47297,#47298,
#47299,#47300,#47301,#47302,#47303,#47304,#47305,#47306,#47307,#47308,#47309,
#47310,#47311,#47312,#47313,#47314,#47315,#47316,#47317,#47318,#47319,#47320,
#47321,#47322,#47323,#47324,#47325,#47326,#47327,#47328,#47329,#47330,#47331,
#47332,#47333,#47334,#47335,#47336,#47337,#47338,#47339,#47340,#47341,#47342,
#47343,#47344,#47345,#47346,#47347,#47348,#47349,#47350,#47351,#47352,#47353,
#47354,#47355,#47356,#47357,#47358,#47359,#47360,#47361,#47362,#47363,#47364,
#47365,#47366,#47367,#47368,#47369,#47370,#47371,#47372,#47373,#47374,#47375,
#47376,#47377,#47378,#47379,#47380,#47381,#47382,#47383,#47384,#47385,#47386,
#47387,#47388,#47389,#47390,#47391,#47392,#47393,#47394,#47395,#47396,#47397,
#47398,#47399,#47400,#47401,#47402,#47403,#47404,#47405,#47406,#47407,#47408,
#47409,#47410,#47411,#47412,#47413,#47414,#47415,#47416,#47417,#47418,#47419,
#47420,#47421,#47422,#47423,#47424,#47425,#47426,#47427,#47428,#47429,#47430,
#47431,#47432,#47433,#47434,#47435,#47436,#47437,#47438,#47439,#47440,#47441,
#47442,#47443,#47444,#47445,#47446,#47447,#47448,#47449,#47450,#47451,#47452,
#47453,#47454,#47455,#47456,#47457,#47458,#47459,#47460,#47461,#47462,#47463,
#47464,#47465,#47466,#47467,#47468,#47469,#47470,#47471,#47472,#47473,#47474,
#47475,#47476,#47477,#47478,#47479,#47480,#47481,#47482,#47483,#47484,#47485,
#47486,#47487,#47488,#47489,#47490,#47491,#47492,#47493,#47494,#47495,#47496,
#47497),.UNSPECIFIED.,.F.,.F.,(4,3,3,3,3,3,3,3,3,3,3,3,3,3,3,3,3,3,3,3,
3,3,3,3,3,3,3,3,3,3,3,3,3,3,3,3,3,3,3,3,3,3,3,3,3,3,3,3,3,3,3,3,3,3,3,3,
3,3,3,3,3,3,3,3,3,3,3,3,3,3,3,3,3,3,3,4),(-66.9246021119902,-66.856006395736,
-66.7674332464294,-66.6789744533797,-66.5906062410072,-66.4990499051323,
-66.4107832615755,-66.3225298709582,-66.2342683886898,-66.1459774695125,
-66.057586483919,-65.9691358956348,-65.8805559708966,-65.8581555540086,
-65.769582404702,-65.6811236116524,-65.5927553992799,-65.5011990634051,
-65.4129324198483,-65.324679029231,-65.2364175469627,-65.1481266277855,
-65.0597356421921,-64.9712850539079,-64.8827051291697,-64.8603047122812,
-64.7717315629746,-64.6832727699248,-64.5949045575522,-64.5033482216774,
-64.4150815781205,-64.3268281875032,-64.2385667052348,-64.1502757860576,
-64.0618848004641,-63.9734342121798,-63.8848542874416,-63.8624538705538,
-63.7738807212472,-63.6854219281975,-63.5970537158249,-63.5054973799501,
-63.4172307363932,-63.3289773457759,-63.2407158635076,-63.1524249443304,
-63.0640339587369,-62.9755833704527,-62.8870034457144,-62.8646030288264,
-62.7760298795198,-62.68757108647,-62.5992028740974,-62.5076465382226,-62.4193798946658,
-62.3311265040484,-62.2428650217801,-62.1545741026029,-62.0661831170094,
-61.9777325287252,-61.889152603987,-61.866752187099,-61.7781790377924,-61.6897202447427,
-61.6013520323702,-61.5097956964953,-61.4215290529385,-61.3332756623212,
-61.245014180053,-61.156723260876,-61.0683322752826,-60.9798816869985,-60.8913017622603,
-60.8689013453716,-60.7496264044044,-60.6414168048105),.UNSPECIFIED.);
#1462=B_SPLINE_CURVE_WITH_KNOTS('',3,(#47499,#47500,#47501,#47502,#47503,
#47504,#47505,#47506,#47507,#47508,#47509,#47510,#47511,#47512,#47513,#47514,
#47515,#47516,#47517,#47518,#47519,#47520,#47521,#47522,#47523,#47524,#47525,
#47526,#47527,#47528,#47529,#47530,#47531,#47532,#47533,#47534,#47535,#47536,
#47537,#47538,#47539,#47540,#47541,#47542,#47543,#47544,#47545,#47546,#47547,
#47548,#47549,#47550,#47551,#47552,#47553,#47554,#47555,#47556,#47557,#47558,
#47559,#47560,#47561,#47562,#47563,#47564,#47565,#47566,#47567,#47568,#47569,
#47570,#47571,#47572,#47573,#47574,#47575,#47576,#47577,#47578,#47579,#47580,
#47581,#47582,#47583,#47584,#47585,#47586,#47587,#47588,#47589,#47590,#47591,
#47592,#47593,#47594,#47595,#47596,#47597,#47598,#47599,#47600,#47601,#47602,
#47603,#47604,#47605,#47606,#47607,#47608,#47609,#47610,#47611,#47612,#47613,
#47614,#47615,#47616,#47617,#47618,#47619,#47620,#47621,#47622,#47623,#47624,
#47625,#47626,#47627,#47628,#47629,#47630,#47631,#47632,#47633,#47634,#47635,
#47636,#47637,#47638,#47639,#47640,#47641,#47642,#47643,#47644,#47645,#47646,
#47647,#47648,#47649,#47650,#47651,#47652,#47653,#47654,#47655,#47656,#47657,
#47658,#47659,#47660,#47661,#47662,#47663,#47664,#47665,#47666,#47667,#47668,
#47669,#47670,#47671,#47672,#47673,#47674,#47675,#47676,#47677,#47678,#47679,
#47680,#47681,#47682,#47683,#47684,#47685,#47686,#47687,#47688,#47689,#47690,
#47691,#47692,#47693,#47694,#47695,#47696,#47697,#47698,#47699,#47700,#47701,
#47702,#47703,#47704,#47705,#47706,#47707,#47708,#47709,#47710,#47711,#47712,
#47713,#47714,#47715,#47716,#47717,#47718,#47719,#47720,#47721,#47722,#47723,
#47724),.UNSPECIFIED.,.F.,.F.,(4,3,3,3,3,3,3,3,3,3,3,3,3,3,3,3,3,3,3,3,
3,3,3,3,3,3,3,3,3,3,3,3,3,3,3,3,3,3,3,3,3,3,3,3,3,3,3,3,3,3,3,3,3,3,3,3,
3,3,3,3,3,3,3,3,3,3,3,3,3,3,3,3,3,3,3,4),(-60.6414168046243,-60.5541977116721,
-60.4670437573164,-60.3799239858169,-60.2928160029574,-60.2056974285119,
-60.1184916827307,-60.0312413215284,-59.9438501868131,-59.8710505036442,
-59.7824773543376,-59.6940185612878,-59.6056503489152,-59.5140940130404,
-59.4258273694834,-59.3375739788659,-59.2493124965977,-59.1610215774201,
-59.0726305918265,-58.9841800035421,-58.8956000788037,-58.8731996619168,
-58.7846265126102,-58.6961677195606,-58.6077995071879,-58.5162431713131,
-58.4279765277562,-58.3397231371388,-58.2514616548706,-58.1631707356933,
-58.0747797500998,-57.9863291618153,-57.8977492370771,-57.8753488201894,
-57.7867756708828,-57.6983168778331,-57.6099486654601,-57.5183923295854,
-57.4301256860287,-57.3418722954114,-57.253610813143,-57.165319893966,-57.0769289083726,
-56.9884783200883,-56.89989839535,-56.877497978462,-56.7889248291553,-56.7004660361056,
-56.6120978237326,-56.5205414878579,-56.432274844301,-56.3440214536834,
-56.2557599714151,-56.167469052238,-56.0790780666444,-55.9906274783599,
-55.9020475536216,-55.8796471367345,-55.7910739874279,-55.7026151943781,
-55.6142469820053,-55.5226906461305,-55.4344240025736,-55.3461706119562,
-55.2579091296879,-55.1696182105113,-55.0812272249179,-54.9927766366333,
-54.904196711895,-54.8817962950071,-54.7896385149843,-54.697634462087,-54.6058196949304,
-54.5141167775388,-54.4225461234993,-54.358231497631),.UNSPECIFIED.);
#1463=B_SPLINE_CURVE_WITH_KNOTS('',3,(#47726,#47727,#47728,#47729,#47730,
#47731,#47732,#47733,#47734,#47735,#47736,#47737,#47738,#47739,#47740,#47741,
#47742,#47743,#47744,#47745,#47746,#47747,#47748,#47749,#47750,#47751,#47752,
#47753,#47754,#47755,#47756,#47757,#47758,#47759,#47760,#47761,#47762,#47763,
#47764,#47765,#47766,#47767,#47768,#47769,#47770,#47771,#47772,#47773,#47774,
#47775,#47776,#47777,#47778,#47779,#47780,#47781,#47782,#47783,#47784,#47785,
#47786,#47787,#47788,#47789,#47790,#47791,#47792,#47793,#47794,#47795,#47796,
#47797,#47798,#47799,#47800,#47801,#47802,#47803,#47804,#47805,#47806,#47807,
#47808,#47809,#47810,#47811,#47812,#47813,#47814,#47815,#47816,#47817,#47818,
#47819,#47820,#47821,#47822,#47823,#47824,#47825,#47826,#47827,#47828,#47829,
#47830,#47831,#47832,#47833,#47834,#47835,#47836,#47837,#47838,#47839,#47840,
#47841,#47842,#47843,#47844,#47845,#47846,#47847,#47848,#47849,#47850,#47851,
#47852,#47853,#47854,#47855,#47856,#47857,#47858,#47859,#47860,#47861,#47862,
#47863,#47864,#47865,#47866,#47867,#47868,#47869,#47870,#47871,#47872,#47873,
#47874,#47875,#47876,#47877,#47878,#47879,#47880,#47881,#47882,#47883,#47884,
#47885,#47886,#47887,#47888,#47889,#47890,#47891,#47892,#47893,#47894,#47895,
#47896,#47897,#47898,#47899,#47900,#47901,#47902,#47903,#47904,#47905,#47906,
#47907,#47908,#47909,#47910,#47911,#47912,#47913,#47914,#47915,#47916,#47917,
#47918,#47919,#47920,#47921,#47922,#47923,#47924,#47925,#47926,#47927,#47928,
#47929,#47930,#47931,#47932,#47933,#47934,#47935,#47936,#47937,#47938,#47939,
#47940,#47941,#47942,#47943,#47944,#47945,#47946,#47947,#47948,#47949,#47950,
#47951),.UNSPECIFIED.,.F.,.F.,(4,3,3,3,3,3,3,3,3,3,3,3,3,3,3,3,3,3,3,3,
3,3,3,3,3,3,3,3,3,3,3,3,3,3,3,3,3,3,3,3,3,3,3,3,3,3,3,3,3,3,3,3,3,3,3,3,
3,3,3,3,3,3,3,3,3,3,3,3,3,3,3,3,3,3,3,4),(-54.3582314975039,-54.264791755642,
-54.1695801800514,-54.0757075390254,-53.9798264961525,-53.8839454532797,
-53.795372303973,-53.7069135109231,-53.6185452985502,-53.5269889626755,
-53.4387223191185,-53.3504689285011,-53.2622074462326,-53.1739165270553,
-53.0855255414617,-52.9970749531774,-52.9084950284391,-52.8860946115523,
-52.7975214622459,-52.7090626691963,-52.6206944568239,-52.529138120949,
-52.4408714773923,-52.3526180867751,-52.264356604507,-52.1760656853299,
-52.0876746997365,-51.9992241114524,-51.9106441867144,-51.8882437698249,
-51.7996706205183,-51.7112118274685,-51.6228436150958,-51.531287279221,
-51.4430206356642,-51.3547672450468,-51.2665057627784,-51.1782148436012,
-51.0898238580077,-51.0013732697234,-50.9127933449851,-50.8903929280975,
-50.8018197787909,-50.7133609857411,-50.6249927733685,-50.5334364374937,
-50.4451697939368,-50.3569164033195,-50.2686549210512,-50.1803640018741,
-50.0919730162806,-50.0035224279963,-49.9149425032581,-49.8925420863701,
-49.8039689370635,-49.7155101440137,-49.6271419316411,-49.5355855957663,
-49.4473189522095,-49.3590655615921,-49.2708040793238,-49.1825131601465,
-49.094122174553,-49.0056715862686,-48.9170916615304,-48.8946912446427,
-48.8074317150175,-48.7158835244647,-48.628840891428,-48.5418520352336,
-48.4548944238696,-48.3679455587889,-48.280947766268,-48.1939214043626,
-48.1068026622925,-48.0750461905954),.UNSPECIFIED.);
#1464=B_SPLINE_CURVE_WITH_KNOTS('',3,(#47953,#47954,#47955,#47956,#47957,
#47958,#47959,#47960,#47961,#47962,#47963,#47964,#47965,#47966,#47967,#47968,
#47969,#47970,#47971,#47972,#47973,#47974,#47975,#47976,#47977,#47978,#47979,
#47980,#47981,#47982,#47983,#47984,#47985,#47986,#47987,#47988,#47989,#47990,
#47991,#47992,#47993,#47994,#47995,#47996,#47997,#47998,#47999,#48000,#48001,
#48002,#48003,#48004,#48005,#48006,#48007,#48008,#48009,#48010,#48011,#48012,
#48013,#48014,#48015,#48016,#48017,#48018,#48019,#48020,#48021,#48022,#48023,
#48024,#48025,#48026,#48027,#48028,#48029,#48030,#48031,#48032,#48033,#48034,
#48035,#48036,#48037,#48038,#48039,#48040,#48041,#48042,#48043,#48044,#48045,
#48046,#48047,#48048,#48049,#48050,#48051,#48052,#48053,#48054,#48055,#48056,
#48057,#48058,#48059,#48060,#48061,#48062,#48063,#48064,#48065,#48066,#48067,
#48068,#48069,#48070,#48071,#48072,#48073,#48074,#48075,#48076,#48077,#48078,
#48079,#48080,#48081,#48082,#48083,#48084,#48085,#48086,#48087,#48088,#48089,
#48090,#48091,#48092,#48093,#48094,#48095,#48096,#48097,#48098,#48099,#48100,
#48101,#48102,#48103,#48104,#48105,#48106,#48107,#48108,#48109,#48110,#48111,
#48112,#48113,#48114,#48115,#48116,#48117,#48118,#48119,#48120,#48121,#48122,
#48123,#48124,#48125,#48126,#48127,#48128,#48129,#48130,#48131,#48132,#48133,
#48134,#48135,#48136,#48137,#48138,#48139,#48140,#48141,#48142,#48143,#48144,
#48145,#48146,#48147,#48148,#48149,#48150,#48151,#48152,#48153,#48154,#48155,
#48156,#48157,#48158,#48159,#48160,#48161,#48162,#48163,#48164,#48165,#48166,
#48167,#48168,#48169,#48170,#48171,#48172,#48173,#48174,#48175,#48176,#48177,
#48178),.UNSPECIFIED.,.F.,.F.,(4,3,3,3,3,3,3,3,3,3,3,3,3,3,3,3,3,3,3,3,
3,3,3,3,3,3,3,3,3,3,3,3,3,3,3,3,3,3,3,3,3,3,3,3,3,3,3,3,3,3,3,3,3,3,3,3,
3,3,3,3,3,3,3,3,3,3,3,3,3,3,3,3,3,3,3,4),(-48.0750461904514,-47.9402553841227,
-47.8968404029153,-47.8082672536088,-47.7198084605591,-47.6314402481864,
-47.5398839123116,-47.4516172687548,-47.3633638781374,-47.2751023958691,
-47.1868114766918,-47.0984204910982,-47.0099699028139,-46.9213899780757,
-46.8989895611879,-46.8104164118817,-46.7219576188323,-46.63358940646,-46.5420330705851,
-46.4537664270286,-46.3655130364117,-46.2772515541438,-46.188960634967,
-46.1005696493739,-46.01211906109,-45.9235391363522,-45.9011387194605,-45.8125655701538,
-45.7241067771039,-45.6357385647311,-45.5441822288564,-45.4559155852994,
-45.3676621946819,-45.2794007124134,-45.191109793236,-45.1027188076424,
-45.014268219358,-44.9256882946196,-44.9032878777331,-44.8147147284265,
-44.7262559353768,-44.6378877230042,-44.5463313871294,-44.4580647435726,
-44.3698113529553,-44.281549870687,-44.1932589515098,-44.1048679659163,
-44.0164173776321,-43.9278374528939,-43.9054370360057,-43.8168638866991,
-43.7284050936493,-43.6400368812767,-43.5484805454019,-43.460213901845,
-43.3719605112277,-43.2836990289593,-43.1954081097822,-43.1070171241887,
-43.0185665359043,-42.9299866111661,-42.9075861942783,-42.8190130449717,
-42.7305542519221,-42.6421860395496,-42.5506297036748,-42.462363060118,
-42.3741096695007,-42.2858481872324,-42.1975572680554,-42.109166282462,
-42.0207156941779,-41.9321357694396,-41.9097353525509,-41.7918608832718),
 .UNSPECIFIED.);
#1465=B_SPLINE_CURVE_WITH_KNOTS('',3,(#48180,#48181,#48182,#48183,#48184,
#48185,#48186,#48187,#48188,#48189,#48190,#48191,#48192,#48193,#48194,#48195,
#48196,#48197,#48198,#48199,#48200,#48201,#48202,#48203,#48204,#48205,#48206,
#48207,#48208,#48209,#48210,#48211,#48212,#48213,#48214,#48215,#48216,#48217,
#48218,#48219,#48220,#48221,#48222,#48223,#48224,#48225,#48226,#48227,#48228,
#48229,#48230,#48231,#48232,#48233,#48234,#48235,#48236,#48237,#48238,#48239,
#48240,#48241,#48242,#48243,#48244,#48245,#48246,#48247,#48248,#48249,#48250,
#48251,#48252,#48253,#48254,#48255,#48256,#48257,#48258,#48259,#48260,#48261,
#48262,#48263,#48264,#48265,#48266,#48267,#48268,#48269,#48270,#48271,#48272,
#48273,#48274,#48275,#48276,#48277,#48278,#48279,#48280,#48281,#48282,#48283,
#48284,#48285,#48286,#48287,#48288,#48289,#48290,#48291,#48292,#48293,#48294,
#48295,#48296,#48297,#48298,#48299,#48300,#48301,#48302,#48303,#48304,#48305,
#48306,#48307,#48308,#48309,#48310,#48311,#48312,#48313,#48314,#48315,#48316,
#48317,#48318,#48319,#48320,#48321,#48322,#48323,#48324,#48325,#48326,#48327,
#48328,#48329,#48330,#48331,#48332,#48333,#48334,#48335,#48336,#48337,#48338,
#48339,#48340,#48341,#48342,#48343,#48344,#48345,#48346,#48347,#48348,#48349,
#48350,#48351,#48352,#48353,#48354,#48355,#48356,#48357,#48358,#48359,#48360,
#48361,#48362,#48363,#48364,#48365,#48366,#48367,#48368,#48369,#48370,#48371,
#48372,#48373,#48374,#48375,#48376,#48377,#48378,#48379,#48380,#48381,#48382,
#48383,#48384,#48385,#48386,#48387,#48388,#48389,#48390,#48391,#48392,#48393,
#48394,#48395,#48396,#48397,#48398,#48399,#48400,#48401,#48402,#48403,#48404,
#48405),.UNSPECIFIED.,.F.,.F.,(4,3,3,3,3,3,3,3,3,3,3,3,3,3,3,3,3,3,3,3,
3,3,3,3,3,3,3,3,3,3,3,3,3,3,3,3,3,3,3,3,3,3,3,3,3,3,3,3,3,3,3,3,3,3,3,3,
3,3,3,3,3,3,3,3,3,3,3,3,3,3,3,3,3,3,3,4),(-41.7918608830424,-41.7045602140835,
-41.6173582378056,-41.5291740219328,-41.4420878042718,-41.3550194179906,
-41.2679464495758,-41.1789309648877,-41.0917343408291,-41.0018094258263,
-40.9118845108235,-40.8233113615169,-40.734852568467,-40.6464843560945,
-40.5549280202197,-40.4666613766628,-40.3784079860455,-40.2901465037771,
-40.2018555846003,-40.1134645990068,-40.0250140107226,-39.9364340859844,
-39.9140336690961,-39.8254605197895,-39.7370017267396,-39.648633514367,
-39.5570771784922,-39.4688105349354,-39.380557144318,-39.2922956620497,
-39.2040047428726,-39.1156137572792,-39.0271631689949,-38.9385832442568,
-38.9161828273687,-38.827609678062,-38.7391508850121,-38.6507826726396,
-38.5592263367648,-38.4709596932079,-38.3827063025904,-38.2944448203221,
-38.2061539011448,-38.1177629155512,-38.0293123272669,-37.9407324025286,
-37.9183319856413,-37.8297588363348,-37.7413000432852,-37.6529318309124,
-37.5613754950376,-37.473108851481,-37.3848554608637,-37.2965939785956,
-37.2083030594185,-37.1199120738252,-37.0314614855414,-36.9428815608032,
-36.9204811439139,-36.8319079946071,-36.7434492015572,-36.655080989184,
-36.5635246533093,-36.4752580097524,-36.387004619135,-36.2987431368667,
-36.2104522176887,-36.122061232095,-36.0336106438104,-35.9450307190722,
-35.9226303021865,-35.8250780891462,-35.7279166626066,-35.6310133554249,
-35.53449733819,-35.5086755762787),.UNSPECIFIED.);
#1466=B_SPLINE_CURVE_WITH_KNOTS('',3,(#48407,#48408,#48409,#48410,#48411,
#48412,#48413,#48414,#48415,#48416,#48417,#48418,#48419,#48420,#48421,#48422,
#48423,#48424,#48425,#48426,#48427,#48428,#48429,#48430,#48431,#48432,#48433,
#48434,#48435,#48436,#48437,#48438,#48439,#48440,#48441,#48442,#48443,#48444,
#48445,#48446,#48447,#48448,#48449,#48450,#48451,#48452,#48453,#48454,#48455,
#48456,#48457,#48458,#48459,#48460,#48461,#48462,#48463,#48464,#48465,#48466,
#48467,#48468,#48469,#48470,#48471,#48472,#48473,#48474,#48475,#48476,#48477,
#48478,#48479,#48480,#48481,#48482,#48483,#48484,#48485,#48486,#48487,#48488,
#48489,#48490,#48491,#48492,#48493,#48494,#48495,#48496,#48497,#48498,#48499,
#48500,#48501,#48502,#48503,#48504,#48505,#48506,#48507,#48508,#48509,#48510,
#48511,#48512,#48513,#48514,#48515,#48516,#48517,#48518,#48519,#48520,#48521,
#48522,#48523,#48524,#48525,#48526,#48527,#48528,#48529,#48530,#48531,#48532,
#48533,#48534,#48535,#48536,#48537,#48538,#48539,#48540,#48541,#48542,#48543,
#48544,#48545,#48546,#48547,#48548,#48549,#48550,#48551,#48552,#48553,#48554,
#48555,#48556,#48557,#48558,#48559,#48560,#48561,#48562,#48563,#48564,#48565,
#48566,#48567,#48568,#48569,#48570,#48571,#48572,#48573,#48574,#48575,#48576,
#48577,#48578,#48579,#48580,#48581,#48582,#48583,#48584,#48585,#48586,#48587,
#48588,#48589,#48590,#48591,#48592,#48593,#48594,#48595,#48596,#48597,#48598,
#48599,#48600,#48601,#48602,#48603,#48604,#48605,#48606,#48607,#48608,#48609,
#48610,#48611,#48612,#48613,#48614,#48615,#48616,#48617,#48618,#48619,#48620,
#48621,#48622,#48623,#48624,#48625,#48626,#48627,#48628,#48629,#48630,#48631,
#48632),.UNSPECIFIED.,.F.,.F.,(4,3,3,3,3,3,3,3,3,3,3,3,3,3,3,3,3,3,3,3,
3,3,3,3,3,3,3,3,3,3,3,3,3,3,3,3,3,3,3,3,3,3,3,3,3,3,3,3,3,3,3,3,3,3,3,3,
3,3,3,3,3,3,3,3,3,3,3,3,3,3,3,3,3,3,3,4),(-35.5086755760922,-35.4188811405786,
-35.3290503078016,-35.2391644975997,-35.1491420297501,-35.0590430664914,
-34.9687826180062,-34.9247794604591,-34.8362063111524,-34.7477475181026,
-34.65937930573,-34.5678229698552,-34.4795563262983,-34.3913029356809,-34.3030414534123,
-34.214750534235,-34.1263595486414,-34.0379089603574,-33.949329035619,-33.9269286187317,
-33.8383554694252,-33.7498966763755,-33.6615284640029,-33.5699721281281,
-33.4817054845714,-33.3934520939542,-33.3051906116858,-33.216899692509,
-33.1285087069156,-33.0400581186316,-32.9514781938935,-32.9290777770043,
-32.8405046276976,-32.7520458346479,-32.6636776222752,-32.5721212864004,
-32.4838546428434,-32.3956012522258,-32.3073397699572,-32.2190488507805,
-32.1306578651869,-32.0422072769025,-31.953627352164,-31.9312269352769,
-31.8426537859705,-31.7541949929209,-31.6658267805485,-31.5742704446736,
-31.4860038011169,-31.3977504104998,-31.3094889282317,-31.2211980090548,
-31.1328070234614,-31.0443564351774,-30.9557765104394,-30.9333760935495,
-30.8448029442431,-30.7563441511937,-30.667975938821,-30.5764196029462,
-30.4881529593893,-30.3998995687722,-30.3116380865043,-30.2233471673271,
-30.1349561817338,-30.0465055934498,-29.9579256687117,-29.9355252518221,
-29.8467708789584,-29.7589851521654,-29.6712833639532,-29.5836434327169,
-29.4941051417658,-29.4065070806612,-29.3159986747869,-29.2254902689126),
 .UNSPECIFIED.);
#1467=B_SPLINE_CURVE_WITH_KNOTS('',3,(#48634,#48635,#48636,#48637,#48638,
#48639,#48640,#48641,#48642,#48643,#48644,#48645,#48646,#48647,#48648,#48649,
#48650,#48651,#48652,#48653,#48654,#48655,#48656,#48657,#48658,#48659,#48660,
#48661,#48662,#48663,#48664,#48665,#48666,#48667,#48668,#48669,#48670,#48671,
#48672,#48673,#48674,#48675,#48676,#48677,#48678,#48679,#48680,#48681,#48682,
#48683,#48684,#48685,#48686,#48687,#48688,#48689,#48690,#48691,#48692,#48693,
#48694,#48695,#48696,#48697,#48698,#48699,#48700,#48701,#48702,#48703,#48704,
#48705,#48706,#48707,#48708,#48709,#48710,#48711,#48712,#48713,#48714,#48715,
#48716,#48717,#48718,#48719,#48720,#48721,#48722,#48723,#48724,#48725,#48726,
#48727,#48728,#48729,#48730,#48731,#48732,#48733,#48734,#48735,#48736,#48737,
#48738,#48739,#48740,#48741,#48742,#48743,#48744,#48745,#48746,#48747,#48748,
#48749,#48750,#48751,#48752,#48753,#48754,#48755,#48756,#48757,#48758,#48759,
#48760,#48761,#48762,#48763,#48764,#48765,#48766,#48767,#48768,#48769,#48770,
#48771,#48772,#48773,#48774,#48775,#48776,#48777,#48778,#48779,#48780,#48781,
#48782,#48783,#48784,#48785,#48786,#48787,#48788,#48789,#48790,#48791,#48792,
#48793,#48794,#48795,#48796,#48797,#48798,#48799,#48800,#48801,#48802,#48803,
#48804,#48805,#48806,#48807,#48808,#48809,#48810,#48811,#48812,#48813,#48814,
#48815,#48816,#48817,#48818,#48819,#48820,#48821,#48822,#48823,#48824,#48825,
#48826,#48827,#48828,#48829,#48830,#48831,#48832,#48833,#48834,#48835,#48836,
#48837,#48838,#48839,#48840,#48841,#48842,#48843,#48844,#48845,#48846,#48847,
#48848,#48849,#48850,#48851,#48852,#48853,#48854,#48855,#48856,#48857,#48858,
#48859,#48860,#48861,#48862),.UNSPECIFIED.,.F.,.F.,(4,3,3,3,3,3,3,3,3,3,
3,3,3,3,3,3,3,3,3,3,3,3,3,3,3,3,3,3,3,3,3,3,3,3,3,3,3,3,3,3,3,3,3,3,3,3,
3,3,3,3,3,3,3,3,3,3,3,3,3,3,3,3,3,3,3,3,3,3,3,3,3,3,3,3,3,3,4),(-29.2254902687766,
-29.1178017627057,-29.0085141589372,-28.9376744100947,-28.8491012607896,
-28.7606424677413,-28.6722742553701,-28.5807179194948,-28.4924512759394,
-28.4041978853234,-28.3159364030565,-28.2276454838808,-28.1392544982887,
-28.0508039100057,-27.9622239852688,-27.9398235683673,-27.8512504190617,
-27.7627916260131,-27.6744234136415,-27.5828670777663,-27.4946004342106,
-27.4063470435944,-27.3180855613272,-27.2297946421512,-27.1414036565588,
-27.0529530682758,-26.9643731435387,-26.9419727266399,-26.8533995773247,
-26.7649407842662,-26.676572571885,-26.5850162360134,-26.4967495924479,
-26.408496201822,-26.320234719545,-26.2319438003593,-26.1435528147574,-26.0551022264647,
-25.9665223017182,-25.9441218849125,-25.8555487356216,-25.7670899425876,
-25.6787217302307,-25.58716539435,-25.4988987508086,-25.4106453602066,-25.3223838779536,
-25.2340929587915,-25.1457019732128,-25.0572513849433,-24.9686714602193,
-24.9462710431851,-24.85769789388,-24.7692391008319,-24.680870888461,-24.5893145525856,
-24.5010479090309,-24.4127945184159,-24.3245330361501,-24.2362421169756,
-24.1478511313848,-24.0594005431034,-23.9708206183682,-23.9484202014577,
-23.8598470520801,-23.771388258959,-23.683020046515,-23.5914637106669,-23.5031970670388,
-23.4149436763502,-23.326682194011,-23.2383912747634,-23.1500002891001,
-23.0615497007464,-22.9729697759399,-22.9505693597303,-22.942304961733),
 .UNSPECIFIED.);
#1468=B_SPLINE_CURVE_WITH_KNOTS('',3,(#48864,#48865,#48866,#48867,#48868,
#48869,#48870,#48871,#48872,#48873,#48874,#48875,#48876,#48877,#48878,#48879,
#48880,#48881,#48882,#48883,#48884,#48885,#48886,#48887,#48888,#48889,#48890,
#48891,#48892,#48893,#48894,#48895,#48896,#48897,#48898,#48899,#48900,#48901,
#48902,#48903,#48904,#48905,#48906,#48907,#48908,#48909,#48910,#48911,#48912,
#48913,#48914,#48915,#48916,#48917,#48918,#48919,#48920,#48921,#48922,#48923,
#48924,#48925,#48926,#48927,#48928,#48929,#48930,#48931,#48932,#48933,#48934,
#48935,#48936,#48937,#48938,#48939,#48940,#48941,#48942,#48943,#48944,#48945,
#48946,#48947,#48948,#48949,#48950,#48951,#48952,#48953,#48954,#48955,#48956,
#48957,#48958,#48959,#48960,#48961,#48962,#48963,#48964,#48965,#48966,#48967,
#48968,#48969,#48970,#48971,#48972,#48973,#48974,#48975,#48976,#48977,#48978,
#48979,#48980,#48981,#48982,#48983,#48984,#48985,#48986,#48987,#48988,#48989,
#48990,#48991,#48992,#48993,#48994,#48995,#48996,#48997,#48998,#48999,#49000,
#49001,#49002,#49003,#49004,#49005,#49006,#49007,#49008,#49009,#49010,#49011,
#49012,#49013,#49014,#49015,#49016,#49017,#49018,#49019,#49020,#49021,#49022,
#49023,#49024,#49025,#49026,#49027,#49028,#49029,#49030,#49031,#49032,#49033,
#49034,#49035,#49036,#49037,#49038,#49039,#49040,#49041,#49042,#49043,#49044,
#49045,#49046,#49047,#49048,#49049,#49050,#49051,#49052,#49053,#49054,#49055,
#49056,#49057,#49058,#49059,#49060,#49061,#49062,#49063,#49064,#49065,#49066,
#49067,#49068,#49069,#49070,#49071,#49072,#49073,#49074,#49075,#49076,#49077,
#49078,#49079,#49080,#49081,#49082,#49083,#49084,#49085,#49086,#49087,#49088,
#49089),.UNSPECIFIED.,.F.,.F.,(4,3,3,3,3,3,3,3,3,3,3,3,3,3,3,3,3,3,3,3,
3,3,3,3,3,3,3,3,3,3,3,3,3,3,3,3,3,3,3,3,3,3,3,3,3,3,3,3,3,3,3,3,3,3,3,3,
3,3,3,3,3,3,3,3,3,3,3,3,3,3,3,3,3,3,3,4),(-22.9423049614834,-22.8538617632608,
-22.7655327557495,-22.6772940078544,-22.586722071623,-22.4985834260939,
-22.4104575188324,-22.3223228662375,-22.2299217791788,-22.1416543081962,
-22.0533253302847,-21.9648699208204,-21.9527185180029,-21.864145368657,
-21.7756865755694,-21.6873183631602,-21.5957620272996,-21.5074953837099,
-21.4192419930611,-21.3309805107628,-21.2426895915571,-21.1542986059373,
-21.065848017628,-20.9772680928667,-20.9548676762754,-20.8662945263978,
-20.7778357327747,-20.6894675198275,-20.5979111841676,-20.5096445400355,
-20.4213911488439,-20.3331296660026,-20.2448387462547,-20.1564477600963,
-20.0679971712501,-19.9794172459584,-19.957016834548,-19.8684436866929,
-19.7799848950942,-19.6916166841704,-19.6000603477517,-19.5117937056287,
-19.4235403164372,-19.3352788355856,-19.246987917814,-19.1585969336029,
-19.0701463466892,-18.9815664232938,-18.9591659928206,-18.8705928427052,
-18.7821340488582,-18.6937658357001,-18.6022095001243,-18.5139428558168,
-18.425689464463,-18.337427981473,-18.2491370615898,-18.1607460753165,-18.0722954863675,
-17.9837155609903,-17.9613151510932,-17.8727419973658,-17.7842831998724,
-17.6959149830392,-17.60435864883,-17.5160920007977,-17.4278386057074,-17.3395771189731,
-17.2512861953413,-17.1628952053342,-17.0744446126548,-16.9858646835816,
-16.9634643093658,-16.856206513481,-16.7502366022154,-16.6591196547223),
 .UNSPECIFIED.);
#1469=B_SPLINE_CURVE_WITH_KNOTS('',3,(#49091,#49092,#49093,#49094,#49095,
#49096,#49097,#49098,#49099,#49100,#49101,#49102,#49103,#49104,#49105,#49106,
#49107,#49108,#49109,#49110,#49111,#49112,#49113,#49114,#49115,#49116,#49117,
#49118,#49119,#49120,#49121,#49122,#49123,#49124,#49125,#49126,#49127,#49128,
#49129,#49130,#49131,#49132,#49133,#49134,#49135,#49136,#49137,#49138,#49139,
#49140,#49141,#49142,#49143,#49144,#49145,#49146,#49147,#49148,#49149,#49150,
#49151,#49152,#49153,#49154,#49155,#49156,#49157,#49158,#49159,#49160,#49161,
#49162,#49163,#49164,#49165,#49166,#49167,#49168,#49169,#49170,#49171,#49172,
#49173,#49174,#49175,#49176,#49177,#49178,#49179,#49180,#49181,#49182,#49183,
#49184,#49185,#49186,#49187,#49188,#49189,#49190,#49191,#49192,#49193,#49194,
#49195,#49196,#49197,#49198,#49199,#49200,#49201,#49202,#49203,#49204,#49205,
#49206,#49207,#49208,#49209,#49210,#49211,#49212,#49213,#49214,#49215,#49216,
#49217,#49218,#49219,#49220,#49221,#49222,#49223,#49224,#49225,#49226,#49227,
#49228,#49229,#49230,#49231,#49232,#49233,#49234,#49235,#49236,#49237,#49238,
#49239,#49240,#49241,#49242,#49243,#49244,#49245,#49246,#49247,#49248,#49249,
#49250,#49251,#49252,#49253,#49254,#49255,#49256,#49257,#49258,#49259,#49260,
#49261,#49262,#49263,#49264,#49265,#49266,#49267,#49268,#49269,#49270,#49271,
#49272,#49273,#49274,#49275,#49276,#49277,#49278,#49279,#49280,#49281,#49282,
#49283,#49284,#49285,#49286,#49287,#49288,#49289,#49290,#49291,#49292,#49293,
#49294,#49295,#49296,#49297,#49298,#49299,#49300,#49301,#49302,#49303,#49304,
#49305,#49306,#49307,#49308,#49309,#49310,#49311,#49312,#49313,#49314,#49315,
#49316),.UNSPECIFIED.,.F.,.F.,(4,3,3,3,3,3,3,3,3,3,3,3,3,3,3,3,3,3,3,3,
3,3,3,3,3,3,3,3,3,3,3,3,3,3,3,3,3,3,3,3,3,3,3,3,3,3,3,3,3,3,3,3,3,3,3,3,
3,3,3,3,3,3,3,3,3,3,3,3,3,3,3,3,3,3,3,4),(-16.6591196545534,-16.5712935284758,
-16.4834950042179,-16.3957022954975,-16.3078936252478,-16.2199901013344,
-16.1320383660111,-16.0439386197209,-15.9656134676384,-15.8770403071815,
-15.7885815030742,-15.700213279748,-15.6086569480184,-15.520390293833,-15.4321368927246,
-15.3438754001135,-15.2555844707522,-15.1671934752597,-15.0787428772304,
-14.9901629430461,-14.967762625911,-14.8791894440136,-14.7907306181554,
-14.7023623727974,-14.6108060492207,-14.5225393724502,-14.4342859485921,
-14.3460244330919,-14.257733480728,-14.1693424621828,-14.0808918410441,
-13.992311883847,-13.9699117841836,-13.8813387560594,-13.7928800842836,
-13.7045119931345,-13.6129556117997,-13.5246890885827,-13.4364358177753,
-13.3481744546603,-13.2598836538524,-13.1714927848746,-13.0830423123262,
-12.9944625011488,-12.9720609424562,-12.8834876608346,-12.7950287362,-12.7066603931155,
-12.6151041065671,-12.5268373352663,-12.4385838182129,-12.350322210946,
-12.2620311683396,-12.1736400622478,-12.0851893550264,-11.9966093145385,
-11.9742101007288,-11.8856367279759,-11.7971777094444,-11.7088092698459,
-11.6172530184903,-11.5289861448337,-11.4407325234554,-11.3524708100167,
-11.2641796595118,-11.1757884435396,-11.0873376251498,-10.9987574724895,
-10.9763592590014,-10.8865298425373,-10.7968247825165,-10.7072244088575,
-10.6177240485907,-10.5282826535782,-10.4388779894314,-10.3759343473738),
 .UNSPECIFIED.);
#1470=B_SPLINE_CURVE_WITH_KNOTS('',3,(#49317,#49318,#49319,#49320,#49321,
#49322,#49323,#49324,#49325,#49326,#49327,#49328,#49329,#49330,#49331,#49332,
#49333,#49334,#49335,#49336,#49337,#49338,#49339,#49340,#49341,#49342,#49343,
#49344,#49345,#49346,#49347,#49348,#49349,#49350,#49351,#49352,#49353,#49354,
#49355,#49356,#49357,#49358,#49359,#49360,#49361,#49362,#49363,#49364,#49365,
#49366,#49367,#49368,#49369,#49370,#49371,#49372,#49373,#49374,#49375,#49376,
#49377,#49378,#49379,#49380,#49381,#49382,#49383,#49384,#49385,#49386,#49387,
#49388,#49389,#49390,#49391,#49392,#49393,#49394,#49395,#49396,#49397,#49398,
#49399,#49400,#49401,#49402,#49403,#49404,#49405,#49406,#49407,#49408,#49409,
#49410,#49411,#49412,#49413,#49414,#49415,#49416,#49417,#49418,#49419,#49420,
#49421,#49422,#49423,#49424,#49425,#49426,#49427,#49428,#49429,#49430,#49431,
#49432,#49433,#49434,#49435,#49436,#49437,#49438,#49439,#49440,#49441,#49442,
#49443,#49444,#49445,#49446,#49447,#49448,#49449,#49450,#49451,#49452,#49453,
#49454,#49455,#49456,#49457,#49458,#49459,#49460,#49461,#49462,#49463,#49464,
#49465,#49466,#49467,#49468,#49469,#49470,#49471,#49472,#49473,#49474,#49475,
#49476,#49477,#49478,#49479,#49480,#49481,#49482,#49483,#49484,#49485,#49486,
#49487,#49488,#49489,#49490,#49491,#49492,#49493,#49494,#49495,#49496,#49497,
#49498,#49499,#49500,#49501,#49502,#49503,#49504,#49505,#49506,#49507,#49508,
#49509,#49510,#49511,#49512,#49513,#49514,#49515,#49516,#49517,#49518,#49519,
#49520,#49521,#49522,#49523,#49524,#49525,#49526,#49527,#49528,#49529,#49530,
#49531,#49532,#49533,#49534,#49535,#49536,#49537,#49538,#49539,#49540,#49541,
#49542),.UNSPECIFIED.,.F.,.F.,(4,3,3,3,3,3,3,3,3,3,3,3,3,3,3,3,3,3,3,3,
3,3,3,3,3,3,3,3,3,3,3,3,3,3,3,3,3,3,3,3,3,3,3,3,3,3,3,3,3,3,3,3,3,3,3,3,
3,3,3,3,3,3,3,3,3,3,3,3,3,3,3,3,3,3,3,4),(-10.3759343471667,-10.2765778646935,
-10.1785460227179,-10.078527219996,-9.97850841727403,-9.88993382098927,
-9.80147358648194,-9.71310393977095,-9.62154814424291,-9.53328009285517,
-9.44502530654547,-9.356762442169,-9.26847015592512,-9.18007783230482,-9.0916259212877,
-9.00304470626163,-8.98065757554662,-8.89208307541407,-8.80362291295577,
-8.7152533144443,-8.62369749186617,-8.53542942965111,-8.44717461086563,
-8.35891169250639,-8.27061933089823,-8.18222690092591,-8.09377486537985,
-8.0051935004333,-7.98280673381922,-7.89424283763284,-7.80579331569487,
-7.71743438141468,-7.62587457024933,-7.53761716398574,-7.44937297991607,
-7.36112066369019,-7.27283886025113,-7.18445687012472,-7.0960152181745,
-7.00744407462594,-6.98495589209182,-6.89636773805667,-6.80789397960917,
-6.71951085805653,-6.62796013209501,-6.53967881125381,-6.45141085365402,
-6.36313492991273,-6.27482971008726,-6.18642470340815,-6.09796023994667,
-6.00936675923615,-5.98710505036441,-5.89852582996034,-5.81006079982164,
-5.72168619395215,-5.63013219578775,-5.54185881368928,-5.45359856941143,
-5.36533012633129,-5.27703214708557,-5.18863399181092,-5.10017616132864,
-5.01158894546892,-4.98925420863701,-4.90186357593316,-4.8145865543858,
-4.72435686514095,-4.63723281771054,-4.55013980149263,-4.46305541288891,
-4.37595725988714,-4.28877946463819,-4.20155379976352,-4.11421368393324,
-4.09274904042707),.UNSPECIFIED.);
#1471=B_SPLINE_CURVE_WITH_KNOTS('',3,(#49545,#49546,#49547,#49548,#49549,
#49550,#49551,#49552,#49553,#49554,#49555,#49556,#49557,#49558,#49559,#49560,
#49561,#49562,#49563,#49564,#49565,#49566,#49567,#49568,#49569,#49570,#49571,
#49572,#49573,#49574,#49575,#49576,#49577,#49578,#49579,#49580,#49581,#49582,
#49583,#49584,#49585,#49586,#49587,#49588,#49589,#49590,#49591,#49592,#49593,
#49594,#49595,#49596,#49597,#49598,#49599,#49600,#49601,#49602,#49603,#49604,
#49605,#49606,#49607,#49608,#49609,#49610,#49611,#49612,#49613,#49614,#49615,
#49616,#49617,#49618,#49619,#49620,#49621,#49622,#49623,#49624,#49625,#49626,
#49627,#49628,#49629,#49630,#49631,#49632,#49633,#49634,#49635,#49636,#49637,
#49638,#49639,#49640,#49641,#49642,#49643,#49644,#49645,#49646,#49647,#49648,
#49649,#49650,#49651,#49652,#49653,#49654,#49655,#49656,#49657,#49658,#49659,
#49660,#49661,#49662,#49663,#49664,#49665,#49666,#49667,#49668,#49669,#49670,
#49671,#49672,#49673,#49674,#49675,#49676,#49677,#49678,#49679,#49680,#49681,
#49682,#49683,#49684,#49685,#49686,#49687,#49688,#49689,#49690,#49691,#49692,
#49693,#49694,#49695,#49696,#49697,#49698,#49699,#49700,#49701,#49702,#49703,
#49704,#49705,#49706),.UNSPECIFIED.,.F.,.F.,(4,2,2,2,2,2,2,2,2,2,2,2,2,
2,2,2,2,2,2,2,2,2,2,2,2,2,2,2,2,2,2,2,2,2,2,2,2,2,2,2,2,2,2,2,2,2,2,2,2,
2,2,2,2,2,2,2,2,2,2,2,2,2,2,2,2,2,2,2,2,2,2,2,2,2,2,2,2,2,2,2,4),(0.00572882946113452,
0.0858386630726596,0.128530379570816,0.137096238848039,0.141978642636408,
0.146211956682032,0.151420454865605,0.159390663536531,0.202369071154075,
0.284374251605654,0.291998189895998,0.297842832080111,0.30076460715983,
0.300782700221492,0.300801156447523,0.300819988452636,0.300839209400581,
0.300858833374834,0.300878875067341,0.300899349764534,0.300920273768506,
0.30094166412418,0.300963538183928,0.300985914819345,0.301008813921572,
0.303334801482,0.306215030609676,0.311717802906198,0.34956040350371,0.406195092989925,
0.433847186656547,0.451856562766573,0.458370988167906,0.462800764011346,
0.467118672123479,0.473289241546835,0.484640963324567,0.547060728319788,
0.608701862231486,0.618469998357093,0.622076456951003,0.624532691107509,
0.626740828914197,0.629788136753773,0.63754739348344,0.69974886415569,0.747007760150307,
0.764006113963808,0.776517543366181,0.782137357791307,0.786367015930682,
0.79090932885459,0.798106135295086,0.820064585285403,0.918326337184996,
0.932306484492328,0.94155550709373,0.945064879357327,0.947486494283003,
0.949713163098311,0.952816722292652,0.9609201408115,1.01180389452782,1.05675228723629,
1.09396577086912,1.10220036045524,1.10698869991128,1.11119611958505,1.11644450890454,
1.12461079772995,1.17366338651836,1.20360532452736,1.25913975687919,1.26508690319042,
1.2680420026153,1.27017188826653,1.27290945616808,1.27769552544157,1.29786694630185,
1.36971036920056,1.36986813415593),.UNSPECIFIED.);
#1472=B_SPLINE_CURVE_WITH_KNOTS('',3,(#49710,#49711,#49712,#49713,#49714,
#49715,#49716,#49717,#49718,#49719,#49720,#49721,#49722,#49723,#49724,#49725,
#49726,#49727,#49728,#49729,#49730,#49731,#49732,#49733,#49734,#49735,#49736,
#49737,#49738,#49739,#49740),.UNSPECIFIED.,.F.,.F.,(4,3,3,3,3,3,3,3,3,3,
4),(135.088484104672,135.18316969008,135.277709840149,135.372951171501,
135.46726055986,135.561508187356,135.655716424704,135.751697441269,135.845921119761,
135.942780805363,136.039640490965),.UNSPECIFIED.);
#1473=B_SPLINE_CURVE_WITH_KNOTS('',3,(#49741,#49742,#49743,#49744,#49745,
#49746,#49747,#49748,#49749,#49750,#49751,#49752,#49753,#49754,#49755,#49756,
#49757,#49758,#49759,#49760,#49761,#49762,#49763,#49764,#49765,#49766,#49767,
#49768,#49769,#49770,#49771,#49772,#49773,#49774,#49775,#49776,#49777,#49778,
#49779,#49780,#49781,#49782,#49783,#49784,#49785,#49786,#49787,#49788,#49789,
#49790,#49791,#49792,#49793,#49794,#49795,#49796,#49797,#49798,#49799,#49800,
#49801,#49802,#49803,#49804,#49805,#49806,#49807,#49808,#49809,#49810,#49811,
#49812,#49813),.UNSPECIFIED.,.F.,.F.,(4,3,3,3,3,3,3,3,3,3,3,3,3,3,3,3,3,
3,3,3,3,3,3,3,4),(133.042160362488,133.046087965783,133.139181123038,133.232150309801,
133.325023106835,133.41783094323,133.510605411329,133.603371293728,133.69615335931,
133.789036617055,133.881973115032,133.97506575282,134.043938807511,134.136312444951,
134.228560254826,134.320710715063,134.41279766222,134.504852253225,134.596900055539,
134.688966624987,134.781142826853,134.873375725362,134.965777975913,135.041789649238,
135.088484104361),.UNSPECIFIED.);
#1474=B_SPLINE_CURVE_WITH_KNOTS('',3,(#50338,#50339,#50340,#50341,#50342,
#50343,#50344,#50345,#50346,#50347,#50348,#50349,#50350,#50351,#50352,#50353,
#50354,#50355,#50356,#50357,#50358,#50359,#50360,#50361,#50362,#50363,#50364,
#50365,#50366,#50367,#50368,#50369,#50370,#50371,#50372,#50373,#50374,#50375,
#50376,#50377,#50378,#50379,#50380,#50381,#50382,#50383,#50384,#50385,#50386,
#50387,#50388,#50389,#50390,#50391,#50392,#50393,#50394,#50395,#50396,#50397,
#50398,#50399,#50400,#50401,#50402,#50403,#50404,#50405,#50406,#50407,#50408,
#50409,#50410,#50411,#50412,#50413,#50414,#50415,#50416,#50417,#50418,#50419,
#50420,#50421,#50422,#50423,#50424,#50425,#50426,#50427,#50428,#50429,#50430,
#50431,#50432,#50433,#50434),.UNSPECIFIED.,.F.,.F.,(4,3,3,3,3,3,3,3,3,3,
3,3,3,3,3,3,3,3,3,3,3,3,3,3,3,3,3,3,3,3,3,3,4),(0.,0.0258260740408245,0.0620924490441423,
0.0993874343281711,0.1366824196122,0.147698904723131,0.154011882090748,
0.189860980974716,0.225553852485871,0.260975001327923,0.278622120241529,
0.288544671238274,0.295091750966326,0.299504106250136,0.334017275552874,
0.368084614094821,0.402151952636769,0.423542327420144,0.431067342396322,
0.436302863184041,0.441119634191273,0.474541969017029,0.508522660804976,
0.54221649566577,0.567489177353895,0.575255797857681,0.608314732463416,
0.642335536640254,0.657701460359135,0.662771582070671,0.694603710062296,
0.725562408530676,0.744397949170667),.UNSPECIFIED.);
#1475=B_SPLINE_CURVE_WITH_KNOTS('',3,(#50435,#50436,#50437,#50438,#50439,
#50440,#50441,#50442,#50443,#50444,#50445,#50446,#50447,#50448,#50449,#50450,
#50451,#50452,#50453,#50454,#50455,#50456,#50457,#50458,#50459,#50460,#50461,
#50462,#50463,#50464,#50465,#50466,#50467,#50468,#50469,#50470,#50471,#50472,
#50473,#50474,#50475,#50476,#50477,#50478,#50479,#50480,#50481,#50482,#50483,
#50484,#50485,#50486,#50487,#50488,#50489,#50490,#50491,#50492,#50493,#50494,
#50495,#50496,#50497,#50498,#50499,#50500,#50501,#50502,#50503,#50504,#50505,
#50506,#50507,#50508,#50509,#50510,#50511,#50512,#50513,#50514,#50515,#50516,
#50517,#50518,#50519,#50520,#50521,#50522,#50523,#50524,#50525,#50526,#50527,
#50528),.UNSPECIFIED.,.F.,.F.,(4,3,3,3,3,3,3,3,3,3,3,3,3,3,3,3,3,3,3,3,
3,3,3,3,3,3,3,3,3,3,3,4),(0.,0.02133074521375,0.0521058403411437,0.0836372654726391,
0.115777344688116,0.125964402355647,0.130783277975323,0.163735803941014,
0.196688329906704,0.230204779895922,0.2470278046079,0.259364835821699,0.264033725823834,
0.298484782009355,0.332689762691114,0.364788977591745,0.388319089517656,
0.39509149622043,0.401763599284906,0.435343669494579,0.46974042676872,0.504994131658741,
0.534528711252189,0.540952849586392,0.546662686863921,0.582645576684806,
0.61886768806574,0.635179337184303,0.644573291322463,0.681413951419206,
0.717770742894507,0.741270768406323),.UNSPECIFIED.);
#1476=B_SPLINE_CURVE_WITH_KNOTS('',3,(#51054,#51055,#51056,#51057,#51058,
#51059,#51060,#51061,#51062,#51063,#51064,#51065,#51066,#51067,#51068,#51069,
#51070,#51071,#51072,#51073,#51074,#51075,#51076,#51077,#51078,#51079,#51080,
#51081,#51082,#51083,#51084,#51085,#51086,#51087,#51088,#51089,#51090,#51091,
#51092,#51093,#51094,#51095,#51096,#51097,#51098,#51099,#51100,#51101,#51102,
#51103,#51104,#51105,#51106,#51107,#51108,#51109,#51110,#51111,#51112,#51113,
#51114,#51115,#51116,#51117,#51118,#51119,#51120,#51121,#51122,#51123,#51124,
#51125,#51126,#51127,#51128,#51129,#51130,#51131,#51132,#51133,#51134,#51135,
#51136,#51137,#51138,#51139,#51140,#51141,#51142,#51143,#51144,#51145,#51146,
#51147),.UNSPECIFIED.,.F.,.F.,(4,3,3,3,3,3,3,3,3,3,3,3,3,3,3,3,3,3,3,3,
3,3,3,3,3,3,3,3,3,3,3,4),(0.,0.0213307452137482,0.0521058429544939,0.0836372697852673,
0.115777349637711,0.125964407042121,0.130783279244603,0.163312913916928,
0.196758848298764,0.2302047826806,0.247027807044509,0.259364835465739,0.264033725682642,
0.298484781608584,0.332689762447923,0.364788977591868,0.388319089517784,
0.395091496414565,0.401763599093259,0.435752013864845,0.469740428636431,
0.504994134467813,0.534528713710151,0.540952860096086,0.546662689054415,
0.582787099736608,0.618867691358632,0.635179341901767,0.644573290300076,
0.681413950020179,0.717770738127119,0.741270768406402),.UNSPECIFIED.);
#1477=B_SPLINE_CURVE_WITH_KNOTS('',3,(#51148,#51149,#51150,#51151),
 .UNSPECIFIED.,.F.,.F.,(4,4),(0.,0.0148373890450924),.UNSPECIFIED.);
#1478=B_SPLINE_CURVE_WITH_KNOTS('',3,(#51152,#51153,#51154,#51155,#51156,
#51157,#51158,#51159,#51160,#51161,#51162,#51163,#51164,#51165,#51166,#51167,
#51168,#51169,#51170,#51171,#51172,#51173,#51174,#51175,#51176,#51177,#51178,
#51179,#51180,#51181,#51182,#51183,#51184,#51185,#51186,#51187,#51188,#51189,
#51190,#51191,#51192,#51193,#51194,#51195,#51196,#51197,#51198,#51199,#51200,
#51201,#51202,#51203,#51204,#51205,#51206,#51207,#51208,#51209,#51210,#51211,
#51212,#51213,#51214,#51215,#51216,#51217,#51218,#51219,#51220,#51221,#51222,
#51223,#51224,#51225,#51226,#51227,#51228,#51229,#51230,#51231,#51232,#51233,
#51234,#51235,#51236,#51237,#51238,#51239,#51240,#51241,#51242,#51243,#51244,
#51245,#51246,#51247,#51248),.UNSPECIFIED.,.F.,.F.,(4,3,3,3,3,3,3,3,3,3,
3,3,3,3,3,3,3,3,3,3,3,3,3,3,3,3,3,3,3,3,3,3,4),(0.,0.0258260740408234,0.0622921374233043,
0.0987582008057851,0.136682419784644,0.147698905558292,0.154011882323251,
0.189890297854231,0.2256941807755,0.260975004111818,0.278622122677423,0.288544677172356,
0.295091839955112,0.299504264726676,0.334017433622103,0.368084693129378,
0.402151952636654,0.423542327420026,0.431067342051171,0.436302864295339,
0.441119634363373,0.474541971383567,0.508522662666217,0.542216494901936,
0.567489176685521,0.575255797837762,0.608314730465952,0.642335535142118,
0.657701457701357,0.662771579392012,0.694603703469968,0.725562396845423,
0.744397949170615),.UNSPECIFIED.);
#1774=VERTEX_POINT('',#31901);
#1775=VERTEX_POINT('',#31902);
#1776=VERTEX_POINT('',#31904);
#1777=VERTEX_POINT('',#32014);
#1778=VERTEX_POINT('',#32093);
#1779=VERTEX_POINT('',#32094);
#1780=VERTEX_POINT('',#32096);
#1781=VERTEX_POINT('',#32525);
#1782=VERTEX_POINT('',#32526);
#1783=VERTEX_POINT('',#32744);
#1784=VERTEX_POINT('',#32994);
#1785=VERTEX_POINT('',#32995);
#1786=VERTEX_POINT('',#32997);
#1787=VERTEX_POINT('',#33437);
#1788=VERTEX_POINT('',#33438);
#1789=VERTEX_POINT('',#33658);
#1790=VERTEX_POINT('',#33896);
#1791=VERTEX_POINT('',#33897);
#1792=VERTEX_POINT('',#33899);
#1793=VERTEX_POINT('',#34347);
#1794=VERTEX_POINT('',#34348);
#1795=VERTEX_POINT('',#34566);
#1796=VERTEX_POINT('',#34782);
#1797=VERTEX_POINT('',#34783);
#1798=VERTEX_POINT('',#34785);
#1799=VERTEX_POINT('',#35229);
#1800=VERTEX_POINT('',#35230);
#1801=VERTEX_POINT('',#35452);
#1802=VERTEX_POINT('',#35664);
#1803=VERTEX_POINT('',#35665);
#1804=VERTEX_POINT('',#35667);
#1805=VERTEX_POINT('',#36107);
#1806=VERTEX_POINT('',#36108);
#1807=VERTEX_POINT('',#36320);
#1808=VERTEX_POINT('',#36548);
#1809=VERTEX_POINT('',#36549);
#1810=VERTEX_POINT('',#36551);
#1811=VERTEX_POINT('',#37011);
#1812=VERTEX_POINT('',#37012);
#1813=VERTEX_POINT('',#37222);
#1814=VERTEX_POINT('',#37482);
#1815=VERTEX_POINT('',#37483);
#1816=VERTEX_POINT('',#37485);
#1817=VERTEX_POINT('',#37925);
#1818=VERTEX_POINT('',#37926);
#1819=VERTEX_POINT('',#38140);
#1820=VERTEX_POINT('',#38368);
#1821=VERTEX_POINT('',#38369);
#1822=VERTEX_POINT('',#38371);
#1823=VERTEX_POINT('',#38835);
#1824=VERTEX_POINT('',#38836);
#1825=VERTEX_POINT('',#39060);
#1826=VERTEX_POINT('',#39296);
#1827=VERTEX_POINT('',#39297);
#1828=VERTEX_POINT('',#39299);
#1829=VERTEX_POINT('',#39735);
#1830=VERTEX_POINT('',#39736);
#1831=VERTEX_POINT('',#39958);
#1832=VERTEX_POINT('',#40179);
#1833=VERTEX_POINT('',#40180);
#1834=VERTEX_POINT('',#40182);
#1835=VERTEX_POINT('',#40392);
#1836=VERTEX_POINT('',#40618);
#1837=VERTEX_POINT('',#40619);
#1838=VERTEX_POINT('',#40693);
#1839=VERTEX_POINT('',#40695);
#1840=VERTEX_POINT('',#40701);
#1841=VERTEX_POINT('',#40931);
#1842=VERTEX_POINT('',#41158);
#1843=VERTEX_POINT('',#41388);
#1844=VERTEX_POINT('',#41615);
#1845=VERTEX_POINT('',#41842);
#1846=VERTEX_POINT('',#42069);
#1847=VERTEX_POINT('',#42296);
#1848=VERTEX_POINT('',#42526);
#1849=VERTEX_POINT('',#42753);
#1850=VERTEX_POINT('',#42980);
#1851=VERTEX_POINT('',#43207);
#1852=VERTEX_POINT('',#43434);
#1853=VERTEX_POINT('',#43661);
#1854=VERTEX_POINT('',#43891);
#1855=VERTEX_POINT('',#44121);
#1856=VERTEX_POINT('',#44348);
#1857=VERTEX_POINT('',#44575);
#1858=VERTEX_POINT('',#44802);
#1859=VERTEX_POINT('',#45029);
#1860=VERTEX_POINT('',#45217);
#1861=VERTEX_POINT('',#45219);
#1862=VERTEX_POINT('',#45228);
#1863=VERTEX_POINT('',#45455);
#1864=VERTEX_POINT('',#45682);
#1865=VERTEX_POINT('',#45906);
#1866=VERTEX_POINT('',#46133);
#1867=VERTEX_POINT('',#46360);
#1868=VERTEX_POINT('',#46590);
#1869=VERTEX_POINT('',#46817);
#1870=VERTEX_POINT('',#47044);
#1871=VERTEX_POINT('',#47271);
#1872=VERTEX_POINT('',#47498);
#1873=VERTEX_POINT('',#47725);
#1874=VERTEX_POINT('',#47952);
#1875=VERTEX_POINT('',#48179);
#1876=VERTEX_POINT('',#48406);
#1877=VERTEX_POINT('',#48633);
#1878=VERTEX_POINT('',#48863);
#1879=VERTEX_POINT('',#49090);
#1880=VERTEX_POINT('',#49544);
#1881=VERTEX_POINT('',#49707);
#1882=VERTEX_POINT('',#49709);
#1883=VERTEX_POINT('',#51053);
#2371=EDGE_CURVE('',#1774,#1775,#852,.T.);
#2372=EDGE_CURVE('',#1776,#1774,#1369,.T.);
#2373=EDGE_CURVE('',#1777,#1776,#653,.T.);
#2374=EDGE_CURVE('',#1777,#1775,#1370,.T.);
#2375=EDGE_CURVE('',#1778,#1779,#853,.T.);
#2376=EDGE_CURVE('',#1780,#1778,#1371,.F.);
#2377=EDGE_CURVE('',#1774,#1780,#1372,.T.);
#2378=EDGE_CURVE('',#1775,#1779,#1373,.T.);
#2379=EDGE_CURVE('',#1781,#1782,#854,.T.);
#2380=EDGE_CURVE('',#1778,#1781,#1374,.F.);
#2381=EDGE_CURVE('',#1779,#1783,#1375,.T.);
#2382=EDGE_CURVE('',#1783,#1782,#1376,.T.);
#2383=EDGE_CURVE('',#1784,#1785,#855,.T.);
#2384=EDGE_CURVE('',#1786,#1784,#1377,.F.);
#2385=EDGE_CURVE('',#1781,#1786,#1378,.F.);
#2386=EDGE_CURVE('',#1782,#1785,#1379,.T.);
#2387=EDGE_CURVE('',#1787,#1788,#856,.T.);
#2388=EDGE_CURVE('',#1784,#1787,#1380,.F.);
#2389=EDGE_CURVE('',#1785,#1789,#1381,.T.);
#2390=EDGE_CURVE('',#1789,#1788,#1382,.T.);
#2391=EDGE_CURVE('',#1790,#1791,#857,.T.);
#2392=EDGE_CURVE('',#1792,#1790,#1383,.F.);
#2393=EDGE_CURVE('',#1787,#1792,#1384,.F.);
#2394=EDGE_CURVE('',#1788,#1791,#1385,.T.);
#2395=EDGE_CURVE('',#1793,#1794,#858,.T.);
#2396=EDGE_CURVE('',#1790,#1793,#1386,.F.);
#2397=EDGE_CURVE('',#1791,#1795,#1387,.T.);
#2398=EDGE_CURVE('',#1795,#1794,#1388,.T.);
#2399=EDGE_CURVE('',#1796,#1797,#859,.T.);
#2400=EDGE_CURVE('',#1798,#1796,#1389,.F.);
#2401=EDGE_CURVE('',#1793,#1798,#1390,.F.);
#2402=EDGE_CURVE('',#1794,#1797,#1391,.T.);
#2403=EDGE_CURVE('',#1799,#1800,#860,.T.);
#2404=EDGE_CURVE('',#1796,#1799,#1392,.F.);
#2405=EDGE_CURVE('',#1797,#1801,#1393,.T.);
#2406=EDGE_CURVE('',#1801,#1800,#1394,.T.);
#2407=EDGE_CURVE('',#1802,#1803,#861,.T.);
#2408=EDGE_CURVE('',#1804,#1802,#1395,.F.);
#2409=EDGE_CURVE('',#1799,#1804,#1396,.F.);
#2410=EDGE_CURVE('',#1800,#1803,#1397,.T.);
#2411=EDGE_CURVE('',#1805,#1806,#862,.T.);
#2412=EDGE_CURVE('',#1802,#1805,#1398,.F.);
#2413=EDGE_CURVE('',#1803,#1807,#1399,.T.);
#2414=EDGE_CURVE('',#1807,#1806,#1400,.T.);
#2415=EDGE_CURVE('',#1808,#1809,#863,.T.);
#2416=EDGE_CURVE('',#1810,#1808,#1401,.F.);
#2417=EDGE_CURVE('',#1805,#1810,#1402,.F.);
#2418=EDGE_CURVE('',#1806,#1809,#1403,.T.);
#2419=EDGE_CURVE('',#1811,#1812,#864,.T.);
#2420=EDGE_CURVE('',#1808,#1811,#1404,.F.);
#2421=EDGE_CURVE('',#1809,#1813,#1405,.T.);
#2422=EDGE_CURVE('',#1813,#1812,#1406,.T.);
#2423=EDGE_CURVE('',#1814,#1815,#865,.T.);
#2424=EDGE_CURVE('',#1816,#1814,#1407,.F.);
#2425=EDGE_CURVE('',#1811,#1816,#1408,.F.);
#2426=EDGE_CURVE('',#1812,#1815,#1409,.T.);
#2427=EDGE_CURVE('',#1817,#1818,#866,.T.);
#2428=EDGE_CURVE('',#1814,#1817,#1410,.F.);
#2429=EDGE_CURVE('',#1815,#1819,#1411,.T.);
#2430=EDGE_CURVE('',#1819,#1818,#1412,.T.);
#2431=EDGE_CURVE('',#1820,#1821,#867,.T.);
#2432=EDGE_CURVE('',#1822,#1820,#1413,.F.);
#2433=EDGE_CURVE('',#1817,#1822,#1414,.F.);
#2434=EDGE_CURVE('',#1818,#1821,#1415,.T.);
#2435=EDGE_CURVE('',#1823,#1824,#868,.T.);
#2436=EDGE_CURVE('',#1820,#1823,#1416,.F.);
#2437=EDGE_CURVE('',#1821,#1825,#1417,.T.);
#2438=EDGE_CURVE('',#1825,#1824,#1418,.T.);
#2439=EDGE_CURVE('',#1826,#1827,#869,.T.);
#2440=EDGE_CURVE('',#1828,#1826,#1419,.F.);
#2441=EDGE_CURVE('',#1823,#1828,#1420,.F.);
#2442=EDGE_CURVE('',#1824,#1827,#1421,.T.);
#2443=EDGE_CURVE('',#1829,#1830,#870,.T.);
#2444=EDGE_CURVE('',#1826,#1829,#1422,.F.);
#2445=EDGE_CURVE('',#1827,#1831,#1423,.T.);
#2446=EDGE_CURVE('',#1831,#1830,#1424,.T.);
#2447=EDGE_CURVE('',#1832,#1833,#871,.T.);
#2448=EDGE_CURVE('',#1834,#1832,#1425,.T.);
#2449=EDGE_CURVE('',#1829,#1834,#1426,.F.);
#2450=EDGE_CURVE('',#1830,#1835,#1427,.T.);
#2451=EDGE_CURVE('',#1835,#1833,#1428,.F.);
#2452=EDGE_CURVE('',#1836,#1837,#1429,.T.);
#2453=EDGE_CURVE('',#1838,#1837,#654,.F.);
#2454=EDGE_CURVE('',#1838,#1839,#1430,.T.);
#2455=EDGE_CURVE('',#1839,#1840,#1431,.T.);
#2456=EDGE_CURVE('',#1840,#1841,#1432,.T.);
#2457=EDGE_CURVE('',#1841,#1842,#1433,.T.);
#2458=EDGE_CURVE('',#1842,#1843,#1434,.T.);
#2459=EDGE_CURVE('',#1843,#1844,#1435,.T.);
#2460=EDGE_CURVE('',#1844,#1845,#1436,.T.);
#2461=EDGE_CURVE('',#1845,#1846,#1437,.T.);
#2462=EDGE_CURVE('',#1846,#1847,#1438,.T.);
#2463=EDGE_CURVE('',#1847,#1848,#1439,.T.);
#2464=EDGE_CURVE('',#1848,#1849,#1440,.T.);
#2465=EDGE_CURVE('',#1849,#1850,#1441,.T.);
#2466=EDGE_CURVE('',#1850,#1851,#1442,.T.);
#2467=EDGE_CURVE('',#1851,#1852,#1443,.T.);
#2468=EDGE_CURVE('',#1852,#1853,#1444,.T.);
#2469=EDGE_CURVE('',#1853,#1854,#1445,.T.);
#2470=EDGE_CURVE('',#1854,#1855,#1446,.T.);
#2471=EDGE_CURVE('',#1855,#1856,#1447,.T.);
#2472=EDGE_CURVE('',#1856,#1857,#1448,.T.);
#2473=EDGE_CURVE('',#1857,#1858,#1449,.T.);
#2474=EDGE_CURVE('',#1858,#1859,#1450,.T.);
#2475=EDGE_CURVE('',#1860,#1859,#655,.T.);
#2476=EDGE_CURVE('',#1860,#1861,#1451,.T.);
#2477=EDGE_CURVE('',#1861,#1862,#1452,.T.);
#2478=EDGE_CURVE('',#1862,#1863,#1453,.T.);
#2479=EDGE_CURVE('',#1863,#1864,#1454,.T.);
#2480=EDGE_CURVE('',#1864,#1865,#1455,.T.);
#2481=EDGE_CURVE('',#1865,#1866,#1456,.T.);
#2482=EDGE_CURVE('',#1866,#1867,#1457,.T.);
#2483=EDGE_CURVE('',#1867,#1868,#1458,.T.);
#2484=EDGE_CURVE('',#1868,#1869,#1459,.T.);
#2485=EDGE_CURVE('',#1869,#1870,#1460,.T.);
#2486=EDGE_CURVE('',#1870,#1871,#1461,.T.);
#2487=EDGE_CURVE('',#1871,#1872,#1462,.T.);
#2488=EDGE_CURVE('',#1872,#1873,#1463,.T.);
#2489=EDGE_CURVE('',#1873,#1874,#1464,.T.);
#2490=EDGE_CURVE('',#1874,#1875,#1465,.T.);
#2491=EDGE_CURVE('',#1875,#1876,#1466,.T.);
#2492=EDGE_CURVE('',#1876,#1877,#1467,.T.);
#2493=EDGE_CURVE('',#1877,#1878,#1468,.T.);
#2494=EDGE_CURVE('',#1878,#1879,#1469,.T.);
#2495=EDGE_CURVE('',#1879,#1836,#1470,.T.);
#2496=EDGE_CURVE('',#1833,#1880,#1471,.F.);
#2497=EDGE_CURVE('',#1881,#1880,#656,.T.);
#2498=EDGE_CURVE('',#1882,#1881,#1472,.T.);
#2499=EDGE_CURVE('',#1832,#1882,#1473,.T.);
#2500=EDGE_CURVE('',#1859,#1881,#1474,.T.);
#2501=EDGE_CURVE('',#1776,#1838,#1475,.T.);
#2502=EDGE_CURVE('',#1883,#1860,#1476,.T.);
#2503=EDGE_CURVE('',#1880,#1883,#1477,.T.);
#2504=EDGE_CURVE('',#1837,#1777,#1478,.T.);
#3435=ORIENTED_EDGE('',*,*,#2371,.F.);
#3436=ORIENTED_EDGE('',*,*,#2372,.F.);
#3437=ORIENTED_EDGE('',*,*,#2373,.F.);
#3438=ORIENTED_EDGE('',*,*,#2374,.T.);
#3439=ORIENTED_EDGE('',*,*,#2375,.F.);
#3440=ORIENTED_EDGE('',*,*,#2376,.F.);
#3441=ORIENTED_EDGE('',*,*,#2377,.F.);
#3442=ORIENTED_EDGE('',*,*,#2371,.T.);
#3443=ORIENTED_EDGE('',*,*,#2378,.T.);
#3444=ORIENTED_EDGE('',*,*,#2379,.F.);
#3445=ORIENTED_EDGE('',*,*,#2380,.F.);
#3446=ORIENTED_EDGE('',*,*,#2375,.T.);
#3447=ORIENTED_EDGE('',*,*,#2381,.T.);
#3448=ORIENTED_EDGE('',*,*,#2382,.T.);
#3449=ORIENTED_EDGE('',*,*,#2383,.F.);
#3450=ORIENTED_EDGE('',*,*,#2384,.F.);
#3451=ORIENTED_EDGE('',*,*,#2385,.F.);
#3452=ORIENTED_EDGE('',*,*,#2379,.T.);
#3453=ORIENTED_EDGE('',*,*,#2386,.T.);
#3454=ORIENTED_EDGE('',*,*,#2387,.F.);
#3455=ORIENTED_EDGE('',*,*,#2388,.F.);
#3456=ORIENTED_EDGE('',*,*,#2383,.T.);
#3457=ORIENTED_EDGE('',*,*,#2389,.T.);
#3458=ORIENTED_EDGE('',*,*,#2390,.T.);
#3459=ORIENTED_EDGE('',*,*,#2391,.F.);
#3460=ORIENTED_EDGE('',*,*,#2392,.F.);
#3461=ORIENTED_EDGE('',*,*,#2393,.F.);
#3462=ORIENTED_EDGE('',*,*,#2387,.T.);
#3463=ORIENTED_EDGE('',*,*,#2394,.T.);
#3464=ORIENTED_EDGE('',*,*,#2395,.F.);
#3465=ORIENTED_EDGE('',*,*,#2396,.F.);
#3466=ORIENTED_EDGE('',*,*,#2391,.T.);
#3467=ORIENTED_EDGE('',*,*,#2397,.T.);
#3468=ORIENTED_EDGE('',*,*,#2398,.T.);
#3469=ORIENTED_EDGE('',*,*,#2399,.F.);
#3470=ORIENTED_EDGE('',*,*,#2400,.F.);
#3471=ORIENTED_EDGE('',*,*,#2401,.F.);
#3472=ORIENTED_EDGE('',*,*,#2395,.T.);
#3473=ORIENTED_EDGE('',*,*,#2402,.T.);
#3474=ORIENTED_EDGE('',*,*,#2403,.F.);
#3475=ORIENTED_EDGE('',*,*,#2404,.F.);
#3476=ORIENTED_EDGE('',*,*,#2399,.T.);
#3477=ORIENTED_EDGE('',*,*,#2405,.T.);
#3478=ORIENTED_EDGE('',*,*,#2406,.T.);
#3479=ORIENTED_EDGE('',*,*,#2407,.F.);
#3480=ORIENTED_EDGE('',*,*,#2408,.F.);
#3481=ORIENTED_EDGE('',*,*,#2409,.F.);
#3482=ORIENTED_EDGE('',*,*,#2403,.T.);
#3483=ORIENTED_EDGE('',*,*,#2410,.T.);
#3484=ORIENTED_EDGE('',*,*,#2411,.F.);
#3485=ORIENTED_EDGE('',*,*,#2412,.F.);
#3486=ORIENTED_EDGE('',*,*,#2407,.T.);
#3487=ORIENTED_EDGE('',*,*,#2413,.T.);
#3488=ORIENTED_EDGE('',*,*,#2414,.T.);
#3489=ORIENTED_EDGE('',*,*,#2415,.F.);
#3490=ORIENTED_EDGE('',*,*,#2416,.F.);
#3491=ORIENTED_EDGE('',*,*,#2417,.F.);
#3492=ORIENTED_EDGE('',*,*,#2411,.T.);
#3493=ORIENTED_EDGE('',*,*,#2418,.T.);
#3494=ORIENTED_EDGE('',*,*,#2419,.F.);
#3495=ORIENTED_EDGE('',*,*,#2420,.F.);
#3496=ORIENTED_EDGE('',*,*,#2415,.T.);
#3497=ORIENTED_EDGE('',*,*,#2421,.T.);
#3498=ORIENTED_EDGE('',*,*,#2422,.T.);
#3499=ORIENTED_EDGE('',*,*,#2423,.F.);
#3500=ORIENTED_EDGE('',*,*,#2424,.F.);
#3501=ORIENTED_EDGE('',*,*,#2425,.F.);
#3502=ORIENTED_EDGE('',*,*,#2419,.T.);
#3503=ORIENTED_EDGE('',*,*,#2426,.T.);
#3504=ORIENTED_EDGE('',*,*,#2427,.F.);
#3505=ORIENTED_EDGE('',*,*,#2428,.F.);
#3506=ORIENTED_EDGE('',*,*,#2423,.T.);
#3507=ORIENTED_EDGE('',*,*,#2429,.T.);
#3508=ORIENTED_EDGE('',*,*,#2430,.T.);
#3509=ORIENTED_EDGE('',*,*,#2431,.F.);
#3510=ORIENTED_EDGE('',*,*,#2432,.F.);
#3511=ORIENTED_EDGE('',*,*,#2433,.F.);
#3512=ORIENTED_EDGE('',*,*,#2427,.T.);
#3513=ORIENTED_EDGE('',*,*,#2434,.T.);
#3514=ORIENTED_EDGE('',*,*,#2435,.F.);
#3515=ORIENTED_EDGE('',*,*,#2436,.F.);
#3516=ORIENTED_EDGE('',*,*,#2431,.T.);
#3517=ORIENTED_EDGE('',*,*,#2437,.T.);
#3518=ORIENTED_EDGE('',*,*,#2438,.T.);
#3519=ORIENTED_EDGE('',*,*,#2439,.F.);
#3520=ORIENTED_EDGE('',*,*,#2440,.F.);
#3521=ORIENTED_EDGE('',*,*,#2441,.F.);
#3522=ORIENTED_EDGE('',*,*,#2435,.T.);
#3523=ORIENTED_EDGE('',*,*,#2442,.T.);
#3524=ORIENTED_EDGE('',*,*,#2443,.F.);
#3525=ORIENTED_EDGE('',*,*,#2444,.F.);
#3526=ORIENTED_EDGE('',*,*,#2439,.T.);
#3527=ORIENTED_EDGE('',*,*,#2445,.T.);
#3528=ORIENTED_EDGE('',*,*,#2446,.T.);
#3529=ORIENTED_EDGE('',*,*,#2447,.F.);
#3530=ORIENTED_EDGE('',*,*,#2448,.F.);
#3531=ORIENTED_EDGE('',*,*,#2449,.F.);
#3532=ORIENTED_EDGE('',*,*,#2443,.T.);
#3533=ORIENTED_EDGE('',*,*,#2450,.T.);
#3534=ORIENTED_EDGE('',*,*,#2451,.T.);
#3535=ORIENTED_EDGE('',*,*,#2452,.T.);
#3536=ORIENTED_EDGE('',*,*,#2453,.F.);
#3537=ORIENTED_EDGE('',*,*,#2454,.T.);
#3538=ORIENTED_EDGE('',*,*,#2455,.T.);
#3539=ORIENTED_EDGE('',*,*,#2456,.T.);
#3540=ORIENTED_EDGE('',*,*,#2457,.T.);
#3541=ORIENTED_EDGE('',*,*,#2458,.T.);
#3542=ORIENTED_EDGE('',*,*,#2459,.T.);
#3543=ORIENTED_EDGE('',*,*,#2460,.T.);
#3544=ORIENTED_EDGE('',*,*,#2461,.T.);
#3545=ORIENTED_EDGE('',*,*,#2462,.T.);
#3546=ORIENTED_EDGE('',*,*,#2463,.T.);
#3547=ORIENTED_EDGE('',*,*,#2464,.T.);
#3548=ORIENTED_EDGE('',*,*,#2465,.T.);
#3549=ORIENTED_EDGE('',*,*,#2466,.T.);
#3550=ORIENTED_EDGE('',*,*,#2467,.T.);
#3551=ORIENTED_EDGE('',*,*,#2468,.T.);
#3552=ORIENTED_EDGE('',*,*,#2469,.T.);
#3553=ORIENTED_EDGE('',*,*,#2470,.T.);
#3554=ORIENTED_EDGE('',*,*,#2471,.T.);
#3555=ORIENTED_EDGE('',*,*,#2472,.T.);
#3556=ORIENTED_EDGE('',*,*,#2473,.T.);
#3557=ORIENTED_EDGE('',*,*,#2474,.T.);
#3558=ORIENTED_EDGE('',*,*,#2475,.F.);
#3559=ORIENTED_EDGE('',*,*,#2476,.T.);
#3560=ORIENTED_EDGE('',*,*,#2477,.T.);
#3561=ORIENTED_EDGE('',*,*,#2478,.T.);
#3562=ORIENTED_EDGE('',*,*,#2479,.T.);
#3563=ORIENTED_EDGE('',*,*,#2480,.T.);
#3564=ORIENTED_EDGE('',*,*,#2481,.T.);
#3565=ORIENTED_EDGE('',*,*,#2482,.T.);
#3566=ORIENTED_EDGE('',*,*,#2483,.T.);
#3567=ORIENTED_EDGE('',*,*,#2484,.T.);
#3568=ORIENTED_EDGE('',*,*,#2485,.T.);
#3569=ORIENTED_EDGE('',*,*,#2486,.T.);
#3570=ORIENTED_EDGE('',*,*,#2487,.T.);
#3571=ORIENTED_EDGE('',*,*,#2488,.T.);
#3572=ORIENTED_EDGE('',*,*,#2489,.T.);
#3573=ORIENTED_EDGE('',*,*,#2490,.T.);
#3574=ORIENTED_EDGE('',*,*,#2491,.T.);
#3575=ORIENTED_EDGE('',*,*,#2492,.T.);
#3576=ORIENTED_EDGE('',*,*,#2493,.T.);
#3577=ORIENTED_EDGE('',*,*,#2494,.T.);
#3578=ORIENTED_EDGE('',*,*,#2495,.T.);
#3579=ORIENTED_EDGE('',*,*,#2447,.T.);
#3580=ORIENTED_EDGE('',*,*,#2496,.T.);
#3581=ORIENTED_EDGE('',*,*,#2497,.F.);
#3582=ORIENTED_EDGE('',*,*,#2498,.F.);
#3583=ORIENTED_EDGE('',*,*,#2499,.F.);
#3584=ORIENTED_EDGE('',*,*,#2500,.F.);
#3585=ORIENTED_EDGE('',*,*,#2474,.F.);
#3586=ORIENTED_EDGE('',*,*,#2473,.F.);
#3587=ORIENTED_EDGE('',*,*,#2472,.F.);
#3588=ORIENTED_EDGE('',*,*,#2471,.F.);
#3589=ORIENTED_EDGE('',*,*,#2470,.F.);
#3590=ORIENTED_EDGE('',*,*,#2469,.F.);
#3591=ORIENTED_EDGE('',*,*,#2468,.F.);
#3592=ORIENTED_EDGE('',*,*,#2467,.F.);
#3593=ORIENTED_EDGE('',*,*,#2466,.F.);
#3594=ORIENTED_EDGE('',*,*,#2465,.F.);
#3595=ORIENTED_EDGE('',*,*,#2464,.F.);
#3596=ORIENTED_EDGE('',*,*,#2463,.F.);
#3597=ORIENTED_EDGE('',*,*,#2462,.F.);
#3598=ORIENTED_EDGE('',*,*,#2461,.F.);
#3599=ORIENTED_EDGE('',*,*,#2460,.F.);
#3600=ORIENTED_EDGE('',*,*,#2459,.F.);
#3601=ORIENTED_EDGE('',*,*,#2458,.F.);
#3602=ORIENTED_EDGE('',*,*,#2457,.F.);
#3603=ORIENTED_EDGE('',*,*,#2456,.F.);
#3604=ORIENTED_EDGE('',*,*,#2455,.F.);
#3605=ORIENTED_EDGE('',*,*,#2454,.F.);
#3606=ORIENTED_EDGE('',*,*,#2501,.F.);
#3607=ORIENTED_EDGE('',*,*,#2372,.T.);
#3608=ORIENTED_EDGE('',*,*,#2377,.T.);
#3609=ORIENTED_EDGE('',*,*,#2376,.T.);
#3610=ORIENTED_EDGE('',*,*,#2380,.T.);
#3611=ORIENTED_EDGE('',*,*,#2385,.T.);
#3612=ORIENTED_EDGE('',*,*,#2384,.T.);
#3613=ORIENTED_EDGE('',*,*,#2388,.T.);
#3614=ORIENTED_EDGE('',*,*,#2393,.T.);
#3615=ORIENTED_EDGE('',*,*,#2392,.T.);
#3616=ORIENTED_EDGE('',*,*,#2396,.T.);
#3617=ORIENTED_EDGE('',*,*,#2401,.T.);
#3618=ORIENTED_EDGE('',*,*,#2400,.T.);
#3619=ORIENTED_EDGE('',*,*,#2404,.T.);
#3620=ORIENTED_EDGE('',*,*,#2409,.T.);
#3621=ORIENTED_EDGE('',*,*,#2408,.T.);
#3622=ORIENTED_EDGE('',*,*,#2412,.T.);
#3623=ORIENTED_EDGE('',*,*,#2417,.T.);
#3624=ORIENTED_EDGE('',*,*,#2416,.T.);
#3625=ORIENTED_EDGE('',*,*,#2420,.T.);
#3626=ORIENTED_EDGE('',*,*,#2425,.T.);
#3627=ORIENTED_EDGE('',*,*,#2424,.T.);
#3628=ORIENTED_EDGE('',*,*,#2428,.T.);
#3629=ORIENTED_EDGE('',*,*,#2433,.T.);
#3630=ORIENTED_EDGE('',*,*,#2432,.T.);
#3631=ORIENTED_EDGE('',*,*,#2436,.T.);
#3632=ORIENTED_EDGE('',*,*,#2441,.T.);
#3633=ORIENTED_EDGE('',*,*,#2440,.T.);
#3634=ORIENTED_EDGE('',*,*,#2444,.T.);
#3635=ORIENTED_EDGE('',*,*,#2449,.T.);
#3636=ORIENTED_EDGE('',*,*,#2448,.T.);
#3637=ORIENTED_EDGE('',*,*,#2499,.T.);
#3638=ORIENTED_EDGE('',*,*,#2498,.T.);
#3639=ORIENTED_EDGE('',*,*,#2502,.F.);
#3640=ORIENTED_EDGE('',*,*,#2503,.F.);
#3641=ORIENTED_EDGE('',*,*,#2496,.F.);
#3642=ORIENTED_EDGE('',*,*,#2451,.F.);
#3643=ORIENTED_EDGE('',*,*,#2450,.F.);
#3644=ORIENTED_EDGE('',*,*,#2446,.F.);
#3645=ORIENTED_EDGE('',*,*,#2445,.F.);
#3646=ORIENTED_EDGE('',*,*,#2442,.F.);
#3647=ORIENTED_EDGE('',*,*,#2438,.F.);
#3648=ORIENTED_EDGE('',*,*,#2437,.F.);
#3649=ORIENTED_EDGE('',*,*,#2434,.F.);
#3650=ORIENTED_EDGE('',*,*,#2430,.F.);
#3651=ORIENTED_EDGE('',*,*,#2429,.F.);
#3652=ORIENTED_EDGE('',*,*,#2426,.F.);
#3653=ORIENTED_EDGE('',*,*,#2422,.F.);
#3654=ORIENTED_EDGE('',*,*,#2421,.F.);
#3655=ORIENTED_EDGE('',*,*,#2418,.F.);
#3656=ORIENTED_EDGE('',*,*,#2414,.F.);
#3657=ORIENTED_EDGE('',*,*,#2413,.F.);
#3658=ORIENTED_EDGE('',*,*,#2410,.F.);
#3659=ORIENTED_EDGE('',*,*,#2406,.F.);
#3660=ORIENTED_EDGE('',*,*,#2405,.F.);
#3661=ORIENTED_EDGE('',*,*,#2402,.F.);
#3662=ORIENTED_EDGE('',*,*,#2398,.F.);
#3663=ORIENTED_EDGE('',*,*,#2397,.F.);
#3664=ORIENTED_EDGE('',*,*,#2394,.F.);
#3665=ORIENTED_EDGE('',*,*,#2390,.F.);
#3666=ORIENTED_EDGE('',*,*,#2389,.F.);
#3667=ORIENTED_EDGE('',*,*,#2386,.F.);
#3668=ORIENTED_EDGE('',*,*,#2382,.F.);
#3669=ORIENTED_EDGE('',*,*,#2381,.F.);
#3670=ORIENTED_EDGE('',*,*,#2378,.F.);
#3671=ORIENTED_EDGE('',*,*,#2374,.F.);
#3672=ORIENTED_EDGE('',*,*,#2504,.F.);
#3673=ORIENTED_EDGE('',*,*,#2452,.F.);
#3674=ORIENTED_EDGE('',*,*,#2495,.F.);
#3675=ORIENTED_EDGE('',*,*,#2494,.F.);
#3676=ORIENTED_EDGE('',*,*,#2493,.F.);
#3677=ORIENTED_EDGE('',*,*,#2492,.F.);
#3678=ORIENTED_EDGE('',*,*,#2491,.F.);
#3679=ORIENTED_EDGE('',*,*,#2490,.F.);
#3680=ORIENTED_EDGE('',*,*,#2489,.F.);
#3681=ORIENTED_EDGE('',*,*,#2488,.F.);
#3682=ORIENTED_EDGE('',*,*,#2487,.F.);
#3683=ORIENTED_EDGE('',*,*,#2486,.F.);
#3684=ORIENTED_EDGE('',*,*,#2485,.F.);
#3685=ORIENTED_EDGE('',*,*,#2484,.F.);
#3686=ORIENTED_EDGE('',*,*,#2483,.F.);
#3687=ORIENTED_EDGE('',*,*,#2482,.F.);
#3688=ORIENTED_EDGE('',*,*,#2481,.F.);
#3689=ORIENTED_EDGE('',*,*,#2480,.F.);
#3690=ORIENTED_EDGE('',*,*,#2479,.F.);
#3691=ORIENTED_EDGE('',*,*,#2478,.F.);
#3692=ORIENTED_EDGE('',*,*,#2477,.F.);
#3693=ORIENTED_EDGE('',*,*,#2476,.F.);
#3694=ORIENTED_EDGE('',*,*,#2500,.T.);
#3695=ORIENTED_EDGE('',*,*,#2497,.T.);
#3696=ORIENTED_EDGE('',*,*,#2503,.T.);
#3697=ORIENTED_EDGE('',*,*,#2502,.T.);
#3698=ORIENTED_EDGE('',*,*,#2475,.T.);
#3699=ORIENTED_EDGE('',*,*,#2501,.T.);
#3700=ORIENTED_EDGE('',*,*,#2453,.T.);
#3701=ORIENTED_EDGE('',*,*,#2504,.T.);
#3702=ORIENTED_EDGE('',*,*,#2373,.T.);
#4018=CYLINDRICAL_SURFACE('',#4531,3.22274999999998);
#4019=CYLINDRICAL_SURFACE('',#4533,3.22274999999998);
#4020=CYLINDRICAL_SURFACE('',#4534,3.22274999999998);
#4021=CYLINDRICAL_SURFACE('',#4535,3.22274999999998);
#4022=CYLINDRICAL_SURFACE('',#4536,3.22274999999998);
#4023=CYLINDRICAL_SURFACE('',#4537,3.22274999999998);
#4024=CYLINDRICAL_SURFACE('',#4538,3.22274999999998);
#4025=CYLINDRICAL_SURFACE('',#4539,3.22274999999998);
#4026=CYLINDRICAL_SURFACE('',#4540,3.22274999999998);
#4027=CYLINDRICAL_SURFACE('',#4541,3.22274999999998);
#4028=CYLINDRICAL_SURFACE('',#4542,3.22274999999998);
#4029=CYLINDRICAL_SURFACE('',#4543,3.22274999999998);
#4030=CYLINDRICAL_SURFACE('',#4544,3.22274999999998);
#4031=CYLINDRICAL_SURFACE('',#4545,3.22274999999998);
#4032=CYLINDRICAL_SURFACE('',#4546,3.22274999999998);
#4033=CYLINDRICAL_SURFACE('',#4547,3.22274999999998);
#4034=CYLINDRICAL_SURFACE('',#4548,3.22274999999998);
#4035=CYLINDRICAL_SURFACE('',#4549,3.22274999999998);
#4036=CYLINDRICAL_SURFACE('',#4550,3.22274999999998);
#4037=CYLINDRICAL_SURFACE('',#4551,3.22274999999998);
#4038=CYLINDRICAL_SURFACE('',#4552,3.933);
#4039=CYLINDRICAL_SURFACE('',#4555,3.22274999999998);
#4185=ADVANCED_FACE('',(#302),#4018,.T.);
#4186=ADVANCED_FACE('',(#303),#4019,.T.);
#4187=ADVANCED_FACE('',(#304),#4020,.T.);
#4188=ADVANCED_FACE('',(#305),#4021,.T.);
#4189=ADVANCED_FACE('',(#306),#4022,.T.);
#4190=ADVANCED_FACE('',(#307),#4023,.T.);
#4191=ADVANCED_FACE('',(#308),#4024,.T.);
#4192=ADVANCED_FACE('',(#309),#4025,.T.);
#4193=ADVANCED_FACE('',(#310),#4026,.T.);
#4194=ADVANCED_FACE('',(#311),#4027,.T.);
#4195=ADVANCED_FACE('',(#312),#4028,.T.);
#4196=ADVANCED_FACE('',(#313),#4029,.T.);
#4197=ADVANCED_FACE('',(#314),#4030,.T.);
#4198=ADVANCED_FACE('',(#315),#4031,.T.);
#4199=ADVANCED_FACE('',(#316),#4032,.T.);
#4200=ADVANCED_FACE('',(#317),#4033,.T.);
#4201=ADVANCED_FACE('',(#318),#4034,.T.);
#4202=ADVANCED_FACE('',(#319),#4035,.T.);
#4203=ADVANCED_FACE('',(#320),#4036,.T.);
#4204=ADVANCED_FACE('',(#321),#4037,.T.);
#4205=ADVANCED_FACE('',(#322),#4038,.T.);
#4206=ADVANCED_FACE('',(#323),#4039,.T.);
#4207=ADVANCED_FACE('',(#324),#62,.F.);
#4208=ADVANCED_FACE('',(#325),#63,.F.);
#4209=ADVANCED_FACE('',(#326),#157,.F.);
#4210=ADVANCED_FACE('',(#327),#158,.T.);
#4264=CLOSED_SHELL('',(#4185,#4186,#4187,#4188,#4189,#4190,#4191,#4192,
#4193,#4194,#4195,#4196,#4197,#4198,#4199,#4200,#4201,#4202,#4203,#4204,
#4205,#4206,#4207,#4208,#4209,#4210));
#4530=AXIS2_PLACEMENT_3D('',#31899,#5158,#5159);
#4531=AXIS2_PLACEMENT_3D('',#31900,#5160,#5161);
#4532=AXIS2_PLACEMENT_3D('',#32015,#5163,#5164);
#4533=AXIS2_PLACEMENT_3D('',#32092,#5165,#5166);
#4534=AXIS2_PLACEMENT_3D('',#32524,#5168,#5169);
#4535=AXIS2_PLACEMENT_3D('',#32993,#5171,#5172);
#4536=AXIS2_PLACEMENT_3D('',#33436,#5174,#5175);
#4537=AXIS2_PLACEMENT_3D('',#33895,#5177,#5178);
#4538=AXIS2_PLACEMENT_3D('',#34346,#5180,#5181);
#4539=AXIS2_PLACEMENT_3D('',#34781,#5183,#5184);
#4540=AXIS2_PLACEMENT_3D('',#35228,#5186,#5187);
#4541=AXIS2_PLACEMENT_3D('',#35663,#5189,#5190);
#4542=AXIS2_PLACEMENT_3D('',#36106,#5192,#5193);
#4543=AXIS2_PLACEMENT_3D('',#36547,#5195,#5196);
#4544=AXIS2_PLACEMENT_3D('',#37010,#5198,#5199);
#4545=AXIS2_PLACEMENT_3D('',#37481,#5201,#5202);
#4546=AXIS2_PLACEMENT_3D('',#37924,#5204,#5205);
#4547=AXIS2_PLACEMENT_3D('',#38367,#5207,#5208);
#4548=AXIS2_PLACEMENT_3D('',#38834,#5210,#5211);
#4549=AXIS2_PLACEMENT_3D('',#39295,#5213,#5214);
#4550=AXIS2_PLACEMENT_3D('',#39734,#5216,#5217);
#4551=AXIS2_PLACEMENT_3D('',#40178,#5219,#5220);
#4552=AXIS2_PLACEMENT_3D('',#40617,#5222,#5223);
#4553=AXIS2_PLACEMENT_3D('',#40694,#5224,#5225);
#4554=AXIS2_PLACEMENT_3D('',#45218,#5226,#5227);
#4555=AXIS2_PLACEMENT_3D('',#49543,#5228,#5229);
#4556=AXIS2_PLACEMENT_3D('',#49708,#5230,#5231);
#4557=AXIS2_PLACEMENT_3D('',#51249,#5232,#5233);
#4558=AXIS2_PLACEMENT_3D('',#51250,#5234,#5235);
#5158=DIRECTION('axis',(0.,0.,1.));
#5159=DIRECTION('refdir',(1.,0.,0.));
#5160=DIRECTION('center_axis',(0.,-1.,0.));
#5161=DIRECTION('ref_axis',(0.853781898007399,0.,-0.520630839112401));
#5162=DIRECTION('',(0.,1.,0.));
#5163=DIRECTION('center_axis',(0.,1.,0.));
#5164=DIRECTION('ref_axis',(1.,0.,1.08690987399046E-13));
#5165=DIRECTION('center_axis',(0.,-1.,0.));
#5166=DIRECTION('ref_axis',(-0.457839658806139,0.,-0.889034783810104));
#5167=DIRECTION('',(0.,1.,0.));
#5168=DIRECTION('center_axis',(0.,-1.,0.));
#5169=DIRECTION('ref_axis',(-0.457839658806139,0.,-0.889034783810104));
#5170=DIRECTION('',(0.,1.,0.));
#5171=DIRECTION('center_axis',(0.,-1.,0.));
#5172=DIRECTION('ref_axis',(-0.457839658806139,0.,-0.889034783810104));
#5173=DIRECTION('',(0.,1.,0.));
#5174=DIRECTION('center_axis',(0.,-1.,0.));
#5175=DIRECTION('ref_axis',(-0.457839658806139,0.,-0.889034783810104));
#5176=DIRECTION('',(0.,1.,0.));
#5177=DIRECTION('center_axis',(0.,-1.,0.));
#5178=DIRECTION('ref_axis',(-0.457839658806139,0.,-0.889034783810104));
#5179=DIRECTION('',(0.,1.,0.));
#5180=DIRECTION('center_axis',(0.,-1.,0.));
#5181=DIRECTION('ref_axis',(-0.457839658806139,0.,-0.889034783810104));
#5182=DIRECTION('',(0.,1.,0.));
#5183=DIRECTION('center_axis',(0.,-1.,0.));
#5184=DIRECTION('ref_axis',(-0.457839658806139,0.,-0.889034783810104));
#5185=DIRECTION('',(0.,1.,0.));
#5186=DIRECTION('center_axis',(0.,-1.,0.));
#5187=DIRECTION('ref_axis',(-0.457839658806139,0.,-0.889034783810104));
#5188=DIRECTION('',(0.,1.,0.));
#5189=DIRECTION('center_axis',(0.,-1.,0.));
#5190=DIRECTION('ref_axis',(-0.457839658806139,0.,-0.889034783810104));
#5191=DIRECTION('',(0.,1.,0.));
#5192=DIRECTION('center_axis',(0.,-1.,0.));
#5193=DIRECTION('ref_axis',(-0.457839658806139,0.,-0.889034783810104));
#5194=DIRECTION('',(0.,1.,0.));
#5195=DIRECTION('center_axis',(0.,-1.,0.));
#5196=DIRECTION('ref_axis',(-0.457839658806139,0.,-0.889034783810104));
#5197=DIRECTION('',(0.,1.,0.));
#5198=DIRECTION('center_axis',(0.,-1.,0.));
#5199=DIRECTION('ref_axis',(-0.457839658806139,0.,-0.889034783810104));
#5200=DIRECTION('',(0.,1.,0.));
#5201=DIRECTION('center_axis',(0.,-1.,0.));
#5202=DIRECTION('ref_axis',(-0.457839658806139,0.,-0.889034783810104));
#5203=DIRECTION('',(0.,1.,0.));
#5204=DIRECTION('center_axis',(0.,-1.,0.));
#5205=DIRECTION('ref_axis',(-0.457839658806139,0.,-0.889034783810104));
#5206=DIRECTION('',(0.,1.,0.));
#5207=DIRECTION('center_axis',(0.,-1.,0.));
#5208=DIRECTION('ref_axis',(-0.457839658806139,0.,-0.889034783810104));
#5209=DIRECTION('',(0.,1.,0.));
#5210=DIRECTION('center_axis',(0.,-1.,0.));
#5211=DIRECTION('ref_axis',(-0.457839658806139,0.,-0.889034783810104));
#5212=DIRECTION('',(0.,1.,0.));
#5213=DIRECTION('center_axis',(0.,-1.,0.));
#5214=DIRECTION('ref_axis',(-0.457839658806139,0.,-0.889034783810104));
#5215=DIRECTION('',(0.,1.,0.));
#5216=DIRECTION('center_axis',(0.,-1.,0.));
#5217=DIRECTION('ref_axis',(-0.457839658806139,0.,-0.889034783810104));
#5218=DIRECTION('',(0.,1.,0.));
#5219=DIRECTION('center_axis',(0.,-1.,0.));
#5220=DIRECTION('ref_axis',(-0.457839658806139,0.,-0.889034783810104));
#5221=DIRECTION('',(0.,1.,0.));
#5222=DIRECTION('center_axis',(0.,-1.,0.));
#5223=DIRECTION('ref_axis',(1.,0.,0.));
#5224=DIRECTION('center_axis',(0.,-1.,0.));
#5225=DIRECTION('ref_axis',(1.,0.,0.));
#5226=DIRECTION('center_axis',(0.,-1.,0.));
#5227=DIRECTION('ref_axis',(1.,0.,0.));
#5228=DIRECTION('center_axis',(0.,-1.,0.));
#5229=DIRECTION('ref_axis',(-0.457839658806139,0.,-0.889034783810104));
#5230=DIRECTION('center_axis',(0.,-1.,0.));
#5231=DIRECTION('ref_axis',(1.,0.,1.08690987399046E-13));
#5232=DIRECTION('center_axis',(0.,1.,0.));
#5233=DIRECTION('ref_axis',(1.,0.,0.));
#5234=DIRECTION('center_axis',(0.,1.,0.));
#5235=DIRECTION('ref_axis',(1.,0.,0.));
#31899=CARTESIAN_POINT('',(0.,0.,0.));
#31900=CARTESIAN_POINT('Origin',(370.834317853224,2.31077344927308,0.));
#31901=CARTESIAN_POINT('',(372.309820613641,-0.653742688831811,2.86513684952401));
#31902=CARTESIAN_POINT('',(372.309820610785,-0.410425323647664,2.8651368509949));
#31903=CARTESIAN_POINT('',(372.309820613641,2.31077344927308,2.86513684952399));
#31904=CARTESIAN_POINT('',(368.962795093421,-8.08730439136318E-5,-2.62364634088498));
#31905=CARTESIAN_POINT('Ctrl Pts',(368.962795093421,-8.08730439141314E-5,
-2.62364634088498));
#31906=CARTESIAN_POINT('Ctrl Pts',(369.042935960825,-0.00619260378656188,
-2.68081313771997));
#31907=CARTESIAN_POINT('Ctrl Pts',(369.125848866233,-0.0123043345292098,
-2.73441167961165));
#31908=CARTESIAN_POINT('Ctrl Pts',(369.211178937621,-0.0184160652718575,
-2.78415833298928));
#31909=CARTESIAN_POINT('Ctrl Pts',(369.2963967607,-0.0245197562763533,-2.83383954662751));
#31910=CARTESIAN_POINT('Ctrl Pts',(369.384025052725,-0.030623447280849,
-2.87967871727806));
#31911=CARTESIAN_POINT('Ctrl Pts',(369.473678013242,-0.0367271382853449,
-2.92143402943727));
#31912=CARTESIAN_POINT('Ctrl Pts',(369.564719999829,-0.0429253960044152,
-2.9638362719021));
#31913=CARTESIAN_POINT('Ctrl Pts',(369.657849557319,-0.0491236537234856,
-3.00202675452611));
#31914=CARTESIAN_POINT('Ctrl Pts',(369.752634214727,-0.0553219114425558,
-3.03579941180366));
#31915=CARTESIAN_POINT('Ctrl Pts',(369.845818119595,-0.0614154910728362,
-3.06900170602479));
#31916=CARTESIAN_POINT('Ctrl Pts',(369.940601220424,-0.0675090707031168,
-3.09793407947053));
#31917=CARTESIAN_POINT('Ctrl Pts',(370.036551456481,-0.0736026503333971,
-3.12244877279476));
#31918=CARTESIAN_POINT('Ctrl Pts',(370.132472827969,-0.0796943968410773,
-3.14695609139985));
#31919=CARTESIAN_POINT('Ctrl Pts',(370.22956020778,-0.0857861433487573,
-3.16704826003044));
#31920=CARTESIAN_POINT('Ctrl Pts',(370.327367221206,-0.0918778898564376,
-3.18262762810807));
#31921=CARTESIAN_POINT('Ctrl Pts',(370.42517220408,-0.0979695098945485,
-3.19820667274545));
#31922=CARTESIAN_POINT('Ctrl Pts',(370.523696352617,-0.10406112993266,-3.20927303428268));
#31923=CARTESIAN_POINT('Ctrl Pts',(370.622485092656,-0.110152749970771,
-3.21578053418605));
#31924=CARTESIAN_POINT('Ctrl Pts',(370.724291754657,-0.116430464435126,
-3.22248683333383));
#31925=CARTESIAN_POINT('Ctrl Pts',(370.826378937163,-0.12270817889948,-3.22435118160919));
#31926=CARTESIAN_POINT('Ctrl Pts',(370.92824739925,-0.128985893363835,-3.22138088447847));
#31927=CARTESIAN_POINT('Ctrl Pts',(371.027231138184,-0.135085834767833,
-3.21849470057305));
#31928=CARTESIAN_POINT('Ctrl Pts',(371.126007932765,-0.141185776171832,
-3.21104412286963));
#31929=CARTESIAN_POINT('Ctrl Pts',(371.224125029667,-0.14728571757583,-3.19908860891562));
#31930=CARTESIAN_POINT('Ctrl Pts',(371.326531325948,-0.153652318570363,
-3.1866104583911));
#31931=CARTESIAN_POINT('Ctrl Pts',(371.428218392319,-0.160018919564898,
-3.16922461802616));
#31932=CARTESIAN_POINT('Ctrl Pts',(371.528685253602,-0.166385520559431,
-3.14705759016134));
#31933=CARTESIAN_POINT('Ctrl Pts',(371.629152114885,-0.172752121553965,
-3.12489056229652));
#31934=CARTESIAN_POINT('Ctrl Pts',(371.728398269154,-0.179118722548498,
-3.09794256249782));
#31935=CARTESIAN_POINT('Ctrl Pts',(371.825944479095,-0.185485323543031,
-3.06639759283822));
#31936=CARTESIAN_POINT('Ctrl Pts',(371.920678070301,-0.191668351836518,
-3.03576218155833));
#31937=CARTESIAN_POINT('Ctrl Pts',(372.014150842681,-0.197851380130005,
-3.00068080518707));
#31938=CARTESIAN_POINT('Ctrl Pts',(372.105916159122,-0.204034408423493,
-2.96127595994333));
#31939=CARTESIAN_POINT('Ctrl Pts',(372.197560363708,-0.210209276356962,
-2.92192312120972));
#31940=CARTESIAN_POINT('Ctrl Pts',(372.28750119774,-0.216384144290432,-2.87825832568418));
#31941=CARTESIAN_POINT('Ctrl Pts',(372.3753076588,-0.222559012223901,-2.83045367063467));
#31942=CARTESIAN_POINT('Ctrl Pts',(372.463023906512,-0.228727536028343,
-2.78269813062746));
#31943=CARTESIAN_POINT('Ctrl Pts',(372.548609763428,-0.234896059832786,
-2.73081139385581));
#31944=CARTESIAN_POINT('Ctrl Pts',(372.631655553263,-0.241064583637228,
-2.67501303819596));
#31945=CARTESIAN_POINT('Ctrl Pts',(372.714643792911,-0.247228832695148,
-2.61925335043047));
#31946=CARTESIAN_POINT('Ctrl Pts',(372.795095107198,-0.253393081753067,
-2.55958767389374));
#31947=CARTESIAN_POINT('Ctrl Pts',(372.872626497259,-0.259557330810986,
-2.49628031962563));
#31948=CARTESIAN_POINT('Ctrl Pts',(372.95013027197,-0.265719384269131,-2.43299551435116));
#31949=CARTESIAN_POINT('Ctrl Pts',(373.024715854482,-0.271881437727276,
-2.36607188230146));
#31950=CARTESIAN_POINT('Ctrl Pts',(373.096031916775,-0.278043491185421,
-2.29581511826106));
#31951=CARTESIAN_POINT('Ctrl Pts',(373.167341459047,-0.284204981282239,
-2.22556477739504));
#31952=CARTESIAN_POINT('Ctrl Pts',(373.23538176733,-0.290366471379056,-2.15198221408947));
#31953=CARTESIAN_POINT('Ctrl Pts',(373.299837822902,-0.296527961475873,
-2.0754105236363));
#31954=CARTESIAN_POINT('Ctrl Pts',(373.364305050632,-0.302690519542834,
-1.99882556102363));
#31955=CARTESIAN_POINT('Ctrl Pts',(373.425186512842,-0.308853077609796,
-1.91925077292984));
#31956=CARTESIAN_POINT('Ctrl Pts',(373.482207625686,-0.315015635676757,
-1.83706214249607));
#31957=CARTESIAN_POINT('Ctrl Pts',(373.539290208567,-0.321184837119358,
-1.75478491087762));
#31958=CARTESIAN_POINT('Ctrl Pts',(373.592503885071,-0.32735403856196,-1.66988856632607));
#31959=CARTESIAN_POINT('Ctrl Pts',(373.641617630156,-0.333523240004562,
-1.58277778760532));
#31960=CARTESIAN_POINT('Ctrl Pts',(373.690759303387,-0.339695949515255,
-1.49561747402238));
#31961=CARTESIAN_POINT('Ctrl Pts',(373.735796207269,-0.345868659025948,
-1.40624060465145));
#31962=CARTESIAN_POINT('Ctrl Pts',(373.776544422404,-0.352041368536641,
-1.31507428615635));
#31963=CARTESIAN_POINT('Ctrl Pts',(373.817360096113,-0.358224296953289,
-1.22375704203721));
#31964=CARTESIAN_POINT('Ctrl Pts',(373.853872741553,-0.364407225369936,
-1.13064483440963));
#31965=CARTESIAN_POINT('Ctrl Pts',(373.885947451266,-0.370590153786584,
-1.0361825895349));
#31966=CARTESIAN_POINT('Ctrl Pts',(373.909138357678,-0.375060582842619,
-0.967883761579969));
#31967=CARTESIAN_POINT('Ctrl Pts',(373.930010291673,-0.379531011898653,
-0.898879524300233));
#31968=CARTESIAN_POINT('Ctrl Pts',(373.948528930951,-0.384001440954687,
-0.82934126019565));
#31969=CARTESIAN_POINT('Ctrl Pts',(373.974081285622,-0.390169820124149,
-0.73339110095887));
#31970=CARTESIAN_POINT('Ctrl Pts',(373.99524054492,-0.39633819929361,-0.636088204984949));
#31971=CARTESIAN_POINT('Ctrl Pts',(374.011865918383,-0.402506578463071,
-0.537871598155227));
#31972=CARTESIAN_POINT('Ctrl Pts',(374.02846865233,-0.408666557873949,-0.439788737284304));
#31973=CARTESIAN_POINT('Ctrl Pts',(374.04054969955,-0.414826537284827,-0.340795063600563));
#31974=CARTESIAN_POINT('Ctrl Pts',(374.048018338277,-0.420986516695705,
-0.241343644769002));
#31975=CARTESIAN_POINT('Ctrl Pts',(374.055479021015,-0.427139934171043,
-0.141998166843434));
#31976=CARTESIAN_POINT('Ctrl Pts',(374.058337030795,-0.433293351646382,
-0.0421963445112613));
#31977=CARTESIAN_POINT('Ctrl Pts',(374.056553059645,-0.43944676912172,0.0576006683885499));
#31978=CARTESIAN_POINT('Ctrl Pts',(374.054770404537,-0.445595647201025,
0.157324060708199));
#31979=CARTESIAN_POINT('Ctrl Pts',(374.048352584441,-0.45174452528033,0.257042217049845));
#31980=CARTESIAN_POINT('Ctrl Pts',(374.037312330982,-0.457893403359635,
0.356291927990994));
#31981=CARTESIAN_POINT('Ctrl Pts',(374.026276302402,-0.464039928388644,
0.455503658090972));
#31982=CARTESIAN_POINT('Ctrl Pts',(374.010621403199,-0.470186453417652,
0.554246867132558));
#31983=CARTESIAN_POINT('Ctrl Pts',(373.990412322606,-0.476332978446661,
0.652062315150099));
#31984=CARTESIAN_POINT('Ctrl Pts',(373.97020555113,-0.482478801165025,0.749866586636176));
#31985=CARTESIAN_POINT('Ctrl Pts',(373.94544572082,-0.488624623883388,0.846742881849301));
#31986=CARTESIAN_POINT('Ctrl Pts',(373.916248665641,-0.494770446601752,
0.942242023035207));
#31987=CARTESIAN_POINT('Ctrl Pts',(373.887047109578,-0.500917216731959,
1.03775588593073));
#31988=CARTESIAN_POINT('Ctrl Pts',(373.853407097286,-0.507063986862167,
1.13189175712116));
#31989=CARTESIAN_POINT('Ctrl Pts',(373.815494063152,-0.513210756992375,
1.22421647099736));
#31990=CARTESIAN_POINT('Ctrl Pts',(373.77754060439,-0.519364081092622,1.31663962574508));
#31991=CARTESIAN_POINT('Ctrl Pts',(373.735305191492,-0.525517405192868,
1.40724736380236));
#31992=CARTESIAN_POINT('Ctrl Pts',(373.689001032213,-0.531670729293115,
1.49562746367374));
#31993=CARTESIAN_POINT('Ctrl Pts',(373.642671032123,-0.53782748735895,1.58405688554031));
#31994=CARTESIAN_POINT('Ctrl Pts',(373.592267983493,-0.543984245424785,
1.67025581806251));
#31995=CARTESIAN_POINT('Ctrl Pts',(373.538049521148,-0.550141003490619,
1.75383939697038));
#31996=CARTESIAN_POINT('Ctrl Pts',(373.48374068311,-0.556308024135873,1.83756229970866));
#31997=CARTESIAN_POINT('Ctrl Pts',(373.425603981768,-0.562475044781126,
1.91866078754878));
#31998=CARTESIAN_POINT('Ctrl Pts',(373.36393864059,-0.568642065426379,1.99678146892028));
#31999=CARTESIAN_POINT('Ctrl Pts',(373.317690646334,-0.573267229739699,
2.05537069837093));
#32000=CARTESIAN_POINT('Ctrl Pts',(373.269458741801,-0.577892394053019,
2.11228565003346));
#32001=CARTESIAN_POINT('Ctrl Pts',(373.219382449764,-0.582517558366338,
2.16739115824313));
#32002=CARTESIAN_POINT('Ctrl Pts',(373.152552371861,-0.588690141814474,
2.24093305315411));
#32003=CARTESIAN_POINT('Ctrl Pts',(373.082200751653,-0.59486272526261,2.31150974165541));
#32004=CARTESIAN_POINT('Ctrl Pts',(373.008621053345,-0.601035308710746,
2.37876504860047));
#32005=CARTESIAN_POINT('Ctrl Pts',(372.935128263089,-0.607200601463062,
2.44594091749672));
#32006=CARTESIAN_POINT('Ctrl Pts',(372.858415284192,-0.613365894215377,
2.50980290584623));
#32007=CARTESIAN_POINT('Ctrl Pts',(372.778814595073,-0.619531186967692,
2.5700291794918));
#32008=CARTESIAN_POINT('Ctrl Pts',(372.699299951336,-0.625689815268,2.63019035077703));
#32009=CARTESIAN_POINT('Ctrl Pts',(372.616904148337,-0.631848443568307,
2.68672336157344));
#32010=CARTESIAN_POINT('Ctrl Pts',(372.531994231394,-0.638007071868615,
2.73934526438414));
#32011=CARTESIAN_POINT('Ctrl Pts',(372.459677807224,-0.643252277523014,
2.78416250106559));
#32012=CARTESIAN_POINT('Ctrl Pts',(372.385538442582,-0.648497483177413,
2.82614329651706));
#32013=CARTESIAN_POINT('Ctrl Pts',(372.309820613641,-0.653742688831811,
2.86513684952399));
#32014=CARTESIAN_POINT('',(372.705904384963,0.,-2.62360084935056));
#32015=CARTESIAN_POINT('Origin',(370.834317853224,0.,0.));
#32016=CARTESIAN_POINT('Ctrl Pts',(372.705904384963,-1.88737914186277E-14,
-2.62360084935056));
#32017=CARTESIAN_POINT('Ctrl Pts',(372.710595199592,-0.000355697368928507,
-2.62025458366962));
#32018=CARTESIAN_POINT('Ctrl Pts',(372.71527706713,-0.000710695953714261,
-2.61689571828344));
#32019=CARTESIAN_POINT('Ctrl Pts',(372.726024488927,-0.00152561838845565,
-2.60914155910339));
#32020=CARTESIAN_POINT('Ctrl Pts',(372.732083798716,-0.0019850712772657,
-2.60473762387074));
#32021=CARTESIAN_POINT('Ctrl Pts',(372.75152913268,-0.00345972216930044,
-2.59050078946874));
#32022=CARTESIAN_POINT('Ctrl Pts',(372.76485471502,-0.00447056845869583,
-2.58058537480191));
#32023=CARTESIAN_POINT('Ctrl Pts',(372.827584205144,-0.00923319459196886,
-2.53315122480681));
#32024=CARTESIAN_POINT('Ctrl Pts',(372.875977245289,-0.012919598606441,
-2.49431226153856));
#32025=CARTESIAN_POINT('Ctrl Pts',(373.062491552304,-0.0272949789361674,
-2.33555318111472));
#32026=CARTESIAN_POINT('Ctrl Pts',(373.191424246573,-0.0376225082491726,
-2.20536226950303));
#32027=CARTESIAN_POINT('Ctrl Pts',(373.411297193783,-0.0573074579025147,
-1.94189968905256));
#32028=CARTESIAN_POINT('Ctrl Pts',(373.504644928321,-0.0665995606112878,
-1.81139252326241));
#32029=CARTESIAN_POINT('Ctrl Pts',(373.603766592501,-0.0780645279400828,
-1.64839445970101));
#32030=CARTESIAN_POINT('Ctrl Pts',(373.619265551378,-0.0799114376741435,
-1.62207177619305));
#32031=CARTESIAN_POINT('Ctrl Pts',(373.643124308413,-0.0828444227877941,
-1.58020102176749));
#32032=CARTESIAN_POINT('Ctrl Pts',(373.651734757191,-0.0839224024414881,
-1.56479741299886));
#32033=CARTESIAN_POINT('Ctrl Pts',(373.667657033818,-0.0859533507183905,
-1.53575586718835));
#32034=CARTESIAN_POINT('Ctrl Pts',(373.674998010408,-0.086905342091268,
-1.52213443177768));
#32035=CARTESIAN_POINT('Ctrl Pts',(373.691269653501,-0.0890513730776003,
-1.49141412385848));
#32036=CARTESIAN_POINT('Ctrl Pts',(373.700145406773,-0.0902471465684238,
-1.4742869759262));
#32037=CARTESIAN_POINT('Ctrl Pts',(373.722442405138,-0.0933171758043124,
-1.43029917307434));
#32038=CARTESIAN_POINT('Ctrl Pts',(373.735642766526,-0.0951984719800697,
-1.40332918718747));
#32039=CARTESIAN_POINT('Ctrl Pts',(373.829711214165,-0.109091545327147,
-1.20413334536655));
#32040=CARTESIAN_POINT('Ctrl Pts',(373.895549522849,-0.12158877127422,-1.02525981580862));
#32041=CARTESIAN_POINT('Ctrl Pts',(373.985444694561,-0.144778976218852,
-0.69299004925008));
#32042=CARTESIAN_POINT('Ctrl Pts',(374.01495630327,-0.155325176176758,-0.5416384720622));
#32043=CARTESIAN_POINT('Ctrl Pts',(374.05066609345,-0.175389091965657,-0.247775798164879));
#32044=CARTESIAN_POINT('Ctrl Pts',(374.05846218053,-0.184898559658955,-0.105791209733848));
#32045=CARTESIAN_POINT('Ctrl Pts',(374.05664542742,-0.195218383926661,0.0556734029323275));
#32046=CARTESIAN_POINT('Ctrl Pts',(374.056251540141,-0.196450884388894,
0.0750858414775472));
#32047=CARTESIAN_POINT('Ctrl Pts',(374.055441860438,-0.198190641023431,
0.102688345798392));
#32048=CARTESIAN_POINT('Ctrl Pts',(374.055170225417,-0.198705467217268,
0.110881766805682));
#32049=CARTESIAN_POINT('Ctrl Pts',(374.054566926671,-0.199727451126924,
0.127198937059484));
#32050=CARTESIAN_POINT('Ctrl Pts',(374.054235779015,-0.20023463366276,0.135322648850631));
#32051=CARTESIAN_POINT('Ctrl Pts',(374.053549122606,-0.201193633047422,
0.150734317590427));
#32052=CARTESIAN_POINT('Ctrl Pts',(374.053199611312,-0.201645760512203,
0.158022241656684));
#32053=CARTESIAN_POINT('Ctrl Pts',(374.05230454207,-0.202723686048867,0.175448907387578));
#32054=CARTESIAN_POINT('Ctrl Pts',(374.051735819817,-0.203348166766796,
0.185586323722907));
#32055=CARTESIAN_POINT('Ctrl Pts',(374.049510339479,-0.20559267071202,0.222163525356412));
#32056=CARTESIAN_POINT('Ctrl Pts',(374.047575449606,-0.207197625732224,
0.248586163341267));
#32057=CARTESIAN_POINT('Ctrl Pts',(374.031446666722,-0.218539957036256,
0.436923222005815));
#32058=CARTESIAN_POINT('Ctrl Pts',(374.005345694926,-0.22770899496835,0.597603616188866));
#32059=CARTESIAN_POINT('Ctrl Pts',(373.910432772169,-0.250374702730624,
0.991113254418384));
#32060=CARTESIAN_POINT('Ctrl Pts',(373.827281499534,-0.263771362180913,
1.21940384889745));
#32061=CARTESIAN_POINT('Ctrl Pts',(373.69846769339,-0.280852199434449,1.4781603786224));
#32062=CARTESIAN_POINT('Ctrl Pts',(373.676678156632,-0.283649918022502,
1.51963810582951));
#32063=CARTESIAN_POINT('Ctrl Pts',(373.644693300662,-0.287640511764521,
1.57742708762179));
#32064=CARTESIAN_POINT('Ctrl Pts',(373.63524367352,-0.288806176561682,1.59414582021381));
#32065=CARTESIAN_POINT('Ctrl Pts',(373.618749342303,-0.290818828170985,
1.62272893775445));
#32066=CARTESIAN_POINT('Ctrl Pts',(373.611776758296,-0.291663116633241,
1.63463449853355));
#32067=CARTESIAN_POINT('Ctrl Pts',(373.598312516365,-0.293281340335338,
1.65728957979945));
#32068=CARTESIAN_POINT('Ctrl Pts',(373.59183404412,-0.294054767673054,1.66804667164073));
#32069=CARTESIAN_POINT('Ctrl Pts',(373.576523354282,-0.295870719838971,
1.69313613547891));
#32070=CARTESIAN_POINT('Ctrl Pts',(373.567641436633,-0.296915124142863,
1.70743759879041));
#32071=CARTESIAN_POINT('Ctrl Pts',(373.536779252183,-0.300513917069573,
1.75627323429129));
#32072=CARTESIAN_POINT('Ctrl Pts',(373.514254047964,-0.30308918526027,1.79045665120519));
#32073=CARTESIAN_POINT('Ctrl Pts',(373.354961334725,-0.320966502662487,
2.02245066841634));
#32074=CARTESIAN_POINT('Ctrl Pts',(373.197101417432,-0.337137514679321,
2.20480414807088));
#32075=CARTESIAN_POINT('Ctrl Pts',(372.879884635299,-0.366556422975145,
2.49767640095164));
#32076=CARTESIAN_POINT('Ctrl Pts',(372.728002084667,-0.379643674779031,
2.61470919996204));
#32077=CARTESIAN_POINT('Ctrl Pts',(372.540420582599,-0.394010056326614,
2.73428169561147));
#32078=CARTESIAN_POINT('Ctrl Pts',(372.513979369807,-0.395996145490956,
2.75060362135331));
#32079=CARTESIAN_POINT('Ctrl Pts',(372.477537012697,-0.39867617672395,2.7723776499127));
#32080=CARTESIAN_POINT('Ctrl Pts',(372.467737949054,-0.399391241965818,
2.77816231347754));
#32081=CARTESIAN_POINT('Ctrl Pts',(372.451103454331,-0.400595424066035,
2.78786368713729));
#32082=CARTESIAN_POINT('Ctrl Pts',(372.444284136164,-0.401086327758437,
2.7918073334043));
#32083=CARTESIAN_POINT('Ctrl Pts',(372.431109945166,-0.402029509338662,
2.79936171238655));
#32084=CARTESIAN_POINT('Ctrl Pts',(372.424757122346,-0.402482019178931,
2.80297590346819));
#32085=CARTESIAN_POINT('Ctrl Pts',(372.409670996141,-0.403551272032026,
2.81149076505466));
#32086=CARTESIAN_POINT('Ctrl Pts',(372.400926977903,-0.404166806379806,
2.81637243694016));
#32087=CARTESIAN_POINT('Ctrl Pts',(372.370008016251,-0.406329039220401,
2.83344554068852));
#32088=CARTESIAN_POINT('Ctrl Pts',(372.347711732291,-0.407862439951093,
2.84541683521823));
#32089=CARTESIAN_POINT('Ctrl Pts',(372.32013108445,-0.409730584608208,2.85980948359887));
#32090=CARTESIAN_POINT('Ctrl Pts',(372.314979276673,-0.410078317270426,
2.86248021498102));
#32091=CARTESIAN_POINT('Ctrl Pts',(372.309820610785,-0.410425323647676,
2.86513685099491));
#32092=CARTESIAN_POINT('Origin',(370.834317853224,2.31077344927308,0.));
#32093=CARTESIAN_POINT('',(372.309820657227,-1.90534924053897,2.86513682707819));
#32094=CARTESIAN_POINT('',(372.309820561356,-1.65539601866286,2.86513687645008));
#32095=CARTESIAN_POINT('',(372.309820613641,2.31077344927308,2.86513684952399));
#32096=CARTESIAN_POINT('',(367.611568223216,-1.06077344924052,0.00154427509180863));
#32097=CARTESIAN_POINT('Ctrl Pts',(372.309820657226,-1.90534924053903,2.86513682707864));
#32098=CARTESIAN_POINT('Ctrl Pts',(372.358965257756,-1.90218876223823,2.83982808956957));
#32099=CARTESIAN_POINT('Ctrl Pts',(372.407491827767,-1.89899741261244,2.81323787201031));
#32100=CARTESIAN_POINT('Ctrl Pts',(372.515632405171,-1.89169475069727,2.75030248885923));
#32101=CARTESIAN_POINT('Ctrl Pts',(372.574756722089,-1.8875660225164,2.71327364968646));
#32102=CARTESIAN_POINT('Ctrl Pts',(372.652227002293,-1.88194537062448,2.66118048270359));
#32103=CARTESIAN_POINT('Ctrl Pts',(372.671677853702,-1.88051578015962,2.64778840148354));
#32104=CARTESIAN_POINT('Ctrl Pts',(372.703310052921,-1.87815965478522,2.62549296325104));
#32105=CARTESIAN_POINT('Ctrl Pts',(372.715579377309,-1.87723793698878,2.61671553831594));
#32106=CARTESIAN_POINT('Ctrl Pts',(372.73925693678,-1.87544368235301,2.59952410699681));
#32107=CARTESIAN_POINT('Ctrl Pts',(372.750672190822,-1.8745715542882,2.59112032477927));
#32108=CARTESIAN_POINT('Ctrl Pts',(372.777281329201,-1.87252170937226,2.57125895545952));
#32109=CARTESIAN_POINT('Ctrl Pts',(372.792429783173,-1.87134167378764,2.5597416529613));
#32110=CARTESIAN_POINT('Ctrl Pts',(372.841651751469,-1.86746377749195,2.52162579260534));
#32111=CARTESIAN_POINT('Ctrl Pts',(372.875291082146,-1.86474422852624,2.4944766995266));
#32112=CARTESIAN_POINT('Ctrl Pts',(372.953780901324,-1.85822886286021,2.42847968696302));
#32113=CARTESIAN_POINT('Ctrl Pts',(372.998123423556,-1.85441068318616,2.38905461252519));
#32114=CARTESIAN_POINT('Ctrl Pts',(373.165708792951,-1.8394365540771,2.23155945434327));
#32115=CARTESIAN_POINT('Ctrl Pts',(373.280575124685,-1.8279627481987,2.10500719673513));
#32116=CARTESIAN_POINT('Ctrl Pts',(373.499302648768,-1.80375852356601,1.82181716839251));
#32117=CARTESIAN_POINT('Ctrl Pts',(373.60061673185,-1.79105943269172,1.66396051308825));
#32118=CARTESIAN_POINT('Ctrl Pts',(373.700070140212,-1.77731752191173,1.47454884321366));
#32119=CARTESIAN_POINT('Ctrl Pts',(373.712188700715,-1.77561705036003,1.45075495997621));
#32120=CARTESIAN_POINT('Ctrl Pts',(373.728566342094,-1.77328485259655,1.41758567057998));
#32121=CARTESIAN_POINT('Ctrl Pts',(373.733077950058,-1.77263864789564,1.40833708909115));
#32122=CARTESIAN_POINT('Ctrl Pts',(373.740755785561,-1.77153264112166,1.39240468282946));
#32123=CARTESIAN_POINT('Ctrl Pts',(373.743943413507,-1.77107154576633,1.38573134367777));
#32124=CARTESIAN_POINT('Ctrl Pts',(373.75057477007,-1.77010836781202,1.37172475041674));
#32125=CARTESIAN_POINT('Ctrl Pts',(373.754013858178,-1.76960658994784,1.36438940059388));
#32126=CARTESIAN_POINT('Ctrl Pts',(373.762385343081,-1.76837937225814,1.34635696984024));
#32127=CARTESIAN_POINT('Ctrl Pts',(373.76728688401,-1.76765580787219,1.33564553300868));
#32128=CARTESIAN_POINT('Ctrl Pts',(373.784966337714,-1.765026553573,1.29644361357424));
#32129=CARTESIAN_POINT('Ctrl Pts',(373.797389204426,-1.76314122303744,1.26779369560465));
#32130=CARTESIAN_POINT('Ctrl Pts',(373.827613233149,-1.75844490671052,1.19521805327377));
#32131=CARTESIAN_POINT('Ctrl Pts',(373.844865962017,-1.75566049989041,1.15107078773375));
#32132=CARTESIAN_POINT('Ctrl Pts',(373.919104361675,-1.74311127397163,0.948002704885711));
#32133=CARTESIAN_POINT('Ctrl Pts',(373.964525400627,-1.73374774983065,0.785127834286161));
#32134=CARTESIAN_POINT('Ctrl Pts',(374.03845215783,-1.71222540834526,0.40767840447732));
#32135=CARTESIAN_POINT('Ctrl Pts',(374.058550192514,-1.70004132606598,0.19232187737371));
#32136=CARTESIAN_POINT('Ctrl Pts',(374.056783881818,-1.68548996994238,-0.0507928044017276));
#32137=CARTESIAN_POINT('Ctrl Pts',(374.056236067526,-1.68384093558131,-0.0781675460567816));
#32138=CARTESIAN_POINT('Ctrl Pts',(374.054766266122,-1.68111974524524,-0.123028731629179));
#32139=CARTESIAN_POINT('Ctrl Pts',(374.054050438088,-1.68005402405042,-0.140520860025591));
#32140=CARTESIAN_POINT('Ctrl Pts',(374.052506903585,-1.67812945151793,-0.171965506213771));
#32141=CARTESIAN_POINT('Ctrl Pts',(374.05173087715,-1.67727223902454,-0.185920205821364));
#32142=CARTESIAN_POINT('Ctrl Pts',(374.049881552839,-1.67543720060339,-0.215681849278053));
#32143=CARTESIAN_POINT('Ctrl Pts',(374.048782416845,-1.67445858620111,-0.231486762674127));
#32144=CARTESIAN_POINT('Ctrl Pts',(374.045488428003,-1.67179684407882,-0.274289619046491));
#32145=CARTESIAN_POINT('Ctrl Pts',(374.043069703146,-1.67010675053642,-0.301268566399799));
#32146=CARTESIAN_POINT('Ctrl Pts',(374.028163648219,-1.66091631187879,-0.44687123367169));
#32147=CARTESIAN_POINT('Ctrl Pts',(374.0094394124,-1.65322214139594,-0.564749648869219));
#32148=CARTESIAN_POINT('Ctrl Pts',(373.951070804538,-1.63502777695632,-0.834606757803964));
#32149=CARTESIAN_POINT('Ctrl Pts',(373.906768675642,-1.62442537289036,-0.985269727399512));
#32150=CARTESIAN_POINT('Ctrl Pts',(373.793126586864,-1.60254174440567,-1.28815845535703));
#32151=CARTESIAN_POINT('Ctrl Pts',(373.722548042371,-1.59129287642241,-1.43945761873371));
#32152=CARTESIAN_POINT('Ctrl Pts',(373.627319453799,-1.57884968316682,-1.60810019270213));
#32153=CARTESIAN_POINT('Ctrl Pts',(373.61377085924,-1.5771326574901,-1.63140591768199));
#32154=CARTESIAN_POINT('Ctrl Pts',(373.594629847911,-1.57478193949283,-1.6634006949898));
#32155=CARTESIAN_POINT('Ctrl Pts',(373.589286119799,-1.57413346665485,-1.67223623841909));
#32156=CARTESIAN_POINT('Ctrl Pts',(373.580037614334,-1.57302462191573,-1.68736344112174));
#32157=CARTESIAN_POINT('Ctrl Pts',(373.576153488163,-1.57256294195627,-1.6936675419275));
#32158=CARTESIAN_POINT('Ctrl Pts',(373.567978616084,-1.57159967929717,-1.70683388016171));
#32159=CARTESIAN_POINT('Ctrl Pts',(373.563683701244,-1.57109839472004,-1.71369341782959));
#32160=CARTESIAN_POINT('Ctrl Pts',(373.553097750191,-1.56987434334923,-1.73045981002238));
#32161=CARTESIAN_POINT('Ctrl Pts',(373.54677827581,-1.56915342915781,-1.74034874322648));
#32162=CARTESIAN_POINT('Ctrl Pts',(373.523610959304,-1.56654503809942,-1.77616902751122));
#32163=CARTESIAN_POINT('Ctrl Pts',(373.506443540912,-1.56467749801854,-1.80189297521584));
#32164=CARTESIAN_POINT('Ctrl Pts',(373.462387008036,-1.56003478393184,-1.86589327534014));
#32165=CARTESIAN_POINT('Ctrl Pts',(373.435029314207,-1.55728541658533,-1.90383967978715));
#32166=CARTESIAN_POINT('Ctrl Pts',(373.205518843448,-1.53515782295162,-2.20799710509426));
#32167=CARTESIAN_POINT('Ctrl Pts',(372.963898410823,-1.51734685381353,-2.44187864696232));
#32168=CARTESIAN_POINT('Ctrl Pts',(372.637020800093,-1.4939564598771,-2.6722046107394));
#32169=CARTESIAN_POINT('Ctrl Pts',(372.582293691837,-1.49006965325307,-2.70831958677603));
#32170=CARTESIAN_POINT('Ctrl Pts',(372.506876953788,-1.48473153999039,-2.75484946657579));
#32171=CARTESIAN_POINT('Ctrl Pts',(372.487118845157,-1.48333470806577,-2.76674869966166));
#32172=CARTESIAN_POINT('Ctrl Pts',(372.45433152374,-1.48101868061711,-2.7860181770424));
#32173=CARTESIAN_POINT('Ctrl Pts',(372.441375447892,-1.48010398125763,-2.79351167010738));
#32174=CARTESIAN_POINT('Ctrl Pts',(372.415999542451,-1.4783131680652,-2.80795354629218));
#32175=CARTESIAN_POINT('Ctrl Pts',(372.403584943946,-1.47743738793837,-2.81491045538196));
#32176=CARTESIAN_POINT('Ctrl Pts',(372.374168278894,-1.47536279228488,-2.83113992442026));
#32177=CARTESIAN_POINT('Ctrl Pts',(372.357128051344,-1.47416149396798,-2.84034182438249));
#32178=CARTESIAN_POINT('Ctrl Pts',(372.30005604942,-1.4701389562297,-2.87050009210162));
#32179=CARTESIAN_POINT('Ctrl Pts',(372.259668057428,-1.46729372929559,-2.89076732053195));
#32180=CARTESIAN_POINT('Ctrl Pts',(372.162091899843,-1.46041986621677,-2.93719031379544));
#32181=CARTESIAN_POINT('Ctrl Pts',(372.104539817312,-1.45636543767094,-2.96253374272594));
#32182=CARTESIAN_POINT('Ctrl Pts',(371.725868913342,-1.42969287408322,-3.11622097019959));
#32183=CARTESIAN_POINT('Ctrl Pts',(371.386677444198,-1.40549755302805,-3.19382820326595));
#32184=CARTESIAN_POINT('Ctrl Pts',(371.01045283922,-1.38118634815374,-3.21808527618487));
#32185=CARTESIAN_POINT('Ctrl Pts',(370.979202609063,-1.37918811537089,-3.21964360675774));
#32186=CARTESIAN_POINT('Ctrl Pts',(370.935788779535,-1.37644590879556,-3.22117507864337));
#32187=CARTESIAN_POINT('Ctrl Pts',(370.92364167345,-1.37568231635751,-3.22153480539511));
#32188=CARTESIAN_POINT('Ctrl Pts',(370.904129631126,-1.37446195725025,-3.22200219158046));
#32189=CARTESIAN_POINT('Ctrl Pts',(370.896765993851,-1.37400282640067,-3.22215332335272));
#32190=CARTESIAN_POINT('Ctrl Pts',(370.88126768742,-1.37303956967436,-3.22241826257151));
#32191=CARTESIAN_POINT('Ctrl Pts',(370.873132998323,-1.37253577189034,-3.22252651387325));
#32192=CARTESIAN_POINT('Ctrl Pts',(370.853059393832,-1.3712968084757,-3.22271762000995));
#32193=CARTESIAN_POINT('Ctrl Pts',(370.84112011722,-1.37056359971414,-3.22276493763734));
#32194=CARTESIAN_POINT('Ctrl Pts',(370.796873188968,-1.36785911869301,-3.22269440584148));
#32195=CARTESIAN_POINT('Ctrl Pts',(370.764566931014,-1.365909745716,-3.2221570921666));
#32196=CARTESIAN_POINT('Ctrl Pts',(370.529252415316,-1.35185965882292,-3.21470236545968));
#32197=CARTESIAN_POINT('Ctrl Pts',(370.327268455537,-1.34058774133008,-3.18909042619886));
#32198=CARTESIAN_POINT('Ctrl Pts',(369.924969777267,-1.31752960102629,-3.09886025870466));
#32199=CARTESIAN_POINT('Ctrl Pts',(369.725882105887,-1.30577769202467,-3.03334894370896));
#32200=CARTESIAN_POINT('Ctrl Pts',(369.496180742314,-1.29087772346656,-2.93210931995807));
#32201=CARTESIAN_POINT('Ctrl Pts',(369.458143958016,-1.28836537950399,-2.91445040410724));
#32202=CARTESIAN_POINT('Ctrl Pts',(369.403749017095,-1.28470194649725,-2.88789479386997));
#32203=CARTESIAN_POINT('Ctrl Pts',(369.387105454044,-1.28357131706961,-2.87959021122137));
#32204=CARTESIAN_POINT('Ctrl Pts',(369.357919342442,-1.28157104828055,-2.86471037312364));
#32205=CARTESIAN_POINT('Ctrl Pts',(369.345346397863,-1.28070354551683,-2.85819559854589));
#32206=CARTESIAN_POINT('Ctrl Pts',(369.331306664723,-1.27972819331574,-2.85080301724165));
#32207=CARTESIAN_POINT('Ctrl Pts',(369.329797010761,-1.27962322992909,-2.85000658077336));
#32208=CARTESIAN_POINT('Ctrl Pts',(369.31480065958,-1.27857970106569,-2.84207983580576));
#32209=CARTESIAN_POINT('Ctrl Pts',(369.301364306594,-1.27763780078315,-2.83485514726422));
#32210=CARTESIAN_POINT('Ctrl Pts',(369.265903631211,-1.27513329932544,-2.81546222073194));
#32211=CARTESIAN_POINT('Ctrl Pts',(369.243969998042,-1.27356492069393,-2.80313116532678));
#32212=CARTESIAN_POINT('Ctrl Pts',(369.196052555179,-1.27009517308511,-2.77544862976222));
#32213=CARTESIAN_POINT('Ctrl Pts',(369.170135689269,-1.26818993601732,-2.75998657778828));
#32214=CARTESIAN_POINT('Ctrl Pts',(369.092861902724,-1.2624216152785,-2.71240077032987));
#32215=CARTESIAN_POINT('Ctrl Pts',(369.042191964607,-1.25852047852587,-2.67919219309292));
#32216=CARTESIAN_POINT('Ctrl Pts',(368.847093909386,-1.24302706700509,-2.5433152903863));
#32217=CARTESIAN_POINT('Ctrl Pts',(368.710310307723,-1.23109204158757,-2.43024510669237));
#32218=CARTESIAN_POINT('Ctrl Pts',(368.456022489768,-1.20705494585068,-2.18210134263997));
#32219=CARTESIAN_POINT('Ctrl Pts',(368.339044748889,-1.1949967853666,-2.04731014431474));
#32220=CARTESIAN_POINT('Ctrl Pts',(368.217903934934,-1.18182015036386,-1.88181298039032));
#32221=CARTESIAN_POINT('Ctrl Pts',(368.202279574723,-1.18010588067814,-1.85989690448217));
#32222=CARTESIAN_POINT('Ctrl Pts',(368.181046223146,-1.17775825134408,-1.82930962764315));
#32223=CARTESIAN_POINT('Ctrl Pts',(368.175202081164,-1.17711016236529,-1.82080404611527));
#32224=CARTESIAN_POINT('Ctrl Pts',(368.165235673742,-1.17600177976766,-1.80614857917896));
#32225=CARTESIAN_POINT('Ctrl Pts',(368.161093601243,-1.17554018077972,-1.80001235332713));
#32226=CARTESIAN_POINT('Ctrl Pts',(368.152469681694,-1.17457720921772,-1.78714112262405));
#32227=CARTESIAN_POINT('Ctrl Pts',(368.147992001893,-1.17407613488385,-1.78040344569922));
#32228=CARTESIAN_POINT('Ctrl Pts',(368.137081197483,-1.17285231355942,-1.76385081588648));
#32229=CARTESIAN_POINT('Ctrl Pts',(368.130676140902,-1.17213142139114,-1.75401732575872));
#32230=CARTESIAN_POINT('Ctrl Pts',(368.107572899926,-1.16952126094381,-1.71812037784747));
#32231=CARTESIAN_POINT('Ctrl Pts',(368.09119612829,-1.16765198804557,-1.69185077241047));
#32232=CARTESIAN_POINT('Ctrl Pts',(368.050994991025,-1.16300365873376,-1.62524627084856));
#32233=CARTESIAN_POINT('Ctrl Pts',(368.027666211943,-1.16025051846008,-1.58461938485034));
#32234=CARTESIAN_POINT('Ctrl Pts',(367.85676982659,-1.13953111491668,-1.27138196596628));
#32235=CARTESIAN_POINT('Ctrl Pts',(367.748336729678,-1.12293168273889,-0.979263670863363));
#32236=CARTESIAN_POINT('Ctrl Pts',(367.665437499162,-1.10004431707633,-0.592922851485402));
#32237=CARTESIAN_POINT('Ctrl Pts',(367.650887003311,-1.09503446001441,-0.509044594904192));
#32238=CARTESIAN_POINT('Ctrl Pts',(367.636330877633,-1.0883951868073,-0.399550051300437));
#32239=CARTESIAN_POINT('Ctrl Pts',(367.633285330436,-1.08686161933463,-0.374368363422848));
#32240=CARTESIAN_POINT('Ctrl Pts',(367.628862282565,-1.08437818070093,-0.333783180586575));
#32241=CARTESIAN_POINT('Ctrl Pts',(367.627297815471,-1.08343420562926,-0.318400834648632));
#32242=CARTESIAN_POINT('Ctrl Pts',(367.624568524469,-1.08165535909282,-0.289501077812639));
#32243=CARTESIAN_POINT('Ctrl Pts',(367.623378248903,-1.08082130833095,-0.275986369158513));
#32244=CARTESIAN_POINT('Ctrl Pts',(367.621167326447,-1.07914695566432,-0.24892908854256));
#32245=CARTESIAN_POINT('Ctrl Pts',(367.620146878716,-1.07830666541041,-0.235386780507604));
#32246=CARTESIAN_POINT('Ctrl Pts',(367.618012431225,-1.07638187314418,-0.20445224183574));
#32247=CARTESIAN_POINT('Ctrl Pts',(367.616953862686,-1.07529565752283,-0.187056729299228));
#32248=CARTESIAN_POINT('Ctrl Pts',(367.613027725727,-1.07062818693322,-0.112579076832374));
#32249=CARTESIAN_POINT('Ctrl Pts',(367.611538005706,-1.06700444690195,-0.0554381735805181));
#32250=CARTESIAN_POINT('Ctrl Pts',(367.611568306237,-1.06333585784792,0.00170877070520201));
#32251=CARTESIAN_POINT('Ctrl Pts',(372.309820613641,-0.653742688831811,
2.86513684952399));
#32252=CARTESIAN_POINT('Ctrl Pts',(372.221003209592,-0.659895342129579,
2.91087648840709));
#32253=CARTESIAN_POINT('Ctrl Pts',(372.130013640704,-0.666047995427347,
2.95250465231268));
#32254=CARTESIAN_POINT('Ctrl Pts',(372.037270397767,-0.672200648725115,
2.98981985043874));
#32255=CARTESIAN_POINT('Ctrl Pts',(371.944541014133,-0.678352382586736,
3.02712947228082));
#32256=CARTESIAN_POINT('Ctrl Pts',(371.850058880057,-0.684504116448356,
3.06012724754406));
#32257=CARTESIAN_POINT('Ctrl Pts',(371.754262553616,-0.690655850309977,
3.08865979200057));
#32258=CARTESIAN_POINT('Ctrl Pts',(371.658454961579,-0.696808307612121,
3.11719569186864));
#32259=CARTESIAN_POINT('Ctrl Pts',(371.561333286326,-0.702960764914265,
3.14126519418015));
#32260=CARTESIAN_POINT('Ctrl Pts',(371.463350361894,-0.709113222216409,
3.16076504434233));
#32261=CARTESIAN_POINT('Ctrl Pts',(371.365265340964,-0.715272090271694,
3.18028521300809));
#32262=CARTESIAN_POINT('Ctrl Pts',(371.266317705121,-0.721430958326981,
3.1952261345892));
#32263=CARTESIAN_POINT('Ctrl Pts',(371.166969482799,-0.727589826382267,
3.20553590774477));
#32264=CARTESIAN_POINT('Ctrl Pts',(371.067569304964,-0.733751915301877,
3.2158510725373));
#32265=CARTESIAN_POINT('Ctrl Pts',(370.967768556964,-0.739914004221487,
3.22153024006408));
#32266=CARTESIAN_POINT('Ctrl Pts',(370.868031268253,-0.746076093141097,
3.22257365596924));
#32267=CARTESIAN_POINT('Ctrl Pts',(370.768124212498,-0.752248670812111,
3.22361884791661));
#32268=CARTESIAN_POINT('Ctrl Pts',(370.668281266254,-0.758421248483125,
3.22001253849878));
#32269=CARTESIAN_POINT('Ctrl Pts',(370.568963573348,-0.764593826154139,
3.21180707214045));
#32270=CARTESIAN_POINT('Ctrl Pts',(370.480790364716,-0.770073776028762,
3.20452234495869));
#32271=CARTESIAN_POINT('Ctrl Pts',(370.393031264093,-0.775553725903385,
3.19361348331574));
#32272=CARTESIAN_POINT('Ctrl Pts',(370.306001381893,-0.781033675778008,
3.17915071498974));
#32273=CARTESIAN_POINT('Ctrl Pts',(370.207941047915,-0.787208172414114,
3.16285488812622));
#32274=CARTESIAN_POINT('Ctrl Pts',(370.110464290368,-0.79338266905022,3.14198940079307));
#32275=CARTESIAN_POINT('Ctrl Pts',(370.01402988079,-0.799557165686327,3.11660796456343));
#32276=CARTESIAN_POINT('Ctrl Pts',(369.917725341106,-0.805723347020595,
3.09126070995472));
#32277=CARTESIAN_POINT('Ctrl Pts',(369.822460775281,-0.811889528354863,
3.061409704322));
#32278=CARTESIAN_POINT('Ctrl Pts',(369.728686991684,-0.818055709689131,
3.02716004871069));
#32279=CARTESIAN_POINT('Ctrl Pts',(369.635011848886,-0.824215404806936,
2.99294642036943));
#32280=CARTESIAN_POINT('Ctrl Pts',(369.542824776041,-0.830375099924741,
2.95434348917374));
#32281=CARTESIAN_POINT('Ctrl Pts',(369.452562653568,-0.836534795042546,
2.91150650535462));
#32282=CARTESIAN_POINT('Ctrl Pts',(369.362365759281,-0.842690038838683,
2.86870047780698));
#32283=CARTESIAN_POINT('Ctrl Pts',(369.274091440567,-0.848845282634821,
2.82166666654779));
#32284=CARTESIAN_POINT('Ctrl Pts',(369.188156918282,-0.855000526430958,
2.77060855025967));
#32285=CARTESIAN_POINT('Ctrl Pts',(369.102254519747,-0.861153469294887,
2.71956952034214));
#32286=CARTESIAN_POINT('Ctrl Pts',(369.01869055236,-0.867306412158817,2.66450939606797));
#32287=CARTESIAN_POINT('Ctrl Pts',(368.937857132645,-0.873459355022746,
2.60567732035315));
#32288=CARTESIAN_POINT('Ctrl Pts',(368.857032353384,-0.879611640185721,
2.54685153332216));
#32289=CARTESIAN_POINT('Ctrl Pts',(368.778937892372,-0.885763925348696,
2.48425485189353));
#32290=CARTESIAN_POINT('Ctrl Pts',(368.703935562196,-0.89191621051167,2.41817883056076));
#32291=CARTESIAN_POINT('Ctrl Pts',(368.628921229419,-0.898069480222924,
2.35209223510286));
#32292=CARTESIAN_POINT('Ctrl Pts',(368.557000336048,-0.904222749934177,
2.28252548067812));
#32293=CARTESIAN_POINT('Ctrl Pts',(368.488499621638,-0.91037601964543,2.20980867652812));
#32294=CARTESIAN_POINT('Ctrl Pts',(368.419925749182,-0.916535860984318,
2.13701421159253));
#32295=CARTESIAN_POINT('Ctrl Pts',(368.35477964779,-0.922695702323206,2.06106329557526));
#32296=CARTESIAN_POINT('Ctrl Pts',(368.293349255475,-0.928855543662094,
1.98232089928827));
#32297=CARTESIAN_POINT('Ctrl Pts',(368.231884417966,-0.935018838941698,
1.9035343506354));
#32298=CARTESIAN_POINT('Ctrl Pts',(368.174139689516,-0.941182134221302,
1.82195355876123));
#32299=CARTESIAN_POINT('Ctrl Pts',(368.120359756326,-0.947345429500906,
1.73797267262242));
#32300=CARTESIAN_POINT('Ctrl Pts',(368.066490578289,-0.95351895243069,1.65385242481322));
#32301=CARTESIAN_POINT('Ctrl Pts',(368.016599554071,-0.959692475360474,
1.56732450350204));
#32302=CARTESIAN_POINT('Ctrl Pts',(367.97088554308,-0.965865998290258,1.47880795498442));
#32303=CARTESIAN_POINT('Ctrl Pts',(367.937110060398,-0.970427263256725,
1.41340811176715));
#32304=CARTESIAN_POINT('Ctrl Pts',(367.90561379285,-0.974988528223193,1.34692320550947));
#32305=CARTESIAN_POINT('Ctrl Pts',(367.876459700432,-0.979549793189661,
1.27952831561645));
#32306=CARTESIAN_POINT('Ctrl Pts',(367.832910215336,-0.986363270276431,
1.1788559053471));
#32307=CARTESIAN_POINT('Ctrl Pts',(367.794457932752,-0.993176747363203,
1.075851191093));
#32308=CARTESIAN_POINT('Ctrl Pts',(367.761333116471,-0.999990224449973,
0.971021302640703));
#32309=CARTESIAN_POINT('Ctrl Pts',(367.728298687738,-1.00678510963019,0.866477463068555));
#32310=CARTESIAN_POINT('Ctrl Pts',(367.700562839212,-1.0135799948104,0.760118637330591));
#32311=CARTESIAN_POINT('Ctrl Pts',(367.678307875351,-1.02037487999061,0.652471135045156));
#32312=CARTESIAN_POINT('Ctrl Pts',(367.656161673856,-1.02713655784738,0.545349717503075));
#32313=CARTESIAN_POINT('Ctrl Pts',(367.63944303279,-1.03389823570415,0.436952446312823));
#32314=CARTESIAN_POINT('Ctrl Pts',(367.628283955551,-1.04065991356092,0.327817341629671));
#32315=CARTESIAN_POINT('Ctrl Pts',(367.617219221671,-1.04736442545412,0.219604909329125));
#32316=CARTESIAN_POINT('Ctrl Pts',(367.611620512735,-1.05406893734732,0.110667337950061));
#32317=CARTESIAN_POINT('Ctrl Pts',(367.611568223216,-1.06077344924052,0.00154427509180863));
#32318=CARTESIAN_POINT('Ctrl Pts',(372.309820610785,-0.410425323647672,
2.8651368509949));
#32319=CARTESIAN_POINT('Ctrl Pts',(372.119941942035,-0.423197833128021,
2.96292153421038));
#32320=CARTESIAN_POINT('Ctrl Pts',(371.920773159846,-0.435011031166651,
3.04160902462825));
#32321=CARTESIAN_POINT('Ctrl Pts',(371.570561117915,-0.455365295974534,
3.14112833017532));
#32322=CARTESIAN_POINT('Ctrl Pts',(371.423184159097,-0.463809664698718,
3.1720613536417));
#32323=CARTESIAN_POINT('Ctrl Pts',(371.191514904662,-0.477376157096664,
3.20398089562839));
#32324=CARTESIAN_POINT('Ctrl Pts',(371.108429490155,-0.482296506753667,
3.21215572210327));
#32325=CARTESIAN_POINT('Ctrl Pts',(371.000727684972,-0.488787789489794,
3.2185435626826));
#32326=CARTESIAN_POINT('Ctrl Pts',(370.976314989707,-0.490266553742547,
3.21971297793058));
#32327=CARTESIAN_POINT('Ctrl Pts',(370.936541031078,-0.492688780240232,
3.22116499829405));
#32328=CARTESIAN_POINT('Ctrl Pts',(370.921186609121,-0.493627005716013,
3.22161563983959));
#32329=CARTESIAN_POINT('Ctrl Pts',(370.891570367116,-0.495442990862056,
3.22227297765019));
#32330=CARTESIAN_POINT('Ctrl Pts',(370.877309218522,-0.496320259239618,
3.22249479829687));
#32331=CARTESIAN_POINT('Ctrl Pts',(370.844475433725,-0.498346687500237,
3.22278750861148));
#32332=CARTESIAN_POINT('Ctrl Pts',(370.825902854575,-0.499497861333115,
3.22279252620998));
#32333=CARTESIAN_POINT('Ctrl Pts',(370.766128421406,-0.503219135805091,
3.22229197662308));
#32334=CARTESIAN_POINT('Ctrl Pts',(370.724937278915,-0.505808507460077,
3.2211567832072));
#32335=CARTESIAN_POINT('Ctrl Pts',(370.468481747744,-0.52209191067235,3.20916445461529));
#32336=CARTESIAN_POINT('Ctrl Pts',(370.25477024742,-0.536427876831839,3.17752557318474));
#32337=CARTESIAN_POINT('Ctrl Pts',(369.923110087315,-0.559479874767384,
3.0938393971939));
#32338=CARTESIAN_POINT('Ctrl Pts',(369.802298286567,-0.568042075491482,
3.0556634690514));
#32339=CARTESIAN_POINT('Ctrl Pts',(369.629762621947,-0.580288959037265,
2.98973923675583));
#32340=CARTESIAN_POINT('Ctrl Pts',(369.576050438681,-0.584103390337076,
2.96753397217963));
#32341=CARTESIAN_POINT('Ctrl Pts',(369.491020414367,-0.590114274140003,
2.92965740609047));
#32342=CARTESIAN_POINT('Ctrl Pts',(369.459307748561,-0.592349721047187,
2.91490788283269));
#32343=CARTESIAN_POINT('Ctrl Pts',(369.41664394902,-0.595342335153094,2.89421372887305));
#32344=CARTESIAN_POINT('Ctrl Pts',(369.405479202283,-0.596124083145451,
2.88871814621087));
#32345=CARTESIAN_POINT('Ctrl Pts',(369.386880512363,-0.597423668686237,
2.87942917074082));
#32346=CARTESIAN_POINT('Ctrl Pts',(369.379429077677,-0.597943614376077,
2.87567137543549));
#32347=CARTESIAN_POINT('Ctrl Pts',(369.365397835357,-0.59892119675938,2.86852685263014));
#32348=CARTESIAN_POINT('Ctrl Pts',(369.358815001273,-0.599379204967817,
2.86514635896507));
#32349=CARTESIAN_POINT('Ctrl Pts',(369.343273293133,-0.60045917451941,2.85709743198338));
#32350=CARTESIAN_POINT('Ctrl Pts',(369.334324520543,-0.601079937244375,
2.85240944189247));
#32351=CARTESIAN_POINT('Ctrl Pts',(369.303158171976,-0.603238654544233,
2.83589510794055));
#32352=CARTESIAN_POINT('Ctrl Pts',(369.281056580626,-0.604763724944505,
2.82385030400531));
#32353=CARTESIAN_POINT('Ctrl Pts',(369.067112382762,-0.619491899769307,
2.70398420051586));
#32354=CARTESIAN_POINT('Ctrl Pts',(368.886621975315,-0.631670572573035,
2.57702410252286));
#32355=CARTESIAN_POINT('Ctrl Pts',(368.608987265892,-0.652267510272439,
2.33577224823941));
#32356=CARTESIAN_POINT('Ctrl Pts',(368.504306348232,-0.660574542953731,
2.23136061940861));
#32357=CARTESIAN_POINT('Ctrl Pts',(368.353043775316,-0.673927048656769,
2.05819411744613));
#32358=CARTESIAN_POINT('Ctrl Pts',(368.301323802834,-0.678780044283537,
1.99419747079431));
#32359=CARTESIAN_POINT('Ctrl Pts',(368.237588639153,-0.685191352666548,
1.90884888262688));
#32360=CARTESIAN_POINT('Ctrl Pts',(368.223286535392,-0.686660402449313,
1.88923849110129));
#32361=CARTESIAN_POINT('Ctrl Pts',(368.200336382318,-0.689068949688434,
1.85701185986968));
#32362=CARTESIAN_POINT('Ctrl Pts',(368.191554075396,-0.690003293275639,
1.84449208152134));
#32363=CARTESIAN_POINT('Ctrl Pts',(368.174775592114,-0.691813283548834,
1.82020736861242));
#32364=CARTESIAN_POINT('Ctrl Pts',(368.166767534539,-0.692688452332769,
1.80845104727943));
#32365=CARTESIAN_POINT('Ctrl Pts',(368.148492857501,-0.6947120996351,1.78123720630651));
#32366=CARTESIAN_POINT('Ctrl Pts',(368.138281465697,-0.695862607645018,
1.76574337516611));
#32367=CARTESIAN_POINT('Ctrl Pts',(368.105781708605,-0.699589366727602,
1.71549202760883));
#32368=CARTESIAN_POINT('Ctrl Pts',(368.084028044846,-0.702185117118837,
1.68039522323594));
#32369=CARTESIAN_POINT('Ctrl Pts',(367.943308335868,-0.719680666495249,
1.44330643755999));
#32370=CARTESIAN_POINT('Ctrl Pts',(367.846032902996,-0.735360211759838,
1.22930300199498));
#32371=CARTESIAN_POINT('Ctrl Pts',(367.728805014992,-0.760744725480299,
0.872796246329542));
#32372=CARTESIAN_POINT('Ctrl Pts',(367.693606705689,-0.770294752523127,
0.736152643239047));
#32373=CARTESIAN_POINT('Ctrl Pts',(367.659483234862,-0.782407371020832,
0.555334170277514));
#32374=CARTESIAN_POINT('Ctrl Pts',(367.652347894886,-0.785214110940032,
0.512872727928576));
#32375=CARTESIAN_POINT('Ctrl Pts',(367.641817908646,-0.789856625837867,
0.44148478900828));
#32376=CARTESIAN_POINT('Ctrl Pts',(367.63796073734,-0.791712165475381,0.41263305780363));
#32377=CARTESIAN_POINT('Ctrl Pts',(367.633126431945,-0.794272213694339,
0.372321261456269));
#32378=CARTESIAN_POINT('Ctrl Pts',(367.631819058225,-0.794993702298846,
0.36090319314314));
#32379=CARTESIAN_POINT('Ctrl Pts',(367.629697688302,-0.79621607773968,0.34145611758651));
#32380=CARTESIAN_POINT('Ctrl Pts',(367.628852727968,-0.796718660978283,
0.333430677237211));
#32381=CARTESIAN_POINT('Ctrl Pts',(367.62718046623,-0.797746581146961,0.316953400114207));
#32382=CARTESIAN_POINT('Ctrl Pts',(367.62635640962,-0.798271731832122,0.308501308231758));
#32383=CARTESIAN_POINT('Ctrl Pts',(367.624292658803,-0.799637694145501,
0.286431138947255));
#32384=CARTESIAN_POINT('Ctrl Pts',(367.623106195881,-0.800475571423377,
0.272808088895184));
#32385=CARTESIAN_POINT('Ctrl Pts',(367.618602485536,-0.803888661164334,
0.216987991109551));
#32386=CARTESIAN_POINT('Ctrl Pts',(367.616029821979,-0.806425348435268,
0.17473308541276));
#32387=CARTESIAN_POINT('Ctrl Pts',(367.606522046713,-0.820106200983126,
-0.0564347744226482));
#32388=CARTESIAN_POINT('Ctrl Pts',(367.61538566553,-0.83060204501898,-0.245645128138436));
#32389=CARTESIAN_POINT('Ctrl Pts',(367.661530625372,-0.849801064754592,
-0.58597804823855));
#32390=CARTESIAN_POINT('Ctrl Pts',(367.693235866667,-0.858453855073586,
-0.737257342582714));
#32391=CARTESIAN_POINT('Ctrl Pts',(367.751034437331,-0.870645748509624,
-0.939474290909169));
#32392=CARTESIAN_POINT('Ctrl Pts',(367.767809934252,-0.87392467487949,-0.992863152935819));
#32393=CARTESIAN_POINT('Ctrl Pts',(367.799364608177,-0.879697793455532,
-1.08484155707613));
#32394=CARTESIAN_POINT('Ctrl Pts',(367.813512005492,-0.882171859061296,
-1.12363437100682));
#32395=CARTESIAN_POINT('Ctrl Pts',(367.835121643227,-0.885798706178858,
-1.17952832453304));
#32396=CARTESIAN_POINT('Ctrl Pts',(367.841993557893,-0.886931732010983,
-1.19685431999605));
#32397=CARTESIAN_POINT('Ctrl Pts',(367.854314131446,-0.888928686346713,
-1.22714840678991));
#32398=CARTESIAN_POINT('Ctrl Pts',(367.859698163615,-0.889790407713328,
-1.24014236535341));
#32399=CARTESIAN_POINT('Ctrl Pts',(367.871054035134,-0.89158576952455,-1.26704946128958));
#32400=CARTESIAN_POINT('Ctrl Pts',(367.877039196298,-0.892519848177695,
-1.28095656667419));
#32401=CARTESIAN_POINT('Ctrl Pts',(367.892790614149,-0.894947355066135,
-1.31685768786658));
#32402=CARTESIAN_POINT('Ctrl Pts',(367.90270548396,-0.896445856722675,-1.33878509626597));
#32403=CARTESIAN_POINT('Ctrl Pts',(367.944129667997,-0.902590502798605,
-1.42773034393341));
#32404=CARTESIAN_POINT('Ctrl Pts',(367.977696876742,-0.90730729189912,-1.49375929552786));
#32405=CARTESIAN_POINT('Ctrl Pts',(368.171128958557,-0.933182627119895,
-1.84384664228556));
#32406=CARTESIAN_POINT('Ctrl Pts',(368.371070091033,-0.955800833142827,
-2.10349441518247));
#32407=CARTESIAN_POINT('Ctrl Pts',(368.640083820829,-0.98037863781435,-2.36085023046784));
#32408=CARTESIAN_POINT('Ctrl Pts',(368.674353426343,-0.983415920881478,
-2.39224390781704));
#32409=CARTESIAN_POINT('Ctrl Pts',(368.732408097809,-0.98839191738177,-2.44316155237734));
#32410=CARTESIAN_POINT('Ctrl Pts',(368.755814516315,-0.990354357634577,
-2.4631051605759));
#32411=CARTESIAN_POINT('Ctrl Pts',(368.788495300124,-0.993030451811923,
-2.49015338328426));
#32412=CARTESIAN_POINT('Ctrl Pts',(368.79752735841,-0.993763452333319,-2.49754645226084));
#32413=CARTESIAN_POINT('Ctrl Pts',(368.812860696712,-0.994996441671589,
-2.50995884783853));
#32414=CARTESIAN_POINT('Ctrl Pts',(368.819140939223,-0.995498250506953,
-2.51500386966016));
#32415=CARTESIAN_POINT('Ctrl Pts',(368.831233118488,-0.996458233722737,
-2.52464333937975));
#32416=CARTESIAN_POINT('Ctrl Pts',(368.837042014871,-0.996916677943237,
-2.52924132374726));
#32417=CARTESIAN_POINT('Ctrl Pts',(368.850986381156,-0.998010835266112,
-2.54020087530193));
#32418=CARTESIAN_POINT('Ctrl Pts',(368.85913673459,-0.998645222558279,-2.54654349468297));
#32419=CARTESIAN_POINT('Ctrl Pts',(368.888686087854,-1.00092729670446,-2.56931163867871));
#32420=CARTESIAN_POINT('Ctrl Pts',(368.910261291199,-1.00255981880434,-2.58550801917814));
#32421=CARTESIAN_POINT('Ctrl Pts',(369.066673026292,-1.01417532589859,-2.69988304614371));
#32422=CARTESIAN_POINT('Ctrl Pts',(369.20876498788,-1.0235770775129,-2.78774606063935));
#32423=CARTESIAN_POINT('Ctrl Pts',(369.584053879852,-1.04722621468534,-2.98130917596579));
#32424=CARTESIAN_POINT('Ctrl Pts',(369.824159291409,-1.06137786718031,-3.07098187056445));
#32425=CARTESIAN_POINT('Ctrl Pts',(370.111057419576,-1.0789288941631,-3.1407962439529));
#32426=CARTESIAN_POINT('Ctrl Pts',(370.149961285456,-1.08131960619163,-3.14950195723821));
#32427=CARTESIAN_POINT('Ctrl Pts',(370.206896899095,-1.08483834895031,-3.16113802495101));
#32428=CARTESIAN_POINT('Ctrl Pts',(370.224808845962,-1.08594819222272,-3.1646404875298));
#32429=CARTESIAN_POINT('Ctrl Pts',(370.256636412491,-1.08792571086705,-3.17058374627483));
#32430=CARTESIAN_POINT('Ctrl Pts',(370.270540252108,-1.08879142452289,-3.17308555598012));
#32431=CARTESIAN_POINT('Ctrl Pts',(370.299558095345,-1.09060221809778,-3.17811018587985));
#32432=CARTESIAN_POINT('Ctrl Pts',(370.314674512214,-1.09154778847688,-3.18061678569745));
#32433=CARTESIAN_POINT('Ctrl Pts',(370.35411655438,-1.09402114511627,-3.18686837266225));
#32434=CARTESIAN_POINT('Ctrl Pts',(370.378467863079,-1.09555427619082,-3.19044260952602));
#32435=CARTESIAN_POINT('Ctrl Pts',(370.488572378034,-1.10251525000373,-3.20531727181961));
#32436=CARTESIAN_POINT('Ctrl Pts',(370.574711758295,-1.10804147832615,-3.2134407039405));
#32437=CARTESIAN_POINT('Ctrl Pts',(370.821568205841,-1.12411413109601,-3.22673056888324));
#32438=CARTESIAN_POINT('Ctrl Pts',(370.982474373337,-1.13488682517902,-3.2233511231144));
#32439=CARTESIAN_POINT('Ctrl Pts',(371.341861005655,-1.15928453935056,-3.188832528809));
#32440=CARTESIAN_POINT('Ctrl Pts',(371.539076727275,-1.17291322313052,-3.15112375449813));
#32441=CARTESIAN_POINT('Ctrl Pts',(371.756682245187,-1.1874581157643,-3.0880491415532));
#32442=CARTESIAN_POINT('Ctrl Pts',(371.781749673725,-1.18912551484148,-3.08045071685477));
#32443=CARTESIAN_POINT('Ctrl Pts',(371.816474160178,-1.19142127359527,-3.06946105514844));
#32444=CARTESIAN_POINT('Ctrl Pts',(371.826211144869,-1.19206347904451,-3.06632840461775));
#32445=CARTESIAN_POINT('Ctrl Pts',(371.842960655554,-1.19316533845838,-3.06085150329645));
#32446=CARTESIAN_POINT('Ctrl Pts',(371.84998026352,-1.19362625193183,-3.05852940133607));
#32447=CARTESIAN_POINT('Ctrl Pts',(371.864712404777,-1.19459165733644,-3.05359966451514));
#32448=CARTESIAN_POINT('Ctrl Pts',(371.87242313574,-1.1950958270013,-3.05098693331585));
#32449=CARTESIAN_POINT('Ctrl Pts',(371.891403844221,-1.19633431212111,-3.04447515704058));
#32450=CARTESIAN_POINT('Ctrl Pts',(371.902662380794,-1.19706668372271,-3.04054267441853));
#32451=CARTESIAN_POINT('Ctrl Pts',(371.944185742159,-1.1997603834005,-3.02577990970987));
#32452=CARTESIAN_POINT('Ctrl Pts',(371.974310973774,-1.20170007273808,-3.01455911480811));
#32453=CARTESIAN_POINT('Ctrl Pts',(372.191003959864,-1.21558069741221,-2.93013400083984));
#32454=CARTESIAN_POINT('Ctrl Pts',(372.370573789216,-1.22671444366037,-2.84010917677809));
#32455=CARTESIAN_POINT('Ctrl Pts',(372.720749727295,-1.24979896747064,-2.62155897384041));
#32456=CARTESIAN_POINT('Ctrl Pts',(372.889296247283,-1.26172030412379,-2.4916354066685));
#32457=CARTESIAN_POINT('Ctrl Pts',(373.071210367654,-1.27655524376267,-2.32031106006873));
#32458=CARTESIAN_POINT('Ctrl Pts',(373.098130216951,-1.27880630825853,-2.29405425897784));
#32459=CARTESIAN_POINT('Ctrl Pts',(373.138959522668,-1.28231197424718,-2.25281199156576));
#32460=CARTESIAN_POINT('Ctrl Pts',(373.153196670712,-1.28355219909704,-2.23815461799345));
#32461=CARTESIAN_POINT('Ctrl Pts',(373.177154786331,-1.28567035139656,-2.21301536224042));
#32462=CARTESIAN_POINT('Ctrl Pts',(373.186947267432,-1.28654515905819,-2.20260226043797));
#32463=CARTESIAN_POINT('Ctrl Pts',(373.206641931004,-1.28832323032658,-2.18137822340416));
#32464=CARTESIAN_POINT('Ctrl Pts',(373.216540258109,-1.28922662740818,-2.17056418608468));
#32465=CARTESIAN_POINT('Ctrl Pts',(373.240805354749,-1.29146575083581,-2.14368837356616));
#32466=CARTESIAN_POINT('Ctrl Pts',(373.255085300534,-1.29280507188753,-2.12754949832327));
#32467=CARTESIAN_POINT('Ctrl Pts',(373.308170328472,-1.29786695920039,-2.06632759840005));
#32468=CARTESIAN_POINT('Ctrl Pts',(373.345884658877,-1.30163365504601,-2.02031859898814));
#32469=CARTESIAN_POINT('Ctrl Pts',(373.438102574751,-1.31129532845678,-1.90124372202778));
#32470=CARTESIAN_POINT('Ctrl Pts',(373.490817073044,-1.3172527418389,-1.82686400301371));
#32471=CARTESIAN_POINT('Ctrl Pts',(373.641287668174,-1.33562447680424,-1.5942418129601));
#32472=CARTESIAN_POINT('Ctrl Pts',(373.728566125857,-1.3482958169094,-1.4296872979638));
#32473=CARTESIAN_POINT('Ctrl Pts',(373.852277799476,-1.36961900811238,-1.13805333331055));
#32474=CARTESIAN_POINT('Ctrl Pts',(373.896008103865,-1.37832321889661,-1.01454819113308));
#32475=CARTESIAN_POINT('Ctrl Pts',(373.936749836048,-1.38773194568131,-0.872534610306835));
#32476=CARTESIAN_POINT('Ctrl Pts',(373.941264569694,-1.38879754095607,-0.856319439980352));
#32477=CARTESIAN_POINT('Ctrl Pts',(373.948289059589,-1.39049251698641,-0.83030308892697));
#32478=CARTESIAN_POINT('Ctrl Pts',(373.950879995614,-1.3911262894118,-0.820524413205781));
#32479=CARTESIAN_POINT('Ctrl Pts',(373.955403725724,-1.39224819039015,-0.803120423362795));
#32480=CARTESIAN_POINT('Ctrl Pts',(373.95735469988,-1.39273734364157,-0.795500029692975));
#32481=CARTESIAN_POINT('Ctrl Pts',(373.961492891511,-1.39378641395246,-0.779086604805082));
#32482=CARTESIAN_POINT('Ctrl Pts',(373.963670937942,-1.39434580655475,-0.770291460256281));
#32483=CARTESIAN_POINT('Ctrl Pts',(373.969633411637,-1.39589796082156,-0.745771740457222));
#32484=CARTESIAN_POINT('Ctrl Pts',(373.973336665247,-1.3968862002701,-0.730027439506591));
#32485=CARTESIAN_POINT('Ctrl Pts',(373.994609544274,-1.40271489282909,-0.6364303745155));
#32486=CARTESIAN_POINT('Ctrl Pts',(374.009402291824,-1.40741200451704,-0.557967959226293));
#32487=CARTESIAN_POINT('Ctrl Pts',(374.053625446024,-1.42459400019484,-0.26375515789267));
#32488=CARTESIAN_POINT('Ctrl Pts',(374.06408995392,-1.43650525950244,-0.0457438994967078));
#32489=CARTESIAN_POINT('Ctrl Pts',(374.044090560933,-1.45770381222186,0.329173123690029));
#32490=CARTESIAN_POINT('Ctrl Pts',(374.024138625789,-1.46677328981929,0.485829420408144));
#32491=CARTESIAN_POINT('Ctrl Pts',(373.987440996958,-1.47783059516145,0.666828332581764));
#32492=CARTESIAN_POINT('Ctrl Pts',(373.981747739896,-1.47945607316099,0.69320316397698));
#32493=CARTESIAN_POINT('Ctrl Pts',(373.971842047904,-1.48214638609823,0.7364521997205));
#32494=CARTESIAN_POINT('Ctrl Pts',(373.967822935575,-1.4832050357469,0.75336962714913));
#32495=CARTESIAN_POINT('Ctrl Pts',(373.960328439762,-1.48512214342538,0.783817910720799));
#32496=CARTESIAN_POINT('Ctrl Pts',(373.956901585872,-1.48597901921,0.797360349651279));
#32497=CARTESIAN_POINT('Ctrl Pts',(373.949378666447,-1.48781917211601,0.826297439133791));
#32498=CARTESIAN_POINT('Ctrl Pts',(373.945256296769,-1.48880328103639,0.8416848067446));
#32499=CARTESIAN_POINT('Ctrl Pts',(373.93371348638,-1.49149489473921,0.883526544361791));
#32500=CARTESIAN_POINT('Ctrl Pts',(373.92606868449,-1.49320963475085,0.909917121305269));
#32501=CARTESIAN_POINT('Ctrl Pts',(373.881561341171,-1.50283314718759,1.0565198829922));
#32502=CARTESIAN_POINT('Ctrl Pts',(373.838029912122,-1.51095849043888,1.17457833811883));
#32503=CARTESIAN_POINT('Ctrl Pts',(373.728443780192,-1.52904514437713,1.42551381175018));
#32504=CARTESIAN_POINT('Ctrl Pts',(373.659885128132,-1.53905743583866,1.55699020692286));
#32505=CARTESIAN_POINT('Ctrl Pts',(373.494568059308,-1.56047030815258,1.8268966065613));
#32506=CARTESIAN_POINT('Ctrl Pts',(373.395469777809,-1.57184192595846,1.96341383995172));
#32507=CARTESIAN_POINT('Ctrl Pts',(373.26866089881,-1.58439566804518,2.11206469754357));
#32508=CARTESIAN_POINT('Ctrl Pts',(373.250919526167,-1.58611173562044,2.13234139263423));
#32509=CARTESIAN_POINT('Ctrl Pts',(373.226029450301,-1.58846147549171,2.16007865739174));
#32510=CARTESIAN_POINT('Ctrl Pts',(373.219096588898,-1.58910991885919,2.16773027805698));
#32511=CARTESIAN_POINT('Ctrl Pts',(373.207128557573,-1.59021876940817,2.18081217873651));
#32512=CARTESIAN_POINT('Ctrl Pts',(373.202111275254,-1.59068048500793,2.18625861023046));
#32513=CARTESIAN_POINT('Ctrl Pts',(373.191566995393,-1.59164417799432,2.19762591134269));
#32514=CARTESIAN_POINT('Ctrl Pts',(373.186036385439,-1.59214585565961,2.20354330830963));
#32515=CARTESIAN_POINT('Ctrl Pts',(373.172429702683,-1.59337103548449,2.21799200737855));
#32516=CARTESIAN_POINT('Ctrl Pts',(373.164329079463,-1.59409268028318,2.22650022701476));
#32517=CARTESIAN_POINT('Ctrl Pts',(373.134705556481,-1.59670450296204,2.25727557349824));
#32518=CARTESIAN_POINT('Ctrl Pts',(373.112907758761,-1.59857468575869,2.27927725458802));
#32519=CARTESIAN_POINT('Ctrl Pts',(373.057342318869,-1.60322478800862,2.33376844138187));
#32520=CARTESIAN_POINT('Ctrl Pts',(373.023176196394,-1.60597880729982,2.36584287316793));
#32521=CARTESIAN_POINT('Ctrl Pts',(372.782942132503,-1.62473310043034,2.58170850428326));
#32522=CARTESIAN_POINT('Ctrl Pts',(372.554880914872,-1.63962221807123,2.73893445371739));
#32523=CARTESIAN_POINT('Ctrl Pts',(372.309820561358,-1.65539601866278,2.86513687644936));
#32524=CARTESIAN_POINT('Origin',(370.834317853224,2.31077344927308,0.));
#32525=CARTESIAN_POINT('',(372.309820619203,-3.1506689542051,2.86513684665969));
#32526=CARTESIAN_POINT('',(372.309820062099,-2.90499717006881,2.86513713356015));
#32527=CARTESIAN_POINT('',(372.309820613641,2.31077344927308,2.86513684952399));
#32528=CARTESIAN_POINT('Ctrl Pts',(372.309820619203,-3.15066895420512,2.86513684665975));
#32529=CARTESIAN_POINT('Ctrl Pts',(372.494256646546,-3.13828665471397,2.77015504193128));
#32530=CARTESIAN_POINT('Ctrl Pts',(372.669133387482,-3.12679078588963,2.65756409005948));
#32531=CARTESIAN_POINT('Ctrl Pts',(373.005201576513,-3.1028362123736,2.39209106534282));
#32532=CARTESIAN_POINT('Ctrl Pts',(373.1638668757,-3.09040604357014,2.23786073095912));
#32533=CARTESIAN_POINT('Ctrl Pts',(373.326034567183,-3.07530311480665,2.04413469922012));
#32534=CARTESIAN_POINT('Ctrl Pts',(373.346181511151,-3.07337874193438,2.01932654733445));
#32535=CARTESIAN_POINT('Ctrl Pts',(373.376401816767,-3.07041521406648,1.9809623083413));
#32536=CARTESIAN_POINT('Ctrl Pts',(373.386743446553,-3.069386754737,1.96761940384665));
#32537=CARTESIAN_POINT('Ctrl Pts',(373.40535132021,-3.06750962299772,1.94321771389924));
#32538=CARTESIAN_POINT('Ctrl Pts',(373.41365228426,-3.06666234481606,1.93218582322144));
#32539=CARTESIAN_POINT('Ctrl Pts',(373.43157897608,-3.06481066079082,1.90804005292954));
#32540=CARTESIAN_POINT('Ctrl Pts',(373.441176771508,-3.06380519967878,1.8949059999212));
#32541=CARTESIAN_POINT('Ctrl Pts',(373.467179785695,-3.06104185673471,1.858750842449));
#32542=CARTESIAN_POINT('Ctrl Pts',(373.483381889237,-3.05927626475275,1.83558609197985));
#32543=CARTESIAN_POINT('Ctrl Pts',(373.570646789636,-3.04951937512063,1.70725816895095));
#32544=CARTESIAN_POINT('Ctrl Pts',(373.635745837506,-3.04130827180882,1.59819299975049));
#32545=CARTESIAN_POINT('Ctrl Pts',(373.796919155135,-3.01819094818559,1.28791587900172));
#32546=CARTESIAN_POINT('Ctrl Pts',(373.878824763584,-3.00293452645181,1.08013824551366));
#32547=CARTESIAN_POINT('Ctrl Pts',(373.957898925665,-2.98323913304865,0.796553532431933));
#32548=CARTESIAN_POINT('Ctrl Pts',(373.974844834627,-2.97849086489083,0.726875368911395));
#32549=CARTESIAN_POINT('Ctrl Pts',(373.995204596727,-2.97199930026233,0.629054171290673));
#32550=CARTESIAN_POINT('Ctrl Pts',(374.00059264999,-2.9701799321999,0.601346972410001));
#32551=CARTESIAN_POINT('Ctrl Pts',(374.009366290876,-2.96703232330613,0.552837191185859));
#32552=CARTESIAN_POINT('Ctrl Pts',(374.012913064436,-2.96569656854798,0.532065859823218));
#32553=CARTESIAN_POINT('Ctrl Pts',(374.017852846103,-2.96373871675195,0.501322087933816));
#32554=CARTESIAN_POINT('Ctrl Pts',(374.019403179898,-2.96310828157868,0.491375981256995));
#32555=CARTESIAN_POINT('Ctrl Pts',(374.022078153826,-2.96199145007601,0.473670035722993));
#32556=CARTESIAN_POINT('Ctrl Pts',(374.023221103251,-2.96150404702677,0.465913192734428));
#32557=CARTESIAN_POINT('Ctrl Pts',(374.025643722601,-2.96044822465561,0.449044993440785));
#32558=CARTESIAN_POINT('Ctrl Pts',(374.026912688976,-2.95988040700818,0.439932301985312));
#32559=CARTESIAN_POINT('Ctrl Pts',(374.030330976285,-2.9583081940656,0.414590956494544));
#32560=CARTESIAN_POINT('Ctrl Pts',(374.032395731984,-2.95730840532546,0.398350914632495));
#32561=CARTESIAN_POINT('Ctrl Pts',(374.043099625045,-2.95182893089433,0.308706667371768));
#32562=CARTESIAN_POINT('Ctrl Pts',(374.049336058315,-2.94747060153796,0.235031937306053));
#32563=CARTESIAN_POINT('Ctrl Pts',(374.054526682938,-2.94146206873297,0.131390984773724));
#32564=CARTESIAN_POINT('Ctrl Pts',(374.055605511493,-2.93974684074643,0.101559832493373));
#32565=CARTESIAN_POINT('Ctrl Pts',(374.062344523622,-2.92244630848787,-0.201194939506387));
#32566=CARTESIAN_POINT('Ctrl Pts',(374.033722096033,-2.90765131912007,-0.473770361912933));
#32567=CARTESIAN_POINT('Ctrl Pts',(373.957751897544,-2.88848200898075,-0.796022256421406));
#32568=CARTESIAN_POINT('Ctrl Pts',(373.942897890869,-2.88508167084649,-0.852186159728038));
#32569=CARTESIAN_POINT('Ctrl Pts',(373.914552920897,-2.87911194319827,-0.948724627983305));
#32570=CARTESIAN_POINT('Ctrl Pts',(373.901764686171,-2.87656450191462,-0.989290738187691));
#32571=CARTESIAN_POINT('Ctrl Pts',(373.882137339628,-2.87284679953868,-1.04750724937452));
#32572=CARTESIAN_POINT('Ctrl Pts',(373.875939370931,-2.87169756811669,-1.06537016037872));
#32573=CARTESIAN_POINT('Ctrl Pts',(373.864826997929,-2.86967883432334,-1.09650912530368));
#32574=CARTESIAN_POINT('Ctrl Pts',(373.85998159342,-2.86881163910406,-1.10980937966301));
#32575=CARTESIAN_POINT('Ctrl Pts',(373.850414306301,-2.86712401918505,-1.13554243015719));
#32576=CARTESIAN_POINT('Ctrl Pts',(373.845702770833,-2.86630395457971,-1.14797878660509));
#32577=CARTESIAN_POINT('Ctrl Pts',(373.832932760268,-2.86411001695393,-1.18106630023375));
#32578=CARTESIAN_POINT('Ctrl Pts',(373.824738067992,-2.86273159804163,-1.2016637907445));
#32579=CARTESIAN_POINT('Ctrl Pts',(373.793888374753,-2.85764678191228,-1.27693470944716));
#32580=CARTESIAN_POINT('Ctrl Pts',(373.769942231703,-2.85389718068263,-1.33106299320422));
#32581=CARTESIAN_POINT('Ctrl Pts',(373.597518565078,-2.82813818248433,-1.69349588898913));
#32582=CARTESIAN_POINT('Ctrl Pts',(373.402293377525,-2.80440328879243,-1.97702303023724));
#32583=CARTESIAN_POINT('Ctrl Pts',(373.133702723644,-2.7787142723145,-2.2585751675315));
#32584=CARTESIAN_POINT('Ctrl Pts',(373.100472854419,-2.77563780842132,-2.29191503580343));
#32585=CARTESIAN_POINT('Ctrl Pts',(373.04411582136,-2.77060271084828,-2.34603401099087));
#32586=CARTESIAN_POINT('Ctrl Pts',(373.021397700749,-2.76861990629522,-2.36722718545441));
#32587=CARTESIAN_POINT('Ctrl Pts',(372.989664091348,-2.76591839539917,-2.39598380002527));
#32588=CARTESIAN_POINT('Ctrl Pts',(372.980909168495,-2.76518006843733,-2.40383059125255));
#32589=CARTESIAN_POINT('Ctrl Pts',(372.966052119984,-2.76393917270545,-2.41700065008793));
#32590=CARTESIAN_POINT('Ctrl Pts',(372.959972564941,-2.76343476037647,-2.42234910329179));
#32591=CARTESIAN_POINT('Ctrl Pts',(372.948298110935,-2.76247267481678,-2.4325418390364));
#32592=CARTESIAN_POINT('Ctrl Pts',(372.942706615918,-2.76201471386794,-2.43738982450511));
#32593=CARTESIAN_POINT('Ctrl Pts',(372.929286083695,-2.76092214591439,-2.44894506962848));
#32594=CARTESIAN_POINT('Ctrl Pts',(372.92144140854,-2.7602888581184,-2.45563415685052));
#32595=CARTESIAN_POINT('Ctrl Pts',(372.893062655972,-2.75801651238711,-2.47959824554528));
#32596=CARTESIAN_POINT('Ctrl Pts',(372.872344475811,-2.75639244273793,-2.49665480476884));
#32597=CARTESIAN_POINT('Ctrl Pts',(372.711363198381,-2.74401752239893,-2.62584563976042));
#32598=CARTESIAN_POINT('Ctrl Pts',(372.562143796891,-2.7339431749126,-2.72635256110259));
#32599=CARTESIAN_POINT('Ctrl Pts',(372.386727736572,-2.72270331291392,-2.82428647269521));
#32600=CARTESIAN_POINT('Ctrl Pts',(372.368042424455,-2.72151342772971,-2.83447693005543));
#32601=CARTESIAN_POINT('Ctrl Pts',(372.20761748265,-2.71135068793101,-2.91991749425213));
#32602=CARTESIAN_POINT('Ctrl Pts',(372.060547142384,-2.70237177119169,-2.98466531683603));
#32603=CARTESIAN_POINT('Ctrl Pts',(371.855266364946,-2.68975724797139,-3.05729681943449));
#32604=CARTESIAN_POINT('Ctrl Pts',(371.800759775434,-2.6864019789633,-3.07496165449587));
#32605=CARTESIAN_POINT('Ctrl Pts',(371.70544912243,-2.68050441865521,-3.10306603542138));
#32606=CARTESIAN_POINT('Ctrl Pts',(371.664857005002,-2.67798333924915,-3.11417613169469));
#32607=CARTESIAN_POINT('Ctrl Pts',(371.605806234928,-2.67429723771714,-3.1291017464783));
#32608=CARTESIAN_POINT('Ctrl Pts',(371.587512353206,-2.67315273965911,-3.13355550211132));
#32609=CARTESIAN_POINT('Ctrl Pts',(371.555410334917,-2.6711394837,-3.14107357779126));
#32610=CARTESIAN_POINT('Ctrl Pts',(371.541618975692,-2.67027299448701,-3.14420780171195));
#32611=CARTESIAN_POINT('Ctrl Pts',(371.514797943536,-2.66858463925068,-3.15011775623333));
#32612=CARTESIAN_POINT('Ctrl Pts',(371.501770792257,-2.66776311942222,-3.15290367710876));
#32613=CARTESIAN_POINT('Ctrl Pts',(371.466903465057,-2.66556019443596,-3.16013445135567));
#32614=CARTESIAN_POINT('Ctrl Pts',(371.445034127,-2.66417417490402,-3.1644335827799));
#32615=CARTESIAN_POINT('Ctrl Pts',(371.364125280448,-2.65902957096483,-3.17946890355102));
#32616=CARTESIAN_POINT('Ctrl Pts',(371.304836904047,-2.65522645119721,-3.18878181593822));
#32617=CARTESIAN_POINT('Ctrl Pts',(370.90696214042,-2.62946894115874,-3.23994190048388));
#32618=CARTESIAN_POINT('Ctrl Pts',(370.563934734911,-2.60580626478598,-3.22944375383793));
#32619=CARTESIAN_POINT('Ctrl Pts',(370.182792393523,-2.58018844944854,-3.15655565993993));
#32620=CARTESIAN_POINT('Ctrl Pts',(370.136799312273,-2.57711449721953,-3.14671215622166));
#32621=CARTESIAN_POINT('Ctrl Pts',(370.060825443393,-2.57208305160301,-3.12870436499419));
#32622=CARTESIAN_POINT('Ctrl Pts',(370.030718683315,-2.57010142920158,-3.12110718363619));
#32623=CARTESIAN_POINT('Ctrl Pts',(369.989371396378,-2.56740124674508,-3.11003556223163));
#32624=CARTESIAN_POINT('Ctrl Pts',(369.978034144666,-2.56666309066174,-3.10693320394771));
#32625=CARTESIAN_POINT('Ctrl Pts',(369.958916186123,-2.5654223979759,-3.10158911519372));
#32626=CARTESIAN_POINT('Ctrl Pts',(369.951126557931,-2.56491801917305,-3.09937997980737));
#32627=CARTESIAN_POINT('Ctrl Pts',(369.936232613975,-2.56395593034292,-3.09509535243999));
#32628=CARTESIAN_POINT('Ctrl Pts',(369.929127034355,-2.5634979330401,-3.09302472051063));
#32629=CARTESIAN_POINT('Ctrl Pts',(369.912138967854,-2.56240519314657,-3.08801068491246));
#32630=CARTESIAN_POINT('Ctrl Pts',(369.90226327888,-2.56177177068374,-3.08504427260112));
#32631=CARTESIAN_POINT('Ctrl Pts',(369.866724478313,-2.55949833130275,-3.07418306741917));
#32632=CARTESIAN_POINT('Ctrl Pts',(369.841145233227,-2.55787332181643,-3.06601479524194));
#32633=CARTESIAN_POINT('Ctrl Pts',(369.644643597079,-2.54545603494258,-3.00054819028005));
#32634=CARTESIAN_POINT('Ctrl Pts',(369.478676720308,-2.5353454816319,-2.92931182610317));
#32635=CARTESIAN_POINT('Ctrl Pts',(369.164500095966,-2.51543223185407,-2.76200530275248));
#32636=CARTESIAN_POINT('Ctrl Pts',(369.016490281316,-2.50565576365396,-2.66692011534032));
#32637=CARTESIAN_POINT('Ctrl Pts',(368.829083047009,-2.49201826760763,-2.5236451214449));
#32638=CARTESIAN_POINT('Ctrl Pts',(368.78223298039,-2.48849404448916,-2.48569877140857));
#32639=CARTESIAN_POINT('Ctrl Pts',(368.70325998499,-2.48232644594049,-2.41797943402869));
#32640=CARTESIAN_POINT('Ctrl Pts',(368.670628353227,-2.47970711428,-2.38882390574285));
#32641=CARTESIAN_POINT('Ctrl Pts',(368.624604875637,-2.47590336312598,-2.34598630615332));
#32642=CARTESIAN_POINT('Ctrl Pts',(368.610724675512,-2.4747413830775,-2.33283444496604));
#32643=CARTESIAN_POINT('Ctrl Pts',(368.586749548561,-2.47270782752138,-2.30970899196102));
#32644=CARTESIAN_POINT('Ctrl Pts',(368.576601838802,-2.47183866319166,-2.29979070781147));
#32645=CARTESIAN_POINT('Ctrl Pts',(368.555825838663,-2.47004146990439,-2.27921439274485));
#32646=CARTESIAN_POINT('Ctrl Pts',(368.545206068762,-2.46911309533973,-2.26854828789052));
#32647=CARTESIAN_POINT('Ctrl Pts',(368.518227578436,-2.46672933682199,-2.24106975716668));
#32648=CARTESIAN_POINT('Ctrl Pts',(368.501977214269,-2.4652692830166,-2.22415262844367));
#32649=CARTESIAN_POINT('Ctrl Pts',(368.438934229154,-2.45950783033517,-2.15707224315787));
#32650=CARTESIAN_POINT('Ctrl Pts',(368.39356628741,-2.45514687447327,-2.10560063082864));
#32651=CARTESIAN_POINT('Ctrl Pts',(368.139251992464,-2.42939235941282,-1.79780049246657));
#32652=CARTESIAN_POINT('Ctrl Pts',(367.969165400526,-2.40646284702157,-1.51204992548336));
#32653=CARTESIAN_POINT('Ctrl Pts',(367.828074730364,-2.38156851011381,-1.16223655203076));
#32654=CARTESIAN_POINT('Ctrl Pts',(367.811573820574,-2.3785215340526,-1.11861989520291));
#32655=CARTESIAN_POINT('Ctrl Pts',(367.785736607136,-2.37352934473963,-1.04557246561894));
#32656=CARTESIAN_POINT('Ctrl Pts',(367.775866518286,-2.37156044957382,-1.0163390131899));
#32657=CARTESIAN_POINT('Ctrl Pts',(367.762826646044,-2.3688745825874,-0.975805716625654));
#32658=CARTESIAN_POINT('Ctrl Pts',(367.759296811055,-2.3681382782774,-0.964624607078675));
#32659=CARTESIAN_POINT('Ctrl Pts',(367.753434371918,-2.36689979286245,-0.945695511522337));
#32660=CARTESIAN_POINT('Ctrl Pts',(367.751069802247,-2.36639578417202,-0.937957614790712));
#32661=CARTESIAN_POINT('Ctrl Pts',(367.746596362837,-2.36543369587093,-0.923118858001552));
#32662=CARTESIAN_POINT('Ctrl Pts',(367.744482806035,-2.36497533366303,-0.916019547807302));
#32663=CARTESIAN_POINT('Ctrl Pts',(367.739478989244,-2.36388080439427,-0.898997651218655));
#32664=CARTESIAN_POINT('Ctrl Pts',(367.736611924758,-2.36324596731442,-0.889068252945829));
#32665=CARTESIAN_POINT('Ctrl Pts',(367.726421249971,-2.3609606395984,-0.853127469308557));
#32666=CARTESIAN_POINT('Ctrl Pts',(367.71937686776,-2.35932536777931,-0.827037206556625));
#32667=CARTESIAN_POINT('Ctrl Pts',(367.671653771437,-2.34781390570902,-0.641018385861111));
#32668=CARTESIAN_POINT('Ctrl Pts',(367.642978621136,-2.3385060377231,-0.478242329656994));
#32669=CARTESIAN_POINT('Ctrl Pts',(367.623318008137,-2.32720143846736,-0.277395091620869));
#32670=CARTESIAN_POINT('Ctrl Pts',(367.620363661911,-2.32514723497933,-0.240762360852559));
#32671=CARTESIAN_POINT('Ctrl Pts',(367.613782807552,-2.3193367437615,-0.137052294487127));
#32672=CARTESIAN_POINT('Ctrl Pts',(367.611625986118,-2.31558027910065,-0.0699016882072931));
#32673=CARTESIAN_POINT('Ctrl Pts',(367.611426460719,-2.30232962703521,0.165325704249052));
#32674=CARTESIAN_POINT('Ctrl Pts',(367.624429434822,-2.29269715389302,0.333117854404309));
#32675=CARTESIAN_POINT('Ctrl Pts',(367.654675637949,-2.28100704750822,0.526057466281077));
#32676=CARTESIAN_POINT('Ctrl Pts',(367.659240257185,-2.27936465206984,0.552940562310314));
#32677=CARTESIAN_POINT('Ctrl Pts',(367.667288723925,-2.2766521683846,0.59695005685734));
#32678=CARTESIAN_POINT('Ctrl Pts',(367.670571784686,-2.27558844298291,0.614112099960196));
#32679=CARTESIAN_POINT('Ctrl Pts',(367.676731317483,-2.27366599201807,0.644949692272733));
#32680=CARTESIAN_POINT('Ctrl Pts',(367.679557503801,-2.27280888906427,0.658634924855483));
#32681=CARTESIAN_POINT('Ctrl Pts',(367.685782580613,-2.27097246476489,0.687818986536376));
#32682=CARTESIAN_POINT('Ctrl Pts',(367.689207098644,-2.26999234311787,0.703311913845366));
#32683=CARTESIAN_POINT('Ctrl Pts',(367.698810888621,-2.26732238908112,0.745287278058035));
#32684=CARTESIAN_POINT('Ctrl Pts',(367.705211061347,-2.26562551852846,0.771717347298704));
#32685=CARTESIAN_POINT('Ctrl Pts',(367.741910819588,-2.25631883178027,0.915302992611616));
#32686=CARTESIAN_POINT('Ctrl Pts',(367.778452717587,-2.24850926187905,1.03074879460554));
#32687=CARTESIAN_POINT('Ctrl Pts',(367.878772725009,-2.22987169017638,1.29499227150133));
#32688=CARTESIAN_POINT('Ctrl Pts',(367.947438512769,-2.21893049770601,1.44158675921385));
#32689=CARTESIAN_POINT('Ctrl Pts',(368.067193597863,-2.20243627285231,1.65405777584262));
#32690=CARTESIAN_POINT('Ctrl Pts',(368.110312478033,-2.19688499021178,1.72414596709367));
#32691=CARTESIAN_POINT('Ctrl Pts',(368.207602897065,-2.18522727202252,1.86951097632006));
#32692=CARTESIAN_POINT('Ctrl Pts',(368.262440819754,-2.1791443702264,1.9442619630939));
#32693=CARTESIAN_POINT('Ctrl Pts',(368.330365858588,-2.17223979953017,2.0289391690068));
#32694=CARTESIAN_POINT('Ctrl Pts',(368.340394132298,-2.17123539107492,2.04125310554076));
#32695=CARTESIAN_POINT('Ctrl Pts',(368.356844370827,-2.16961258071302,2.06115051165966));
#32696=CARTESIAN_POINT('Ctrl Pts',(368.363210971184,-2.16899043771208,2.06877912581562));
#32697=CARTESIAN_POINT('Ctrl Pts',(368.374658490684,-2.16788250678358,2.08236757388315));
#32698=CARTESIAN_POINT('Ctrl Pts',(368.37972593866,-2.16739577664318,2.08833843749012));
#32699=CARTESIAN_POINT('Ctrl Pts',(368.390857813417,-2.16633466372496,2.10135838373816));
#32700=CARTESIAN_POINT('Ctrl Pts',(368.396930998223,-2.16576093384717,2.10839971238249));
#32701=CARTESIAN_POINT('Ctrl Pts',(368.414382127844,-2.1641267384332,2.12845660094871));
#32702=CARTESIAN_POINT('Ctrl Pts',(368.425834635548,-2.16307160143824,2.1414072563427));
#32703=CARTESIAN_POINT('Ctrl Pts',(368.507648908458,-2.15565019748023,2.23243727316014));
#32704=CARTESIAN_POINT('Ctrl Pts',(368.581696551776,-2.14953410541245,2.30713382454027));
#32705=CARTESIAN_POINT('Ctrl Pts',(368.821603144342,-2.13097894252752,2.52655760934273));
#32706=CARTESIAN_POINT('Ctrl Pts',(368.998713745804,-2.11894688404738,2.65802146027684));
#32707=CARTESIAN_POINT('Ctrl Pts',(369.299829473686,-2.0990136181496,2.8369761854604));
#32708=CARTESIAN_POINT('Ctrl Pts',(369.415738243686,-2.09145740983911,2.89667303631612));
#32709=CARTESIAN_POINT('Ctrl Pts',(369.560961845954,-2.0819466673311,2.96065720434556));
#32710=CARTESIAN_POINT('Ctrl Pts',(369.587141089391,-2.08023084974059,2.97178004641657));
#32711=CARTESIAN_POINT('Ctrl Pts',(369.628555050189,-2.07751288666328,2.98873209583485));
#32712=CARTESIAN_POINT('Ctrl Pts',(369.64369303525,-2.0765186399789,2.99479481858454));
#32713=CARTESIAN_POINT('Ctrl Pts',(369.671729545066,-2.07467555498135,3.00577719528103));
#32714=CARTESIAN_POINT('Ctrl Pts',(369.684614979387,-2.0738278341478,3.01072938246388));
#32715=CARTESIAN_POINT('Ctrl Pts',(369.713285015953,-2.07194003946472,3.0215370879688));
#32716=CARTESIAN_POINT('Ctrl Pts',(369.729084403441,-2.07089863658552,3.02735197829491));
#32717=CARTESIAN_POINT('Ctrl Pts',(369.774796307102,-2.06788209406325,3.0437704961702));
#32718=CARTESIAN_POINT('Ctrl Pts',(369.804820159089,-2.06589651441403,3.05405617533953));
#32719=CARTESIAN_POINT('Ctrl Pts',(369.87293830879,-2.06138062060792,3.07627375102281));
#32720=CARTESIAN_POINT('Ctrl Pts',(369.911111694824,-2.05884221388878,3.08794445917764));
#32721=CARTESIAN_POINT('Ctrl Pts',(370.03685612037,-2.05045400100331,3.12384816199758));
#32722=CARTESIAN_POINT('Ctrl Pts',(370.125230485309,-2.04451535904278,3.14508589738989));
#32723=CARTESIAN_POINT('Ctrl Pts',(370.350851779475,-2.02927120626128,3.18931323785587));
#32724=CARTESIAN_POINT('Ctrl Pts',(370.488907247141,-2.0198624217125,3.20720216957262));
#32725=CARTESIAN_POINT('Ctrl Pts',(370.79195465275,-1.99932174985938,3.22667341307807));
#32726=CARTESIAN_POINT('Ctrl Pts',(370.956815300839,-1.98821820321541,3.2246272095518));
#32727=CARTESIAN_POINT('Ctrl Pts',(371.147753243404,-1.97590094640662,3.20758593100874));
#32728=CARTESIAN_POINT('Ctrl Pts',(371.174665544676,-1.97417783571976,3.20484208799174));
#32729=CARTESIAN_POINT('Ctrl Pts',(371.211812331567,-1.97182031607334,3.20058156702063));
#32730=CARTESIAN_POINT('Ctrl Pts',(371.22207799187,-1.97117101573503,3.19935408013054));
#32731=CARTESIAN_POINT('Ctrl Pts',(371.239689214252,-1.97006111120245,3.19716225793784));
#32732=CARTESIAN_POINT('Ctrl Pts',(371.247037609574,-1.96959919377444,3.19622196495526));
#32733=CARTESIAN_POINT('Ctrl Pts',(371.262404231841,-1.96863585265251,3.1942017892765));
#32734=CARTESIAN_POINT('Ctrl Pts',(371.270421722098,-1.96813472476631,3.19311704067928));
#32735=CARTESIAN_POINT('Ctrl Pts',(371.290044130519,-1.96691171723678,3.19038688892539));
#32736=CARTESIAN_POINT('Ctrl Pts',(371.301644464318,-1.96619168256136,3.188708326151));
#32737=CARTESIAN_POINT('Ctrl Pts',(371.343717274083,-1.96359020216431,3.18238588287451));
#32738=CARTESIAN_POINT('Ctrl Pts',(371.374132952802,-1.9617285541274,3.17736801370667));
#32739=CARTESIAN_POINT('Ctrl Pts',(371.450307084205,-1.95710353647795,3.16367562343212));
#32740=CARTESIAN_POINT('Ctrl Pts',(371.495959301325,-1.95436572106415,3.15444404045581));
#32741=CARTESIAN_POINT('Ctrl Pts',(371.808552996556,-1.93575593317946,3.08414735308054));
#32742=CARTESIAN_POINT('Ctrl Pts',(372.066748857434,-1.92098113377829,2.99031518462765));
#32743=CARTESIAN_POINT('Ctrl Pts',(372.309820657226,-1.90534924053903,2.86513682707866));
#32744=CARTESIAN_POINT('',(367.61156894943,-2.06176984286323,0.0015491427833167));
#32745=CARTESIAN_POINT('Ctrl Pts',(372.309820561358,-1.65539601866277,2.86513687644937));
#32746=CARTESIAN_POINT('Ctrl Pts',(372.256427656497,-1.65883275994792,2.89263342517085));
#32747=CARTESIAN_POINT('Ctrl Pts',(372.202227534331,-1.66230651349411,2.91865739099724));
#32748=CARTESIAN_POINT('Ctrl Pts',(372.088942520497,-1.6695691048338,2.96919430498641));
#32749=CARTESIAN_POINT('Ctrl Pts',(372.029849064809,-1.67335869469997,2.99347660446399));
#32750=CARTESIAN_POINT('Ctrl Pts',(371.948695006037,-1.67858363058956,3.02403754878361));
#32751=CARTESIAN_POINT('Ctrl Pts',(371.927229498561,-1.67996751717465,3.03186141330077));
#32752=CARTESIAN_POINT('Ctrl Pts',(371.891602832077,-1.68226826229659,3.04441930754466));
#32753=CARTESIAN_POINT('Ctrl Pts',(371.877488503411,-1.68318075362313,3.04928441268975));
#32754=CARTESIAN_POINT('Ctrl Pts',(371.849817280911,-1.68497186995512,3.0586078746352));
#32755=CARTESIAN_POINT('Ctrl Pts',(371.836263556777,-1.68585019417586,3.06307460162666));
#32756=CARTESIAN_POINT('Ctrl Pts',(371.804081815276,-1.68793827176251,3.0734438754171));
#32757=CARTESIAN_POINT('Ctrl Pts',(371.785429064989,-1.68915058944043,3.07926725591095));
#32758=CARTESIAN_POINT('Ctrl Pts',(371.722534160148,-1.69324588665021,3.09827703182328));
#32759=CARTESIAN_POINT('Ctrl Pts',(371.6780635561,-1.69615403627469,3.11068185585343));
#32760=CARTESIAN_POINT('Ctrl Pts',(371.570697304627,-1.70320842622309,3.1381594087761));
#32761=CARTESIAN_POINT('Ctrl Pts',(371.507586334424,-1.70738227212509,3.15230198587124));
#32762=CARTESIAN_POINT('Ctrl Pts',(371.25598829793,-1.72412475413989,3.20078270499804));
#32763=CARTESIAN_POINT('Ctrl Pts',(371.065040122354,-1.73708826581574,3.22018150893149));
#32764=CARTESIAN_POINT('Ctrl Pts',(370.794216674312,-1.75540057084861,3.22347637137753));
#32765=CARTESIAN_POINT('Ctrl Pts',(370.714899010365,-1.76074997606981,3.22151329963644));
#32766=CARTESIAN_POINT('Ctrl Pts',(370.543968104798,-1.77216053525531,3.21096050591037));
#32767=CARTESIAN_POINT('Ctrl Pts',(370.452479012519,-1.77819469180759,3.2013704385472));
#32768=CARTESIAN_POINT('Ctrl Pts',(370.345828073707,-1.78505214873581,3.18555283518526));
#32769=CARTESIAN_POINT('Ctrl Pts',(370.330155815924,-1.78605530746706,3.18311008201246));
#32770=CARTESIAN_POINT('Ctrl Pts',(370.304696405869,-1.78767684059574,3.17894910313233));
#32771=CARTESIAN_POINT('Ctrl Pts',(370.294898252696,-1.78829894048797,3.17730117844474));
#32772=CARTESIAN_POINT('Ctrl Pts',(370.277384095224,-1.78940725311997,3.1742721670413));
#32773=CARTESIAN_POINT('Ctrl Pts',(370.26966537397,-1.78989440474434,3.17290822164588));
#32774=CARTESIAN_POINT('Ctrl Pts',(370.252783819291,-1.79095699538033,3.16986159201016));
#32775=CARTESIAN_POINT('Ctrl Pts',(370.243623279859,-1.7915317760844,3.16816733636552));
#32776=CARTESIAN_POINT('Ctrl Pts',(370.21742640976,-1.7931706279896,3.16320461257788));
#32777=CARTESIAN_POINT('Ctrl Pts',(370.200408651208,-1.79422932871363,3.15983822816909));
#32778=CARTESIAN_POINT('Ctrl Pts',(370.079095348345,-1.80173947406436,3.13482099598137));
#32779=CARTESIAN_POINT('Ctrl Pts',(369.975891443623,-1.80793396323129,3.10814617211976));
#32780=CARTESIAN_POINT('Ctrl Pts',(369.656186870956,-1.82703720164101,3.00836811791855));
#32781=CARTESIAN_POINT('Ctrl Pts',(369.446032725797,-1.83951095116339,2.91735196177768));
#32782=CARTESIAN_POINT('Ctrl Pts',(369.141829889757,-1.8594617631227,2.74522785258736));
#32783=CARTESIAN_POINT('Ctrl Pts',(369.039858199459,-1.86650800055447,2.67968306097314));
#32784=CARTESIAN_POINT('Ctrl Pts',(368.91914078599,-1.87544936356169,2.59210333776315));
#32785=CARTESIAN_POINT('Ctrl Pts',(368.896673689478,-1.87714032265486,2.57535200160633));
#32786=CARTESIAN_POINT('Ctrl Pts',(368.861552889903,-1.87982794179045,2.54844639651482));
#32787=CARTESIAN_POINT('Ctrl Pts',(368.848752184977,-1.88081700477486,2.53848569002763));
#32788=CARTESIAN_POINT('Ctrl Pts',(368.825535570872,-1.88262856022891,2.52013692884033));
#32789=CARTESIAN_POINT('Ctrl Pts',(368.815095588292,-1.88344980725576,2.51177981404762));
#32790=CARTESIAN_POINT('Ctrl Pts',(368.804498644258,-1.88429027674603,2.50318828977826));
#32791=CARTESIAN_POINT('Ctrl Pts',(368.804289264825,-1.88430688589198,2.5030184908338));
#32792=CARTESIAN_POINT('Ctrl Pts',(368.80389752159,-1.8843379663048,2.50270072013022));
#32793=CARTESIAN_POINT('Ctrl Pts',(368.803715152861,-1.8843524372987,2.50255275487497));
#32794=CARTESIAN_POINT('Ctrl Pts',(368.803373368314,-1.88437956188626,2.50227538529875));
#32795=CARTESIAN_POINT('Ctrl Pts',(368.803213948856,-1.88439221527622,2.50214598581336));
#32796=CARTESIAN_POINT('Ctrl Pts',(368.802914734581,-1.88441596741558,2.50190306856553));
#32797=CARTESIAN_POINT('Ctrl Pts',(368.802774936996,-1.8844270660158,2.50178955438925));
#32798=CARTESIAN_POINT('Ctrl Pts',(368.802512214525,-1.88444792599529,2.50157618995164));
#32799=CARTESIAN_POINT('Ctrl Pts',(368.802389287178,-1.88445768729145,2.50147634209593));
#32800=CARTESIAN_POINT('Ctrl Pts',(368.802017404867,-1.88448722024115,2.50117423483383));
#32801=CARTESIAN_POINT('Ctrl Pts',(368.801768473088,-1.88450699300504,2.50097194760267));
#32802=CARTESIAN_POINT('Ctrl Pts',(368.801276676802,-1.88454606432086,2.50057218161234));
#32803=CARTESIAN_POINT('Ctrl Pts',(368.801033810647,-1.88456536281757,2.50037470445559));
#32804=CARTESIAN_POINT('Ctrl Pts',(368.800553708391,-1.88460351979304,2.49998421179604));
#32805=CARTESIAN_POINT('Ctrl Pts',(368.800316471404,-1.88462237817355,2.49979119823808));
#32806=CARTESIAN_POINT('Ctrl Pts',(368.7998472235,-1.8846596865331,2.49940931197583));
#32807=CARTESIAN_POINT('Ctrl Pts',(368.79961521128,-1.88467813646258,2.49922044063089));
#32808=CARTESIAN_POINT('Ctrl Pts',(368.799156037245,-1.88471465734252,2.49884654012972));
#32809=CARTESIAN_POINT('Ctrl Pts',(368.798928873944,-1.8847327282719,2.49866151196304));
#32810=CARTESIAN_POINT('Ctrl Pts',(368.786018800195,-1.88575991516695,2.48814312017868));
#32811=CARTESIAN_POINT('Ctrl Pts',(368.773414922018,-1.88677291736464,2.47771352046107));
#32812=CARTESIAN_POINT('Ctrl Pts',(368.746534915753,-1.88895554737861,2.45512354789626));
#32813=CARTESIAN_POINT('Ctrl Pts',(368.73228448108,-1.89012636229239,2.4429336683449));
#32814=CARTESIAN_POINT('Ctrl Pts',(368.695217002445,-1.89320832797246,2.41066152700094));
#32815=CARTESIAN_POINT('Ctrl Pts',(368.672576686812,-1.89512763637953,2.39037998569962));
#32816=CARTESIAN_POINT('Ctrl Pts',(368.605235293649,-1.9009500001155,2.32831532375715));
#32817=CARTESIAN_POINT('Ctrl Pts',(368.561435915633,-1.90489193131936,2.2855783122875));
#32818=CARTESIAN_POINT('Ctrl Pts',(368.393364739012,-1.92064500992626,2.11197278671562));
#32819=CARTESIAN_POINT('Ctrl Pts',(368.278971183362,-1.93281174592096,1.97202224398151));
#32820=CARTESIAN_POINT('Ctrl Pts',(368.07864342318,-1.95676751090956,1.68004163338432));
#32821=CARTESIAN_POINT('Ctrl Pts',(367.992114455196,-1.96850972103909,1.52910839604845));
#32822=CARTESIAN_POINT('Ctrl Pts',(367.906684779315,-1.98140340992467,1.34751978341968));
#32823=CARTESIAN_POINT('Ctrl Pts',(367.895509715891,-1.98312141594579,1.32297083285518));
#32824=CARTESIAN_POINT('Ctrl Pts',(367.880481183239,-1.98547355709268,1.28882630959208));
#32825=CARTESIAN_POINT('Ctrl Pts',(367.876364059119,-1.98612248703803,1.27934893129843));
#32826=CARTESIAN_POINT('Ctrl Pts',(367.869372724665,-1.98723214000185,1.26304111465651));
#32827=CARTESIAN_POINT('Ctrl Pts',(367.866476389915,-1.98769417265049,1.25622033257258));
#32828=CARTESIAN_POINT('Ctrl Pts',(367.860463652257,-1.98865816994591,1.24192365003193));
#32829=CARTESIAN_POINT('Ctrl Pts',(367.857351870958,-1.98915983585674,1.23444590943358));
#32830=CARTESIAN_POINT('Ctrl Pts',(367.849796326701,-1.99038492395569,1.21609489440479));
#32831=CARTESIAN_POINT('Ctrl Pts',(367.845383700749,-1.99110648961312,1.20520876887073));
#32832=CARTESIAN_POINT('Ctrl Pts',(367.829556095328,-1.99371793443876,1.16553981950728));
#32833=CARTESIAN_POINT('Ctrl Pts',(367.818496149464,-1.99558782319623,1.13661598815687));
#32834=CARTESIAN_POINT('Ctrl Pts',(367.791755328348,-2.00023710176736,1.0635437667978));
#32835=CARTESIAN_POINT('Ctrl Pts',(367.776616630551,-2.00299059945996,1.01920347747206));
#32836=CARTESIAN_POINT('Ctrl Pts',(367.662615351118,-2.02488194521479,0.659860088865763));
#32837=CARTESIAN_POINT('Ctrl Pts',(367.611727293097,-2.04248769501544,0.331713486549737));
#32838=CARTESIAN_POINT('Ctrl Pts',(367.611568227248,-2.06176838145633,0.00155266577040972));
#32839=CARTESIAN_POINT('Ctrl Pts',(367.611568225518,-2.06176859143958,0.00154907003543143));
#32840=CARTESIAN_POINT('Ctrl Pts',(367.611546633093,-2.06439192849467,-0.0433727063854235));
#32841=CARTESIAN_POINT('Ctrl Pts',(367.612464284761,-2.0670394314014,-0.0882888458202929));
#32842=CARTESIAN_POINT('Ctrl Pts',(367.615628263428,-2.07159962404561,-0.164792515275044));
#32843=CARTESIAN_POINT('Ctrl Pts',(367.617401797135,-2.07349803938567,-0.196393052452183));
#32844=CARTESIAN_POINT('Ctrl Pts',(367.620729361154,-2.07634126754824,-0.243317832966538));
#32845=CARTESIAN_POINT('Ctrl Pts',(367.621928323142,-2.07727507846268,-0.258665920748005));
#32846=CARTESIAN_POINT('Ctrl Pts',(367.624351168571,-2.0790100022435,-0.287059427078281));
#32847=CARTESIAN_POINT('Ctrl Pts',(367.62554473616,-2.07981015341681,-0.300107158391464));
#32848=CARTESIAN_POINT('Ctrl Pts',(367.62809848877,-2.08142023748647,-0.326264710521572));
#32849=CARTESIAN_POINT('Ctrl Pts',(367.629459599074,-2.08223018463649,-0.339374184267279));
#32850=CARTESIAN_POINT('Ctrl Pts',(367.632802323081,-2.08411431600601,-0.369754054174064));
#32851=CARTESIAN_POINT('Ctrl Pts',(367.63484332118,-2.08519034836884,-0.3870173770874));
#32852=CARTESIAN_POINT('Ctrl Pts',(367.640404633975,-2.08794597749298,-0.431001488096569));
#32853=CARTESIAN_POINT('Ctrl Pts',(367.644120609317,-2.08963167681436,-0.457695760212168));
#32854=CARTESIAN_POINT('Ctrl Pts',(367.661353683028,-2.09684869458605,-0.571060639319669));
#32855=CARTESIAN_POINT('Ctrl Pts',(367.678070430414,-2.10247912570915,-0.657199931490127));
#32856=CARTESIAN_POINT('Ctrl Pts',(367.738432555735,-2.11958476397544,-0.912131615638865));
#32857=CARTESIAN_POINT('Ctrl Pts',(367.792273324021,-2.13133289366246,-1.07816676233011));
#32858=CARTESIAN_POINT('Ctrl Pts',(367.931791879193,-2.15588417851675,-1.41317009708529));
#32859=CARTESIAN_POINT('Ctrl Pts',(368.0194799626,-2.16864660013255,-1.58063575687867));
#32860=CARTESIAN_POINT('Ctrl Pts',(368.131533699801,-2.18187099570145,-1.75540110910275));
#32861=CARTESIAN_POINT('Ctrl Pts',(368.141881798728,-2.18306780038168,-1.77123216044541));
#32862=CARTESIAN_POINT('Ctrl Pts',(368.157714737254,-2.18486142011126,-1.79499478286253));
#32863=CARTESIAN_POINT('Ctrl Pts',(368.16309658641,-2.18546472374789,-1.80299402669822));
#32864=CARTESIAN_POINT('Ctrl Pts',(368.172480589219,-2.18650553100239,-1.81680757406896));
#32865=CARTESIAN_POINT('Ctrl Pts',(368.176466002879,-2.18694413230798,-1.82263296515406));
#32866=CARTESIAN_POINT('Ctrl Pts',(368.185706266837,-2.18795314990762,-1.83604449427088));
#32867=CARTESIAN_POINT('Ctrl Pts',(368.190974577409,-2.18852264380473,-1.84362117899666));
#32868=CARTESIAN_POINT('Ctrl Pts',(368.205738330371,-2.19010285076731,-1.86466046566565));
#32869=CARTESIAN_POINT('Ctrl Pts',(368.215304715869,-2.1911088859725,-1.87807326077123));
#32870=CARTESIAN_POINT('Ctrl Pts',(368.269333861316,-2.19669551929634,-1.95261048438364));
#32871=CARTESIAN_POINT('Ctrl Pts',(368.315837006173,-2.20114909003744,-2.01223426153285));
#32872=CARTESIAN_POINT('Ctrl Pts',(368.381480855756,-2.20706066195212,-2.09055386817888));
#32873=CARTESIAN_POINT('Ctrl Pts',(368.398815907494,-2.20858886995154,-2.11072384266777));
#32874=CARTESIAN_POINT('Ctrl Pts',(368.597656367092,-2.22578045549424,-2.33637044740378));
#32875=CARTESIAN_POINT('Ctrl Pts',(368.804416905435,-2.24063341297452,-2.51809342576822));
#32876=CARTESIAN_POINT('Ctrl Pts',(369.079939811531,-2.25987609302753,-2.70400861958595));
#32877=CARTESIAN_POINT('Ctrl Pts',(369.129055609753,-2.26328285912067,-2.7352486258766));
#32878=CARTESIAN_POINT('Ctrl Pts',(369.204172117929,-2.26847708825232,-2.78021652995913));
#32879=CARTESIAN_POINT('Ctrl Pts',(369.22956003075,-2.27022992155853,-2.7949474629069));
#32880=CARTESIAN_POINT('Ctrl Pts',(369.276592838333,-2.27347453210016,-2.82138542232974));
#32881=CARTESIAN_POINT('Ctrl Pts',(369.29817755057,-2.27496257576627,-2.83319534143244));
#32882=CARTESIAN_POINT('Ctrl Pts',(369.329969612686,-2.27715375935871,-2.85012003224718));
#32883=CARTESIAN_POINT('Ctrl Pts',(369.340072617701,-2.27784999996492,-2.8554297396209));
#32884=CARTESIAN_POINT('Ctrl Pts',(369.362342841243,-2.27938467181118,-2.86698345874105));
#32885=CARTESIAN_POINT('Ctrl Pts',(369.37452198169,-2.2802239124323,-2.87320388989754));
#32886=CARTESIAN_POINT('Ctrl Pts',(369.401230291938,-2.2820644191832,-2.88663136470035));
#32887=CARTESIAN_POINT('Ctrl Pts',(369.415774952658,-2.28306676995659,-2.89380659648641));
#32888=CARTESIAN_POINT('Ctrl Pts',(369.455593469559,-2.28581135181107,-2.91307770225725));
#32889=CARTESIAN_POINT('Ctrl Pts',(369.480971438898,-2.2875611135408,-2.92495402163588));
#32890=CARTESIAN_POINT('Ctrl Pts',(369.617033355851,-2.29694747097019,-2.98647812592677));
#32891=CARTESIAN_POINT('Ctrl Pts',(369.730287102389,-2.30478386760349,-3.03017214018948));
#32892=CARTESIAN_POINT('Ctrl Pts',(370.061681290645,-2.32776056841907,-3.13697829753263));
#32893=CARTESIAN_POINT('Ctrl Pts',(370.284380038398,-2.34330083795763,-3.18357561894358));
#32894=CARTESIAN_POINT('Ctrl Pts',(370.582674517578,-2.3633685698636,-3.21373847321718));
#32895=CARTESIAN_POINT('Ctrl Pts',(370.655487941078,-2.3682035039931,-3.21861158485213));
#32896=CARTESIAN_POINT('Ctrl Pts',(370.770878612462,-2.37570704911475,-3.22240573385288));
#32897=CARTESIAN_POINT('Ctrl Pts',(370.813374951208,-2.37843641072064,-3.22296215457504));
#32898=CARTESIAN_POINT('Ctrl Pts',(370.869107368796,-2.38196067640316,-3.22258939845419));
#32899=CARTESIAN_POINT('Ctrl Pts',(370.882342189019,-2.38279350117328,-3.22241934247874));
#32900=CARTESIAN_POINT('Ctrl Pts',(370.903989983376,-2.38414863332975,-3.22200778707792));
#32901=CARTESIAN_POINT('Ctrl Pts',(370.912403571084,-2.3846735628551,-3.22181486280806));
#32902=CARTESIAN_POINT('Ctrl Pts',(370.928827448387,-2.3856947092498,-3.22137388729834));
#32903=CARTESIAN_POINT('Ctrl Pts',(370.936837692888,-2.38619108357238,-3.22112891229201));
#32904=CARTESIAN_POINT('Ctrl Pts',(370.956558825057,-2.38740924266884,-3.22045214769007));
#32905=CARTESIAN_POINT('Ctrl Pts',(370.968268575687,-2.38812915185582,-3.2199863516109));
#32906=CARTESIAN_POINT('Ctrl Pts',(371.008580204285,-2.39059659983677,-3.21816253257003));
#32907=CARTESIAN_POINT('Ctrl Pts',(371.037167278517,-2.39232751339454,-3.21648716642913));
#32908=CARTESIAN_POINT('Ctrl Pts',(371.389293736767,-2.41345692753949,-3.19113707990928));
#32909=CARTESIAN_POINT('Ctrl Pts',(371.707529922617,-2.43072098806815,-3.11912207645665));
#32910=CARTESIAN_POINT('Ctrl Pts',(372.118449290802,-2.45596755326888,-2.95816981991702));
#32911=CARTESIAN_POINT('Ctrl Pts',(372.224806962655,-2.46277778123383,-2.90969035176546));
#32912=CARTESIAN_POINT('Ctrl Pts',(372.352167340394,-2.47140557027467,-2.84305761203099));
#32913=CARTESIAN_POINT('Ctrl Pts',(372.375884956472,-2.47303305553731,-2.83026755807345));
#32914=CARTESIAN_POINT('Ctrl Pts',(372.413268377565,-2.47563279096866,-2.809498725831));
#32915=CARTESIAN_POINT('Ctrl Pts',(372.427040927419,-2.47659811348342,-2.80171394752034));
#32916=CARTESIAN_POINT('Ctrl Pts',(372.452885742144,-2.47842412816016,-2.78685330531481));
#32917=CARTESIAN_POINT('Ctrl Pts',(372.464970363672,-2.47928400609428,-2.77979958571805));
#32918=CARTESIAN_POINT('Ctrl Pts',(372.492129672036,-2.48123043958634,-2.76370882018954));
#32919=CARTESIAN_POINT('Ctrl Pts',(372.507177042042,-2.48231861714963,-2.75462675950499));
#32920=CARTESIAN_POINT('Ctrl Pts',(372.545647251175,-2.48512625548045,-2.73097603571204));
#32921=CARTESIAN_POINT('Ctrl Pts',(372.568958320109,-2.4868522174586,-2.71622914913098));
#32922=CARTESIAN_POINT('Ctrl Pts',(372.752800690613,-2.50066485059672,-2.59659627707509));
#32923=CARTESIAN_POINT('Ctrl Pts',(372.903842121649,-2.51327904557552,-2.47788936103686));
#32924=CARTESIAN_POINT('Ctrl Pts',(373.179072185367,-2.53869480083802,-2.21877367999824));
#32925=CARTESIAN_POINT('Ctrl Pts',(373.303395187075,-2.55142849190428,-2.07954034199217));
#32926=CARTESIAN_POINT('Ctrl Pts',(373.460739176643,-2.56881759540263,-1.8691874027074));
#32927=CARTESIAN_POINT('Ctrl Pts',(373.504300779354,-2.57379713306532,-1.80641736822578));
#32928=CARTESIAN_POINT('Ctrl Pts',(373.554235222029,-2.57966059369886,-1.72870546663604));
#32929=CARTESIAN_POINT('Ctrl Pts',(373.562776437828,-2.58066944973846,-1.71519295128393));
#32930=CARTESIAN_POINT('Ctrl Pts',(373.575980673352,-2.58223776543875,-1.69395511820842));
#32931=CARTESIAN_POINT('Ctrl Pts',(373.58071225831,-2.58280154183277,-1.68627303191747));
#32932=CARTESIAN_POINT('Ctrl Pts',(373.589512585921,-2.58385333842673,-1.67184973663547));
#32933=CARTESIAN_POINT('Ctrl Pts',(373.593588854309,-2.58434182656368,-1.66511353996758));
#32934=CARTESIAN_POINT('Ctrl Pts',(373.602878870233,-2.58545820722565,-1.64963362200546));
#32935=CARTESIAN_POINT('Ctrl Pts',(373.608075909937,-2.58608501793485,-1.64088008127678));
#32936=CARTESIAN_POINT('Ctrl Pts',(373.624485834297,-2.58807201306248,-1.61293957000483));
#32937=CARTESIAN_POINT('Ctrl Pts',(373.635542051682,-2.58942253808624,-1.5936607140069));
#32938=CARTESIAN_POINT('Ctrl Pts',(373.648990927178,-2.59108214438442,-1.56963728881009));
#32939=CARTESIAN_POINT('Ctrl Pts',(373.651572122507,-2.59140145520163,-1.56499971714145));
#32940=CARTESIAN_POINT('Ctrl Pts',(373.759866287628,-2.60483243227363,-1.3692940353964));
#32941=CARTESIAN_POINT('Ctrl Pts',(373.845913690395,-2.61691322161687,-1.1679541444941));
#32942=CARTESIAN_POINT('Ctrl Pts',(373.955451091337,-2.63749536761685,-0.816700205933311));
#32943=CARTESIAN_POINT('Ctrl Pts',(373.989973260656,-2.64589345959054,-0.67104871204428));
#32944=CARTESIAN_POINT('Ctrl Pts',(374.023189153743,-2.65775822384725,-0.469296341066459));
#32945=CARTESIAN_POINT('Ctrl Pts',(374.030729409801,-2.6609820745336,-0.414839613979763));
#32946=CARTESIAN_POINT('Ctrl Pts',(374.041430004338,-2.6666689564829,-0.319705078219756));
#32947=CARTESIAN_POINT('Ctrl Pts',(374.045217580092,-2.66911285026489,-0.2791100250101));
#32948=CARTESIAN_POINT('Ctrl Pts',(374.049610226146,-2.6727067626466,-0.219905671871226));
#32949=CARTESIAN_POINT('Ctrl Pts',(374.050825871232,-2.67383770653679,-0.201344718078478));
#32950=CARTESIAN_POINT('Ctrl Pts',(374.052681399325,-2.67583587484425,-0.168680009214052));
#32951=CARTESIAN_POINT('Ctrl Pts',(374.053389414298,-2.67670094369416,-0.154580513190758));
#32952=CARTESIAN_POINT('Ctrl Pts',(374.054589081127,-2.67839314300787,-0.127084540769422));
#32953=CARTESIAN_POINT('Ctrl Pts',(374.055089829709,-2.67921997022517,-0.113688735568026));
#32954=CARTESIAN_POINT('Ctrl Pts',(374.05621307486,-2.68145340217471,-0.0776116366943328));
#32955=CARTESIAN_POINT('Ctrl Pts',(374.056679629077,-2.6828648505158,-0.0549265746182278));
#32956=CARTESIAN_POINT('Ctrl Pts',(374.05753450255,-2.68820931738686,0.0305261789265668));
#32957=CARTESIAN_POINT('Ctrl Pts',(374.056328570001,-2.69219145687869,0.0932924190315749));
#32958=CARTESIAN_POINT('Ctrl Pts',(374.036946291238,-2.71794374131263,0.493285979181566));
#32959=CARTESIAN_POINT('Ctrl Pts',(373.967699108441,-2.74136510917914,0.825832790318517));
#32960=CARTESIAN_POINT('Ctrl Pts',(373.8315113794,-2.76674557473438,1.18538961381349));
#32961=CARTESIAN_POINT('Ctrl Pts',(373.813941009317,-2.76981131404731,1.22888724651558));
#32962=CARTESIAN_POINT('Ctrl Pts',(373.783194111084,-2.7748311099694,1.30046411082045));
#32963=CARTESIAN_POINT('Ctrl Pts',(373.770551066057,-2.7768091516012,1.32876362560782));
#32964=CARTESIAN_POINT('Ctrl Pts',(373.752553770127,-2.77950563687249,1.36753602381804));
#32965=CARTESIAN_POINT('Ctrl Pts',(373.747547983375,-2.78024359871316,1.37816757398072));
#32966=CARTESIAN_POINT('Ctrl Pts',(373.738993407933,-2.78148432513536,1.39608133713833));
#32967=CARTESIAN_POINT('Ctrl Pts',(373.735475138047,-2.78198892871152,1.40337792195803));
#32968=CARTESIAN_POINT('Ctrl Pts',(373.728686130343,-2.78295174815612,1.41732308822957));
#32969=CARTESIAN_POINT('Ctrl Pts',(373.725419936904,-2.78341024972644,1.42397373724846));
#32970=CARTESIAN_POINT('Ctrl Pts',(373.717545398587,-2.78450460115969,1.43986915510599));
#32971=CARTESIAN_POINT('Ctrl Pts',(373.712915452721,-2.7851391245458,1.44910321546769));
#32972=CARTESIAN_POINT('Ctrl Pts',(373.696047624343,-2.78741952614218,1.48234489805956));
#32973=CARTESIAN_POINT('Ctrl Pts',(373.683552774476,-2.78905028160114,1.50622181331525));
#32974=CARTESIAN_POINT('Ctrl Pts',(373.591263161743,-2.80070406741627,1.67732269595656));
#32975=CARTESIAN_POINT('Ctrl Pts',(373.500390394921,-2.81014106916837,1.81830407623108));
#32976=CARTESIAN_POINT('Ctrl Pts',(373.304333824479,-2.82827230167331,2.07594697970285));
#32977=CARTESIAN_POINT('Ctrl Pts',(373.200790340985,-2.83695256375842,2.19324887137075));
#32978=CARTESIAN_POINT('Ctrl Pts',(373.004070942733,-2.85269064435811,2.38588964324588));
#32979=CARTESIAN_POINT('Ctrl Pts',(372.914446505848,-2.85962817517038,2.46441840999463));
#32980=CARTESIAN_POINT('Ctrl Pts',(372.79935786551,-2.86839971160625,2.55449977818439));
#32981=CARTESIAN_POINT('Ctrl Pts',(372.77781721384,-2.87003566975625,2.57092620157335));
#32982=CARTESIAN_POINT('Ctrl Pts',(372.743347608119,-2.87264582586219,2.59653119174095));
#32983=CARTESIAN_POINT('Ctrl Pts',(372.730553296375,-2.87361299875585,2.60588947671575));
#32984=CARTESIAN_POINT('Ctrl Pts',(372.706339610666,-2.87544057515436,2.62332761481063));
#32985=CARTESIAN_POINT('Ctrl Pts',(372.694935621003,-2.87630014830955,2.63142827137717));
#32986=CARTESIAN_POINT('Ctrl Pts',(372.669123861875,-2.87824328090601,2.64951159709431));
#32987=CARTESIAN_POINT('Ctrl Pts',(372.654686749923,-2.87932843979613,2.65945141956297));
#32988=CARTESIAN_POINT('Ctrl Pts',(372.617454031289,-2.88212309541942,2.68464058928198));
#32989=CARTESIAN_POINT('Ctrl Pts',(372.594543908417,-2.8838389925197,2.69971737096328));
#32990=CARTESIAN_POINT('Ctrl Pts',(372.486580169867,-2.89190973654399,2.76880808397516));
#32991=CARTESIAN_POINT('Ctrl Pts',(372.399273068547,-2.89839472972295,2.81907019070487));
#32992=CARTESIAN_POINT('Ctrl Pts',(372.309820062099,-2.90499717006879,2.86513713356016));
#32993=CARTESIAN_POINT('Origin',(370.834317853224,2.31077344927308,0.));
#32994=CARTESIAN_POINT('',(372.30982074573,-4.40407334669084,2.86513678150015));
#32995=CARTESIAN_POINT('',(372.309820591895,-4.15988901539236,2.86513686072291));
#32996=CARTESIAN_POINT('',(372.309820613641,2.31077344927308,2.86513684952399));
#32997=CARTESIAN_POINT('',(367.611567856376,-3.55765537866733,-0.00014252679442044));
#32998=CARTESIAN_POINT('Ctrl Pts',(372.30982074573,-4.40407334669084,2.86513678150013));
#32999=CARTESIAN_POINT('Ctrl Pts',(372.356820336721,-4.40050650002824,2.84093269012777));
#33000=CARTESIAN_POINT('Ctrl Pts',(372.403229895877,-4.39692788281758,2.8155692833783));
#33001=CARTESIAN_POINT('Ctrl Pts',(372.594590100041,-4.38196998916824,2.70478418667755));
#33002=CARTESIAN_POINT('Ctrl Pts',(372.733365395875,-4.37061300566367,2.60922306379554));
#33003=CARTESIAN_POINT('Ctrl Pts',(372.88497741809,-4.35807259069125,2.48629010110657));
#33004=CARTESIAN_POINT('Ctrl Pts',(372.905687217492,-4.35635683435112,2.46906301756107));
#33005=CARTESIAN_POINT('Ctrl Pts',(372.934032335231,-4.35400751349806,2.44487693464788));
#33006=CARTESIAN_POINT('Ctrl Pts',(372.941853200669,-4.353359192509,2.43813840821318));
#33007=CARTESIAN_POINT('Ctrl Pts',(372.955227619482,-4.35225052391116,2.42650245145076));
#33008=CARTESIAN_POINT('Ctrl Pts',(372.960796865606,-4.35178886936453,2.42162329771172));
#33009=CARTESIAN_POINT('Ctrl Pts',(372.972418853882,-4.35082558807084,2.41137039542081));
#33010=CARTESIAN_POINT('Ctrl Pts',(372.978468234431,-4.35032425993365,2.4059929795146));
#33011=CARTESIAN_POINT('Ctrl Pts',(372.993241635538,-4.34909994440325,2.39276063782111));
#33012=CARTESIAN_POINT('Ctrl Pts',(373.001943227888,-4.34837881145916,2.38488062861831));
#33013=CARTESIAN_POINT('Ctrl Pts',(373.033427699975,-4.34576870835481,2.35605416646881));
#33014=CARTESIAN_POINT('Ctrl Pts',(373.055952412938,-4.34389970945168,2.33482663105801));
#33015=CARTESIAN_POINT('Ctrl Pts',(373.111778109745,-4.33925259613662,2.28067637627111));
#33016=CARTESIAN_POINT('Ctrl Pts',(373.144674672588,-4.3365003512048,2.24734549056114));
#33017=CARTESIAN_POINT('Ctrl Pts',(373.407319713652,-4.31429258103204,1.96936770421954));
#33018=CARTESIAN_POINT('Ctrl Pts',(373.598296227912,-4.2964143340372,1.69092014962956));
#33019=CARTESIAN_POINT('Ctrl Pts',(373.770608954436,-4.27299697573036,1.32983577508168));
#33020=CARTESIAN_POINT('Ctrl Pts',(373.79660581065,-4.26917547823155,1.27087286522773));
#33021=CARTESIAN_POINT('Ctrl Pts',(373.829427365802,-4.26391382785677,1.18994179907895));
#33022=CARTESIAN_POINT('Ctrl Pts',(373.837810954837,-4.26252612439066,1.16861953798211));
#33023=CARTESIAN_POINT('Ctrl Pts',(373.851282340918,-4.26022128232695,1.133254543545));
#33024=CARTESIAN_POINT('Ctrl Pts',(373.856501218672,-4.25930855223057,1.1192623795593));
#33025=CARTESIAN_POINT('Ctrl Pts',(373.866508753866,-4.25751865360689,1.09185113324143));
#33026=CARTESIAN_POINT('Ctrl Pts',(373.871306048396,-4.25664179745701,1.0784355553817));
#33027=CARTESIAN_POINT('Ctrl Pts',(373.882446480422,-4.25455993733679,1.04661755714939));
#33028=CARTESIAN_POINT('Ctrl Pts',(373.888712107683,-4.25335240176869,1.02818877184621));
#33029=CARTESIAN_POINT('Ctrl Pts',(373.90915164639,-4.24928650769127,0.966234959734304));
#33030=CARTESIAN_POINT('Ctrl Pts',(373.922564602881,-4.24640344643216,0.922466541764184));
#33031=CARTESIAN_POINT('Ctrl Pts',(373.952473300675,-4.23942067017441,0.816893334582244));
#33032=CARTESIAN_POINT('Ctrl Pts',(373.968069561371,-4.23529406305667,0.754855920454128));
#33033=CARTESIAN_POINT('Ctrl Pts',(374.022127095938,-4.21886069056194,0.509122368967236));
#33034=CARTESIAN_POINT('Ctrl Pts',(374.046356150456,-4.20617490837765,0.322691357908466));
#33035=CARTESIAN_POINT('Ctrl Pts',(374.057161237622,-4.18875979158576,0.0654234177713689));
#33036=CARTESIAN_POINT('Ctrl Pts',(374.057822188569,-4.18404169576746,-0.00446586208591672));
#33037=CARTESIAN_POINT('Ctrl Pts',(374.055220281539,-4.17649153413159,-0.117258592036203));
#33038=CARTESIAN_POINT('Ctrl Pts',(374.053371637904,-4.17363416235853,-0.160171786559151));
#33039=CARTESIAN_POINT('Ctrl Pts',(374.046481593723,-4.16642384790428,-0.269318549531825));
#33040=CARTESIAN_POINT('Ctrl Pts',(374.040249203542,-4.16210810448749,-0.33546077485909));
#33041=CARTESIAN_POINT('Ctrl Pts',(374.030001833576,-4.15688482982029,-0.417100557186794));
#33042=CARTESIAN_POINT('Ctrl Pts',(374.027910959258,-4.15588398668096,-0.432818754315248));
#33043=CARTESIAN_POINT('Ctrl Pts',(374.024439936618,-4.15431962361985,-0.457516299855573));
#33044=CARTESIAN_POINT('Ctrl Pts',(374.023137719238,-4.15375192185907,-0.466506096929454));
#33045=CARTESIAN_POINT('Ctrl Pts',(374.020754585345,-4.15274628160205,-0.482481584146566));
#33046=CARTESIAN_POINT('Ctrl Pts',(374.019688698739,-4.15230752304586,-0.489469207220433));
#33047=CARTESIAN_POINT('Ctrl Pts',(374.017088619077,-4.15126294634592,-0.506146271740775));
#33048=CARTESIAN_POINT('Ctrl Pts',(374.015533168222,-4.15065833349952,-0.515832261393103));
#33049=CARTESIAN_POINT('Ctrl Pts',(374.010710197986,-4.14884263443907,-0.545013738709289));
#33050=CARTESIAN_POINT('Ctrl Pts',(374.007307449573,-4.14763888316993,-0.564486819332759));
#33051=CARTESIAN_POINT('Ctrl Pts',(373.969765559872,-4.13511386628366,-0.768254366939748));
#33052=CARTESIAN_POINT('Ctrl Pts',(373.91978493487,-4.12458483459276,-0.949294351220609));
#33053=CARTESIAN_POINT('Ctrl Pts',(373.819833751023,-4.10856162533082,-1.21761392715217));
#33054=CARTESIAN_POINT('Ctrl Pts',(373.781084386549,-4.1030515975203,-1.30860822257572));
#33055=CARTESIAN_POINT('Ctrl Pts',(373.667695485865,-4.08830598020329,-1.544191875326));
#33056=CARTESIAN_POINT('Ctrl Pts',(373.586197573693,-4.07897021820306,-1.68514264495063));
#33057=CARTESIAN_POINT('Ctrl Pts',(373.479103553636,-4.06761338849572,-1.84172807314838));
#33058=CARTESIAN_POINT('Ctrl Pts',(373.463505062924,-4.065979013034,-1.86392817597613));
#33059=CARTESIAN_POINT('Ctrl Pts',(373.437427317206,-4.06327708255522,-1.90006383082037));
#33060=CARTESIAN_POINT('Ctrl Pts',(373.427111790021,-4.06221580468078,-1.91411625179955));
#33061=CARTESIAN_POINT('Ctrl Pts',(373.408324669152,-4.06029599635024,-1.93927864233283));
#33062=CARTESIAN_POINT('Ctrl Pts',(373.399893820278,-4.05943906902534,-1.95041859317688));
#33063=CARTESIAN_POINT('Ctrl Pts',(373.381716654477,-4.05760106768792,-1.97411487876878));
#33064=CARTESIAN_POINT('Ctrl Pts',(373.371949371963,-4.05661917912857,-1.9866545919824));
#33065=CARTESIAN_POINT('Ctrl Pts',(373.34514195245,-4.05393942922595,-2.0205510056913));
#33066=CARTESIAN_POINT('Ctrl Pts',(373.327922651327,-4.05223444196566,-2.04176371328451));
#33067=CARTESIAN_POINT('Ctrl Pts',(373.231612482809,-4.04278425163842,-2.15737387419143));
#33068=CARTESIAN_POINT('Ctrl Pts',(373.147439633739,-4.03483182100616,-2.24738622962639));
#33069=CARTESIAN_POINT('Ctrl Pts',(372.949899411766,-4.01681960922254,-2.43575054674697));
#33070=CARTESIAN_POINT('Ctrl Pts',(372.834394890547,-4.00669466629736,-2.5314525460864));
#33071=CARTESIAN_POINT('Ctrl Pts',(372.57499181843,-3.98509897833282,-2.71751277023943));
#33072=CARTESIAN_POINT('Ctrl Pts',(372.429735509719,-3.97365730965254,-2.80525842180363));
#33073=CARTESIAN_POINT('Ctrl Pts',(372.254162065999,-3.96103988422441,-2.89324824363864));
#33074=CARTESIAN_POINT('Ctrl Pts',(372.22993170662,-3.95932428414451,-2.90501378140044));
#33075=CARTESIAN_POINT('Ctrl Pts',(372.196213935869,-3.95697513767979,-2.92086685503076));
#33076=CARTESIAN_POINT('Ctrl Pts',(372.186850878523,-3.95632683767809,-2.9252142736942));
#33077=CARTESIAN_POINT('Ctrl Pts',(372.17073659314,-3.95521819550737,-2.9326024847951));
#33078=CARTESIAN_POINT('Ctrl Pts',(372.163995546321,-3.95475654653658,-2.93566510646598));
#33079=CARTESIAN_POINT('Ctrl Pts',(372.149863373954,-3.95379326605578,-2.94202703201353));
#33080=CARTESIAN_POINT('Ctrl Pts',(372.142470292408,-3.95329193321712,-2.94532176032525));
#33081=CARTESIAN_POINT('Ctrl Pts',(372.124324048026,-3.95206758840162,-2.95332683504522));
#33082=CARTESIAN_POINT('Ctrl Pts',(372.113557276421,-3.95134643108233,-2.95800640385837));
#33083=CARTESIAN_POINT('Ctrl Pts',(372.074312249028,-3.94873613852915,-2.97480914018418));
#33084=CARTESIAN_POINT('Ctrl Pts',(372.045684301878,-3.94686697834984,-2.986581157422));
#33085=CARTESIAN_POINT('Ctrl Pts',(371.973328101669,-3.94221938030647,-3.01512290463813));
#33086=CARTESIAN_POINT('Ctrl Pts',(371.929394637014,-3.93946681882986,-3.03135576059474));
#33087=CARTESIAN_POINT('Ctrl Pts',(371.567720028278,-3.91725038484891,-3.15609990962591));
#33088=CARTESIAN_POINT('Ctrl Pts',(371.23515525825,-3.89936487727849,-3.21530939151872));
#33089=CARTESIAN_POINT('Ctrl Pts',(370.835118414114,-3.87594445282317,-3.22339148369575));
#33090=CARTESIAN_POINT('Ctrl Pts',(370.770800946733,-3.87212983958409,-3.22276559302365));
#33091=CARTESIAN_POINT('Ctrl Pts',(370.683671783539,-3.86687626716856,-3.2193085411111));
#33092=CARTESIAN_POINT('Ctrl Pts',(370.660806061208,-3.86548954623362,-3.21815713379013));
#33093=CARTESIAN_POINT('Ctrl Pts',(370.623052479826,-3.8631859050584,-3.21585251789856));
#33094=CARTESIAN_POINT('Ctrl Pts',(370.608156672431,-3.86227338388473,-3.2148392780038));
#33095=CARTESIAN_POINT('Ctrl Pts',(370.579059110299,-3.86048357332093,-3.2126567795609));
#33096=CARTESIAN_POINT('Ctrl Pts',(370.564856993383,-3.85960659398358,-3.21149676066196));
#33097=CARTESIAN_POINT('Ctrl Pts',(370.531263101636,-3.85752392407555,-3.20852842949336));
#33098=CARTESIAN_POINT('Ctrl Pts',(370.511879276313,-3.85631569651385,-3.2066384583778));
#33099=CARTESIAN_POINT('Ctrl Pts',(370.446932874968,-3.85224498910158,-3.19971119422618));
#33100=CARTESIAN_POINT('Ctrl Pts',(370.401462566226,-3.84935772663629,-3.19387770606642));
#33101=CARTESIAN_POINT('Ctrl Pts',(370.292765285308,-3.84236283082331,-3.17756893902443));
#33102=CARTESIAN_POINT('Ctrl Pts',(370.229698011863,-3.83822818160346,-3.16617395339352));
#33103=CARTESIAN_POINT('Ctrl Pts',(369.982775837391,-3.82174239440779,-3.1139137007705));
#33104=CARTESIAN_POINT('Ctrl Pts',(369.802325379488,-3.80900954444348,-3.05884948296285));
#33105=CARTESIAN_POINT('Ctrl Pts',(369.478699228753,-3.78540588260638,-2.9281817511395));
#33106=CARTESIAN_POINT('Ctrl Pts',(369.334358961332,-3.77457644246989,-2.85693603057764));
#33107=CARTESIAN_POINT('Ctrl Pts',(369.172764043659,-3.76252036520117,-2.76153580439345));
#33108=CARTESIAN_POINT('Ctrl Pts',(369.14977261488,-3.7608070608928,-2.74757138408088));
#33109=CARTESIAN_POINT('Ctrl Pts',(369.117428846552,-3.75840263417235,-2.72736794971393));
#33110=CARTESIAN_POINT('Ctrl Pts',(369.107930848259,-3.7576972765344,-2.72136578067754));
#33111=CARTESIAN_POINT('Ctrl Pts',(369.091791514999,-3.75650020344815,-2.71104818208775));
#33112=CARTESIAN_POINT('Ctrl Pts',(369.085134389634,-3.75600687491644,-2.70675774690817));
#33113=CARTESIAN_POINT('Ctrl Pts',(369.072364509496,-3.75506150243121,-2.6984609299233));
#33114=CARTESIAN_POINT('Ctrl Pts',(369.066249494605,-3.75460921029972,-2.69445824936202));
#33115=CARTESIAN_POINT('Ctrl Pts',(369.053182277428,-3.75364346645604,-2.68584125475485));
#33116=CARTESIAN_POINT('Ctrl Pts',(369.046234253935,-3.7531304318148,-2.68122066056447));
#33117=CARTESIAN_POINT('Ctrl Pts',(369.019388682129,-3.75114966551596,-2.66321697917447));
#33118=CARTESIAN_POINT('Ctrl Pts',(368.99962221371,-3.74969438922306,-2.64963857197487));
#33119=CARTESIAN_POINT('Ctrl Pts',(368.892919872959,-3.74184517466493,-2.5745736500928));
#33120=CARTESIAN_POINT('Ctrl Pts',(368.808912229926,-3.73568853385702,-2.50902214528503));
#33121=CARTESIAN_POINT('Ctrl Pts',(368.540094203558,-3.71550721996651,-2.2769444046196));
#33122=CARTESIAN_POINT('Ctrl Pts',(368.371328920377,-3.70195302775649,-2.09323389094672));
#33123=CARTESIAN_POINT('Ctrl Pts',(368.170026241403,-3.68217321679005,-1.81564081844182));
#33124=CARTESIAN_POINT('Ctrl Pts',(368.118071956698,-3.67664234250873,-1.73695342040547));
#33125=CARTESIAN_POINT('Ctrl Pts',(368.056097606065,-3.66939965566806,-1.63349461299386));
#33126=CARTESIAN_POINT('Ctrl Pts',(368.042830177055,-3.66780697896265,-1.61071688494918));
#33127=CARTESIAN_POINT('Ctrl Pts',(368.022116281324,-3.66525050605913,-1.57413020451759));
#33128=CARTESIAN_POINT('Ctrl Pts',(368.014488477137,-3.66429324674535,-1.56042489659651));
#33129=CARTESIAN_POINT('Ctrl Pts',(368.000913391225,-3.662560425152,-1.53560916766059));
#33130=CARTESIAN_POINT('Ctrl Pts',(367.994930619681,-3.6617861497307,-1.52451844590893));
#33131=CARTESIAN_POINT('Ctrl Pts',(367.980995440456,-3.65995733597459,-1.49831915047281));
#33132=CARTESIAN_POINT('Ctrl Pts',(367.973097807401,-3.65890088624625,-1.48318201826607));
#33133=CARTESIAN_POINT('Ctrl Pts',(367.950338710095,-3.65579669096998,-1.4387020914458));
#33134=CARTESIAN_POINT('Ctrl Pts',(367.935806080932,-3.65373754648814,-1.4091943737659));
#33135=CARTESIAN_POINT('Ctrl Pts',(367.903851192017,-3.64902821329003,-1.34172536976308));
#33136=CARTESIAN_POINT('Ctrl Pts',(367.886710442178,-3.64636889319304,-1.30363802979962));
#33137=CARTESIAN_POINT('Ctrl Pts',(367.83216280498,-3.63744234058219,-1.17585148246727));
#33138=CARTESIAN_POINT('Ctrl Pts',(367.798075726298,-3.63107312681071,-1.0848007015654));
#33139=CARTESIAN_POINT('Ctrl Pts',(367.710264086302,-3.6121106062235,-0.813481981640369));
#33140=CARTESIAN_POINT('Ctrl Pts',(367.668137518932,-3.59927912810973,-0.629889307343783));
#33141=CARTESIAN_POINT('Ctrl Pts',(367.626128087694,-3.57878885385889,-0.327657132336179));
#33142=CARTESIAN_POINT('Ctrl Pts',(367.616336929242,-3.57102517716654,-0.210820564885843));
#33143=CARTESIAN_POINT('Ctrl Pts',(367.612365008877,-3.56231404483283,-0.0742658328475275));
#33144=CARTESIAN_POINT('Ctrl Pts',(367.61197560134,-3.56108262042694,-0.0548270000785654));
#33145=CARTESIAN_POINT('Ctrl Pts',(367.611671746325,-3.5593430140859,-0.0271547736545808));
#33146=CARTESIAN_POINT('Ctrl Pts',(367.611612901793,-3.5588272649062,-0.0189238359192423));
#33147=CARTESIAN_POINT('Ctrl Pts',(367.611573923759,-3.55809363972904,-0.00717598306127299));
#33148=CARTESIAN_POINT('Ctrl Pts',(367.611568011904,-3.55787434821804,-0.00365926833753844));
#33149=CARTESIAN_POINT('Ctrl Pts',(367.611567856376,-3.55765537866733,-0.00014252679442044));
#33150=CARTESIAN_POINT('Ctrl Pts',(367.611567856366,-3.55765536469338,-0.00014230236719019));
#33151=CARTESIAN_POINT('Ctrl Pts',(367.611567829866,-3.55761799647536,0.000457846706114776));
#33152=CARTESIAN_POINT('Ctrl Pts',(367.611567971008,-3.55758063764161,0.00105799643576072));
#33153=CARTESIAN_POINT('Ctrl Pts',(367.61157075936,-3.55724336969791,0.00647739667062727));
#33154=CARTESIAN_POINT('Ctrl Pts',(367.61158404864,-3.55694406733888,0.0112965967864436));
#33155=CARTESIAN_POINT('Ctrl Pts',(367.611652082637,-3.55610084187474,0.024901450644145));
#33156=CARTESIAN_POINT('Ctrl Pts',(367.611731943653,-3.55555833350072,0.0336869542414703));
#33157=CARTESIAN_POINT('Ctrl Pts',(367.612046172872,-3.55409132298816,0.0575283286255893));
#33158=CARTESIAN_POINT('Ctrl Pts',(367.61235013472,-3.5531705924886,0.0725832746862368));
#33159=CARTESIAN_POINT('Ctrl Pts',(367.614346293638,-3.54870787142136,0.145963525277752));
#33160=CARTESIAN_POINT('Ctrl Pts',(367.617516869005,-3.54524079870716,0.204241448695378));
#33161=CARTESIAN_POINT('Ctrl Pts',(367.625786436883,-3.53930385541055,0.305467638002747));
#33162=CARTESIAN_POINT('Ctrl Pts',(367.630170149061,-3.53680942521572,0.348456714715536));
#33163=CARTESIAN_POINT('Ctrl Pts',(367.660584617158,-3.52247539848918,0.597067511163521));
#33164=CARTESIAN_POINT('Ctrl Pts',(367.70553853136,-3.51111512367214,0.799887186822757));
#33165=CARTESIAN_POINT('Ctrl Pts',(367.800494870066,-3.49374226226303,1.09177377903907));
#33166=CARTESIAN_POINT('Ctrl Pts',(367.835707505049,-3.48803061199899,1.18506778974916));
#33167=CARTESIAN_POINT('Ctrl Pts',(367.892009772254,-3.47970109678367,1.31557781088509));
#33168=CARTESIAN_POINT('Ctrl Pts',(367.909604168867,-3.47718971066936,1.35424201974225));
#33169=CARTESIAN_POINT('Ctrl Pts',(367.942360117787,-3.47266274249192,1.42260644571472));
#33170=CARTESIAN_POINT('Ctrl Pts',(367.957228287441,-3.47065707821311,1.45244075559862));
#33171=CARTESIAN_POINT('Ctrl Pts',(367.98044907226,-3.46759429225963,1.49727924227374));
#33172=CARTESIAN_POINT('Ctrl Pts',(367.988463516651,-3.46654902539147,1.5124566855182));
#33173=CARTESIAN_POINT('Ctrl Pts',(368.003211429787,-3.46464633343383,1.53985343893699));
#33174=CARTESIAN_POINT('Ctrl Pts',(368.009903777199,-3.46379038421298,1.55209449187227));
#33175=CARTESIAN_POINT('Ctrl Pts',(368.024484543626,-3.46194119084425,1.57835774671204));
#33176=CARTESIAN_POINT('Ctrl Pts',(368.03239888159,-3.46094703421216,1.59236505416481));
#33177=CARTESIAN_POINT('Ctrl Pts',(368.054115324162,-3.45824440146888,1.63013701956501));
#33178=CARTESIAN_POINT('Ctrl Pts',(368.0681168208,-3.45652876402522,1.65378492501516));
#33179=CARTESIAN_POINT('Ctrl Pts',(368.141916134403,-3.44761936118916,1.7748689807496));
#33180=CARTESIAN_POINT('Ctrl Pts',(368.206559006927,-3.44024910185309,1.86924189523738));
#33181=CARTESIAN_POINT('Ctrl Pts',(368.416262833981,-3.41755386877325,2.14295681260095));
#33182=CARTESIAN_POINT('Ctrl Pts',(368.575676492069,-3.40177312332332,2.31036272296844));
#33183=CARTESIAN_POINT('Ctrl Pts',(368.829767106105,-3.37946119270624,2.52554911837101));
#33184=CARTESIAN_POINT('Ctrl Pts',(368.911102326798,-3.37268277922018,2.58802396646093));
#33185=CARTESIAN_POINT('Ctrl Pts',(369.01460666062,-3.364615032296,2.6599478160917));
#33186=CARTESIAN_POINT('Ctrl Pts',(369.034076362535,-3.36312064213182,2.67316326830018));
#33187=CARTESIAN_POINT('Ctrl Pts',(369.06060672089,-3.3611173396641,2.6907499420766));
#33188=CARTESIAN_POINT('Ctrl Pts',(369.067541510324,-3.36059670975951,2.69530847761069));
#33189=CARTESIAN_POINT('Ctrl Pts',(369.080617009859,-3.35962083802367,2.70383141787077));
#33190=CARTESIAN_POINT('Ctrl Pts',(369.086753732208,-3.35916520699288,2.70780180769196));
#33191=CARTESIAN_POINT('Ctrl Pts',(369.09943459671,-3.35822866912669,2.71594511828762));
#33192=CARTESIAN_POINT('Ctrl Pts',(369.105980385522,-3.3577479546418,2.72011532822708));
#33193=CARTESIAN_POINT('Ctrl Pts',(369.122043307154,-3.35657479965343,2.730267348895));
#33194=CARTESIAN_POINT('Ctrl Pts',(369.131576903321,-3.35588405656928,2.73622316045245));
#33195=CARTESIAN_POINT('Ctrl Pts',(369.164054935429,-3.35354897406428,2.75627729733774));
#33196=CARTESIAN_POINT('Ctrl Pts',(369.187145527261,-3.35191925768542,2.77013829806946));
#33197=CARTESIAN_POINT('Ctrl Pts',(369.354447708721,-3.34030827535417,2.86773603079442));
#33198=CARTESIAN_POINT('Ctrl Pts',(369.50481053641,-3.33090809950149,2.94046754668799));
#33199=CARTESIAN_POINT('Ctrl Pts',(369.806155769874,-3.31278502378425,3.0583627921969));
#33200=CARTESIAN_POINT('Ctrl Pts',(369.956139636517,-3.30407663110238,3.10475460573256));
#33201=CARTESIAN_POINT('Ctrl Pts',(370.225097507132,-3.28829901733509,3.16688980919041));
#33202=CARTESIAN_POINT('Ctrl Pts',(370.342686052497,-3.28135139917287,3.18726122239711));
#33203=CARTESIAN_POINT('Ctrl Pts',(370.488029244925,-3.27256924428055,3.20420590125974));
#33204=CARTESIAN_POINT('Ctrl Pts',(370.514971660014,-3.27093340694136,3.20700314917601));
#33205=CARTESIAN_POINT('Ctrl Pts',(370.557723914031,-3.26832385039949,3.2108977527887));
#33206=CARTESIAN_POINT('Ctrl Pts',(370.573512462089,-3.2673571582495,3.2122187223159));
#33207=CARTESIAN_POINT('Ctrl Pts',(370.603246645412,-3.26553074901222,3.21448580984111));
#33208=CARTESIAN_POINT('Ctrl Pts',(370.617189986974,-3.26467186312405,3.21545772864211));
#33209=CARTESIAN_POINT('Ctrl Pts',(370.648612609444,-3.26273063926348,3.21744272195414));
#33210=CARTESIAN_POINT('Ctrl Pts',(370.666094602899,-3.26164670724076,3.21840411155972));
#33211=CARTESIAN_POINT('Ctrl Pts',(370.710936715245,-3.25885594024044,3.22050376610953));
#33212=CARTESIAN_POINT('Ctrl Pts',(370.738304647765,-3.25714272815167,3.22143582937388));
#33213=CARTESIAN_POINT('Ctrl Pts',(370.978412778047,-3.24202146271751,3.22655075669993));
#33214=CARTESIAN_POINT('Ctrl Pts',(371.191032416868,-3.22795410939271,3.21000280670159));
#33215=CARTESIAN_POINT('Ctrl Pts',(371.613777981251,-3.19899209760355,3.13456915176621));
#33216=CARTESIAN_POINT('Ctrl Pts',(371.822747055675,-3.18416695670709,3.07507728358897));
#33217=CARTESIAN_POINT('Ctrl Pts',(372.054998044556,-3.16803520284136,2.98281036824715));
#33218=CARTESIAN_POINT('Ctrl Pts',(372.085635200027,-3.16591543623544,2.97008803244851));
#33219=CARTESIAN_POINT('Ctrl Pts',(372.127136193383,-3.16306057174462,2.95209819037317));
#33220=CARTESIAN_POINT('Ctrl Pts',(372.138173767819,-3.16230291152344,2.94723985299111));
#33221=CARTESIAN_POINT('Ctrl Pts',(372.15663233412,-3.16103888397526,2.9389910739153));
#33222=CARTESIAN_POINT('Ctrl Pts',(372.164068111902,-3.16053051946372,2.93563423692895));
#33223=CARTESIAN_POINT('Ctrl Pts',(372.178170663718,-3.15956805875611,2.92920314755624));
#33224=CARTESIAN_POINT('Ctrl Pts',(372.184839787428,-3.15911362747474,2.92613430377092));
#33225=CARTESIAN_POINT('Ctrl Pts',(372.200640510535,-3.15803854488296,2.9187979637927));
#33226=CARTESIAN_POINT('Ctrl Pts',(372.209762753533,-3.15741911740308,2.91451033448505));
#33227=CARTESIAN_POINT('Ctrl Pts',(372.241804253353,-3.15524729819495,2.89926627247825));
#33228=CARTESIAN_POINT('Ctrl Pts',(372.264614605347,-3.15370822051652,2.88808140070798));
#33229=CARTESIAN_POINT('Ctrl Pts',(372.294816617636,-3.1516767028354,2.87282648332488));
#33230=CARTESIAN_POINT('Ctrl Pts',(372.302326508682,-3.15117207890497,2.86899620186515));
#33231=CARTESIAN_POINT('Ctrl Pts',(372.309820619203,-3.15066895420511,2.86513684665975));
#33232=CARTESIAN_POINT('Ctrl Pts',(372.309820062099,-2.9049971700688,2.86513713356014));
#33233=CARTESIAN_POINT('Ctrl Pts',(372.212990497692,-2.9121440670608,2.91500289198845));
#33234=CARTESIAN_POINT('Ctrl Pts',(372.113646582387,-2.91942904114421,2.95995312199687));
#33235=CARTESIAN_POINT('Ctrl Pts',(371.807974008103,-2.9415687748639,3.07997266155052));
#33236=CARTESIAN_POINT('Ctrl Pts',(371.596125083592,-2.95658437889865,3.13909193096567));
#33237=CARTESIAN_POINT('Ctrl Pts',(371.347045112705,-2.97290044565745,3.18187678968539));
#33238=CARTESIAN_POINT('Ctrl Pts',(371.314098772515,-2.97503131292557,3.18701107940408));
#33239=CARTESIAN_POINT('Ctrl Pts',(371.269105515018,-2.97789890008957,3.19330915849462));
#33240=CARTESIAN_POINT('Ctrl Pts',(371.257124246555,-2.97865842483268,3.19491759787925));
#33241=CARTESIAN_POINT('Ctrl Pts',(371.23703213408,-2.979924954863,3.1974998819085));
#33242=CARTESIAN_POINT('Ctrl Pts',(371.228926214098,-2.98043397059477,3.19851036153577));
#33243=CARTESIAN_POINT('Ctrl Pts',(371.213526068135,-2.98139721724477,3.20037069989908));
#33244=CARTESIAN_POINT('Ctrl Pts',(371.206232661043,-2.98185178672203,3.20122646267032));
#33245=CARTESIAN_POINT('Ctrl Pts',(371.18892736776,-2.98292665733528,3.20319701743692));
#33246=CARTESIAN_POINT('Ctrl Pts',(371.178912985396,-2.983545738333,3.20428981858283));
#33247=CARTESIAN_POINT('Ctrl Pts',(371.143687146139,-2.98571357513805,3.20796672135347));
#33248=CARTESIAN_POINT('Ctrl Pts',(371.118449754988,-2.98724908709812,3.21030045283448));
#33249=CARTESIAN_POINT('Ctrl Pts',(370.876717096777,-3.00181066886283,3.22978067537564));
#33250=CARTESIAN_POINT('Ctrl Pts',(370.659007524435,-3.01383060881662,3.22530206277619));
#33251=CARTESIAN_POINT('Ctrl Pts',(370.294203025646,-3.03438817927249,3.18071999993724));
#33252=CARTESIAN_POINT('Ctrl Pts',(370.146491447725,-3.04282735445192,3.15207773805954));
#33253=CARTESIAN_POINT('Ctrl Pts',(369.948060920604,-3.05474533432585,3.09898475081882));
#33254=CARTESIAN_POINT('Ctrl Pts',(369.895172777709,-3.05797876640334,3.08336891676003));
#33255=CARTESIAN_POINT('Ctrl Pts',(369.803829858491,-3.0636810643626,3.05383072187969));
#33256=CARTESIAN_POINT('Ctrl Pts',(369.765190559135,-3.06613064613561,3.04051873664162));
#33257=CARTESIAN_POINT('Ctrl Pts',(369.709331707476,-3.06973140073274,3.02007787563735));
#33258=CARTESIAN_POINT('Ctrl Pts',(369.691903390251,-3.07086339430153,3.01352839297769));
#33259=CARTESIAN_POINT('Ctrl Pts',(369.661359169208,-3.07286277121287,3.00174696812662));
#33260=CARTESIAN_POINT('Ctrl Pts',(369.648218964491,-3.07372799056319,2.99657910811594));
#33261=CARTESIAN_POINT('Ctrl Pts',(369.622675797214,-3.0754199956706,2.98633900348051));
#33262=CARTESIAN_POINT('Ctrl Pts',(369.610269657893,-3.07624647497355,2.98127541875283));
#33263=CARTESIAN_POINT('Ctrl Pts',(369.576968726971,-3.0784777571452,2.96744069136204));
#33264=CARTESIAN_POINT('Ctrl Pts',(369.556134572482,-3.07988738685624,2.95852641373332));
#33265=CARTESIAN_POINT('Ctrl Pts',(369.4781407185,-3.08521703500485,2.92417769704913));
#33266=CARTESIAN_POINT('Ctrl Pts',(369.421634725397,-3.08918582422223,2.89730169846489));
#33267=CARTESIAN_POINT('Ctrl Pts',(369.065112621371,-3.11493823966977,2.71481920817199));
#33268=CARTESIAN_POINT('Ctrl Pts',(368.790448867474,-3.13837725266613,2.51452731906935));
#33269=CARTESIAN_POINT('Ctrl Pts',(368.51881711562,-3.16377513663097,2.24204700986508));
#33270=CARTESIAN_POINT('Ctrl Pts',(368.486423571826,-3.16684151399197,2.20810129998184));
#33271=CARTESIAN_POINT('Ctrl Pts',(368.433876482635,-3.17186224090437,2.15057192472469));
#33272=CARTESIAN_POINT('Ctrl Pts',(368.413302120969,-3.17384058586332,2.12738369046839));
#33273=CARTESIAN_POINT('Ctrl Pts',(368.385392955192,-3.17653741522548,2.09499940434961));
#33274=CARTESIAN_POINT('Ctrl Pts',(368.377769849716,-3.17727542397237,2.08605550667594));
#33275=CARTESIAN_POINT('Ctrl Pts',(368.364974898184,-3.17851620822447,2.07087627618417));
#33276=CARTESIAN_POINT('Ctrl Pts',(368.359777372325,-3.17902082307195,2.06466282824706));
#33277=CARTESIAN_POINT('Ctrl Pts',(368.349870873617,-3.17998364447989,2.05272883334959));
#33278=CARTESIAN_POINT('Ctrl Pts',(368.345158141807,-3.18044213686891,2.04701157578841));
#33279=CARTESIAN_POINT('Ctrl Pts',(368.333922761546,-3.18153644559037,2.03328518321275));
#33280=CARTESIAN_POINT('Ctrl Pts',(368.32741877071,-3.1821709356715,2.02526078508258));
#33281=CARTESIAN_POINT('Ctrl Pts',(368.304089310004,-3.18445106059485,1.99619312254939));
#33282=CARTESIAN_POINT('Ctrl Pts',(368.287488780277,-3.18608157755797,1.97496968185856));
#33283=CARTESIAN_POINT('Ctrl Pts',(368.169292390578,-3.19777043982276,1.81988888447335));
#33284=CARTESIAN_POINT('Ctrl Pts',(368.078025428772,-3.20723851439143,1.67845825364984));
#33285=CARTESIAN_POINT('Ctrl Pts',(367.928125676097,-3.22491379972707,1.40069099692061));
#33286=CARTESIAN_POINT('Ctrl Pts',(367.867053271532,-3.23311396081248,1.26618618897768));
#33287=CARTESIAN_POINT('Ctrl Pts',(367.771169655093,-3.24873262785019,1.00956395124081));
#33288=CARTESIAN_POINT('Ctrl Pts',(367.733936138239,-3.25607965892257,0.888664263684783));
#33289=CARTESIAN_POINT('Ctrl Pts',(367.697359130642,-3.26531336639497,0.739165096227663));
#33290=CARTESIAN_POINT('Ctrl Pts',(367.691161129629,-3.26697507139554,0.712348795432458));
#33291=CARTESIAN_POINT('Ctrl Pts',(367.681915896509,-3.26961688578751,0.669875913463045));
#33292=CARTESIAN_POINT('Ctrl Pts',(367.678640036096,-3.27058967052463,0.654270079049063));
#33293=CARTESIAN_POINT('Ctrl Pts',(367.672710501913,-3.27242206845296,0.624941485819358));
#33294=CARTESIAN_POINT('Ctrl Pts',(367.670030014276,-3.2732808027859,0.611224481747655));
#33295=CARTESIAN_POINT('Ctrl Pts',(367.664215093501,-3.27521434445588,0.580403663803702));
#33296=CARTESIAN_POINT('Ctrl Pts',(367.6611297111,-3.27629068538196,0.563291146628433));
#33297=CARTESIAN_POINT('Ctrl Pts',(367.653613197444,-3.27904752273958,0.519579249319347));
#33298=CARTESIAN_POINT('Ctrl Pts',(367.649377225552,-3.28073412997337,0.492948101564355));
#33299=CARTESIAN_POINT('Ctrl Pts',(367.622762044809,-3.2923124245762,0.310924716107186));
#33300=CARTESIAN_POINT('Ctrl Pts',(367.611432623364,-3.30254997493467,0.154152664312409));
#33301=CARTESIAN_POINT('Ctrl Pts',(367.611779203676,-3.32915016553059,-0.244515246666114));
#33302=CARTESIAN_POINT('Ctrl Pts',(367.639180874197,-3.34579243102028,-0.485426413940841));
#33303=CARTESIAN_POINT('Ctrl Pts',(367.706259561983,-3.36547561738465,-0.777654906549834));
#33304=CARTESIAN_POINT('Ctrl Pts',(367.72079412074,-3.36923911200978,-0.833946492865908));
#33305=CARTESIAN_POINT('Ctrl Pts',(367.741085105635,-3.37390019904172,-0.90457980847519));
#33306=CARTESIAN_POINT('Ctrl Pts',(367.745431371501,-3.37486893053905,-0.919311582398069));
#33307=CARTESIAN_POINT('Ctrl Pts',(367.752457942647,-3.376388769133,-0.942515781451098));
#33308=CARTESIAN_POINT('Ctrl Pts',(367.755068187148,-3.37694377818999,-0.951008940629364));
#33309=CARTESIAN_POINT('Ctrl Pts',(367.760066683813,-3.37798858435168,-0.967036596165972));
#33310=CARTESIAN_POINT('Ctrl Pts',(367.762447505092,-3.3784787736131,-0.97457303286626));
#33311=CARTESIAN_POINT('Ctrl Pts',(367.768084933984,-3.37962232265652,-0.992192274379373));
#33312=CARTESIAN_POINT('Ctrl Pts',(367.771363566489,-3.3802743905606,-1.00226786295412));
#33313=CARTESIAN_POINT('Ctrl Pts',(367.782197697417,-3.38238800377416,-1.03501259831202));
#33314=CARTESIAN_POINT('Ctrl Pts',(367.789955829606,-3.38383823618245,-1.05761451862846));
#33315=CARTESIAN_POINT('Ctrl Pts',(367.83337690453,-3.39163356579976,-1.17967561754491));
#33316=CARTESIAN_POINT('Ctrl Pts',(367.873666605061,-3.39774498281753,-1.27743090109817));
#33317=CARTESIAN_POINT('Ctrl Pts',(368.022759711864,-3.41763768935576,-1.59402795990486));
#33318=CARTESIAN_POINT('Ctrl Pts',(368.151613355638,-3.43095997806631,-1.80246656955757));
#33319=CARTESIAN_POINT('Ctrl Pts',(368.363998610368,-3.4507187537325,-2.07205847557383));
#33320=CARTESIAN_POINT('Ctrl Pts',(368.428756474573,-3.45651493851356,-2.14689896862242));
#33321=CARTESIAN_POINT('Ctrl Pts',(368.515228055924,-3.46405605097678,-2.2380019670637));
#33322=CARTESIAN_POINT('Ctrl Pts',(368.533846541543,-3.46566875661021,-2.25713578934491));
#33323=CARTESIAN_POINT('Ctrl Pts',(368.563834822089,-3.46825031338518,-2.28719761658069));
#33324=CARTESIAN_POINT('Ctrl Pts',(368.575051066068,-3.46921240536457,-2.29827755125347));
#33325=CARTESIAN_POINT('Ctrl Pts',(368.595376984848,-3.47094995899639,-2.3180638741087));
#33326=CARTESIAN_POINT('Ctrl Pts',(368.604457331219,-3.47172409630808,-2.32680003046726));
#33327=CARTESIAN_POINT('Ctrl Pts',(368.625898177617,-3.47354727828909,-2.34718738640369));
#33328=CARTESIAN_POINT('Ctrl Pts',(368.638299932047,-3.47459819147874,-2.35879447232996));
#33329=CARTESIAN_POINT('Ctrl Pts',(368.674643196603,-3.47766773458439,-2.39227392190985));
#33330=CARTESIAN_POINT('Ctrl Pts',(368.698823241024,-3.47969737047273,-2.41388313258036));
#33331=CARTESIAN_POINT('Ctrl Pts',(368.883444555114,-3.49510530886284,-2.57393021356425));
#33332=CARTESIAN_POINT('Ctrl Pts',(369.056836071296,-3.50913069089222,-2.69658166691028));
#33333=CARTESIAN_POINT('Ctrl Pts',(369.436485797651,-3.53859704341476,-2.91252017197192));
#33334=CARTESIAN_POINT('Ctrl Pts',(369.643112447912,-3.55398798522191,-3.00295713774306));
#33335=CARTESIAN_POINT('Ctrl Pts',(369.881074744475,-3.56999902556909,-3.0786454756534));
#33336=CARTESIAN_POINT('Ctrl Pts',(369.90475202913,-3.5715735346865,-3.0858771612309));
#33337=CARTESIAN_POINT('Ctrl Pts',(369.938082484053,-3.57376170804045,-3.09563873774642));
#33338=CARTESIAN_POINT('Ctrl Pts',(369.947666967893,-3.57438767929088,-3.09839752860961));
#33339=CARTESIAN_POINT('Ctrl Pts',(369.964306346375,-3.57546858327716,-3.10310346237015));
#33340=CARTESIAN_POINT('Ctrl Pts',(369.971355288168,-3.57592467907679,-3.10507113188542));
#33341=CARTESIAN_POINT('Ctrl Pts',(369.986315308536,-3.57688873431455,-3.10919225311614));
#33342=CARTESIAN_POINT('Ctrl Pts',(369.994228027728,-3.57739632476171,-3.11133956209253));
#33343=CARTESIAN_POINT('Ctrl Pts',(370.013967964446,-3.57865703174619,-3.11661567907993));
#33344=CARTESIAN_POINT('Ctrl Pts',(370.025805099449,-3.57940803680223,-3.11970741724982));
#33345=CARTESIAN_POINT('Ctrl Pts',(370.070989022946,-3.58225676144758,-3.13123454825162));
#33346=CARTESIAN_POINT('Ctrl Pts',(370.104453800288,-3.58432943358858,-3.13920362199423));
#33347=CARTESIAN_POINT('Ctrl Pts',(370.190849493394,-3.58960014192736,-3.15832096003903));
#33348=CARTESIAN_POINT('Ctrl Pts',(370.243946429728,-3.5927625748746,-3.16867559553745));
#33349=CARTESIAN_POINT('Ctrl Pts',(370.457813844205,-3.60528317841956,-3.20481964511786));
#33350=CARTESIAN_POINT('Ctrl Pts',(370.620180687067,-3.61430985243349,-3.21974779953513));
#33351=CARTESIAN_POINT('Ctrl Pts',(370.993741959887,-3.63522415055653,-3.22569835500643));
#33352=CARTESIAN_POINT('Ctrl Pts',(371.204287589343,-3.64714496323274,-3.20837224024529));
#33353=CARTESIAN_POINT('Ctrl Pts',(371.438607084134,-3.66139951906262,-3.16570757580315));
#33354=CARTESIAN_POINT('Ctrl Pts',(371.465528244942,-3.66305148646487,-3.16044985747343));
#33355=CARTESIAN_POINT('Ctrl Pts',(371.509538178868,-3.66577698185465,-3.15126995727593));
#33356=CARTESIAN_POINT('Ctrl Pts',(371.526668194596,-3.66684404759612,-3.14755076491498));
#33357=CARTESIAN_POINT('Ctrl Pts',(371.557411967435,-3.6687707054668,-3.14061270116702));
#33358=CARTESIAN_POINT('Ctrl Pts',(371.571036809727,-3.6696286523253,-3.13744456622157));
#33359=CARTESIAN_POINT('Ctrl Pts',(371.60005559418,-3.67146489637807,-3.13049748775872));
#33360=CARTESIAN_POINT('Ctrl Pts',(371.615443100201,-3.67244398056333,-3.12669348401505));
#33361=CARTESIAN_POINT('Ctrl Pts',(371.657046692551,-3.67510609735314,-3.11608222419833));
#33362=CARTESIAN_POINT('Ctrl Pts',(371.683205583709,-3.67679609056244,-3.10905785087844));
#33363=CARTESIAN_POINT('Ctrl Pts',(371.823827128,-3.68597053619749,-3.06939017089466));
#33364=CARTESIAN_POINT('Ctrl Pts',(371.936490663738,-3.6936479276592,-3.03075798727444));
#33365=CARTESIAN_POINT('Ctrl Pts',(372.191391209001,-3.7117757586918,-2.92725809461126));
#33366=CARTESIAN_POINT('Ctrl Pts',(372.331564547322,-3.7223267048198,-2.85809963701444));
#33367=CARTESIAN_POINT('Ctrl Pts',(372.610762336887,-3.74422881938056,-2.69415673114183));
#33368=CARTESIAN_POINT('Ctrl Pts',(372.748527627384,-3.75554801241723,-2.59808526955013));
#33369=CARTESIAN_POINT('Ctrl Pts',(372.899032600674,-3.76805463356073,-2.47463060025924));
#33370=CARTESIAN_POINT('Ctrl Pts',(372.919651222622,-3.76977097162885,-2.45728070124938));
#33371=CARTESIAN_POINT('Ctrl Pts',(372.947870054799,-3.77212125364152,-2.4329244437565));
#33372=CARTESIAN_POINT('Ctrl Pts',(372.955657165518,-3.77276996167892,-2.42613762733044));
#33373=CARTESIAN_POINT('Ctrl Pts',(372.968973728147,-3.77387933443189,-2.41441851276293));
#33374=CARTESIAN_POINT('Ctrl Pts',(372.974518991729,-3.7743413073408,-2.40950441968526));
#33375=CARTESIAN_POINT('Ctrl Pts',(372.986091333157,-3.77530531981232,-2.39917779089605));
#33376=CARTESIAN_POINT('Ctrl Pts',(372.992115018516,-3.77580705990702,-2.39376159558856));
#33377=CARTESIAN_POINT('Ctrl Pts',(373.006826800607,-3.7770325234044,-2.38043284392909));
#33378=CARTESIAN_POINT('Ctrl Pts',(373.015492272111,-3.77775438793283,-2.37249527191035));
#33379=CARTESIAN_POINT('Ctrl Pts',(373.04685457927,-3.78036800144486,-2.34345032872171));
#33380=CARTESIAN_POINT('Ctrl Pts',(373.069290834093,-3.78223971845508,-2.32206247619523));
#33381=CARTESIAN_POINT('Ctrl Pts',(373.124898309436,-3.78689445588478,-2.26750062999015));
#33382=CARTESIAN_POINT('Ctrl Pts',(373.157661076496,-3.78965150877388,-2.23391912022644));
#33383=CARTESIAN_POINT('Ctrl Pts',(373.420178234749,-3.81198467921825,-1.95281622241874));
#33384=CARTESIAN_POINT('Ctrl Pts',(373.610458269654,-3.82996805825992,-1.67130180618511));
#33385=CARTESIAN_POINT('Ctrl Pts',(373.780113394984,-3.8534287674637,-1.30856238574083));
#33386=CARTESIAN_POINT('Ctrl Pts',(373.805006399867,-3.85714928361983,-1.25102185254051));
#33387=CARTESIAN_POINT('Ctrl Pts',(373.836598209323,-3.86229303504222,-1.17172715313238));
#33388=CARTESIAN_POINT('Ctrl Pts',(373.844768976411,-3.86366688147504,-1.15057196758881));
#33389=CARTESIAN_POINT('Ctrl Pts',(373.857412394046,-3.86586458791856,-1.11677956681121));
#33390=CARTESIAN_POINT('Ctrl Pts',(373.862030738563,-3.86668357060054,-1.10419739133355));
#33391=CARTESIAN_POINT('Ctrl Pts',(373.871352498341,-3.86837064607648,-1.07830304487691));
#33392=CARTESIAN_POINT('Ctrl Pts',(373.876047182889,-3.86923900727129,-1.0649880596574));
#33393=CARTESIAN_POINT('Ctrl Pts',(373.886726272867,-3.87125864715333,-1.03405350763706));
#33394=CARTESIAN_POINT('Ctrl Pts',(373.892645821064,-3.87241203792564,-1.0164122366533));
#33395=CARTESIAN_POINT('Ctrl Pts',(373.911058673749,-3.87611115906772,-0.959921266544794));
#33396=CARTESIAN_POINT('Ctrl Pts',(373.922966585009,-3.87867589013796,-0.920886356140307));
#33397=CARTESIAN_POINT('Ctrl Pts',(373.949186490513,-3.88475572296247,-0.828697904603664));
#33398=CARTESIAN_POINT('Ctrl Pts',(373.9628839076,-3.88828937970205,-0.775384235249085));
#33399=CARTESIAN_POINT('Ctrl Pts',(374.008765095857,-3.90158860469663,-0.575719352182483));
#33400=CARTESIAN_POINT('Ctrl Pts',(374.0320931526,-3.9115989174222,-0.427542673436495));
#33401=CARTESIAN_POINT('Ctrl Pts',(374.063845229113,-3.9364230442883,-0.0612172094050287));
#33402=CARTESIAN_POINT('Ctrl Pts',(374.060598827227,-3.95130997040103,0.15722391718154));
#33403=CARTESIAN_POINT('Ctrl Pts',(374.032396816226,-3.9669133748851,0.398809107101842));
#33404=CARTESIAN_POINT('Ctrl Pts',(374.029167073468,-3.96852327796972,0.423906014817121));
#33405=CARTESIAN_POINT('Ctrl Pts',(374.024239582691,-3.97075220844494,0.458931650489408));
#33406=CARTESIAN_POINT('Ctrl Pts',(374.022790470839,-3.97138413487997,0.468893669184143));
#33407=CARTESIAN_POINT('Ctrl Pts',(374.020203842003,-3.97247246227818,0.486108966869099));
#33408=CARTESIAN_POINT('Ctrl Pts',(374.019088184484,-3.97293006401439,0.493365382703262));
#33409=CARTESIAN_POINT('Ctrl Pts',(374.01667852328,-3.97389392191113,0.508689380776045));
#33410=CARTESIAN_POINT('Ctrl Pts',(374.015378617927,-3.97439982786514,0.516755971664285));
#33411=CARTESIAN_POINT('Ctrl Pts',(374.012077868809,-3.97565058972185,0.536754331800457));
#33412=CARTESIAN_POINT('Ctrl Pts',(374.010040464796,-3.97639340598691,0.548680083936111));
#33413=CARTESIAN_POINT('Ctrl Pts',(374.002124123033,-3.97917427346625,0.593495818295456));
#33414=CARTESIAN_POINT('Ctrl Pts',(373.995800777476,-3.9811887861083,0.626306449499276));
#33415=CARTESIAN_POINT('Ctrl Pts',(373.943875778393,-3.99632733087697,0.874867399492619));
#33416=CARTESIAN_POINT('Ctrl Pts',(373.876742610989,-4.00848282831185,1.08555047116196));
#33417=CARTESIAN_POINT('Ctrl Pts',(373.705280189953,-4.03250861791472,1.47891205875771));
#33418=CARTESIAN_POINT('Ctrl Pts',(373.603607089236,-4.04431114045585,1.66151350072321));
#33419=CARTESIAN_POINT('Ctrl Pts',(373.469416803599,-4.05843153649002,1.85556554642088));
#33420=CARTESIAN_POINT('Ctrl Pts',(373.453528325431,-4.06008355264648,1.87792609219064));
#33421=CARTESIAN_POINT('Ctrl Pts',(373.427021695981,-4.06280911222559,1.91423917636079));
#33422=CARTESIAN_POINT('Ctrl Pts',(373.41657149612,-4.06387619287794,1.92831297911782));
#33423=CARTESIAN_POINT('Ctrl Pts',(373.397576580063,-4.06580286700543,1.95346306253045));
#33424=CARTESIAN_POINT('Ctrl Pts',(373.389073522046,-4.06666081509207,1.96457036022048));
#33425=CARTESIAN_POINT('Ctrl Pts',(373.370781741681,-4.06849705016439,1.98814480010711));
#33426=CARTESIAN_POINT('Ctrl Pts',(373.360972842844,-4.06947612405606,2.00059574945215));
#33427=CARTESIAN_POINT('Ctrl Pts',(373.334155308242,-4.07213818354391,2.03412483121249));
#33428=CARTESIAN_POINT('Ctrl Pts',(373.316972452335,-4.07382812923219,2.05506136162226));
#33429=CARTESIAN_POINT('Ctrl Pts',(373.222871453893,-4.08300176313569,2.16681643109897));
#33430=CARTESIAN_POINT('Ctrl Pts',(373.141239622164,-4.09067834932071,2.25352789169221));
#33431=CARTESIAN_POINT('Ctrl Pts',(372.941899247381,-4.10880314254793,2.44306743086542));
#33432=CARTESIAN_POINT('Ctrl Pts',(372.821134419252,-4.11935178358883,2.54224917994442));
#33433=CARTESIAN_POINT('Ctrl Pts',(372.571281966395,-4.14004479943622,2.71873611795599));
#33434=CARTESIAN_POINT('Ctrl Pts',(372.443019729746,-4.15015981842891,2.79654129191001));
#33435=CARTESIAN_POINT('Ctrl Pts',(372.309820591895,-4.15988901539235,2.86513686072284));
#33436=CARTESIAN_POINT('Origin',(370.834317853224,2.31077344927308,0.));
#33437=CARTESIAN_POINT('',(372.30982061461,-5.65649214416028,2.86513684902517));
#33438=CARTESIAN_POINT('',(372.309820461314,-5.4072724248197,2.86513692797037));
#33439=CARTESIAN_POINT('',(372.309820613641,2.31077344927308,2.86513684952399));
#33440=CARTESIAN_POINT('Ctrl Pts',(372.30982061461,-5.65649214416028,2.86513684902516));
#33441=CARTESIAN_POINT('Ctrl Pts',(372.324646905427,-5.65549151767139,2.85750153029707));
#33442=CARTESIAN_POINT('Ctrl Pts',(372.339413897489,-5.65448700712985,2.849751145584));
#33443=CARTESIAN_POINT('Ctrl Pts',(372.371287420897,-5.65230123425484,2.83270561624129));
#33444=CARTESIAN_POINT('Ctrl Pts',(372.388370738551,-5.65111860453467,2.82336964709382));
#33445=CARTESIAN_POINT('Ctrl Pts',(372.417808569281,-5.64906086813046,2.80693386502652));
#33446=CARTESIAN_POINT('Ctrl Pts',(372.430202641378,-5.64818834276088,2.79990576683099));
#33447=CARTESIAN_POINT('Ctrl Pts',(372.455490109454,-5.6463952677621,2.78534397623984));
#33448=CARTESIAN_POINT('Ctrl Pts',(372.46837854585,-5.64547444838736,2.77780240319494));
#33449=CARTESIAN_POINT('Ctrl Pts',(372.500903467046,-5.64313281882727,2.7584659965061));
#33450=CARTESIAN_POINT('Ctrl Pts',(372.520467218694,-5.64170765669649,2.7465510255415));
#33451=CARTESIAN_POINT('Ctrl Pts',(372.594539642962,-5.63624671857717,2.70034878146331));
#33452=CARTESIAN_POINT('Ctrl Pts',(372.648140259158,-5.632159007086,2.66464099260271));
#33453=CARTESIAN_POINT('Ctrl Pts',(372.974343310244,-5.6064060655082,2.43292589040928));
#33454=CARTESIAN_POINT('Ctrl Pts',(373.215920612553,-5.58312211048917,2.19698114644329));
#33455=CARTESIAN_POINT('Ctrl Pts',(373.444722237587,-5.55787786934681,1.89052877422227));
#33456=CARTESIAN_POINT('Ctrl Pts',(373.471915974453,-5.55481751501434,1.85240025159212));
#33457=CARTESIAN_POINT('Ctrl Pts',(373.515687780797,-5.54980585174876,1.78810813736598));
#33458=CARTESIAN_POINT('Ctrl Pts',(373.532736485199,-5.54783063961079,1.76227479427757));
#33459=CARTESIAN_POINT('Ctrl Pts',(373.555735366145,-5.54513766641326,1.72630880515592));
#33460=CARTESIAN_POINT('Ctrl Pts',(373.562005659106,-5.54440044224962,1.71638416855106));
#33461=CARTESIAN_POINT('Ctrl Pts',(373.572507294621,-5.54316086084008,1.6995592530596));
#33462=CARTESIAN_POINT('Ctrl Pts',(373.576767091321,-5.54265666874517,1.69267694885435));
#33463=CARTESIAN_POINT('Ctrl Pts',(373.584873988485,-5.54169458086278,1.67946816877427));
#33464=CARTESIAN_POINT('Ctrl Pts',(373.588725262863,-5.54123640015409,1.67314440723975));
#33465=CARTESIAN_POINT('Ctrl Pts',(373.597893884134,-5.54014276182353,1.65797215025059));
#33466=CARTESIAN_POINT('Ctrl Pts',(373.603190615228,-5.53950862927065,1.64911120431293));
#33467=CARTESIAN_POINT('Ctrl Pts',(373.622153620668,-5.53722928122978,1.61703890362909));
#33468=CARTESIAN_POINT('Ctrl Pts',(373.635571772745,-5.53559917782147,1.59368116887163));
#33469=CARTESIAN_POINT('Ctrl Pts',(373.730812085376,-5.52388065936735,1.42297070013873));
#33470=CARTESIAN_POINT('Ctrl Pts',(373.801265837483,-5.51438616685968,1.26955030696506));
#33471=CARTESIAN_POINT('Ctrl Pts',(373.91303122637,-5.49623676717866,0.965314205608621));
#33472=CARTESIAN_POINT('Ctrl Pts',(373.956023607588,-5.48759516155223,0.815633857660002));
#33473=CARTESIAN_POINT('Ctrl Pts',(374.012495896879,-5.47191324494361,0.547187947629447));
#33474=CARTESIAN_POINT('Ctrl Pts',(374.03050277524,-5.46499155525484,0.429683314757538));
#33475=CARTESIAN_POINT('Ctrl Pts',(374.044597052922,-5.4562386729318,0.284529725317868));
#33476=CARTESIAN_POINT('Ctrl Pts',(374.046872732845,-5.45460453789132,0.257567044231749));
#33477=CARTESIAN_POINT('Ctrl Pts',(374.049941713462,-5.45199707482328,0.214782628524611));
#33478=CARTESIAN_POINT('Ctrl Pts',(374.050958367269,-5.45103075423221,0.198977831542825));
#33479=CARTESIAN_POINT('Ctrl Pts',(374.052652920555,-5.44920466006201,0.169210941900602));
#33480=CARTESIAN_POINT('Ctrl Pts',(374.053356557146,-5.44834571445371,0.155250640445523));
#33481=CARTESIAN_POINT('Ctrl Pts',(374.054737334368,-5.44640383512622,0.12378531742598));
#33482=CARTESIAN_POINT('Ctrl Pts',(374.05536260377,-5.44531930287454,0.10627857225238));
#33483=CARTESIAN_POINT('Ctrl Pts',(374.056600220576,-5.44252595655696,0.061363489917607));
#33484=CARTESIAN_POINT('Ctrl Pts',(374.057005608462,-5.44081074544034,0.0339512958255219));
#33485=CARTESIAN_POINT('Ctrl Pts',(374.057489157858,-5.42580277844255,-0.204404840944728));
#33486=CARTESIAN_POINT('Ctrl Pts',(374.03720586316,-5.41186293169812,-0.414841996855587));
#33487=CARTESIAN_POINT('Ctrl Pts',(373.965074170965,-5.38665259642414,-0.781699283207342));
#33488=CARTESIAN_POINT('Ctrl Pts',(373.921535743419,-5.37554454534307,-0.93902970781249));
#33489=CARTESIAN_POINT('Ctrl Pts',(373.839017853861,-5.35940211354028,-1.16806000342722));
#33490=CARTESIAN_POINT('Ctrl Pts',(373.808930079924,-5.35414993751283,-1.24268687981371));
#33491=CARTESIAN_POINT('Ctrl Pts',(373.769461387083,-5.34801344151446,-1.33090666728788));
#33492=CARTESIAN_POINT('Ctrl Pts',(373.762732468218,-5.34699056539046,-1.34564779551968));
#33493=CARTESIAN_POINT('Ctrl Pts',(373.752065852021,-5.34540559487515,-1.36855630626528));
#33494=CARTESIAN_POINT('Ctrl Pts',(373.748204496745,-5.34483903301053,-1.37675865036442));
#33495=CARTESIAN_POINT('Ctrl Pts',(373.740931212906,-5.34378533172292,-1.39204098473887));
#33496=CARTESIAN_POINT('Ctrl Pts',(373.737528022902,-5.34329769776267,-1.39912474001386));
#33497=CARTESIAN_POINT('Ctrl Pts',(373.729694571067,-5.34218741273633,-1.41527845638848));
#33498=CARTESIAN_POINT('Ctrl Pts',(373.725247585582,-5.34156580450749,-1.42434010556204));
#33499=CARTESIAN_POINT('Ctrl Pts',(373.713297930534,-5.33991797806365,-1.44840346899508));
#33500=CARTESIAN_POINT('Ctrl Pts',(373.7057204856,-5.33889620727996,-1.46336797989245));
#33501=CARTESIAN_POINT('Ctrl Pts',(373.639414499747,-5.33014576237488,-1.5918158479939));
#33502=CARTESIAN_POINT('Ctrl Pts',(373.574094472916,-5.32278681951285,-1.70178630154783));
#33503=CARTESIAN_POINT('Ctrl Pts',(373.396857078838,-5.30490381028631,-1.96339615710775));
#33504=CARTESIAN_POINT('Ctrl Pts',(373.277862871147,-5.29454528626369,-2.10964958834086));
#33505=CARTESIAN_POINT('Ctrl Pts',(373.050446434535,-5.2760017292912,-2.343933216325));
#33506=CARTESIAN_POINT('Ctrl Pts',(372.947829120339,-5.26799294342707,-2.43686525887041));
#33507=CARTESIAN_POINT('Ctrl Pts',(372.817542964072,-5.25801339699229,-2.54041872357883));
#33508=CARTESIAN_POINT('Ctrl Pts',(372.795290011404,-5.25631539458875,-2.55763508934913));
#33509=CARTESIAN_POINT('Ctrl Pts',(372.759976195503,-5.25362941032637,-2.58422440899075));
#33510=CARTESIAN_POINT('Ctrl Pts',(372.747065424199,-5.25264918796207,-2.59379501162311));
#33511=CARTESIAN_POINT('Ctrl Pts',(372.722813275474,-5.25081091728813,-2.61149330351116));
#33512=CARTESIAN_POINT('Ctrl Pts',(372.711489612163,-5.24995381594216,-2.61964471100201));
#33513=CARTESIAN_POINT('Ctrl Pts',(372.686100387786,-5.24803457993975,-2.63767215093226));
#33514=CARTESIAN_POINT('Ctrl Pts',(372.672008117829,-5.2469710032909,-2.64750966082783));
#33515=CARTESIAN_POINT('Ctrl Pts',(372.6361326769,-5.24426732579149,-2.67212909414519));
#33516=CARTESIAN_POINT('Ctrl Pts',(372.614246148032,-5.24262150458826,-2.68675747954303));
#33517=CARTESIAN_POINT('Ctrl Pts',(372.474954430997,-5.23216743712715,-2.77740746607341));
#33518=CARTESIAN_POINT('Ctrl Pts',(372.352898979344,-5.22308754895868,-2.84597661227349));
#33519=CARTESIAN_POINT('Ctrl Pts',(372.035785492412,-5.19974105518724,-2.99790763950144));
#33520=CARTESIAN_POINT('Ctrl Pts',(371.836240520109,-5.18524077418099,-3.07036104077704));
#33521=CARTESIAN_POINT('Ctrl Pts',(371.56359393141,-5.16643288900253,-3.13992340680465));
#33522=CARTESIAN_POINT('Ctrl Pts',(371.495604097281,-5.1618267467785,-3.15494283536281));
#33523=CARTESIAN_POINT('Ctrl Pts',(371.399975495633,-5.15550962580159,-3.17284018677567));
#33524=CARTESIAN_POINT('Ctrl Pts',(371.372708253527,-5.1537265760859,-3.1775807313505));
#33525=CARTESIAN_POINT('Ctrl Pts',(371.324893927462,-5.15063554013575,-3.18526031649999));
#33526=CARTESIAN_POINT('Ctrl Pts',(371.304373529068,-5.14932038718332,-3.18835316147302));
#33527=CARTESIAN_POINT('Ctrl Pts',(371.273917867183,-5.14738680647311,-3.19264302267347));
#33528=CARTESIAN_POINT('Ctrl Pts',(371.264005056932,-5.14676032759744,-3.19399225981672));
#33529=CARTESIAN_POINT('Ctrl Pts',(371.246316843103,-5.14564775979524,-3.19631597246973));
#33530=CARTESIAN_POINT('Ctrl Pts',(371.238544017884,-5.14516069489457,-3.19730827033428));
#33531=CARTESIAN_POINT('Ctrl Pts',(371.221591426488,-5.1441024264937,-3.19940966959952));
#33532=CARTESIAN_POINT('Ctrl Pts',(371.212410480767,-5.1435318486785,-3.20050761980941));
#33533=CARTESIAN_POINT('Ctrl Pts',(371.186761338326,-5.14194458820511,-3.20346309433044));
#33534=CARTESIAN_POINT('Ctrl Pts',(371.170283084457,-5.14093265493638,-3.20523315798925));
#33535=CARTESIAN_POINT('Ctrl Pts',(371.076900694595,-5.13523844693912,-3.21453604746284));
#33536=CARTESIAN_POINT('Ctrl Pts',(370.999752534408,-5.13068904940357,-3.21942880606091));
#33537=CARTESIAN_POINT('Ctrl Pts',(370.900340452009,-5.12494139558371,-3.22214988071866));
#33538=CARTESIAN_POINT('Ctrl Pts',(370.878177992615,-5.12366737439745,-3.22252775905837));
#33539=CARTESIAN_POINT('Ctrl Pts',(370.778335001081,-5.11795415573871,-3.22319990607404));
#33540=CARTESIAN_POINT('Ctrl Pts',(370.700660688103,-5.11358073492079,-3.22091420292741));
#33541=CARTESIAN_POINT('Ctrl Pts',(370.435261082579,-5.09867398897162,-3.20348605622059));
#33542=CARTESIAN_POINT('Ctrl Pts',(370.248832148169,-5.08824278153732,-3.17470815883318));
#33543=CARTESIAN_POINT('Ctrl Pts',(370.003759684228,-5.07369140125921,-3.11454588050704));
#33544=CARTESIAN_POINT('Ctrl Pts',(369.94200666875,-5.06995358368212,-3.09741875352984));
#33545=CARTESIAN_POINT('Ctrl Pts',(369.837022645712,-5.06344652433765,-3.06490144816775));
#33546=CARTESIAN_POINT('Ctrl Pts',(369.793533650584,-5.06070518925956,-3.05040760317297));
#33547=CARTESIAN_POINT('Ctrl Pts',(369.732029457587,-5.05675584460028,-3.0284413718049));
#33548=CARTESIAN_POINT('Ctrl Pts',(369.713748871939,-5.05557277196612,-3.02172500106408));
#33549=CARTESIAN_POINT('Ctrl Pts',(369.682200473244,-5.05351451464985,-3.00980832444101));
#33550=CARTESIAN_POINT('Ctrl Pts',(369.668904071322,-5.05264191495387,-3.00468489426048));
#33551=CARTESIAN_POINT('Ctrl Pts',(369.641746267532,-5.05084891683763,-2.99401294114284));
#33552=CARTESIAN_POINT('Ctrl Pts',(369.627888589966,-5.04992825024649,-2.9884559390301));
#33553=CARTESIAN_POINT('Ctrl Pts',(369.592879723652,-5.04758747589247,-2.97413401170751));
#33554=CARTESIAN_POINT('Ctrl Pts',(369.571782671624,-5.04616302256331,-2.96523972402519));
#33555=CARTESIAN_POINT('Ctrl Pts',(369.491789167395,-5.04070789426281,-2.93050688937293));
#33556=CARTESIAN_POINT('Ctrl Pts',(369.433579388903,-5.03662542487482,-2.90313360149514));
#33557=CARTESIAN_POINT('Ctrl Pts',(369.07673267804,-5.01087243452327,-2.72209441703721));
#33558=CARTESIAN_POINT('Ctrl Pts',(368.802904312656,-4.98758156421748,-2.52431833925148));
#33559=CARTESIAN_POINT('Ctrl Pts',(368.531329336638,-4.96233049908931,-2.2548956390582));
#33560=CARTESIAN_POINT('Ctrl Pts',(368.498806320119,-4.95926989002745,-2.22119264687658));
#33561=CARTESIAN_POINT('Ctrl Pts',(368.446026246626,-4.95425785607234,-2.16405607960657));
#33562=CARTESIAN_POINT('Ctrl Pts',(368.425352334165,-4.95228252375283,-2.14101863755636));
#33563=CARTESIAN_POINT('Ctrl Pts',(368.3972986173,-4.94958941537574,-2.10883679324896));
#33564=CARTESIAN_POINT('Ctrl Pts',(368.389632841798,-4.94885217372389,-2.09994537589614));
#33565=CARTESIAN_POINT('Ctrl Pts',(368.376764180204,-4.94761257147218,-2.08485323625828));
#33566=CARTESIAN_POINT('Ctrl Pts',(368.371535800518,-4.94710837588572,-2.07867449074258));
#33567=CARTESIAN_POINT('Ctrl Pts',(368.361569281017,-4.94614628805035,-2.06680596112113));
#33568=CARTESIAN_POINT('Ctrl Pts',(368.356827412674,-4.94568811083578,-2.06111947782452));
#33569=CARTESIAN_POINT('Ctrl Pts',(368.345521344389,-4.94459448952684,-2.04746576592711));
#33570=CARTESIAN_POINT('Ctrl Pts',(368.338975696935,-4.94396037040533,-2.03948318326187));
#33571=CARTESIAN_POINT('Ctrl Pts',(368.315490599295,-4.94168113495278,-2.01056018534058));
#33572=CARTESIAN_POINT('Ctrl Pts',(368.298774936091,-4.94005112870489,-1.98943841747473));
#33573=CARTESIAN_POINT('Ctrl Pts',(368.178843752613,-4.92827835760766,-1.83392695778037));
#33574=CARTESIAN_POINT('Ctrl Pts',(368.086092707703,-4.91873606956641,-1.6917752193104));
#33575=CARTESIAN_POINT('Ctrl Pts',(367.933190535076,-4.9008545141536,-1.4113960598316));
#33576=CARTESIAN_POINT('Ctrl Pts',(367.870703303659,-4.89252431986466,-1.27497665699189));
#33577=CARTESIAN_POINT('Ctrl Pts',(367.774603510989,-4.87694528387461,-1.01951608987162));
#33578=CARTESIAN_POINT('Ctrl Pts',(367.737908231019,-4.86978422037394,-0.901946457321207));
#33579=CARTESIAN_POINT('Ctrl Pts',(367.701393753535,-4.86076114382184,-0.756075639030048));
#33580=CARTESIAN_POINT('Ctrl Pts',(367.695097743755,-4.8591116428621,-0.729493537308239));
#33581=CARTESIAN_POINT('Ctrl Pts',(367.685674336434,-4.85648528368446,-0.687323927583807));
#33582=CARTESIAN_POINT('Ctrl Pts',(367.682322959629,-4.85551561081848,-0.671787432043597));
#33583=CARTESIAN_POINT('Ctrl Pts',(367.676241920511,-4.85368665205122,-0.642548945607366));
#33584=CARTESIAN_POINT('Ctrl Pts',(367.673486159424,-4.85282822314324,-0.628852715667466));
#33585=CARTESIAN_POINT('Ctrl Pts',(367.667491963347,-4.85089215113474,-0.598026148405397));
#33586=CARTESIAN_POINT('Ctrl Pts',(367.664303321402,-4.84981294929722,-0.580886684207893));
#33587=CARTESIAN_POINT('Ctrl Pts',(367.656507260779,-4.84704248606099,-0.537004454162611));
#33588=CARTESIAN_POINT('Ctrl Pts',(367.652098343247,-4.84534500352673,-0.510228246203521));
#33589=CARTESIAN_POINT('Ctrl Pts',(367.623610513318,-4.83338949410468,-0.322453233494839));
#33590=CARTESIAN_POINT('Ctrl Pts',(367.611426003885,-4.82275828032377,-0.159911944217903));
#33591=CARTESIAN_POINT('Ctrl Pts',(367.611724882292,-4.80004385520079,0.180009964118632));
#33592=CARTESIAN_POINT('Ctrl Pts',(367.626490871899,-4.78795182583808,0.356863727043824));
#33593=CARTESIAN_POINT('Ctrl Pts',(367.674066768005,-4.76862171279464,0.641332939805374));
#33594=CARTESIAN_POINT('Ctrl Pts',(367.698090140048,-4.76126992786214,0.750050526311881));
#33595=CARTESIAN_POINT('Ctrl Pts',(367.732087468951,-4.75313447488548,0.873245219936679));
#33596=CARTESIAN_POINT('Ctrl Pts',(367.736605453394,-4.75208872822624,0.889139182453399));
#33597=CARTESIAN_POINT('Ctrl Pts',(367.744089750632,-4.75041271698354,0.914718764157189));
#33598=CARTESIAN_POINT('Ctrl Pts',(367.746979768377,-4.74977831020298,0.924426146285701));
#33599=CARTESIAN_POINT('Ctrl Pts',(367.752189658175,-4.7486571670899,0.941628858885629));
#33600=CARTESIAN_POINT('Ctrl Pts',(367.754491188119,-4.74816939323319,0.949129514875481));
#33601=CARTESIAN_POINT('Ctrl Pts',(367.759538076874,-4.74711588470862,0.965365592880919));
#33602=CARTESIAN_POINT('Ctrl Pts',(367.762293278958,-4.74655072837297,0.9740977471101));
#33603=CARTESIAN_POINT('Ctrl Pts',(367.770155145203,-4.74496547387296,0.998649483639158));
#33604=CARTESIAN_POINT('Ctrl Pts',(367.775347127892,-4.74395021555722,1.01444172872425));
#33605=CARTESIAN_POINT('Ctrl Pts',(367.809042829425,-4.73755300007197,1.11432112568646));
#33606=CARTESIAN_POINT('Ctrl Pts',(367.840891668857,-4.73234889711195,1.19724817837271));
#33607=CARTESIAN_POINT('Ctrl Pts',(367.992824178923,-4.71033604001266,1.54871742555803));
#33608=CARTESIAN_POINT('Ctrl Pts',(368.145921593542,-4.69448974080339,1.80143171329925));
#33609=CARTESIAN_POINT('Ctrl Pts',(368.382236139445,-4.67271488014358,2.09284079008715));
#33610=CARTESIAN_POINT('Ctrl Pts',(368.435642198235,-4.66793638707432,2.15384326446947));
#33611=CARTESIAN_POINT('Ctrl Pts',(368.508395871514,-4.6615646349442,2.23087995053426));
#33612=CARTESIAN_POINT('Ctrl Pts',(368.525713198257,-4.66005764673338,2.24879588059757));
#33613=CARTESIAN_POINT('Ctrl Pts',(368.55404512125,-4.65760653609023,2.27743497038722));
#33614=CARTESIAN_POINT('Ctrl Pts',(368.564931946076,-4.65666802129122,2.28828349820155));
#33615=CARTESIAN_POINT('Ctrl Pts',(368.585936113334,-4.65486345078466,2.30891645540075));
#33616=CARTESIAN_POINT('Ctrl Pts',(368.596040791321,-4.65399797103665,2.31871331355835));
#33617=CARTESIAN_POINT('Ctrl Pts',(368.619471309767,-4.65199701372289,2.34113418829121));
#33618=CARTESIAN_POINT('Ctrl Pts',(368.63284138339,-4.65085954099763,2.35371107595666));
#33619=CARTESIAN_POINT('Ctrl Pts',(368.675301905866,-4.64726019371105,2.39297431863524));
#33620=CARTESIAN_POINT('Ctrl Pts',(368.704774769939,-4.64478072081449,2.41923996015343));
#33621=CARTESIAN_POINT('Ctrl Pts',(368.856871465799,-4.63207466577503,2.5498523535447));
#33622=CARTESIAN_POINT('Ctrl Pts',(368.986692802258,-4.62150107512343,2.64543188349788));
#33623=CARTESIAN_POINT('Ctrl Pts',(369.277044173948,-4.59853658134947,2.82737030229153));
#33624=CARTESIAN_POINT('Ctrl Pts',(369.438871391191,-4.58612404896,2.91064457028469));
#33625=CARTESIAN_POINT('Ctrl Pts',(369.69429547435,-4.56770124604273,3.015859834663));
#33626=CARTESIAN_POINT('Ctrl Pts',(369.783292055932,-4.56148820231008,3.04801735906208));
#33627=CARTESIAN_POINT('Ctrl Pts',(369.888814923402,-4.55445601495591,3.08097329393238));
#33628=CARTESIAN_POINT('Ctrl Pts',(369.904083061098,-4.55344658837929,3.08561752065752));
#33629=CARTESIAN_POINT('Ctrl Pts',(369.928935184991,-4.55181730817089,3.09297574825196));
#33630=CARTESIAN_POINT('Ctrl Pts',(369.938498153885,-4.55119366570206,3.09575900672334));
#33631=CARTESIAN_POINT('Ctrl Pts',(369.955604887496,-4.55008413455439,3.10065193790939));
#33632=CARTESIAN_POINT('Ctrl Pts',(369.963143576507,-4.54959729198648,3.10277848063583));
#33633=CARTESIAN_POINT('Ctrl Pts',(369.979630917529,-4.54853717935907,3.10736446613637));
#33634=CARTESIAN_POINT('Ctrl Pts',(369.988582463895,-4.54796455268825,3.10981274994618));
#33635=CARTESIAN_POINT('Ctrl Pts',(370.01415602629,-4.54633668878438,3.11668863177166));
#33636=CARTESIAN_POINT('Ctrl Pts',(370.030803371767,-4.5452867156206,3.1210219412368));
#33637=CARTESIAN_POINT('Ctrl Pts',(370.147091868934,-4.53801460299677,3.15029973668505));
#33638=CARTESIAN_POINT('Ctrl Pts',(370.247851427951,-4.53203128649899,3.17060396442827));
#33639=CARTESIAN_POINT('Ctrl Pts',(370.49347607998,-4.51783754306373,3.20798655603339));
#33640=CARTESIAN_POINT('Ctrl Pts',(370.638860227859,-4.50975440810934,3.22011654137405));
#33641=CARTESIAN_POINT('Ctrl Pts',(370.988721150358,-4.49015482597942,3.22551770126043));
#33642=CARTESIAN_POINT('Ctrl Pts',(371.192681092834,-4.47858288576605,3.20926245224846));
#33643=CARTESIAN_POINT('Ctrl Pts',(371.420712669612,-4.46472461313978,3.16907083084951));
#33644=CARTESIAN_POINT('Ctrl Pts',(371.447643079774,-4.46307385105367,3.16396916994804));
#33645=CARTESIAN_POINT('Ctrl Pts',(371.49167159215,-4.46035035335377,3.15504523570459));
#33646=CARTESIAN_POINT('Ctrl Pts',(371.508809728201,-4.4592840703786,3.15142587873747));
#33647=CARTESIAN_POINT('Ctrl Pts',(371.539569490001,-4.45735883915971,3.14466740258357));
#33648=CARTESIAN_POINT('Ctrl Pts',(371.553201897568,-4.45650153378486,3.14157900825419));
#33649=CARTESIAN_POINT('Ctrl Pts',(371.582237709249,-4.45466668314576,3.13480211716403));
#33650=CARTESIAN_POINT('Ctrl Pts',(371.597634830338,-4.45368835217053,3.13108856517249));
#33651=CARTESIAN_POINT('Ctrl Pts',(371.639265326823,-4.45102835527231,3.12072260197273));
#33652=CARTESIAN_POINT('Ctrl Pts',(371.665442837501,-4.44933974013695,3.11385310868284));
#33653=CARTESIAN_POINT('Ctrl Pts',(371.806132368478,-4.44017564550926,3.07503296523369));
#33654=CARTESIAN_POINT('Ctrl Pts',(371.918883867167,-4.43250769055062,3.0370976318991));
#33655=CARTESIAN_POINT('Ctrl Pts',(372.12480754239,-4.41789825027614,2.95488337808739));
#33656=CARTESIAN_POINT('Ctrl Pts',(372.218429702573,-4.41100910571352,2.91220181148356));
#33657=CARTESIAN_POINT('Ctrl Pts',(372.30982074573,-4.40407334669083,2.86513678150012));
#33658=CARTESIAN_POINT('',(367.611567853362,-4.5673390469264,2.97967533004691E-5));
#33659=CARTESIAN_POINT('Ctrl Pts',(372.309820591896,-4.15988901539235,2.86513686072284));
#33660=CARTESIAN_POINT('Ctrl Pts',(372.293919473726,-4.16105047268937,2.87332569935363));
#33661=CARTESIAN_POINT('Ctrl Pts',(372.27794799162,-4.16220630468556,2.88138329414723));
#33662=CARTESIAN_POINT('Ctrl Pts',(372.23775092834,-4.16508694134537,2.90124441904508));
#33663=CARTESIAN_POINT('Ctrl Pts',(372.213444456082,-4.16680325451408,2.91287718567665));
#33664=CARTESIAN_POINT('Ctrl Pts',(372.179621627552,-4.16915350879268,2.92854605760678));
#33665=CARTESIAN_POINT('Ctrl Pts',(372.170228240372,-4.16980221353723,2.93284293835819));
#33666=CARTESIAN_POINT('Ctrl Pts',(372.154061726601,-4.17091158218854,2.94014431067768));
#33667=CARTESIAN_POINT('Ctrl Pts',(372.147298667945,-4.17137355426733,2.94317071229736));
#33668=CARTESIAN_POINT('Ctrl Pts',(372.133119786015,-4.17233756672996,2.94945702136365));
#33669=CARTESIAN_POINT('Ctrl Pts',(372.125702026984,-4.17283930763598,2.95271232920548));
#33670=CARTESIAN_POINT('Ctrl Pts',(372.107493718593,-4.17406477600753,2.96062136524162));
#33671=CARTESIAN_POINT('Ctrl Pts',(372.096689704679,-4.17478664456424,2.96524416719236));
#33672=CARTESIAN_POINT('Ctrl Pts',(372.057298401016,-4.17740028914764,2.98184453228169));
#33673=CARTESIAN_POINT('Ctrl Pts',(372.028562986718,-4.17927203258121,2.99346905068147));
#33674=CARTESIAN_POINT('Ctrl Pts',(371.955928295334,-4.18392684939651,3.02163995791922));
#33675=CARTESIAN_POINT('Ctrl Pts',(371.911826108893,-4.18668395411857,3.03764619624868));
#33676=CARTESIAN_POINT('Ctrl Pts',(371.547476813413,-4.20901857090006,3.16094698166854));
#33677=CARTESIAN_POINT('Ctrl Pts',(371.212530176513,-4.22700316287315,3.21825685678827));
#33678=CARTESIAN_POINT('Ctrl Pts',(370.812104007818,-4.25046439235811,3.22328263691059));
#33679=CARTESIAN_POINT('Ctrl Pts',(370.749438150346,-4.25418376327138,3.22224131227551));
#33680=CARTESIAN_POINT('Ctrl Pts',(370.664193817272,-4.25932617057299,3.21833645612469));
#33681=CARTESIAN_POINT('Ctrl Pts',(370.641554295781,-4.26069985223141,3.21705982273558));
#33682=CARTESIAN_POINT('Ctrl Pts',(370.605558036364,-4.26289736099131,3.21464867995924));
#33683=CARTESIAN_POINT('Ctrl Pts',(370.592191386704,-4.26371631237675,3.21366954665046));
#33684=CARTESIAN_POINT('Ctrl Pts',(370.564757161574,-4.26540337247315,3.21148780671581));
#33685=CARTESIAN_POINT('Ctrl Pts',(370.550690622039,-4.26627174989232,3.21027607579472));
#33686=CARTESIAN_POINT('Ctrl Pts',(370.518102643931,-4.268291511133,3.20725300230315));
#33687=CARTESIAN_POINT('Ctrl Pts',(370.499588170261,-4.26944500784393,3.20537359685805));
#33688=CARTESIAN_POINT('Ctrl Pts',(370.440519256952,-4.27314481708523,3.19886016187596));
#33689=CARTESIAN_POINT('Ctrl Pts',(370.400037435893,-4.27571014026193,3.19361612333886));
#33690=CARTESIAN_POINT('Ctrl Pts',(370.305212883206,-4.28179162241,3.17949627377124));
#33691=CARTESIAN_POINT('Ctrl Pts',(370.250977701844,-4.28532634999213,3.16999405610348));
#33692=CARTESIAN_POINT('Ctrl Pts',(370.050066431028,-4.29863158101186,3.1294632045557));
#33693=CARTESIAN_POINT('Ctrl Pts',(369.905380234927,-4.30864707151545,3.08960461346886));
#33694=CARTESIAN_POINT('Ctrl Pts',(369.558292334868,-4.33349003476182,2.9673963601132));
#33695=CARTESIAN_POINT('Ctrl Pts',(369.360448027307,-4.34839063702113,2.87426577960914));
#33696=CARTESIAN_POINT('Ctrl Pts',(369.152012984451,-4.36399048017446,2.74892662005306));
#33697=CARTESIAN_POINT('Ctrl Pts',(369.130659354596,-4.36558686294989,2.73574396532394));
#33698=CARTESIAN_POINT('Ctrl Pts',(369.10024050926,-4.36785596639115,2.7164705922847));
#33699=CARTESIAN_POINT('Ctrl Pts',(369.091049466776,-4.36854091191462,2.71058149748293));
#33700=CARTESIAN_POINT('Ctrl Pts',(369.075290139734,-4.36971395926281,2.70037050786144));
#33701=CARTESIAN_POINT('Ctrl Pts',(369.0687074606,-4.37020351985001,2.69607109014549));
#33702=CARTESIAN_POINT('Ctrl Pts',(369.056028713149,-4.37114554483955,2.68772372850348));
#33703=CARTESIAN_POINT('Ctrl Pts',(369.049930650029,-4.37159823151033,2.68367908253868));
#33704=CARTESIAN_POINT('Ctrl Pts',(369.033354950083,-4.3728277910272,2.67260348645659));
#33705=CARTESIAN_POINT('Ctrl Pts',(369.02290461539,-4.37360196400808,2.66553162958238));
#33706=CARTESIAN_POINT('Ctrl Pts',(368.981709227445,-4.3766508711397,2.63730009682714));
#33707=CARTESIAN_POINT('Ctrl Pts',(368.951289879049,-4.3788958135154,2.61566749467324));
#33708=CARTESIAN_POINT('Ctrl Pts',(368.872484131582,-4.38471416435397,2.55753755169612));
#33709=CARTESIAN_POINT('Ctrl Pts',(368.824737986983,-4.3882419632125,2.52019433461088));
#33710=CARTESIAN_POINT('Ctrl Pts',(368.538200455607,-4.40962103051671,2.28276291406079));
#33711=CARTESIAN_POINT('Ctrl Pts',(368.328415428144,-4.42636054749662,2.0502768366703));
#33712=CARTESIAN_POINT('Ctrl Pts',(368.118629672299,-4.44843421413053,1.73651818524964));
#33713=CARTESIAN_POINT('Ctrl Pts',(368.083702052769,-4.45233959453823,1.68064556938772));
#33714=CARTESIAN_POINT('Ctrl Pts',(368.038865894922,-4.45769994605102,1.60377687690108));
#33715=CARTESIAN_POINT('Ctrl Pts',(368.027434475627,-4.45909986279602,1.58368481207129));
#33716=CARTESIAN_POINT('Ctrl Pts',(368.008950513878,-4.46142009575002,1.5503681882121));
#33717=CARTESIAN_POINT('Ctrl Pts',(368.001772195655,-4.46233588881326,1.53721410582272));
#33718=CARTESIAN_POINT('Ctrl Pts',(367.987953259396,-4.46412817661317,1.51146579954769));
#33719=CARTESIAN_POINT('Ctrl Pts',(367.981303838433,-4.46500433226035,1.49887667446756));
#33720=CARTESIAN_POINT('Ctrl Pts',(367.965810983394,-4.46707876434762,1.46906794037193));
#33721=CARTESIAN_POINT('Ctrl Pts',(367.957038924547,-4.4682795162656,1.45181204570901));
#33722=CARTESIAN_POINT('Ctrl Pts',(367.928354426482,-4.47229533909766,1.39410435122466));
#33723=CARTESIAN_POINT('Ctrl Pts',(367.90913618507,-4.47513427619917,1.35331528389806));
#33724=CARTESIAN_POINT('Ctrl Pts',(367.865258708932,-4.48198937111957,1.25488434570314));
#33725=CARTESIAN_POINT('Ctrl Pts',(367.841414085328,-4.4860311237511,1.19690146764548));
#33726=CARTESIAN_POINT('Ctrl Pts',(367.758603451583,-4.50133180203989,0.97755193973707));
#33727=CARTESIAN_POINT('Ctrl Pts',(367.710882855977,-4.51290203098739,0.812262034469767));
#33728=CARTESIAN_POINT('Ctrl Pts',(367.639129133981,-4.53719522700026,0.460415284340354));
#33729=CARTESIAN_POINT('Ctrl Pts',(367.617767905853,-4.54988161519056,0.273922287603608));
#33730=CARTESIAN_POINT('Ctrl Pts',(367.612195881093,-4.56313526092677,0.0666743665876585));
#33731=CARTESIAN_POINT('Ctrl Pts',(367.61184489797,-4.5644019459049,0.0467287152035062));
#33732=CARTESIAN_POINT('Ctrl Pts',(367.61162440377,-4.56607408325113,0.0201955132305951));
#33733=CARTESIAN_POINT('Ctrl Pts',(367.611589864399,-4.56648803135677,0.0136102795926603));
#33734=CARTESIAN_POINT('Ctrl Pts',(367.611570427038,-4.56704708473222,0.00469322337694372));
#33735=CARTESIAN_POINT('Ctrl Pts',(367.61156787492,-4.56719313445545,0.00236151425848598));
#33736=CARTESIAN_POINT('Ctrl Pts',(367.611567853362,-4.5673390469264,2.97967533004691E-5));
#33737=CARTESIAN_POINT('Ctrl Pts',(367.611567853355,-4.5673390901344,2.9106277886545E-5));
#33738=CARTESIAN_POINT('Ctrl Pts',(367.61156783133,-4.56749169558373,-0.00240956713773506));
#33739=CARTESIAN_POINT('Ctrl Pts',(367.611570577343,-4.56764415094795,-0.00484825048755294));
#33740=CARTESIAN_POINT('Ctrl Pts',(367.611590360164,-4.56819056498431,-0.013597455458878));
#33741=CARTESIAN_POINT('Ctrl Pts',(367.611623164111,-4.56858365646499,-0.0199079810364738));
#33742=CARTESIAN_POINT('Ctrl Pts',(367.611739809861,-4.5694743820323,-0.0342455138049178));
#33743=CARTESIAN_POINT('Ctrl Pts',(367.611835107448,-4.56997135991083,-0.042272412898108));
#33744=CARTESIAN_POINT('Ctrl Pts',(367.612143532491,-4.57119072346036,-0.0620313833186715));
#33745=CARTESIAN_POINT('Ctrl Pts',(367.612390745664,-4.57191123222472,-0.0737629251980433));
#33746=CARTESIAN_POINT('Ctrl Pts',(367.613502174776,-4.57447190567572,-0.115644657201449));
#33747=CARTESIAN_POINT('Ctrl Pts',(367.614725600891,-4.57629331399327,-0.145784767931852));
#33748=CARTESIAN_POINT('Ctrl Pts',(367.61788208994,-4.5797494032511,-0.203528670621334));
#33749=CARTESIAN_POINT('Ctrl Pts',(367.619747819506,-4.5813869001697,-0.23113314977507));
#33750=CARTESIAN_POINT('Ctrl Pts',(367.635394725314,-4.59282944384832,-0.425416800950013));
#33751=CARTESIAN_POINT('Ctrl Pts',(367.661778371179,-4.6021543633138,-0.590840015721989));
#33752=CARTESIAN_POINT('Ctrl Pts',(367.736884862957,-4.62011598369071,-0.903178918229882));
#33753=CARTESIAN_POINT('Ctrl Pts',(367.783562354811,-4.62872678280989,-1.0501000850242));
#33754=CARTESIAN_POINT('Ctrl Pts',(367.863380652703,-4.64117900050485,-1.25037988907046));
#33755=CARTESIAN_POINT('Ctrl Pts',(367.887840056502,-4.64478014190965,-1.3069757656596));
#33756=CARTESIAN_POINT('Ctrl Pts',(367.93273146274,-4.65107058671465,-1.40317344158835));
#33757=CARTESIAN_POINT('Ctrl Pts',(367.952389672441,-4.65373449939021,-1.44311779116309));
#33758=CARTESIAN_POINT('Ctrl Pts',(367.981729119955,-4.65759202267539,-1.49974199418895));
#33759=CARTESIAN_POINT('Ctrl Pts',(367.99074298682,-4.65876230109209,-1.51676316033512));
#33760=CARTESIAN_POINT('Ctrl Pts',(368.006676485508,-4.66080605425554,-1.54620958950122));
#33761=CARTESIAN_POINT('Ctrl Pts',(368.013526860387,-4.66167705309079,-1.55867185885553));
#33762=CARTESIAN_POINT('Ctrl Pts',(368.026903593353,-4.6633633927571,-1.58262992335582));
#33763=CARTESIAN_POINT('Ctrl Pts',(368.033418651477,-4.66417831552572,-1.59413172422668));
#33764=CARTESIAN_POINT('Ctrl Pts',(368.049050274562,-4.66611870116859,-1.62133641315909));
#33765=CARTESIAN_POINT('Ctrl Pts',(368.058229074867,-4.66724639672523,-1.63700284740387));
#33766=CARTESIAN_POINT('Ctrl Pts',(368.091396324818,-4.67128076144585,-1.69253167803771));
#33767=CARTESIAN_POINT('Ctrl Pts',(368.116114040863,-4.674213831618,-1.73194967137018));
#33768=CARTESIAN_POINT('Ctrl Pts',(368.288398268864,-4.69418858768308,-1.9939190200968));
#33769=CARTESIAN_POINT('Ctrl Pts',(368.46225853107,-4.71225594868572,-2.1978861758204));
#33770=CARTESIAN_POINT('Ctrl Pts',(368.739749156881,-4.73765921718434,-2.45169504942337));
#33771=CARTESIAN_POINT('Ctrl Pts',(368.823968767106,-4.7449912016118,-2.52121521921582));
#33772=CARTESIAN_POINT('Ctrl Pts',(368.941239434253,-4.7545640243675,-2.60839789022961));
#33773=CARTESIAN_POINT('Ctrl Pts',(368.971299750482,-4.7569650906298,-2.62995232684662));
#33774=CARTESIAN_POINT('Ctrl Pts',(369.023062455875,-4.76100219775396,-2.66573521965481));
#33775=CARTESIAN_POINT('Ctrl Pts',(369.044577285141,-4.76265236078809,-2.68022744816824));
#33776=CARTESIAN_POINT('Ctrl Pts',(369.073407207015,-4.76482441100863,-2.6991450911493));
#33777=CARTESIAN_POINT('Ctrl Pts',(369.080567591396,-4.76536070513963,-2.70380297914112));
#33778=CARTESIAN_POINT('Ctrl Pts',(369.094617881,-4.76640671404711,-2.7128635092179));
#33779=CARTESIAN_POINT('Ctrl Pts',(369.101506185877,-4.76691657976865,-2.71726850753316));
#33780=CARTESIAN_POINT('Ctrl Pts',(369.114935001524,-4.76790472565494,-2.72578426242777));
#33781=CARTESIAN_POINT('Ctrl Pts',(369.121473632023,-4.76838318269839,-2.72989778412489));
#33782=CARTESIAN_POINT('Ctrl Pts',(369.137563540009,-4.7695541343471,-2.73993954883162));
#33783=CARTESIAN_POINT('Ctrl Pts',(369.147131275099,-4.7702449166131,-2.74584147211256));
#33784=CARTESIAN_POINT('Ctrl Pts',(369.17970226886,-4.77257855395983,-2.76569859346902));
#33785=CARTESIAN_POINT('Ctrl Pts',(369.20285001411,-4.77420681799314,-2.77941616874181));
#33786=CARTESIAN_POINT('Ctrl Pts',(369.365414364712,-4.78545232999753,-2.87302254474681));
#33787=CARTESIAN_POINT('Ctrl Pts',(369.510480136433,-4.79453092395336,-2.94268619286354));
#33788=CARTESIAN_POINT('Ctrl Pts',(369.835516443079,-4.81409272413024,-3.06984894306167));
#33789=CARTESIAN_POINT('Ctrl Pts',(370.016546079625,-4.82452491184807,-3.12295089737209));
#33790=CARTESIAN_POINT('Ctrl Pts',(370.264007762305,-4.83907789093516,-3.17253380302107));
#33791=CARTESIAN_POINT('Ctrl Pts',(370.327201399934,-4.84281630296755,-3.18324622114236));
#33792=CARTESIAN_POINT('Ctrl Pts',(370.436082814754,-4.84932467247368,-3.19837905885008));
#33793=CARTESIAN_POINT('Ctrl Pts',(370.481623606829,-4.85206672020446,-3.20372068107175));
#33794=CARTESIAN_POINT('Ctrl Pts',(370.546658504854,-4.85601742984184,-3.20994538329748));
#33795=CARTESIAN_POINT('Ctrl Pts',(370.56607190082,-4.85720114455174,-3.21162596634361));
#33796=CARTESIAN_POINT('Ctrl Pts',(370.599715813797,-4.85926065809297,-3.21423128832623));
#33797=CARTESIAN_POINT('Ctrl Pts',(370.613939573923,-4.86013386999416,-3.2152378287568));
#33798=CARTESIAN_POINT('Ctrl Pts',(370.643081708342,-4.86192825955075,-3.21710577863768));
#33799=CARTESIAN_POINT('Ctrl Pts',(370.658000311999,-4.86284970664928,-3.21795788765467));
#33800=CARTESIAN_POINT('Ctrl Pts',(370.695814222956,-4.86519275008332,-3.21985396901567));
#33801=CARTESIAN_POINT('Ctrl Pts',(370.718715442905,-4.86661870224337,-3.22075750042442));
#33802=CARTESIAN_POINT('Ctrl Pts',(370.806011772148,-4.87208169168222,-3.22326939001521));
#33803=CARTESIAN_POINT('Ctrl Pts',(370.870436706153,-4.87617069144845,-3.22319116274022));
#33804=CARTESIAN_POINT('Ctrl Pts',(371.270331054117,-4.90192170300657,-3.21071523171121));
#33805=CARTESIAN_POINT('Ctrl Pts',(371.602062342495,-4.92520163733484,-3.14790228335611));
#33806=CARTESIAN_POINT('Ctrl Pts',(371.962182829444,-4.95044256361864,-3.0193096845631));
#33807=CARTESIAN_POINT('Ctrl Pts',(372.005936928852,-4.95350313697301,-3.00260213193215));
#33808=CARTESIAN_POINT('Ctrl Pts',(372.077984227813,-4.95851541854305,-2.97327592352257));
#33809=CARTESIAN_POINT('Ctrl Pts',(372.106486621939,-4.9604910258847,-2.96119275921003));
#33810=CARTESIAN_POINT('Ctrl Pts',(372.145558182348,-4.96318477632228,-2.94396065076232));
#33811=CARTESIAN_POINT('Ctrl Pts',(372.156278891141,-4.96392238701745,-2.93916221706436));
#33812=CARTESIAN_POINT('Ctrl Pts',(372.174347706462,-4.96516269709834,-2.93095601357467));
#33813=CARTESIAN_POINT('Ctrl Pts',(372.1817095747,-4.96566723267963,-2.9275789852835));
#33814=CARTESIAN_POINT('Ctrl Pts',(372.19578270486,-4.96663005582166,-2.92105904345576));
#33815=CARTESIAN_POINT('Ctrl Pts',(372.202495939613,-4.96708862819769,-2.91792069873949));
#33816=CARTESIAN_POINT('Ctrl Pts',(372.218544847323,-4.96818332561718,-2.91035049170517));
#33817=CARTESIAN_POINT('Ctrl Pts',(372.227870213606,-4.96881812228117,-2.90589679468957));
#33818=CARTESIAN_POINT('Ctrl Pts',(372.261463792011,-4.97110081962247,-2.88965394944243));
#33819=CARTESIAN_POINT('Ctrl Pts',(372.285605908921,-4.97273355670686,-2.87760465762333));
#33820=CARTESIAN_POINT('Ctrl Pts',(372.457232121304,-4.98430520807724,-2.78923683433564));
#33821=CARTESIAN_POINT('Ctrl Pts',(372.5987922299,-4.99366823639472,-2.70191346638495));
#33822=CARTESIAN_POINT('Ctrl Pts',(372.860040759497,-5.01177753712549,-2.51143033901138));
#33823=CARTESIAN_POINT('Ctrl Pts',(372.980127787805,-5.02050877192922,-2.40963343452384));
#33824=CARTESIAN_POINT('Ctrl Pts',(373.177519001036,-5.03631980452203,-2.21580461291884));
#33825=CARTESIAN_POINT('Ctrl Pts',(373.258010337101,-5.04327702672265,-2.12746136562321));
#33826=CARTESIAN_POINT('Ctrl Pts',(373.350526322932,-5.05207079180567,-2.01383899041327));
#33827=CARTESIAN_POINT('Ctrl Pts',(373.367377678986,-5.05370803698993,-1.99260141355721));
#33828=CARTESIAN_POINT('Ctrl Pts',(373.393656996375,-5.05631977412781,-1.95860974520919));
#33829=CARTESIAN_POINT('Ctrl Pts',(373.403262430015,-5.05728722614092,-1.94599402132065));
#33830=CARTESIAN_POINT('Ctrl Pts',(373.421165326502,-5.05911503633787,-1.9221168970291));
#33831=CARTESIAN_POINT('Ctrl Pts',(373.42948335571,-5.05997456172435,-1.9108713250162));
#33832=CARTESIAN_POINT('Ctrl Pts',(373.448054977356,-5.06191719154415,-1.88541846394029));
#33833=CARTESIAN_POINT('Ctrl Pts',(373.458266384025,-5.06300189202151,-1.87118107796508));
#33834=CARTESIAN_POINT('Ctrl Pts',(373.484149126359,-5.06579458313312,-1.8344652183583));
#33835=CARTESIAN_POINT('Ctrl Pts',(373.499650535105,-5.06750895898634,-1.81186920992117));
#33836=CARTESIAN_POINT('Ctrl Pts',(373.634721617425,-5.08282862561395,-1.60949470714902));
#33837=CARTESIAN_POINT('Ctrl Pts',(373.736209965257,-5.09711416821223,-1.41835311086057));
#33838=CARTESIAN_POINT('Ctrl Pts',(373.881592565808,-5.12305659503884,-1.06239466764015));
#33839=CARTESIAN_POINT('Ctrl Pts',(373.933011139083,-5.13455036461611,-0.901481487870583));
#33840=CARTESIAN_POINT('Ctrl Pts',(373.982437730418,-5.14881683692809,-0.691160760332164));
#33841=CARTESIAN_POINT('Ctrl Pts',(373.992258202229,-5.15191426667614,-0.644806303276504));
#33842=CARTESIAN_POINT('Ctrl Pts',(374.006849284367,-5.15698014063531,-0.567570856328441));
#33843=CARTESIAN_POINT('Ctrl Pts',(374.012199202389,-5.15897309814704,-0.536807840724318));
#33844=CARTESIAN_POINT('Ctrl Pts',(374.018951618596,-5.16168635478182,-0.494332096734604));
#33845=CARTESIAN_POINT('Ctrl Pts',(374.020737992468,-5.1624264823062,-0.482683278927524));
#33846=CARTESIAN_POINT('Ctrl Pts',(374.023645356971,-5.16366979310232,-0.463004709257983));
#33847=CARTESIAN_POINT('Ctrl Pts',(374.024800008722,-5.16417483246384,-0.454980117632955));
#33848=CARTESIAN_POINT('Ctrl Pts',(374.026950962201,-5.16513765447608,-0.43962050152736));
#33849=CARTESIAN_POINT('Ctrl Pts',(374.027952288016,-5.16559572831676,-0.432286309539131));
#33850=CARTESIAN_POINT('Ctrl Pts',(374.030286794076,-5.16668799422482,-0.414736335829573));
#33851=CARTESIAN_POINT('Ctrl Pts',(374.03159628511,-5.16732087123557,-0.404517409809721));
#33852=CARTESIAN_POINT('Ctrl Pts',(374.036129707252,-5.16958779118483,-0.367741824506884));
#33853=CARTESIAN_POINT('Ctrl Pts',(374.039072053837,-5.17120694875675,-0.341150725042209));
#33854=CARTESIAN_POINT('Ctrl Pts',(374.059739493092,-5.18390397495795,-0.130394811709377));
#33855=CARTESIAN_POINT('Ctrl Pts',(374.061908748277,-5.19426255870464,0.0549731295664442));
#33856=CARTESIAN_POINT('Ctrl Pts',(374.035357905991,-5.21424318585932,0.411224608262495));
#33857=CARTESIAN_POINT('Ctrl Pts',(374.008822082956,-5.22383835415168,0.581619532240991));
#33858=CARTESIAN_POINT('Ctrl Pts',(373.954945366254,-5.23724444174472,0.807067104760386));
#33859=CARTESIAN_POINT('Ctrl Pts',(373.939478912231,-5.24073195937061,0.864666168279185));
#33860=CARTESIAN_POINT('Ctrl Pts',(373.910010248708,-5.24684135682526,0.963388552580442));
#33861=CARTESIAN_POINT('Ctrl Pts',(373.896757918642,-5.24943983191205,1.00471975742616));
#33862=CARTESIAN_POINT('Ctrl Pts',(373.876487902059,-5.25321914263788,1.06380569319686));
#33863=CARTESIAN_POINT('Ctrl Pts',(373.870140499877,-5.25437795698478,1.08178648206707));
#33864=CARTESIAN_POINT('Ctrl Pts',(373.858792129035,-5.25640833400212,1.11304728351068));
#33865=CARTESIAN_POINT('Ctrl Pts',(373.853862276741,-5.25727751481283,1.1263526821669));
#33866=CARTESIAN_POINT('Ctrl Pts',(373.843509540213,-5.25907698678434,1.15373765974165));
#33867=CARTESIAN_POINT('Ctrl Pts',(373.838075335545,-5.26000763949256,1.16781255842225));
#33868=CARTESIAN_POINT('Ctrl Pts',(373.823891583472,-5.26240199504537,1.20379523536076));
#33869=CARTESIAN_POINT('Ctrl Pts',(373.815000076283,-5.26387044215318,1.2256457460806));
#33870=CARTESIAN_POINT('Ctrl Pts',(373.778963788829,-5.26969816501012,1.31149152155546));
#33871=CARTESIAN_POINT('Ctrl Pts',(373.749993010801,-5.27411871197094,1.37469519565188));
#33872=CARTESIAN_POINT('Ctrl Pts',(373.693283396761,-5.2823269444942,1.48854330779087));
#33873=CARTESIAN_POINT('Ctrl Pts',(373.666183137504,-5.28609279136623,1.53947509423521));
#33874=CARTESIAN_POINT('Ctrl Pts',(373.524893301944,-5.30497582567348,1.78864561345945));
#33875=CARTESIAN_POINT('Ctrl Pts',(373.391190336137,-5.3206423688271,1.97505358556245));
#33876=CARTESIAN_POINT('Ctrl Pts',(373.166295787833,-5.343259300714,2.22708083387742));
#33877=CARTESIAN_POINT('Ctrl Pts',(373.089596701636,-5.35045574351338,2.30471960462456));
#33878=CARTESIAN_POINT('Ctrl Pts',(372.996236868403,-5.35850040755049,2.39008945022414));
#33879=CARTESIAN_POINT('Ctrl Pts',(372.983277444187,-5.35960204742744,2.40174813754398));
#33880=CARTESIAN_POINT('Ctrl Pts',(372.963234798735,-5.36128199031781,2.41948699280532));
#33881=CARTESIAN_POINT('Ctrl Pts',(372.956218925378,-5.36186563473029,2.42564228904179));
#33882=CARTESIAN_POINT('Ctrl Pts',(372.943264027227,-5.36293508759162,2.43690890078574));
#33883=CARTESIAN_POINT('Ctrl Pts',(372.937333107867,-5.3634215295444,2.44202903271365));
#33884=CARTESIAN_POINT('Ctrl Pts',(372.92385876704,-5.36451956682261,2.45357586616033));
#33885=CARTESIAN_POINT('Ctrl Pts',(372.916304346764,-5.36513020483426,2.45998943256101));
#33886=CARTESIAN_POINT('Ctrl Pts',(372.896644362223,-5.36670686378338,2.47652496921642));
#33887=CARTESIAN_POINT('Ctrl Pts',(372.884493666959,-5.36766913245581,2.48659319320744));
#33888=CARTESIAN_POINT('Ctrl Pts',(372.802510091008,-5.37408442786569,2.55351637515286));
#33889=CARTESIAN_POINT('Ctrl Pts',(372.730388073186,-5.37935507280865,2.60751746871394));
#33890=CARTESIAN_POINT('Ctrl Pts',(372.586728704315,-5.38935477448608,2.70596461712801));
#33891=CARTESIAN_POINT('Ctrl Pts',(372.515528521158,-5.39409276530735,2.75076718665827));
#33892=CARTESIAN_POINT('Ctrl Pts',(372.398932304311,-5.40163546964469,2.81791498784454));
#33893=CARTESIAN_POINT('Ctrl Pts',(372.354641551306,-5.40445302519935,2.84205473788886));
#33894=CARTESIAN_POINT('Ctrl Pts',(372.309820461314,-5.4072724248197,2.86513692797036));
#33895=CARTESIAN_POINT('Origin',(370.834317853224,2.31077344927308,0.));
#33896=CARTESIAN_POINT('',(372.309820841127,-6.90205582396877,2.86513673237215));
#33897=CARTESIAN_POINT('',(372.309820613387,-6.65415806382429,2.86513684965521));
#33898=CARTESIAN_POINT('',(372.309820613641,2.31077344927308,2.86513684952399));
#33899=CARTESIAN_POINT('',(367.611568185609,-6.06328577097763,-0.00146369061351841));
#33900=CARTESIAN_POINT('Ctrl Pts',(372.309820841127,-6.90205582396877,2.86513673237218));
#33901=CARTESIAN_POINT('Ctrl Pts',(372.446892394609,-6.89335341312441,2.79454691219575));
#33902=CARTESIAN_POINT('Ctrl Pts',(372.578798052852,-6.88482060320103,2.71417238188656));
#33903=CARTESIAN_POINT('Ctrl Pts',(372.834224677179,-6.86711783945021,2.53216542364717));
#33904=CARTESIAN_POINT('Ctrl Pts',(372.956898778901,-6.85796300922688,2.43025308518973));
#33905=CARTESIAN_POINT('Ctrl Pts',(373.09098498409,-6.84680990289232,2.30093495123234));
#33906=CARTESIAN_POINT('Ctrl Pts',(373.110203648382,-6.84518154058616,2.28192724901351));
#33907=CARTESIAN_POINT('Ctrl Pts',(373.14139789483,-6.84248752696836,2.25028932561982));
#33908=CARTESIAN_POINT('Ctrl Pts',(373.153514522936,-6.84142808893705,2.23779962375938));
#33909=CARTESIAN_POINT('Ctrl Pts',(373.175173777093,-6.83951026579169,2.21510862347118));
#33910=CARTESIAN_POINT('Ctrl Pts',(373.184752413597,-6.83865346919856,2.20494218467981));
#33911=CARTESIAN_POINT('Ctrl Pts',(373.205103405779,-6.83681427000154,2.18305903350481));
#33912=CARTESIAN_POINT('Ctrl Pts',(373.215855626105,-6.83583104204865,2.17132418164365));
#33913=CARTESIAN_POINT('Ctrl Pts',(373.244893132356,-6.83314384750216,2.139157818121));
#33914=CARTESIAN_POINT('Ctrl Pts',(373.263004978278,-6.83143268790175,2.11857218927035));
#33915=CARTESIAN_POINT('Ctrl Pts',(373.362098925185,-6.8218708082262,2.00300279412954));
#33916=CARTESIAN_POINT('Ctrl Pts',(373.43776309168,-6.81380693543997,1.90361856566612));
#33917=CARTESIAN_POINT('Ctrl Pts',(373.590511133459,-6.79575020330898,1.67678860460122));
#33918=CARTESIAN_POINT('Ctrl Pts',(373.664916411395,-6.7857015446068,1.54787839974188));
#33919=CARTESIAN_POINT('Ctrl Pts',(373.804199150838,-6.76423127927737,1.26269210935036));
#33920=CARTESIAN_POINT('Ctrl Pts',(373.866231334591,-6.75283865110786,1.10548526078697));
#33921=CARTESIAN_POINT('Ctrl Pts',(373.923561418022,-6.74026581267486,0.918377516961789));
#33922=CARTESIAN_POINT('Ctrl Pts',(373.931129427964,-6.73855011828964,0.892525208007266));
#33923=CARTESIAN_POINT('Ctrl Pts',(373.941148526574,-6.73620086657586,0.856637202069017));
#33924=CARTESIAN_POINT('Ctrl Pts',(373.943876606714,-6.73555255390665,0.846680869181379));
#33925=CARTESIAN_POINT('Ctrl Pts',(373.948479139774,-6.73444389578485,0.829561248101092));
#33926=CARTESIAN_POINT('Ctrl Pts',(373.950376813739,-6.73398224344689,0.82240436538717));
#33927=CARTESIAN_POINT('Ctrl Pts',(373.95429729247,-6.73301896247213,0.807410287350992));
#33928=CARTESIAN_POINT('Ctrl Pts',(373.956315260584,-6.73251763246957,0.7995719252528));
#33929=CARTESIAN_POINT('Ctrl Pts',(373.961187639811,-6.73129330532713,0.780346531507207));
#33930=CARTESIAN_POINT('Ctrl Pts',(373.964009439518,-6.73057216271791,0.768951205270003));
#33931=CARTESIAN_POINT('Ctrl Pts',(373.974043906044,-6.72796198450127,0.727458406749683));
#33932=CARTESIAN_POINT('Ctrl Pts',(373.980885446218,-6.72609292165653,0.697271800410228));
#33933=CARTESIAN_POINT('Ctrl Pts',(373.996982421315,-6.7214456161622,0.621178710459467));
#33934=CARTESIAN_POINT('Ctrl Pts',(374.00567440897,-6.71869324573128,0.575159273926589));
#33935=CARTESIAN_POINT('Ctrl Pts',(374.068454496733,-6.69648204196127,0.197854993716503));
#33936=CARTESIAN_POINT('Ctrl Pts',(374.07148820629,-6.67860091751119,-0.139836432719794));
#33937=CARTESIAN_POINT('Ctrl Pts',(374.012897362792,-6.6551823444063,-0.535625657501086));
#33938=CARTESIAN_POINT('Ctrl Pts',(374.001563567063,-6.65136357540348,-0.599012767866996));
#33939=CARTESIAN_POINT('Ctrl Pts',(373.983634672657,-6.64610512671085,-0.684430966943835));
#33940=CARTESIAN_POINT('Ctrl Pts',(373.978690911363,-6.64471781268548,-0.706795732458364));
#33941=CARTESIAN_POINT('Ctrl Pts',(373.970131015667,-6.64241344662177,-0.743650690081685));
#33942=CARTESIAN_POINT('Ctrl Pts',(373.966651752029,-6.64150079934517,-0.758172060434328));
#33943=CARTESIAN_POINT('Ctrl Pts',(373.959655649395,-6.63971093570322,-0.786501262742072));
#33944=CARTESIAN_POINT('Ctrl Pts',(373.956147904371,-6.6388340307947,-0.800311000707794));
#33945=CARTESIAN_POINT('Ctrl Pts',(373.947630670008,-6.63675185004074,-0.832934518771759));
#33946=CARTESIAN_POINT('Ctrl Pts',(373.942542085688,-6.63554404046041,-0.851726893882208));
#33947=CARTESIAN_POINT('Ctrl Pts',(373.924912884816,-6.63147624093134,-0.914569612306046));
#33948=CARTESIAN_POINT('Ctrl Pts',(373.911604043972,-6.6285915166329,-0.958396879757595));
#33949=CARTESIAN_POINT('Ctrl Pts',(373.877467718884,-6.62160394354454,-1.06275731639248));
#33950=CARTESIAN_POINT('Ctrl Pts',(373.855762434972,-6.61747415369357,-1.12298084149327));
#33951=CARTESIAN_POINT('Ctrl Pts',(373.763326588186,-6.6010200597628,-1.35732807196608));
#33952=CARTESIAN_POINT('Ctrl Pts',(373.679221629631,-6.58831567479994,-1.52575899481742));
#33953=CARTESIAN_POINT('Ctrl Pts',(373.542229000303,-6.57060449359006,-1.74894528109535));
#33954=CARTESIAN_POINT('Ctrl Pts',(373.501361069712,-6.56560896492734,-1.81065551816899));
#33955=CARTESIAN_POINT('Ctrl Pts',(373.44098132957,-6.55865727947021,-1.89534266333292));
#33956=CARTESIAN_POINT('Ctrl Pts',(373.423217458109,-6.55665991678401,-1.91953567475778));
#33957=CARTESIAN_POINT('Ctrl Pts',(373.360515991192,-6.54978094402636,-2.00247614013516));
#33958=CARTESIAN_POINT('Ctrl Pts',(373.313892447476,-6.54495999603694,-2.05992703600282));
#33959=CARTESIAN_POINT('Ctrl Pts',(373.254580636894,-6.53922091527929,-2.12807746373779));
#33960=CARTESIAN_POINT('Ctrl Pts',(373.243737656792,-6.53818692128459,-2.14034620332716));
#33961=CARTESIAN_POINT('Ctrl Pts',(373.226655825798,-6.53658224054839,-2.15937982929537));
#33962=CARTESIAN_POINT('Ctrl Pts',(373.220480879619,-6.53600702305893,-2.1662013384265));
#33963=CARTESIAN_POINT('Ctrl Pts',(373.208990054352,-6.53494573298259,-2.1787865830763));
#33964=CARTESIAN_POINT('Ctrl Pts',(373.203682378979,-6.53445909343855,-2.18455734267345));
#33965=CARTESIAN_POINT('Ctrl Pts',(373.191512849654,-6.53335138689304,-2.19769211180579));
#33966=CARTESIAN_POINT('Ctrl Pts',(373.184637524374,-6.53273135560205,-2.2050433826243));
#33967=CARTESIAN_POINT('Ctrl Pts',(373.163266056152,-6.53082137009418,-2.2276807722289));
#33968=CARTESIAN_POINT('Ctrl Pts',(373.148654061155,-6.52953991727228,-2.24285740183799));
#33969=CARTESIAN_POINT('Ctrl Pts',(373.114125204356,-6.52656521624545,-2.27802374156552));
#33970=CARTESIAN_POINT('Ctrl Pts',(373.094092292398,-6.52487991779016,-2.29789758696194));
#33971=CARTESIAN_POINT('Ctrl Pts',(373.022272209683,-6.51896827323452,-2.36729968616246));
#33972=CARTESIAN_POINT('Ctrl Pts',(372.969094493663,-6.51482532170411,-2.41536375030839));
#33973=CARTESIAN_POINT('Ctrl Pts',(372.744273465411,-6.49803271466705,-2.60533483974566));
#33974=CARTESIAN_POINT('Ctrl Pts',(372.559753280602,-6.48585916314058,-2.73103995950967));
#33975=CARTESIAN_POINT('Ctrl Pts',(372.251943300907,-6.46593764364697,-2.89699630579767));
#33976=CARTESIAN_POINT('Ctrl Pts',(372.136691447572,-6.45856297045994,-2.95060454869883));
#33977=CARTESIAN_POINT('Ctrl Pts',(371.992290975987,-6.44925650623475,-3.00765941634025));
#33978=CARTESIAN_POINT('Ctrl Pts',(371.965861299857,-6.44755080829368,-3.01770215049889));
#33979=CARTESIAN_POINT('Ctrl Pts',(371.924021409797,-6.44484538739048,-3.03297352075642));
#33980=CARTESIAN_POINT('Ctrl Pts',(371.908697494484,-6.44385344139408,-3.03843554977043));
#33981=CARTESIAN_POINT('Ctrl Pts',(371.880167647274,-6.44200435787329,-3.04836186860532));
#33982=CARTESIAN_POINT('Ctrl Pts',(371.8669727836,-6.44114826531107,-3.05285696664257));
#33983=CARTESIAN_POINT('Ctrl Pts',(371.837679272839,-6.43924549464988,-3.06262475410036));
#33984=CARTESIAN_POINT('Ctrl Pts',(371.821567462975,-6.43819749130379,-3.06785637103739));
#33985=CARTESIAN_POINT('Ctrl Pts',(371.774673251665,-6.43514263972458,-3.08267558247427));
#33986=CARTESIAN_POINT('Ctrl Pts',(371.743787990991,-6.43312493735024,-3.09192835773758));
#33987=CARTESIAN_POINT('Ctrl Pts',(371.51372314424,-6.41804810885342,-3.1571071611854));
#33988=CARTESIAN_POINT('Ctrl Pts',(371.309744021941,-6.40437421990259,-3.19419157391678));
#33989=CARTESIAN_POINT('Ctrl Pts',(370.873228545825,-6.37484117695963,-3.23080057504636));
#33990=CARTESIAN_POINT('Ctrl Pts',(370.641381343263,-6.35899736323217,-3.22527138914597));
#33991=CARTESIAN_POINT('Ctrl Pts',(370.387670777281,-6.34259864488468,-3.19174431074535));
#33992=CARTESIAN_POINT('Ctrl Pts',(370.363266789622,-6.34103163207958,-3.18823404674786));
#33993=CARTESIAN_POINT('Ctrl Pts',(370.329358362898,-6.33887098415899,-3.18295881418284));
#33994=CARTESIAN_POINT('Ctrl Pts',(370.319818662773,-6.33826495491931,-3.18143072976608));
#33995=CARTESIAN_POINT('Ctrl Pts',(370.302431506568,-6.33716393930254,-3.17856537491825));
#33996=CARTESIAN_POINT('Ctrl Pts',(370.294581857678,-6.3366681920633,-3.17724188387632));
#33997=CARTESIAN_POINT('Ctrl Pts',(370.278372924292,-6.33564734401255,-3.17444717017625));
#33998=CARTESIAN_POINT('Ctrl Pts',(370.27001444868,-6.33512246817047,-3.17297199353753));
#33999=CARTESIAN_POINT('Ctrl Pts',(370.248297181179,-6.33376251190411,-3.16905061028242));
#34000=CARTESIAN_POINT('Ctrl Pts',(370.234947691061,-6.33293029178216,-3.16655292429836));
#34001=CARTESIAN_POINT('Ctrl Pts',(370.176713327614,-6.32931467659187,-3.15527582553062));
#34002=CARTESIAN_POINT('Ctrl Pts',(370.132000091599,-6.32657693748643,-3.14562545339615));
#34003=CARTESIAN_POINT('Ctrl Pts',(370.008410714701,-6.31907878876051,-3.11618450289966));
#34004=CARTESIAN_POINT('Ctrl Pts',(369.930052477949,-6.31440344224549,-3.09435523613195));
#34005=CARTESIAN_POINT('Ctrl Pts',(369.600246962528,-6.29474813856902,-2.98887636784676));
#34006=CARTESIAN_POINT('Ctrl Pts',(369.358818170017,-6.2803272324562,-2.87736290000783));
#34007=CARTESIAN_POINT('Ctrl Pts',(369.067385788044,-6.26038725858426,-2.69632593445081));
#34008=CARTESIAN_POINT('Ctrl Pts',(369.002540926176,-6.25577614474766,-2.65269943919194));
#34009=CARTESIAN_POINT('Ctrl Pts',(368.919455444492,-6.24959751185227,-2.59230098450764));
#34010=CARTESIAN_POINT('Ctrl Pts',(368.899728718044,-6.2481097057964,-2.57761270665809));
#34011=CARTESIAN_POINT('Ctrl Pts',(368.86800707355,-6.24568216215418,-2.5534238837455));
#34012=CARTESIAN_POINT('Ctrl Pts',(368.855908078481,-6.24474783205663,-2.54406099826553));
#34013=CARTESIAN_POINT('Ctrl Pts',(368.833235093359,-6.24298071598243,-2.52625581063233));
#34014=CARTESIAN_POINT('Ctrl Pts',(368.822646682586,-6.24214869153614,-2.51783234647173));
#34015=CARTESIAN_POINT('Ctrl Pts',(368.797981664877,-6.24019443576712,-2.49795552691375));
#34016=CARTESIAN_POINT('Ctrl Pts',(368.783948243745,-6.23907009968133,-2.4864495428932));
#34017=CARTESIAN_POINT('Ctrl Pts',(368.754838493488,-6.23671138649727,-2.4621684809128));
#34018=CARTESIAN_POINT('Ctrl Pts',(368.739781028224,-6.23547616548171,-2.44937206172184));
#34019=CARTESIAN_POINT('Ctrl Pts',(368.699984154187,-6.23217043294926,-2.4149158106224));
#34020=CARTESIAN_POINT('Ctrl Pts',(368.675457452492,-6.23009009851335,-2.3930149088394));
#34021=CARTESIAN_POINT('Ctrl Pts',(368.600871512289,-6.2236281338583,-2.32433407742402));
#34022=CARTESIAN_POINT('Ctrl Pts',(368.551968043607,-6.21919710828186,-2.27633251774844));
#34023=CARTESIAN_POINT('Ctrl Pts',(368.356101315751,-6.20062939238671,-2.07141732366066));
#34024=CARTESIAN_POINT('Ctrl Pts',(368.223500222658,-6.18599376763104,-1.9015626888273));
#34025=CARTESIAN_POINT('Ctrl Pts',(368.0344254805,-6.16211132973905,-1.60192033437473));
#34026=CARTESIAN_POINT('Ctrl Pts',(367.967760098142,-6.15281687364757,-1.47932464634205));
#34027=CARTESIAN_POINT('Ctrl Pts',(367.901454239857,-6.14275633088275,-1.33595376161416));
#34028=CARTESIAN_POINT('Ctrl Pts',(367.893815554852,-6.14158290300053,-1.31905560863843));
#34029=CARTESIAN_POINT('Ctrl Pts',(367.882411098926,-6.13980967031998,-1.29323540717272));
#34030=CARTESIAN_POINT('Ctrl Pts',(367.878539121885,-6.13920373995296,-1.28436108689566));
#34031=CARTESIAN_POINT('Ctrl Pts',(367.871611748158,-6.13811273588198,-1.26828674529169));
#34032=CARTESIAN_POINT('Ctrl Pts',(367.868542536894,-6.13762684725247,-1.26109298217696));
#34033=CARTESIAN_POINT('Ctrl Pts',(367.861796606737,-6.13655326646389,-1.24512070728884));
#34034=CARTESIAN_POINT('Ctrl Pts',(367.85813257332,-6.13596633891776,-1.23633705826225));
#34035=CARTESIAN_POINT('Ctrl Pts',(367.847526010034,-6.13425566946592,-1.21058993773158));
#34036=CARTESIAN_POINT('Ctrl Pts',(367.840689089049,-6.13313806371801,-1.19358299669216));
#34037=CARTESIAN_POINT('Ctrl Pts',(367.780222024197,-6.12310804971261,-1.03938175458849));
#34038=CARTESIAN_POINT('Ctrl Pts',(367.735904898476,-6.11468928018671,-0.898701273464923));
#34039=CARTESIAN_POINT('Ctrl Pts',(367.641820444849,-6.09208711059418,-0.508528810391087));
#34040=CARTESIAN_POINT('Ctrl Pts',(367.611683538068,-6.07815590120095,-0.255446393395135));
#34041=CARTESIAN_POINT('Ctrl Pts',(367.611568185609,-6.06328577097763,-0.00146369061351841));
#34042=CARTESIAN_POINT('Ctrl Pts',(367.611568184028,-6.06328556681864,-0.00146020356699756));
#34043=CARTESIAN_POINT('Ctrl Pts',(367.611539244412,-6.05954603902345,0.062411120851928));
#34044=CARTESIAN_POINT('Ctrl Pts',(367.613409087385,-6.05575672432227,0.126266582787961));
#34045=CARTESIAN_POINT('Ctrl Pts',(367.618182957693,-6.05087840916228,0.207089875612405));
#34046=CARTESIAN_POINT('Ctrl Pts',(367.619326856252,-6.04984414080902,0.224148957221984));
#34047=CARTESIAN_POINT('Ctrl Pts',(367.621615547105,-6.04798666905739,0.254643387303945));
#34048=CARTESIAN_POINT('Ctrl Pts',(367.622709026922,-6.04716507779549,0.268082264691209));
#34049=CARTESIAN_POINT('Ctrl Pts',(367.625085669961,-6.04550183866907,0.295185911476749));
#34050=CARTESIAN_POINT('Ctrl Pts',(367.626371856455,-6.04466011273546,0.308850127116892));
#34051=CARTESIAN_POINT('Ctrl Pts',(367.629321910275,-6.04284619567293,0.338181597033085));
#34052=CARTESIAN_POINT('Ctrl Pts',(367.631013460942,-6.04187315438594,0.353845648839862));
#34053=CARTESIAN_POINT('Ctrl Pts',(367.635878782547,-6.03924247684461,0.396001176480478));
#34054=CARTESIAN_POINT('Ctrl Pts',(367.639266736747,-6.03757815017155,0.422466229345509));
#34055=CARTESIAN_POINT('Ctrl Pts',(367.6552555992,-6.03037271326554,0.5361384512225));
#34056=CARTESIAN_POINT('Ctrl Pts',(367.671100442776,-6.02473081457682,0.622843867273276));
#34057=CARTESIAN_POINT('Ctrl Pts',(367.749485152616,-6.00150712561223,0.970522076588505));
#34058=CARTESIAN_POINT('Ctrl Pts',(367.840948055225,-5.98308396179967,1.22385001830504));
#34059=CARTESIAN_POINT('Ctrl Pts',(368.009489108193,-5.95826542715404,1.55469658778462));
#34060=CARTESIAN_POINT('Ctrl Pts',(368.06065307993,-5.95147878890013,1.64424055670162));
#34061=CARTESIAN_POINT('Ctrl Pts',(368.125272828011,-5.94383115329439,1.745705855968));
#34062=CARTESIAN_POINT('Ctrl Pts',(368.134636209348,-5.94274345555182,1.76015139584845));
#34063=CARTESIAN_POINT('Ctrl Pts',(368.149226465424,-5.94108050121446,1.78227045436131));
#34064=CARTESIAN_POINT('Ctrl Pts',(368.154371337295,-5.9405000611648,1.78999732127292));
#34065=CARTESIAN_POINT('Ctrl Pts',(368.163918816166,-5.93943399659535,1.8042028424957));
#34066=CARTESIAN_POINT('Ctrl Pts',(368.168311645713,-5.9389477620736,1.81068766430725));
#34067=CARTESIAN_POINT('Ctrl Pts',(368.178341994965,-5.93784710102366,1.82537911859818));
#34068=CARTESIAN_POINT('Ctrl Pts',(368.183993925263,-5.93723365688225,1.83357567864285));
#34069=CARTESIAN_POINT('Ctrl Pts',(368.198797117646,-5.93564406068218,1.8548321522468));
#34070=CARTESIAN_POINT('Ctrl Pts',(368.208007612657,-5.93467176730296,1.86785074471336));
#34071=CARTESIAN_POINT('Ctrl Pts',(368.272340714533,-5.9279910604388,1.95736577711319));
#34072=CARTESIAN_POINT('Ctrl Pts',(368.330705976247,-5.92248278159927,2.03148681455096));
#34073=CARTESIAN_POINT('Ctrl Pts',(368.574619507245,-5.90106205422521,2.3147344375505));
#34074=CARTESIAN_POINT('Ctrl Pts',(368.783768902299,-5.88594776528905,2.50189825819353));
#34075=CARTESIAN_POINT('Ctrl Pts',(369.062872364133,-5.86637546771942,2.69286846076214));
#34076=CARTESIAN_POINT('Ctrl Pts',(369.112185755965,-5.86294221292882,2.72466881132525));
#34077=CARTESIAN_POINT('Ctrl Pts',(369.187565934845,-5.85771163265759,2.77041450901184));
#34078=CARTESIAN_POINT('Ctrl Pts',(369.213002706554,-5.85594954045975,2.78537709184092));
#34079=CARTESIAN_POINT('Ctrl Pts',(369.26010913922,-5.8526893287266,2.81222244178752));
#34080=CARTESIAN_POINT('Ctrl Pts',(369.28171703119,-5.85119500215675,2.82420940670251));
#34081=CARTESIAN_POINT('Ctrl Pts',(369.313473676777,-5.84899956767055,2.84135179821847));
#34082=CARTESIAN_POINT('Ctrl Pts',(369.323515630691,-5.84830544561255,2.84670400454189));
#34083=CARTESIAN_POINT('Ctrl Pts',(369.345681470656,-5.84677341666518,2.85836773424642));
#34084=CARTESIAN_POINT('Ctrl Pts',(369.35781753995,-5.84593469208649,2.86465551148483));
#34085=CARTESIAN_POINT('Ctrl Pts',(369.384382160909,-5.84409880537337,2.87820516326082));
#34086=CARTESIAN_POINT('Ctrl Pts',(369.398825987761,-5.8431005863361,2.88543611308199));
#34087=CARTESIAN_POINT('Ctrl Pts',(369.438242490569,-5.84037617479904,2.90479981544941));
#34088=CARTESIAN_POINT('Ctrl Pts',(369.463318124988,-5.83864262613811,2.91671871350854));
#34089=CARTESIAN_POINT('Ctrl Pts',(369.595130666028,-5.82952594022202,2.97729623363457));
#34090=CARTESIAN_POINT('Ctrl Pts',(369.704300119261,-5.82195659181683,3.02041920593439));
#34091=CARTESIAN_POINT('Ctrl Pts',(370.033243110302,-5.7991092016066,3.13002242793859));
#34092=CARTESIAN_POINT('Ctrl Pts',(370.258035125555,-5.78339689622959,3.17909470302125));
#34093=CARTESIAN_POINT('Ctrl Pts',(370.559930554501,-5.76306051872167,3.2119067123616));
#34094=CARTESIAN_POINT('Ctrl Pts',(370.634022713615,-5.75813544528334,3.21737724870512));
#34095=CARTESIAN_POINT('Ctrl Pts',(370.737116578394,-5.75142769137663,3.221413431359));
#34096=CARTESIAN_POINT('Ctrl Pts',(370.766006159496,-5.74956385637366,3.2221555235457));
#34097=CARTESIAN_POINT('Ctrl Pts',(370.816360771322,-5.74634716202605,3.22277141875104));
#34098=CARTESIAN_POINT('Ctrl Pts',(370.837821468653,-5.74498635293178,3.2228195507165));
#34099=CARTESIAN_POINT('Ctrl Pts',(370.869422040718,-5.74299903829848,3.22257476113986));
#34100=CARTESIAN_POINT('Ctrl Pts',(370.879562113329,-5.74236383949316,3.22244834847615));
#34101=CARTESIAN_POINT('Ctrl Pts',(370.897547290067,-5.7412418329857,3.22213922327345));
#34102=CARTESIAN_POINT('Ctrl Pts',(370.905392506158,-5.74075398162457,3.22197571903854));
#34103=CARTESIAN_POINT('Ctrl Pts',(370.922382310282,-5.73970091844178,3.22155954393622));
#34104=CARTESIAN_POINT('Ctrl Pts',(370.931526448042,-5.73913628038372,3.22129659262414));
#34105=CARTESIAN_POINT('Ctrl Pts',(370.956798681234,-5.7375813509795,3.22046214761416));
#34106=CARTESIAN_POINT('Ctrl Pts',(370.972924044491,-5.73659550455844,3.21980843311473));
#34107=CARTESIAN_POINT('Ctrl Pts',(371.059423094149,-5.73133784858712,3.21565076238878));
#34108=CARTESIAN_POINT('Ctrl Pts',(371.129677865334,-5.72717612557223,3.20996047387969));
#34109=CARTESIAN_POINT('Ctrl Pts',(371.235447617676,-5.72099990598649,3.19789108264644));
#34110=CARTESIAN_POINT('Ctrl Pts',(371.27113049078,-5.718931765215,3.19321269628482));
#34111=CARTESIAN_POINT('Ctrl Pts',(371.377983281881,-5.7127661268078,3.17737851210452));
#34112=CARTESIAN_POINT('Ctrl Pts',(371.44886629653,-5.70871242291332,3.16443314720259));
#34113=CARTESIAN_POINT('Ctrl Pts',(371.702802991032,-5.69414850917993,3.10920145387516));
#34114=CARTESIAN_POINT('Ctrl Pts',(371.882496989033,-5.68374071244819,3.05331242588356));
#34115=CARTESIAN_POINT('Ctrl Pts',(372.115510217665,-5.66921920274728,2.95783004317388));
#34116=CARTESIAN_POINT('Ctrl Pts',(372.173984236574,-5.66548598465645,2.93180928669995));
#34117=CARTESIAN_POINT('Ctrl Pts',(372.257877872205,-5.65997371746155,2.89144290609159));
#34118=CARTESIAN_POINT('Ctrl Pts',(372.283939590603,-5.65823885468281,2.87846519053259));
#34119=CARTESIAN_POINT('Ctrl Pts',(372.30982061461,-5.65649214416028,2.86513684902516));
#34120=CARTESIAN_POINT('Ctrl Pts',(372.309820461314,-5.4072724248197,2.86513692797033));
#34121=CARTESIAN_POINT('Ctrl Pts',(372.186239463848,-5.4150460915779,2.92877929085081));
#34122=CARTESIAN_POINT('Ctrl Pts',(372.058627177371,-5.42284083113338,2.98438186264552));
#34123=CARTESIAN_POINT('Ctrl Pts',(371.867273855704,-5.43456887136001,3.05340065678803));
#34124=CARTESIAN_POINT('Ctrl Pts',(371.806139567173,-5.43832013238138,3.07340454444319));
#34125=CARTESIAN_POINT('Ctrl Pts',(371.700348157215,-5.44484885616589,3.10454870238293));
#34126=CARTESIAN_POINT('Ctrl Pts',(371.655974979956,-5.44759816664708,3.11658633448786));
#34127=CARTESIAN_POINT('Ctrl Pts',(371.592429936567,-5.45155752707934,3.1323735635436));
#34128=CARTESIAN_POINT('Ctrl Pts',(371.573456789038,-5.45274247695973,3.13690479297624));
#34129=CARTESIAN_POINT('Ctrl Pts',(371.540541678734,-5.4548034435136,3.14445049293052));
#34130=CARTESIAN_POINT('Ctrl Pts',(371.526618541187,-5.45567686300672,3.14754519289953));
#34131=CARTESIAN_POINT('Ctrl Pts',(371.498073849647,-5.45747103982129,3.15369127088984));
#34132=CARTESIAN_POINT('Ctrl Pts',(371.483450725912,-5.45839206219915,3.15673362140282));
#34133=CARTESIAN_POINT('Ctrl Pts',(371.446367399543,-5.46073272770172,3.1641802672731));
#34134=CARTESIAN_POINT('Ctrl Pts',(371.423880737914,-5.46215670891125,3.16844709164471));
#34135=CARTESIAN_POINT('Ctrl Pts',(371.338162263589,-5.46760354590136,3.18376801036029));
#34136=CARTESIAN_POINT('Ctrl Pts',(371.274654148141,-5.47167797227647,3.19317098493991));
#34137=CARTESIAN_POINT('Ctrl Pts',(370.877256354232,-5.4974291217939,3.23992909185907));
#34138=CARTESIAN_POINT('Ctrl Pts',(370.539607690508,-5.52072828445761,3.22677088942471));
#34139=CARTESIAN_POINT('Ctrl Pts',(370.164178289157,-5.5459881856634,3.15265353728662));
#34140=CARTESIAN_POINT('Ctrl Pts',(370.118428010833,-5.54904946714131,3.14258071344138));
#34141=CARTESIAN_POINT('Ctrl Pts',(370.042827808043,-5.55406277923187,3.12419903259107));
#34142=CARTESIAN_POINT('Ctrl Pts',(370.01284989712,-5.55603872070489,3.11645097003691));
#34143=CARTESIAN_POINT('Ctrl Pts',(369.971658253245,-5.55873284699157,3.10516890787206));
#34144=CARTESIAN_POINT('Ctrl Pts',(369.960346300446,-5.55947050632391,3.10200407266341));
#34145=CARTESIAN_POINT('Ctrl Pts',(369.941263824579,-5.56071087436503,3.0965525452388));
#34146=CARTESIAN_POINT('Ctrl Pts',(369.933484222796,-5.56121541965395,3.09429829507254));
#34147=CARTESIAN_POINT('Ctrl Pts',(369.918603341941,-5.56217824264502,3.08992546981398));
#34148=CARTESIAN_POINT('Ctrl Pts',(369.911500784834,-5.56263680528618,3.08781170670755));
#34149=CARTESIAN_POINT('Ctrl Pts',(369.894511558581,-5.56373145531434,3.082691757458));
#34150=CARTESIAN_POINT('Ctrl Pts',(369.884631861335,-5.56436621458216,3.07966245983421));
#34151=CARTESIAN_POINT('Ctrl Pts',(369.849014855198,-5.56664859678286,3.06855393192067));
#34152=CARTESIAN_POINT('Ctrl Pts',(369.823363857998,-5.5682810617331,3.06019890833389));
#34153=CARTESIAN_POINT('Ctrl Pts',(369.634697472273,-5.58022519345597,2.99611537870492));
#34154=CARTESIAN_POINT('Ctrl Pts',(369.476259274897,-5.589916022736,2.92771036007857));
#34155=CARTESIAN_POINT('Ctrl Pts',(369.298807585165,-5.60116034997856,2.83357394148913));
#34156=CARTESIAN_POINT('Ctrl Pts',(369.273759454107,-5.60275682758361,2.81985647756629));
#34157=CARTESIAN_POINT('Ctrl Pts',(369.109318899195,-5.61331755039553,2.72693938952893));
#34158=CARTESIAN_POINT('Ctrl Pts',(368.975826813608,-5.62228812348054,2.63776916406592));
#34159=CARTESIAN_POINT('Ctrl Pts',(368.804413680532,-5.63489234161843,2.50377435913618));
#34160=CARTESIAN_POINT('Ctrl Pts',(368.760246525718,-5.63824624820379,2.46731120468146));
#34161=CARTESIAN_POINT('Ctrl Pts',(368.685354763773,-5.6441419642904,2.402050272421));
#34162=CARTESIAN_POINT('Ctrl Pts',(368.654179139217,-5.64666259071267,2.37379081057311));
#34163=CARTESIAN_POINT('Ctrl Pts',(368.609861956208,-5.65034864833123,2.33200949541366));
#34164=CARTESIAN_POINT('Ctrl Pts',(368.596270949407,-5.65149356851119,2.31896924461198));
#34165=CARTESIAN_POINT('Ctrl Pts',(368.572669405879,-5.6535078311931,2.29592337793145));
#34166=CARTESIAN_POINT('Ctrl Pts',(368.56260893164,-5.65437490505648,2.28596947097292));
#34167=CARTESIAN_POINT('Ctrl Pts',(368.543197891067,-5.65606460104076,2.26650935899122));
#34168=CARTESIAN_POINT('Ctrl Pts',(368.533840104199,-5.65688687773175,2.25701073836825));
#34169=CARTESIAN_POINT('Ctrl Pts',(368.508979071966,-5.65909232983623,2.23146031118641));
#34170=CARTESIAN_POINT('Ctrl Pts',(368.493583372466,-5.66048013314703,2.21530531042468));
#34171=CARTESIAN_POINT('Ctrl Pts',(368.437323955151,-5.66563470700402,2.1550299740053));
#34172=CARTESIAN_POINT('Ctrl Pts',(368.397531829565,-5.66944621620575,2.10993057575255));
#34173=CARTESIAN_POINT('Ctrl Pts',(368.175314089758,-5.69172948204876,1.84339902400083));
#34174=CARTESIAN_POINT('Ctrl Pts',(368.021868594206,-5.71134792605097,1.59952964443848));
#34175=CARTESIAN_POINT('Ctrl Pts',(367.857022921374,-5.73799640278554,1.23852645710416));
#34176=CARTESIAN_POINT('Ctrl Pts',(367.816457563919,-5.7452964325378,1.13611480142608));
#34177=CARTESIAN_POINT('Ctrl Pts',(367.773403710924,-5.75391104960634,1.0087203098643));
#34178=CARTESIAN_POINT('Ctrl Pts',(367.765859465314,-5.75546052358208,0.985532980055936));
#34179=CARTESIAN_POINT('Ctrl Pts',(367.755389394627,-5.75766815478191,0.952066811207538));
#34180=CARTESIAN_POINT('Ctrl Pts',(367.752250593291,-5.75833789029135,0.941856188082666));
#34181=CARTESIAN_POINT('Ctrl Pts',(367.746874362096,-5.75949880478419,0.924052437148957));
#34182=CARTESIAN_POINT('Ctrl Pts',(367.74461405419,-5.75999129187723,0.916466397142653));
#34183=CARTESIAN_POINT('Ctrl Pts',(367.739888503829,-5.7610302960024,0.900390313591055));
#34184=CARTESIAN_POINT('Ctrl Pts',(367.737430230393,-5.76157641215277,0.891898408533948));
#34185=CARTESIAN_POINT('Ctrl Pts',(367.730852388209,-5.76305344236891,0.868820683870069));
#34186=CARTESIAN_POINT('Ctrl Pts',(367.726800659244,-5.7639805253179,0.854215536666795));
#34187=CARTESIAN_POINT('Ctrl Pts',(367.708351195327,-5.76828712690331,0.785842375956361));
#34188=CARTESIAN_POINT('Ctrl Pts',(367.695244059027,-5.77159891140568,0.73173241766537));
#34189=CARTESIAN_POINT('Ctrl Pts',(367.674240686848,-5.7774511503991,0.634026490146115));
#34190=CARTESIAN_POINT('Ctrl Pts',(367.665829375583,-5.78001001950418,0.590557656326112));
#34191=CARTESIAN_POINT('Ctrl Pts',(367.627365642879,-5.79299171439672,0.367199311458932));
#34192=CARTESIAN_POINT('Ctrl Pts',(367.611725866657,-5.80303882109623,0.185161274399618));
#34193=CARTESIAN_POINT('Ctrl Pts',(367.611419465318,-5.82308882301199,-0.171195433130785));
#34194=CARTESIAN_POINT('Ctrl Pts',(367.625355720298,-5.83304143910263,-0.344866322988589));
#34195=CARTESIAN_POINT('Ctrl Pts',(367.657623113375,-5.8450906358744,-0.543578693342448));
#34196=CARTESIAN_POINT('Ctrl Pts',(367.662355922668,-5.84673972965104,-0.570547725989014));
#34197=CARTESIAN_POINT('Ctrl Pts',(367.670678608738,-5.84946144372453,-0.614663360760454));
#34198=CARTESIAN_POINT('Ctrl Pts',(367.674065726059,-5.85052763272903,-0.631847125681856));
#34199=CARTESIAN_POINT('Ctrl Pts',(367.680409424716,-5.85245333840517,-0.662702666909461));
#34200=CARTESIAN_POINT('Ctrl Pts',(367.683315284648,-5.85331121677272,-0.676384508407327));
#34201=CARTESIAN_POINT('Ctrl Pts',(367.689706079449,-5.85514800174256,-0.705539445109354));
#34202=CARTESIAN_POINT('Ctrl Pts',(367.693216349764,-5.85612770033602,-0.721006551264223));
#34203=CARTESIAN_POINT('Ctrl Pts',(367.703040149695,-5.85879322649739,-0.762858786501047));
#34204=CARTESIAN_POINT('Ctrl Pts',(367.709572806134,-5.86048604505668,-0.789190663364817));
#34205=CARTESIAN_POINT('Ctrl Pts',(367.746735799547,-5.86970890343693,-0.931286112576606));
#34206=CARTESIAN_POINT('Ctrl Pts',(367.7834643043,-5.87743433897533,-1.04534374219022));
#34207=CARTESIAN_POINT('Ctrl Pts',(367.883206651629,-5.89574451353938,-1.30462668954683));
#34208=CARTESIAN_POINT('Ctrl Pts',(367.95073986068,-5.90643416708659,-1.44778419797886));
#34209=CARTESIAN_POINT('Ctrl Pts',(368.109553035553,-5.92827086630111,-1.72885020926833));
#34210=CARTESIAN_POINT('Ctrl Pts',(368.201499436149,-5.93938519581037,-1.86588956408876));
#34211=CARTESIAN_POINT('Ctrl Pts',(368.320277867226,-5.95171211272316,-2.01654457803009));
#34212=CARTESIAN_POINT('Ctrl Pts',(368.337290681605,-5.95343503684842,-2.03757318934979));
#34213=CARTESIAN_POINT('Ctrl Pts',(368.361173006976,-5.95579265964947,-2.06634438335263));
#34214=CARTESIAN_POINT('Ctrl Pts',(368.367817541967,-5.9564422433307,-2.07427114007633));
#34215=CARTESIAN_POINT('Ctrl Pts',(368.379289538424,-5.95755271877109,-2.08782386376487));
#34216=CARTESIAN_POINT('Ctrl Pts',(368.384098412003,-5.9580149243778,-2.0934653579804));
#34217=CARTESIAN_POINT('Ctrl Pts',(368.394200783242,-5.95897897110095,-2.10523438424517));
#34218=CARTESIAN_POINT('Ctrl Pts',(368.399497966312,-5.95948051531581,-2.11135862607016));
#34219=CARTESIAN_POINT('Ctrl Pts',(368.412528065296,-5.96070475901002,-2.12630888608184));
#34220=CARTESIAN_POINT('Ctrl Pts',(368.420286307752,-5.96142560826559,-2.13511286898364));
#34221=CARTESIAN_POINT('Ctrl Pts',(368.448635518875,-5.96403133900457,-2.16693123783337));
#34222=CARTESIAN_POINT('Ctrl Pts',(368.469509638147,-5.96589634637568,-2.1896925481519));
#34223=CARTESIAN_POINT('Ctrl Pts',(368.522747754332,-5.97053092370751,-2.24609436269053));
#34224=CARTESIAN_POINT('Ctrl Pts',(368.555522180627,-5.97327481306805,-2.27933914119107));
#34225=CARTESIAN_POINT('Ctrl Pts',(368.826968421333,-5.99525100898732,-2.54297112291339));
#34226=CARTESIAN_POINT('Ctrl Pts',(369.099185866976,-6.01293529023208,-2.73596591989263));
#34227=CARTESIAN_POINT('Ctrl Pts',(369.456610086862,-6.03627228767671,-2.91420869580126));
#34228=CARTESIAN_POINT('Ctrl Pts',(369.518060963434,-6.04027863151131,-2.94247478348002));
#34229=CARTESIAN_POINT('Ctrl Pts',(369.601856275252,-6.04575669451562,-2.97786852213719));
#34230=CARTESIAN_POINT('Ctrl Pts',(369.623457722889,-6.04717012579401,-2.98671729113938));
#34231=CARTESIAN_POINT('Ctrl Pts',(369.659126259294,-6.0495068977796,-3.0008779227979));
#34232=CARTESIAN_POINT('Ctrl Pts',(369.673138009274,-6.05042558363183,-3.00632748514916));
#34233=CARTESIAN_POINT('Ctrl Pts',(369.700469797614,-6.05221924207341,-3.0167380020541));
#34234=CARTESIAN_POINT('Ctrl Pts',(369.713785553786,-6.05309384432302,-3.02170927487675));
#34235=CARTESIAN_POINT('Ctrl Pts',(369.745179601369,-6.05515782555169,-3.0331938068646));
#34236=CARTESIAN_POINT('Ctrl Pts',(369.763283969941,-6.0563496105485,-3.03963372742106));
#34237=CARTESIAN_POINT('Ctrl Pts',(369.823270520261,-6.0603040423247,-3.06036914382988));
#34238=CARTESIAN_POINT('Ctrl Pts',(369.86538808978,-6.06308956684437,-3.07396337112632));
#34239=CARTESIAN_POINT('Ctrl Pts',(369.966357865119,-6.06979182859552,-3.10427201982976));
#34240=CARTESIAN_POINT('Ctrl Pts',(370.025430656397,-6.0737326709091,-3.12018589783273));
#34241=CARTESIAN_POINT('Ctrl Pts',(370.26034608079,-6.08947921254514,-3.17635142081367));
#34242=CARTESIAN_POINT('Ctrl Pts',(370.438969159845,-6.10164017966511,-3.20348849598836));
#34243=CARTESIAN_POINT('Ctrl Pts',(370.792282445117,-6.12559644672119,-3.22715754906267));
#34244=CARTESIAN_POINT('Ctrl Pts',(370.96633357674,-6.13734497591492,-3.22473190618839));
#34245=CARTESIAN_POINT('Ctrl Pts',(371.166197746252,-6.1502440447933,-3.2057293140122));
#34246=CARTESIAN_POINT('Ctrl Pts',(371.193010081644,-6.15196170685305,-3.20284009807007));
#34247=CARTESIAN_POINT('Ctrl Pts',(371.230041939978,-6.15431346637567,-3.19837877094988));
#34248=CARTESIAN_POINT('Ctrl Pts',(371.24029405509,-6.15496235218232,-3.19709362478578));
#34249=CARTESIAN_POINT('Ctrl Pts',(371.257887873061,-6.15607194878778,-3.19480217044204));
#34250=CARTESIAN_POINT('Ctrl Pts',(371.265232536767,-6.15653396892638,-3.19381981459431));
#34251=CARTESIAN_POINT('Ctrl Pts',(371.280598459769,-6.15749798822373,-3.19171063704249));
#34252=CARTESIAN_POINT('Ctrl Pts',(371.288618947901,-6.15799968843602,-3.19057889536439));
#34253=CARTESIAN_POINT('Ctrl Pts',(371.308261322736,-6.15922490370889,-3.1877316634573));
#34254=CARTESIAN_POINT('Ctrl Pts',(371.319878403891,-6.15994656165555,-3.18598282042769));
#34255=CARTESIAN_POINT('Ctrl Pts',(371.36208627872,-6.16255856943343,-3.17939259365022));
#34256=CARTESIAN_POINT('Ctrl Pts',(371.392617512743,-6.1644289195043,-3.1741736604391));
#34257=CARTESIAN_POINT('Ctrl Pts',(371.469142194923,-6.16907954763586,-3.15995435886714));
#34258=CARTESIAN_POINT('Ctrl Pts',(371.515024481363,-6.17183391679983,-3.15038924827447));
#34259=CARTESIAN_POINT('Ctrl Pts',(371.888485220933,-6.19409262858897,-3.06399299279539));
#34260=CARTESIAN_POINT('Ctrl Pts',(372.202398297669,-6.21201358385623,-2.93729768488005));
#34261=CARTESIAN_POINT('Ctrl Pts',(372.545687215412,-6.23544765087213,-2.73155462476746));
#34262=CARTESIAN_POINT('Ctrl Pts',(372.599343085592,-6.23922719549706,-2.6971950022383));
#34263=CARTESIAN_POINT('Ctrl Pts',(372.670787501203,-6.24444021101523,-2.64839905596115));
#34264=CARTESIAN_POINT('Ctrl Pts',(372.689494318392,-6.24582251914817,-2.63532893005722));
#34265=CARTESIAN_POINT('Ctrl Pts',(372.718987452923,-6.24803038246378,-2.61425294044089));
#34266=CARTESIAN_POINT('Ctrl Pts',(372.729865463735,-6.24885097723792,-2.60637625533105));
#34267=CARTESIAN_POINT('Ctrl Pts',(372.75206730125,-6.25053887106962,-2.59008756639953));
#34268=CARTESIAN_POINT('Ctrl Pts',(372.763385752716,-6.25140642281705,-2.58166875801697));
#34269=CARTESIAN_POINT('Ctrl Pts',(372.789438071178,-6.25341993850836,-2.56202373191591));
#34270=CARTESIAN_POINT('Ctrl Pts',(372.804131036853,-6.2545679739355,-2.55074433610989));
#34271=CARTESIAN_POINT('Ctrl Pts',(372.850513409426,-6.25823240996628,-2.51449807625842));
#34272=CARTESIAN_POINT('Ctrl Pts',(372.881830638747,-6.26076731335264,-2.48906332831767));
#34273=CARTESIAN_POINT('Ctrl Pts',(373.041221218716,-6.27399261236492,-2.35456806503931));
#34274=CARTESIAN_POINT('Ctrl Pts',(373.161072123743,-6.28506324721286,-2.23620506278547));
#34275=CARTESIAN_POINT('Ctrl Pts',(373.327844290165,-6.30217209919381,-2.04351532255935));
#34276=CARTESIAN_POINT('Ctrl Pts',(373.381894558315,-6.30803808864141,-1.97572298571586));
#34277=CARTESIAN_POINT('Ctrl Pts',(373.531389509746,-6.32513809661236,-1.77186936324884));
#34278=CARTESIAN_POINT('Ctrl Pts',(373.619137203418,-6.3363479292754,-1.6304932444753));
#34279=CARTESIAN_POINT('Ctrl Pts',(373.708012340677,-6.34875729366153,-1.4590152444706));
#34280=CARTESIAN_POINT('Ctrl Pts',(373.720126612015,-6.35047590745691,-1.43490536590241));
#34281=CARTESIAN_POINT('Ctrl Pts',(373.736460513246,-6.35282872848166,-1.40135375167505));
#34282=CARTESIAN_POINT('Ctrl Pts',(373.740939263383,-6.35347774150518,-1.39204035188978));
#34283=CARTESIAN_POINT('Ctrl Pts',(373.748552639291,-6.35458749829496,-1.37601166034474));
#34284=CARTESIAN_POINT('Ctrl Pts',(373.751709011472,-6.35504955222302,-1.36930687215259));
#34285=CARTESIAN_POINT('Ctrl Pts',(373.758266719398,-6.35601357640553,-1.35525133853584));
#34286=CARTESIAN_POINT('Ctrl Pts',(373.761663509263,-6.35651524808664,-1.34789857721087));
#34287=CARTESIAN_POINT('Ctrl Pts',(373.769918111233,-6.35774028581146,-1.32985211139402));
#34288=CARTESIAN_POINT('Ctrl Pts',(373.774745312679,-6.35846179600048,-1.31914437367508));
#34289=CARTESIAN_POINT('Ctrl Pts',(373.792081288789,-6.36107265594432,-1.28012156141589));
#34290=CARTESIAN_POINT('Ctrl Pts',(373.804240929777,-6.36294202894683,-1.25165204143015));
#34291=CARTESIAN_POINT('Ctrl Pts',(373.83375947724,-6.36758972050476,-1.17968651364065));
#34292=CARTESIAN_POINT('Ctrl Pts',(373.850584497862,-6.37034217201583,-1.13597811962276));
#34293=CARTESIAN_POINT('Ctrl Pts',(373.980149387566,-6.39254822546715,-0.77619044425526));
#34294=CARTESIAN_POINT('Ctrl Pts',(374.043845046602,-6.41042504550552,-0.444637494304166));
#34295=CARTESIAN_POINT('Ctrl Pts',(374.057400341852,-6.43384043187916,-0.0448069411441706));
#34296=CARTESIAN_POINT('Ctrl Pts',(374.057651872717,-6.4376618020501,0.0196303817915023));
#34297=CARTESIAN_POINT('Ctrl Pts',(374.055374571373,-6.44292389101207,0.106941743267279));
#34298=CARTESIAN_POINT('Ctrl Pts',(374.05453253706,-6.44431217079368,0.12984708855978));
#34299=CARTESIAN_POINT('Ctrl Pts',(374.05273803169,-6.44661817461632,0.16766758839743));
#34300=CARTESIAN_POINT('Ctrl Pts',(374.051925999098,-6.44753148784421,0.182588808939438));
#34301=CARTESIAN_POINT('Ctrl Pts',(374.050136373031,-6.44932268809116,0.211735999864728));
#34302=CARTESIAN_POINT('Ctrl Pts',(374.04916807607,-6.45020026335615,0.225962209781886));
#34303=CARTESIAN_POINT('Ctrl Pts',(374.046653275178,-6.45228409406142,0.259611933047504));
#34304=CARTESIAN_POINT('Ctrl Pts',(374.045024976747,-6.45349288755933,0.279028599144768));
#34305=CARTESIAN_POINT('Ctrl Pts',(374.03897566626,-6.45756436300435,0.344074730035997));
#34306=CARTESIAN_POINT('Ctrl Pts',(374.033757322504,-6.46045182619141,0.389622706998321));
#34307=CARTESIAN_POINT('Ctrl Pts',(374.018920380266,-6.46744655095895,0.498527321177381));
#34308=CARTESIAN_POINT('Ctrl Pts',(374.008380493129,-6.4715808129513,0.561736782739229));
#34309=CARTESIAN_POINT('Ctrl Pts',(373.959481311576,-6.48806132015112,0.809263486138512));
#34310=CARTESIAN_POINT('Ctrl Pts',(373.906890783748,-6.50078891824815,0.99037160556896));
#34311=CARTESIAN_POINT('Ctrl Pts',(373.810588761087,-6.51879287909948,1.23855287275506));
#34312=CARTESIAN_POINT('Ctrl Pts',(373.779740210269,-6.52405819203512,1.31022499802935));
#34313=CARTESIAN_POINT('Ctrl Pts',(373.736044100385,-6.53086626734648,1.40238287158192));
#34314=CARTESIAN_POINT('Ctrl Pts',(373.725525664752,-6.53246163041849,1.42394184020765));
#34315=CARTESIAN_POINT('Ctrl Pts',(373.680967156958,-6.53903880636466,1.51274089347325));
#34316=CARTESIAN_POINT('Ctrl Pts',(373.644811590333,-6.54395395856,1.57889966590804));
#34317=CARTESIAN_POINT('Ctrl Pts',(373.597970883461,-6.54978841168879,1.65789337363744));
#34318=CARTESIAN_POINT('Ctrl Pts',(373.589466804292,-6.55082802564608,1.67198767757387));
#34319=CARTESIAN_POINT('Ctrl Pts',(373.576028756203,-6.55243978822487,1.6938783861857));
#34320=CARTESIAN_POINT('Ctrl Pts',(373.571168804601,-6.55301652606224,1.70171958255));
#34321=CARTESIAN_POINT('Ctrl Pts',(373.562113860181,-6.5540796010804,1.71618997982436));
#34322=CARTESIAN_POINT('Ctrl Pts',(373.557928348137,-6.55456651500292,1.72282470855387));
#34323=CARTESIAN_POINT('Ctrl Pts',(373.548325259104,-6.55567358391706,1.73792473023129));
#34324=CARTESIAN_POINT('Ctrl Pts',(373.542892284489,-6.55629271271324,1.74638000554083));
#34325=CARTESIAN_POINT('Ctrl Pts',(373.526003763162,-6.55819568423188,1.77239501449796));
#34326=CARTESIAN_POINT('Ctrl Pts',(373.514416093333,-6.55947112100088,1.78986887822688));
#34327=CARTESIAN_POINT('Ctrl Pts',(373.486935469234,-6.56242931638564,1.83044351798534));
#34328=CARTESIAN_POINT('Ctrl Pts',(373.470909733037,-6.56410425008228,1.85345273945323));
#34329=CARTESIAN_POINT('Ctrl Pts',(373.413273615909,-6.56996536372484,1.93394413587852));
#34330=CARTESIAN_POINT('Ctrl Pts',(373.37006518626,-6.57406970619767,1.99026115369087));
#34331=CARTESIAN_POINT('Ctrl Pts',(373.185798105848,-6.59064283709314,2.21467769875871));
#34332=CARTESIAN_POINT('Ctrl Pts',(373.029612304558,-6.60264404547919,2.36958764979766));
#34333=CARTESIAN_POINT('Ctrl Pts',(372.757039786174,-6.62257607109155,2.58967091665331));
#34334=CARTESIAN_POINT('Ctrl Pts',(372.650280601474,-6.63016767624629,2.66561974775489));
#34335=CARTESIAN_POINT('Ctrl Pts',(372.515030912718,-6.63971901318882,2.74993323761919));
#34336=CARTESIAN_POINT('Ctrl Pts',(372.49065644522,-6.64143753371583,2.76468290942012));
#34337=CARTESIAN_POINT('Ctrl Pts',(372.452012924334,-6.64415928925798,2.78737272520168));
#34338=CARTESIAN_POINT('Ctrl Pts',(372.437873245029,-6.64515459617277,2.79553110202655));
#34339=CARTESIAN_POINT('Ctrl Pts',(372.411654742565,-6.64699936070706,2.81039440977952));
#34340=CARTESIAN_POINT('Ctrl Pts',(372.399593562393,-6.64784769649852,2.81712980635673));
#34341=CARTESIAN_POINT('Ctrl Pts',(372.372732512545,-6.64973651083064,2.83190422745332));
#34342=CARTESIAN_POINT('Ctrl Pts',(372.357912255929,-6.65077831752186,2.83990515621556));
#34343=CARTESIAN_POINT('Ctrl Pts',(372.331993764463,-6.65259994732182,2.85363634972696));
#34344=CARTESIAN_POINT('Ctrl Pts',(372.320923718942,-6.65337787613019,2.85941891583469));
#34345=CARTESIAN_POINT('Ctrl Pts',(372.309820613387,-6.65415806382428,2.86513684965516));
#34346=CARTESIAN_POINT('Origin',(370.834317853224,2.31077344927308,0.));
#34347=CARTESIAN_POINT('',(372.309820650725,-8.15202831126679,2.86513683042648));
#34348=CARTESIAN_POINT('',(372.309820607824,-7.90820793933162,2.86513685252006));
#34349=CARTESIAN_POINT('',(372.309820613641,2.31077344927308,2.86513684952399));
#34350=CARTESIAN_POINT('Ctrl Pts',(372.309820650725,-8.15202831126679,2.86513683042647));
#34351=CARTESIAN_POINT('Ctrl Pts',(372.323157571693,-8.15102149794463,2.85826851475322));
#34352=CARTESIAN_POINT('Ctrl Pts',(372.336448474012,-8.15001625546536,2.85130607789403));
#34353=CARTESIAN_POINT('Ctrl Pts',(372.441400777517,-8.14206547264375,2.79538903575093));
#34354=CARTESIAN_POINT('Ctrl Pts',(372.53070234652,-8.13522062520822,2.74211587856899));
#34355=CARTESIAN_POINT('Ctrl Pts',(372.631646819999,-8.12751651434263,2.67507449152134));
#34356=CARTESIAN_POINT('Ctrl Pts',(372.645935751365,-8.12642683112325,2.66541846089678));
#34357=CARTESIAN_POINT('Ctrl Pts',(372.667801608005,-8.12476149377197,2.65038509965079));
#34358=CARTESIAN_POINT('Ctrl Pts',(372.675433692125,-8.1241806335481,2.645089096483));
#34359=CARTESIAN_POINT('Ctrl Pts',(372.689458234654,-8.12311417906914,2.63526717255438));
#34360=CARTESIAN_POINT('Ctrl Pts',(372.695857082674,-8.12262797136739,2.63075095836954));
#34361=CARTESIAN_POINT('Ctrl Pts',(372.71034593757,-8.1215278512809,2.62044560045896));
#34362=CARTESIAN_POINT('Ctrl Pts',(372.71842564001,-8.12091491714605,2.61464230290493));
#34363=CARTESIAN_POINT('Ctrl Pts',(372.739364531988,-8.11932753178647,2.59945535011332));
#34364=CARTESIAN_POINT('Ctrl Pts',(372.752181470257,-8.11835692159696,2.59001353961863));
#34365=CARTESIAN_POINT('Ctrl Pts',(372.839870118988,-8.11171962291826,2.52440837494779));
#34366=CARTESIAN_POINT('Ctrl Pts',(372.912341449471,-8.10625011593137,2.46509611666199));
#34367=CARTESIAN_POINT('Ctrl Pts',(373.190987653675,-8.08482534328028,2.2160100859226));
#34368=CARTESIAN_POINT('Ctrl Pts',(373.374608888315,-8.06967948590491,2.00288013568444));
#34369=CARTESIAN_POINT('Ctrl Pts',(373.560593229343,-8.05006733033921,1.71958972527295));
#34370=CARTESIAN_POINT('Ctrl Pts',(373.591473130989,-8.04663090798016,1.66962883496073));
#34371=CARTESIAN_POINT('Ctrl Pts',(373.642514071746,-8.04060347027495,1.58176834041408));
#34372=CARTESIAN_POINT('Ctrl Pts',(373.663315143799,-8.0380350026733,1.54425747654311));
#34373=CARTESIAN_POINT('Ctrl Pts',(373.692227763668,-8.03429211329185,1.48957322332976));
#34374=CARTESIAN_POINT('Ctrl Pts',(373.700946370354,-8.03313912880729,1.4727248096038));
#34375=CARTESIAN_POINT('Ctrl Pts',(373.715914443979,-8.03111604140217,1.44316295276664));
#34376=CARTESIAN_POINT('Ctrl Pts',(373.722229837002,-8.03024827618769,1.43048333927043));
#34377=CARTESIAN_POINT('Ctrl Pts',(373.735107500368,-8.02844894997796,1.40419557843276));
#34378=CARTESIAN_POINT('Ctrl Pts',(373.741658073453,-8.027517008733,1.39058211944082));
#34379=CARTESIAN_POINT('Ctrl Pts',(373.758245514548,-8.02511343484465,1.35548038274676));
#34380=CARTESIAN_POINT('Ctrl Pts',(373.768141195735,-8.02363698020214,1.33392675335642));
#34381=CARTESIAN_POINT('Ctrl Pts',(373.806551858351,-8.01773161845332,1.24776968568249));
#34382=CARTESIAN_POINT('Ctrl Pts',(373.833176265874,-8.01323931822478,1.18234983921741));
#34383=CARTESIAN_POINT('Ctrl Pts',(373.971318862361,-7.98748304324973,0.808150860148312));
#34384=CARTESIAN_POINT('Ctrl Pts',(374.037265187733,-7.96472207678056,0.484707553345173));
#34385=CARTESIAN_POINT('Ctrl Pts',(374.055510525264,-7.9399942349586,0.110454362570149));
#34386=CARTESIAN_POINT('Ctrl Pts',(374.056769568199,-7.93695384560728,0.0639357420940327));
#34387=CARTESIAN_POINT('Ctrl Pts',(374.057187210583,-7.9319712493563,-0.0133994785397873));
#34388=CARTESIAN_POINT('Ctrl Pts',(374.056911919766,-7.93000546910445,-0.0442050364260089));
#34389=CARTESIAN_POINT('Ctrl Pts',(374.055922254066,-7.92732310805148,-0.0867176435588243));
#34390=CARTESIAN_POINT('Ctrl Pts',(374.055585657342,-7.92658725898352,-0.0984307337497683));
#34391=CARTESIAN_POINT('Ctrl Pts',(374.054908705317,-7.92534931591621,-0.118226759624611));
#34392=CARTESIAN_POINT('Ctrl Pts',(374.054601788839,-7.9248453979212,-0.126310658308434));
#34393=CARTESIAN_POINT('Ctrl Pts',(374.053955474544,-7.92388330419433,-0.141795765460727));
#34394=CARTESIAN_POINT('Ctrl Pts',(374.053620991389,-7.92342484704272,-0.149197047335861));
#34395=CARTESIAN_POINT('Ctrl Pts',(374.052758516461,-7.92232986400548,-0.166925702656494));
#34396=CARTESIAN_POINT('Ctrl Pts',(374.052206332691,-7.92169467055758,-0.177251892698772));
#34397=CARTESIAN_POINT('Ctrl Pts',(374.050029071712,-7.91940630419859,-0.214596193861981));
#34398=CARTESIAN_POINT('Ctrl Pts',(374.048113293538,-7.91776840435768,-0.241597069532205));
#34399=CARTESIAN_POINT('Ctrl Pts',(374.032169695779,-7.90630095566361,-0.432248266640488));
#34400=CARTESIAN_POINT('Ctrl Pts',(374.005987382573,-7.89703406587436,-0.59465987295074));
#34401=CARTESIAN_POINT('Ctrl Pts',(373.909999865642,-7.87406182893423,-0.993329125360318));
#34402=CARTESIAN_POINT('Ctrl Pts',(373.825332180905,-7.86045494851778,-1.22488525863979));
#34403=CARTESIAN_POINT('Ctrl Pts',(373.693666467329,-7.8430871635382,-1.48746296230229));
#34404=CARTESIAN_POINT('Ctrl Pts',(373.671201036714,-7.8402198124507,-1.52987385218172));
#34405=CARTESIAN_POINT('Ctrl Pts',(373.638126957642,-7.83612063277615,-1.58907686100853));
#34406=CARTESIAN_POINT('Ctrl Pts',(373.628296620073,-7.83491645981166,-1.60629803818117));
#34407=CARTESIAN_POINT('Ctrl Pts',(373.611098560172,-7.83283329000884,-1.63579072784455));
#34408=CARTESIAN_POINT('Ctrl Pts',(373.603806782248,-7.83195705423776,-1.64810602249446));
#34409=CARTESIAN_POINT('Ctrl Pts',(373.589696093211,-7.8302744698756,-1.67157988733902));
#34410=CARTESIAN_POINT('Ctrl Pts',(373.582890808186,-7.82946863143004,-1.68274634700933));
#34411=CARTESIAN_POINT('Ctrl Pts',(373.56675890601,-7.82757133727133,-1.70885744822382));
#34412=CARTESIAN_POINT('Ctrl Pts',(373.557377411126,-7.82647787498777,-1.72376753353049));
#34413=CARTESIAN_POINT('Ctrl Pts',(373.529272924605,-7.82323067319133,-1.76763220776888));
#34414=CARTESIAN_POINT('Ctrl Pts',(373.510207430439,-7.82106429128604,-1.79636334887088));
#34415=CARTESIAN_POINT('Ctrl Pts',(373.33765255225,-7.80176567000371,-2.04755450253322));
#34416=CARTESIAN_POINT('Ctrl Pts',(373.157230007828,-7.78354596247333,-2.2501528156186));
#34417=CARTESIAN_POINT('Ctrl Pts',(372.829493271979,-7.75413405289148,-2.53625254655176));
#34418=CARTESIAN_POINT('Ctrl Pts',(372.697133136911,-7.74304758107349,-2.63500151689255));
#34419=CARTESIAN_POINT('Ctrl Pts',(372.540652015528,-7.73123338819568,-2.73403590439073));
#34420=CARTESIAN_POINT('Ctrl Pts',(372.523418181754,-7.72994895536709,-2.74471651157215));
#34421=CARTESIAN_POINT('Ctrl Pts',(372.497611366226,-7.72805164044615,-2.76037505978007));
#34422=CARTESIAN_POINT('Ctrl Pts',(372.489114731316,-7.72743112682183,-2.76547700757778));
#34423=CARTESIAN_POINT('Ctrl Pts',(372.474508783813,-7.72637173762073,-2.7741559774975));
#34424=CARTESIAN_POINT('Ctrl Pts',(372.46841108259,-7.72593163433138,-2.77775214830033));
#34425=CARTESIAN_POINT('Ctrl Pts',(372.45452368636,-7.72493426176666,-2.78588080125242));
#34426=CARTESIAN_POINT('Ctrl Pts',(372.446726802409,-7.72437780467917,-2.79040071777072));
#34427=CARTESIAN_POINT('Ctrl Pts',(372.425430052538,-7.72286711090915,-2.80262754712821));
#34428=CARTESIAN_POINT('Ctrl Pts',(372.411893024294,-7.72191691725905,-2.81026970246221));
#34429=CARTESIAN_POINT('Ctrl Pts',(372.343535287058,-7.7171664166256,-2.84821058562495));
#34430=CARTESIAN_POINT('Ctrl Pts',(372.287891038818,-7.7134526572714,-2.87700659480662));
#34431=CARTESIAN_POINT('Ctrl Pts',(371.95518424719,-7.691930420183,-3.0370635331236));
#34432=CARTESIAN_POINT('Ctrl Pts',(371.661367406825,-7.67551157967861,-3.12987553083968));
#34433=CARTESIAN_POINT('Ctrl Pts',(371.296503535557,-7.65417528237968,-3.1900616464876));
#34434=CARTESIAN_POINT('Ctrl Pts',(371.233882925903,-7.65048786005654,-3.19850839667869));
#34435=CARTESIAN_POINT('Ctrl Pts',(371.125955601382,-7.64406070290072,-3.2098475958595));
#34436=CARTESIAN_POINT('Ctrl Pts',(371.080760867094,-7.6413479346913,-3.21363341086185));
#34437=CARTESIAN_POINT('Ctrl Pts',(371.016147307277,-7.63743263312576,-3.21767489303943));
#34438=CARTESIAN_POINT('Ctrl Pts',(370.996781505073,-7.63625444010609,-3.21871079845043));
#34439=CARTESIAN_POINT('Ctrl Pts',(370.963186613776,-7.63420191680255,-3.22020388301992));
#34440=CARTESIAN_POINT('Ctrl Pts',(370.948961525339,-7.63333013111012,-3.22074168847104));
#34441=CARTESIAN_POINT('Ctrl Pts',(370.919783655442,-7.63153626076234,-3.22165126522741));
#34442=CARTESIAN_POINT('Ctrl Pts',(370.904830934777,-7.63061389047283,-3.22201321713528));
#34443=CARTESIAN_POINT('Ctrl Pts',(370.866859975986,-7.62826358734271,-3.22266791456972));
#34444=CARTESIAN_POINT('Ctrl Pts',(370.843840421863,-7.62683123769316,-3.22281813850644));
#34445=CARTESIAN_POINT('Ctrl Pts',(370.755597316853,-7.62131067278134,-3.22244859304872));
#34446=CARTESIAN_POINT('Ctrl Pts',(370.690400384602,-7.61716905993425,-3.22019543387633));
#34447=CARTESIAN_POINT('Ctrl Pts',(370.291298361409,-7.59141642045302,-3.194258793749));
#34448=CARTESIAN_POINT('Ctrl Pts',(369.962787658226,-7.56820328390233,-3.12065960283085));
#34449=CARTESIAN_POINT('Ctrl Pts',(369.608007679616,-7.54302893225164,-2.98068277514726));
#34450=CARTESIAN_POINT('Ctrl Pts',(369.564863831115,-7.53997120041452,-2.96256533731893));
#34451=CARTESIAN_POINT('Ctrl Pts',(369.493877736847,-7.53496335372641,-2.93092042130605));
#34452=CARTESIAN_POINT('Ctrl Pts',(369.465809288591,-7.53298937911568,-2.91792026868126));
#34453=CARTESIAN_POINT('Ctrl Pts',(369.427353755438,-7.5302977979533,-2.89943224299359));
#34454=CARTESIAN_POINT('Ctrl Pts',(369.416803992326,-7.52956075391121,-2.89428916460341));
#34455=CARTESIAN_POINT('Ctrl Pts',(369.399027069736,-7.52832138715674,-2.8855022837462));
#34456=CARTESIAN_POINT('Ctrl Pts',(369.391785171819,-7.52781723101786,-2.88188870896051));
#34457=CARTESIAN_POINT('Ctrl Pts',(369.377943654053,-7.52685514260679,-2.87491679602573));
#34458=CARTESIAN_POINT('Ctrl Pts',(369.371341915294,-7.52639692587111,-2.87156295416354));
#34459=CARTESIAN_POINT('Ctrl Pts',(369.355562279615,-7.525303112136,-2.86347797800529));
#34460=CARTESIAN_POINT('Ctrl Pts',(369.346395378789,-7.52466884116482,-2.85872539671211));
#34461=CARTESIAN_POINT('Ctrl Pts',(369.313383481942,-7.52238833038305,-2.84140856451865));
#34462=CARTESIAN_POINT('Ctrl Pts',(369.289672743804,-7.520757223314,-2.82858897437589));
#34463=CARTESIAN_POINT('Ctrl Pts',(369.115420176268,-7.50880040062977,-2.73153186273132));
#34464=CARTESIAN_POINT('Ctrl Pts',(368.971678985961,-7.49909736519989,-2.63561504726192));
#34465=CARTESIAN_POINT('Ctrl Pts',(368.694002091452,-7.4792875841634,-2.41620660401064));
#34466=CARTESIAN_POINT('Ctrl Pts',(368.561462072474,-7.46921219845437,-2.29197033975356));
#34467=CARTESIAN_POINT('Ctrl Pts',(368.399016158113,-7.45519289122496,-2.11167847528777));
#34468=CARTESIAN_POINT('Ctrl Pts',(368.359266765488,-7.45160885639228,-2.06494595403237));
#34469=CARTESIAN_POINT('Ctrl Pts',(368.293122554077,-7.44534598711505,-1.98252624511162));
#34470=CARTESIAN_POINT('Ctrl Pts',(368.266086228567,-7.44269224625346,-1.94737512978056));
#34471=CARTESIAN_POINT('Ctrl Pts',(368.228382321813,-7.43884737968185,-1.89620332964473));
#34472=CARTESIAN_POINT('Ctrl Pts',(368.217118842233,-7.43767938450671,-1.88062659061397));
#34473=CARTESIAN_POINT('Ctrl Pts',(368.197774577265,-7.43563880836797,-1.85336422160413));
#34474=CARTESIAN_POINT('Ctrl Pts',(368.189630389842,-7.43476868794977,-1.84172408214783));
#34475=CARTESIAN_POINT('Ctrl Pts',(368.173037068899,-7.4329728092505,-1.81767093061318));
#34476=CARTESIAN_POINT('Ctrl Pts',(368.164597206876,-7.43204672798182,-1.8052519722493));
#34477=CARTESIAN_POINT('Ctrl Pts',(368.143288198828,-7.42967572275531,-1.77342026075095));
#34478=CARTESIAN_POINT('Ctrl Pts',(368.130542319421,-7.42822622592957,-1.75392640642534));
#34479=CARTESIAN_POINT('Ctrl Pts',(368.08179318308,-7.42255752835863,-1.67757400424202));
#34480=CARTESIAN_POINT('Ctrl Pts',(368.047365227766,-7.41828118425131,-1.61973472511951));
#34481=CARTESIAN_POINT('Ctrl Pts',(367.880049433157,-7.39601259155364,-1.31749556208095));
#34482=CARTESIAN_POINT('Ctrl Pts',(367.777415490948,-7.37698557944799,-1.05773187813221));
#34483=CARTESIAN_POINT('Ctrl Pts',(367.680111915811,-7.35027017100145,-0.671907276102211));
#34484=CARTESIAN_POINT('Ctrl Pts',(367.657309979484,-7.34233413642857,-0.554167597318695));
#34485=CARTESIAN_POINT('Ctrl Pts',(367.638720169622,-7.33358130100331,-0.417837180098143));
#34486=CARTESIAN_POINT('Ctrl Pts',(367.636467811545,-7.33245947710066,-0.400234442104032));
#34487=CARTESIAN_POINT('Ctrl Pts',(367.633245482514,-7.33075561254188,-0.37328475771412));
#34488=CARTESIAN_POINT('Ctrl Pts',(367.632170838178,-7.33016799345792,-0.363951002411286));
#34489=CARTESIAN_POINT('Ctrl Pts',(367.630275959976,-7.32909515796473,-0.346834750679004));
#34490=CARTESIAN_POINT('Ctrl Pts',(367.629443251316,-7.32860927305682,-0.339053958120386));
#34491=CARTESIAN_POINT('Ctrl Pts',(367.627629655405,-7.32751736791617,-0.321503901199308));
#34492=CARTESIAN_POINT('Ctrl Pts',(367.626665065784,-7.32691226224077,-0.311733151380875));
#34493=CARTESIAN_POINT('Ctrl Pts',(367.624293843185,-7.32535870049262,-0.286536798747629));
#34494=CARTESIAN_POINT('Ctrl Pts',(367.62295372125,-7.32441382017259,-0.271104990043831));
#34495=CARTESIAN_POINT('Ctrl Pts',(367.615011734892,-7.31834262474473,-0.171308412292787));
#34496=CARTESIAN_POINT('Ctrl Pts',(367.611623045353,-7.31337726984258,-0.0867134915978316));
#34497=CARTESIAN_POINT('Ctrl Pts',(367.611398677425,-7.29332513466613,0.261575697431371));
#34498=CARTESIAN_POINT('Ctrl Pts',(367.643581452442,-7.27904210008449,0.524258573570218));
#34499=CARTESIAN_POINT('Ctrl Pts',(367.733961813044,-7.25763832999817,0.886534589102296));
#34500=CARTESIAN_POINT('Ctrl Pts',(367.765929793215,-7.25123338405258,0.991535287627039));
#34501=CARTESIAN_POINT('Ctrl Pts',(367.812416071019,-7.24302267440763,1.12025245319812));
#34502=CARTESIAN_POINT('Ctrl Pts',(367.821968802864,-7.24138217694595,1.14569152500224));
#34503=CARTESIAN_POINT('Ctrl Pts',(367.837662172459,-7.23875760046087,1.18592954094534));
#34504=CARTESIAN_POINT('Ctrl Pts',(367.843593580217,-7.23778053325284,1.2008090828753));
#34505=CARTESIAN_POINT('Ctrl Pts',(367.854900349201,-7.23594509224851,1.22856977968898));
#34506=CARTESIAN_POINT('Ctrl Pts',(367.860248963296,-7.2350876387046,1.24146147547367));
#34507=CARTESIAN_POINT('Ctrl Pts',(367.872397832818,-7.23316358341588,1.27021461839161));
#34508=CARTESIAN_POINT('Ctrl Pts',(367.879242053537,-7.23209550602635,1.28605691305561));
#34509=CARTESIAN_POINT('Ctrl Pts',(367.89986559245,-7.22892274708251,1.33276019660347));
#34510=CARTESIAN_POINT('Ctrl Pts',(367.914003165366,-7.22680588802463,1.36345949577465));
#34511=CARTESIAN_POINT('Ctrl Pts',(367.947318411436,-7.22194373666216,1.43290633405652));
#34512=CARTESIAN_POINT('Ctrl Pts',(367.966797900388,-7.21918844284527,1.47150106144193));
#34513=CARTESIAN_POINT('Ctrl Pts',(368.034988357602,-7.20982476546895,1.6001079828204));
#34514=CARTESIAN_POINT('Ctrl Pts',(368.087205169262,-7.2031030347132,1.68818240651719));
#34515=CARTESIAN_POINT('Ctrl Pts',(368.262551758136,-7.18187098121895,1.95420506679225));
#34516=CARTESIAN_POINT('Ctrl Pts',(368.399454113501,-7.16703821124287,2.12234092774425));
#34517=CARTESIAN_POINT('Ctrl Pts',(368.612262213029,-7.14700621075816,2.33577226344528));
#34518=CARTESIAN_POINT('Ctrl Pts',(368.674734942209,-7.14143370600362,2.393651529463));
#34519=CARTESIAN_POINT('Ctrl Pts',(368.751220366321,-7.1350349565875,2.45907768911558));
#34520=CARTESIAN_POINT('Ctrl Pts',(368.763081882362,-7.13405413794183,2.46907670925603));
#34521=CARTESIAN_POINT('Ctrl Pts',(368.782573159931,-7.1324617668334,2.48526815695573));
#34522=CARTESIAN_POINT('Ctrl Pts',(368.790159701091,-7.13184669449722,2.49151190113257));
#34523=CARTESIAN_POINT('Ctrl Pts',(368.80383982628,-7.13074622739279,2.50266613516056));
#34524=CARTESIAN_POINT('Ctrl Pts',(368.809922825616,-7.13025994572069,2.50758919640876));
#34525=CARTESIAN_POINT('Ctrl Pts',(368.823343735524,-7.12919376210525,2.5183702696963));
#34526=CARTESIAN_POINT('Ctrl Pts',(368.830689332612,-7.12861455975534,2.52421838871857));
#34527=CARTESIAN_POINT('Ctrl Pts',(368.851968703662,-7.12694883614547,2.54100831892204));
#34528=CARTESIAN_POINT('Ctrl Pts',(368.865967529408,-7.12586796980399,2.55186764210009));
#34529=CARTESIAN_POINT('Ctrl Pts',(368.974486765301,-7.11759729905259,2.63462504487918));
#34530=CARTESIAN_POINT('Ctrl Pts',(369.072837534192,-7.11072753403957,2.70137266597804));
#34531=CARTESIAN_POINT('Ctrl Pts',(369.401727301336,-7.08894275969346,2.89896034947317));
#34532=CARTESIAN_POINT('Ctrl Pts',(369.644739486146,-7.07452662493812,3.00685783437668));
#34533=CARTESIAN_POINT('Ctrl Pts',(369.973626959232,-7.05455706417947,3.10669258537339));
#34534=CARTESIAN_POINT('Ctrl Pts',(370.049842495721,-7.04990751279688,3.12680740869598));
#34535=CARTESIAN_POINT('Ctrl Pts',(370.150781871333,-7.04368448810621,3.14952452084542));
#34536=CARTESIAN_POINT('Ctrl Pts',(370.174910237852,-7.0421922091585,3.15466443399327));
#34537=CARTESIAN_POINT('Ctrl Pts',(370.214109418506,-7.0397591711853,3.16254543260609));
#34538=CARTESIAN_POINT('Ctrl Pts',(370.229145221786,-7.03882386606374,3.16545702691748));
#34539=CARTESIAN_POINT('Ctrl Pts',(370.258053162049,-7.03702146179978,3.17084138790783));
#34540=CARTESIAN_POINT('Ctrl Pts',(370.271921911155,-7.03615490780868,3.17333056832926));
#34541=CARTESIAN_POINT('Ctrl Pts',(370.304009206815,-7.03414556912704,3.17887268228503));
#34542=CARTESIAN_POINT('Ctrl Pts',(370.322238431475,-7.03300073368005,3.18186005878463));
#34543=CARTESIAN_POINT('Ctrl Pts',(370.380127875912,-7.02935418407008,3.19083653620975));
#34544=CARTESIAN_POINT('Ctrl Pts',(370.419873484355,-7.0268342094576,3.1962418507338));
#34545=CARTESIAN_POINT('Ctrl Pts',(370.624903415305,-7.01374565902768,3.22023700644114));
#34546=CARTESIAN_POINT('Ctrl Pts',(370.791323285555,-7.00280570432569,3.2267503742865));
#34547=CARTESIAN_POINT('Ctrl Pts',(371.094498413275,-6.98244568196471,3.21515547391714));
#34548=CARTESIAN_POINT('Ctrl Pts',(371.231040246453,-6.97312078503562,3.20117615178233));
#34549=CARTESIAN_POINT('Ctrl Pts',(371.495712460876,-6.95505694371268,3.15688118846149));
#34550=CARTESIAN_POINT('Ctrl Pts',(371.623723969885,-6.9463279985614,3.12732909856004));
#34551=CARTESIAN_POINT('Ctrl Pts',(371.76572018431,-6.93689701975914,3.08526989477441));
#34552=CARTESIAN_POINT('Ctrl Pts',(371.78181463671,-6.93583187166918,3.08036531912207));
#34553=CARTESIAN_POINT('Ctrl Pts',(371.807516755451,-6.93413779228415,3.07231242672921));
#34554=CARTESIAN_POINT('Ctrl Pts',(371.817149056633,-6.93350447064289,3.06924462739969));
#34555=CARTESIAN_POINT('Ctrl Pts',(371.834245375026,-6.93238337401258,3.06371087090298));
#34556=CARTESIAN_POINT('Ctrl Pts',(371.841714999078,-6.93189457627174,3.06126286761943));
#34557=CARTESIAN_POINT('Ctrl Pts',(371.857770834179,-6.93084616677663,3.05593579192734));
#34558=CARTESIAN_POINT('Ctrl Pts',(371.866353897612,-6.93028707934126,3.05304785032756));
#34559=CARTESIAN_POINT('Ctrl Pts',(371.890217403953,-6.92873616194583,3.04490636735421));
#34560=CARTESIAN_POINT('Ctrl Pts',(371.905470921954,-6.92774884187755,3.0395739463662));
#34561=CARTESIAN_POINT('Ctrl Pts',(371.995615437618,-6.9219343370987,3.00729778987409));
#34562=CARTESIAN_POINT('Ctrl Pts',(372.069533992445,-6.91724962241963,2.97769968093071));
#34563=CARTESIAN_POINT('Ctrl Pts',(372.198919375538,-6.90907263694122,2.92024313659028));
#34564=CARTESIAN_POINT('Ctrl Pts',(372.254786456931,-6.90554985179344,2.89347862523926));
#34565=CARTESIAN_POINT('Ctrl Pts',(372.309820841127,-6.90205582396876,2.86513673237218));
#34566=CARTESIAN_POINT('',(367.611569021564,-7.06162094379804,-0.00160891364598954));
#34567=CARTESIAN_POINT('Ctrl Pts',(372.309820613387,-6.65415806382428,2.86513684965516));
#34568=CARTESIAN_POINT('Ctrl Pts',(372.292714814035,-6.65536004592608,2.87394608128435));
#34569=CARTESIAN_POINT('Ctrl Pts',(372.275530545294,-6.65656739170384,2.8826019051552));
#34570=CARTESIAN_POINT('Ctrl Pts',(372.050564813285,-6.67237282628404,2.99340403598632));
#34571=CARTESIAN_POINT('Ctrl Pts',(371.832478903887,-6.68776556693163,3.07300526760262));
#34572=CARTESIAN_POINT('Ctrl Pts',(371.409105348385,-6.71724093813562,3.17767631938501));
#34573=CARTESIAN_POINT('Ctrl Pts',(371.206174504654,-6.73118248846332,3.20776299651676));
#34574=CARTESIAN_POINT('Ctrl Pts',(370.975790578942,-6.74599160673359,3.21974822736512));
#34575=CARTESIAN_POINT('Ctrl Pts',(370.949816687413,-6.74764624100932,3.22078457808238));
#34576=CARTESIAN_POINT('Ctrl Pts',(370.913653238748,-6.74992655959511,3.22178943285873));
#34577=CARTESIAN_POINT('Ctrl Pts',(370.903472865778,-6.75056590929184,3.22202402906313));
#34578=CARTESIAN_POINT('Ctrl Pts',(370.885921488494,-6.75166352459439,3.22234525788378));
#34579=CARTESIAN_POINT('Ctrl Pts',(370.878551055494,-6.75212303827263,3.22245485966527));
#34580=CARTESIAN_POINT('Ctrl Pts',(370.863042820153,-6.75308684240395,3.22263225714373));
#34581=CARTESIAN_POINT('Ctrl Pts',(370.854905031971,-6.75359080547268,3.22269451837233));
#34582=CARTESIAN_POINT('Ctrl Pts',(370.834828492493,-6.7548299083099,3.22277207267103));
#34583=CARTESIAN_POINT('Ctrl Pts',(370.822889580034,-6.75556309208547,3.22275185177327));
#34584=CARTESIAN_POINT('Ctrl Pts',(370.778670236786,-6.75826595864589,3.22243122460895));
#34585=CARTESIAN_POINT('Ctrl Pts',(370.746393564111,-6.76021377567416,3.22171214651434));
#34586=CARTESIAN_POINT('Ctrl Pts',(370.51164755989,-6.77423279404112,3.21295166462082));
#34587=CARTESIAN_POINT('Ctrl Pts',(370.310301049912,-6.78547882240443,3.18631470827144));
#34588=CARTESIAN_POINT('Ctrl Pts',(369.908343296722,-6.80854281449839,3.09397552209954));
#34589=CARTESIAN_POINT('Ctrl Pts',(369.709013461959,-6.82032748692682,3.0271752803054));
#34590=CARTESIAN_POINT('Ctrl Pts',(369.479312238753,-6.83526531066406,2.92435235518205));
#34591=CARTESIAN_POINT('Ctrl Pts',(369.441367910337,-6.83777827620923,2.90646987339364));
#34592=CARTESIAN_POINT('Ctrl Pts',(369.3871098529,-6.84144283512145,2.87959247882223));
#34593=CARTESIAN_POINT('Ctrl Pts',(369.370507182731,-6.84257395538906,2.87118827991933));
#34594=CARTESIAN_POINT('Ctrl Pts',(369.34139340426,-6.84457518527662,2.85613285602634));
#34595=CARTESIAN_POINT('Ctrl Pts',(369.328851532944,-6.84544315654891,2.84954197196294));
#34596=CARTESIAN_POINT('Ctrl Pts',(369.31482980478,-6.84642025051363,2.84205499901586));
#34597=CARTESIAN_POINT('Ctrl Pts',(369.313306580803,-6.8465264844598,2.84124009121787));
#34598=CARTESIAN_POINT('Ctrl Pts',(369.298320249221,-6.84757255336302,2.83320706612694));
#34599=CARTESIAN_POINT('Ctrl Pts',(369.284908155408,-6.84851573178744,2.82589463613572));
#34600=CARTESIAN_POINT('Ctrl Pts',(369.257497529659,-6.85045793605267,2.81069624214544));
#34601=CARTESIAN_POINT('Ctrl Pts',(369.243504988307,-6.85145729699466,2.80280040534842));
#34602=CARTESIAN_POINT('Ctrl Pts',(369.208866699075,-6.85395117135782,2.78291145661275));
#34603=CARTESIAN_POINT('Ctrl Pts',(369.188294347554,-6.85545015644211,2.77079306326534));
#34604=CARTESIAN_POINT('Ctrl Pts',(369.130792736727,-6.85969106238078,2.73605465662089));
#34605=CARTESIAN_POINT('Ctrl Pts',(369.094183110506,-6.86245134426193,2.71291793037405));
#34606=CARTESIAN_POINT('Ctrl Pts',(368.972455356669,-6.87183626518595,2.63251008330424));
#34607=CARTESIAN_POINT('Ctrl Pts',(368.889614430949,-6.87857478917699,2.57191886111249));
#34608=CARTESIAN_POINT('Ctrl Pts',(368.635864483499,-6.90031020789244,2.36704475180542));
#34609=CARTESIAN_POINT('Ctrl Pts',(368.477014553453,-6.91565888791342,2.20889417015381));
#34610=CARTESIAN_POINT('Ctrl Pts',(368.286472538878,-6.9356530371954,1.97502003431186));
#34611=CARTESIAN_POINT('Ctrl Pts',(368.239345180718,-6.94075329982927,1.91267844525905));
#34612=CARTESIAN_POINT('Ctrl Pts',(368.18498718465,-6.94677476770478,1.8350588872182));
#34613=CARTESIAN_POINT('Ctrl Pts',(368.175553126101,-6.94782524413817,1.82136329826252));
#34614=CARTESIAN_POINT('Ctrl Pts',(368.161029669103,-6.9494501941447,1.79992601353452));
#34615=CARTESIAN_POINT('Ctrl Pts',(368.155867077405,-6.95002937441498,1.79223458735709));
#34616=CARTESIAN_POINT('Ctrl Pts',(368.146395881394,-6.9510946786067,1.77799170893899));
#34617=CARTESIAN_POINT('Ctrl Pts',(368.142078033952,-6.95158139943007,1.77144681018766));
#34618=CARTESIAN_POINT('Ctrl Pts',(368.132308237288,-6.95268515688996,1.75651973397462));
#34619=CARTESIAN_POINT('Ctrl Pts',(368.126871385587,-6.95330119238561,1.74812790480814));
#34620=CARTESIAN_POINT('Ctrl Pts',(368.110298055638,-6.95518507856482,1.72228403259902));
#34621=CARTESIAN_POINT('Ctrl Pts',(368.099290363321,-6.95644476499212,1.70474949094696));
#34622=CARTESIAN_POINT('Ctrl Pts',(368.074011026351,-6.95936063101553,1.66360594754182));
#34623=CARTESIAN_POINT('Ctrl Pts',(368.059871843923,-6.96100929032781,1.63991706274016));
#34624=CARTESIAN_POINT('Ctrl Pts',(368.011309865285,-6.96674596015214,1.55612975027016));
#34625=CARTESIAN_POINT('Ctrl Pts',(367.978519915078,-6.97075585652661,1.49510307797678));
#34626=CARTESIAN_POINT('Ctrl Pts',(367.823527142657,-6.99066965287483,1.18290356230497));
#34627=CARTESIAN_POINT('Ctrl Pts',(367.732379285683,-7.00579167713607,0.917665187718701));
#34628=CARTESIAN_POINT('Ctrl Pts',(367.660375132727,-7.02670475077214,0.564597279851319));
#34629=CARTESIAN_POINT('Ctrl Pts',(367.647185239816,-7.03148147685216,0.484630364062586));
#34630=CARTESIAN_POINT('Ctrl Pts',(367.633895666356,-7.03785220601611,0.379521983584453));
#34631=CARTESIAN_POINT('Ctrl Pts',(367.631055567865,-7.03936002166402,0.354753136926414));
#34632=CARTESIAN_POINT('Ctrl Pts',(367.626928570105,-7.04181259935233,0.314655499392359));
#34633=CARTESIAN_POINT('Ctrl Pts',(367.625463511737,-7.04275174832619,0.299345785059292));
#34634=CARTESIAN_POINT('Ctrl Pts',(367.622915484472,-7.04452374600888,0.270546692274248));
#34635=CARTESIAN_POINT('Ctrl Pts',(367.621807785001,-7.04535579774585,0.257059797362288));
#34636=CARTESIAN_POINT('Ctrl Pts',(367.619753967572,-7.04703210872499,0.229962433911934));
#34637=CARTESIAN_POINT('Ctrl Pts',(367.618809271689,-7.04787639473124,0.216352140870095));
#34638=CARTESIAN_POINT('Ctrl Pts',(367.616844520928,-7.04981543936561,0.185181821329923));
#34639=CARTESIAN_POINT('Ctrl Pts',(367.615881759504,-7.05091196771938,0.167618739758486));
#34640=CARTESIAN_POINT('Ctrl Pts',(367.612708007927,-7.05517899842007,0.0995268477100366));
#34641=CARTESIAN_POINT('Ctrl Pts',(367.611542957261,-7.05838171058188,0.04895922325798));
#34642=CARTESIAN_POINT('Ctrl Pts',(367.611568256498,-7.06161982618061,-0.00161223563090186));
#34643=CARTESIAN_POINT('Ctrl Pts',(367.611568254881,-7.06161961892771,-0.00160899884609024));
#34644=CARTESIAN_POINT('Ctrl Pts',(367.611737235074,-7.08329133490289,-0.340068440858395));
#34645=CARTESIAN_POINT('Ctrl Pts',(367.665231320938,-7.10671891120355,-0.67639080493669));
#34646=CARTESIAN_POINT('Ctrl Pts',(367.794381854883,-7.13434941397816,-1.07288818642694));
#34647=CARTESIAN_POINT('Ctrl Pts',(367.821464099035,-7.13948047276956,-1.14674076032872));
#34648=CARTESIAN_POINT('Ctrl Pts',(367.857320765052,-7.14549618592994,-1.23444948557229));
#34649=CARTESIAN_POINT('Ctrl Pts',(367.863530123105,-7.14651325527707,-1.24931880762661));
#34650=CARTESIAN_POINT('Ctrl Pts',(367.8734008267,-7.14809148099084,-1.27246604203168));
#34651=CARTESIAN_POINT('Ctrl Pts',(367.876985863791,-7.14865704107256,-1.28077592695885));
#34652=CARTESIAN_POINT('Ctrl Pts',(367.883753324101,-7.14971033106886,-1.29628254583913));
#34653=CARTESIAN_POINT('Ctrl Pts',(367.886927075202,-7.15019854408521,-1.30348267434354));
#34654=CARTESIAN_POINT('Ctrl Pts',(367.894249632532,-7.15131199810259,-1.31993149996014));
#34655=CARTESIAN_POINT('Ctrl Pts',(367.898415726098,-7.15193617807314,-1.32917230385051));
#34656=CARTESIAN_POINT('Ctrl Pts',(367.909646272212,-7.15359460698061,-1.35377232508654));
#34657=CARTESIAN_POINT('Ctrl Pts',(367.916788202708,-7.15462432127332,-1.36909610005323));
#34658=CARTESIAN_POINT('Ctrl Pts',(367.982869881789,-7.16393506312115,-1.50801580729049));
#34659=CARTESIAN_POINT('Ctrl Pts',(368.049517702996,-7.17179105464176,-1.62780971233834));
#34660=CARTESIAN_POINT('Ctrl Pts',(368.240898971664,-7.19176483792071,-1.92544500554169));
#34661=CARTESIAN_POINT('Ctrl Pts',(368.376317251127,-7.20367490969703,-2.095565052367));
#34662=CARTESIAN_POINT('Ctrl Pts',(368.575855084087,-7.22009998685957,-2.30004315068532));
#34663=CARTESIAN_POINT('Ctrl Pts',(368.625476020897,-7.224103682233,-2.3477370922521));
#34664=CARTESIAN_POINT('Ctrl Pts',(368.701085346637,-7.23012079500241,-2.41589005770033));
#34665=CARTESIAN_POINT('Ctrl Pts',(368.72592442422,-7.23208484004625,-2.4375977377705));
#34666=CARTESIAN_POINT('Ctrl Pts',(368.766204957531,-7.23525280248554,-2.47172388618119));
#34667=CARTESIAN_POINT('Ctrl Pts',(368.781435678765,-7.23644686178719,-2.48438818831003));
#34668=CARTESIAN_POINT('Ctrl Pts',(368.810790446389,-7.23874165976861,-2.50834234283804));
#34669=CARTESIAN_POINT('Ctrl Pts',(368.824894691603,-7.23984141744036,-2.51965533594577));
#34670=CARTESIAN_POINT('Ctrl Pts',(368.849739001197,-7.24177407751539,-2.53924164170816));
#34671=CARTESIAN_POINT('Ctrl Pts',(368.860437554667,-7.24260487805318,-2.54756705368057));
#34672=CARTESIAN_POINT('Ctrl Pts',(368.881818160794,-7.24426249275967,-2.56398950372236));
#34673=CARTESIAN_POINT('Ctrl Pts',(368.89249883648,-7.24508923036988,-2.57208789151719));
#34674=CARTESIAN_POINT('Ctrl Pts',(368.921388769529,-7.24732209474109,-2.59371053901141));
#34675=CARTESIAN_POINT('Ctrl Pts',(368.939690538482,-7.24873306062043,-2.60710938309576));
#34676=CARTESIAN_POINT('Ctrl Pts',(369.009121902536,-7.2540735659085,-2.65682333749758));
#34677=CARTESIAN_POINT('Ctrl Pts',(369.061163675774,-7.25805213216131,-2.69183466965255));
#34678=CARTESIAN_POINT('Ctrl Pts',(369.399822900707,-7.28380437890523,-2.9055858410807));
#34679=CARTESIAN_POINT('Ctrl Pts',(369.711936760824,-7.30723037477153,-3.03979988864536));
#34680=CARTESIAN_POINT('Ctrl Pts',(370.084600425111,-7.33261541774669,-3.13468364931452));
#34681=CARTESIAN_POINT('Ctrl Pts',(370.130306544316,-7.33568132364134,-3.14526411090766));
#34682=CARTESIAN_POINT('Ctrl Pts',(370.206570090419,-7.34070136474734,-3.16117239510582));
#34683=CARTESIAN_POINT('Ctrl Pts',(370.237001664605,-7.34267948751487,-3.16706357708475));
#34684=CARTESIAN_POINT('Ctrl Pts',(370.279082600522,-7.34537606724552,-3.17458177761866));
#34685=CARTESIAN_POINT('Ctrl Pts',(370.290661864862,-7.34611404392689,-3.17658524598284));
#34686=CARTESIAN_POINT('Ctrl Pts',(370.3102412994,-7.34735479017406,-3.17986272424727));
#34687=CARTESIAN_POINT('Ctrl Pts',(370.318235720087,-7.34785939882693,-3.1811699760106));
#34688=CARTESIAN_POINT('Ctrl Pts',(370.333551738313,-7.34882222094985,-3.18361520250084));
#34689=CARTESIAN_POINT('Ctrl Pts',(370.340872420381,-7.34928072016564,-3.1847580860805));
#34690=CARTESIAN_POINT('Ctrl Pts',(370.358408300754,-7.3503750613516,-3.18743382007305));
#34691=CARTESIAN_POINT('Ctrl Pts',(370.368627129046,-7.35100957689574,-3.18894283668358));
#34692=CARTESIAN_POINT('Ctrl Pts',(370.405528348079,-7.35328991282478,-3.19421088668329));
#34693=CARTESIAN_POINT('Ctrl Pts',(370.432251203193,-7.35492061160393,-3.19768449740244));
#34694=CARTESIAN_POINT('Ctrl Pts',(370.62542270702,-7.36657985750924,-3.22033421450083));
#34695=CARTESIAN_POINT('Ctrl Pts',(370.793119564321,-7.3760217122969,-3.22684149060996));
#34696=CARTESIAN_POINT('Ctrl Pts',(371.116654714395,-7.39415431732153,-3.21415627551405));
#34697=CARTESIAN_POINT('Ctrl Pts',(371.272076725129,-7.40283116220469,-3.1966982529753));
#34698=CARTESIAN_POINT('Ctrl Pts',(371.54265045725,-7.41856434178197,-3.14619724817188));
#34699=CARTESIAN_POINT('Ctrl Pts',(371.658374907922,-7.42550054096438,-3.11788672454404));
#34700=CARTESIAN_POINT('Ctrl Pts',(371.798174858124,-7.43427057135227,-3.07535867146352));
#34701=CARTESIAN_POINT('Ctrl Pts',(371.823988540252,-7.43590643892557,-3.06714902593804));
#34702=CARTESIAN_POINT('Ctrl Pts',(371.864738992345,-7.43851648187748,-3.05362098161577));
#34703=CARTESIAN_POINT('Ctrl Pts',(371.879745632013,-7.43948363320663,-3.04851596167851));
#34704=CARTESIAN_POINT('Ctrl Pts',(371.907923194807,-7.44131118832227,-3.03869787993647));
#34705=CARTESIAN_POINT('Ctrl Pts',(371.921102320756,-7.44217076192382,-3.03400935172418));
#34706=CARTESIAN_POINT('Ctrl Pts',(371.950726227592,-7.44411392166302,-3.02325274316792));
#34707=CARTESIAN_POINT('Ctrl Pts',(371.967152763123,-7.44519910747048,-3.0171360352015));
#34708=CARTESIAN_POINT('Ctrl Pts',(372.009152308528,-7.44799388415985,-3.00110543094856));
#34709=CARTESIAN_POINT('Ctrl Pts',(372.034649731752,-7.44970987639238,-2.99099868133295));
#34710=CARTESIAN_POINT('Ctrl Pts',(372.254765927177,-7.4646956437799,-2.90048047448044));
#34711=CARTESIAN_POINT('Ctrl Pts',(372.441164298007,-7.47861007205944,-2.80151302856067));
#34712=CARTESIAN_POINT('Ctrl Pts',(372.760639029563,-7.50446409931744,-2.58946167500162));
#34713=CARTESIAN_POINT('Ctrl Pts',(372.896796432942,-7.5162577173633,-2.48237995002616));
#34714=CARTESIAN_POINT('Ctrl Pts',(373.058918865243,-7.53085261190641,-2.33228868700919));
#34715=CARTESIAN_POINT('Ctrl Pts',(373.093400608728,-7.53399115836358,-2.29890533956787));
#34716=CARTESIAN_POINT('Ctrl Pts',(373.149274510799,-7.53911671423045,-2.24233953918816));
#34717=CARTESIAN_POINT('Ctrl Pts',(373.171094265287,-7.54112893030326,-2.2195916536104));
#34718=CARTESIAN_POINT('Ctrl Pts',(373.20063938389,-7.54386381452045,-2.18787108403626));
#34719=CARTESIAN_POINT('Ctrl Pts',(373.208653498791,-7.54460671514471,-2.17917133775323));
#34720=CARTESIAN_POINT('Ctrl Pts',(373.222085350019,-7.54585333557096,-2.16442828662905));
#34721=CARTESIAN_POINT('Ctrl Pts',(373.22752843721,-7.54635893341554,-2.15840833309759));
#34722=CARTESIAN_POINT('Ctrl Pts',(373.237886453824,-7.54732176987865,-2.14686520372296));
#34723=CARTESIAN_POINT('Ctrl Pts',(373.242805183746,-7.54777930664708,-2.14134560546803));
#34724=CARTESIAN_POINT('Ctrl Pts',(373.254509705343,-7.54886894217175,-2.12811991891983));
#34725=CARTESIAN_POINT('Ctrl Pts',(373.261277797574,-7.54949974026796,-2.12039817617203));
#34726=CARTESIAN_POINT('Ctrl Pts',(373.285392543592,-7.55175043150226,-2.09261884345245));
#34727=CARTESIAN_POINT('Ctrl Pts',(373.302528925134,-7.55335571976284,-2.072379060183));
#34728=CARTESIAN_POINT('Ctrl Pts',(373.441774012092,-7.56647131394683,-1.90373901782998));
#34729=CARTESIAN_POINT('Ctrl Pts',(373.550650052763,-7.5772031526525,-1.74488064433265));
#34730=CARTESIAN_POINT('Ctrl Pts',(373.682595817303,-7.5922785978866,-1.509773784623));
#34731=CARTESIAN_POINT('Ctrl Pts',(373.718020701275,-7.59660055451943,-1.44095866765114));
#34732=CARTESIAN_POINT('Ctrl Pts',(373.816689762544,-7.60966616493837,-1.23104387852857));
#34733=CARTESIAN_POINT('Ctrl Pts',(373.87228856369,-7.61851166975053,-1.08661736524141));
#34734=CARTESIAN_POINT('Ctrl Pts',(373.92858184387,-7.63000758238224,-0.901745947322941));
#34735=CARTESIAN_POINT('Ctrl Pts',(373.93918726849,-7.63232986865382,-0.864523636628074));
#34736=CARTESIAN_POINT('Ctrl Pts',(373.953795578101,-7.63577729023261,-0.809511114016146));
#34737=CARTESIAN_POINT('Ctrl Pts',(373.958322180466,-7.6368855220434,-0.791862653459371));
#34738=CARTESIAN_POINT('Ctrl Pts',(373.966077516124,-7.63885784522248,-0.760524027585623));
#34739=CARTESIAN_POINT('Ctrl Pts',(373.969366754259,-7.6397199634918,-0.746849222345889));
#34740=CARTESIAN_POINT('Ctrl Pts',(373.976082010248,-7.64153543839229,-0.718104706916323));
#34741=CARTESIAN_POINT('Ctrl Pts',(373.979489347771,-7.64248937039048,-0.703031041324144));
#34742=CARTESIAN_POINT('Ctrl Pts',(373.988182371304,-7.64501243310841,-0.663245626646811));
#34743=CARTESIAN_POINT('Ctrl Pts',(373.993285957855,-7.64658733235627,-0.638495587424803));
#34744=CARTESIAN_POINT('Ctrl Pts',(374.014089557158,-7.65343636603863,-0.53124574344785));
#34745=CARTESIAN_POINT('Ctrl Pts',(374.026851399402,-7.65880232043154,-0.448216028682624));
#34746=CARTESIAN_POINT('Ctrl Pts',(374.06256070805,-7.67930581152035,-0.134767092402776));
#34747=CARTESIAN_POINT('Ctrl Pts',(374.063900551766,-7.6950498575698,0.0973863939785096));
#34748=CARTESIAN_POINT('Ctrl Pts',(374.025652589839,-7.72042561626714,0.471652412540713));
#34749=CARTESIAN_POINT('Ctrl Pts',(374.001247125828,-7.73009142531755,0.6145257545992));
#34750=CARTESIAN_POINT('Ctrl Pts',(373.9630248196,-7.7404730992766,0.773075075186207));
#34751=CARTESIAN_POINT('Ctrl Pts',(373.958585120696,-7.74163037428862,0.790826422800244));
#34752=CARTESIAN_POINT('Ctrl Pts',(373.951607259095,-7.7433768912815,0.817749871478434));
#34753=CARTESIAN_POINT('Ctrl Pts',(373.949179347836,-7.74397213319706,0.826949797206087));
#34754=CARTESIAN_POINT('Ctrl Pts',(373.944679904098,-7.74505276218778,0.843698252808411));
#34755=CARTESIAN_POINT('Ctrl Pts',(373.942621608022,-7.74553887658771,0.851250022073007));
#34756=CARTESIAN_POINT('Ctrl Pts',(373.937950882415,-7.74662383152421,0.868143809570159));
#34757=CARTESIAN_POINT('Ctrl Pts',(373.9353237814,-7.74722181823945,0.877481562834963));
#34758=CARTESIAN_POINT('Ctrl Pts',(373.927534240669,-7.74896007427734,0.90469673740681));
#34759=CARTESIAN_POINT('Ctrl Pts',(373.922258984267,-7.75009405373213,0.922541822769922));
#34760=CARTESIAN_POINT('Ctrl Pts',(373.870635078861,-7.76080123712691,1.09176908423008));
#34761=CARTESIAN_POINT('Ctrl Pts',(373.813338724544,-7.76980570429237,1.23960874869254));
#34762=CARTESIAN_POINT('Ctrl Pts',(373.686695191316,-7.78638916741775,1.50624791177519));
#34763=CARTESIAN_POINT('Ctrl Pts',(373.620181426628,-7.79397935946015,1.62597764351755));
#34764=CARTESIAN_POINT('Ctrl Pts',(373.468722904602,-7.80981707124958,1.86188747062503));
#34765=CARTESIAN_POINT('Ctrl Pts',(373.383213883506,-7.8180625026075,1.97733083356222));
#34766=CARTESIAN_POINT('Ctrl Pts',(373.266154626798,-7.82882769092561,2.11510720020611));
#34767=CARTESIAN_POINT('Ctrl Pts',(373.241515159255,-7.831067186585,2.14310744436421));
#34768=CARTESIAN_POINT('Ctrl Pts',(373.204303590403,-7.83441453951614,2.1839431066735));
#34769=CARTESIAN_POINT('Ctrl Pts',(373.192100642457,-7.83550689776189,2.19711178280888));
#34770=CARTESIAN_POINT('Ctrl Pts',(373.170165168159,-7.83746140903825,2.22039000746612));
#34771=CARTESIAN_POINT('Ctrl Pts',(373.160475373136,-7.83832171567159,2.2305393174434));
#34772=CARTESIAN_POINT('Ctrl Pts',(373.139877645865,-7.84014421114563,2.25183365102323));
#34773=CARTESIAN_POINT('Ctrl Pts',(373.128954509048,-7.84110705206922,2.26296340081473));
#34774=CARTESIAN_POINT('Ctrl Pts',(373.099667329586,-7.84367928483321,2.29237447748929));
#34775=CARTESIAN_POINT('Ctrl Pts',(373.081163147025,-7.84529485629347,2.31051404622877));
#34776=CARTESIAN_POINT('Ctrl Pts',(372.997142582082,-7.85258959482103,2.39091520004956));
#34777=CARTESIAN_POINT('Ctrl Pts',(372.929248543643,-7.858376075824,2.45062219217586));
#34778=CARTESIAN_POINT('Ctrl Pts',(372.688450949868,-7.87854936501975,2.64505690195918));
#34779=CARTESIAN_POINT('Ctrl Pts',(372.504442393296,-7.89343311657087,2.76490953516983));
#34780=CARTESIAN_POINT('Ctrl Pts',(372.309820607824,-7.90820793933161,2.86513685252006));
#34781=CARTESIAN_POINT('Origin',(370.834317853224,2.31077344927308,0.));
#34782=CARTESIAN_POINT('',(372.309820613643,-9.40650395364997,2.86513684952317));
#34783=CARTESIAN_POINT('',(372.309820498245,-9.15921048455973,2.86513690895124));
#34784=CARTESIAN_POINT('',(372.309820613641,2.31077344927308,2.86513684952399));
#34785=CARTESIAN_POINT('',(367.611569014087,-8.55988254489073,0.00273538678758171));
#34786=CARTESIAN_POINT('Ctrl Pts',(372.309820613642,-9.40650395365004,2.86513684952373));
#34787=CARTESIAN_POINT('Ctrl Pts',(372.310235252672,-9.40647438359926,2.86492331660494));
#34788=CARTESIAN_POINT('Ctrl Pts',(372.310649845599,-9.40644481045213,2.86470969354901));
#34789=CARTESIAN_POINT('Ctrl Pts',(372.460746735871,-9.39573600244663,2.78732956637538));
#34790=CARTESIAN_POINT('Ctrl Pts',(372.604128589944,-9.38465237160275,2.69856113744389));
#34791=CARTESIAN_POINT('Ctrl Pts',(372.804867072,-9.36794059467473,2.55138049742846));
#34792=CARTESIAN_POINT('Ctrl Pts',(372.868021324973,-9.36249139473812,2.50133091792677));
#34793=CARTESIAN_POINT('Ctrl Pts',(372.947463023267,-9.35541891085743,2.4333743217127));
#34794=CARTESIAN_POINT('Ctrl Pts',(372.965518642425,-9.35379618144939,2.41757653467915));
#34795=CARTESIAN_POINT('Ctrl Pts',(373.103615286895,-9.34127317902388,2.29399927014254));
#34796=CARTESIAN_POINT('Ctrl Pts',(373.215601010952,-9.33044557639409,2.17753203008764));
#34797=CARTESIAN_POINT('Ctrl Pts',(373.329134174731,-9.31909655968901,2.04016981703633));
#34798=CARTESIAN_POINT('Ctrl Pts',(373.3397649326,-9.31803000775799,2.02710047135573));
#34799=CARTESIAN_POINT('Ctrl Pts',(373.356614109945,-9.31633413346828,2.00605121382949));
#34800=CARTESIAN_POINT('Ctrl Pts',(373.362898129198,-9.3157004064943,1.99812453906841));
#34801=CARTESIAN_POINT('Ctrl Pts',(373.37399938043,-9.31457885958607,1.98398515636269));
#34802=CARTESIAN_POINT('Ctrl Pts',(373.37883132897,-9.31409001382978,1.97778424931847));
#34803=CARTESIAN_POINT('Ctrl Pts',(373.389178127794,-9.31304180923482,1.96440537333118));
#34804=CARTESIAN_POINT('Ctrl Pts',(373.394685447933,-9.31248297245838,1.95722182646843));
#34805=CARTESIAN_POINT('Ctrl Pts',(373.409927854732,-9.31093346841135,1.9371657517056));
#34806=CARTESIAN_POINT('Ctrl Pts',(373.419596775547,-9.30994729767633,1.92424295452978));
#34807=CARTESIAN_POINT('Ctrl Pts',(373.476162334993,-9.30415496411573,1.84744538910572));
#34808=CARTESIAN_POINT('Ctrl Pts',(373.520791292912,-9.2994900068193,1.78192575243756));
#34809=CARTESIAN_POINT('Ctrl Pts',(373.676875412186,-9.28254382888852,1.53356284640514));
#34810=CARTESIAN_POINT('Ctrl Pts',(373.772449935031,-9.27081910472854,1.34139487439183));
#34811=CARTESIAN_POINT('Ctrl Pts',(373.905534919934,-9.24961746995725,0.989900031823699));
#34812=CARTESIAN_POINT('Ctrl Pts',(373.951330776188,-9.24032890708503,0.834564118866942));
#34813=CARTESIAN_POINT('Ctrl Pts',(373.990963030249,-9.22902519565164,0.649956575266833));
#34814=CARTESIAN_POINT('Ctrl Pts',(373.996317980896,-9.22739231734514,0.62338386927893));
#34815=CARTESIAN_POINT('Ctrl Pts',(374.004563418352,-9.22469235787126,0.579624215887875));
#34816=CARTESIAN_POINT('Ctrl Pts',(374.007650885082,-9.22363153791964,0.562475444112357));
#34817=CARTESIAN_POINT('Ctrl Pts',(374.012962870042,-9.22171222410289,0.53153417600609));
#34818=CARTESIAN_POINT('Ctrl Pts',(374.015237070075,-9.22085532973306,0.517750566732708));
#34819=CARTESIAN_POINT('Ctrl Pts',(374.019907897939,-9.21901703227588,0.488248339236894));
#34820=CARTESIAN_POINT('Ctrl Pts',(374.022277951556,-9.21803481196214,0.472525947138395));
#34821=CARTESIAN_POINT('Ctrl Pts',(374.028407436891,-9.2153532185202,0.429717432479312));
#34822=CARTESIAN_POINT('Ctrl Pts',(374.031938554337,-9.21364670288811,0.402600444660568));
#34823=CARTESIAN_POINT('Ctrl Pts',(374.049518557405,-9.20416905991896,0.252723461269151));
#34824=CARTESIAN_POINT('Ctrl Pts',(374.056841966402,-9.19618925733215,0.129292913971071));
#34825=CARTESIAN_POINT('Ctrl Pts',(374.05732994103,-9.17816558293361,-0.143793467991667));
#34826=CARTESIAN_POINT('Ctrl Pts',(374.047186826692,-9.16805883277381,-0.293173302346878));
#34827=CARTESIAN_POINT('Ctrl Pts',(374.003536190119,-9.14649399125949,-0.608946596703439));
#34828=CARTESIAN_POINT('Ctrl Pts',(373.967188941042,-9.13506495643688,-0.774525891563327));
#34829=CARTESIAN_POINT('Ctrl Pts',(373.910172669352,-9.12245901464209,-0.962268236715053));
#34830=CARTESIAN_POINT('Ctrl Pts',(373.9020228287,-9.12074338881162,-0.987941953141894));
#34831=CARTESIAN_POINT('Ctrl Pts',(373.890305339226,-9.11839421360435,-1.02331061328434));
#34832=CARTESIAN_POINT('Ctrl Pts',(373.887011793877,-9.11774591013995,-1.03309430226435));
#34833=CARTESIAN_POINT('Ctrl Pts',(373.881275338012,-9.11663726360898,-1.04986783374305));
#34834=CARTESIAN_POINT('Ctrl Pts',(373.878855269032,-9.11617561371591,-1.05686532197827));
#34835=CARTESIAN_POINT('Ctrl Pts',(373.873739213191,-9.11521233309134,-1.0714946899445));
#34836=CARTESIAN_POINT('Ctrl Pts',(373.871038561442,-9.11471100102112,-1.07912483803275));
#34837=CARTESIAN_POINT('Ctrl Pts',(373.864350528575,-9.11348666101865,-1.09779659408055));
#34838=CARTESIAN_POINT('Ctrl Pts',(373.860331457331,-9.11276550770738,-1.10882688158799));
#34839=CARTESIAN_POINT('Ctrl Pts',(373.845497517911,-9.11015524633411,-1.14885705000511));
#34840=CARTESIAN_POINT('Ctrl Pts',(373.834324931301,-9.10828611270239,-1.17772373097182));
#34841=CARTESIAN_POINT('Ctrl Pts',(373.805207972477,-9.10363859445548,-1.24984890662164));
#34842=CARTESIAN_POINT('Ctrl Pts',(373.786732975756,-9.10088608509017,-1.29288660285058));
#34843=CARTESIAN_POINT('Ctrl Pts',(373.628200862637,-9.07867107788594,-1.64105058824508));
#34844=CARTESIAN_POINT('Ctrl Pts',(373.442188700875,-9.060786765978,-1.92298691041463));
#34845=CARTESIAN_POINT('Ctrl Pts',(373.172635579764,-9.03736684685816,-2.21867663895522));
#34846=CARTESIAN_POINT('Ctrl Pts',(373.127886259431,-9.03355110023065,-2.26490594744137));
#34847=CARTESIAN_POINT('Ctrl Pts',(373.065375173721,-9.02829619794196,-2.32573108469422));
#34848=CARTESIAN_POINT('Ctrl Pts',(373.048795225766,-9.02690931525824,-2.34152338674893));
#34849=CARTESIAN_POINT('Ctrl Pts',(373.021128231472,-9.0246054763901,-2.36731934090845));
#34850=CARTESIAN_POINT('Ctrl Pts',(373.010137257783,-9.02369292082535,-2.37742516164395));
#34851=CARTESIAN_POINT('Ctrl Pts',(372.98852066386,-9.02190309580222,-2.3970254172284));
#34852=CARTESIAN_POINT('Ctrl Pts',(372.977901503438,-9.02102613677911,-2.40652648528043));
#34853=CARTESIAN_POINT('Ctrl Pts',(372.95262108032,-9.01894360036062,-2.42884504097996));
#34854=CARTESIAN_POINT('Ctrl Pts',(372.937906087321,-9.01773548686279,-2.44160056309272));
#34855=CARTESIAN_POINT('Ctrl Pts',(372.888176487528,-9.01366557316071,-2.48392483158043));
#34856=CARTESIAN_POINT('Ctrl Pts',(372.85264824625,-9.0107790035216,-2.51287881451377));
#34857=CARTESIAN_POINT('Ctrl Pts',(372.766007813455,-9.00378610675437,-2.58046408540649));
#34858=CARTESIAN_POINT('Ctrl Pts',(372.714338988455,-8.99965278418863,-2.61834692889301));
#34859=CARTESIAN_POINT('Ctrl Pts',(372.50654368449,-8.98317565633936,-2.76137681311871));
#34860=CARTESIAN_POINT('Ctrl Pts',(372.342472802998,-8.9704505851579,-2.8542943230937));
#34861=CARTESIAN_POINT('Ctrl Pts',(372.024946931316,-8.94684943402383,-2.99906237760608));
#34862=CARTESIAN_POINT('Ctrl Pts',(371.873838512743,-8.93601484324683,-3.0547306722474));
#34863=CARTESIAN_POINT('Ctrl Pts',(371.693262896961,-8.92394927217498,-3.10629331854499));
#34864=CARTESIAN_POINT('Ctrl Pts',(371.667239640493,-8.92223153189595,-3.11337215503224));
#34865=CARTESIAN_POINT('Ctrl Pts',(371.631131117034,-8.91987999810629,-3.12270921475377));
#34866=CARTESIAN_POINT('Ctrl Pts',(371.621120074106,-8.91923141176799,-3.12524662855973));
#34867=CARTESIAN_POINT('Ctrl Pts',(371.603909957456,-8.91812240905198,-3.12952079283518));
#34868=CARTESIAN_POINT('Ctrl Pts',(371.596716850296,-8.91766068402621,-3.13128091546647));
#34869=CARTESIAN_POINT('Ctrl Pts',(371.581650141689,-8.91669739252614,-3.13491267937807));
#34870=CARTESIAN_POINT('Ctrl Pts',(371.573775470693,-8.91619612388408,-3.13677947749655));
#34871=CARTESIAN_POINT('Ctrl Pts',(371.554466171337,-8.91497217861105,-3.14128025617816));
#34872=CARTESIAN_POINT('Ctrl Pts',(371.543023887539,-8.91425135380599,-3.14388152046965));
#34873=CARTESIAN_POINT('Ctrl Pts',(371.501385863074,-8.91164364383092,-3.15310854453773));
#34874=CARTESIAN_POINT('Ctrl Pts',(371.471108337201,-8.90977668199887,-3.15936247730658));
#34875=CARTESIAN_POINT('Ctrl Pts',(371.394826943607,-8.90513568987098,-3.17397746006157));
#34876=CARTESIAN_POINT('Ctrl Pts',(371.348721320573,-8.90238744192274,-3.18177511176734));
#34877=CARTESIAN_POINT('Ctrl Pts',(370.972215557926,-8.88028805195974,-3.23705331939835));
#34878=CARTESIAN_POINT('Ctrl Pts',(370.636435223777,-8.8625006098788,-3.2339467583194));
#34879=CARTESIAN_POINT('Ctrl Pts',(370.242047286525,-8.83912076040069,-3.16854539704267));
#34880=CARTESIAN_POINT('Ctrl Pts',(370.177355306584,-8.83521243613071,-3.15576673338328));
#34881=CARTESIAN_POINT('Ctrl Pts',(370.090577235932,-8.82984924984167,-3.13584145923221));
#34882=CARTESIAN_POINT('Ctrl Pts',(370.06810740405,-8.82844954180482,-3.13042701052146));
#34883=CARTESIAN_POINT('Ctrl Pts',(370.031176443963,-8.82613002043022,-3.12110649486808));
#34884=CARTESIAN_POINT('Ctrl Pts',(370.016680615896,-8.82521473144255,-3.11734040679316));
#34885=CARTESIAN_POINT('Ctrl Pts',(369.988468987625,-8.82342370563535,-3.10980057444666));
#34886=CARTESIAN_POINT('Ctrl Pts',(369.974750867716,-8.82254830934492,-3.10603678396981));
#34887=CARTESIAN_POINT('Ctrl Pts',(369.942447845319,-8.82047612227923,-3.09694353277807));
#34888=CARTESIAN_POINT('Ctrl Pts',(369.923885256421,-8.81927686426009,-3.09153745194477));
#34889=CARTESIAN_POINT('Ctrl Pts',(369.86228578262,-8.81526821728355,-3.07299461893091));
#34890=CARTESIAN_POINT('Ctrl Pts',(369.819477036711,-8.81243506504613,-3.05912406793632));
#34891=CARTESIAN_POINT('Ctrl Pts',(369.717904046284,-8.80559583727269,-3.02384655322788));
#34892=CARTESIAN_POINT('Ctrl Pts',(369.659446730677,-8.80156431086839,-3.00161702765854));
#34893=CARTESIAN_POINT('Ctrl Pts',(369.289577077117,-8.77544341746029,-2.84850675220071));
#34894=CARTESIAN_POINT('Ctrl Pts',(368.999790558607,-8.75185733027583,-2.67108026706115));
#34895=CARTESIAN_POINT('Ctrl Pts',(368.714077869421,-8.72751766118726,-2.42737126107469));
#34896=CARTESIAN_POINT('Ctrl Pts',(368.685727653493,-8.72509219348832,-2.40231331664379));
#34897=CARTESIAN_POINT('Ctrl Pts',(368.648153858862,-8.72187114619697,-2.36790550415481));
#34898=CARTESIAN_POINT('Ctrl Pts',(368.638537771904,-8.72104621490378,-2.35899116893977));
#34899=CARTESIAN_POINT('Ctrl Pts',(368.6234700361,-8.71975306463301,-2.34485106328122));
#34900=CARTESIAN_POINT('Ctrl Pts',(368.617982014262,-8.7192819547028,-2.33966451252136));
#34901=CARTESIAN_POINT('Ctrl Pts',(368.606728257555,-8.71831575569929,-2.32895382372231));
#34902=CARTESIAN_POINT('Ctrl Pts',(368.600964789967,-8.71782086879321,-2.32342751461853));
#34903=CARTESIAN_POINT('Ctrl Pts',(368.587672132874,-8.71667919427406,-2.3105866696381));
#34904=CARTESIAN_POINT('Ctrl Pts',(368.580157951719,-8.71603359993077,-2.30325658498164));
#34905=CARTESIAN_POINT('Ctrl Pts',(368.555524355962,-8.71391588625051,-2.27899048886646));
#34906=CARTESIAN_POINT('Ctrl Pts',(368.538558484274,-8.71245530964267,-2.26189885925911));
#34907=CARTESIAN_POINT('Ctrl Pts',(368.497829716912,-8.70893910993424,-2.21993777743265));
#34908=CARTESIAN_POINT('Ctrl Pts',(368.474269872882,-8.70689672524812,-2.19487454480052));
#34909=CARTESIAN_POINT('Ctrl Pts',(368.385724278261,-8.6991658851745,-2.0976041319295));
#34910=CARTESIAN_POINT('Ctrl Pts',(368.323610172938,-8.69362542709458,-2.02284531400815));
#34911=CARTESIAN_POINT('Ctrl Pts',(368.190413642978,-8.68118128868767,-1.84692738991976));
#34912=CARTESIAN_POINT('Ctrl Pts',(368.121583524464,-8.67432377286514,-1.74426015045791));
#34913=CARTESIAN_POINT('Ctrl Pts',(367.964323094424,-8.65695042181107,-1.47777372018729));
#34914=CARTESIAN_POINT('Ctrl Pts',(367.883876583687,-8.6463531005557,-1.30979717732786));
#34915=CARTESIAN_POINT('Ctrl Pts',(367.808675775431,-8.63358351280057,-1.11011836402132));
#34916=CARTESIAN_POINT('Ctrl Pts',(367.799319883033,-8.63192849258957,-1.08427856924537));
#34917=CARTESIAN_POINT('Ctrl Pts',(367.784536501266,-8.62919939233742,-1.04175757560133));
#34918=CARTESIAN_POINT('Ctrl Pts',(367.778912609586,-8.62813181088882,-1.02514580393077));
#34919=CARTESIAN_POINT('Ctrl Pts',(367.7690499777,-8.62620516760918,-0.995211460094527));
#34920=CARTESIAN_POINT('Ctrl Pts',(367.764761783044,-8.62534775895542,-0.981905556206899));
#34921=CARTESIAN_POINT('Ctrl Pts',(367.755804455931,-8.62351370061803,-0.95347954156082));
#34922=CARTESIAN_POINT('Ctrl Pts',(367.751159859272,-8.62253627257639,-0.938352142615064));
#34923=CARTESIAN_POINT('Ctrl Pts',(367.738893040261,-8.61988128451211,-0.897324737810711));
#34924=CARTESIAN_POINT('Ctrl Pts',(367.731484697227,-8.61819681978445,-0.87136260683261));
#34925=CARTESIAN_POINT('Ctrl Pts',(367.715862537183,-8.61445725475984,-0.813888406633107));
#34926=CARTESIAN_POINT('Ctrl Pts',(367.707798480677,-8.61239755177541,-0.782339047878178));
#34927=CARTESIAN_POINT('Ctrl Pts',(367.641095844426,-8.59415230024176,-0.503851933487073));
#34928=CARTESIAN_POINT('Ctrl Pts',(367.611353684704,-8.57703667973339,-0.250959089753795));
#34929=CARTESIAN_POINT('Ctrl Pts',(367.611569014087,-8.55988254489073,0.00273538678758171));
#34930=CARTESIAN_POINT('Ctrl Pts',(367.611569016176,-8.5598823785129,0.00273784736845979));
#34931=CARTESIAN_POINT('Ctrl Pts',(367.611710073435,-8.54865520450604,0.168777824769111));
#34932=CARTESIAN_POINT('Ctrl Pts',(367.624682860913,-8.5374813403058,0.334581747335591));
#34933=CARTESIAN_POINT('Ctrl Pts',(367.652687367032,-8.52592348092959,0.513387817692194));
#34934=CARTESIAN_POINT('Ctrl Pts',(367.655095167938,-8.52497669480409,0.528093493947375));
#34935=CARTESIAN_POINT('Ctrl Pts',(367.659221475309,-8.52342866708339,0.552243314487704));
#34936=CARTESIAN_POINT('Ctrl Pts',(367.660880301606,-8.52282437709589,0.561697248361017));
#34937=CARTESIAN_POINT('Ctrl Pts',(367.664185425579,-8.52165470049485,0.580051615344668));
#34938=CARTESIAN_POINT('Ctrl Pts',(367.665827030268,-8.5210890652104,0.588952795079713));
#34939=CARTESIAN_POINT('Ctrl Pts',(367.668964487263,-8.52003614966302,0.605571987683803));
#34940=CARTESIAN_POINT('Ctrl Pts',(367.670451067393,-8.51954838270824,0.613291388094639));
#34941=CARTESIAN_POINT('Ctrl Pts',(367.673915194919,-8.51843662218971,0.630931795346051));
#34942=CARTESIAN_POINT('Ctrl Pts',(367.675911218284,-8.51781368197542,0.64084898986419));
#34943=CARTESIAN_POINT('Ctrl Pts',(367.68135611575,-8.51615994237848,0.667258362000366));
#34944=CARTESIAN_POINT('Ctrl Pts',(367.684887732579,-8.515133641166,0.683733414723344));
#34945=CARTESIAN_POINT('Ctrl Pts',(367.717434045385,-8.50606631976406,0.829957434330452));
#34946=CARTESIAN_POINT('Ctrl Pts',(367.754326454239,-8.49842584579882,0.957838955793525));
#34947=CARTESIAN_POINT('Ctrl Pts',(367.833825202285,-8.48505898317226,1.18062999785816));
#34948=CARTESIAN_POINT('Ctrl Pts',(367.873313215786,-8.47929114719,1.27643866269208));
#34949=CARTESIAN_POINT('Ctrl Pts',(367.95610779294,-8.46839233689487,1.45269961353418));
#34950=CARTESIAN_POINT('Ctrl Pts',(367.998352062536,-8.46327302329506,1.53353397823649));
#34951=CARTESIAN_POINT('Ctrl Pts',(368.103258836621,-8.45132299681722,1.71507383420621));
#34952=CARTESIAN_POINT('Ctrl Pts',(368.168161612095,-8.44444675266607,1.81432306891983));
#34953=CARTESIAN_POINT('Ctrl Pts',(368.257749982054,-8.43541423760068,1.93610028770842));
#34954=CARTESIAN_POINT('Ctrl Pts',(368.277521821667,-8.43344645502713,1.96213665524159));
#34955=CARTESIAN_POINT('Ctrl Pts',(368.308191949848,-8.43042989292646,2.00127349334745));
#34956=CARTESIAN_POINT('Ctrl Pts',(368.318804062212,-8.42939242109623,2.01459624360935));
#34957=CARTESIAN_POINT('Ctrl Pts',(368.338294879654,-8.42749792103585,2.03867145611712));
#34958=CARTESIAN_POINT('Ctrl Pts',(368.347138761054,-8.42664230654933,2.04945166919761));
#34959=CARTESIAN_POINT('Ctrl Pts',(368.366402777224,-8.42478698494851,2.07262512393192));
#34960=CARTESIAN_POINT('Ctrl Pts',(368.37684687266,-8.42378631415337,2.08499786357069));
#34961=CARTESIAN_POINT('Ctrl Pts',(368.40556256551,-8.42104873819463,2.1185007992694));
#34962=CARTESIAN_POINT('Ctrl Pts',(368.424016035646,-8.41930435799133,2.13947258766219));
#34963=CARTESIAN_POINT('Ctrl Pts',(368.523877736363,-8.40994029135481,2.25003038381158));
#34964=CARTESIAN_POINT('Ctrl Pts',(368.610003139831,-8.40212161839698,2.33520626645115));
#34965=CARTESIAN_POINT('Ctrl Pts',(368.857147886366,-8.38036315177978,2.55352473298532));
#34966=CARTESIAN_POINT('Ctrl Pts',(369.026639745582,-8.36611442495966,2.67618701099045));
#34967=CARTESIAN_POINT('Ctrl Pts',(369.280675047732,-8.34632871629645,2.82482596858817));
#34968=CARTESIAN_POINT('Ctrl Pts',(369.356270036233,-8.34062382844952,2.8651045815561));
#34969=CARTESIAN_POINT('Ctrl Pts',(369.461953680405,-8.33297274252521,2.91611737569494));
#34970=CARTESIAN_POINT('Ctrl Pts',(369.490726674257,-8.33092165918123,2.92948576935605));
#34971=CARTESIAN_POINT('Ctrl Pts',(369.540551523768,-8.32743017097682,2.95174662694954));
#34972=CARTESIAN_POINT('Ctrl Pts',(369.561508775393,-8.32597963866046,2.96084389745094));
#34973=CARTESIAN_POINT('Ctrl Pts',(369.59213729467,-8.32388771728713,2.97375402578185));
#34974=CARTESIAN_POINT('Ctrl Pts',(369.601732540538,-8.32323632750502,2.97774394464626));
#34975=CARTESIAN_POINT('Ctrl Pts',(369.618656140426,-8.32209461736922,2.9846853389217));
#34976=CARTESIAN_POINT('Ctrl Pts',(369.625976291165,-8.32160313956004,2.98765638034294));
#34977=CARTESIAN_POINT('Ctrl Pts',(369.641537313387,-8.32056343174632,2.99390560959195));
#34978=CARTESIAN_POINT('Ctrl Pts',(369.64978083243,-8.32001562209281,2.99717671587013));
#34979=CARTESIAN_POINT('Ctrl Pts',(369.672285079689,-8.31852797463428,3.00599926418696));
#34980=CARTESIAN_POINT('Ctrl Pts',(369.686572220416,-8.31759206600672,3.01148331005089));
#34981=CARTESIAN_POINT('Ctrl Pts',(369.754761254107,-8.31316331518592,3.03710155205793));
#34982=CARTESIAN_POINT('Ctrl Pts',(369.809160345929,-8.30974303628744,3.05589287830984));
#34983=CARTESIAN_POINT('Ctrl Pts',(369.904320288055,-8.30390669536128,3.08593690536323));
#34984=CARTESIAN_POINT('Ctrl Pts',(369.944851123363,-8.3014660611637,3.09786236649158));
#34985=CARTESIAN_POINT('Ctrl Pts',(370.057384557568,-8.29478493070474,3.12858247710776));
#34986=CARTESIAN_POINT('Ctrl Pts',(370.129822672428,-8.29059037874307,3.14568608802348));
#34987=CARTESIAN_POINT('Ctrl Pts',(370.326783099405,-8.2793246359618,3.18504540739398));
#34988=CARTESIAN_POINT('Ctrl Pts',(370.452125370521,-8.2722996112935,3.20250438614265));
#34989=CARTESIAN_POINT('Ctrl Pts',(370.735459976461,-8.25624423185949,3.22509574663828));
#34990=CARTESIAN_POINT('Ctrl Pts',(370.893441169133,-8.24716430606265,3.22606738962386));
#34991=CARTESIAN_POINT('Ctrl Pts',(371.079752218701,-8.23597487965228,3.2135212557643));
#34992=CARTESIAN_POINT('Ctrl Pts',(371.108629580974,-8.23422730335871,3.21118512113918));
#34993=CARTESIAN_POINT('Ctrl Pts',(371.153650157234,-8.23148041914378,3.20693132912214));
#34994=CARTESIAN_POINT('Ctrl Pts',(371.16981745274,-8.23048947741362,3.2052802800547));
#34995=CARTESIAN_POINT('Ctrl Pts',(371.198438471837,-8.22872693759028,3.20213851040646));
#34996=CARTESIAN_POINT('Ctrl Pts',(371.210897364925,-8.22795691110852,3.2006972254573));
#34997=CARTESIAN_POINT('Ctrl Pts',(371.239594160215,-8.22617673326256,3.19720761575582));
#34998=CARTESIAN_POINT('Ctrl Pts',(371.25582539991,-8.22516499189884,3.19510826037917));
#34999=CARTESIAN_POINT('Ctrl Pts',(371.300481151716,-8.22236776516191,3.18898627473215));
#35000=CARTESIAN_POINT('Ctrl Pts',(371.328868455988,-8.22057425551758,3.18470741151137));
#35001=CARTESIAN_POINT('Ctrl Pts',(371.490987138291,-8.21024099090766,3.15805122471671));
#35002=CARTESIAN_POINT('Ctrl Pts',(371.623241172016,-8.20144870670018,3.12763389163054));
#35003=CARTESIAN_POINT('Ctrl Pts',(371.945317704611,-8.17916813330987,3.03182834146058));
#35004=CARTESIAN_POINT('Ctrl Pts',(372.131675733991,-8.16547659336062,2.95687880945177));
#35005=CARTESIAN_POINT('Ctrl Pts',(372.309820650725,-8.15202831126679,2.86513683042647));
#35006=CARTESIAN_POINT('Ctrl Pts',(372.309820607824,-7.90820793933159,2.86513685252009));
#35007=CARTESIAN_POINT('Ctrl Pts',(372.280086990719,-7.91046518366678,2.88044922194635));
#35008=CARTESIAN_POINT('Ctrl Pts',(372.250105592529,-7.91271861207407,2.89530359235541));
#35009=CARTESIAN_POINT('Ctrl Pts',(372.123144234145,-7.92215390123291,2.95576140355205));
#35010=CARTESIAN_POINT('Ctrl Pts',(372.024154646074,-7.92925280294976,2.99698043300587));
#35011=CARTESIAN_POINT('Ctrl Pts',(371.90064077752,-7.93765725365726,3.04132404111153));
#35012=CARTESIAN_POINT('Ctrl Pts',(371.877903717594,-7.9391859834764,3.04920073553008));
#35013=CARTESIAN_POINT('Ctrl Pts',(371.845001799018,-7.94136957640213,3.06018764390311));
#35014=CARTESIAN_POINT('Ctrl Pts',(371.834907045115,-7.94203568195476,3.0635031794916));
#35015=CARTESIAN_POINT('Ctrl Pts',(371.817271076785,-7.94319246436888,3.06919908971726));
#35016=CARTESIAN_POINT('Ctrl Pts',(371.80973723436,-7.94368442135543,3.07160172031258));
#35017=CARTESIAN_POINT('Ctrl Pts',(371.793734337252,-7.94472466543712,3.07664041460402));
#35018=CARTESIAN_POINT('Ctrl Pts',(371.785263200904,-7.94527253492709,3.07926926083995));
#35019=CARTESIAN_POINT('Ctrl Pts',(371.762161253595,-7.94675935033236,3.08633405820965));
#35020=CARTESIAN_POINT('Ctrl Pts',(371.747509345397,-7.94769437851849,3.09070099076668));
#35021=CARTESIAN_POINT('Ctrl Pts',(371.677823149475,-7.95210625765782,3.11093181213383));
#35022=CARTESIAN_POINT('Ctrl Pts',(371.622399981856,-7.9555112425893,3.12543203121512));
#35023=CARTESIAN_POINT('Ctrl Pts',(371.529803482967,-7.96107326358394,3.14703769447499));
#35024=CARTESIAN_POINT('Ctrl Pts',(371.492841385017,-7.9632604330401,3.1549791524786));
#35025=CARTESIAN_POINT('Ctrl Pts',(371.373907483905,-7.97021662422249,3.17835129379364));
#35026=CARTESIAN_POINT('Ctrl Pts',(371.291471179694,-7.97491538445874,3.19125145335398));
#35027=CARTESIAN_POINT('Ctrl Pts',(371.047721419616,-7.98867206365104,3.21975469172786));
#35028=CARTESIAN_POINT('Ctrl Pts',(370.885630253705,-7.99765689301431,3.22641078265614));
#35029=CARTESIAN_POINT('Ctrl Pts',(370.602659606326,-8.01382900628593,3.2166951716844));
#35030=CARTESIAN_POINT('Ctrl Pts',(370.481929849426,-8.02088202712811,3.20571541323337));
#35031=CARTESIAN_POINT('Ctrl Pts',(370.335191684674,-8.02978393543228,3.18398041564805));
#35032=CARTESIAN_POINT('Ctrl Pts',(370.308322637838,-8.03142738105898,3.17965205389522));
#35033=CARTESIAN_POINT('Ctrl Pts',(370.26586856675,-8.03404674330235,3.17226025329552));
#35034=CARTESIAN_POINT('Ctrl Pts',(370.250245461198,-8.03501554826466,3.16942094596043));
#35035=CARTESIAN_POINT('Ctrl Pts',(370.220903815099,-8.0368445111308,3.16386414842194));
#35036=CARTESIAN_POINT('Ctrl Pts',(370.207180696864,-8.03770382449859,3.16117258452826));
#35037=CARTESIAN_POINT('Ctrl Pts',(370.176338439494,-8.03964409371157,3.15491464703476));
#35038=CARTESIAN_POINT('Ctrl Pts',(370.159230039825,-8.04072662942793,3.1512981077441));
#35039=CARTESIAN_POINT('Ctrl Pts',(370.115500467723,-8.04351002337406,3.14168168229503));
#35040=CARTESIAN_POINT('Ctrl Pts',(370.088924950514,-8.04521719513872,3.13548266995461));
#35041=CARTESIAN_POINT('Ctrl Pts',(369.898860192772,-8.05754191029404,3.0885952364427));
#35042=CARTESIAN_POINT('Ctrl Pts',(369.73872979055,-8.06856056585794,3.03548561696092));
#35043=CARTESIAN_POINT('Ctrl Pts',(369.391753120084,-8.09375346791797,2.88936216438681));
#35044=CARTESIAN_POINT('Ctrl Pts',(369.208279525975,-8.10801324738904,2.79023369857103));
#35045=CARTESIAN_POINT('Ctrl Pts',(368.970692334742,-8.12698279462253,2.63042670521092));
#35046=CARTESIAN_POINT('Ctrl Pts',(368.907349021084,-8.13209018822261,2.58438348545078));
#35047=CARTESIAN_POINT('Ctrl Pts',(368.833075972817,-8.13808215731996,2.52614478967241));
#35048=CARTESIAN_POINT('Ctrl Pts',(368.820485809273,-8.13909796617689,2.51611944987794));
#35049=CARTESIAN_POINT('Ctrl Pts',(368.800937002428,-8.14067467146286,2.50031232135528));
#35050=CARTESIAN_POINT('Ctrl Pts',(368.793926906349,-8.1412399582074,2.49459499264479));
#35051=CARTESIAN_POINT('Ctrl Pts',(368.780863494022,-8.14229301839339,2.48384876462252));
#35052=CARTESIAN_POINT('Ctrl Pts',(368.774804568482,-8.14278127261454,2.47882724737233));
#35053=CARTESIAN_POINT('Ctrl Pts',(368.760978202766,-8.14389517052357,2.46728254054745));
#35054=CARTESIAN_POINT('Ctrl Pts',(368.753223116981,-8.14451975002664,2.46074483567939));
#35055=CARTESIAN_POINT('Ctrl Pts',(368.732607649836,-8.14617995528916,2.44319838648328));
#35056=CARTESIAN_POINT('Ctrl Pts',(368.719802732146,-8.14721103104995,2.43212457852127));
#35057=CARTESIAN_POINT('Ctrl Pts',(368.602484079485,-8.15666297402621,2.32903941019326));
#35058=CARTESIAN_POINT('Ctrl Pts',(368.503935995164,-8.16464417543573,2.23043414790647));
#35059=CARTESIAN_POINT('Ctrl Pts',(368.387882662782,-8.17456952934213,2.09819367433383));
#35060=CARTESIAN_POINT('Ctrl Pts',(368.364170342609,-8.17662825253761,2.07022539108675));
#35061=CARTESIAN_POINT('Ctrl Pts',(368.239858184967,-8.18762204986215,1.91842388925832));
#35062=CARTESIAN_POINT('Ctrl Pts',(368.148082930536,-8.19647654078909,1.78765521064309));
#35063=CARTESIAN_POINT('Ctrl Pts',(368.004770448704,-8.21246346180662,1.54733462404254));
#35064=CARTESIAN_POINT('Ctrl Pts',(367.949006095433,-8.21946769979819,1.44067843270663));
#35065=CARTESIAN_POINT('Ctrl Pts',(367.888116111698,-8.22831454150035,1.30642666780241));
#35066=CARTESIAN_POINT('Ctrl Pts',(367.877210216209,-8.22995484545603,1.28154972385356));
#35067=CARTESIAN_POINT('Ctrl Pts',(367.860433640642,-8.23257034421545,1.24192674102022));
#35068=CARTESIAN_POINT('Ctrl Pts',(367.854355048219,-8.23353846373981,1.22726973669558));
#35069=CARTESIAN_POINT('Ctrl Pts',(367.843122710824,-8.23536684163724,1.19961026756124));
#35070=CARTESIAN_POINT('Ctrl Pts',(367.837944873807,-8.23622626141706,1.18661793867848));
#35071=CARTESIAN_POINT('Ctrl Pts',(367.826477688442,-8.23816772173516,1.15729058029123));
#35072=CARTESIAN_POINT('Ctrl Pts',(367.820236561862,-8.23925135030846,1.14093728741634));
#35073=CARTESIAN_POINT('Ctrl Pts',(367.804587178898,-8.24203943674257,1.09890736046548));
#35074=CARTESIAN_POINT('Ctrl Pts',(367.795372103528,-8.24375024427384,1.07316075319971));
#35075=CARTESIAN_POINT('Ctrl Pts',(367.719352860111,-8.25847836583262,0.851931177819804));
#35076=CARTESIAN_POINT('Ctrl Pts',(367.671171783565,-8.27211457550284,0.650594435583398));
#35077=CARTESIAN_POINT('Ctrl Pts',(367.621842352533,-8.29613128936243,0.297628820466118));
#35078=CARTESIAN_POINT('Ctrl Pts',(367.611477319688,-8.30633729566589,0.147924090474079));
#35079=CARTESIAN_POINT('Ctrl Pts',(367.611595484732,-8.31930199709675,-0.0464266309118273));
#35080=CARTESIAN_POINT('Ctrl Pts',(367.612542851662,-8.32224784993948,-0.0908902097798106));
#35081=CARTESIAN_POINT('Ctrl Pts',(367.616739587707,-8.32879973082755,-0.190749436956861));
#35082=CARTESIAN_POINT('Ctrl Pts',(367.620500025738,-8.33238772592903,-0.246111879924262));
#35083=CARTESIAN_POINT('Ctrl Pts',(367.62710395784,-8.33686573344007,-0.316426615952528));
#35084=CARTESIAN_POINT('Ctrl Pts',(367.628625877529,-8.33782041940696,-0.331490198857738));
#35085=CARTESIAN_POINT('Ctrl Pts',(367.631204149121,-8.33932326440921,-0.355328368646034));
#35086=CARTESIAN_POINT('Ctrl Pts',(367.632190512579,-8.3398751842414,-0.364110079067891));
#35087=CARTESIAN_POINT('Ctrl Pts',(367.63412899826,-8.34091767433136,-0.380751269397729));
#35088=CARTESIAN_POINT('Ctrl Pts',(367.63507394976,-8.34140860954351,-0.388611224535128));
#35089=CARTESIAN_POINT('Ctrl Pts',(367.637362880658,-8.34255861599188,-0.407075821014035));
#35090=CARTESIAN_POINT('Ctrl Pts',(367.638730668435,-8.34321634959959,-0.417677354710722));
#35091=CARTESIAN_POINT('Ctrl Pts',(367.643396795445,-8.34536766636677,-0.452478567840202));
#35092=CARTESIAN_POINT('Ctrl Pts',(367.646917564716,-8.34684936931321,-0.476648228589994));
#35093=CARTESIAN_POINT('Ctrl Pts',(367.667874803233,-8.35496004467795,-0.609880497263251));
#35094=CARTESIAN_POINT('Ctrl Pts',(367.690635811715,-8.3613340615535,-0.718041730571144));
#35095=CARTESIAN_POINT('Ctrl Pts',(367.794062685897,-8.38426282485431,-1.10868821028692));
#35096=CARTESIAN_POINT('Ctrl Pts',(367.907650662578,-8.40019927814039,-1.3809283401776));
#35097=CARTESIAN_POINT('Ctrl Pts',(368.084294270505,-8.42070211348759,-1.6812153366278));
#35098=CARTESIAN_POINT('Ctrl Pts',(368.113248759935,-8.42396179906062,-1.72768549722269));
#35099=CARTESIAN_POINT('Ctrl Pts',(368.155200102014,-8.42856160374572,-1.79134243183714));
#35100=CARTESIAN_POINT('Ctrl Pts',(368.167207736691,-8.42986506810926,-1.8091719721473));
#35101=CARTESIAN_POINT('Ctrl Pts',(368.186864084206,-8.43197860263268,-1.83773769116824));
#35102=CARTESIAN_POINT('Ctrl Pts',(368.194402001872,-8.43278446625057,-1.84854958556695));
#35103=CARTESIAN_POINT('Ctrl Pts',(368.210226023406,-8.43446676269025,-1.87095233311898));
#35104=CARTESIAN_POINT('Ctrl Pts',(368.218523080912,-8.43534360369057,-1.88253506286116));
#35105=CARTESIAN_POINT('Ctrl Pts',(368.238309556923,-8.43742259020282,-1.9097737023508));
#35106=CARTESIAN_POINT('Ctrl Pts',(368.249864115778,-8.43862724150266,-1.92538139629195));
#35107=CARTESIAN_POINT('Ctrl Pts',(368.288932171767,-8.44266997912132,-1.97716848021377));
#35108=CARTESIAN_POINT('Ctrl Pts',(368.317068880426,-8.445532371904,-2.01286878287935));
#35109=CARTESIAN_POINT('Ctrl Pts',(368.38620945163,-8.45245486558623,-2.09687780221178));
#35110=CARTESIAN_POINT('Ctrl Pts',(368.427900205423,-8.45654123444005,-2.14459425201078));
#35111=CARTESIAN_POINT('Ctrl Pts',(368.642178747393,-8.47711837533822,-2.3757233866474));
#35112=CARTESIAN_POINT('Ctrl Pts',(368.834435899457,-8.49436476774445,-2.53968101669466));
#35113=CARTESIAN_POINT('Ctrl Pts',(369.137148184271,-8.51877219145563,-2.74195998620847));
#35114=CARTESIAN_POINT('Ctrl Pts',(369.233730580566,-8.52619606239747,-2.79943836340262));
#35115=CARTESIAN_POINT('Ctrl Pts',(369.347787486643,-8.53440170116251,-2.8594788935041));
#35116=CARTESIAN_POINT('Ctrl Pts',(369.362508231564,-8.53545036804817,-2.86708362932596));
#35117=CARTESIAN_POINT('Ctrl Pts',(369.386336786683,-8.53713037258166,-2.87916156644804));
#35118=CARTESIAN_POINT('Ctrl Pts',(369.395408003137,-8.53776587949882,-2.88370576596471));
#35119=CARTESIAN_POINT('Ctrl Pts',(369.411538065397,-8.53888854459019,-2.89169101050481));
#35120=CARTESIAN_POINT('Ctrl Pts',(369.418588191206,-8.53937674661113,-2.89514917637948));
#35121=CARTESIAN_POINT('Ctrl Pts',(369.433887041093,-8.5404307279767,-2.90258418543496));
#35122=CARTESIAN_POINT('Ctrl Pts',(369.442140099764,-8.54099593147818,-2.90655165457691));
#35123=CARTESIAN_POINT('Ctrl Pts',(369.465407992438,-8.54258025177585,-2.91761531896628));
#35124=CARTESIAN_POINT('Ctrl Pts',(369.480461174431,-8.54359454220465,-2.9246308274129));
#35125=CARTESIAN_POINT('Ctrl Pts',(369.575854256771,-8.54995908941189,-2.96819424163794));
#35126=CARTESIAN_POINT('Ctrl Pts',(369.657620342324,-8.55513363284189,-3.00154853061383));
#35127=CARTESIAN_POINT('Ctrl Pts',(370.011507173406,-8.5767672644845,-3.12921810364449));
#35128=CARTESIAN_POINT('Ctrl Pts',(370.294228938767,-8.5922973475263,-3.19019520220454));
#35129=CARTESIAN_POINT('Ctrl Pts',(370.667600248984,-8.61397741452302,-3.21959870439427));
#35130=CARTESIAN_POINT('Ctrl Pts',(370.754127713609,-8.61907070089868,-3.222914550765));
#35131=CARTESIAN_POINT('Ctrl Pts',(370.866206202885,-8.62580659224822,-3.22269333834952));
#35132=CARTESIAN_POINT('Ctrl Pts',(370.891731653546,-8.62734986083329,-3.22233964974608));
#35133=CARTESIAN_POINT('Ctrl Pts',(370.932754814432,-8.62984601932619,-3.22128364106536));
#35134=CARTESIAN_POINT('Ctrl Pts',(370.948256665357,-8.63079291850305,-3.22077258828468));
#35135=CARTESIAN_POINT('Ctrl Pts',(370.977793593374,-8.63260433022701,-3.2195853308684));
#35136=CARTESIAN_POINT('Ctrl Pts',(370.991829151669,-8.63346819381622,-3.21892919643937));
#35137=CARTESIAN_POINT('Ctrl Pts',(371.023943843725,-8.63545209835819,-3.21721735482709));
#35138=CARTESIAN_POINT('Ctrl Pts',(371.042019141172,-8.63657401386671,-3.21610100556774));
#35139=CARTESIAN_POINT('Ctrl Pts',(371.0981077301,-8.64007231940927,-3.21216210901745));
#35140=CARTESIAN_POINT('Ctrl Pts',(371.13607993156,-8.64246492162768,-3.20881753324871));
#35141=CARTESIAN_POINT('Ctrl Pts',(371.323065390468,-8.6543709789313,-3.18899964625002));
#35142=CARTESIAN_POINT('Ctrl Pts',(371.470843709041,-8.66418340480201,-3.16281788971042));
#35143=CARTESIAN_POINT('Ctrl Pts',(371.808019720595,-8.68740877898196,-3.07848978745767));
#35144=CARTESIAN_POINT('Ctrl Pts',(371.994964430348,-8.70093656470399,-3.01298701823323));
#35145=CARTESIAN_POINT('Ctrl Pts',(372.258324434379,-8.72023247264507,-2.89253752275486));
#35146=CARTESIAN_POINT('Ctrl Pts',(372.340256801282,-8.726265901354,-2.85074011217185));
#35147=CARTESIAN_POINT('Ctrl Pts',(372.434101420843,-8.73312241580129,-2.79768861184771));
#35148=CARTESIAN_POINT('Ctrl Pts',(372.447848604417,-8.73412538383268,-2.78978271029323));
#35149=CARTESIAN_POINT('Ctrl Pts',(372.470111171759,-8.73574657819729,-2.77676006328427));
#35150=CARTESIAN_POINT('Ctrl Pts',(372.478662054648,-8.73636853007917,-2.77170495966517));
#35151=CARTESIAN_POINT('Ctrl Pts',(372.493917045511,-8.73747659588031,-2.76259108389033));
#35152=CARTESIAN_POINT('Ctrl Pts',(372.500629837353,-8.73796364820118,-2.7585473262954));
#35153=CARTESIAN_POINT('Ctrl Pts',(372.515288894549,-8.7390260496834,-2.74964373610651));
#35154=CARTESIAN_POINT('Ctrl Pts',(372.523228864249,-8.73960074045243,-2.74477392861657));
#35155=CARTESIAN_POINT('Ctrl Pts',(372.545891413785,-8.74123922101606,-2.73073877537181));
#35156=CARTESIAN_POINT('Ctrl Pts',(372.560561533682,-8.74229764303158,-2.72148876513128));
#35157=CARTESIAN_POINT('Ctrl Pts',(372.664710263777,-8.74980125781713,-2.65463843694444));
#35158=CARTESIAN_POINT('Ctrl Pts',(372.751371734914,-8.75598996992613,-2.59274966585779));
#35159=CARTESIAN_POINT('Ctrl Pts',(373.010350760912,-8.7748321634107,-2.38770266431179));
#35160=CARTESIAN_POINT('Ctrl Pts',(373.170923815391,-8.78707004260135,-2.23081203975934));
#35161=CARTESIAN_POINT('Ctrl Pts',(373.39405240962,-8.80698051993958,-1.96204129408293));
#35162=CARTESIAN_POINT('Ctrl Pts',(373.468453722652,-8.81426622328595,-1.86095945832559));
#35163=CARTESIAN_POINT('Ctrl Pts',(373.552135841529,-8.82347335762787,-1.73215998039783));
#35164=CARTESIAN_POINT('Ctrl Pts',(373.56718835851,-8.82517475105587,-1.70831248317346));
#35165=CARTESIAN_POINT('Ctrl Pts',(373.590422957371,-8.82787528104109,-1.6704091044658));
#35166=CARTESIAN_POINT('Ctrl Pts',(373.598815135508,-8.82886669560793,-1.65648322735324));
#35167=CARTESIAN_POINT('Ctrl Pts',(373.614211714903,-8.83071596970691,-1.6304914329712));
#35168=CARTESIAN_POINT('Ctrl Pts',(373.62124386395,-8.83157279323784,-1.61844233639485));
#35169=CARTESIAN_POINT('Ctrl Pts',(373.636660077512,-8.83347868913804,-1.59162931583972));
#35170=CARTESIAN_POINT('Ctrl Pts',(373.645006106512,-8.83452910087984,-1.57684410968404));
#35171=CARTESIAN_POINT('Ctrl Pts',(373.668933256872,-8.83759572173967,-1.53366298663896));
#35172=CARTESIAN_POINT('Ctrl Pts',(373.68420324782,-8.83962290476539,-1.50509792302008));
#35173=CARTESIAN_POINT('Ctrl Pts',(373.795591967154,-8.85495618681343,-1.28895223108716));
#35174=CARTESIAN_POINT('Ctrl Pts',(373.873514766549,-8.86890196104991,-1.09260953094886));
#35175=CARTESIAN_POINT('Ctrl Pts',(373.994218893703,-8.89838177070537,-0.672581343437026));
#35176=CARTESIAN_POINT('Ctrl Pts',(374.03364455971,-8.91387318540343,-0.449068537048291));
#35177=CARTESIAN_POINT('Ctrl Pts',(374.051031039861,-8.929963350414,-0.198695842773865));
#35178=CARTESIAN_POINT('Ctrl Pts',(374.05245521497,-8.93152917483734,-0.174114241255168));
#35179=CARTESIAN_POINT('Ctrl Pts',(374.054059219456,-8.93370732945663,-0.139578312620742));
#35180=CARTESIAN_POINT('Ctrl Pts',(374.05447483004,-8.93433182340271,-0.129636497798358));
#35181=CARTESIAN_POINT('Ctrl Pts',(374.055142970111,-8.93545630637857,-0.111659113525762));
#35182=CARTESIAN_POINT('Ctrl Pts',(374.055411489563,-8.93595716670393,-0.103624233659263));
#35183=CARTESIAN_POINT('Ctrl Pts',(374.055898440098,-8.93697648770251,-0.087213965188911));
#35184=CARTESIAN_POINT('Ctrl Pts',(374.056114282651,-8.93749480269508,-0.0788385980667228));
#35185=CARTESIAN_POINT('Ctrl Pts',(374.056583116144,-8.93881681083265,-0.0574006034985904));
#35186=CARTESIAN_POINT('Ctrl Pts',(374.05678934283,-8.93961794002964,-0.0443369604012309));
#35187=CARTESIAN_POINT('Ctrl Pts',(374.057314010573,-8.9429164726124,0.00973007392690714));
#35188=CARTESIAN_POINT('Ctrl Pts',(374.056929353104,-8.94537754778542,0.0507383650268841));
#35189=CARTESIAN_POINT('Ctrl Pts',(374.053790212408,-8.95191054952937,0.160980788662421));
#35190=CARTESIAN_POINT('Ctrl Pts',(374.049585704021,-8.95592172200404,0.230154105139503));
#35191=CARTESIAN_POINT('Ctrl Pts',(374.029619917176,-8.96821056709524,0.444323061536362));
#35192=CARTESIAN_POINT('Ctrl Pts',(374.006247755122,-8.97629888771257,0.588423605037938));
#35193=CARTESIAN_POINT('Ctrl Pts',(373.926928661078,-8.99590137912172,0.929272088240766));
#35194=CARTESIAN_POINT('Ctrl Pts',(373.861882524801,-9.00747079204436,1.12322093847833));
#35195=CARTESIAN_POINT('Ctrl Pts',(373.767783107977,-9.02132862110302,1.33478564010711));
#35196=CARTESIAN_POINT('Ctrl Pts',(373.756307574278,-9.02298185513137,1.35972317252434));
#35197=CARTESIAN_POINT('Ctrl Pts',(373.736981758354,-9.02570901715247,1.40034542629178));
#35198=CARTESIAN_POINT('Ctrl Pts',(373.729319383169,-9.02677646923472,1.41611835020823));
#35199=CARTESIAN_POINT('Ctrl Pts',(373.715313669313,-9.02870354703405,1.44436019077459));
#35200=CARTESIAN_POINT('Ctrl Pts',(373.709017101887,-9.02956152441111,1.45685190496375));
#35201=CARTESIAN_POINT('Ctrl Pts',(373.695414818185,-9.03139753168407,1.48340582142249));
#35202=CARTESIAN_POINT('Ctrl Pts',(373.688086333106,-9.03237634637523,1.49745588343914));
#35203=CARTESIAN_POINT('Ctrl Pts',(373.667960981138,-9.03503696789336,1.53535557357796));
#35204=CARTESIAN_POINT('Ctrl Pts',(373.654967023997,-9.03672572201427,1.55909855278998));
#35205=CARTESIAN_POINT('Ctrl Pts',(373.583377403597,-9.04587906329855,1.6860846744109));
#35206=CARTESIAN_POINT('Ctrl Pts',(373.519416571169,-9.0535355239846,1.78618283356527));
#35207=CARTESIAN_POINT('Ctrl Pts',(373.359394680087,-9.07158455493074,2.00853436468186));
#35208=CARTESIAN_POINT('Ctrl Pts',(373.259720159933,-9.08207575872823,2.12782521489966));
#35209=CARTESIAN_POINT('Ctrl Pts',(373.034486012881,-9.10400256145632,2.36091118785168));
#35210=CARTESIAN_POINT('Ctrl Pts',(372.907748531155,-9.11540677438659,2.47296128975212));
#35211=CARTESIAN_POINT('Ctrl Pts',(372.751278684957,-9.12799060859756,2.59077296261676));
#35212=CARTESIAN_POINT('Ctrl Pts',(372.729553149703,-9.12970667999619,2.60670801113934));
#35213=CARTESIAN_POINT('Ctrl Pts',(372.699224948657,-9.13205666435531,2.62837321771799));
#35214=CARTESIAN_POINT('Ctrl Pts',(372.690791413357,-9.13270533652586,2.63433676160869));
#35215=CARTESIAN_POINT('Ctrl Pts',(372.676259281883,-9.13381466415075,2.64450831542047));
#35216=CARTESIAN_POINT('Ctrl Pts',(372.670174638739,-9.13427662756676,2.64873598583141));
#35217=CARTESIAN_POINT('Ctrl Pts',(372.657406982543,-9.13524063877535,2.65754194887807));
#35218=CARTESIAN_POINT('Ctrl Pts',(372.650721213465,-9.13574238699454,2.66211607902084));
#35219=CARTESIAN_POINT('Ctrl Pts',(372.634294188691,-9.13696790086603,2.67326408328522));
#35220=CARTESIAN_POINT('Ctrl Pts',(372.624533965104,-9.13768980728556,2.6798100585528));
#35221=CARTESIAN_POINT('Ctrl Pts',(372.588898999434,-9.14030374623606,2.7034281013089));
#35222=CARTESIAN_POINT('Ctrl Pts',(372.5628131861,-9.1421757402663,2.72018060855473));
#35223=CARTESIAN_POINT('Ctrl Pts',(372.496649094611,-9.14683131053973,2.76133548802704));
#35224=CARTESIAN_POINT('Ctrl Pts',(372.456271155149,-9.14958890736441,2.78524446962735));
#35225=CARTESIAN_POINT('Ctrl Pts',(372.380529333718,-9.15463595027393,2.82788746361087));
#35226=CARTESIAN_POINT('Ctrl Pts',(372.345335160387,-9.1569324153513,2.84684738925577));
#35227=CARTESIAN_POINT('Ctrl Pts',(372.309820498245,-9.15921048455975,2.86513690895141));
#35228=CARTESIAN_POINT('Origin',(370.834317853224,2.31077344927308,0.));
#35229=CARTESIAN_POINT('',(372.309820694103,-10.6540649855006,2.86513680808755));
#35230=CARTESIAN_POINT('',(372.30982057914,-10.4044982614434,2.86513686729153));
#35231=CARTESIAN_POINT('',(372.309820613641,2.31077344927308,2.86513684952399));
#35232=CARTESIAN_POINT('Ctrl Pts',(372.309820694103,-10.6540649855006,2.86513680808753));
#35233=CARTESIAN_POINT('Ctrl Pts',(372.415741525282,-10.6473842167664,2.81058915546863));
#35234=CARTESIAN_POINT('Ctrl Pts',(372.518580798336,-10.6406504991396,2.75019705918438));
#35235=CARTESIAN_POINT('Ctrl Pts',(372.689950599824,-10.6287318346147,2.63633005567726));
#35236=CARTESIAN_POINT('Ctrl Pts',(372.760076734383,-10.6236348626481,2.5855482700573));
#35237=CARTESIAN_POINT('Ctrl Pts',(372.847388158359,-10.6169502380564,2.51679758430738));
#35238=CARTESIAN_POINT('Ctrl Pts',(372.866531028819,-10.6154628004408,2.5013659651471));
#35239=CARTESIAN_POINT('Ctrl Pts',(372.897293933122,-10.613035709347,2.47598086920582));
#35240=CARTESIAN_POINT('Ctrl Pts',(372.909023179202,-10.6121014595408,2.46616085619295));
#35241=CARTESIAN_POINT('Ctrl Pts',(372.931425337172,-10.6102997498211,2.44713229312994));
#35242=CARTESIAN_POINT('Ctrl Pts',(372.942108637489,-10.6094328248293,2.43793647559723));
#35243=CARTESIAN_POINT('Ctrl Pts',(372.96644637373,-10.6074399092532,2.41670783489947));
#35244=CARTESIAN_POINT('Ctrl Pts',(372.980059799273,-10.6063120152557,2.40462892488927));
#35245=CARTESIAN_POINT('Ctrl Pts',(373.023043057009,-10.6027081602531,2.36583511495597));
#35246=CARTESIAN_POINT('Ctrl Pts',(373.052020967307,-10.6002142601995,2.33869332760768));
#35247=CARTESIAN_POINT('Ctrl Pts',(373.264490521334,-10.5814331886314,2.13218617716722));
#35248=CARTESIAN_POINT('Ctrl Pts',(373.426443558802,-10.5641845555086,1.93204392985168));
#35249=CARTESIAN_POINT('Ctrl Pts',(373.629624906426,-10.53835596795,1.60875283777286));
#35250=CARTESIAN_POINT('Ctrl Pts',(373.690075553573,-10.5298954413006,1.49882580397127));
#35251=CARTESIAN_POINT('Ctrl Pts',(373.761250745643,-10.5190223178478,1.34936888296517));
#35252=CARTESIAN_POINT('Ctrl Pts',(373.777850077721,-10.5164073757771,1.31276459435082));
#35253=CARTESIAN_POINT('Ctrl Pts',(373.804693393816,-10.5120507616063,1.25049960492534));
#35254=CARTESIAN_POINT('Ctrl Pts',(373.815299717004,-10.5102920479727,1.22500096351926));
#35255=CARTESIAN_POINT('Ctrl Pts',(373.829754117939,-10.5078442784519,1.18895126212215));
#35256=CARTESIAN_POINT('Ctrl Pts',(373.833876487293,-10.5071400020856,1.17851242218445));
#35257=CARTESIAN_POINT('Ctrl Pts',(373.840842876917,-10.5059393896853,1.16059846735347));
#35258=CARTESIAN_POINT('Ctrl Pts',(373.843713738303,-10.5054414766271,1.15313396138523));
#35259=CARTESIAN_POINT('Ctrl Pts',(373.849233797692,-10.5044780319269,1.1386202682177));
#35260=CARTESIAN_POINT('Ctrl Pts',(373.851886094659,-10.5040123039837,1.13157243622031));
#35261=CARTESIAN_POINT('Ctrl Pts',(373.859052311108,-10.5027460584633,1.11232558616725));
#35262=CARTESIAN_POINT('Ctrl Pts',(373.863517176132,-10.5019484094258,1.10010827910782));
#35263=CARTESIAN_POINT('Ctrl Pts',(373.880422393603,-10.4988929268736,1.05296681646964));
#35264=CARTESIAN_POINT('Ctrl Pts',(373.892334263822,-10.4966640817572,1.01785455082374));
#35265=CARTESIAN_POINT('Ctrl Pts',(373.970297874108,-10.4814759300663,0.774307632696504));
#35266=CARTESIAN_POINT('Ctrl Pts',(374.015601465828,-10.4694320878432,0.559804046312851));
#35267=CARTESIAN_POINT('Ctrl Pts',(374.053506787591,-10.4494456948658,0.204991168080699));
#35268=CARTESIAN_POINT('Ctrl Pts',(374.059333589791,-10.4416540011318,0.0668444972291463));
#35269=CARTESIAN_POINT('Ctrl Pts',(374.054537275212,-10.4290396379657,-0.150072582958748));
#35270=CARTESIAN_POINT('Ctrl Pts',(374.049901859715,-10.4243838796136,-0.228807595503647));
#35271=CARTESIAN_POINT('Ctrl Pts',(374.040112152152,-10.4182036649417,-0.331011139607474));
#35272=CARTESIAN_POINT('Ctrl Pts',(374.037576901499,-10.4167612575597,-0.354706758597773));
#35273=CARTESIAN_POINT('Ctrl Pts',(374.03300251922,-10.4143894342811,-0.393399232292983));
#35274=CARTESIAN_POINT('Ctrl Pts',(374.03112009593,-10.4134649634536,-0.408413953272359));
#35275=CARTESIAN_POINT('Ctrl Pts',(374.027272268394,-10.4116692263162,-0.437447180121927));
#35276=CARTESIAN_POINT('Ctrl Pts',(374.025320104872,-10.4107983974421,-0.451467111277666));
#35277=CARTESIAN_POINT('Ctrl Pts',(374.020592119474,-10.4087777317335,-0.483858524143309));
#35278=CARTESIAN_POINT('Ctrl Pts',(374.017749679383,-10.4076258131369,-0.50221962942411));
#35279=CARTESIAN_POINT('Ctrl Pts',(374.007992449998,-10.4038641473306,-0.56183331753423));
#35280=CARTESIAN_POINT('Ctrl Pts',(374.000433510625,-10.4012341729069,-0.602974711503038));
#35281=CARTESIAN_POINT('Ctrl Pts',(373.952074777466,-10.3858717522614,-0.840110843280658));
#35282=CARTESIAN_POINT('Ctrl Pts',(373.893889855258,-10.3725864559325,-1.03208036171677));
#35283=CARTESIAN_POINT('Ctrl Pts',(373.738344645398,-10.3447968384968,-1.41334230820427));
#35284=CARTESIAN_POINT('Ctrl Pts',(373.639286716143,-10.330335908604,-1.60095872227118));
#35285=CARTESIAN_POINT('Ctrl Pts',(373.504422093613,-10.3145559849695,-1.80492113770066));
#35286=CARTESIAN_POINT('Ctrl Pts',(373.485882370986,-10.3124567905547,-1.83204879058598));
#35287=CARTESIAN_POINT('Ctrl Pts',(373.460000085102,-10.3096248813643,-1.86870402526228));
#35288=CARTESIAN_POINT('Ctrl Pts',(373.453014987551,-10.3088700582358,-1.87848003614963));
#35289=CARTESIAN_POINT('Ctrl Pts',(373.441200678865,-10.3076094346248,-1.89482081042498));
#35290=CARTESIAN_POINT('Ctrl Pts',(373.436400993078,-10.3071016596251,-1.90140666564402));
#35291=CARTESIAN_POINT('Ctrl Pts',(373.427225254403,-10.3061392992245,-1.91389727620356));
#35292=CARTESIAN_POINT('Ctrl Pts',(373.422853917679,-10.3056843855036,-1.91980536005951));
#35293=CARTESIAN_POINT('Ctrl Pts',(373.412420466632,-10.3046068780036,-1.93380627716237));
#35294=CARTESIAN_POINT('Ctrl Pts',(373.406340358575,-10.3039855212452,-1.9418856920961));
#35295=CARTESIAN_POINT('Ctrl Pts',(373.384736728914,-10.3018002408709,-1.9703137195946));
#35296=CARTESIAN_POINT('Ctrl Pts',(373.369008484605,-10.3002498480299,-1.99050649112826));
#35297=CARTESIAN_POINT('Ctrl Pts',(373.221344187678,-10.2860412327013,-2.17549705016967));
#35298=CARTESIAN_POINT('Ctrl Pts',(373.073736493984,-10.2743315392092,-2.32716795294932));
#35299=CARTESIAN_POINT('Ctrl Pts',(372.73967997459,-10.2498908493973,-2.60897218066535));
#35300=CARTESIAN_POINT('Ctrl Pts',(372.552215875762,-10.2371887553865,-2.73604641797113));
#35301=CARTESIAN_POINT('Ctrl Pts',(372.325154975338,-10.2217948018951,-2.85736247829873));
#35302=CARTESIAN_POINT('Ctrl Pts',(372.297073551525,-10.219892015444,-2.8718393613519));
#35303=CARTESIAN_POINT('Ctrl Pts',(372.253735470561,-10.2169548854607,-2.89338100158729));
#35304=CARTESIAN_POINT('Ctrl Pts',(372.238628322626,-10.2159309391726,-2.90074336707067));
#35305=CARTESIAN_POINT('Ctrl Pts',(372.21100942225,-10.2140584665893,-2.91393692714074));
#35306=CARTESIAN_POINT('Ctrl Pts',(372.198516402964,-10.2132112985569,-2.919806568779));
#35307=CARTESIAN_POINT('Ctrl Pts',(372.171159133501,-10.2113555883724,-2.93244603073415));
#35308=CARTESIAN_POINT('Ctrl Pts',(372.156280414326,-10.2103459586,-2.93918344156425));
#35309=CARTESIAN_POINT('Ctrl Pts',(372.115246014143,-10.2075601374036,-2.95739010904267));
#35310=CARTESIAN_POINT('Ctrl Pts',(372.088988578359,-10.2057760280703,-2.96862501802488));
#35311=CARTESIAN_POINT('Ctrl Pts',(371.940027992579,-10.1956436316819,-3.0300322916562));
#35312=CARTESIAN_POINT('Ctrl Pts',(371.814485154875,-10.1870545093825,-3.07293912366423));
#35313=CARTESIAN_POINT('Ctrl Pts',(371.476374945725,-10.1638304929175,-3.16566433186801));
#35314=CARTESIAN_POINT('Ctrl Pts',(371.260772581709,-10.1488966286129,-3.20184218662922));
#35315=CARTESIAN_POINT('Ctrl Pts',(370.93883539114,-10.1273226578798,-3.22275202845005));
#35316=CARTESIAN_POINT('Ctrl Pts',(370.834195735814,-10.1204322204589,-3.22444709406019));
#35317=CARTESIAN_POINT('Ctrl Pts',(370.712389506187,-10.1126839171305,-3.22048897732294));
#35318=CARTESIAN_POINT('Ctrl Pts',(370.695134128803,-10.1115926996635,-3.21978938696392));
#35319=CARTESIAN_POINT('Ctrl Pts',(370.668601244764,-10.1099255211121,-3.21849995426178));
#35320=CARTESIAN_POINT('Ctrl Pts',(370.659319576147,-10.1093443364125,-3.21800863237166));
#35321=CARTESIAN_POINT('Ctrl Pts',(370.642221066809,-10.1082775802635,-3.21702933213768));
#35322=CARTESIAN_POINT('Ctrl Pts',(370.634403892445,-10.107791392709,-3.21655301676784));
#35323=CARTESIAN_POINT('Ctrl Pts',(370.616667775857,-10.1066916878459,-3.21540741322286));
#35324=CARTESIAN_POINT('Ctrl Pts',(370.60675015163,-10.1060791456074,-3.21472072449741));
#35325=CARTESIAN_POINT('Ctrl Pts',(370.580981869276,-10.1044934584687,-3.21281670163236));
#35326=CARTESIAN_POINT('Ctrl Pts',(370.565136546395,-10.1035241410763,-3.21152794265536));
#35327=CARTESIAN_POINT('Ctrl Pts',(370.456599671647,-10.0969199898325,-3.20189128895898));
#35328=CARTESIAN_POINT('Ctrl Pts',(370.364289072983,-10.0914800973842,-3.18964812211196));
#35329=CARTESIAN_POINT('Ctrl Pts',(370.192049563125,-10.0814507214033,-3.15916216569419));
#35330=CARTESIAN_POINT('Ctrl Pts',(370.112038713102,-10.0768415896112,-3.14183513193206));
#35331=CARTESIAN_POINT('Ctrl Pts',(369.904123323024,-10.0648094668687,-3.08844578453568));
#35332=CARTESIAN_POINT('Ctrl Pts',(369.77764099103,-10.0574298816126,-3.04748954826187));
#35333=CARTESIAN_POINT('Ctrl Pts',(369.563073460735,-10.044368665128,-2.96304133064751));
#35334=CARTESIAN_POINT('Ctrl Pts',(369.473779898286,-10.0387612151918,-2.92311659164266));
#35335=CARTESIAN_POINT('Ctrl Pts',(369.348980086566,-10.0305711989814,-2.8603579670742));
#35336=CARTESIAN_POINT('Ctrl Pts',(369.311889355979,-10.0280909851026,-2.8407898943253));
#35337=CARTESIAN_POINT('Ctrl Pts',(369.246314092647,-10.0236153951195,-2.80454102964509));
#35338=CARTESIAN_POINT('Ctrl Pts',(369.217683754261,-10.0216296074474,-2.78813564939189));
#35339=CARTESIAN_POINT('Ctrl Pts',(369.174610866055,-10.0185910685047,-2.76256810203123));
#35340=CARTESIAN_POINT('Ctrl Pts',(369.159980489497,-10.0175498834542,-2.75372550856372));
#35341=CARTESIAN_POINT('Ctrl Pts',(369.133542900844,-10.0156514934899,-2.73745806241422));
#35342=CARTESIAN_POINT('Ctrl Pts',(369.121712151216,-10.0147957319319,-2.73007212027283));
#35343=CARTESIAN_POINT('Ctrl Pts',(369.096293196338,-10.0129433889968,-2.71397280922609));
#35344=CARTESIAN_POINT('Ctrl Pts',(369.082721815101,-10.0119458686376,-2.70523370917275));
#35345=CARTESIAN_POINT('Ctrl Pts',(369.046028282768,-10.0092252057127,-2.68121355074157));
#35346=CARTESIAN_POINT('Ctrl Pts',(369.023037096694,-10.0074947406822,-2.66573585270437));
#35347=CARTESIAN_POINT('Ctrl Pts',(368.903486427584,-9.99835798773544,-2.5829935325827));
#35348=CARTESIAN_POINT('Ctrl Pts',(368.810475589367,-9.99076416128919,-2.51078125963479));
#35349=CARTESIAN_POINT('Ctrl Pts',(368.548459215239,-9.96789807647326,-2.28332111387894));
#35350=CARTESIAN_POINT('Ctrl Pts',(368.391836290433,-9.952193870532,-2.11494035279609));
#35351=CARTESIAN_POINT('Ctrl Pts',(368.188816641251,-9.92950865905699,-1.84375328090339));
#35352=CARTESIAN_POINT('Ctrl Pts',(368.127707999806,-9.92228321129425,-1.75281801243335));
#35353=CARTESIAN_POINT('Ctrl Pts',(368.06236637864,-9.91421120829735,-1.64399105824542));
#35354=CARTESIAN_POINT('Ctrl Pts',(368.053512260778,-9.91310925728834,-1.62896957172511));
#35355=CARTESIAN_POINT('Ctrl Pts',(368.040108053289,-9.91142920358036,-1.60580079844673));
#35356=CARTESIAN_POINT('Ctrl Pts',(368.035470861427,-9.91084575397493,-1.59770464479745));
#35357=CARTESIAN_POINT('Ctrl Pts',(368.027007174854,-9.90977687864003,-1.58277781552506));
#35358=CARTESIAN_POINT('Ctrl Pts',(368.023170413075,-9.90929081829687,-1.57595334012942));
#35359=CARTESIAN_POINT('Ctrl Pts',(368.014539881358,-9.90819395160339,-1.5604703442929));
#35360=CARTESIAN_POINT('Ctrl Pts',(368.009761105403,-9.90758409848121,-1.55180368940004));
#35361=CARTESIAN_POINT('Ctrl Pts',(367.997481206433,-9.90601004980853,-1.52928854079146));
#35362=CARTESIAN_POINT('Ctrl Pts',(367.99004143927,-9.9050495896514,-1.51540664685358));
#35363=CARTESIAN_POINT('Ctrl Pts',(367.940998404392,-9.89866823344856,-1.42226340956446));
#35364=CARTESIAN_POINT('Ctrl Pts',(367.902607415758,-9.89342755858152,-1.34134543194303));
#35365=CARTESIAN_POINT('Ctrl Pts',(367.835175261897,-9.88351335012752,-1.18244024274981));
#35366=CARTESIAN_POINT('Ctrl Pts',(367.805686641122,-9.87882982640742,-1.10472407921425));
#35367=CARTESIAN_POINT('Ctrl Pts',(367.718492793758,-9.86347216751284,-0.845077957968715));
#35368=CARTESIAN_POINT('Ctrl Pts',(367.67393722504,-9.8529101072069,-0.659176161326178));
#35369=CARTESIAN_POINT('Ctrl Pts',(367.636668234636,-9.83819189763902,-0.406593296607283));
#35370=CARTESIAN_POINT('Ctrl Pts',(367.629169019626,-9.83442860254649,-0.342492924896701));
#35371=CARTESIAN_POINT('Ctrl Pts',(367.619620860445,-9.82788119238462,-0.232302480160832));
#35372=CARTESIAN_POINT('Ctrl Pts',(367.61662796937,-9.82512546604046,-0.186313413736238));
#35373=CARTESIAN_POINT('Ctrl Pts',(367.613772762875,-9.82115898221448,-0.12077984025312));
#35374=CARTESIAN_POINT('Ctrl Pts',(367.613100414752,-9.81997346498977,-0.101275055972246));
#35375=CARTESIAN_POINT('Ctrl Pts',(367.612243568114,-9.81791233101388,-0.0675137868352983));
#35376=CARTESIAN_POINT('Ctrl Pts',(367.611976438764,-9.81703931953154,-0.053259821080117));
#35377=CARTESIAN_POINT('Ctrl Pts',(367.611644812505,-9.81535567478545,-0.0258613429985518));
#35378=CARTESIAN_POINT('Ctrl Pts',(367.611566140869,-9.81454550279893,-0.0127172636289814));
#35379=CARTESIAN_POINT('Ctrl Pts',(367.611570707206,-9.81241346131295,0.0217649042256376));
#35380=CARTESIAN_POINT('Ctrl Pts',(367.611785455238,-9.81108750896086,0.043102053378294));
#35381=CARTESIAN_POINT('Ctrl Pts',(367.613372946402,-9.80612873477627,0.122485262543873));
#35382=CARTESIAN_POINT('Ctrl Pts',(367.616102304005,-9.80245402730413,0.180490194762853));
#35383=CARTESIAN_POINT('Ctrl Pts',(367.626917124544,-9.79308232685239,0.326295110971551));
#35384=CARTESIAN_POINT('Ctrl Pts',(367.637041018937,-9.7873275175316,0.41389202447117));
#35385=CARTESIAN_POINT('Ctrl Pts',(367.672936450188,-9.77203660827862,0.642006614529326));
#35386=CARTESIAN_POINT('Ctrl Pts',(367.704479436494,-9.76237855112307,0.781416477289189));
#35387=CARTESIAN_POINT('Ctrl Pts',(367.792269608571,-9.74153734005061,1.07675327426295));
#35388=CARTESIAN_POINT('Ctrl Pts',(367.851511979887,-9.73038293077823,1.23139540690404));
#35389=CARTESIAN_POINT('Ctrl Pts',(367.93393988401,-9.71802208414474,1.40522408116741));
#35390=CARTESIAN_POINT('Ctrl Pts',(367.945819220213,-9.71630156781658,1.42948341740365));
#35391=CARTESIAN_POINT('Ctrl Pts',(367.962663256538,-9.71394694087683,1.46281380006098));
#35392=CARTESIAN_POINT('Ctrl Pts',(367.967368326692,-9.71329798647084,1.47201384350399));
#35393=CARTESIAN_POINT('Ctrl Pts',(367.975521807922,-9.71218852023634,1.48776933477997));
#35394=CARTESIAN_POINT('Ctrl Pts',(367.97894868406,-9.71172669738386,1.49433574960594));
#35395=CARTESIAN_POINT('Ctrl Pts',(367.986166543092,-9.71076339135411,1.50805077795278));
#35396=CARTESIAN_POINT('Ctrl Pts',(367.989961851224,-9.7102622049316,1.51519700697216));
#35397=CARTESIAN_POINT('Ctrl Pts',(367.999323485461,-9.70903877182838,1.53266500482356));
#35398=CARTESIAN_POINT('Ctrl Pts',(368.004919381531,-9.70831837334509,1.54297095906417));
#35399=CARTESIAN_POINT('Ctrl Pts',(368.025447864189,-9.70571397135917,1.58029100742341));
#35400=CARTESIAN_POINT('Ctrl Pts',(368.040712612498,-9.70384982505603,1.60712171344446));
#35401=CARTESIAN_POINT('Ctrl Pts',(368.080012314441,-9.69921728940689,1.67394601553831));
#35402=CARTESIAN_POINT('Ctrl Pts',(368.104535207033,-9.69647456230415,1.71364564534499));
#35403=CARTESIAN_POINT('Ctrl Pts',(368.310114399419,-9.67452187568904,2.03083484222454));
#35404=CARTESIAN_POINT('Ctrl Pts',(368.532114510248,-9.65685728132207,2.27942790262382));
#35405=CARTESIAN_POINT('Ctrl Pts',(368.84065651892,-9.63352664798685,2.53299306624615));
#35406=CARTESIAN_POINT('Ctrl Pts',(368.894529132123,-9.62949968022464,2.57448210942296));
#35407=CARTESIAN_POINT('Ctrl Pts',(368.968635310251,-9.62399819829661,2.62790654137544));
#35408=CARTESIAN_POINT('Ctrl Pts',(368.987747753885,-9.62258265125986,2.6413714175596));
#35409=CARTESIAN_POINT('Ctrl Pts',(369.019388733511,-9.62024374373543,2.6631514954789));
#35410=CARTESIAN_POINT('Ctrl Pts',(369.031832172095,-9.61932506207504,2.67158921894026));
#35411=CARTESIAN_POINT('Ctrl Pts',(369.056140197593,-9.61753241040407,2.68782502318446));
#35412=CARTESIAN_POINT('Ctrl Pts',(369.067998189696,-9.6166588174323,2.6956323870706));
#35413=CARTESIAN_POINT('Ctrl Pts',(369.09598646403,-9.61459879470184,2.71379604515744));
#35414=CARTESIAN_POINT('Ctrl Pts',(369.112158186814,-9.61340997846805,2.72408719598076));
#35415=CARTESIAN_POINT('Ctrl Pts',(369.165775693384,-9.60947269531497,2.75753933919425));
#35416=CARTESIAN_POINT('Ctrl Pts',(369.203603019968,-9.60670160949175,2.78007643261634));
#35417=CARTESIAN_POINT('Ctrl Pts',(369.294714929813,-9.60003980452121,2.83186049374975));
#35418=CARTESIAN_POINT('Ctrl Pts',(369.348387050004,-9.59612535377562,2.86038806814491));
#35419=CARTESIAN_POINT('Ctrl Pts',(369.562553882867,-9.58054565408234,2.96656634793586));
#35420=CARTESIAN_POINT('Ctrl Pts',(369.72855644991,-9.56853335902953,3.03235530765771));
#35421=CARTESIAN_POINT('Ctrl Pts',(370.06818933598,-9.5445228591354,3.13534287379665));
#35422=CARTESIAN_POINT('Ctrl Pts',(370.241196925875,-9.53256978487021,3.1726246022994));
#35423=CARTESIAN_POINT('Ctrl Pts',(370.443092925915,-9.51948819719132,3.19902879411396));
#35424=CARTESIAN_POINT('Ctrl Pts',(370.469827870093,-9.51777358157234,3.2021850869973));
#35425=CARTESIAN_POINT('Ctrl Pts',(370.506864213815,-9.51542553403473,3.20608767752409));
#35426=CARTESIAN_POINT('Ctrl Pts',(370.517133515464,-9.51477736651232,3.20711992052349));
#35427=CARTESIAN_POINT('Ctrl Pts',(370.534777602471,-9.51366889113543,3.2088078802466));
#35428=CARTESIAN_POINT('Ctrl Pts',(370.542149939316,-9.51320727733466,3.20948754271655));
#35429=CARTESIAN_POINT('Ctrl Pts',(370.55758740504,-9.51224400184884,3.21085710385552));
#35430=CARTESIAN_POINT('Ctrl Pts',(370.565652880191,-9.51174263922369,3.21154203092224));
#35431=CARTESIAN_POINT('Ctrl Pts',(370.585424469277,-9.5105181091752,3.21314604719509));
#35432=CARTESIAN_POINT('Ctrl Pts',(370.597133334978,-9.50979679772263,3.21403157286778));
#35433=CARTESIAN_POINT('Ctrl Pts',(370.639739263711,-9.50718530738156,3.21701970180967));
#35434=CARTESIAN_POINT('Ctrl Pts',(370.67066246517,-9.5053151275566,3.2187410060747));
#35435=CARTESIAN_POINT('Ctrl Pts',(370.748431055638,-9.50066446460427,3.2219461884893));
#35436=CARTESIAN_POINT('Ctrl Pts',(370.795294039223,-9.49790990156003,3.2228545359463));
#35437=CARTESIAN_POINT('Ctrl Pts',(371.178835821806,-9.47563839904368,3.22192094910913));
#35438=CARTESIAN_POINT('Ctrl Pts',(371.513309657422,-9.45770673532695,3.16835561884218));
#35439=CARTESIAN_POINT('Ctrl Pts',(371.89387440878,-9.43426675632815,3.04425632251717));
#35440=CARTESIAN_POINT('Ctrl Pts',(371.953697459722,-9.43049587881588,3.02277110324761));
#35441=CARTESIAN_POINT('Ctrl Pts',(372.034054553671,-9.42529361814119,2.99119855187404));
#35442=CARTESIAN_POINT('Ctrl Pts',(372.055176222941,-9.42391314169579,2.98264005996886));
#35443=CARTESIAN_POINT('Ctrl Pts',(372.088586395174,-9.42170788983338,2.9686879293413));
#35444=CARTESIAN_POINT('Ctrl Pts',(372.100935289884,-9.42088805941205,2.96344020654134));
#35445=CARTESIAN_POINT('Ctrl Pts',(372.1261900843,-9.41920150914475,2.95252136632115));
#35446=CARTESIAN_POINT('Ctrl Pts',(372.139092248708,-9.41833453551171,2.94684238582082));
#35447=CARTESIAN_POINT('Ctrl Pts',(372.168855114058,-9.41632198277008,2.93350826462769));
#35448=CARTESIAN_POINT('Ctrl Pts',(372.185687796228,-9.41517433160365,2.92579214801831));
#35449=CARTESIAN_POINT('Ctrl Pts',(372.238567030593,-9.41153865911797,2.90099858233017));
#35450=CARTESIAN_POINT('Ctrl Pts',(372.274362404469,-9.40903266167922,2.88339729859175));
#35451=CARTESIAN_POINT('Ctrl Pts',(372.309820613642,-9.40650395365004,2.86513684952373));
#35452=CARTESIAN_POINT('',(367.611569056541,-9.56531811886281,0.00278495561203112));
#35453=CARTESIAN_POINT('Ctrl Pts',(372.309820498245,-9.15921048455976,2.86513690895142));
#35454=CARTESIAN_POINT('Ctrl Pts',(372.045257012626,-9.1761807693358,3.00138314611619));
#35455=CARTESIAN_POINT('Ctrl Pts',(371.762917332346,-9.19227741905944,3.10042508082463));
#35456=CARTESIAN_POINT('Ctrl Pts',(371.409521784279,-9.21339959172196,3.17161809370236));
#35457=CARTESIAN_POINT('Ctrl Pts',(371.347933050406,-9.2171080785855,3.18217214439677));
#35458=CARTESIAN_POINT('Ctrl Pts',(371.263654022811,-9.22223771045259,3.19410409845714));
#35459=CARTESIAN_POINT('Ctrl Pts',(371.241196293265,-9.22360982419175,3.19704245094925));
#35460=CARTESIAN_POINT('Ctrl Pts',(371.20540808486,-9.22580545168389,3.20134176463265));
#35461=CARTESIAN_POINT('Ctrl Pts',(371.192096606922,-9.226624105055,3.20285675747336));
#35462=CARTESIAN_POINT('Ctrl Pts',(371.164736113994,-9.22831101875315,3.20579798773435));
#35463=CARTESIAN_POINT('Ctrl Pts',(371.150686415713,-9.22917955072291,3.20721497374243));
#35464=CARTESIAN_POINT('Ctrl Pts',(371.118084588137,-9.23120046862997,3.21028673402436));
#35465=CARTESIAN_POINT('Ctrl Pts',(371.099526664826,-9.23235497512238,3.21187308862051));
#35466=CARTESIAN_POINT('Ctrl Pts',(371.040170063283,-9.23606134972561,3.21642903714309));
#35467=CARTESIAN_POINT('Ctrl Pts',(370.99932947443,-9.23863232352634,3.21878265825869));
#35468=CARTESIAN_POINT('Ctrl Pts',(370.903288161155,-9.24472955145762,3.22248487026863));
#35469=CARTESIAN_POINT('Ctrl Pts',(370.848077003594,-9.24827450458236,3.22319340830129));
#35470=CARTESIAN_POINT('Ctrl Pts',(370.642273076936,-9.26163718980462,3.22054681420285));
#35471=CARTESIAN_POINT('Ctrl Pts',(370.492005027425,-9.27170223664362,3.20805491508853));
#35472=CARTESIAN_POINT('Ctrl Pts',(370.128731790619,-9.29652023958033,3.15203830833367));
#35473=CARTESIAN_POINT('Ctrl Pts',(369.918161207519,-9.31134101637858,3.09739695999033));
#35474=CARTESIAN_POINT('Ctrl Pts',(369.690987179753,-9.32688091622255,3.01322922080392));
#35475=CARTESIAN_POINT('Ctrl Pts',(369.667408632598,-9.32848762481068,3.00417681376603));
#35476=CARTESIAN_POINT('Ctrl Pts',(369.634630697396,-9.33071012809269,2.99114837556744));
#35477=CARTESIAN_POINT('Ctrl Pts',(369.625340435998,-9.33133879928386,2.98740547756661));
#35478=CARTESIAN_POINT('Ctrl Pts',(369.609282630978,-9.33242306560802,2.98084886871542));
#35479=CARTESIAN_POINT('Ctrl Pts',(369.602507019862,-9.33287984087892,2.97805529619938));
#35480=CARTESIAN_POINT('Ctrl Pts',(369.588183845859,-9.33384378875778,2.97209263056451));
#35481=CARTESIAN_POINT('Ctrl Pts',(369.5806387121,-9.33435060094625,2.96891784709778));
#35482=CARTESIAN_POINT('Ctrl Pts',(369.562225366736,-9.3355852448794,2.96108731021022));
#35483=CARTESIAN_POINT('Ctrl Pts',(369.551370404249,-9.33631121212037,2.95640037987552));
#35484=CARTESIAN_POINT('Ctrl Pts',(369.511122356572,-9.33899685227492,2.93875875058399));
#35485=CARTESIAN_POINT('Ctrl Pts',(369.48189657857,-9.34093486285725,2.92542410440424));
#35486=CARTESIAN_POINT('Ctrl Pts',(369.269694971775,-9.35495168008341,2.82474434340459));
#35487=CARTESIAN_POINT('Ctrl Pts',(369.095102702806,-9.36620412274226,2.72073088868787));
#35488=CARTESIAN_POINT('Ctrl Pts',(368.762048351349,-9.38928181707787,2.47706719861769));
#35489=CARTESIAN_POINT('Ctrl Pts',(368.60519808438,-9.40107375287663,2.33691560534751));
#35490=CARTESIAN_POINT('Ctrl Pts',(368.437609907184,-9.41576388976557,2.15483741495324));
#35491=CARTESIAN_POINT('Ctrl Pts',(368.412616446288,-9.41801623037446,2.1267099904393));
#35492=CARTESIAN_POINT('Ctrl Pts',(368.374817993984,-9.42152323709554,2.08264149184215));
#35493=CARTESIAN_POINT('Ctrl Pts',(368.361662146937,-9.42276349489443,2.06700480639254));
#35494=CARTESIAN_POINT('Ctrl Pts',(368.339561175187,-9.42488135398421,2.04022323842938));
#35495=CARTESIAN_POINT('Ctrl Pts',(368.33053974323,-9.42575583124762,2.02914191489885));
#35496=CARTESIAN_POINT('Ctrl Pts',(368.312418926522,-9.42753292676025,2.00657867791763));
#35497=CARTESIAN_POINT('Ctrl Pts',(368.303323552697,-9.42843567636029,1.99509398941074));
#35498=CARTESIAN_POINT('Ctrl Pts',(368.281058585542,-9.43067261123724,1.96658282419045));
#35499=CARTESIAN_POINT('Ctrl Pts',(368.267980818051,-9.43201038196785,1.94948584971037));
#35500=CARTESIAN_POINT('Ctrl Pts',(368.219489336903,-9.43706244657457,1.88475785590913));
#35501=CARTESIAN_POINT('Ctrl Pts',(368.185224204153,-9.44082068097463,1.8362849549399));
#35502=CARTESIAN_POINT('Ctrl Pts',(368.062071945621,-9.45506814848143,1.65144250113473));
#35503=CARTESIAN_POINT('Ctrl Pts',(367.982227781839,-9.46586991942624,1.50936400519982));
#35504=CARTESIAN_POINT('Ctrl Pts',(367.864051718674,-9.48471106711013,1.2559092634263));
#35505=CARTESIAN_POINT('Ctrl Pts',(367.820445302843,-9.4926537294396,1.14732780257992));
#35506=CARTESIAN_POINT('Ctrl Pts',(367.741564502796,-9.50915225145384,0.91512703877353));
#35507=CARTESIAN_POINT('Ctrl Pts',(367.707580597534,-9.51767828594383,0.791266189145504));
#35508=CARTESIAN_POINT('Ctrl Pts',(367.677603031087,-9.52691986021442,0.649269564824457));
#35509=CARTESIAN_POINT('Ctrl Pts',(367.674263381166,-9.52798273049701,0.632815294994851));
#35510=CARTESIAN_POINT('Ctrl Pts',(367.669120366267,-9.52967413850922,0.606419399754992));
#35511=CARTESIAN_POINT('Ctrl Pts',(367.667234947006,-9.53030704156733,0.596494334808006));
#35512=CARTESIAN_POINT('Ctrl Pts',(367.663964748241,-9.53142798766573,0.578826924144435));
#35513=CARTESIAN_POINT('Ctrl Pts',(367.662561602145,-9.53191704814549,0.571088177873209));
#35514=CARTESIAN_POINT('Ctrl Pts',(367.659894291716,-9.53286271346055,0.556064100408563));
#35515=CARTESIAN_POINT('Ctrl Pts',(367.658626870661,-9.53331951156078,0.548779570916097));
#35516=CARTESIAN_POINT('Ctrl Pts',(367.655872944471,-9.53432903539977,0.532622247088352));
#35517=CARTESIAN_POINT('Ctrl Pts',(367.654398493157,-9.53488109326968,0.52374742383042));
#35518=CARTESIAN_POINT('Ctrl Pts',(367.650816443817,-9.53625206580573,0.501613961626277));
#35519=CARTESIAN_POINT('Ctrl Pts',(367.64875447149,-9.5370685638991,0.488347975274731));
#35520=CARTESIAN_POINT('Ctrl Pts',(367.623475330361,-9.54744592060516,0.318734098999937));
#35521=CARTESIAN_POINT('Ctrl Pts',(367.611705674635,-9.55643615325176,0.160879323418296));
#35522=CARTESIAN_POINT('Ctrl Pts',(367.611569056541,-9.56531811886281,0.00278495561203112));
#35523=CARTESIAN_POINT('Ctrl Pts',(367.611569059112,-9.56531795180948,0.00278792907424184));
#35524=CARTESIAN_POINT('Ctrl Pts',(367.611374172123,-9.57797464776861,-0.222494634597293));
#35525=CARTESIAN_POINT('Ctrl Pts',(367.634800609163,-9.59038930068433,-0.44717314711833));
#35526=CARTESIAN_POINT('Ctrl Pts',(367.69778522171,-9.60806751235912,-0.744637333014133));
#35527=CARTESIAN_POINT('Ctrl Pts',(367.716919768297,-9.61271842768905,-0.821066016533812));
#35528=CARTESIAN_POINT('Ctrl Pts',(367.745464853836,-9.61889374241953,-0.919604653320842));
#35529=CARTESIAN_POINT('Ctrl Pts',(367.752349822658,-9.62033628917451,-0.942421658366697));
#35530=CARTESIAN_POINT('Ctrl Pts',(367.764021323441,-9.62270873649172,-0.979605026105658));
#35531=CARTESIAN_POINT('Ctrl Pts',(367.768657233967,-9.62363369382537,-0.994017979332718));
#35532=CARTESIAN_POINT('Ctrl Pts',(367.777827397613,-9.6254306631561,-1.0218533985905));
#35533=CARTESIAN_POINT('Ctrl Pts',(367.782348948311,-9.62630223914439,-1.03527970457614));
#35534=CARTESIAN_POINT('Ctrl Pts',(367.793012022966,-9.6283250692593,-1.06626566159175));
#35535=CARTESIAN_POINT('Ctrl Pts',(367.799217306512,-9.62947841237908,-1.08380268607457));
#35536=CARTESIAN_POINT('Ctrl Pts',(367.819895569708,-9.63324669919461,-1.14067187016413));
#35537=CARTESIAN_POINT('Ctrl Pts',(367.834983546852,-9.63588195686505,-1.17977433081536));
#35538=CARTESIAN_POINT('Ctrl Pts',(367.928309995146,-9.6515501820604,-1.40827034991521));
#35539=CARTESIAN_POINT('Ctrl Pts',(368.023693893456,-9.66516478128069,-1.5901178178407));
#35540=CARTESIAN_POINT('Ctrl Pts',(368.224719601683,-9.68999659920125,-1.89806525664835));
#35541=CARTESIAN_POINT('Ctrl Pts',(368.323984258249,-9.70108602589383,-2.02753141354491));
#35542=CARTESIAN_POINT('Ctrl Pts',(368.463638879596,-9.71490781374781,-2.18361246233849));
#35543=CARTESIAN_POINT('Ctrl Pts',(368.495411016946,-9.71794806548861,-2.21761074822583));
#35544=CARTESIAN_POINT('Ctrl Pts',(368.549180301427,-9.72290801528488,-2.27270574216118));
#35545=CARTESIAN_POINT('Ctrl Pts',(368.570759642753,-9.7248517069936,-2.29419907715357));
#35546=CARTESIAN_POINT('Ctrl Pts',(368.600898333283,-9.72749855066466,-2.32337833674725));
#35547=CARTESIAN_POINT('Ctrl Pts',(368.609198208362,-9.72822054925767,-2.33132842455728));
#35548=CARTESIAN_POINT('Ctrl Pts',(368.623484941243,-9.72945127667924,-2.34486725976424));
#35549=CARTESIAN_POINT('Ctrl Pts',(368.629450846296,-9.72996165005176,-2.35047784858138));
#35550=CARTESIAN_POINT('Ctrl Pts',(368.640793788178,-9.73092518988405,-2.36106404071736));
#35551=CARTESIAN_POINT('Ctrl Pts',(368.64616649649,-9.73137871007436,-2.36604413966812));
#35552=CARTESIAN_POINT('Ctrl Pts',(368.658915646814,-9.7324482530211,-2.37778108051946));
#35553=CARTESIAN_POINT('Ctrl Pts',(368.666306708626,-9.73306308458857,-2.38452202958564));
#35554=CARTESIAN_POINT('Ctrl Pts',(368.692226065064,-9.7352015783609,-2.40794140055877));
#35555=CARTESIAN_POINT('Ctrl Pts',(368.710916919099,-9.73671246115249,-2.42443964176917));
#35556=CARTESIAN_POINT('Ctrl Pts',(368.896608023939,-9.75144086370525,-2.58455249254069));
#35557=CARTESIAN_POINT('Ctrl Pts',(369.077748129916,-9.76361956425793,-2.71092623051227));
#35558=CARTESIAN_POINT('Ctrl Pts',(369.400251270259,-9.78425412023531,-2.88991875753721));
#35559=CARTESIAN_POINT('Ctrl Pts',(369.534936453644,-9.79259969663299,-2.95292751441202));
#35560=CARTESIAN_POINT('Ctrl Pts',(369.724555575888,-9.8043964067138,-3.02614327457104));
#35561=CARTESIAN_POINT('Ctrl Pts',(369.776125144813,-9.80760796278115,-3.04455959784097));
#35562=CARTESIAN_POINT('Ctrl Pts',(369.866750065077,-9.81327506245225,-3.0743425559846));
#35563=CARTESIAN_POINT('Ctrl Pts',(369.905598519424,-9.81571165623632,-3.08630033412424));
#35564=CARTESIAN_POINT('Ctrl Pts',(369.96251776364,-9.81929679522666,-3.10264843581423));
#35565=CARTESIAN_POINT('Ctrl Pts',(369.980417775942,-9.82042639985378,-3.10762245906316));
#35566=CARTESIAN_POINT('Ctrl Pts',(370.011990510846,-9.8224230379357,-3.11610245536534));
#35567=CARTESIAN_POINT('Ctrl Pts',(370.02564524214,-9.82328792667124,-3.11967392020961));
#35568=CARTESIAN_POINT('Ctrl Pts',(370.052320829798,-9.82498040758377,-3.12646415508091));
#35569=CARTESIAN_POINT('Ctrl Pts',(370.065339203983,-9.8258077006709,-3.12969156403486));
#35570=CARTESIAN_POINT('Ctrl Pts',(370.100470566911,-9.82804396550752,-3.13816861563279));
#35571=CARTESIAN_POINT('Ctrl Pts',(370.122619248991,-9.8294578027969,-3.14326568301474));
#35572=CARTESIAN_POINT('Ctrl Pts',(370.20639766189,-9.83482168440393,-3.1616147065844));
#35573=CARTESIAN_POINT('Ctrl Pts',(370.268354463503,-9.83882130925147,-3.17329101536853));
#35574=CARTESIAN_POINT('Ctrl Pts',(370.663833344441,-9.86457327862878,-3.23587245037377));
#35575=CARTESIAN_POINT('Ctrl Pts',(371.003175169231,-9.88797134872904,-3.23594515554636));
#35576=CARTESIAN_POINT('Ctrl Pts',(371.382626258822,-9.91332884128186,-3.17610992980054));
#35577=CARTESIAN_POINT('Ctrl Pts',(371.428783103526,-9.91639373590926,-3.16779543322743));
#35578=CARTESIAN_POINT('Ctrl Pts',(371.505112546398,-9.92141230563556,-3.15231854201093));
#35579=CARTESIAN_POINT('Ctrl Pts',(371.535391762622,-9.92338995150959,-3.14572300899859));
#35580=CARTESIAN_POINT('Ctrl Pts',(371.577015853217,-9.92608599487546,-3.13602539911766));
#35581=CARTESIAN_POINT('Ctrl Pts',(371.588444844284,-9.92682390219903,-3.13329668472403));
#35582=CARTESIAN_POINT('Ctrl Pts',(371.607727217903,-9.92806456578325,-3.12858132873243));
#35583=CARTESIAN_POINT('Ctrl Pts',(371.615588434331,-9.92856916058394,-3.12662748981293));
#35584=CARTESIAN_POINT('Ctrl Pts',(371.630626284116,-9.92953198287824,-3.12282970169105));
#35585=CARTESIAN_POINT('Ctrl Pts',(371.63780401275,-9.92999049594136,-3.12099062109069));
#35586=CARTESIAN_POINT('Ctrl Pts',(371.654973568019,-9.93108490456682,-3.11652827285055));
#35587=CARTESIAN_POINT('Ctrl Pts',(371.664959322165,-9.93171947333414,-3.11388166675038));
#35588=CARTESIAN_POINT('Ctrl Pts',(371.700951407435,-9.93400025499506,-3.10415693222677));
#35589=CARTESIAN_POINT('Ctrl Pts',(371.726882234413,-9.93563133836677,-3.09680043114646));
#35590=CARTESIAN_POINT('Ctrl Pts',(371.913329200562,-9.94729156433648,-3.04136940572132));
#35591=CARTESIAN_POINT('Ctrl Pts',(372.069991842799,-9.95673397126023,-2.98116031299773));
#35592=CARTESIAN_POINT('Ctrl Pts',(372.36225415704,-9.974866370819,-2.84181648196921));
#35593=CARTESIAN_POINT('Ctrl Pts',(372.498157510861,-9.98354246735299,-2.76444311621066));
#35594=CARTESIAN_POINT('Ctrl Pts',(372.726821603085,-9.99927457473014,-2.61126799175011));
#35595=CARTESIAN_POINT('Ctrl Pts',(372.821975521353,-10.0062104834711,-2.53958725327049));
#35596=CARTESIAN_POINT('Ctrl Pts',(372.933639845739,-10.0149801859474,-2.44534219248962));
#35597=CARTESIAN_POINT('Ctrl Pts',(372.954118023159,-10.0166160344453,-2.42761167368367));
#35598=CARTESIAN_POINT('Ctrl Pts',(372.986221582983,-10.019226053939,-2.39909965590004));
#35599=CARTESIAN_POINT('Ctrl Pts',(372.997995369783,-10.020193201105,-2.3884866362171));
#35600=CARTESIAN_POINT('Ctrl Pts',(373.02001097942,-10.0220207526901,-2.36834515925642));
#35601=CARTESIAN_POINT('Ctrl Pts',(373.030270020756,-10.0228803269618,-2.35883600604154));
#35602=CARTESIAN_POINT('Ctrl Pts',(373.053244311182,-10.0248234940531,-2.3372612573991));
#35603=CARTESIAN_POINT('Ctrl Pts',(373.065923603716,-10.0259086865919,-2.32515818087744));
#35604=CARTESIAN_POINT('Ctrl Pts',(373.098187844792,-10.0287034922108,-2.29385319618085));
#35605=CARTESIAN_POINT('Ctrl Pts',(373.117627226727,-10.0304195068655,-2.27450391394032));
#35606=CARTESIAN_POINT('Ctrl Pts',(373.284265463584,-10.0454153790246,-2.10434879572518));
#35607=CARTESIAN_POINT('Ctrl Pts',(373.416564719196,-10.0593409399028,-1.93971627864066));
#35608=CARTESIAN_POINT('Ctrl Pts',(373.651396583044,-10.0882791371823,-1.58048469338463));
#35609=CARTESIAN_POINT('Ctrl Pts',(373.752052765583,-10.1032334677743,-1.38589249067822));
#35610=CARTESIAN_POINT('Ctrl Pts',(373.844460532,-10.1194904834031,-1.15163655282704));
#35611=CARTESIAN_POINT('Ctrl Pts',(373.856195998022,-10.1216179767421,-1.12048131483597));
#35612=CARTESIAN_POINT('Ctrl Pts',(373.871530035646,-10.1244818011271,-1.07777812000613));
#35613=CARTESIAN_POINT('Ctrl Pts',(373.875549048358,-10.1252408620281,-1.06638470808806));
#35614=CARTESIAN_POINT('Ctrl Pts',(373.882177433506,-10.126506833729,-1.04725175619422));
#35615=CARTESIAN_POINT('Ctrl Pts',(373.884821597103,-10.1270157512751,-1.03952449469791));
#35616=CARTESIAN_POINT('Ctrl Pts',(373.889787834812,-10.1279789770894,-1.02482910646506));
#35617=CARTESIAN_POINT('Ctrl Pts',(373.892115501845,-10.1284336228179,-1.01786298119242));
#35618=CARTESIAN_POINT('Ctrl Pts',(373.897580781238,-10.1295088795441,-1.00131881883271));
#35619=CARTESIAN_POINT('Ctrl Pts',(373.900697338943,-10.1301282682982,-0.991733834724223));
#35620=CARTESIAN_POINT('Ctrl Pts',(373.911501526658,-10.1322982459361,-0.957967650593053));
#35621=CARTESIAN_POINT('Ctrl Pts',(373.918948724475,-10.133835556711,-0.933709729210991));
#35622=CARTESIAN_POINT('Ctrl Pts',(373.987230439323,-10.148364916497,-0.701555786713309));
#35623=CARTESIAN_POINT('Ctrl Pts',(374.027253650709,-10.1603562817405,-0.488083311405805));
#35624=CARTESIAN_POINT('Ctrl Pts',(374.058277074835,-10.180902539974,-0.122069923036281));
#35625=CARTESIAN_POINT('Ctrl Pts',(374.060458474449,-10.1893611934321,0.0287453736501252));
#35626=CARTESIAN_POINT('Ctrl Pts',(374.049014956875,-10.2013043954855,0.234284410818763));
#35627=CARTESIAN_POINT('Ctrl Pts',(374.044529051576,-10.2045423556791,0.28932719662586));
#35628=CARTESIAN_POINT('Ctrl Pts',(374.034261754948,-10.2102519365239,0.38490303560071));
#35629=CARTESIAN_POINT('Ctrl Pts',(374.029117919296,-10.2127042034623,0.425492222881452));
#35630=CARTESIAN_POINT('Ctrl Pts',(374.02050981543,-10.2163081856516,0.48440199315364));
#35631=CARTESIAN_POINT('Ctrl Pts',(374.017656946779,-10.2174406721144,0.502808814423645));
#35632=CARTESIAN_POINT('Ctrl Pts',(374.012361021227,-10.2194406145943,0.535124837384966));
#35633=CARTESIAN_POINT('Ctrl Pts',(374.0099857848,-10.220305902641,0.549044759218781));
#35634=CARTESIAN_POINT('Ctrl Pts',(374.005178966445,-10.2219978115404,0.576139606670014));
#35635=CARTESIAN_POINT('Ctrl Pts',(374.002756558398,-10.2228241244243,0.589315881866638));
#35636=CARTESIAN_POINT('Ctrl Pts',(373.996018285707,-10.2250543869519,0.624724611938763));
#35637=CARTESIAN_POINT('Ctrl Pts',(373.991550167995,-10.2264631555314,0.646926992828327));
#35638=CARTESIAN_POINT('Ctrl Pts',(373.973879958686,-10.2317858144228,0.730184416723781));
#35639=CARTESIAN_POINT('Ctrl Pts',(373.959138398811,-10.2357483110284,0.790895179689501));
#35640=CARTESIAN_POINT('Ctrl Pts',(373.853357065961,-10.2615007859608,1.17720564480226));
#35641=CARTESIAN_POINT('Ctrl Pts',(373.713353147188,-10.2849481191647,1.48710594764328));
#35642=CARTESIAN_POINT('Ctrl Pts',(373.50202844593,-10.3103542115884,1.80876727923314));
#35643=CARTESIAN_POINT('Ctrl Pts',(373.47541192508,-10.3134208875347,1.84741479583875));
#35644=CARTESIAN_POINT('Ctrl Pts',(373.429823611049,-10.3184420490098,1.91060942439129));
#35645=CARTESIAN_POINT('Ctrl Pts',(373.411324969121,-10.3204205348764,1.93548779416751));
#35646=CARTESIAN_POINT('Ctrl Pts',(373.385321920382,-10.3231175229761,1.96942476815169));
#35647=CARTESIAN_POINT('Ctrl Pts',(373.378123282078,-10.3238555524564,1.97871413252315));
#35648=CARTESIAN_POINT('Ctrl Pts',(373.365876989178,-10.325096361632,1.99433987151783));
#35649=CARTESIAN_POINT('Ctrl Pts',(373.36085600536,-10.3256009808318,2.00069691678825));
#35650=CARTESIAN_POINT('Ctrl Pts',(373.351196847659,-10.3265638028315,2.01283198111394));
#35651=CARTESIAN_POINT('Ctrl Pts',(373.346562662281,-10.3270222915113,2.01861300867648));
#35652=CARTESIAN_POINT('Ctrl Pts',(373.335420496608,-10.3281165813806,2.03241477382579));
#35653=CARTESIAN_POINT('Ctrl Pts',(373.328893765864,-10.3287510564248,2.04042036561849));
#35654=CARTESIAN_POINT('Ctrl Pts',(373.30520493142,-10.3310310535965,2.06919317853767));
#35655=CARTESIAN_POINT('Ctrl Pts',(373.287820541963,-10.3326614601318,2.08977702812144));
#35656=CARTESIAN_POINT('Ctrl Pts',(373.15952684514,-10.344407321397,2.23787407789459));
#35657=CARTESIAN_POINT('Ctrl Pts',(373.038984139717,-10.3539256374363,2.35672182770263));
#35658=CARTESIAN_POINT('Ctrl Pts',(372.795555062396,-10.3717421407932,2.56162280161342));
#35659=CARTESIAN_POINT('Ctrl Pts',(372.674920444555,-10.380031876609,2.64963073928684));
#35660=CARTESIAN_POINT('Ctrl Pts',(372.470981900944,-10.3937737300137,2.77774310757113));
#35661=CARTESIAN_POINT('Ctrl Pts',(372.391306039511,-10.3990793543797,2.82317307133056));
#35662=CARTESIAN_POINT('Ctrl Pts',(372.30982057914,-10.4044982614434,2.86513686729151));
#35663=CARTESIAN_POINT('Origin',(370.834317853224,2.31077344927308,0.));
#35664=CARTESIAN_POINT('',(372.3098206137,-11.9006401642978,2.86513684949388));
#35665=CARTESIAN_POINT('',(372.309820451737,-11.6561638218248,2.86513693290212));
#35666=CARTESIAN_POINT('',(372.309820613641,2.31077344927308,2.86513684952399));
#35667=CARTESIAN_POINT('',(367.611569193008,-11.0603970329327,-0.00293863513896361));
#35668=CARTESIAN_POINT('Ctrl Pts',(372.3098206137,-11.9006401642978,2.86513684949403));
#35669=CARTESIAN_POINT('Ctrl Pts',(372.320887123176,-11.8998481329448,2.85943776210708));
#35670=CARTESIAN_POINT('Ctrl Pts',(372.331920823068,-11.8990595518313,2.85367445082586));
#35671=CARTESIAN_POINT('Ctrl Pts',(372.352050304904,-11.8976232943015,2.84301116710232));
#35672=CARTESIAN_POINT('Ctrl Pts',(372.361156299895,-11.8969744795422,2.83813119072117));
#35673=CARTESIAN_POINT('Ctrl Pts',(372.376749767643,-11.8958651891777,2.82967775603535));
#35674=CARTESIAN_POINT('Ctrl Pts',(372.383248611172,-11.8954034034494,2.82612560289196));
#35675=CARTESIAN_POINT('Ctrl Pts',(372.396822359976,-11.8944401029819,2.81864554514496));
#35676=CARTESIAN_POINT('Ctrl Pts',(372.403894794462,-11.8939388854061,2.8147133548693));
#35677=CARTESIAN_POINT('Ctrl Pts',(372.421182455932,-11.8927152581753,2.80501619919042));
#35678=CARTESIAN_POINT('Ctrl Pts',(372.431381290609,-11.8919946980927,2.79922195116702));
#35679=CARTESIAN_POINT('Ctrl Pts',(372.468317846365,-11.8893890426104,2.77796965773682));
#35680=CARTESIAN_POINT('Ctrl Pts',(372.494865584004,-11.8875238294583,2.76218261350526));
#35681=CARTESIAN_POINT('Ctrl Pts',(372.560968328264,-11.8828880900452,2.72157598524606));
#35682=CARTESIAN_POINT('Ctrl Pts',(372.600219457421,-11.8801432714929,2.6962732912217));
#35683=CARTESIAN_POINT('Ctrl Pts',(372.914185345415,-11.858135406756,2.48408101525441));
#35684=CARTESIAN_POINT('Ctrl Pts',(373.159046879565,-11.8404246156689,2.25658614530807));
#35685=CARTESIAN_POINT('Ctrl Pts',(373.406444320867,-11.8170756250387,1.94288448731513));
#35686=CARTESIAN_POINT('Ctrl Pts',(373.446399812459,-11.8130933742174,1.88882545267499));
#35687=CARTESIAN_POINT('Ctrl Pts',(373.497878856238,-11.8076439902955,1.81441513298575));
#35688=CARTESIAN_POINT('Ctrl Pts',(373.510915383146,-11.8062343715419,1.79512816001135));
#35689=CARTESIAN_POINT('Ctrl Pts',(373.532013544191,-11.8039027221997,1.7631735337854));
#35690=CARTESIAN_POINT('Ctrl Pts',(373.540197769463,-11.8029853124016,1.7505875637137));
#35691=CARTESIAN_POINT('Ctrl Pts',(373.555955413499,-11.8011932870378,1.72598041924931));
#35692=CARTESIAN_POINT('Ctrl Pts',(373.56353787497,-11.8003190349298,1.71396542548348));
#35693=CARTESIAN_POINT('Ctrl Pts',(373.581195374352,-11.7982545362831,1.68557148020296));
#35694=CARTESIAN_POINT('Ctrl Pts',(373.59120366744,-11.7970618735664,1.66915185427608));
#35695=CARTESIAN_POINT('Ctrl Pts',(373.623824617233,-11.7930984108247,1.61454003267695));
#35696=CARTESIAN_POINT('Ctrl Pts',(373.645794435294,-11.7903045755265,1.57597164213616));
#35697=CARTESIAN_POINT('Ctrl Pts',(373.696249952073,-11.7835778788395,1.48298151272684));
#35698=CARTESIAN_POINT('Ctrl Pts',(373.723989222069,-11.7796206649567,1.42817649355118));
#35699=CARTESIAN_POINT('Ctrl Pts',(373.827562443791,-11.7637645441808,1.20815739692203));
#35700=CARTESIAN_POINT('Ctrl Pts',(373.890920561161,-11.7515047564412,1.03746052311287));
#35701=CARTESIAN_POINT('Ctrl Pts',(373.94951301404,-11.7366911101456,0.826476367141626));
#35702=CARTESIAN_POINT('Ctrl Pts',(373.958854224937,-11.7341727228967,0.790428091315009));
#35703=CARTESIAN_POINT('Ctrl Pts',(374.002145409845,-11.7216896197043,0.61058522475395));
#35704=CARTESIAN_POINT('Ctrl Pts',(374.02680766142,-11.7118127780099,0.46471972060924));
#35705=CARTESIAN_POINT('Ctrl Pts',(374.043205344678,-11.701216983972,0.299171989120469));
#35706=CARTESIAN_POINT('Ctrl Pts',(374.044876944958,-11.7000411585449,0.280665580748561));
#35707=CARTESIAN_POINT('Ctrl Pts',(374.047176649361,-11.698265043123,0.252487260352363));
#35708=CARTESIAN_POINT('Ctrl Pts',(374.04792131143,-11.697658598335,0.242825615839519));
#35709=CARTESIAN_POINT('Ctrl Pts',(374.049188255117,-11.696567067973,0.225359789170082));
#35710=CARTESIAN_POINT('Ctrl Pts',(374.049725711691,-11.6960811634039,0.217556987121091));
#35711=CARTESIAN_POINT('Ctrl Pts',(374.050853697834,-11.6950080265341,0.200262710367463));
#35712=CARTESIAN_POINT('Ctrl Pts',(374.051430626296,-11.6944215550342,0.190770552149279));
#35713=CARTESIAN_POINT('Ctrl Pts',(374.0529944711,-11.6927135537238,0.163012293398545));
#35714=CARTESIAN_POINT('Ctrl Pts',(374.053867914116,-11.6915981309754,0.144739833031209));
#35715=CARTESIAN_POINT('Ctrl Pts',(374.0602777455,-11.6817059299301,-0.0184841254605742));
#35716=CARTESIAN_POINT('Ctrl Pts',(374.056177975124,-11.6734077790748,-0.163666974720797));
#35717=CARTESIAN_POINT('Ctrl Pts',(374.020101455934,-11.6521452406507,-0.539307437473672));
#35718=CARTESIAN_POINT('Ctrl Pts',(373.972967030071,-11.6393917575428,-0.767429847222778));
#35719=CARTESIAN_POINT('Ctrl Pts',(373.876220794709,-11.6211040583421,-1.06764085759085));
#35720=CARTESIAN_POINT('Ctrl Pts',(373.847667164305,-11.6162059588548,-1.14575508753241));
#35721=CARTESIAN_POINT('Ctrl Pts',(373.806587126127,-11.6096961468074,-1.24593950358361));
#35722=CARTESIAN_POINT('Ctrl Pts',(373.79677531661,-11.6081755580457,-1.26909243171847));
#35723=CARTESIAN_POINT('Ctrl Pts',(373.780511556818,-11.6057077318139,-1.30625341323168));
#35724=CARTESIAN_POINT('Ctrl Pts',(373.774228121332,-11.6047662456154,-1.32033439749536));
#35725=CARTESIAN_POINT('Ctrl Pts',(373.762022319352,-11.6029596010847,-1.34716807228741));
#35726=CARTESIAN_POINT('Ctrl Pts',(373.756117055158,-11.6020950468478,-1.35992818545921));
#35727=CARTESIAN_POINT('Ctrl Pts',(373.742354477998,-11.6001015105034,-1.38916294770131));
#35728=CARTESIAN_POINT('Ctrl Pts',(373.734440383379,-11.5989705825393,-1.40561018579794));
#35729=CARTESIAN_POINT('Ctrl Pts',(373.709214757367,-11.59541285945,-1.45691456002696));
#35730=CARTESIAN_POINT('Ctrl Pts',(373.691411772917,-11.5929690394266,-1.4915248458353));
#35731=CARTESIAN_POINT('Ctrl Pts',(373.598925939798,-11.5805931954734,-1.66358943624273));
#35732=CARTESIAN_POINT('Ctrl Pts',(373.514941732477,-11.5703344507448,-1.79578151136795));
#35733=CARTESIAN_POINT('Ctrl Pts',(373.327868312766,-11.5493287222662,-2.04770533943167));
#35734=CARTESIAN_POINT('Ctrl Pts',(373.224901291494,-11.5386075605444,-2.16702551988096));
#35735=CARTESIAN_POINT('Ctrl Pts',(373.026757717973,-11.5197721560197,-2.36525402913432));
#35736=CARTESIAN_POINT('Ctrl Pts',(372.934970722332,-11.5116206078163,-2.44713777501089));
#35737=CARTESIAN_POINT('Ctrl Pts',(372.825647998361,-11.5027313277034,-2.53396932714878));
#35738=CARTESIAN_POINT('Ctrl Pts',(372.812493815498,-11.5016744889197,-2.54425159674552));
#35739=CARTESIAN_POINT('Ctrl Pts',(372.791277347711,-11.4999910379849,-2.5605719142001));
#35740=CARTESIAN_POINT('Ctrl Pts',(372.783265826697,-11.4993601195465,-2.56667504642992));
#35741=CARTESIAN_POINT('Ctrl Pts',(372.768953868342,-11.4982416866483,-2.57747216764089));
#35742=CARTESIAN_POINT('Ctrl Pts',(372.76266472158,-11.4977531676548,-2.58218079265951));
#35743=CARTESIAN_POINT('Ctrl Pts',(372.749069224202,-11.4967035164074,-2.59228223947809));
#35744=CARTESIAN_POINT('Ctrl Pts',(372.741757275658,-11.4961429219943,-2.59766719890255));
#35745=CARTESIAN_POINT('Ctrl Pts',(372.72127863592,-11.4945834996618,-2.61261581279615));
#35746=CARTESIAN_POINT('Ctrl Pts',(372.708061914113,-11.4935892623801,-2.62211090543475));
#35747=CARTESIAN_POINT('Ctrl Pts',(372.628035154467,-11.4876385322912,-2.678689250818));
#35748=CARTESIAN_POINT('Ctrl Pts',(372.559519852168,-11.4828324101999,-2.72332119126683));
#35749=CARTESIAN_POINT('Ctrl Pts',(372.35055285699,-11.4687818229412,-2.84838974560999));
#35750=CARTESIAN_POINT('Ctrl Pts',(372.20566245711,-11.4598111685699,-2.92090960257575));
#35751=CARTESIAN_POINT('Ctrl Pts',(371.860945564956,-11.4389578149869,-3.06211560251359));
#35752=CARTESIAN_POINT('Ctrl Pts',(371.658624094335,-11.4270405695998,-3.1226622874181));
#35753=CARTESIAN_POINT('Ctrl Pts',(371.424947018585,-11.4127908146274,-3.16828445764703));
#35754=CARTESIAN_POINT('Ctrl Pts',(371.397973471801,-11.4111396169713,-3.17319420921733));
#35755=CARTESIAN_POINT('Ctrl Pts',(371.353667378644,-11.4084155461436,-3.18067611145235));
#35756=CARTESIAN_POINT('Ctrl Pts',(371.336370354483,-11.4073491303045,-3.18345217062455));
#35757=CARTESIAN_POINT('Ctrl Pts',(371.305232742327,-11.4054237546951,-3.18818947317329));
#35758=CARTESIAN_POINT('Ctrl Pts',(371.291400310104,-11.4045664388484,-3.19020196343595));
#35759=CARTESIAN_POINT('Ctrl Pts',(371.26186872399,-11.4027316697443,-3.19430252658275));
#35760=CARTESIAN_POINT('Ctrl Pts',(371.246166440934,-11.4017534315306,-3.19636498305872));
#35761=CARTESIAN_POINT('Ctrl Pts',(371.203598242637,-11.3990939492932,-3.20163733486297));
#35762=CARTESIAN_POINT('Ctrl Pts',(371.176706537124,-11.3974057606356,-3.20462471241331));
#35763=CARTESIAN_POINT('Ctrl Pts',(371.031574679082,-11.3882489311397,-3.21889969261471));
#35764=CARTESIAN_POINT('Ctrl Pts',(370.912829598672,-11.3805881815316,-3.22398134024731));
#35765=CARTESIAN_POINT('Ctrl Pts',(370.638620772259,-11.3625202194038,-3.22055794130342));
#35766=CARTESIAN_POINT('Ctrl Pts',(370.483510330732,-11.3520138328805,-3.20736933985001));
#35767=CARTESIAN_POINT('Ctrl Pts',(370.163412571277,-11.3300897111804,-3.15665037287258));
#35768=CARTESIAN_POINT('Ctrl Pts',(369.999167052317,-11.3187035207236,-3.11722462139496));
#35769=CARTESIAN_POINT('Ctrl Pts',(369.813131730597,-11.3061365401617,-3.05679930265338));
#35770=CARTESIAN_POINT('Ctrl Pts',(369.787618201556,-11.3044208368281,-3.04815731598887));
#35771=CARTESIAN_POINT('Ctrl Pts',(369.752479921424,-11.3020715751282,-3.03576198318334));
#35772=CARTESIAN_POINT('Ctrl Pts',(369.742761165726,-11.3014232612559,-3.03228101171567));
#35773=CARTESIAN_POINT('Ctrl Pts',(369.726100755185,-11.300314601618,-3.02622326451399));
#35774=CARTESIAN_POINT('Ctrl Pts',(369.719151016771,-11.299852948962,-3.02366918041048));
#35775=CARTESIAN_POINT('Ctrl Pts',(369.704622644207,-11.2988896679432,-3.01827298435493));
#35776=CARTESIAN_POINT('Ctrl Pts',(369.697045830819,-11.298388338211,-3.01542624220812));
#35777=CARTESIAN_POINT('Ctrl Pts',(369.679570214041,-11.2972342754912,-3.00878510915621));
#35778=CARTESIAN_POINT('Ctrl Pts',(369.669679147295,-11.2965827447286,-3.00497032185768));
#35779=CARTESIAN_POINT('Ctrl Pts',(369.634663329396,-11.2942815221975,-2.99126655706561));
#35780=CARTESIAN_POINT('Ctrl Pts',(369.609643450908,-11.2926469224985,-2.9811104154166));
#35781=CARTESIAN_POINT('Ctrl Pts',(369.548396883766,-11.2886625801397,-2.95534777651579));
#35782=CARTESIAN_POINT('Ctrl Pts',(369.512322698067,-11.2863306303508,-2.93938808335048));
#35783=CARTESIAN_POINT('Ctrl Pts',(369.366423591752,-11.2769246545106,-2.87161084084019));
#35784=CARTESIAN_POINT('Ctrl Pts',(369.25926915961,-11.2700736231069,-2.81426513984629));
#35785=CARTESIAN_POINT('Ctrl Pts',(368.967409907263,-11.2509103219685,-2.63616685057348));
#35786=CARTESIAN_POINT('Ctrl Pts',(368.791513593849,-11.2387123209317,-2.50233180527531));
#35787=CARTESIAN_POINT('Ctrl Pts',(368.580386531614,-11.2218178870088,-2.30448640455306));
#35788=CARTESIAN_POINT('Ctrl Pts',(368.531641807648,-11.2177385087443,-2.25578057619202));
#35789=CARTESIAN_POINT('Ctrl Pts',(368.468395623869,-11.2121740366731,-2.18839739198008));
#35790=CARTESIAN_POINT('Ctrl Pts',(368.452482296116,-11.2107496139405,-2.17106666746102));
#35791=CARTESIAN_POINT('Ctrl Pts',(368.426692322339,-11.2083998349384,-2.14235474921373));
#35792=CARTESIAN_POINT('Ctrl Pts',(368.416703036576,-11.207479244875,-2.13107558633624));
#35793=CARTESIAN_POINT('Ctrl Pts',(368.397464716824,-11.205685617414,-2.10904374256293));
#35794=CARTESIAN_POINT('Ctrl Pts',(368.388206839009,-11.2048129772168,-2.09829921897255));
#35795=CARTESIAN_POINT('Ctrl Pts',(368.366661843566,-11.202759490021,-2.07295812923782));
#35796=CARTESIAN_POINT('Ctrl Pts',(368.354432932613,-11.2015762998832,-2.05831298470395));
#35797=CARTESIAN_POINT('Ctrl Pts',(368.316242556199,-11.1978244522742,-2.01174241837882));
#35798=CARTESIAN_POINT('Ctrl Pts',(368.290762923699,-11.1952366614314,-1.97942891472614));
#35799=CARTESIAN_POINT('Ctrl Pts',(368.177530232997,-11.1833366662052,-1.83002886782835));
#35800=CARTESIAN_POINT('Ctrl Pts',(368.097205825692,-11.1737464961292,-1.70755205000281));
#35801=CARTESIAN_POINT('Ctrl Pts',(367.963736059794,-11.1555461206006,-1.47028586089492));
#35802=CARTESIAN_POINT('Ctrl Pts',(367.908475908128,-11.1470029753757,-1.35699200572998));
#35803=CARTESIAN_POINT('Ctrl Pts',(367.798590787857,-11.127718229268,-1.09357728486061));
#35804=CARTESIAN_POINT('Ctrl Pts',(367.748194884252,-11.1170197416778,-0.942022589411725));
#35805=CARTESIAN_POINT('Ctrl Pts',(367.704679507146,-11.1056746809298,-0.769303276358909));
#35806=CARTESIAN_POINT('Ctrl Pts',(367.700290341204,-11.1044973053141,-0.751222537038615));
#35807=CARTESIAN_POINT('Ctrl Pts',(367.693852416808,-11.1027193262758,-0.723663184199534));
#35808=CARTESIAN_POINT('Ctrl Pts',(367.691689530151,-11.1021125491315,-0.714212006525329));
#35809=CARTESIAN_POINT('Ctrl Pts',(367.687858906583,-11.1010206783313,-0.69711895270795));
#35810=CARTESIAN_POINT('Ctrl Pts',(367.686176319008,-11.1005347630543,-0.68948068941004));
#35811=CARTESIAN_POINT('Ctrl Pts',(367.68251060642,-11.0994619111551,-0.672546637401109));
#35812=CARTESIAN_POINT('Ctrl Pts',(367.680540790178,-11.0988757328808,-0.663248175635086));
#35813=CARTESIAN_POINT('Ctrl Pts',(367.67653338447,-11.0976624428529,-0.643909744087673));
#35814=CARTESIAN_POINT('Ctrl Pts',(367.674502469142,-11.0970357018055,-0.633868483641668));
#35815=CARTESIAN_POINT('Ctrl Pts',(367.669329469642,-11.0954072472061,-0.607649308772214));
#35816=CARTESIAN_POINT('Ctrl Pts',(367.666263493032,-11.0944095047552,-0.591456461788419));
#35817=CARTESIAN_POINT('Ctrl Pts',(367.629067436936,-11.081868259145,-0.386414294620745));
#35818=CARTESIAN_POINT('Ctrl Pts',(367.611744217969,-11.0711319694304,-0.194885383249188));
#35819=CARTESIAN_POINT('Ctrl Pts',(367.611569193008,-11.0603970329327,-0.00293863513896361));
#35820=CARTESIAN_POINT('Ctrl Pts',(367.611569193971,-11.0603970919897,-0.00293969111161769));
#35821=CARTESIAN_POINT('Ctrl Pts',(367.61139238361,-11.0495565454987,0.19089542073948));
#35822=CARTESIAN_POINT('Ctrl Pts',(367.628702684857,-11.0387500880331,0.384342450413428));
#35823=CARTESIAN_POINT('Ctrl Pts',(367.674481422554,-11.0237740215398,0.636777309751511));
#35824=CARTESIAN_POINT('Ctrl Pts',(367.687472116422,-11.0200658030643,0.698149526749735));
#35825=CARTESIAN_POINT('Ctrl Pts',(367.708609147836,-11.0146797500261,0.785361562531312));
#35826=CARTESIAN_POINT('Ctrl Pts',(367.71530365185,-11.0130478202635,0.811540534408275));
#35827=CARTESIAN_POINT('Ctrl Pts',(367.726440646869,-11.010443069287,0.852916995845585));
#35828=CARTESIAN_POINT('Ctrl Pts',(367.730667394687,-11.0094772301302,0.868171612544893));
#35829=CARTESIAN_POINT('Ctrl Pts',(367.738838150592,-11.0076515433216,0.896837995507693));
#35830=CARTESIAN_POINT('Ctrl Pts',(367.742757388951,-11.0067925194552,0.91025648340098));
#35831=CARTESIAN_POINT('Ctrl Pts',(367.75178797674,-11.0048497865332,0.940443742714512));
#35832=CARTESIAN_POINT('Ctrl Pts',(367.756949066781,-11.0037644731157,0.957197056729903));
#35833=CARTESIAN_POINT('Ctrl Pts',(367.770543532753,-11.00096776888,1.00007914114168));
#35834=CARTESIAN_POINT('Ctrl Pts',(367.779174461213,-10.9992499550086,1.02614334020761));
#35835=CARTESIAN_POINT('Ctrl Pts',(367.847834951257,-10.986006866201,1.22493961651566));
#35836=CARTESIAN_POINT('Ctrl Pts',(367.922125588808,-10.9740045664149,1.39236271946672));
#35837=CARTESIAN_POINT('Ctrl Pts',(368.073191078554,-10.9529566154958,1.66715199469731));
#35838=CARTESIAN_POINT('Ctrl Pts',(368.143102233134,-10.9440689366667,1.77780037995044));
#35839=CARTESIAN_POINT('Ctrl Pts',(368.29810935476,-10.9262037967182,1.99294499057722));
#35840=CARTESIAN_POINT('Ctrl Pts',(368.383433898668,-10.9172484529346,2.09698808581342));
#35841=CARTESIAN_POINT('Ctrl Pts',(368.488355152492,-10.9074264869318,2.20974206344318));
#35842=CARTESIAN_POINT('Ctrl Pts',(368.501824946052,-10.9061861812607,2.2239554541784));
#35843=CARTESIAN_POINT('Ctrl Pts',(368.522335268448,-10.9043296249808,2.24520670310338));
#35844=CARTESIAN_POINT('Ctrl Pts',(368.529279949688,-10.9037064416096,2.25233587225381));
#35845=CARTESIAN_POINT('Ctrl Pts',(368.541748857501,-10.9025974003231,2.26501794889453));
#35846=CARTESIAN_POINT('Ctrl Pts',(368.547260398606,-10.9021105920982,2.27058298952859));
#35847=CARTESIAN_POINT('Ctrl Pts',(368.559350582887,-10.9010501735651,2.2827018434581));
#35848=CARTESIAN_POINT('Ctrl Pts',(368.565937280082,-10.9004772095513,2.28924733649943));
#35849=CARTESIAN_POINT('Ctrl Pts',(368.584482823347,-10.8988769031982,2.30751823227752));
#35850=CARTESIAN_POINT('Ctrl Pts',(368.596505109759,-10.8978544357002,2.3191792096998));
#35851=CARTESIAN_POINT('Ctrl Pts',(368.666709483167,-10.8919657590337,2.3862194815426));
#35852=CARTESIAN_POINT('Ctrl Pts',(368.726859763971,-10.8872433303529,2.43950653240532));
#35853=CARTESIAN_POINT('Ctrl Pts',(368.995567621563,-10.8671800252795,2.66018888019764));
#35854=CARTESIAN_POINT('Ctrl Pts',(369.222511785332,-10.8527112689899,2.80351683829633));
#35855=CARTESIAN_POINT('Ctrl Pts',(369.565485473205,-10.8309983570869,2.96455935818278));
#35856=CARTESIAN_POINT('Ctrl Pts',(369.668786693791,-10.8244895539486,3.00667276212425));
#35857=CARTESIAN_POINT('Ctrl Pts',(369.799610433895,-10.8161748668473,3.05225006557322));
#35858=CARTESIAN_POINT('Ctrl Pts',(369.825276327981,-10.8145405105438,3.06083077594337));
#35859=CARTESIAN_POINT('Ctrl Pts',(369.866129765756,-10.8119327753655,3.07391936151035));
#35860=CARTESIAN_POINT('Ctrl Pts',(369.881248072983,-10.810966406475,3.07864034823302));
#35861=CARTESIAN_POINT('Ctrl Pts',(369.909773248725,-10.8091402713797,3.08731764152384));
#35862=CARTESIAN_POINT('Ctrl Pts',(369.923172294087,-10.8082813335659,3.09129854683643));
#35863=CARTESIAN_POINT('Ctrl Pts',(369.953419994172,-10.8063395395976,3.1000715085185));
#35864=CARTESIAN_POINT('Ctrl Pts',(369.97028256979,-10.8052550854951,3.10481358628746));
#35865=CARTESIAN_POINT('Ctrl Pts',(370.013629467184,-10.8024620750477,3.11662308945992));
#35866=CARTESIAN_POINT('Ctrl Pts',(370.040166396249,-10.8007471242499,3.12349040298824));
#35867=CARTESIAN_POINT('Ctrl Pts',(370.272554216889,-10.7856815322223,3.18047563367261));
#35868=CARTESIAN_POINT('Ctrl Pts',(370.482758211437,-10.7716777243932,3.2105108608682));
#35869=CARTESIAN_POINT('Ctrl Pts',(370.86446198308,-10.7459125953276,3.2271041092211));
#35870=CARTESIAN_POINT('Ctrl Pts',(371.034893406283,-10.7343042700751,3.22100636779373));
#35871=CARTESIAN_POINT('Ctrl Pts',(371.2525783519,-10.7198199754348,3.19586643870176));
#35872=CARTESIAN_POINT('Ctrl Pts',(371.300977282873,-10.7166230298801,3.18915876247364));
#35873=CARTESIAN_POINT('Ctrl Pts',(371.380728253609,-10.7114132060564,3.17625137989719));
#35874=CARTESIAN_POINT('Ctrl Pts',(371.412172987592,-10.7093741132156,3.17068143740342));
#35875=CARTESIAN_POINT('Ctrl Pts',(371.455199716385,-10.7066094260425,3.16239853231012));
#35876=CARTESIAN_POINT('Ctrl Pts',(371.466856047054,-10.7058630251494,3.16008769006207));
#35877=CARTESIAN_POINT('Ctrl Pts',(371.486457966996,-10.7046124879783,3.15608884648769));
#35878=CARTESIAN_POINT('Ctrl Pts',(371.494410366497,-10.7041064442171,3.15443519725787));
#35879=CARTESIAN_POINT('Ctrl Pts',(371.509570937284,-10.7031442918299,3.15122281323952));
#35880=CARTESIAN_POINT('Ctrl Pts',(371.516780110177,-10.702687875336,3.14966938211372));
#35881=CARTESIAN_POINT('Ctrl Pts',(371.533957201878,-10.701602889661,3.14590632144601));
#35882=CARTESIAN_POINT('Ctrl Pts',(371.543920148239,-10.7009755982443,3.14367402746045));
#35883=CARTESIAN_POINT('Ctrl Pts',(371.579390749205,-10.6987489264585,3.13554928041131));
#35884=CARTESIAN_POINT('Ctrl Pts',(371.604837782224,-10.6971637531869,3.12939323965));
#35885=CARTESIAN_POINT('Ctrl Pts',(371.82526351139,-10.6835172774205,3.07321689997358));
#35886=CARTESIAN_POINT('Ctrl Pts',(372.015259989424,-10.6723133849633,3.00533403589829));
#35887=CARTESIAN_POINT('Ctrl Pts',(372.235435482354,-10.6587270039936,2.90253706113548));
#35888=CARTESIAN_POINT('Ctrl Pts',(372.272816132784,-10.6563989826335,2.88419360677096));
#35889=CARTESIAN_POINT('Ctrl Pts',(372.309820694103,-10.6540649855006,2.86513680808753));
#35890=CARTESIAN_POINT('Ctrl Pts',(372.30982057914,-10.4044982614434,2.86513686729151));
#35891=CARTESIAN_POINT('Ctrl Pts',(372.28102533937,-10.406413188689,2.87996598601847));
#35892=CARTESIAN_POINT('Ctrl Pts',(372.252004110942,-10.4083420726229,2.89436226250651));
#35893=CARTESIAN_POINT('Ctrl Pts',(372.198048404882,-10.4119295058265,2.92012102184648));
#35894=CARTESIAN_POINT('Ctrl Pts',(372.173181478393,-10.4135833605025,2.93160569018576));
#35895=CARTESIAN_POINT('Ctrl Pts',(372.133637366772,-10.4162155226362,2.94926087715187));
#35896=CARTESIAN_POINT('Ctrl Pts',(372.119055315084,-10.417186597351,2.955642156904));
#35897=CARTESIAN_POINT('Ctrl Pts',(372.091578405281,-10.4190175116088,2.96742462465725));
#35898=CARTESIAN_POINT('Ctrl Pts',(372.078694469542,-10.4198764870069,2.97285045466003));
#35899=CARTESIAN_POINT('Ctrl Pts',(372.049668400213,-10.4218128815473,2.98485249518078));
#35900=CARTESIAN_POINT('Ctrl Pts',(372.033507494459,-10.4228918539382,2.9913818805526));
#35901=CARTESIAN_POINT('Ctrl Pts',(371.992084008194,-10.4256599629665,3.00772831957247));
#35902=CARTESIAN_POINT('Ctrl Pts',(371.966749496577,-10.4273552960831,3.01735821787974));
#35903=CARTESIAN_POINT('Ctrl Pts',(371.789892933096,-10.4392091415508,3.08204208973065));
#35904=CARTESIAN_POINT('Ctrl Pts',(371.634569949385,-10.4497332820341,3.12597027064345));
#35905=CARTESIAN_POINT('Ctrl Pts',(371.266400149232,-10.4748291166729,3.20085121771368));
#35906=CARTESIAN_POINT('Ctrl Pts',(371.052432698529,-10.4895434691031,3.22250926574736));
#35907=CARTESIAN_POINT('Ctrl Pts',(370.758583385094,-10.5090195668122,3.22283627695545));
#35908=CARTESIAN_POINT('Ctrl Pts',(370.679278897745,-10.5141972422438,3.21999604533427));
#35909=CARTESIAN_POINT('Ctrl Pts',(370.584044771735,-10.5202596899877,3.21305801654526));
#35910=CARTESIAN_POINT('Ctrl Pts',(370.567944634089,-10.5212792188829,3.21176334221661));
#35911=CARTESIAN_POINT('Ctrl Pts',(370.542830986558,-10.5228604110062,3.20955371097847));
#35912=CARTESIAN_POINT('Ctrl Pts',(370.533810704415,-10.5234265041432,3.20872171983508));
#35913=CARTESIAN_POINT('Ctrl Pts',(370.516962999273,-10.5244802437164,3.20709609357777));
#35914=CARTESIAN_POINT('Ctrl Pts',(370.509135030264,-10.5249683777756,3.2063118360434));
#35915=CARTESIAN_POINT('Ctrl Pts',(370.491240475586,-10.5260809722575,3.20445283318289));
#35916=CARTESIAN_POINT('Ctrl Pts',(370.481176022159,-10.5267043777651,3.20335931496087));
#35917=CARTESIAN_POINT('Ctrl Pts',(370.454362532064,-10.5283593651757,3.20031808273724));
#35918=CARTESIAN_POINT('Ctrl Pts',(370.437623097078,-10.5293864421138,3.19828628719821));
#35919=CARTESIAN_POINT('Ctrl Pts',(370.26173407472,-10.5401212579035,3.17553507806191));
#35920=CARTESIAN_POINT('Ctrl Pts',(370.104306100148,-10.5492422760347,3.14308315349049));
#35921=CARTESIAN_POINT('Ctrl Pts',(369.759038104664,-10.569406645226,3.0445525463515));
#35922=CARTESIAN_POINT('Ctrl Pts',(369.573592062951,-10.5803691433512,2.97255686567412));
#35923=CARTESIAN_POINT('Ctrl Pts',(369.306805288342,-10.5975400906141,2.83949758377183));
#35924=CARTESIAN_POINT('Ctrl Pts',(369.219777102473,-10.603380610344,2.79093111637788));
#35925=CARTESIAN_POINT('Ctrl Pts',(369.113285565928,-10.6109113536359,2.72485359507424));
#35926=CARTESIAN_POINT('Ctrl Pts',(369.091591814171,-10.6124662448358,2.71103027333172));
#35927=CARTESIAN_POINT('Ctrl Pts',(369.057050737254,-10.61497669521,2.68843468599537));
#35928=CARTESIAN_POINT('Ctrl Pts',(369.044097134028,-10.6159261376987,2.6798263424437));
#35929=CARTESIAN_POINT('Ctrl Pts',(369.019568811645,-10.6177394518686,2.66326878668728));
#35930=CARTESIAN_POINT('Ctrl Pts',(369.007982712556,-10.6186026511869,2.65533701403667));
#35931=CARTESIAN_POINT('Ctrl Pts',(368.981639039998,-10.6205808288341,2.63704831616705));
#35932=CARTESIAN_POINT('Ctrl Pts',(368.966915905387,-10.6216976434386,2.62664282894199));
#35933=CARTESIAN_POINT('Ctrl Pts',(368.921684068266,-10.6251640730828,2.59410297654295));
#35934=CARTESIAN_POINT('Ctrl Pts',(368.891476657028,-10.627529478509,2.57155714326813));
#35935=CARTESIAN_POINT('Ctrl Pts',(368.643987088356,-10.6473405501515,2.37998895583847));
#35936=CARTESIAN_POINT('Ctrl Pts',(368.448825304466,-10.6659167818329,2.18432209240417));
#35937=CARTESIAN_POINT('Ctrl Pts',(368.182734410084,-10.6953929415021,1.83878406913836));
#35938=CARTESIAN_POINT('Ctrl Pts',(368.094214589393,-10.7062024377311,1.7040736705516));
#35939=CARTESIAN_POINT('Ctrl Pts',(368.006338889797,-10.717758251913,1.54565827992494));
#35940=CARTESIAN_POINT('Ctrl Pts',(367.996718606948,-10.71903621659,1.52792509682853));
#35941=CARTESIAN_POINT('Ctrl Pts',(367.982628619844,-10.7209261590427,1.50136071305961));
#35942=CARTESIAN_POINT('Ctrl Pts',(367.978032252252,-10.7215456791031,1.49259775099669));
#35943=CARTESIAN_POINT('Ctrl Pts',(367.970215609066,-10.722604241189,1.47752700510939));
#35944=CARTESIAN_POINT('Ctrl Pts',(367.966975691584,-10.7230445018471,1.47122963783327));
#35945=CARTESIAN_POINT('Ctrl Pts',(367.959649466246,-10.7240434402104,1.45687366019148));
#35946=CARTESIAN_POINT('Ctrl Pts',(367.955576274191,-10.7246012959304,1.4488085182886));
#35947=CARTESIAN_POINT('Ctrl Pts',(367.94455071852,-10.7261184258169,1.42674724114561));
#35948=CARTESIAN_POINT('Ctrl Pts',(367.937666050786,-10.7270736035622,1.41271728981498));
#35949=CARTESIAN_POINT('Ctrl Pts',(367.903410899324,-10.7318691125973,1.34160695398074));
#35950=CARTESIAN_POINT('Ctrl Pts',(367.877622474084,-10.7356210420017,1.28377506192694));
#35951=CARTESIAN_POINT('Ctrl Pts',(367.830834886233,-10.7427918739453,1.16994802340883));
#35952=CARTESIAN_POINT('Ctrl Pts',(367.809657659782,-10.7462162281929,1.11405549531615));
#35953=CARTESIAN_POINT('Ctrl Pts',(367.734890425714,-10.7591479296147,0.898840962485617));
#35954=CARTESIAN_POINT('Ctrl Pts',(367.692237923036,-10.7684238651686,0.736004002226138));
#35955=CARTESIAN_POINT('Ctrl Pts',(367.642916121727,-10.7841294534494,0.461825549680339));
#35956=CARTESIAN_POINT('Ctrl Pts',(367.628959831884,-10.7904316810727,0.352143527385429));
#35957=CARTESIAN_POINT('Ctrl Pts',(367.617249825942,-10.7995486151241,0.196618990034791));
#35958=CARTESIAN_POINT('Ctrl Pts',(367.614795757088,-10.8022319064359,0.151204847244372));
#35959=CARTESIAN_POINT('Ctrl Pts',(367.612149228961,-10.8070414867095,0.0705990553209585));
#35960=CARTESIAN_POINT('Ctrl Pts',(367.611570633997,-10.8091559366688,0.035427173120199));
#35961=CARTESIAN_POINT('Ctrl Pts',(367.611566481463,-10.8123516288331,-0.0172867449321208));
#35962=CARTESIAN_POINT('Ctrl Pts',(367.611708303411,-10.8134193811027,-0.0348268039943945));
#35963=CARTESIAN_POINT('Ctrl Pts',(367.612220607262,-10.8153467853,-0.0663521158392946));
#35964=CARTESIAN_POINT('Ctrl Pts',(367.612538983666,-10.8162047865025,-0.0803378592582764));
#35965=CARTESIAN_POINT('Ctrl Pts',(367.613412090387,-10.8180406103638,-0.110157325405297));
#35966=CARTESIAN_POINT('Ctrl Pts',(367.61399254239,-10.8190192161161,-0.125989870620044));
#35967=CARTESIAN_POINT('Ctrl Pts',(367.615880063823,-10.8216786785127,-0.168841613204498));
#35968=CARTESIAN_POINT('Ctrl Pts',(367.61741059473,-10.8233664721422,-0.195849210292671));
#35969=CARTESIAN_POINT('Ctrl Pts',(367.627472276449,-10.8325035074752,-0.341018811442123));
#35970=CARTESIAN_POINT('Ctrl Pts',(367.642173112825,-10.8401438017132,-0.458648746005031));
#35971=CARTESIAN_POINT('Ctrl Pts',(367.690907019629,-10.8581322282262,-0.727316490725006));
#35972=CARTESIAN_POINT('Ctrl Pts',(367.729410405031,-10.8685775664986,-0.877247943545817));
#35973=CARTESIAN_POINT('Ctrl Pts',(367.832467983323,-10.8905231015617,-1.18484255702983));
#35974=CARTESIAN_POINT('Ctrl Pts',(367.89906327074,-10.9019924697251,-1.34135972040181));
#35975=CARTESIAN_POINT('Ctrl Pts',(367.990162180432,-10.9146356714281,-1.5157908435751));
#35976=CARTESIAN_POINT('Ctrl Pts',(368.002933371595,-10.9163517407998,-1.53951466373764));
#35977=CARTESIAN_POINT('Ctrl Pts',(368.021010630988,-10.9187017228962,-1.5721090036773));
#35978=CARTESIAN_POINT('Ctrl Pts',(368.026063699478,-10.9193503947947,-1.58111759869966));
#35979=CARTESIAN_POINT('Ctrl Pts',(368.03481570302,-10.9204597220778,-1.59654632501731));
#35980=CARTESIAN_POINT('Ctrl Pts',(368.038493591263,-10.9209216854215,-1.6029782143781));
#35981=CARTESIAN_POINT('Ctrl Pts',(368.046239040571,-10.9218856966206,-1.61641570084551));
#35982=CARTESIAN_POINT('Ctrl Pts',(368.050310878784,-10.9223874449018,-1.623418723424));
#35983=CARTESIAN_POINT('Ctrl Pts',(368.060354410511,-10.9236129591553,-1.64054335079539));
#35984=CARTESIAN_POINT('Ctrl Pts',(368.066355219001,-10.9243348658934,-1.65064791304022));
#35985=CARTESIAN_POINT('Ctrl Pts',(368.088385403696,-10.9269488073206,-1.68728583305302));
#35986=CARTESIAN_POINT('Ctrl Pts',(368.104742679193,-10.9288208034593,-1.71362132061252));
#35987=CARTESIAN_POINT('Ctrl Pts',(368.146805424064,-10.9334763800723,-1.77921212436636));
#35988=CARTESIAN_POINT('Ctrl Pts',(368.17299347815,-10.9362339810375,-1.81815066666817));
#35989=CARTESIAN_POINT('Ctrl Pts',(368.394713608224,-10.9585824686333,-2.13276115063203));
#35990=CARTESIAN_POINT('Ctrl Pts',(368.631646856875,-10.976578691745,-2.37668251492858));
#35991=CARTESIAN_POINT('Ctrl Pts',(368.952189429709,-11.0000449202257,-2.61679446924443));
#35992=CARTESIAN_POINT('Ctrl Pts',(369.003267431008,-11.0037533154348,-2.65278613555255));
#35993=CARTESIAN_POINT('Ctrl Pts',(369.074242249901,-11.0088828397131,-2.69977117527084));
#35994=CARTESIAN_POINT('Ctrl Pts',(369.093258645705,-11.0102549402371,-2.71207362068144));
#35995=CARTESIAN_POINT('Ctrl Pts',(369.123727524093,-11.012450551874,-2.73133260126661));
#35996=CARTESIAN_POINT('Ctrl Pts',(369.135096669497,-11.0132692027341,-2.73842005782962));
#35997=CARTESIAN_POINT('Ctrl Pts',(369.158539135722,-11.0149561152051,-2.75283175216709));
#35998=CARTESIAN_POINT('Ctrl Pts',(369.170617048954,-11.0158246484833,-2.76014792892698));
#35999=CARTESIAN_POINT('Ctrl Pts',(369.198736451597,-11.0178455761679,-2.7769295918656));
#36000=CARTESIAN_POINT('Ctrl Pts',(369.214812571435,-11.019000091194,-2.78633578350582));
#36001=CARTESIAN_POINT('Ctrl Pts',(369.266454175674,-11.0227065213142,-2.81595355662285));
#36002=CARTESIAN_POINT('Ctrl Pts',(369.302322178669,-11.0252775429032,-2.83562690607293));
#36003=CARTESIAN_POINT('Ctrl Pts',(369.387457581168,-11.0313749040399,-2.88023629930319));
#36004=CARTESIAN_POINT('Ctrl Pts',(369.437009425748,-11.0349199436871,-2.90459883016439));
#36005=CARTESIAN_POINT('Ctrl Pts',(369.623992074772,-11.0482831158258,-2.99063810855335));
#36006=CARTESIAN_POINT('Ctrl Pts',(369.765055682297,-11.0583485828385,-3.04392421484232));
#36007=CARTESIAN_POINT('Ctrl Pts',(370.116882147649,-11.0831472667146,-3.14934221342488));
#36008=CARTESIAN_POINT('Ctrl Pts',(370.330207794822,-11.097947759704,-3.1904477860507));
#36009=CARTESIAN_POINT('Ctrl Pts',(370.571324604508,-11.1134791106813,-3.2121014515382));
#36010=CARTESIAN_POINT('Ctrl Pts',(370.596619444875,-11.1150933923199,-3.2140722990005));
#36011=CARTESIAN_POINT('Ctrl Pts',(370.631991974651,-11.1173273567192,-3.21640845802767));
#36012=CARTESIAN_POINT('Ctrl Pts',(370.642051355567,-11.1179600126692,-3.21702544755913));
#36013=CARTESIAN_POINT('Ctrl Pts',(370.659446323678,-11.1190492512129,-3.2180104803428));
#36014=CARTESIAN_POINT('Ctrl Pts',(370.66678051127,-11.119507039215,-3.21840065017561));
#36015=CARTESIAN_POINT('Ctrl Pts',(370.6822731821,-11.1204708826753,-3.21917173882222));
#36016=CARTESIAN_POINT('Ctrl Pts',(370.690431896567,-11.1209765901982,-3.21954672275972));
#36017=CARTESIAN_POINT('Ctrl Pts',(370.710663386302,-11.1222261711082,-3.22039952675435));
#36018=CARTESIAN_POINT('Ctrl Pts',(370.722737733258,-11.1229680133612,-3.22084048451602));
#36019=CARTESIAN_POINT('Ctrl Pts',(370.768093832273,-11.1257409055048,-3.22224153541367));
#36020=CARTESIAN_POINT('Ctrl Pts',(370.801388592911,-11.1277485908794,-3.22275379062642));
#36021=CARTESIAN_POINT('Ctrl Pts',(371.053288027091,-11.1427678276117,-3.22272495494509));
#36022=CARTESIAN_POINT('Ctrl Pts',(371.271347816626,-11.1548266277656,-3.20045827703818));
#36023=CARTESIAN_POINT('Ctrl Pts',(371.691754190141,-11.1788566222239,-3.11372354671763));
#36024=CARTESIAN_POINT('Ctrl Pts',(371.893317763489,-11.1907681165754,-3.05106124510824));
#36025=CARTESIAN_POINT('Ctrl Pts',(372.11258790595,-11.2050120749109,-2.95852929458606));
#36026=CARTESIAN_POINT('Ctrl Pts',(372.13772112052,-11.2066640256381,-2.9475430052081));
#36027=CARTESIAN_POINT('Ctrl Pts',(372.178681100618,-11.2093894991024,-2.92901216929298));
#36028=CARTESIAN_POINT('Ctrl Pts',(372.19459226322,-11.2104565597733,-2.92165677988419));
#36029=CARTESIAN_POINT('Ctrl Pts',(372.223091359081,-11.2123832121548,-2.90819899352922));
#36030=CARTESIAN_POINT('Ctrl Pts',(372.235701145268,-11.2132411586356,-2.90214370691042));
#36031=CARTESIAN_POINT('Ctrl Pts',(372.262514703988,-11.215077405873,-2.88905219164578));
#36032=CARTESIAN_POINT('Ctrl Pts',(372.276706744185,-11.2160564936493,-2.88199290135788));
#36033=CARTESIAN_POINT('Ctrl Pts',(372.315007313719,-11.2187186302899,-2.86258797360678));
#36034=CARTESIAN_POINT('Ctrl Pts',(372.339012797886,-11.2204086399349,-2.85004284820731));
#36035=CARTESIAN_POINT('Ctrl Pts',(372.467646289397,-11.2295833657861,-2.78074159869951));
#36036=CARTESIAN_POINT('Ctrl Pts',(372.569215616735,-11.2372610351857,-2.71853078414517));
#36037=CARTESIAN_POINT('Ctrl Pts',(372.795519823749,-11.2553899161026,-2.56206526432011));
#36038=CARTESIAN_POINT('Ctrl Pts',(372.917306582943,-11.2659416592702,-2.46407035035053));
#36039=CARTESIAN_POINT('Ctrl Pts',(373.154163118018,-11.2878434324473,-2.2433341237176));
#36040=CARTESIAN_POINT('Ctrl Pts',(373.267726844679,-11.2991614802583,-2.11961349159814));
#36041=CARTESIAN_POINT('Ctrl Pts',(373.387772417076,-11.3116670670705,-1.96639604197878));
#36042=CARTESIAN_POINT('Ctrl Pts',(373.404124610886,-11.3133834141312,-1.94497736285598));
#36043=CARTESIAN_POINT('Ctrl Pts',(373.426371468753,-11.3157337062222,-1.91506718222495));
#36044=CARTESIAN_POINT('Ctrl Pts',(373.432496306388,-11.3163824155087,-1.9067493255678));
#36045=CARTESIAN_POINT('Ctrl Pts',(373.442945645317,-11.3174917898624,-1.89241472767484));
#36046=CARTESIAN_POINT('Ctrl Pts',(373.447289539021,-11.3179537631312,-1.88641231734846));
#36047=CARTESIAN_POINT('Ctrl Pts',(373.456339208495,-11.3189177757352,-1.87381621129467));
#36048=CARTESIAN_POINT('Ctrl Pts',(373.461040877175,-11.319419515606,-1.86721968135541));
#36049=CARTESIAN_POINT('Ctrl Pts',(373.472501969401,-11.3206449775615,-1.85101059412344));
#36050=CARTESIAN_POINT('Ctrl Pts',(373.479233869248,-11.3213668407829,-1.84137854025664));
#36051=CARTESIAN_POINT('Ctrl Pts',(373.503529137048,-11.3239804439054,-1.80620854839717));
#36052=CARTESIAN_POINT('Ctrl Pts',(373.520777168093,-11.3258521520454,-1.78045351212091));
#36053=CARTESIAN_POINT('Ctrl Pts',(373.563188088894,-11.3305068627522,-1.71510499426295));
#36054=CARTESIAN_POINT('Ctrl Pts',(373.587863686439,-11.3332638981738,-1.67520258007805));
#36055=CARTESIAN_POINT('Ctrl Pts',(373.782962925474,-11.3555965803475,-1.34374543995809));
#36056=CARTESIAN_POINT('Ctrl Pts',(373.907466825137,-11.3735795501286,-1.02759680397341));
#36057=CARTESIAN_POINT('Ctrl Pts',(373.994180076412,-11.3970400834009,-0.636646258040273));
#36058=CARTESIAN_POINT('Ctrl Pts',(374.005965632103,-11.4007609858015,-0.575062882965707));
#36059=CARTESIAN_POINT('Ctrl Pts',(374.019558633886,-11.405905190604,-0.490788212587248));
#36060=CARTESIAN_POINT('Ctrl Pts',(374.022933437463,-11.4072790926738,-0.468361522806853));
#36061=CARTESIAN_POINT('Ctrl Pts',(374.027925671493,-11.4094768659157,-0.432627220025935));
#36062=CARTESIAN_POINT('Ctrl Pts',(374.029697295778,-11.4102958592154,-0.419341648307175));
#36063=CARTESIAN_POINT('Ctrl Pts',(374.03316479133,-11.4119829400325,-0.392039738432337));
#36064=CARTESIAN_POINT('Ctrl Pts',(374.034851532109,-11.412851295845,-0.378022552482008));
#36065=CARTESIAN_POINT('Ctrl Pts',(374.038547708966,-11.4148708950449,-0.345506624511931));
#36066=CARTESIAN_POINT('Ctrl Pts',(374.040489128683,-11.4160242502487,-0.327000802996365));
#36067=CARTESIAN_POINT('Ctrl Pts',(374.046176038974,-11.4197231400437,-0.267861261491525));
#36068=CARTESIAN_POINT('Ctrl Pts',(374.049309976814,-11.4222876719901,-0.227174075804159));
#36069=CARTESIAN_POINT('Ctrl Pts',(374.054854204941,-11.4283669500942,-0.131498492328237));
#36070=CARTESIAN_POINT('Ctrl Pts',(374.056629964147,-11.4319002466529,-0.0764874524782389));
#36071=CARTESIAN_POINT('Ctrl Pts',(374.057993990782,-11.4451974516397,0.128346304726189));
#36072=CARTESIAN_POINT('Ctrl Pts',(374.048544694044,-11.4552060229506,0.278025119399729));
#36073=CARTESIAN_POINT('Ctrl Pts',(373.99988267551,-11.480030968619,0.642503451707805));
#36074=CARTESIAN_POINT('Ctrl Pts',(373.949204069565,-11.4949206420902,0.855049036034128));
#36075=CARTESIAN_POINT('Ctrl Pts',(373.869127262658,-11.5105263255276,1.08475319314395));
#36076=CARTESIAN_POINT('Ctrl Pts',(373.86051776058,-11.5121360803272,1.10854492660686));
#36077=CARTESIAN_POINT('Ctrl Pts',(373.848092134179,-11.5143648403111,1.1416582131315));
#36078=CARTESIAN_POINT('Ctrl Pts',(373.844511408485,-11.5149967420305,1.15106631362049));
#36079=CARTESIAN_POINT('Ctrl Pts',(373.838243064212,-11.5160850385809,1.16730663774686));
#36080=CARTESIAN_POINT('Ctrl Pts',(373.835576096994,-11.5165426340296,1.17414667588696));
#36081=CARTESIAN_POINT('Ctrl Pts',(373.829891605292,-11.517506492469,1.18857991662423));
#36082=CARTESIAN_POINT('Ctrl Pts',(373.826868534533,-11.5180124051761,1.19617086765528));
#36083=CARTESIAN_POINT('Ctrl Pts',(373.819297508777,-11.5192632072153,1.21497341476285));
#36084=CARTESIAN_POINT('Ctrl Pts',(373.814715172117,-11.5200060566222,1.22617118502375));
#36085=CARTESIAN_POINT('Ctrl Pts',(373.797240506955,-11.5227871959108,1.26819693300365));
#36086=CARTESIAN_POINT('Ctrl Pts',(373.783931555685,-11.524801941274,1.29885076850193));
#36087=CARTESIAN_POINT('Ctrl Pts',(373.679165325883,-11.539944573511,1.53023371099417));
#36088=CARTESIAN_POINT('Ctrl Pts',(373.567781924503,-11.5521033828109,1.7213283579283));
#36089=CARTESIAN_POINT('Ctrl Pts',(373.314860167131,-11.5761289845239,2.06796652793123));
#36090=CARTESIAN_POINT('Ctrl Pts',(373.17595323639,-11.5879277187175,2.22402874121356));
#36091=CARTESIAN_POINT('Ctrl Pts',(373.002826645283,-11.6020438502495,2.38420628766738));
#36092=CARTESIAN_POINT('Ctrl Pts',(372.98245533906,-11.6036958966408,2.40257679907413));
#36093=CARTESIAN_POINT('Ctrl Pts',(372.948685645018,-11.606421495981,2.43225691221069));
#36094=CARTESIAN_POINT('Ctrl Pts',(372.935424824993,-11.6074885858325,2.44372140807376));
#36095=CARTESIAN_POINT('Ctrl Pts',(372.911415035386,-11.609415269923,2.46413890306841));
#36096=CARTESIAN_POINT('Ctrl Pts',(372.900699983294,-11.6102732187006,2.4731312380325));
#36097=CARTESIAN_POINT('Ctrl Pts',(372.877719350153,-11.6121094480167,2.4921635425335));
#36098=CARTESIAN_POINT('Ctrl Pts',(372.865437597991,-11.6130885154087,2.50218332031478));
#36099=CARTESIAN_POINT('Ctrl Pts',(372.831970815276,-11.6157505389467,2.52907764773245));
#36100=CARTESIAN_POINT('Ctrl Pts',(372.81064653442,-11.6174404548668,2.54577610504094));
#36101=CARTESIAN_POINT('Ctrl Pts',(372.694500863901,-11.6266135816091,2.63438780729107));
#36102=CARTESIAN_POINT('Ctrl Pts',(372.595972237138,-11.6342896647715,2.70126785832075));
#36103=CARTESIAN_POINT('Ctrl Pts',(372.433707983684,-11.6467627568836,2.79875201198031));
#36104=CARTESIAN_POINT('Ctrl Pts',(372.372287377688,-11.6514471413943,2.83296740183991));
#36105=CARTESIAN_POINT('Ctrl Pts',(372.309820451737,-11.6561638218248,2.86513693290211));
#36106=CARTESIAN_POINT('Origin',(370.834317853224,2.31077344927308,0.));
#36107=CARTESIAN_POINT('',(372.309820665215,-13.1553703139997,2.86513682296437));
#36108=CARTESIAN_POINT('',(372.309820613641,-12.9102404761535,2.86513684952405));
#36109=CARTESIAN_POINT('',(372.309820613641,2.31077344927308,2.86513684952399));
#36110=CARTESIAN_POINT('Ctrl Pts',(372.309820665215,-13.1553703139997,2.86513682296442));
#36111=CARTESIAN_POINT('Ctrl Pts',(372.49600560238,-13.1414843015589,2.76925435196471));
#36112=CARTESIAN_POINT('Ctrl Pts',(372.672435253176,-13.1271546951046,2.65543345258058));
#36113=CARTESIAN_POINT('Ctrl Pts',(372.894767161932,-13.1081534012158,2.47914895204465));
#36114=CARTESIAN_POINT('Ctrl Pts',(372.951341412221,-13.1032293604608,2.43101697135416));
#36115=CARTESIAN_POINT('Ctrl Pts',(373.027551591667,-13.0965228666838,2.36149912705992));
#36116=CARTESIAN_POINT('Ctrl Pts',(373.048635621919,-13.0946592891503,2.34174065592088));
#36117=CARTESIAN_POINT('Ctrl Pts',(373.084909869162,-13.0914429942513,2.30681892568052));
#36118=CARTESIAN_POINT('Ctrl Pts',(373.100219392852,-13.0900823296938,2.29178276637832));
#36119=CARTESIAN_POINT('Ctrl Pts',(373.122541249142,-13.0880951848621,2.2694171226996));
#36120=CARTESIAN_POINT('Ctrl Pts',(373.129670634175,-13.0874600133889,2.26220600387378));
#36121=CARTESIAN_POINT('Ctrl Pts',(373.142256411684,-13.0863380366953,2.24935518440584));
#36122=CARTESIAN_POINT('Ctrl Pts',(373.147726371234,-13.0858501880285,2.24372907646196));
#36123=CARTESIAN_POINT('Ctrl Pts',(373.15952889113,-13.0847971095648,2.23150058891496));
#36124=CARTESIAN_POINT('Ctrl Pts',(373.165853908903,-13.0842324536888,2.22489120521256));
#36125=CARTESIAN_POINT('Ctrl Pts',(373.183259646226,-13.0826774275886,2.20654718790194));
#36126=CARTESIAN_POINT('Ctrl Pts',(373.194280664324,-13.081691503186,2.19475593047308));
#36127=CARTESIAN_POINT('Ctrl Pts',(373.252951194433,-13.0764325984922,2.13103207236588));
#36128=CARTESIAN_POINT('Ctrl Pts',(373.298979645796,-13.0722697667568,2.07762575252782));
#36129=CARTESIAN_POINT('Ctrl Pts',(373.365787890776,-13.0660944131815,1.99476051905157));
#36130=CARTESIAN_POINT('Ctrl Pts',(373.387883495148,-13.0640281801022,1.96639587342609));
#36131=CARTESIAN_POINT('Ctrl Pts',(373.452816296596,-13.057863806368,1.88009939258955));
#36132=CARTESIAN_POINT('Ctrl Pts',(373.494190992327,-13.0538095070511,1.8210939934438));
#36133=CARTESIAN_POINT('Ctrl Pts',(373.636179186345,-13.0392449640128,1.60342553247583));
#36134=CARTESIAN_POINT('Ctrl Pts',(373.724848251512,-13.028837132229,1.43743888227736));
#36135=CARTESIAN_POINT('Ctrl Pts',(373.823667322106,-13.0143155777988,1.20582013899002));
#36136=CARTESIAN_POINT('Ctrl Pts',(373.847019103417,-13.0105823528121,1.1462298657046));
#36137=CARTESIAN_POINT('Ctrl Pts',(373.884011757468,-13.0040825702657,1.04287182608386));
#36138=CARTESIAN_POINT('Ctrl Pts',(373.898521522852,-13.0013438329883,0.999434895927137));
#36139=CARTESIAN_POINT('Ctrl Pts',(373.917873567437,-12.9973975829333,0.937112969718748));
#36140=CARTESIAN_POINT('Ctrl Pts',(373.923478072031,-12.9962149525484,0.918469203347576));
#36141=CARTESIAN_POINT('Ctrl Pts',(373.93289122067,-12.9941572153639,0.886094609553033));
#36142=CARTESIAN_POINT('Ctrl Pts',(373.936778391633,-12.9932846898834,0.872387051638313));
#36143=CARTESIAN_POINT('Ctrl Pts',(373.94455310719,-12.9914916149991,0.844261342964246));
#36144=CARTESIAN_POINT('Ctrl Pts',(373.948431586621,-12.9905707958538,0.829841065349289));
#36145=CARTESIAN_POINT('Ctrl Pts',(373.958005227728,-12.9882291675783,0.793233539173976));
#36146=CARTESIAN_POINT('Ctrl Pts',(373.963564239652,-12.9868040065122,0.771011848701875));
#36147=CARTESIAN_POINT('Ctrl Pts',(373.983846500876,-12.9813430771181,0.686100264265635));
#36148=CARTESIAN_POINT('Ctrl Pts',(373.996925697725,-12.9772553735,0.623036873719591));
#36149=CARTESIAN_POINT('Ctrl Pts',(374.066407095776,-12.9515024318494,0.22899033315953));
#36150=CARTESIAN_POINT('Ctrl Pts',(374.072674931922,-12.9282184664451,-0.108634208726018));
#36151=CARTESIAN_POINT('Ctrl Pts',(374.020330143661,-12.9029742150544,-0.487479006504268));
#36152=CARTESIAN_POINT('Ctrl Pts',(374.012910844455,-12.8999138603393,-0.53372009315687));
#36153=CARTESIAN_POINT('Ctrl Pts',(373.998918243087,-12.8949021965163,-0.610229278273118));
#36154=CARTESIAN_POINT('Ctrl Pts',(373.992911910017,-12.8929269841979,-0.640592810210678));
#36155=CARTESIAN_POINT('Ctrl Pts',(373.984025152851,-12.8902340107996,-0.682348369296394));
#36156=CARTESIAN_POINT('Ctrl Pts',(373.981518698094,-12.8894967866087,-0.693817139071653));
#36157=CARTESIAN_POINT('Ctrl Pts',(373.977178331509,-12.8882572051641,-0.713169745346141));
#36158=CARTESIAN_POINT('Ctrl Pts',(373.975377299232,-12.8877530130654,-0.721060769536663));
#36159=CARTESIAN_POINT('Ctrl Pts',(373.971871807403,-12.8867909251843,-0.736157298244396));
#36160=CARTESIAN_POINT('Ctrl Pts',(373.970172225456,-12.8863327444806,-0.74336380185075));
#36161=CARTESIAN_POINT('Ctrl Pts',(373.966043589247,-12.8852391061759,-0.760603736481957));
#36162=CARTESIAN_POINT('Ctrl Pts',(373.963591115057,-12.8846049736435,-0.770631552123071));
#36163=CARTESIAN_POINT('Ctrl Pts',(373.954565874849,-12.8823256257672,-0.806780865854768));
#36164=CARTESIAN_POINT('Ctrl Pts',(373.947713673173,-12.8806955225009,-0.832832310758043));
#36165=CARTESIAN_POINT('Ctrl Pts',(373.895621635161,-12.8689769024962,-1.02124638395038));
#36166=CARTESIAN_POINT('Ctrl Pts',(373.838027299363,-12.8594823205243,-1.17994426072656));
#36167=CARTESIAN_POINT('Ctrl Pts',(373.703923084344,-12.8413328960078,-1.4750162691959));
#36168=CARTESIAN_POINT('Ctrl Pts',(373.629407457263,-12.8326913540337,-1.61176274286099));
#36169=CARTESIAN_POINT('Ctrl Pts',(373.481078512035,-12.817009528736,-1.84252224867932));
#36170=CARTESIAN_POINT('Ctrl Pts',(373.411373283167,-12.810087863881,-1.93881691050339));
#36171=CARTESIAN_POINT('Ctrl Pts',(373.319464814596,-12.8013350095954,-2.05204636485041));
#36172=CARTESIAN_POINT('Ctrl Pts',(373.302148799156,-12.7997008761898,-2.07283864728086));
#36173=CARTESIAN_POINT('Ctrl Pts',(373.274285831344,-12.7970934151326,-2.10545117578254));
#36174=CARTESIAN_POINT('Ctrl Pts',(373.263909773589,-12.7961270948983,-2.11741622605177));
#36175=CARTESIAN_POINT('Ctrl Pts',(373.24421064373,-12.7943010010314,-2.13979664612373));
#36176=CARTESIAN_POINT('Ctrl Pts',(373.234907151148,-12.793442055366,-2.15022881606107));
#36177=CARTESIAN_POINT('Ctrl Pts',(373.213791822752,-12.7915001754068,-2.17359795454437));
#36178=CARTESIAN_POINT('Ctrl Pts',(373.201941850476,-12.7904156425777,-2.18649972053431));
#36179=CARTESIAN_POINT('Ctrl Pts',(373.171278751713,-12.7876222937791,-2.21934289676662));
#36180=CARTESIAN_POINT('Ctrl Pts',(373.152315586551,-12.7859070807398,-2.2391417034649));
#36181=CARTESIAN_POINT('Ctrl Pts',(372.985240095778,-12.7708972330847,-2.40918257738566));
#36182=CARTESIAN_POINT('Ctrl Pts',(372.822984839879,-12.7569553114394,-2.54475965031107));
#36183=CARTESIAN_POINT('Ctrl Pts',(372.513919452844,-12.7317395819529,-2.7552936770313));
#36184=CARTESIAN_POINT('Ctrl Pts',(372.372384972132,-12.7206281929807,-2.83673342572432));
#36185=CARTESIAN_POINT('Ctrl Pts',(372.152806263446,-12.704487753263,-2.94179588980917));
#36186=CARTESIAN_POINT('Ctrl Pts',(372.07904120381,-12.6992404018993,-2.97375870496275));
#36187=CARTESIAN_POINT('Ctrl Pts',(371.989057330074,-12.6931087321774,-3.0088131774361));
#36188=CARTESIAN_POINT('Ctrl Pts',(371.973917989345,-12.69208610397,-3.01457982998576));
#36189=CARTESIAN_POINT('Ctrl Pts',(371.950240299646,-12.6905014323673,-3.02339491734955));
#36190=CARTESIAN_POINT('Ctrl Pts',(371.941731724599,-12.6899349241486,-3.02652180810113));
#36191=CARTESIAN_POINT('Ctrl Pts',(371.925821833805,-12.6888812685009,-3.03229259610586));
#36192=CARTESIAN_POINT('Ctrl Pts',(371.918424091957,-12.6883936269904,-3.03494530308634));
#36193=CARTESIAN_POINT('Ctrl Pts',(371.901501468835,-12.6872832571903,-3.04094370278729));
#36194=CARTESIAN_POINT('Ctrl Pts',(371.891970516232,-12.6866615723428,-3.04427172305381));
#36195=CARTESIAN_POINT('Ctrl Pts',(371.866558674392,-12.6850134059558,-3.05301128848853));
#36196=CARTESIAN_POINT('Ctrl Pts',(371.850650664581,-12.6839913747568,-3.05834378125594));
#36197=CARTESIAN_POINT('Ctrl Pts',(371.712967360517,-12.6752236784987,-3.10330339317272));
#36198=CARTESIAN_POINT('Ctrl Pts',(371.588957205672,-12.6678493895597,-3.13576849423365));
#36199=CARTESIAN_POINT('Ctrl Pts',(371.278963947459,-12.6499635312317,-3.19745909801766));
#36200=CARTESIAN_POINT('Ctrl Pts',(371.091741179984,-12.6396157762381,-3.21794809066764));
#36201=CARTESIAN_POINT('Ctrl Pts',(370.765592500594,-12.621087838473,-3.2249812385774));
#36202=CARTESIAN_POINT('Ctrl Pts',(370.627353731725,-12.6130833855475,-3.21906607256498));
#36203=CARTESIAN_POINT('Ctrl Pts',(370.461961725342,-12.6031087283913,-3.20129033845343));
#36204=CARTESIAN_POINT('Ctrl Pts',(370.434033038417,-12.6014109518887,-3.19791821473489));
#36205=CARTESIAN_POINT('Ctrl Pts',(370.390224773501,-12.5987252452508,-3.19204592029569));
#36206=CARTESIAN_POINT('Ctrl Pts',(370.374313243102,-12.5977450718917,-3.18979177451796));
#36207=CARTESIAN_POINT('Ctrl Pts',(370.344619874513,-12.5959068454444,-3.18535839831712));
#36208=CARTESIAN_POINT('Ctrl Pts',(370.330833990999,-12.5950497389054,-3.18320847995466));
#36209=CARTESIAN_POINT('Ctrl Pts',(370.300098115071,-12.5931304293834,-3.17821054052797));
#36210=CARTESIAN_POINT('Ctrl Pts',(370.283156166674,-12.5920667838938,-3.17531632211955));
#36211=CARTESIAN_POINT('Ctrl Pts',(370.240322393274,-12.5893628130667,-3.16764583495307));
#36212=CARTESIAN_POINT('Ctrl Pts',(370.214464834338,-12.5877167652188,-3.16268760882752));
#36213=CARTESIAN_POINT('Ctrl Pts',(370.051546648608,-12.5772564992531,-3.12937314545875));
#36214=CARTESIAN_POINT('Ctrl Pts',(369.916412330756,-12.5681702555884,-3.09243389223329));
#36215=CARTESIAN_POINT('Ctrl Pts',(369.583963781493,-12.5448222477043,-2.97784397960769));
#36216=CARTESIAN_POINT('Ctrl Pts',(369.391107927493,-12.5303276186846,-2.88930380136953));
#36217=CARTESIAN_POINT('Ctrl Pts',(369.14824784654,-12.5115261759108,-2.7473857954625));
#36218=CARTESIAN_POINT('Ctrl Pts',(369.089310847549,-12.5069209284005,-2.71033439234708));
#36219=CARTESIAN_POINT('Ctrl Pts',(369.008679829616,-12.5006049074782,-2.65592338612546));
#36220=CARTESIAN_POINT('Ctrl Pts',(368.985942566465,-12.4988220880429,-2.64015002104584));
#36221=CARTESIAN_POINT('Ctrl Pts',(368.946515867076,-12.495731411226,-2.61203976714881));
#36222=CARTESIAN_POINT('Ctrl Pts',(368.929737438446,-12.4944163893038,-2.5998310675668));
#36223=CARTESIAN_POINT('Ctrl Pts',(368.905045965816,-12.4924829630885,-2.58149716618719));
#36224=CARTESIAN_POINT('Ctrl Pts',(368.89704202107,-12.4918565094882,-2.57549606697923));
#36225=CARTESIAN_POINT('Ctrl Pts',(368.882818598311,-12.4907439688227,-2.56472798190366));
#36226=CARTESIAN_POINT('Ctrl Pts',(368.876588441152,-12.4902569059786,-2.55997549136882));
#36227=CARTESIAN_POINT('Ctrl Pts',(368.863044269302,-12.4891986214843,-2.54956535851149));
#36228=CARTESIAN_POINT('Ctrl Pts',(368.855737248165,-12.4886280256751,-2.54389894733636));
#36229=CARTESIAN_POINT('Ctrl Pts',(368.835401336629,-12.4870406669556,-2.52798833272601));
#36230=CARTESIAN_POINT('Ctrl Pts',(368.822426721905,-12.4860286543729,-2.51767479098975));
#36231=CARTESIAN_POINT('Ctrl Pts',(368.749398197081,-12.4803330125717,-2.45869923673588));
#36232=CARTESIAN_POINT('Ctrl Pts',(368.691025727176,-12.4757823392948,-2.40798521776679));
#36233=CARTESIAN_POINT('Ctrl Pts',(368.617937024324,-12.4700023173779,-2.33971986210335));
#36234=CARTESIAN_POINT('Ctrl Pts',(368.601509019523,-12.4686975160501,-2.32404771006862));
#36235=CARTESIAN_POINT('Ctrl Pts',(368.387635965418,-12.4516145941784,-2.11565378029722));
#36236=CARTESIAN_POINT('Ctrl Pts',(368.215568602294,-12.4366757671791,-1.89852767511086));
#36237=CARTESIAN_POINT('Ctrl Pts',(368.027834970809,-12.4156045582098,-1.5866720369017));
#36238=CARTESIAN_POINT('Ctrl Pts',(367.985527311873,-12.4104208200727,-1.50939217932632));
#36239=CARTESIAN_POINT('Ctrl Pts',(367.935463443943,-12.4036372741364,-1.40832246913053));
#36240=CARTESIAN_POINT('Ctrl Pts',(367.924742839065,-12.4021414851364,-1.38603832856428));
#36241=CARTESIAN_POINT('Ctrl Pts',(367.907794249931,-12.3997041350919,-1.3497452021626));
#36242=CARTESIAN_POINT('Ctrl Pts',(367.901407792238,-12.398768064484,-1.3358110168862));
#36243=CARTESIAN_POINT('Ctrl Pts',(367.88934342893,-12.3969651508468,-1.30898496169207));
#36244=CARTESIAN_POINT('Ctrl Pts',(367.883650158951,-12.396098860356,-1.29610035786242));
#36245=CARTESIAN_POINT('Ctrl Pts',(367.870821192278,-12.3941106708024,-1.26654410012409));
#36246=CARTESIAN_POINT('Ctrl Pts',(367.863741427568,-12.3929868987645,-1.24984882877824));
#36247=CARTESIAN_POINT('Ctrl Pts',(367.841749054565,-12.3894096700996,-1.19674455220788));
#36248=CARTESIAN_POINT('Ctrl Pts',(367.827362544945,-12.3869386465185,-1.16012287795443));
#36249=CARTESIAN_POINT('Ctrl Pts',(367.722896263078,-12.367944326494,-0.87918954374385));
#36250=CARTESIAN_POINT('Ctrl Pts',(367.662070667211,-12.3504266921635,-0.625073285691753));
#36251=CARTESIAN_POINT('Ctrl Pts',(367.618497233372,-12.324509842423,-0.24437346261009));
#36252=CARTESIAN_POINT('Ctrl Pts',(367.61151703475,-12.3162197348941,-0.12156920414431));
#36253=CARTESIAN_POINT('Ctrl Pts',(367.611592421954,-12.3043134011387,0.0597676870176285));
#36254=CARTESIAN_POINT('Ctrl Pts',(367.613205645872,-12.3005296732742,0.118188417210321));
#36255=CARTESIAN_POINT('Ctrl Pts',(367.617249032242,-12.2958479450795,0.191891186069334));
#36256=CARTESIAN_POINT('Ctrl Pts',(367.618201283009,-12.2948780331451,0.20723960753836));
#36257=CARTESIAN_POINT('Ctrl Pts',(367.619877027616,-12.2933570223259,0.231444776764523));
#36258=CARTESIAN_POINT('Ctrl Pts',(367.620527338041,-12.2928020077697,0.240306127718133));
#36259=CARTESIAN_POINT('Ctrl Pts',(367.621824768854,-12.2917576693635,0.257037140878664));
#36260=CARTESIAN_POINT('Ctrl Pts',(367.622464156501,-12.2912679501679,0.26490704208438));
#36261=CARTESIAN_POINT('Ctrl Pts',(367.624027475232,-12.290126170531,0.28331089402103));
#36262=CARTESIAN_POINT('Ctrl Pts',(367.624974333418,-12.2894753935578,0.293842734986465));
#36263=CARTESIAN_POINT('Ctrl Pts',(367.62822097301,-12.2873687020081,0.32806536820198));
#36264=CARTESIAN_POINT('Ctrl Pts',(367.630731433243,-12.2859240044538,0.351736004271204));
#36265=CARTESIAN_POINT('Ctrl Pts',(367.645721739493,-12.2781794625601,0.479557165374106));
#36266=CARTESIAN_POINT('Ctrl Pts',(367.663019712849,-12.2721100077012,0.583088893248654));
#36267=CARTESIAN_POINT('Ctrl Pts',(367.7365527273,-12.2524553506403,0.92082721406705));
#36268=CARTESIAN_POINT('Ctrl Pts',(367.813959929309,-12.2393206129761,1.14957147026003));
#36269=CARTESIAN_POINT('Ctrl Pts',(367.959725240114,-12.2195757517179,1.46061424285653));
#36270=CARTESIAN_POINT('Ctrl Pts',(368.007751609373,-12.213562601036,1.55151437941975));
#36271=CARTESIAN_POINT('Ctrl Pts',(368.073780734393,-12.2057745076088,1.66321439620616));
#36272=CARTESIAN_POINT('Ctrl Pts',(368.087818793883,-12.2041429980597,1.68629480276344));
#36273=CARTESIAN_POINT('Ctrl Pts',(368.110539366544,-12.2015387638579,1.72261395507653));
#36274=CARTESIAN_POINT('Ctrl Pts',(368.119032324797,-12.2005730164447,1.73597020938261));
#36275=CARTESIAN_POINT('Ctrl Pts',(368.134452153272,-12.1988330377429,1.7598298365244));
#36276=CARTESIAN_POINT('Ctrl Pts',(368.141342838454,-12.1980601661762,1.77035629578006));
#36277=CARTESIAN_POINT('Ctrl Pts',(368.157617870291,-12.1962454310831,1.79490373371024));
#36278=CARTESIAN_POINT('Ctrl Pts',(368.167050966097,-12.1952017482351,1.80889180092038));
#36279=CARTESIAN_POINT('Ctrl Pts',(368.194641813012,-12.1921719933352,1.84912038979499));
#36280=CARTESIAN_POINT('Ctrl Pts',(368.213079607661,-12.1901753392797,1.87516552752499));
#36281=CARTESIAN_POINT('Ctrl Pts',(368.359693232522,-12.1745070924586,2.07588278465164));
#36282=CARTESIAN_POINT('Ctrl Pts',(368.504778611106,-12.1601556614552,2.23747002720002));
#36283=CARTESIAN_POINT('Ctrl Pts',(368.828014960294,-12.1306539401921,2.53169747694085));
#36284=CARTESIAN_POINT('Ctrl Pts',(369.005900956564,-12.1155792608168,2.66301497277864));
#36285=CARTESIAN_POINT('Ctrl Pts',(369.217446443184,-12.0998220248413,2.78791598369941));
#36286=CARTESIAN_POINT('Ctrl Pts',(369.239228844746,-12.0982237706409,2.80043565073749));
#36287=CARTESIAN_POINT('Ctrl Pts',(369.269911650619,-12.096008511827,2.8175967480308));
#36288=CARTESIAN_POINT('Ctrl Pts',(369.278690073995,-12.0953788020518,2.82245290837999));
#36289=CARTESIAN_POINT('Ctrl Pts',(369.29392100273,-12.0942934636862,2.83078590207893));
#36290=CARTESIAN_POINT('Ctrl Pts',(369.3003628979,-12.0938366471131,2.83428182755363));
#36291=CARTESIAN_POINT('Ctrl Pts',(369.314012692121,-12.0928734833343,2.84162920958441));
#36292=CARTESIAN_POINT('Ctrl Pts',(369.321223421529,-12.0923674911335,2.84547528385905));
#36293=CARTESIAN_POINT('Ctrl Pts',(369.33917019943,-12.0911149122453,2.85496026455033));
#36294=CARTESIAN_POINT('Ctrl Pts',(369.349923718276,-12.0903703819586,2.86056614707844));
#36295=CARTESIAN_POINT('Ctrl Pts',(369.390639428174,-12.0875730138946,2.88150009958209));
#36296=CARTESIAN_POINT('Ctrl Pts',(369.420810608834,-12.085544087922,2.89641980602257));
#36297=CARTESIAN_POINT('Ctrl Pts',(369.654217698994,-12.0701412091494,3.00732391770185));
#36298=CARTESIAN_POINT('Ctrl Pts',(369.866784059059,-12.0577713433233,3.08229423175975));
#36299=CARTESIAN_POINT('Ctrl Pts',(370.283962469053,-12.0337453157742,3.18196243918804));
#36300=CARTESIAN_POINT('Ctrl Pts',(370.486508898001,-12.0221767290818,3.21041894804239));
#36301=CARTESIAN_POINT('Ctrl Pts',(370.717710435035,-12.0083247464554,3.22075598967847));
#36302=CARTESIAN_POINT('Ctrl Pts',(370.745062459255,-12.0066765496578,3.22162999741955));
#36303=CARTESIAN_POINT('Ctrl Pts',(370.789921452465,-12.0039564275453,3.22249171871243));
#36304=CARTESIAN_POINT('Ctrl Pts',(370.807423398502,-12.0028909272542,3.22268530686467));
#36305=CARTESIAN_POINT('Ctrl Pts',(370.838902455543,-12.000966546165,3.22277704670787));
#36306=CARTESIAN_POINT('Ctrl Pts',(370.852879061455,-12.000109302022,3.22272685519326));
#36307=CARTESIAN_POINT('Ctrl Pts',(370.882701207031,-11.9982739688793,3.22242575556139));
#36308=CARTESIAN_POINT('Ctrl Pts',(370.898546060121,-11.9972950897108,3.22214888267738));
#36309=CARTESIAN_POINT('Ctrl Pts',(370.941482826763,-11.9946320509501,3.2210817769527));
#36310=CARTESIAN_POINT('Ctrl Pts',(370.968567385448,-11.9929409150576,3.22006663539389));
#36311=CARTESIAN_POINT('Ctrl Pts',(371.115012571724,-11.9837336904496,3.21272699963873));
#36312=CARTESIAN_POINT('Ctrl Pts',(371.233950718978,-11.9760229413001,3.20010813209078));
#36313=CARTESIAN_POINT('Ctrl Pts',(371.507379194614,-11.9577658650598,3.1556170684407));
#36314=CARTESIAN_POINT('Ctrl Pts',(371.660781586098,-11.9471158236094,3.11895517610208));
#36315=CARTESIAN_POINT('Ctrl Pts',(371.968762483035,-11.9252552637023,3.02102654134208));
#36316=CARTESIAN_POINT('Ctrl Pts',(372.122557955454,-11.9140773479105,2.95871827768179));
#36317=CARTESIAN_POINT('Ctrl Pts',(372.283911797408,-11.9024959660093,2.87836872897477));
#36318=CARTESIAN_POINT('Ctrl Pts',(372.296888607273,-11.9015657094817,2.87179663999732));
#36319=CARTESIAN_POINT('Ctrl Pts',(372.3098206137,-11.9006401642978,2.86513684949403));
#36320=CARTESIAN_POINT('',(367.611569135124,-12.0643987628337,-0.00293017485288484));
#36321=CARTESIAN_POINT('Ctrl Pts',(372.309820451737,-11.6561638218248,2.86513693290211));
#36322=CARTESIAN_POINT('Ctrl Pts',(372.233646148644,-11.6619155030425,2.90436555784629));
#36323=CARTESIAN_POINT('Ctrl Pts',(372.155915978518,-11.667715600594,2.94055195391155));
#36324=CARTESIAN_POINT('Ctrl Pts',(371.922021774511,-11.684863447988,3.03828260009214));
#36325=CARTESIAN_POINT('Ctrl Pts',(371.762401954571,-11.6961879915007,3.09078170024604));
#36326=CARTESIAN_POINT('Ctrl Pts',(371.573233095442,-11.7086994482014,3.1370125642238));
#36327=CARTESIAN_POINT('Ctrl Pts',(371.546978798975,-11.7104157468404,3.1430809804797));
#36328=CARTESIAN_POINT('Ctrl Pts',(371.510558203509,-11.7127659848792,3.15101939771138));
#36329=CARTESIAN_POINT('Ctrl Pts',(371.500455218983,-11.7134146876485,3.15317066979705));
#36330=CARTESIAN_POINT('Ctrl Pts',(371.483087832725,-11.7145240537977,3.15678158454162));
#36331=CARTESIAN_POINT('Ctrl Pts',(371.475828493191,-11.7149860253362,3.158264802108));
#36332=CARTESIAN_POINT('Ctrl Pts',(371.460621876423,-11.7159500376946,3.16131720207498));
#36333=CARTESIAN_POINT('Ctrl Pts',(371.452673710002,-11.7164517790309,3.16288147387551));
#36334=CARTESIAN_POINT('Ctrl Pts',(371.43318116481,-11.7176772501,3.1666414996639));
#36335=CARTESIAN_POINT('Ctrl Pts',(371.421630369145,-11.7183991209048,3.16880413909285));
#36336=CARTESIAN_POINT('Ctrl Pts',(371.379571462711,-11.7210127829815,3.17644089381874));
#36337=CARTESIAN_POINT('Ctrl Pts',(371.348995547353,-11.7228845413085,3.18153819449621));
#36338=CARTESIAN_POINT('Ctrl Pts',(371.271972149776,-11.7275394029052,3.19323923066429));
#36339=CARTESIAN_POINT('Ctrl Pts',(371.225444078168,-11.7302965368757,3.19927160134797));
#36340=CARTESIAN_POINT('Ctrl Pts',(370.842986406272,-11.7526319702875,3.24038819394931));
#36341=CARTESIAN_POINT('Ctrl Pts',(370.503579009262,-11.7706172470013,3.2234830302667));
#36342=CARTESIAN_POINT('Ctrl Pts',(370.111641754296,-11.7940787705607,3.1413026390152));
#36343=CARTESIAN_POINT('Ctrl Pts',(370.050713090677,-11.7977974952003,3.1266604894858));
#36344=CARTESIAN_POINT('Ctrl Pts',(369.968370410376,-11.802939143971,3.10431420570989));
#36345=CARTESIAN_POINT('Ctrl Pts',(369.946551859236,-11.8043127326096,3.09814511622357));
#36346=CARTESIAN_POINT('Ctrl Pts',(369.911943237407,-11.8065101297563,3.08796409458348));
#36347=CARTESIAN_POINT('Ctrl Pts',(369.899109710719,-11.8073290634588,3.0841016362982));
#36348=CARTESIAN_POINT('Ctrl Pts',(369.872806684709,-11.8090161148345,3.0760060428892));
#36349=CARTESIAN_POINT('Ctrl Pts',(369.859340182432,-11.8098845013897,3.07176422181933));
#36350=CARTESIAN_POINT('Ctrl Pts',(369.828188527615,-11.8119043310831,3.06172626058127));
#36351=CARTESIAN_POINT('Ctrl Pts',(369.81052497947,-11.8130578875643,3.05586518729984));
#36352=CARTESIAN_POINT('Ctrl Pts',(369.755242552884,-11.8166947886424,3.03698841249678));
#36353=CARTESIAN_POINT('Ctrl Pts',(369.717814615654,-11.8191959671586,3.02342891666998));
#36354=CARTESIAN_POINT('Ctrl Pts',(369.630340167541,-11.8251360263154,2.98989268230858));
#36355=CARTESIAN_POINT('Ctrl Pts',(369.580525720259,-11.828592884644,2.96934761609316));
#36356=CARTESIAN_POINT('Ctrl Pts',(369.39899606385,-11.8414663844915,2.88909657554114));
#36357=CARTESIAN_POINT('Ctrl Pts',(369.270838623976,-11.8511109151109,2.82179952828718));
#36358=CARTESIAN_POINT('Ctrl Pts',(368.980461504223,-11.8740980524893,2.64345002079298));
#36359=CARTESIAN_POINT('Ctrl Pts',(368.822999134951,-11.8874964287456,2.52571083767808));
#36360=CARTESIAN_POINT('Ctrl Pts',(368.641845763597,-11.9034050575931,2.36250935539747));
#36361=CARTESIAN_POINT('Ctrl Pts',(368.60718137038,-11.906472889388,2.32986007244789));
#36362=CARTESIAN_POINT('Ctrl Pts',(368.56304485247,-11.9103958185939,2.28640365458869));
#36363=CARTESIAN_POINT('Ctrl Pts',(368.552905395979,-11.911298220028,2.2762864348408));
#36364=CARTESIAN_POINT('Ctrl Pts',(368.536746912794,-11.9127377203612,2.25994696046144));
#36365=CARTESIAN_POINT('Ctrl Pts',(368.530685052261,-11.9132780727926,2.25376760401024));
#36366=CARTESIAN_POINT('Ctrl Pts',(368.519083410428,-11.914312727692,2.24184537901794));
#36367=CARTESIAN_POINT('Ctrl Pts',(368.513540003973,-11.9148072990716,2.23610630427298));
#36368=CARTESIAN_POINT('Ctrl Pts',(368.500343216698,-11.9159853164569,2.22234176887064));
#36369=CARTESIAN_POINT('Ctrl Pts',(368.492709753879,-11.916667237063,2.2142971930392));
#36370=CARTESIAN_POINT('Ctrl Pts',(368.467462117026,-11.9189250638317,2.1874132328381));
#36371=CARTESIAN_POINT('Ctrl Pts',(368.450032075139,-11.9204876738813,2.16840128916409));
#36372=CARTESIAN_POINT('Ctrl Pts',(368.344532698208,-11.92998502054,2.05051673010516));
#36373=CARTESIAN_POINT('Ctrl Pts',(368.262388059105,-11.9375535760171,1.94649269399025));
#36374=CARTESIAN_POINT('Ctrl Pts',(368.112532472945,-11.9523636394316,1.73060591633995));
#36375=CARTESIAN_POINT('Ctrl Pts',(368.044761239028,-11.9595961258843,1.619100688336));
#36376=CARTESIAN_POINT('Ctrl Pts',(367.901745689382,-11.9768335638925,1.34802020291204));
#36377=CARTESIAN_POINT('Ctrl Pts',(367.832479999995,-11.9869029856521,1.18578920271957));
#36378=CARTESIAN_POINT('Ctrl Pts',(367.768152498204,-11.9990827204937,0.992722890854623));
#36379=CARTESIAN_POINT('Ctrl Pts',(367.759821191599,-12.0007333857915,0.966612088844642));
#36380=CARTESIAN_POINT('Ctrl Pts',(367.746711062784,-12.0034571678305,0.923638947765207));
#36381=CARTESIAN_POINT('Ctrl Pts',(367.741734867764,-12.00452383636,0.906837944387569));
#36382=CARTESIAN_POINT('Ctrl Pts',(367.733033131896,-12.0064500627239,0.8765536477412));
#36383=CARTESIAN_POINT('Ctrl Pts',(367.729257873778,-12.0073079784438,0.863085009950679));
#36384=CARTESIAN_POINT('Ctrl Pts',(367.721390677083,-12.0091444670223,0.834298114550317));
#36385=CARTESIAN_POINT('Ctrl Pts',(367.717323875372,-12.0101238291342,0.818973427886168));
#36386=CARTESIAN_POINT('Ctrl Pts',(367.709256713097,-12.0121297367344,0.787643690997719));
#36387=CARTESIAN_POINT('Ctrl Pts',(367.705265841131,-12.0131565561216,0.771636703934783));
#36388=CARTESIAN_POINT('Ctrl Pts',(367.695555025851,-12.0157445624619,0.731373066669527));
#36389=CARTESIAN_POINT('Ctrl Pts',(367.689993305191,-12.017310747722,0.707079719589981));
#36390=CARTESIAN_POINT('Ctrl Pts',(367.635871250697,-12.0334580580604,0.457399293725478));
#36391=CARTESIAN_POINT('Ctrl Pts',(367.61135968054,-12.04881759431,0.227531725336061));
#36392=CARTESIAN_POINT('Ctrl Pts',(367.611569184861,-12.0643988168543,-0.00292968685778758));
#36393=CARTESIAN_POINT('Ctrl Pts',(367.611569185299,-12.064398849448,-0.00293016895121727));
#36394=CARTESIAN_POINT('Ctrl Pts',(367.6117542083,-12.0781570872375,-0.206427864357887));
#36395=CARTESIAN_POINT('Ctrl Pts',(367.631213200604,-12.092003793772,-0.409474255385796));
#36396=CARTESIAN_POINT('Ctrl Pts',(367.672822275905,-12.1060932782021,-0.625568631365891));
#36397=CARTESIAN_POINT('Ctrl Pts',(367.676070129401,-12.1071450578305,-0.64176455055575));
#36398=CARTESIAN_POINT('Ctrl Pts',(367.681537530109,-12.1088400013017,-0.667981371427391));
#36399=CARTESIAN_POINT('Ctrl Pts',(367.683680630376,-12.109487045387,-0.678017680393728));
#36400=CARTESIAN_POINT('Ctrl Pts',(367.68790391966,-12.1107292439422,-0.697343194677214));
#36401=CARTESIAN_POINT('Ctrl Pts',(367.689977393266,-12.111324754986,-0.706633745173765));
#36402=CARTESIAN_POINT('Ctrl Pts',(367.693830803858,-12.1124056494757,-0.723546764713816));
#36403=CARTESIAN_POINT('Ctrl Pts',(367.695597352845,-12.112891762404,-0.731171971110376));
#36404=CARTESIAN_POINT('Ctrl Pts',(367.699614361482,-12.1139764411908,-0.748228297610602));
#36405=CARTESIAN_POINT('Ctrl Pts',(367.70187960662,-12.1145741554716,-0.757655728814642));
#36406=CARTESIAN_POINT('Ctrl Pts',(367.708611379465,-12.1163108716069,-0.785125511946817));
#36407=CARTESIAN_POINT('Ctrl Pts',(367.713191571816,-12.117443600389,-0.803139964331464));
#36408=CARTESIAN_POINT('Ctrl Pts',(367.754821781399,-12.127331997432,-0.961139879758404));
#36409=CARTESIAN_POINT('Ctrl Pts',(367.801116540184,-12.1356130786958,-1.09853822829092));
#36410=CARTESIAN_POINT('Ctrl Pts',(367.868425382003,-12.145529286286,-1.26117858748274));
#36411=CARTESIAN_POINT('Ctrl Pts',(367.880764969715,-12.1472793310625,-1.28981199337713));
#36412=CARTESIAN_POINT('Ctrl Pts',(367.966316636863,-12.1589980429197,-1.48066199187576));
#36413=CARTESIAN_POINT('Ctrl Pts',(368.052438422537,-12.1688667573075,-1.63674510195214));
#36414=CARTESIAN_POINT('Ctrl Pts',(368.208491808732,-12.1850669192214,-1.87134434351492));
#36415=CARTESIAN_POINT('Ctrl Pts',(368.270118424236,-12.1911442262168,-1.9549348308105));
#36416=CARTESIAN_POINT('Ctrl Pts',(368.351519434048,-12.1988865545592,-2.05486243783097));
#36417=CARTESIAN_POINT('Ctrl Pts',(368.367599090316,-12.2004031621987,-2.07413743980714));
#36418=CARTESIAN_POINT('Ctrl Pts',(368.394207442995,-12.2028933404432,-2.10528632118395));
#36419=CARTESIAN_POINT('Ctrl Pts',(368.404601764913,-12.2038614007074,-2.11727396063826));
#36420=CARTESIAN_POINT('Ctrl Pts',(368.424324378021,-12.2056897281283,-2.13968330065915));
#36421=CARTESIAN_POINT('Ctrl Pts',(368.433632846758,-12.2065491572045,-2.15012201225571));
#36422=CARTESIAN_POINT('Ctrl Pts',(368.45474420808,-12.2084907209646,-2.17348873104953));
#36423=CARTESIAN_POINT('Ctrl Pts',(368.466585007136,-12.2095744443927,-2.18638174774153));
#36424=CARTESIAN_POINT('Ctrl Pts',(368.497193880956,-12.2123629382171,-2.21917037543752));
#36425=CARTESIAN_POINT('Ctrl Pts',(368.516110963808,-12.2140740614256,-2.23892437584725));
#36426=CARTESIAN_POINT('Ctrl Pts',(368.684843314623,-12.2292336658742,-2.4106905148894));
#36427=CARTESIAN_POINT('Ctrl Pts',(368.849137322963,-12.2433458292923,-2.54768477596626));
#36428=CARTESIAN_POINT('Ctrl Pts',(369.204638274566,-12.2723160136977,-2.7887245465417));
#36429=CARTESIAN_POINT('Ctrl Pts',(369.395304238252,-12.2871010895774,-2.8917279797209));
#36430=CARTESIAN_POINT('Ctrl Pts',(369.625263340919,-12.3031817715121,-2.98753910223039));
#36431=CARTESIAN_POINT('Ctrl Pts',(369.655864929045,-12.3052870289112,-2.99974192270293));
#36432=CARTESIAN_POINT('Ctrl Pts',(369.69800522219,-12.3081337649691,-3.01580152624724));
#36433=CARTESIAN_POINT('Ctrl Pts',(369.709385456639,-12.3088973701244,-3.02006495879653));
#36434=CARTESIAN_POINT('Ctrl Pts',(369.728467547946,-12.3101688013097,-3.02709094761138));
#36435=CARTESIAN_POINT('Ctrl Pts',(369.736156211174,-12.3106786705317,-3.02988869681788));
#36436=CARTESIAN_POINT('Ctrl Pts',(369.75075519135,-12.3116420927194,-3.03513809899712));
#36437=CARTESIAN_POINT('Ctrl Pts',(369.757663337707,-12.3120959938415,-3.03759549297509));
#36438=CARTESIAN_POINT('Ctrl Pts',(369.774040176534,-12.3131674787552,-3.04335824206276));
#36439=CARTESIAN_POINT('Ctrl Pts',(369.783516094295,-12.31378386081,-3.04664303961672));
#36440=CARTESIAN_POINT('Ctrl Pts',(369.816741636835,-12.3159330244633,-3.0579871141462));
#36441=CARTESIAN_POINT('Ctrl Pts',(369.840570550915,-12.3174528587969,-3.06581358423771));
#36442=CARTESIAN_POINT('Ctrl Pts',(370.072634868581,-12.3320681881517,-3.13904370386693));
#36443=CARTESIAN_POINT('Ctrl Pts',(370.286944776711,-12.3441449553992,-3.18342043523946));
#36444=CARTESIAN_POINT('Ctrl Pts',(370.653116228036,-12.3647362895077,-3.22113628653369));
#36445=CARTESIAN_POINT('Ctrl Pts',(370.802993564648,-12.3731487806624,-3.22607614518034));
#36446=CARTESIAN_POINT('Ctrl Pts',(371.007654082844,-12.3850322006007,-3.21855562424913));
#36447=CARTESIAN_POINT('Ctrl Pts',(371.062582810677,-12.388259416517,-3.215126806208));
#36448=CARTESIAN_POINT('Ctrl Pts',(371.158040213895,-12.393951715271,-3.20670957445177));
#36449=CARTESIAN_POINT('Ctrl Pts',(371.19861248608,-12.3963976093135,-3.20235408048675));
#36450=CARTESIAN_POINT('Ctrl Pts',(371.257549385472,-12.3999939307747,-3.19489261949645));
#36451=CARTESIAN_POINT('Ctrl Pts',(371.275988067461,-12.4011252468538,-3.1923958368837));
#36452=CARTESIAN_POINT('Ctrl Pts',(371.308377461968,-12.4031238466458,-3.18772401181968));
#36453=CARTESIAN_POINT('Ctrl Pts',(371.322337549143,-12.4039889718342,-3.1856166835572));
#36454=CARTESIAN_POINT('Ctrl Pts',(371.349522925206,-12.4056811102607,-3.18133005924607));
#36455=CARTESIAN_POINT('Ctrl Pts',(371.362749369204,-12.406507819128,-3.17915984755733));
#36456=CARTESIAN_POINT('Ctrl Pts',(371.398318854658,-12.4087405074716,-3.17309546078506));
#36457=CARTESIAN_POINT('Ctrl Pts',(371.420634641974,-12.4101513246997,-3.1690478875971));
#36458=CARTESIAN_POINT('Ctrl Pts',(371.504473746837,-12.4154906214598,-3.15292554294454));
#36459=CARTESIAN_POINT('Ctrl Pts',(371.565679742452,-12.4194680992977,-3.13929248548913));
#36460=CARTESIAN_POINT('Ctrl Pts',(371.953872177133,-12.4452203610336,-3.04085792280429));
#36461=CARTESIAN_POINT('Ctrl Pts',(372.266119793206,-12.4686478013374,-2.90690209656326));
#36462=CARTESIAN_POINT('Ctrl Pts',(372.591529587359,-12.4940342692912,-2.70194833360715));
#36463=CARTESIAN_POINT('Ctrl Pts',(372.630672175652,-12.4971002273867,-2.67608472801488));
#36464=CARTESIAN_POINT('Ctrl Pts',(372.694717727381,-12.5021203444426,-2.63172766390991));
#36465=CARTESIAN_POINT('Ctrl Pts',(372.719942623918,-12.5040984918251,-2.61371336953807));
#36466=CARTESIAN_POINT('Ctrl Pts',(372.754368096213,-12.5067950992395,-2.58837066788114));
#36467=CARTESIAN_POINT('Ctrl Pts',(372.763793431962,-12.5075330795006,-2.58135229115478));
#36468=CARTESIAN_POINT('Ctrl Pts',(372.779650836886,-12.5087738300136,-2.56940902975383));
#36469=CARTESIAN_POINT('Ctrl Pts',(372.78610305614,-12.5092784393818,-2.56451120221236));
#36470=CARTESIAN_POINT('Ctrl Pts',(372.798421472808,-12.5102412614971,-2.5550869712785));
#36471=CARTESIAN_POINT('Ctrl Pts',(372.804290600115,-12.5106997599992,-2.55056461168414));
#36472=CARTESIAN_POINT('Ctrl Pts',(372.818304515359,-12.5117940977031,-2.53968919023706));
#36473=CARTESIAN_POINT('Ctrl Pts',(372.826434517592,-12.5124286105004,-2.53331708651532));
#36474=CARTESIAN_POINT('Ctrl Pts',(372.855661222793,-12.5147089234502,-2.5101821831586));
#36475=CARTESIAN_POINT('Ctrl Pts',(372.876578790837,-12.5163396024031,-2.49319353053628));
#36476=CARTESIAN_POINT('Ctrl Pts',(373.026031480407,-12.5280010398704,-2.3686691103941));
#36477=CARTESIAN_POINT('Ctrl Pts',(373.146234265238,-12.5374448404194,-2.25150131218711));
#36478=CARTESIAN_POINT('Ctrl Pts',(373.359786753583,-12.5555779962044,-2.00811191026386));
#36479=CARTESIAN_POINT('Ctrl Pts',(373.454114890907,-12.5642534711891,-1.88339267682397));
#36480=CARTESIAN_POINT('Ctrl Pts',(373.603757577794,-12.579984688018,-1.65242051387925));
#36481=CARTESIAN_POINT('Ctrl Pts',(373.662896443344,-12.5869203555053,-1.54900889517241));
#36482=CARTESIAN_POINT('Ctrl Pts',(373.728300777583,-12.5956897856033,-1.41834907046158));
#36483=CARTESIAN_POINT('Ctrl Pts',(373.740119215168,-12.5973256182555,-1.39397619388687));
#36484=CARTESIAN_POINT('Ctrl Pts',(373.758364430698,-12.5999356182627,-1.35510901111668));
#36485=CARTESIAN_POINT('Ctrl Pts',(373.764994052675,-12.6009027619704,-1.34071093796499));
#36486=CARTESIAN_POINT('Ctrl Pts',(373.777273736883,-12.6027303106228,-1.31351585537812));
#36487=CARTESIAN_POINT('Ctrl Pts',(373.782947237534,-12.6035898854513,-1.30072978734645));
#36488=CARTESIAN_POINT('Ctrl Pts',(373.795542200142,-12.6055330586501,-1.27183929074661));
#36489=CARTESIAN_POINT('Ctrl Pts',(373.802415830859,-12.6066182567808,-1.25571461327399));
#36490=CARTESIAN_POINT('Ctrl Pts',(373.819706714671,-12.6094130864331,-1.21421710840575));
#36491=CARTESIAN_POINT('Ctrl Pts',(373.829932049533,-12.6111291197151,-1.18876631537478));
#36492=CARTESIAN_POINT('Ctrl Pts',(373.915959652653,-12.626136811526,-0.966483301202008));
#36493=CARTESIAN_POINT('Ctrl Pts',(373.972580178387,-12.6400754043301,-0.762814937114291));
#36494=CARTESIAN_POINT('Ctrl Pts',(374.036838934751,-12.6652303425127,-0.39533131920048));
#36495=CARTESIAN_POINT('Ctrl Pts',(374.052676132839,-12.6762831120727,-0.233666969480691));
#36496=CARTESIAN_POINT('Ctrl Pts',(374.058074828667,-12.6924245341085,0.00962796764017243));
#36497=CARTESIAN_POINT('Ctrl Pts',(374.056810661789,-12.6977248817109,0.0907975905886753));
#36498=CARTESIAN_POINT('Ctrl Pts',(374.051616806316,-12.7039100781261,0.188066680497945));
#36499=CARTESIAN_POINT('Ctrl Pts',(374.05062759326,-12.7049359339655,0.204287326461232));
#36500=CARTESIAN_POINT('Ctrl Pts',(374.048894465196,-12.7065247547634,0.229558732048791));
#36501=CARTESIAN_POINT('Ctrl Pts',(374.048234935932,-12.7070922173073,0.238614743759082));
#36502=CARTESIAN_POINT('Ctrl Pts',(374.046932802362,-12.7081471202061,0.255508492960422));
#36503=CARTESIAN_POINT('Ctrl Pts',(374.046299790357,-12.7086350597758,0.263346612889715));
#36504=CARTESIAN_POINT('Ctrl Pts',(374.044788954213,-12.7097454826759,0.281237800384297));
#36505=CARTESIAN_POINT('Ctrl Pts',(374.043892598549,-12.710366926586,0.291289119642901));
#36506=CARTESIAN_POINT('Ctrl Pts',(374.041382843648,-12.7120132079993,0.318013015696647));
#36507=CARTESIAN_POINT('Ctrl Pts',(374.039686624672,-12.7130336151994,0.334677751157605));
#36508=CARTESIAN_POINT('Ctrl Pts',(374.024654089963,-12.7213812569281,0.471749781399621));
#36509=CARTESIAN_POINT('Ctrl Pts',(374.004666643777,-12.7283768241564,0.591344543833876));
#36510=CARTESIAN_POINT('Ctrl Pts',(373.965984771626,-12.7383401045756,0.762727125022461));
#36511=CARTESIAN_POINT('Ctrl Pts',(373.952632546719,-12.7414049217965,0.815600427294968));
#36512=CARTESIAN_POINT('Ctrl Pts',(373.93375679263,-12.7453315351225,0.883084127791017));
#36513=CARTESIAN_POINT('Ctrl Pts',(373.92946020549,-12.7462019627148,0.898027358878514));
#36514=CARTESIAN_POINT('Ctrl Pts',(373.874828557825,-12.7569926517417,1.08298178415095));
#36515=CARTESIAN_POINT('Ctrl Pts',(373.810655724516,-12.766856655951,1.24858446194856));
#36516=CARTESIAN_POINT('Ctrl Pts',(373.706715849474,-12.7806063867538,1.46257310957854));
#36517=CARTESIAN_POINT('Ctrl Pts',(373.678706258615,-12.7841487937767,1.51632592820138));
#36518=CARTESIAN_POINT('Ctrl Pts',(373.627802713589,-12.7903457274994,1.60763513833001));
#36519=CARTESIAN_POINT('Ctrl Pts',(373.605624456292,-12.7929759012183,1.64557219087209));
#36520=CARTESIAN_POINT('Ctrl Pts',(373.57267127624,-12.7967931184625,1.69938379028608));
#36521=CARTESIAN_POINT('Ctrl Pts',(373.562518899433,-12.797957510414,1.71563509026561));
#36522=CARTESIAN_POINT('Ctrl Pts',(373.544589298647,-12.7999943867305,1.74377407530293));
#36523=CARTESIAN_POINT('Ctrl Pts',(373.536877209764,-12.8008644435524,1.75570277887974));
#36524=CARTESIAN_POINT('Ctrl Pts',(373.520830289611,-12.8026626389804,1.78016715392233));
#36525=CARTESIAN_POINT('Ctrl Pts',(373.512485994002,-12.8035911178598,1.79269617175429));
#36526=CARTESIAN_POINT('Ctrl Pts',(373.490929217907,-12.80597339085,1.82457739949695));
#36527=CARTESIAN_POINT('Ctrl Pts',(373.477593070142,-12.8074318367744,1.84384454626085));
#36528=CARTESIAN_POINT('Ctrl Pts',(373.424554595977,-12.8131741134941,1.91871280885195));
#36529=CARTESIAN_POINT('Ctrl Pts',(373.383300777297,-12.8175169728635,1.97318781334541));
#36530=CARTESIAN_POINT('Ctrl Pts',(373.13224641922,-12.8432692579326,2.28367874991006));
#36531=CARTESIAN_POINT('Ctrl Pts',(372.885797985714,-12.8662196272001,2.50739310013837));
#36532=CARTESIAN_POINT('Ctrl Pts',(372.570733274303,-12.8911352031827,2.71535533576008));
#36533=CARTESIAN_POINT('Ctrl Pts',(372.531250598471,-12.8941833496627,2.7402030604942));
#36534=CARTESIAN_POINT('Ctrl Pts',(372.464767604646,-12.8991775411935,2.7800546391492));
#36535=CARTESIAN_POINT('Ctrl Pts',(372.438066932157,-12.9011472798606,2.79554274580632));
#36536=CARTESIAN_POINT('Ctrl Pts',(372.400915074615,-12.9038344276492,2.81638568832534));
#36537=CARTESIAN_POINT('Ctrl Pts',(372.390651938227,-12.9045711830227,2.82207006031603));
#36538=CARTESIAN_POINT('Ctrl Pts',(372.373253644609,-12.9058104740178,2.83158255195063));
#36539=CARTESIAN_POINT('Ctrl Pts',(372.36613474309,-12.9063148390825,2.83544002573733));
#36540=CARTESIAN_POINT('Ctrl Pts',(372.352470004893,-12.9072776657621,2.84277796611814));
#36541=CARTESIAN_POINT('Ctrl Pts',(372.345926618902,-12.9077364100132,2.84626271844423));
#36542=CARTESIAN_POINT('Ctrl Pts',(372.330223581879,-12.9088319435341,2.8545561183552));
#36543=CARTESIAN_POINT('Ctrl Pts',(372.32105262085,-12.90946739984,2.85934333709121));
#36544=CARTESIAN_POINT('Ctrl Pts',(372.311179410827,-12.9101470130225,2.86443678343236));
#36545=CARTESIAN_POINT('Ctrl Pts',(372.310500074469,-12.9101937516832,2.86478693732804));
#36546=CARTESIAN_POINT('Ctrl Pts',(372.309820613641,-12.9102404761534,2.86513684952402));
#36547=CARTESIAN_POINT('Origin',(370.834317853224,2.31077344927308,0.));
#36548=CARTESIAN_POINT('',(372.309820634558,-14.4057934188676,2.86513683875239));
#36549=CARTESIAN_POINT('',(372.309820586043,-14.1558998485283,2.86513686373655));
#36550=CARTESIAN_POINT('',(372.309820613641,2.31077344927308,2.86513684952399));
#36551=CARTESIAN_POINT('',(367.61156856641,-13.562992962766,0.00214402399713387));
#36552=CARTESIAN_POINT('Ctrl Pts',(372.309820634558,-14.4057934188676,2.86513683875233));
#36553=CARTESIAN_POINT('Ctrl Pts',(372.382959820302,-14.4010303765177,2.82747124787015));
#36554=CARTESIAN_POINT('Ctrl Pts',(372.454634639736,-14.3961920686039,2.78701651963437));
#36555=CARTESIAN_POINT('Ctrl Pts',(372.547881285588,-14.3896216220975,2.7295713953753));
#36556=CARTESIAN_POINT('Ctrl Pts',(372.570891775765,-14.3879770929918,2.71498997819747));
#36557=CARTESIAN_POINT('Ctrl Pts',(372.607147668188,-14.3853475157019,2.6913656551277));
#36558=CARTESIAN_POINT('Ctrl Pts',(372.620515499913,-14.3843695256475,2.68251236620994));
#36559=CARTESIAN_POINT('Ctrl Pts',(372.645394096121,-14.3825332607743,2.66576727580749));
#36560=CARTESIAN_POINT('Ctrl Pts',(372.656920780774,-14.3816759140363,2.65789971314251));
#36561=CARTESIAN_POINT('Ctrl Pts',(372.682568802527,-14.3797532865835,2.64014830757586));
#36562=CARTESIAN_POINT('Ctrl Pts',(372.696662596199,-14.3786865401734,2.63022559820126));
#36563=CARTESIAN_POINT('Ctrl Pts',(372.738069216955,-14.3755216678856,2.60057369039509));
#36564=CARTESIAN_POINT('Ctrl Pts',(372.765152344579,-14.3734114553449,2.58052917105951));
#36565=CARTESIAN_POINT('Ctrl Pts',(372.826121092228,-14.3685669504248,2.5339083607561));
#36566=CARTESIAN_POINT('Ctrl Pts',(372.859797725736,-14.3658227592624,2.50707054699286));
#36567=CARTESIAN_POINT('Ctrl Pts',(372.971201364079,-14.3565101106993,2.4145800614553));
#36568=CARTESIAN_POINT('Ctrl Pts',(373.046349533906,-14.3498296651165,2.34592852847286));
#36569=CARTESIAN_POINT('Ctrl Pts',(373.275874905621,-14.328156722674,2.11539791273994));
#36570=CARTESIAN_POINT('Ctrl Pts',(373.416703716113,-14.3128072206561,1.94097560180862));
#36571=CARTESIAN_POINT('Ctrl Pts',(373.581504569827,-14.292720980829,1.68682431361183));
#36572=CARTESIAN_POINT('Ctrl Pts',(373.622197794874,-14.2875390088689,1.61868426949237));
#36573=CARTESIAN_POINT('Ctrl Pts',(373.668361004254,-14.2814359224326,1.53446915732441));
#36574=CARTESIAN_POINT('Ctrl Pts',(373.676270727446,-14.2803814665871,1.51976974082362));
#36575=CARTESIAN_POINT('Ctrl Pts',(373.688396570875,-14.2787519441865,1.4968093486478));
#36576=CARTESIAN_POINT('Ctrl Pts',(373.692691714588,-14.2781721257322,1.48859075184633));
#36577=CARTESIAN_POINT('Ctrl Pts',(373.700549684036,-14.2771066364563,1.47339540480515));
#36578=CARTESIAN_POINT('Ctrl Pts',(373.704122539358,-14.2766203607312,1.46642421981053));
#36579=CARTESIAN_POINT('Ctrl Pts',(373.712184429058,-14.2755188925491,1.45055193239317));
#36580=CARTESIAN_POINT('Ctrl Pts',(373.716657602832,-14.2749046886393,1.44164299009492));
#36581=CARTESIAN_POINT('Ctrl Pts',(373.730234105623,-14.2730306562572,1.41428771774177));
#36582=CARTESIAN_POINT('Ctrl Pts',(373.739202426687,-14.2717788741983,1.39577446395072));
#36583=CARTESIAN_POINT('Ctrl Pts',(373.759686696425,-14.2688839102828,1.35243613433621));
#36584=CARTESIAN_POINT('Ctrl Pts',(373.771065085396,-14.267248104756,1.32754742374431));
#36585=CARTESIAN_POINT('Ctrl Pts',(373.809789460465,-14.2615708282221,1.23990780177785));
#36586=CARTESIAN_POINT('Ctrl Pts',(373.835453580168,-14.2576057437109,1.17643025079055));
#36587=CARTESIAN_POINT('Ctrl Pts',(373.909704284815,-14.2453073855096,0.974492976662644));
#36588=CARTESIAN_POINT('Ctrl Pts',(373.950872306543,-14.2371700212011,0.833504716140744));
#36589=CARTESIAN_POINT('Ctrl Pts',(374.026064586071,-14.2175044293184,0.490554448711123));
#36590=CARTESIAN_POINT('Ctrl Pts',(374.050740718488,-14.2059223217358,0.287227620574676));
#36591=CARTESIAN_POINT('Ctrl Pts',(374.056708562384,-14.1920461094147,0.0554353521423061));
#36592=CARTESIAN_POINT('Ctrl Pts',(374.057064441013,-14.1903887291902,0.0279163228751384));
#36593=CARTESIAN_POINT('Ctrl Pts',(374.05706998929,-14.1876565241123,-0.0171532497813603));
#36594=CARTESIAN_POINT('Ctrl Pts',(374.056928793026,-14.186588223383,-0.0347026831279217));
#36595=CARTESIAN_POINT('Ctrl Pts',(374.056417596576,-14.1846607970022,-0.0662289496220695));
#36596=CARTESIAN_POINT('Ctrl Pts',(374.056099964636,-14.1838033302386,-0.0802062760947148));
#36597=CARTESIAN_POINT('Ctrl Pts',(374.055229179271,-14.1819697064445,-0.109990704766894));
#36598=CARTESIAN_POINT('Ctrl Pts',(374.054650587014,-14.1809927751095,-0.125796640763847));
#36599=CARTESIAN_POINT('Ctrl Pts',(374.052771048867,-14.1783405416755,-0.168533511177363));
#36600=CARTESIAN_POINT('Ctrl Pts',(374.051248469167,-14.1766583592929,-0.195452956420964));
#36601=CARTESIAN_POINT('Ctrl Pts',(374.041297529638,-14.1676028854456,-0.339338927783878));
#36602=CARTESIAN_POINT('Ctrl Pts',(374.026828302817,-14.1600425603066,-0.455786220552487));
#36603=CARTESIAN_POINT('Ctrl Pts',(373.960066060415,-14.1352374836005,-0.826516142479432));
#36604=CARTESIAN_POINT('Ctrl Pts',(373.883425862925,-14.1173738428641,-1.07533706582195));
#36605=CARTESIAN_POINT('Ctrl Pts',(373.74421844654,-14.0946748731369,-1.38758679756752));
#36606=CARTESIAN_POINT('Ctrl Pts',(373.707756374582,-14.0892815335187,-1.46159915732633));
#36607=CARTESIAN_POINT('Ctrl Pts',(373.661168151996,-14.083060811931,-1.54766651114144));
#36608=CARTESIAN_POINT('Ctrl Pts',(373.653747723095,-14.0820882694192,-1.56114364229234));
#36609=CARTESIAN_POINT('Ctrl Pts',(373.641449574097,-14.0805065921476,-1.58310607155174));
#36610=CARTESIAN_POINT('Ctrl Pts',(373.636629304403,-14.0798940137871,-1.59162302968303));
#36611=CARTESIAN_POINT('Ctrl Pts',(373.627885568865,-14.078796150606,-1.60690951693122));
#36612=CARTESIAN_POINT('Ctrl Pts',(373.623976198221,-14.0783099984584,-1.61368680335597));
#36613=CARTESIAN_POINT('Ctrl Pts',(373.615304157931,-14.0772418968173,-1.62859495365853));
#36614=CARTESIAN_POINT('Ctrl Pts',(373.610530498217,-14.0766606641023,-1.63671918944388));
#36615=CARTESIAN_POINT('Ctrl Pts',(373.596597463081,-14.0749831783583,-1.6601953155702));
#36616=CARTESIAN_POINT('Ctrl Pts',(373.587345733388,-14.0738927043682,-1.675492361436));
#36617=CARTESIAN_POINT('Ctrl Pts',(373.512470932783,-14.0652451293225,-1.79699748838582));
#36618=CARTESIAN_POINT('Ctrl Pts',(373.440846147328,-14.0580419709269,-1.89940027668488));
#36619=CARTESIAN_POINT('Ctrl Pts',(373.174275389007,-14.0336708237858,-2.23693585166541));
#36620=CARTESIAN_POINT('Ctrl Pts',(372.952046215584,-14.0171031812076,-2.44836893354479));
#36621=CARTESIAN_POINT('Ctrl Pts',(372.667994101945,-13.9964396180221,-2.65059181889527));
#36622=CARTESIAN_POINT('Ctrl Pts',(372.632092139148,-13.9938398088349,-2.67507250791494));
#36623=CARTESIAN_POINT('Ctrl Pts',(372.580937561458,-13.990146398229,-2.70845864449811));
#36624=CARTESIAN_POINT('Ctrl Pts',(372.566089017181,-13.9890755924274,-2.71797668325954));
#36625=CARTESIAN_POINT('Ctrl Pts',(372.540092179425,-13.9872026588786,-2.73434135571468));
#36626=CARTESIAN_POINT('Ctrl Pts',(372.528978839859,-13.9864025788897,-2.74124293595799));
#36627=CARTESIAN_POINT('Ctrl Pts',(372.505623705291,-13.9847222212517,-2.75555058330692));
#36628=CARTESIAN_POINT('Ctrl Pts',(372.493374018661,-13.9838414729973,-2.76294315861555));
#36629=CARTESIAN_POINT('Ctrl Pts',(372.464052347579,-13.9817344556938,-2.78037321881766));
#36630=CARTESIAN_POINT('Ctrl Pts',(372.44693642711,-13.9805054869996,-2.79033529617702));
#36631=CARTESIAN_POINT('Ctrl Pts',(372.388169695081,-13.9762884892279,-2.82381833715494));
#36632=CARTESIAN_POINT('Ctrl Pts',(372.346089189989,-13.9732731852639,-2.84656856216098));
#36633=CARTESIAN_POINT('Ctrl Pts',(372.108282807119,-13.9562485296687,-2.96837475240721));
#36634=CARTESIAN_POINT('Ctrl Pts',(371.903377006328,-13.9415795104655,-3.0481663906488));
#36635=CARTESIAN_POINT('Ctrl Pts',(371.507306265598,-13.9137899329238,-3.15751708262114));
#36636=CARTESIAN_POINT('Ctrl Pts',(371.318422412028,-13.9007788168646,-3.19194031028099));
#36637=CARTESIAN_POINT('Ctrl Pts',(371.101158331279,-13.886766863588,-3.21179357663753));
#36638=CARTESIAN_POINT('Ctrl Pts',(371.074700769921,-13.8850769066204,-3.21388207289667));
#36639=CARTESIAN_POINT('Ctrl Pts',(371.037975892387,-13.8827565610804,-3.21632497745265));
#36640=CARTESIAN_POINT('Ctrl Pts',(371.027728962352,-13.8821118829606,-3.21695743009893));
#36641=CARTESIAN_POINT('Ctrl Pts',(371.010101777729,-13.8810077974023,-3.21796087212121));
#36642=CARTESIAN_POINT('Ctrl Pts',(371.002723021314,-13.880547106484,-3.21835545963772));
#36643=CARTESIAN_POINT('Ctrl Pts',(370.987245095855,-13.8795839425694,-3.21912978291905));
#36644=CARTESIAN_POINT('Ctrl Pts',(370.979145755956,-13.8790817789292,-3.21950433783194));
#36645=CARTESIAN_POINT('Ctrl Pts',(370.959245408341,-13.8778522930659,-3.22034938328103));
#36646=CARTESIAN_POINT('Ctrl Pts',(370.947442917026,-13.8771268619889,-3.2207855834317));
#36647=CARTESIAN_POINT('Ctrl Pts',(370.904221940353,-13.8744831850842,-3.22214508232847));
#36648=CARTESIAN_POINT('Ctrl Pts',(370.872791682018,-13.8725855892519,-3.22267364858954));
#36649=CARTESIAN_POINT('Ctrl Pts',(370.793540387236,-13.8678522942749,-3.22284676010578));
#36650=CARTESIAN_POINT('Ctrl Pts',(370.74572452772,-13.8650437088517,-3.22188698149173));
#36651=CARTESIAN_POINT('Ctrl Pts',(370.526308521112,-13.8523017492764,-3.2125939503536));
#36652=CARTESIAN_POINT('Ctrl Pts',(370.355515650009,-13.8427820520571,-3.19161188295868));
#36653=CARTESIAN_POINT('Ctrl Pts',(369.979506076188,-13.821297895616,-3.11454065240209));
#36654=CARTESIAN_POINT('Ctrl Pts',(369.776548204138,-13.8093120954196,-3.05158548845113));
#36655=CARTESIAN_POINT('Ctrl Pts',(369.555993682115,-13.7949844123601,-2.95850579948095));
#36656=CARTESIAN_POINT('Ctrl Pts',(369.530871718826,-13.7933331753907,-2.94752393661939));
#36657=CARTESIAN_POINT('Ctrl Pts',(369.489932466155,-13.7906090528347,-2.92900194496375));
#36658=CARTESIAN_POINT('Ctrl Pts',(369.474030832833,-13.7895426250041,-2.9216508459907));
#36659=CARTESIAN_POINT('Ctrl Pts',(369.44555046054,-13.7876172363621,-2.90820186354971));
#36660=CARTESIAN_POINT('Ctrl Pts',(369.432949883728,-13.7867599195693,-2.90215105645311));
#36661=CARTESIAN_POINT('Ctrl Pts',(369.420163116282,-13.7858842630214,-2.89590814871538));
#36662=CARTESIAN_POINT('Ctrl Pts',(369.419937021312,-13.7858687778962,-2.8957977291467));
#36663=CARTESIAN_POINT('Ctrl Pts',(369.419423412503,-13.7858335969847,-2.89554681994938));
#36664=CARTESIAN_POINT('Ctrl Pts',(369.419135906786,-13.7858139006363,-2.89540631403934));
#36665=CARTESIAN_POINT('Ctrl Pts',(369.418580457975,-13.7857758424659,-2.89513476010358));
#36666=CARTESIAN_POINT('Ctrl Pts',(369.418312512383,-13.7857574808575,-2.8950037178176));
#36667=CARTESIAN_POINT('Ctrl Pts',(369.417794824369,-13.7857220001333,-2.89475044667677));
#36668=CARTESIAN_POINT('Ctrl Pts',(369.417545079384,-13.7857048811757,-2.8946282226075));
#36669=CARTESIAN_POINT('Ctrl Pts',(369.417062527004,-13.7856717999805,-2.89439198623828));
#36670=CARTESIAN_POINT('Ctrl Pts',(369.416829717291,-13.7856558378738,-2.89427797804366));
#36671=CARTESIAN_POINT('Ctrl Pts',(369.416379857303,-13.7856249904511,-2.89405761183954));
#36672=CARTESIAN_POINT('Ctrl Pts',(369.416162805518,-13.7856101052832,-2.8939512576389));
#36673=CARTESIAN_POINT('Ctrl Pts',(369.415743367183,-13.7855813374358,-2.8937456766034));
#36674=CARTESIAN_POINT('Ctrl Pts',(369.415540979105,-13.7855674548697,-2.89364645296755));
#36675=CARTESIAN_POINT('Ctrl Pts',(369.415149851497,-13.7855406231272,-2.89345464619168));
#36676=CARTESIAN_POINT('Ctrl Pts',(369.414961110401,-13.7855276740329,-2.89336206571109));
#36677=CARTESIAN_POINT('Ctrl Pts',(369.414596331939,-13.7855026449676,-2.89318309184767));
#36678=CARTESIAN_POINT('Ctrl Pts',(369.414420293248,-13.7854905650704,-2.89309670079112));
#36679=CARTESIAN_POINT('Ctrl Pts',(369.414080041353,-13.785467214616,-2.89292968350416));
#36680=CARTESIAN_POINT('Ctrl Pts',(369.413915827316,-13.7854559441447,-2.89284905945031));
#36681=CARTESIAN_POINT('Ctrl Pts',(369.399052406199,-13.784435738794,-2.88555000502674));
#36682=CARTESIAN_POINT('Ctrl Pts',(369.384408646909,-13.7834229104053,-2.87821976446236));
#36683=CARTESIAN_POINT('Ctrl Pts',(369.34280321651,-13.7805229127941,-2.85699520808018));
#36684=CARTESIAN_POINT('Ctrl Pts',(369.31598153105,-13.7786263393954,-2.84283172950432));
#36685=CARTESIAN_POINT('Ctrl Pts',(369.255929342394,-13.7743173716255,-2.81002824712919));
#36686=CARTESIAN_POINT('Ctrl Pts',(369.22282190765,-13.7718976156395,-2.79117352762084));
#36687=CARTESIAN_POINT('Ctrl Pts',(369.117096494607,-13.7640249521677,-2.72845469854341));
#36688=CARTESIAN_POINT('Ctrl Pts',(369.045878288009,-13.7584949218541,-2.68231172756911));
#36689=CARTESIAN_POINT('Ctrl Pts',(368.857022539799,-13.7432162600115,-2.54908296526954));
#36690=CARTESIAN_POINT('Ctrl Pts',(368.743365791275,-13.7333248526963,-2.45671222381672));
#36691=CARTESIAN_POINT('Ctrl Pts',(368.514004177493,-13.7121100277976,-2.24282479034526));
#36692=CARTESIAN_POINT('Ctrl Pts',(368.400686537784,-13.700815447,-2.1193319262361));
#36693=CARTESIAN_POINT('Ctrl Pts',(368.28084874251,-13.6883314452662,-1.96637712221873));
#36694=CARTESIAN_POINT('Ctrl Pts',(368.26449802244,-13.686615246178,-1.9449600596472));
#36695=CARTESIAN_POINT('Ctrl Pts',(368.24225575235,-13.6842654312969,-1.9150556691456));
#36696=CARTESIAN_POINT('Ctrl Pts',(368.23613403124,-13.6836170509212,-1.90674198168176));
#36697=CARTESIAN_POINT('Ctrl Pts',(368.225690641883,-13.6825083075489,-1.89241550917802));
#36698=CARTESIAN_POINT('Ctrl Pts',(368.221349594436,-13.6820466372323,-1.88641704517071));
#36699=CARTESIAN_POINT('Ctrl Pts',(368.212306754553,-13.6810833536757,-1.87383053335703));
#36700=CARTESIAN_POINT('Ctrl Pts',(368.207609054231,-13.6805820388714,-1.86723966227124));
#36701=CARTESIAN_POINT('Ctrl Pts',(368.196159401585,-13.6793578062898,-1.85104708879848));
#36702=CARTESIAN_POINT('Ctrl Pts',(368.189434897602,-13.6786367423717,-1.84142594254094));
#36703=CARTESIAN_POINT('Ctrl Pts',(368.165176832569,-13.6760271754919,-1.80631145923769));
#36704=CARTESIAN_POINT('Ctrl Pts',(368.147957447199,-13.6741586330463,-1.78060180987894));
#36705=CARTESIAN_POINT('Ctrl Pts',(368.10562582034,-13.6695128915414,-1.7153857478109));
#36706=CARTESIAN_POINT('Ctrl Pts',(368.08099844256,-13.6667615424212,-1.67557188147986));
#36707=CARTESIAN_POINT('Ctrl Pts',(367.916574611333,-13.6479437582438,-1.39633547379169));
#36708=CARTESIAN_POINT('Ctrl Pts',(367.807309376793,-13.632985027028,-1.14027317804745));
#36709=CARTESIAN_POINT('Ctrl Pts',(367.70632921381,-13.6116528487885,-0.781596973584567));
#36710=CARTESIAN_POINT('Ctrl Pts',(367.684579531842,-13.6061090129003,-0.688732860389243));
#36711=CARTESIAN_POINT('Ctrl Pts',(367.659866652626,-13.5981460572751,-0.557190128808284));
#36712=CARTESIAN_POINT('Ctrl Pts',(367.653434067656,-13.5958345392764,-0.519210378170908));
#36713=CARTESIAN_POINT('Ctrl Pts',(367.644999344619,-13.5924124102355,-0.463344773650182));
#36714=CARTESIAN_POINT('Ctrl Pts',(367.642463658908,-13.5913186208338,-0.445542041214505));
#36715=CARTESIAN_POINT('Ctrl Pts',(367.638210461133,-13.5893609195195,-0.413778831887916));
#36716=CARTESIAN_POINT('Ctrl Pts',(367.636435090719,-13.5884988552767,-0.39982647593943));
#36717=CARTESIAN_POINT('Ctrl Pts',(367.633186368712,-13.5868301723381,-0.372888159366781));
#36718=CARTESIAN_POINT('Ctrl Pts',(367.631700565209,-13.5860239643604,-0.359903958032274));
#36719=CARTESIAN_POINT('Ctrl Pts',(367.628665579648,-13.5842792491737,-0.331873251813965));
#36720=CARTESIAN_POINT('Ctrl Pts',(367.627143276899,-13.5833399153545,-0.316824208058947));
#36721=CARTESIAN_POINT('Ctrl Pts',(367.623706862157,-13.5810526565072,-0.280285705166007));
#36722=CARTESIAN_POINT('Ctrl Pts',(367.62190251251,-13.5797013341269,-0.25878689084371));
#36723=CARTESIAN_POINT('Ctrl Pts',(367.614432138253,-13.5733140782682,-0.157595806312809));
#36724=CARTESIAN_POINT('Ctrl Pts',(367.611515424219,-13.5681940848949,-0.0777356595354613));
#36725=CARTESIAN_POINT('Ctrl Pts',(367.61156856641,-13.562992962766,0.00214402399713387));
#36726=CARTESIAN_POINT('Ctrl Pts',(367.611568563846,-13.5629932138988,0.00214016705816293));
#36727=CARTESIAN_POINT('Ctrl Pts',(367.611619927406,-13.557957112477,0.0794854733120579));
#36728=CARTESIAN_POINT('Ctrl Pts',(367.614455661285,-13.5528481869056,0.156800545342477));
#36729=CARTESIAN_POINT('Ctrl Pts',(367.639344176801,-13.5299673258588,0.498765407849578));
#36730=CARTESIAN_POINT('Ctrl Pts',(367.69127196486,-13.5116185112246,0.760187110722052));
#36731=CARTESIAN_POINT('Ctrl Pts',(367.782882992887,-13.4927122912455,1.03708523160422));
#36732=CARTESIAN_POINT('Ctrl Pts',(367.791393124169,-13.4910309177668,1.061795493531));
#36733=CARTESIAN_POINT('Ctrl Pts',(367.806892903958,-13.4880989852698,1.10508350503192));
#36734=CARTESIAN_POINT('Ctrl Pts',(367.813755260639,-13.4868421895369,1.12370505323839));
#36735=CARTESIAN_POINT('Ctrl Pts',(367.824271867526,-13.4849775772108,1.15145007036586));
#36736=CARTESIAN_POINT('Ctrl Pts',(367.827796399084,-13.4843624979651,1.16062175248465));
#36737=CARTESIAN_POINT('Ctrl Pts',(367.833929114425,-13.4833091288076,1.17636514898691));
#36738=CARTESIAN_POINT('Ctrl Pts',(367.836517029087,-13.4828696516199,1.18294453364756));
#36739=CARTESIAN_POINT('Ctrl Pts',(367.842475177597,-13.4818692528679,1.19794710675121));
#36740=CARTESIAN_POINT('Ctrl Pts',(367.845859337157,-13.4813091751001,1.20636460854323));
#36741=CARTESIAN_POINT('Ctrl Pts',(367.855237110171,-13.4797789420895,1.22940853161697));
#36742=CARTESIAN_POINT('Ctrl Pts',(367.86130294611,-13.478813005324,1.24400554526578));
#36743=CARTESIAN_POINT('Ctrl Pts',(367.893149447667,-13.4738597185039,1.3190784108256));
#36744=CARTESIAN_POINT('Ctrl Pts',(367.92067064821,-13.4699678988689,1.37880409079837));
#36745=CARTESIAN_POINT('Ctrl Pts',(368.076266780615,-13.4496749719134,1.69097209189934));
#36746=CARTESIAN_POINT('Ctrl Pts',(368.235359057283,-13.4344264362882,1.92657030279664));
#36747=CARTESIAN_POINT('Ctrl Pts',(368.472693005957,-13.4139335943455,2.19417633649147));
#36748=CARTESIAN_POINT('Ctrl Pts',(368.524107252617,-13.4096068135094,2.2482454517249));
#36749=CARTESIAN_POINT('Ctrl Pts',(368.602244660278,-13.4031480404878,2.32490499330277));
#36750=CARTESIAN_POINT('Ctrl Pts',(368.627534854404,-13.4010745231461,2.34892371680636));
#36751=CARTESIAN_POINT('Ctrl Pts',(368.673948398402,-13.3972952285242,2.39159256691016));
#36752=CARTESIAN_POINT('Ctrl Pts',(368.694936188115,-13.395595555034,2.41038528086994));
#36753=CARTESIAN_POINT('Ctrl Pts',(368.728078139256,-13.3929244134895,2.4392871076154));
#36754=CARTESIAN_POINT('Ctrl Pts',(368.740065195887,-13.3919608522778,2.44958631597652));
#36755=CARTESIAN_POINT('Ctrl Pts',(368.761725899739,-13.3902239997095,2.46792185968114));
#36756=CARTESIAN_POINT('Ctrl Pts',(368.771371809608,-13.389452058033,2.47599057453288));
#36757=CARTESIAN_POINT('Ctrl Pts',(368.793558802275,-13.3876797765275,2.49433013514207));
#36758=CARTESIAN_POINT('Ctrl Pts',(368.80613056884,-13.3866779330902,2.50456316574871));
#36759=CARTESIAN_POINT('Ctrl Pts',(368.840639518646,-13.383934055128,2.53222217638655));
#36760=CARTESIAN_POINT('Ctrl Pts',(368.862727185813,-13.3821844883585,2.54945731733406));
#36761=CARTESIAN_POINT('Ctrl Pts',(368.982607180709,-13.372721866308,2.64051081783952));
#36762=CARTESIAN_POINT('Ctrl Pts',(369.084313404639,-13.3648046876333,2.70898652628737));
#36763=CARTESIAN_POINT('Ctrl Pts',(369.386402610686,-13.3416147704767,2.88825159746158));
#36764=CARTESIAN_POINT('Ctrl Pts',(369.595012725193,-13.3259379015153,2.98371646321091));
#36765=CARTESIAN_POINT('Ctrl Pts',(369.911412793433,-13.3036251017204,3.0895575315269));
#36766=CARTESIAN_POINT('Ctrl Pts',(370.012460965395,-13.2967134845157,3.11796011900538));
#36767=CARTESIAN_POINT('Ctrl Pts',(370.131567631651,-13.2889446623812,3.14524375545559));
#36768=CARTESIAN_POINT('Ctrl Pts',(370.148442398851,-13.2878527382977,3.14896666336384));
#36769=CARTESIAN_POINT('Ctrl Pts',(370.174441044922,-13.2861847118285,3.15448356965894));
#36770=CARTESIAN_POINT('Ctrl Pts',(370.18354381022,-13.2856033777491,3.15637404998738));
#36771=CARTESIAN_POINT('Ctrl Pts',(370.200329550209,-13.2845364825549,3.15978444327086));
#36772=CARTESIAN_POINT('Ctrl Pts',(370.208009871634,-13.2840503041112,3.16131574043263));
#36773=CARTESIAN_POINT('Ctrl Pts',(370.225449333487,-13.282950789669,3.16472675845341));
#36774=CARTESIAN_POINT('Ctrl Pts',(370.235211628193,-13.2823384272811,3.16658934300879));
#36775=CARTESIAN_POINT('Ctrl Pts',(370.260601800901,-13.2807535193165,3.17131200857584));
#36776=CARTESIAN_POINT('Ctrl Pts',(370.276242698395,-13.2797847950483,3.17410177992173));
#36777=CARTESIAN_POINT('Ctrl Pts',(370.383404182243,-13.2731957956341,3.19239890952743));
#36778=CARTESIAN_POINT('Ctrl Pts',(370.475545808282,-13.2677694422553,3.20406302671581));
#36779=CARTESIAN_POINT('Ctrl Pts',(370.649829625188,-13.2577409588413,3.21851085224441));
#36780=CARTESIAN_POINT('Ctrl Pts',(370.731820691672,-13.253120069872,3.22216439074434));
#36781=CARTESIAN_POINT('Ctrl Pts',(370.946559975826,-13.2410832183528,3.22352726875965));
#36782=CARTESIAN_POINT('Ctrl Pts',(371.07918011889,-13.2337104991944,3.21617290162159));
#36783=CARTESIAN_POINT('Ctrl Pts',(371.308176168338,-13.220650542556,3.18922506027394));
#36784=CARTESIAN_POINT('Ctrl Pts',(371.404808141843,-13.2150369429599,3.17336365952173));
#36785=CARTESIAN_POINT('Ctrl Pts',(371.541622956355,-13.206838688433,3.1444551470027));
#36786=CARTESIAN_POINT('Ctrl Pts',(371.582507278427,-13.2043566270811,3.13497863405927));
#36787=CARTESIAN_POINT('Ctrl Pts',(371.655205642414,-13.1998779904951,3.11662491904643));
#36788=CARTESIAN_POINT('Ctrl Pts',(371.687090636013,-13.1978910230441,3.10805181873635));
#36789=CARTESIAN_POINT('Ctrl Pts',(371.735279867953,-13.1948510444987,3.09429755986037));
#36790=CARTESIAN_POINT('Ctrl Pts',(371.751684446398,-13.1938096166597,3.08947381557511));
#36791=CARTESIAN_POINT('Ctrl Pts',(371.781398649639,-13.1919109715576,3.08047886756549));
#36792=CARTESIAN_POINT('Ctrl Pts',(371.79472113775,-13.1910551995858,3.07635134694511));
#36793=CARTESIAN_POINT('Ctrl Pts',(371.823400530402,-13.1892030475853,3.06726155900706));
#36794=CARTESIAN_POINT('Ctrl Pts',(371.838747738697,-13.1882057301692,3.06227017156905));
#36795=CARTESIAN_POINT('Ctrl Pts',(371.880334357556,-13.1854861558645,3.04839865894157));
#36796=CARTESIAN_POINT('Ctrl Pts',(371.906497336331,-13.1837565862836,3.03929531144641));
#36797=CARTESIAN_POINT('Ctrl Pts',(372.042965976973,-13.1746346813086,2.98983000534895));
#36798=CARTESIAN_POINT('Ctrl Pts',(372.151109583158,-13.1670555444702,2.94380158585669));
#36799=CARTESIAN_POINT('Ctrl Pts',(372.274353687302,-13.1580053499999,2.88319451772756));
#36800=CARTESIAN_POINT('Ctrl Pts',(372.292131192624,-13.1566896271526,2.87424663801461));
#36801=CARTESIAN_POINT('Ctrl Pts',(372.309820665215,-13.1553703139997,2.86513682296442));
#36802=CARTESIAN_POINT('Ctrl Pts',(372.309820613641,-12.9102404761534,2.86513684952402));
#36803=CARTESIAN_POINT('Ctrl Pts',(372.286441448171,-12.9118481907954,2.87717677117527));
#36804=CARTESIAN_POINT('Ctrl Pts',(372.262914918194,-12.913439105659,2.8889305350896));
#36805=CARTESIAN_POINT('Ctrl Pts',(372.091259356577,-12.9248716141687,2.9720791210119));
#36806=CARTESIAN_POINT('Ctrl Pts',(371.937984292497,-12.93414837264,3.03234062545723));
#36807=CARTESIAN_POINT('Ctrl Pts',(371.631953577968,-12.9520831075474,3.12636035604413));
#36808=CARTESIAN_POINT('Ctrl Pts',(371.480029325723,-12.9607269411464,3.16123498556991));
#36809=CARTESIAN_POINT('Ctrl Pts',(371.205434394874,-12.9765912106468,3.20364146885486));
#36810=CARTESIAN_POINT('Ctrl Pts',(371.083732505223,-12.9837023403462,3.21540566941334));
#36811=CARTESIAN_POINT('Ctrl Pts',(370.934409147797,-12.9926698366404,3.2213108124567));
#36812=CARTESIAN_POINT('Ctrl Pts',(370.907141152546,-12.9943169823515,3.22204256883709));
#36813=CARTESIAN_POINT('Ctrl Pts',(370.863976761459,-12.9969408946726,3.22265270955231));
#36814=CARTESIAN_POINT('Ctrl Pts',(370.848084532995,-12.9979105066855,3.22275978031297));
#36815=CARTESIAN_POINT('Ctrl Pts',(370.818209505811,-12.999740160901,3.22274007710108));
#36816=CARTESIAN_POINT('Ctrl Pts',(370.80422701618,-13.0005993515836,3.22263985191666));
#36817=CARTESIAN_POINT('Ctrl Pts',(370.77278116585,-13.0025382309515,3.22220978039875));
#36818=CARTESIAN_POINT('Ctrl Pts',(370.755319050345,-13.0036194899701,3.22182895304918));
#36819=CARTESIAN_POINT('Ctrl Pts',(370.71065148109,-13.0063974048413,3.22049145652653));
#36820=CARTESIAN_POINT('Ctrl Pts',(370.683453910574,-13.0081003321547,3.21933201004996));
#36821=CARTESIAN_POINT('Ctrl Pts',(370.491005328473,-13.0202342218608,3.2086838016476));
#36822=CARTESIAN_POINT('Ctrl Pts',(370.326711147957,-13.0310516420342,3.1868222384294));
#36823=CARTESIAN_POINT('Ctrl Pts',(369.958765212766,-13.0562041397443,3.10868275352858));
#36824=CARTESIAN_POINT('Ctrl Pts',(369.75748295412,-13.0706473433724,3.04481935190261));
#36825=CARTESIAN_POINT('Ctrl Pts',(369.491545499704,-13.0898216482894,2.93074635264705));
#36826=CARTESIAN_POINT('Ctrl Pts',(369.420369690378,-13.0949577700784,2.89707862443679));
#36827=CARTESIAN_POINT('Ctrl Pts',(369.336185061289,-13.1009785614437,2.85341470315282));
#36828=CARTESIAN_POINT('Ctrl Pts',(369.321933237326,-13.1019958994197,2.84588652780748));
#36829=CARTESIAN_POINT('Ctrl Pts',(369.299767029154,-13.1035744491439,2.83396422894176));
#36830=CARTESIAN_POINT('Ctrl Pts',(369.2918138888,-13.104140067464,2.82964326497738));
#36831=CARTESIAN_POINT('Ctrl Pts',(369.276980814297,-13.1051934064889,2.82150329148875));
#36832=CARTESIAN_POINT('Ctrl Pts',(369.270096712352,-13.1056816107886,2.81769261997482));
#36833=CARTESIAN_POINT('Ctrl Pts',(369.254377410618,-13.1067949705037,2.80891588984633));
#36834=CARTESIAN_POINT('Ctrl Pts',(369.245551626509,-13.107419065559,2.80393333760559));
#36835=CARTESIAN_POINT('Ctrl Pts',(369.222071217853,-13.109077117009,2.79053113013592));
#36836=CARTESIAN_POINT('Ctrl Pts',(369.207458853609,-13.110106542019,2.78203756709756));
#36837=CARTESIAN_POINT('Ctrl Pts',(369.05425721264,-13.1208811750762,2.69136793071538));
#36838=CARTESIAN_POINT('Ctrl Pts',(368.92193049366,-13.1300352627029,2.59901242594719));
#36839=CARTESIAN_POINT('Ctrl Pts',(368.643651016654,-13.1502022446611,2.37198062945402));
#36840=CARTESIAN_POINT('Ctrl Pts',(368.502113231917,-13.1611368512133,2.23296483055141));
#36841=CARTESIAN_POINT('Ctrl Pts',(368.309966137865,-13.1782697287666,2.00590670831466));
#36842=CARTESIAN_POINT('Ctrl Pts',(368.249261099568,-13.184102314845,1.92704230999386));
#36843=CARTESIAN_POINT('Ctrl Pts',(368.177579646931,-13.1916240614231,1.82442341090055));
#36844=CARTESIAN_POINT('Ctrl Pts',(368.163108733336,-13.1931782950302,1.80316955900734));
#36845=CARTESIAN_POINT('Ctrl Pts',(368.140296556113,-13.1956879367448,1.76878733534828));
#36846=CARTESIAN_POINT('Ctrl Pts',(368.131793138716,-13.1966372353208,1.75576750772298));
#36847=CARTESIAN_POINT('Ctrl Pts',(368.115791465747,-13.1984504407747,1.7308752149771));
#36848=CARTESIAN_POINT('Ctrl Pts',(368.108275906739,-13.1993136766097,1.71901425978035));
#36849=CARTESIAN_POINT('Ctrl Pts',(368.091285776715,-13.2012921730912,1.69180903070548));
#36850=CARTESIAN_POINT('Ctrl Pts',(368.081862072861,-13.2024092721472,1.67643369242913));
#36851=CARTESIAN_POINT('Ctrl Pts',(368.053129705791,-13.2058774746273,1.62865973149475));
#36852=CARTESIAN_POINT('Ctrl Pts',(368.034260918995,-13.2082443917468,1.59600156753857));
#36853=CARTESIAN_POINT('Ctrl Pts',(367.882553599153,-13.2280451782023,1.3224518192703));
#36854=CARTESIAN_POINT('Ctrl Pts',(367.780511068324,-13.2466077894303,1.06583145084524));
#36855=CARTESIAN_POINT('Ctrl Pts',(367.684067631582,-13.2728850866084,0.689197048027816));
#36856=CARTESIAN_POINT('Ctrl Pts',(367.661694710313,-13.2805421359322,0.577524557258675));
#36857=CARTESIAN_POINT('Ctrl Pts',(367.639802412825,-13.2904920994799,0.427350364695475));
#36858=CARTESIAN_POINT('Ctrl Pts',(367.634992214044,-13.292957093208,0.389708792662808));
#36859=CARTESIAN_POINT('Ctrl Pts',(367.627959231019,-13.2970901554726,0.325701330360645));
#36860=CARTESIAN_POINT('Ctrl Pts',(367.625394342988,-13.2987731905339,0.299377656379266));
#36861=CARTESIAN_POINT('Ctrl Pts',(367.622218740492,-13.3011347187371,0.262027954688159));
#36862=CARTESIAN_POINT('Ctrl Pts',(367.621340257219,-13.3018270603767,0.251026562332427));
#36863=CARTESIAN_POINT('Ctrl Pts',(367.61992470504,-13.3030140191443,0.232072775333055));
#36864=CARTESIAN_POINT('Ctrl Pts',(367.619360595705,-13.3035101189282,0.224122560233915));
#36865=CARTESIAN_POINT('Ctrl Pts',(367.618243879003,-13.3045428646993,0.207511598722008));
#36866=CARTESIAN_POINT('Ctrl Pts',(367.617696753942,-13.3050792063444,0.198850645169217));
#36867=CARTESIAN_POINT('Ctrl Pts',(367.616333495844,-13.3065018251594,0.175790330038743));
#36868=CARTESIAN_POINT('Ctrl Pts',(367.615579014496,-13.3073847380687,0.161387330596565));
#36869=CARTESIAN_POINT('Ctrl Pts',(367.612708634049,-13.3112161736672,0.0985153197607862));
#36870=CARTESIAN_POINT('Ctrl Pts',(367.611590537686,-13.314113725755,0.0500044601927247));
#36871=CARTESIAN_POINT('Ctrl Pts',(367.61152611906,-13.3223474708209,-0.0898895087334478));
#36872=CARTESIAN_POINT('Ctrl Pts',(367.615370097351,-13.3275739217479,-0.181230011163106));
#36873=CARTESIAN_POINT('Ctrl Pts',(367.631837053038,-13.3385888302066,-0.375432012577366));
#36874=CARTESIAN_POINT('Ctrl Pts',(367.645547218232,-13.3443540436448,-0.478095287026382));
#36875=CARTESIAN_POINT('Ctrl Pts',(367.699506737512,-13.3611356608664,-0.773064853962441));
#36876=CARTESIAN_POINT('Ctrl Pts',(367.752410616362,-13.3722147322438,-0.962551610862094));
#36877=CARTESIAN_POINT('Ctrl Pts',(367.835582377936,-13.3860994397021,-1.18114967775128));
#36878=CARTESIAN_POINT('Ctrl Pts',(367.849554857877,-13.38834846445,-1.21602578044464));
#36879=CARTESIAN_POINT('Ctrl Pts',(367.872057632562,-13.391851202847,-1.26946796292063));
#36880=CARTESIAN_POINT('Ctrl Pts',(367.880160390833,-13.3930905602898,-1.28821123330226));
#36881=CARTESIAN_POINT('Ctrl Pts',(367.894233939394,-13.3952073447871,-1.31993493907177));
#36882=CARTESIAN_POINT('Ctrl Pts',(367.900113996605,-13.3960816555932,-1.33295513097699));
#36883=CARTESIAN_POINT('Ctrl Pts',(367.912200235318,-13.3978588092789,-1.35925013091248));
#36884=CARTESIAN_POINT('Ctrl Pts',(367.918410770279,-13.3987617862099,-1.37252255485698));
#36885=CARTESIAN_POINT('Ctrl Pts',(367.933974561353,-13.4010000345116,-1.40520120538701));
#36886=CARTESIAN_POINT('Ctrl Pts',(367.943432190366,-13.40233890062,-1.42455666311944));
#36887=CARTESIAN_POINT('Ctrl Pts',(367.979730626407,-13.4074000944877,-1.49699273367187));
#36888=CARTESIAN_POINT('Ctrl Pts',(368.007843817285,-13.4111665687017,-1.54941900455738));
#36889=CARTESIAN_POINT('Ctrl Pts',(368.08266968058,-13.4208287695286,-1.68013605331761));
#36890=CARTESIAN_POINT('Ctrl Pts',(368.131280990857,-13.4267869839536,-1.75727464185757));
#36891=CARTESIAN_POINT('Ctrl Pts',(368.288882662348,-13.4451693581102,-1.98532149386245));
#36892=CARTESIAN_POINT('Ctrl Pts',(368.40772836387,-13.4578510523412,-2.12894281901863));
#36893=CARTESIAN_POINT('Ctrl Pts',(368.629914280375,-13.4791617846146,-2.35452146243552));
#36894=CARTESIAN_POINT('Ctrl Pts',(368.727119483038,-13.4878444156479,-2.44190274432244));
#36895=CARTESIAN_POINT('Ctrl Pts',(368.842539968626,-13.4972326517366,-2.53361824978247));
#36896=CARTESIAN_POINT('Ctrl Pts',(368.855793124139,-13.4982977068734,-2.54398123059253));
#36897=CARTESIAN_POINT('Ctrl Pts',(368.877141753162,-13.4999919089834,-2.56040651717105));
#36898=CARTESIAN_POINT('Ctrl Pts',(368.885185468138,-13.5006254434494,-2.56653516861279));
#36899=CARTESIAN_POINT('Ctrl Pts',(368.899537156368,-13.5017470900766,-2.57736359295761));
#36900=CARTESIAN_POINT('Ctrl Pts',(368.905833650295,-13.5022362244657,-2.58207825580126));
#36901=CARTESIAN_POINT('Ctrl Pts',(368.919424265962,-13.5032855859277,-2.59217713514573));
#36902=CARTESIAN_POINT('Ctrl Pts',(368.926723869801,-13.5038452861916,-2.59755364711292));
#36903=CARTESIAN_POINT('Ctrl Pts',(368.947118509198,-13.5053984723475,-2.6124429495335));
#36904=CARTESIAN_POINT('Ctrl Pts',(368.960262871797,-13.5063874311281,-2.621888151746));
#36905=CARTESIAN_POINT('Ctrl Pts',(369.038745747931,-13.5122246628598,-2.67739216387715));
#36906=CARTESIAN_POINT('Ctrl Pts',(369.105714076279,-13.5169292039206,-2.7211099237281));
#36907=CARTESIAN_POINT('Ctrl Pts',(369.361522119318,-13.5341642077513,-2.87484442207167));
#36908=CARTESIAN_POINT('Ctrl Pts',(369.559769261021,-13.5461176600429,-2.96806263918945));
#36909=CARTESIAN_POINT('Ctrl Pts',(369.91389369616,-13.5673162083844,-3.09249602278798));
#36910=CARTESIAN_POINT('Ctrl Pts',(370.065432153398,-13.576336753536,-3.13361104587745));
#36911=CARTESIAN_POINT('Ctrl Pts',(370.245815020426,-13.5873393023443,-3.16867619986333));
#36912=CARTESIAN_POINT('Ctrl Pts',(370.272343236258,-13.5889635615388,-3.17348844447893));
#36913=CARTESIAN_POINT('Ctrl Pts',(370.316073489549,-13.5916525827218,-3.18085564732622));
#36914=CARTESIAN_POINT('Ctrl Pts',(370.33324169018,-13.5927111781906,-3.18360527232994));
#36915=CARTESIAN_POINT('Ctrl Pts',(370.364248977605,-13.5946286782402,-3.18831431226065));
#36916=CARTESIAN_POINT('Ctrl Pts',(370.378080242129,-13.5954860048598,-3.19032288868732));
#36917=CARTESIAN_POINT('Ctrl Pts',(370.407719992446,-13.5973276749636,-3.19443048668303));
#36918=CARTESIAN_POINT('Ctrl Pts',(370.423531819054,-13.5983128547538,-3.19650225850004));
#36919=CARTESIAN_POINT('Ctrl Pts',(370.46667817246,-13.6010088363461,-3.20183016298354));
#36920=CARTESIAN_POINT('Ctrl Pts',(370.49403959225,-13.602726903101,-3.20485350009033));
#36921=CARTESIAN_POINT('Ctrl Pts',(370.647330769736,-13.6124016167754,-3.21980648017633));
#36922=CARTESIAN_POINT('Ctrl Pts',(370.773824213373,-13.6205774322014,-3.22466302329149));
#36923=CARTESIAN_POINT('Ctrl Pts',(371.04773027127,-13.6386776900056,-3.2190570557427));
#36924=CARTESIAN_POINT('Ctrl Pts',(371.194807116949,-13.6486485731016,-3.20591877876712));
#36925=CARTESIAN_POINT('Ctrl Pts',(371.506385445597,-13.6699907999034,-3.15636998119395));
#36926=CARTESIAN_POINT('Ctrl Pts',(371.670013244976,-13.6813332456391,-3.11704510448327));
#36927=CARTESIAN_POINT('Ctrl Pts',(371.855465674427,-13.6938609177849,-3.05681216452416));
#36928=CARTESIAN_POINT('Ctrl Pts',(371.88098647857,-13.6955771186469,-3.04816803683828));
#36929=CARTESIAN_POINT('Ctrl Pts',(371.916137600917,-13.6979272475361,-3.03576848349016));
#36930=CARTESIAN_POINT('Ctrl Pts',(371.925861964596,-13.698575937143,-3.03228555904644));
#36931=CARTESIAN_POINT('Ctrl Pts',(371.942532723594,-13.6996852867208,-3.02622409267568));
#36932=CARTESIAN_POINT('Ctrl Pts',(371.949487209822,-13.7001472547651,-3.02366826333973));
#36933=CARTESIAN_POINT('Ctrl Pts',(371.964026624075,-13.7011112666287,-3.01826792639088));
#36934=CARTESIAN_POINT('Ctrl Pts',(371.971609725868,-13.7016130109258,-3.0154187736737));
#36935=CARTESIAN_POINT('Ctrl Pts',(371.99016701882,-13.7028385004059,-3.00836639485828));
#36936=CARTESIAN_POINT('Ctrl Pts',(372.001129253375,-13.7035603865304,-3.00413162589996));
#36937=CARTESIAN_POINT('Ctrl Pts',(372.040920960685,-13.7061741677018,-2.98850920993887));
#36938=CARTESIAN_POINT('Ctrl Pts',(372.069609935322,-13.7080460274139,-2.97676535690087));
#36939=CARTESIAN_POINT('Ctrl Pts',(372.141281523077,-13.712701193836,-2.94621186656439));
#36940=CARTESIAN_POINT('Ctrl Pts',(372.18403217977,-13.7154585268944,-2.92687377064477));
#36941=CARTESIAN_POINT('Ctrl Pts',(372.531046997476,-13.73779952212,-2.76068182405692));
#36942=CARTESIAN_POINT('Ctrl Pts',(372.810915458976,-13.7557894625375,-2.5677531210639));
#36943=CARTESIAN_POINT('Ctrl Pts',(373.101056629995,-13.7792529894048,-2.29170871048624));
#36944=CARTESIAN_POINT('Ctrl Pts',(373.14512481176,-13.7829673123751,-2.24726587778122));
#36945=CARTESIAN_POINT('Ctrl Pts',(373.203351313582,-13.788103794728,-2.18501982654348));
#36946=CARTESIAN_POINT('Ctrl Pts',(373.21865792552,-13.7894767495379,-2.1683066107217));
#36947=CARTESIAN_POINT('Ctrl Pts',(373.24273233124,-13.7916733861606,-2.14145670716934));
#36948=CARTESIAN_POINT('Ctrl Pts',(373.251615543488,-13.7924921993686,-2.13142417053377));
#36949=CARTESIAN_POINT('Ctrl Pts',(373.269729978326,-13.7941791914049,-2.11070715889527));
#36950=CARTESIAN_POINT('Ctrl Pts',(373.278954055497,-13.7950476403,-2.10001684711344));
#36951=CARTESIAN_POINT('Ctrl Pts',(373.300176618383,-13.7970679369184,-2.07509149318551));
#36952=CARTESIAN_POINT('Ctrl Pts',(373.312122505579,-13.7982219010803,-2.0608125184652));
#36953=CARTESIAN_POINT('Ctrl Pts',(373.349888968601,-13.8019247485918,-2.01486698551734));
#36954=CARTESIAN_POINT('Ctrl Pts',(373.375230504184,-13.804492686541,-1.98281357161192));
#36955=CARTESIAN_POINT('Ctrl Pts',(373.433315409033,-13.8105814537097,-1.90640189792378));
#36956=CARTESIAN_POINT('Ctrl Pts',(373.465542668351,-13.8141209117993,-1.86166911273971));
#36957=CARTESIAN_POINT('Ctrl Pts',(373.581268781811,-13.8274526996217,-1.69202512678628));
#36958=CARTESIAN_POINT('Ctrl Pts',(373.657141591922,-13.8374910907921,-1.56216070074749));
#36959=CARTESIAN_POINT('Ctrl Pts',(373.819915694065,-13.8623021416418,-1.23269299518507));
#36960=CARTESIAN_POINT('Ctrl Pts',(373.896216542839,-13.8771449200178,-1.02864792981419));
#36961=CARTESIAN_POINT('Ctrl Pts',(373.957839906154,-13.8927116088205,-0.793958151326303));
#36962=CARTESIAN_POINT('Ctrl Pts',(373.963985783887,-13.8943238182866,-0.769375264308963));
#36963=CARTESIAN_POINT('Ctrl Pts',(373.972168925151,-13.8965554005894,-0.734921541099628));
#36964=CARTESIAN_POINT('Ctrl Pts',(373.974450623041,-13.8971877114994,-0.725110484981698));
#36965=CARTESIAN_POINT('Ctrl Pts',(373.978316116783,-13.8982765190564,-0.70812880337608));
#36966=CARTESIAN_POINT('Ctrl Pts',(373.979921457231,-13.8987342189227,-0.700963231882924));
#36967=CARTESIAN_POINT('Ctrl Pts',(373.983260885726,-13.8996980689643,-0.685814894684934));
#36968=CARTESIAN_POINT('Ctrl Pts',(373.984989139596,-13.9002038701308,-0.677830907726856));
#36969=CARTESIAN_POINT('Ctrl Pts',(373.989199847953,-13.9014540086259,-0.658014682701625));
#36970=CARTESIAN_POINT('Ctrl Pts',(373.991646143872,-13.9021963108078,-0.646174743527935));
#36971=CARTESIAN_POINT('Ctrl Pts',(374.00058990562,-13.9049729664398,-0.601623687266634));
#36972=CARTESIAN_POINT('Ctrl Pts',(374.006646370228,-13.9069838733238,-0.568824884895273));
#36973=CARTESIAN_POINT('Ctrl Pts',(374.048695384909,-13.9220592638356,-0.319492168098219));
#36974=CARTESIAN_POINT('Ctrl Pts',(374.062994254528,-13.9341635823893,-0.0998567989383284));
#36975=CARTESIAN_POINT('Ctrl Pts',(374.047073243879,-13.9581918143032,0.329040435217189));
#36976=CARTESIAN_POINT('Ctrl Pts',(374.01887701453,-13.970052312387,0.537244822403206));
#36977=CARTESIAN_POINT('Ctrl Pts',(373.964361770695,-13.9842382770039,0.767915933856757));
#36978=CARTESIAN_POINT('Ctrl Pts',(373.957713286412,-13.9858901114944,0.794525458908267));
#36979=CARTESIAN_POINT('Ctrl Pts',(373.946260492195,-13.9886154320116,0.837996312467507));
#36980=CARTESIAN_POINT('Ctrl Pts',(373.941656710622,-13.9896824572253,0.854909360333761));
#36981=CARTESIAN_POINT('Ctrl Pts',(373.933131291607,-13.9916090710798,0.885250534677492));
#36982=CARTESIAN_POINT('Ctrl Pts',(373.929259736393,-13.9924670147716,0.898692363991566));
#36983=CARTESIAN_POINT('Ctrl Pts',(373.920814607482,-13.9943032837923,0.927311495096885));
#36984=CARTESIAN_POINT('Ctrl Pts',(373.916216334613,-13.9952823963435,0.942481065620265));
#36985=CARTESIAN_POINT('Ctrl Pts',(373.903457628865,-13.9979446704448,0.983479699779878));
#36986=CARTESIAN_POINT('Ctrl Pts',(373.895083299703,-13.9996347940009,1.00924035391709));
#36987=CARTESIAN_POINT('Ctrl Pts',(373.848153266492,-14.0088114639682,1.14764481084955));
#36988=CARTESIAN_POINT('Ctrl Pts',(373.803706827241,-14.016491061896,1.25817959056921));
#36989=CARTESIAN_POINT('Ctrl Pts',(373.687045960847,-14.0346272231469,1.50746757623478));
#36990=CARTESIAN_POINT('Ctrl Pts',(373.61064550124,-14.0451844921597,1.64393250650828));
#36991=CARTESIAN_POINT('Ctrl Pts',(373.432411304373,-14.0670839221323,1.91418462638725));
#36992=CARTESIAN_POINT('Ctrl Pts',(373.329385395488,-14.0783940545185,2.0466658113701));
#36993=CARTESIAN_POINT('Ctrl Pts',(373.198365967598,-14.0908925000118,2.1904611785077));
#36994=CARTESIAN_POINT('Ctrl Pts',(373.179967713129,-14.0926089168508,2.21015169310762));
#36995=CARTESIAN_POINT('Ctrl Pts',(373.154177656337,-14.0949592868305,2.23706833940101));
#36996=CARTESIAN_POINT('Ctrl Pts',(373.146995412898,-14.0956080055059,2.24449254243677));
#36997=CARTESIAN_POINT('Ctrl Pts',(373.134600289968,-14.0967173916809,2.2571825736921));
#36998=CARTESIAN_POINT('Ctrl Pts',(373.129404770621,-14.0971793674422,2.26246513873443));
#36999=CARTESIAN_POINT('Ctrl Pts',(373.1184909944,-14.0981433804003,2.27348548307801));
#37000=CARTESIAN_POINT('Ctrl Pts',(373.112769259521,-14.0986451181604,2.27921968479659));
#37001=CARTESIAN_POINT('Ctrl Pts',(373.098694521531,-14.099870566984,2.29321912389067));
#37002=CARTESIAN_POINT('Ctrl Pts',(373.090317713041,-14.1005924192794,2.30146046861299));
#37003=CARTESIAN_POINT('Ctrl Pts',(373.059684110036,-14.1032059374681,2.33127071471267));
#37004=CARTESIAN_POINT('Ctrl Pts',(373.037160773617,-14.1050775733042,2.35256484534791));
#37005=CARTESIAN_POINT('Ctrl Pts',(372.979787410027,-14.1097320666282,2.40526049532694));
#37006=CARTESIAN_POINT('Ctrl Pts',(372.94455168734,-14.1124889600739,2.43623300820811));
#37007=CARTESIAN_POINT('Ctrl Pts',(372.724322232064,-14.1291979847971,2.62145204803921));
#37008=CARTESIAN_POINT('Ctrl Pts',(372.523427225698,-14.1422930003608,2.75513263163544));
#37009=CARTESIAN_POINT('Ctrl Pts',(372.309820586046,-14.1558998485281,2.86513686373549));
#37010=CARTESIAN_POINT('Origin',(370.834317853224,2.31077344927308,0.));
#37011=CARTESIAN_POINT('',(372.309820655984,-15.6509557951682,2.86513682771809));
#37012=CARTESIAN_POINT('',(372.309820571668,-15.4046310424783,2.86513687113949));
#37013=CARTESIAN_POINT('',(372.309820613641,2.31077344927308,2.86513684952399));
#37014=CARTESIAN_POINT('Ctrl Pts',(372.309820655984,-15.6509557951682,2.8651368277181));
#37015=CARTESIAN_POINT('Ctrl Pts',(372.419480262493,-15.6437537932502,2.80866376325994));
#37016=CARTESIAN_POINT('Ctrl Pts',(372.525847643811,-15.6368020532833,2.74592082701906));
#37017=CARTESIAN_POINT('Ctrl Pts',(372.744053914637,-15.6220875706104,2.59969457905109));
#37018=CARTESIAN_POINT('Ctrl Pts',(372.854572862225,-15.614350038891,2.51477082310849));
#37019=CARTESIAN_POINT('Ctrl Pts',(373.027440542832,-15.6012859858726,2.36316664714977));
#37020=CARTESIAN_POINT('Ctrl Pts',(373.093071307726,-15.5960669541733,2.30051620411554));
#37021=CARTESIAN_POINT('Ctrl Pts',(373.197073026259,-15.5872595003788,2.19249122515072));
#37022=CARTESIAN_POINT('Ctrl Pts',(373.236988817073,-15.5837348427075,2.14867432550738));
#37023=CARTESIAN_POINT('Ctrl Pts',(373.289709410992,-15.5788621102471,2.08749425296974));
#37024=CARTESIAN_POINT('Ctrl Pts',(373.303582982364,-15.5775582010808,2.07106485791478));
#37025=CARTESIAN_POINT('Ctrl Pts',(373.326622540085,-15.5753553706888,2.04322029672452));
#37026=CARTESIAN_POINT('Ctrl Pts',(373.335877163479,-15.574460078054,2.03187913992358));
#37027=CARTESIAN_POINT('Ctrl Pts',(373.354006433012,-15.5726852242698,2.00935087147635));
#37028=CARTESIAN_POINT('Ctrl Pts',(373.362884629099,-15.5718058345628,1.99816703839138));
#37029=CARTESIAN_POINT('Ctrl Pts',(373.384280025972,-15.5696613691217,1.97084439100659));
#37030=CARTESIAN_POINT('Ctrl Pts',(373.396718571911,-15.5683932203344,1.95464503735853));
#37031=CARTESIAN_POINT('Ctrl Pts',(373.431624614934,-15.5647722144595,1.90827930400172));
#37032=CARTESIAN_POINT('Ctrl Pts',(373.453718541171,-15.5624050363577,1.8778370963787));
#37033=CARTESIAN_POINT('Ctrl Pts',(373.595803116957,-15.5466689259618,1.67467746921286));
#37034=CARTESIAN_POINT('Ctrl Pts',(373.699154175144,-15.5326791833423,1.49098326481295));
#37035=CARTESIAN_POINT('Ctrl Pts',(373.865428829333,-15.5048019344976,1.11330875122911));
#37036=CARTESIAN_POINT('Ctrl Pts',(373.92936052755,-15.4910015914261,0.920767265776321));
#37037=CARTESIAN_POINT('Ctrl Pts',(373.982050123253,-15.4758622826663,0.69205470833421));
#37038=CARTESIAN_POINT('Ctrl Pts',(373.988819887316,-15.4738018889293,0.660511366434027));
#37039=CARTESIAN_POINT('Ctrl Pts',(373.997443121209,-15.4710133500097,0.617169689688758));
#37040=CARTESIAN_POINT('Ctrl Pts',(373.999706128549,-15.4702639410783,0.605455996560258));
#37041=CARTESIAN_POINT('Ctrl Pts',(374.003402213955,-15.46900980477,0.585737145734349));
#37042=CARTESIAN_POINT('Ctrl Pts',(374.004870118756,-15.4685031460104,0.577738717446529));
#37043=CARTESIAN_POINT('Ctrl Pts',(374.007609840541,-15.4675409350271,0.562485354214488));
#37044=CARTESIAN_POINT('Ctrl Pts',(374.008887080997,-15.4670850675665,0.555231511283665));
#37045=CARTESIAN_POINT('Ctrl Pts',(374.011869374486,-15.466002801693,0.537947397897834));
#37046=CARTESIAN_POINT('Ctrl Pts',(374.013551832461,-15.4653776662136,0.527913236144369));
#37047=CARTESIAN_POINT('Ctrl Pts',(374.019359269913,-15.4631660700878,0.492242783413518));
#37048=CARTESIAN_POINT('Ctrl Pts',(374.023222035485,-15.461593568289,0.466564033176625));
#37049=CARTESIAN_POINT('Ctrl Pts',(374.054825391804,-15.4477302503329,0.237700450547395));
#37050=CARTESIAN_POINT('Ctrl Pts',(374.063427402746,-15.436331269634,0.0323181754851601));
#37051=CARTESIAN_POINT('Ctrl Pts',(374.04397147451,-15.4160080442741,-0.330625899390931));
#37052=CARTESIAN_POINT('Ctrl Pts',(374.02385455652,-15.4071418901333,-0.48789422927185));
#37053=CARTESIAN_POINT('Ctrl Pts',(373.975153476964,-15.3929977768492,-0.727064156446861));
#37054=CARTESIAN_POINT('Ctrl Pts',(373.95469809173,-15.3879466991154,-0.810367812538036));
#37055=CARTESIAN_POINT('Ctrl Pts',(373.924156535075,-15.3813144317105,-0.916305272060674));
#37056=CARTESIAN_POINT('Ctrl Pts',(373.917097800655,-15.3798314760725,-0.939779855343723));
#37057=CARTESIAN_POINT('Ctrl Pts',(373.905205178846,-15.3774098897247,-0.977753599119451));
#37058=CARTESIAN_POINT('Ctrl Pts',(373.900534650598,-15.3764766163456,-0.992303182575875));
#37059=CARTESIAN_POINT('Ctrl Pts',(373.891355505176,-15.3746755411495,-1.0202142929322));
#37060=CARTESIAN_POINT('Ctrl Pts',(373.886862308014,-15.3738082647416,-1.03358054860042));
#37061=CARTESIAN_POINT('Ctrl Pts',(373.876357839396,-15.3718127616344,-1.06416296155162));
#37062=CARTESIAN_POINT('Ctrl Pts',(373.87028791874,-15.3706826148698,-1.08135832432973));
#37063=CARTESIAN_POINT('Ctrl Pts',(373.850472831337,-15.3670641533708,-1.13600994017068));
#37064=CARTESIAN_POINT('Ctrl Pts',(373.83617830905,-15.3645576937593,-1.17326169737432));
#37065=CARTESIAN_POINT('Ctrl Pts',(373.725679012622,-15.3459035874339,-1.44597516383213));
#37066=CARTESIAN_POINT('Ctrl Pts',(373.602605639725,-15.3288135254764,-1.66953579757567));
#37067=CARTESIAN_POINT('Ctrl Pts',(373.380752189736,-15.3030358408299,-1.97936063482201));
#37068=CARTESIAN_POINT('Ctrl Pts',(373.300904160425,-15.2944731657276,-2.07801636328373));
#37069=CARTESIAN_POINT('Ctrl Pts',(373.188180531725,-15.2834834480622,-2.20160967827205));
#37070=CARTESIAN_POINT('Ctrl Pts',(373.160352957041,-15.2808501318521,-2.23098984393509));
#37071=CARTESIAN_POINT('Ctrl Pts',(373.112515222625,-15.2764662125022,-2.27962819584946));
#37072=CARTESIAN_POINT('Ctrl Pts',(373.092796609984,-15.2746983057297,-2.29916545533747));
#37073=CARTESIAN_POINT('Ctrl Pts',(373.064736959048,-15.2722400531265,-2.32625764825913));
#37074=CARTESIAN_POINT('Ctrl Pts',(373.056605654732,-15.2715343164733,-2.3340267714441));
#37075=CARTESIAN_POINT('Ctrl Pts',(373.042619629455,-15.270331991283,-2.34725048729455));
#37076=CARTESIAN_POINT('Ctrl Pts',(373.036784996689,-15.2698338143784,-2.35272609380507));
#37077=CARTESIAN_POINT('Ctrl Pts',(373.025424391811,-15.2688704885271,-2.36330833977107));
#37078=CARTESIAN_POINT('Ctrl Pts',(373.019900892674,-15.2684051391282,-2.36841739409777));
#37079=CARTESIAN_POINT('Ctrl Pts',(373.004803466878,-15.2671412232917,-2.38228422285441));
#37080=CARTESIAN_POINT('Ctrl Pts',(372.995194341379,-15.266345507034,-2.39100370842384));
#37081=CARTESIAN_POINT('Ctrl Pts',(372.958098806748,-15.2633058301426,-2.42425854155291));
#37082=CARTESIAN_POINT('Ctrl Pts',(372.930243927449,-15.2610904781993,-2.44838092792098));
#37083=CARTESIAN_POINT('Ctrl Pts',(372.734110165144,-15.2459007574512,-2.61243225085012));
#37084=CARTESIAN_POINT('Ctrl Pts',(372.552353899354,-15.2338455841046,-2.73539546495539));
#37085=CARTESIAN_POINT('Ctrl Pts',(372.237775341001,-15.213844292626,-2.9043972369454));
#37086=CARTESIAN_POINT('Ctrl Pts',(372.111959712414,-15.206049221562,-2.96189861757119));
#37087=CARTESIAN_POINT('Ctrl Pts',(371.909155490287,-15.193429998353,-3.03925361898433));
#37088=CARTESIAN_POINT('Ctrl Pts',(371.834459248779,-15.1887729294291,-3.06464585342348));
#37089=CARTESIAN_POINT('Ctrl Pts',(371.736079904299,-15.1825912126904,-3.09410904419484));
#37090=CARTESIAN_POINT('Ctrl Pts',(371.713174145387,-15.1811486648937,-3.10069301047388));
#37091=CARTESIAN_POINT('Ctrl Pts',(371.675608547669,-15.1787766694294,-3.1110410687437));
#37092=CARTESIAN_POINT('Ctrl Pts',(371.660991240289,-15.1778521682368,-3.11495708844222));
#37093=CARTESIAN_POINT('Ctrl Pts',(371.632648776992,-15.1760564139625,-3.12233657107358));
#37094=CARTESIAN_POINT('Ctrl Pts',(371.618927294203,-15.175185598627,-3.12581284498552));
#37095=CARTESIAN_POINT('Ctrl Pts',(371.587144307575,-15.1731650258625,-3.13364245786491));
#37096=CARTESIAN_POINT('Ctrl Pts',(371.569067309054,-15.1720131872693,-3.13793019968481));
#37097=CARTESIAN_POINT('Ctrl Pts',(371.51018106823,-15.1682520546185,-3.15136088623723));
#37098=CARTESIAN_POINT('Ctrl Pts',(371.469232069749,-15.1656225413159,-3.15986553422013));
#37099=CARTESIAN_POINT('Ctrl Pts',(371.232875652219,-15.1503581367911,-3.20417440198651));
#37100=CARTESIAN_POINT('Ctrl Pts',(371.03468581796,-15.1371796311015,-3.22264042956758));
#37101=CARTESIAN_POINT('Ctrl Pts',(370.668032052834,-15.1124392265908,-3.22284182234561));
#37102=CARTESIAN_POINT('Ctrl Pts',(370.500222374741,-15.100988250811,-3.20978877467439));
#37103=CARTESIAN_POINT('Ctrl Pts',(370.287485838501,-15.0867693371363,-3.17637019941516));
#37104=CARTESIAN_POINT('Ctrl Pts',(370.240943955677,-15.0836783706995,-3.16800580337536));
#37105=CARTESIAN_POINT('Ctrl Pts',(370.164050381591,-15.0786221906244,-3.1524325030785));
#37106=CARTESIAN_POINT('Ctrl Pts',(370.133590064929,-15.0766325640451,-3.14580194936312));
#37107=CARTESIAN_POINT('Ctrl Pts',(370.091764456354,-15.0739233845355,-3.13605972412198));
#37108=CARTESIAN_POINT('Ctrl Pts',(370.08031395383,-15.0731840689812,-3.13332639063653));
#37109=CARTESIAN_POINT('Ctrl Pts',(370.061010042763,-15.0719419940891,-3.12860643201375));
#37110=CARTESIAN_POINT('Ctrl Pts',(370.053148746188,-15.0714373833856,-3.12665284408184));
#37111=CARTESIAN_POINT('Ctrl Pts',(370.038122705319,-15.0704752964603,-3.12285855697789));
#37112=CARTESIAN_POINT('Ctrl Pts',(370.030956842656,-15.070017530024,-3.12102280826911));
#37113=CARTESIAN_POINT('Ctrl Pts',(370.013831546844,-15.0689259122627,-3.11657276595199));
#37114=CARTESIAN_POINT('Ctrl Pts',(370.003878125414,-15.0682933749425,-3.11393536374566));
#37115=CARTESIAN_POINT('Ctrl Pts',(369.968116878759,-15.0660271213258,-3.10427588552541));
#37116=CARTESIAN_POINT('Ctrl Pts',(369.942383265577,-15.0644082864606,-3.09698009331305));
#37117=CARTESIAN_POINT('Ctrl Pts',(369.740479012171,-15.0517798096493,-3.03701230371523));
#37118=CARTESIAN_POINT('Ctrl Pts',(369.568995670286,-15.0414805518083,-2.96966397531245));
#37119=CARTESIAN_POINT('Ctrl Pts',(369.249091931811,-15.021513446328,-2.81124977245585));
#37120=CARTESIAN_POINT('Ctrl Pts',(369.100450592914,-15.0118720703791,-2.72208855957599));
#37121=CARTESIAN_POINT('Ctrl Pts',(368.91105929198,-14.9984072896181,-2.5866520869862));
#37122=CARTESIAN_POINT('Ctrl Pts',(368.863404077777,-14.9949107079591,-2.55052755251698));
#37123=CARTESIAN_POINT('Ctrl Pts',(368.782874126573,-14.98878719572,-2.48587752626968));
#37124=CARTESIAN_POINT('Ctrl Pts',(368.749520877183,-14.9861838322952,-2.45797268836977));
#37125=CARTESIAN_POINT('Ctrl Pts',(368.702364835397,-14.9823991790438,-2.41686940475033));
#37126=CARTESIAN_POINT('Ctrl Pts',(368.688097903176,-14.9812400116569,-2.40420907818868));
#37127=CARTESIAN_POINT('Ctrl Pts',(368.663420734415,-14.9792097353485,-2.3819161177755));
#37128=CARTESIAN_POINT('Ctrl Pts',(368.652960042747,-14.9783410146094,-2.37233993877343));
#37129=CARTESIAN_POINT('Ctrl Pts',(368.631515767031,-14.9765431826628,-2.35244715030342));
#37130=CARTESIAN_POINT('Ctrl Pts',(368.620540668944,-14.9756137151383,-2.34212194216377));
#37131=CARTESIAN_POINT('Ctrl Pts',(368.592609027097,-14.9732238738964,-2.31547254237094));
#37132=CARTESIAN_POINT('Ctrl Pts',(368.575758404433,-14.9717587837716,-2.29903908724636));
#37133=CARTESIAN_POINT('Ctrl Pts',(368.510165120646,-14.9659617516298,-2.23365256711393));
#37134=CARTESIAN_POINT('Ctrl Pts',(368.462824626564,-14.9615693598081,-2.18332508364247));
#37135=CARTESIAN_POINT('Ctrl Pts',(368.198832778224,-14.9358162937266,-1.88395391810426));
#37136=CARTESIAN_POINT('Ctrl Pts',(368.019904299637,-14.9129295125544,-1.60439022650103));
#37137=CARTESIAN_POINT('Ctrl Pts',(367.867704232485,-14.8880773822789,-1.25995747772335));
#37138=CARTESIAN_POINT('Ctrl Pts',(367.849794628134,-14.8850320631716,-1.21692677633703));
#37139=CARTESIAN_POINT('Ctrl Pts',(367.821593902832,-14.8800422872204,-1.14479825725582));
#37140=CARTESIAN_POINT('Ctrl Pts',(367.810776409617,-14.8780741757684,-1.11591485013125));
#37141=CARTESIAN_POINT('Ctrl Pts',(367.796421163476,-14.8753891912276,-1.07584324722349));
#37142=CARTESIAN_POINT('Ctrl Pts',(367.792527745835,-14.8746530017986,-1.06478539750903));
#37143=CARTESIAN_POINT('Ctrl Pts',(367.786049393996,-14.8734146532972,-1.0460604287733));
#37144=CARTESIAN_POINT('Ctrl Pts',(367.783432857731,-14.8729106675423,-1.0384044344821));
#37145=CARTESIAN_POINT('Ctrl Pts',(367.778475947558,-14.8719485756502,-1.02372002141383));
#37146=CARTESIAN_POINT('Ctrl Pts',(367.776130945283,-14.871490187225,-1.01669330349784));
#37147=CARTESIAN_POINT('Ctrl Pts',(367.770571877757,-14.8703955382334,-0.999842487840838));
#37148=CARTESIAN_POINT('Ctrl Pts',(367.767380783738,-14.8697606082728,-0.990010818754165));
#37149=CARTESIAN_POINT('Ctrl Pts',(367.756014991185,-14.8674745043403,-0.954410746900676));
#37150=CARTESIAN_POINT('Ctrl Pts',(367.748117044674,-14.8658385628919,-0.928554286094378));
#37151=CARTESIAN_POINT('Ctrl Pts',(367.694385006868,-14.8543387201679,-0.744381217167028));
#37152=CARTESIAN_POINT('Ctrl Pts',(367.660424408554,-14.8450416444261,-0.582833759388019));
#37153=CARTESIAN_POINT('Ctrl Pts',(367.620828268992,-14.8279965498355,-0.281142552622508));
#37154=CARTESIAN_POINT('Ctrl Pts',(367.611675000397,-14.820248482665,-0.141874364625561));
#37155=CARTESIAN_POINT('Ctrl Pts',(367.61146598773,-14.804658615031,0.132486177532188));
#37156=CARTESIAN_POINT('Ctrl Pts',(367.619838339009,-14.7968431345822,0.267286335011411));
#37157=CARTESIAN_POINT('Ctrl Pts',(367.640201994004,-14.7870406000304,0.429608870738332));
#37158=CARTESIAN_POINT('Ctrl Pts',(367.644151057036,-14.7853109856536,0.458012703061152));
#37159=CARTESIAN_POINT('Ctrl Pts',(367.650947421777,-14.7825759298296,0.502531482584673));
#37160=CARTESIAN_POINT('Ctrl Pts',(367.653539369659,-14.7815785546884,0.518684314282673));
#37161=CARTESIAN_POINT('Ctrl Pts',(367.658335537501,-14.7798096189369,0.547184795146043));
#37162=CARTESIAN_POINT('Ctrl Pts',(367.660489084109,-14.7790396811135,0.559540710868483));
#37163=CARTESIAN_POINT('Ctrl Pts',(367.665599739343,-14.7772663855529,0.587883839175676));
#37164=CARTESIAN_POINT('Ctrl Pts',(367.668605794752,-14.7762614891453,0.603861773061856));
#37165=CARTESIAN_POINT('Ctrl Pts',(367.677310623361,-14.7734531319098,0.648277794445586));
#37166=CARTESIAN_POINT('Ctrl Pts',(367.683272475573,-14.7716413476168,0.676662166689679));
#37167=CARTESIAN_POINT('Ctrl Pts',(367.724321222029,-14.7598393553334,0.85977295159897));
#37168=CARTESIAN_POINT('Ctrl Pts',(367.77040500797,-14.7494966607915,1.01178731832911));
#37169=CARTESIAN_POINT('Ctrl Pts',(367.91446306147,-14.7227872473142,1.3852728399237));
#37170=CARTESIAN_POINT('Ctrl Pts',(368.026526912386,-14.7061464893408,1.60026214889701));
#37171=CARTESIAN_POINT('Ctrl Pts',(368.194058917271,-14.6864626421441,1.8489272177312));
#37172=CARTESIAN_POINT('Ctrl Pts',(368.227852344572,-14.6826973002642,1.89626939476469));
#37173=CARTESIAN_POINT('Ctrl Pts',(368.272166239886,-14.6780347556983,1.95492517038413));
#37174=CARTESIAN_POINT('Ctrl Pts',(368.281509354715,-14.6770663338005,1.96711008926563));
#37175=CARTESIAN_POINT('Ctrl Pts',(368.296392936976,-14.675547125083,1.98623602188887));
#37176=CARTESIAN_POINT('Ctrl Pts',(368.301875481864,-14.6749924376846,1.99322152691901));
#37177=CARTESIAN_POINT('Ctrl Pts',(368.312288307713,-14.6739483497035,2.0063765600934));
#37178=CARTESIAN_POINT('Ctrl Pts',(368.317212346674,-14.6734585566383,2.01255057064139));
#37179=CARTESIAN_POINT('Ctrl Pts',(368.328788742094,-14.6723161165162,2.02695669682146));
#37180=CARTESIAN_POINT('Ctrl Pts',(368.335459011149,-14.6716647576191,2.03517421176685));
#37181=CARTESIAN_POINT('Ctrl Pts',(368.357295241436,-14.6695542213975,2.06180640113035));
#37182=CARTESIAN_POINT('Ctrl Pts',(368.372625605345,-14.668106318037,2.08008605786806));
#37183=CARTESIAN_POINT('Ctrl Pts',(368.456761783862,-14.6603301514437,2.17817541405429));
#37184=CARTESIAN_POINT('Ctrl Pts',(368.529253925528,-14.654234353839,2.25475179065898));
#37185=CARTESIAN_POINT('Ctrl Pts',(368.780858471539,-14.6344294578026,2.49568726017511));
#37186=CARTESIAN_POINT('Ctrl Pts',(368.974779197389,-14.62117631311,2.64334470517025));
#37187=CARTESIAN_POINT('Ctrl Pts',(369.269662967429,-14.6014205130628,2.81922828196928));
#37188=CARTESIAN_POINT('Ctrl Pts',(369.358217772903,-14.5955419526884,2.86658659373234));
#37189=CARTESIAN_POINT('Ctrl Pts',(369.473027051763,-14.5879082740031,2.92125367503386));
#37190=CARTESIAN_POINT('Ctrl Pts',(369.497364152839,-14.5862895928417,2.93247172488076));
#37191=CARTESIAN_POINT('Ctrl Pts',(369.536250510381,-14.5837011358999,2.94981147975506));
#37192=CARTESIAN_POINT('Ctrl Pts',(369.550710049389,-14.582738190549,2.9561322001436));
#37193=CARTESIAN_POINT('Ctrl Pts',(369.576785568937,-14.5810006088074,2.96730324701622));
#37194=CARTESIAN_POINT('Ctrl Pts',(369.588384718044,-14.5802273082243,2.97219222482454));
#37195=CARTESIAN_POINT('Ctrl Pts',(369.615656826155,-14.5784080911209,2.98349957203311));
#37196=CARTESIAN_POINT('Ctrl Pts',(369.631352214069,-14.5773603258432,2.98986254679237));
#37197=CARTESIAN_POINT('Ctrl Pts',(369.677053059222,-14.5743068596351,3.00797174884617));
#37198=CARTESIAN_POINT('Ctrl Pts',(369.707184755305,-14.5722903196723,3.01939177712752));
#37199=CARTESIAN_POINT('Ctrl Pts',(369.931522667188,-14.5572476653161,3.1005907432903));
#37200=CARTESIAN_POINT('Ctrl Pts',(370.13182645524,-14.543610081372,3.15201218383113));
#37201=CARTESIAN_POINT('Ctrl Pts',(370.564734213961,-14.5140699315101,3.21981609019599));
#37202=CARTESIAN_POINT('Ctrl Pts',(370.797047834559,-14.4981788607032,3.23086916491071));
#37203=CARTESIAN_POINT('Ctrl Pts',(371.052768884613,-14.4817639507858,3.21542929740228));
#37204=CARTESIAN_POINT('Ctrl Pts',(371.076974714773,-14.4802214603532,3.21369322571111));
#37205=CARTESIAN_POINT('Ctrl Pts',(371.110886678961,-14.4780784505727,3.2108756623871));
#37206=CARTESIAN_POINT('Ctrl Pts',(371.120610336352,-14.4774660585031,3.21002327944402));
#37207=CARTESIAN_POINT('Ctrl Pts',(371.138281787113,-14.4763570811278,3.20839325152281));
#37208=CARTESIAN_POINT('Ctrl Pts',(371.146230846521,-14.4758596962908,3.20763021858007));
#37209=CARTESIAN_POINT('Ctrl Pts',(371.162579548382,-14.4748398467784,3.20599955155334));
#37210=CARTESIAN_POINT('Ctrl Pts',(371.170978727587,-14.4743175779978,3.20512844120082));
#37211=CARTESIAN_POINT('Ctrl Pts',(371.192681651692,-14.4729721934408,3.20279129577709));
#37212=CARTESIAN_POINT('Ctrl Pts',(371.205980016667,-14.4721518242902,3.20127536258272));
#37213=CARTESIAN_POINT('Ctrl Pts',(371.262848154292,-14.468659351576,3.19443359472653));
#37214=CARTESIAN_POINT('Ctrl Pts',(371.306318290806,-14.4660291521273,3.18830052353345));
#37215=CARTESIAN_POINT('Ctrl Pts',(371.425177468573,-14.4589127948247,3.16904658591004));
#37216=CARTESIAN_POINT('Ctrl Pts',(371.500248395448,-14.4545015619683,3.15412576860375));
#37217=CARTESIAN_POINT('Ctrl Pts',(371.802124908353,-14.436852394796,3.08286570568824));
#37218=CARTESIAN_POINT('Ctrl Pts',(372.02301539167,-14.4240935452109,3.00461561056256));
#37219=CARTESIAN_POINT('Ctrl Pts',(372.259116579889,-14.4090751790053,2.89082587148885));
#37220=CARTESIAN_POINT('Ctrl Pts',(372.28455597185,-14.4074387292058,2.87814776360241));
#37221=CARTESIAN_POINT('Ctrl Pts',(372.309820634558,-14.4057934188676,2.86513683875233));
#37222=CARTESIAN_POINT('',(367.611568484837,-14.5621367793278,0.00201768782053767));
#37223=CARTESIAN_POINT('Ctrl Pts',(372.309820586045,-14.1558998485281,2.86513686373551));
#37224=CARTESIAN_POINT('Ctrl Pts',(372.223986561129,-14.1613675181967,2.90934010579923));
#37225=CARTESIAN_POINT('Ctrl Pts',(372.136099635432,-14.1669097736879,2.94972063990983));
#37226=CARTESIAN_POINT('Ctrl Pts',(371.988269349969,-14.1762564371237,3.0097259781714));
#37227=CARTESIAN_POINT('Ctrl Pts',(371.929457461496,-14.1799804756913,3.03162052081622));
#37228=CARTESIAN_POINT('Ctrl Pts',(371.848563681688,-14.1851283612968,3.05907463848042));
#37229=CARTESIAN_POINT('Ctrl Pts',(371.827004648204,-14.1865027145504,3.06613847225981));
#37230=CARTESIAN_POINT('Ctrl Pts',(371.792591562831,-14.1887010291996,3.07701295819168));
#37231=CARTESIAN_POINT('Ctrl Pts',(371.77978495866,-14.1895201083055,3.08097211792375));
#37232=CARTESIAN_POINT('Ctrl Pts',(371.753440591567,-14.1912072316123,3.08893675282229));
#37233=CARTESIAN_POINT('Ctrl Pts',(371.739900480351,-14.1920755432671,3.09293339185411));
#37234=CARTESIAN_POINT('Ctrl Pts',(371.708458733053,-14.1940948111414,3.10198990130513));
#37235=CARTESIAN_POINT('Ctrl Pts',(371.690538811805,-14.19524787698,3.10698395110427));
#37236=CARTESIAN_POINT('Ctrl Pts',(371.633200270867,-14.1989448871394,3.12242974014236));
#37237=CARTESIAN_POINT('Ctrl Pts',(371.593627335898,-14.20150780166,3.13228821534759));
#37238=CARTESIAN_POINT('Ctrl Pts',(371.500278255754,-14.2075825748627,3.15367058063603));
#37239=CARTESIAN_POINT('Ctrl Pts',(371.446374388373,-14.2111129467584,3.16457384372551));
#37240=CARTESIAN_POINT('Ctrl Pts',(371.244871072057,-14.2243937593663,3.19999159751943));
#37241=CARTESIAN_POINT('Ctrl Pts',(371.095912009801,-14.2343882016061,3.21559640364351));
#37242=CARTESIAN_POINT('Ctrl Pts',(370.728312221536,-14.2592198316396,3.22839125848892));
#37243=CARTESIAN_POINT('Ctrl Pts',(370.509980669571,-14.2741318438301,3.213808701539));
#37244=CARTESIAN_POINT('Ctrl Pts',(370.269786349402,-14.2897610465618,3.17302140301347));
#37245=CARTESIAN_POINT('Ctrl Pts',(370.244835285122,-14.2913745081963,3.168480872173));
#37246=CARTESIAN_POINT('Ctrl Pts',(370.210089462614,-14.293604826614,3.16173325281457));
#37247=CARTESIAN_POINT('Ctrl Pts',(370.200248220215,-14.2942346736358,3.15977435149492));
#37248=CARTESIAN_POINT('Ctrl Pts',(370.183230598161,-14.2953204059993,3.15630428310791));
#37249=CARTESIAN_POINT('Ctrl Pts',(370.176049997681,-14.2957774789257,3.15481453879244));
#37250=CARTESIAN_POINT('Ctrl Pts',(370.160870548104,-14.2967413894517,3.15161120782683));
#37251=CARTESIAN_POINT('Ctrl Pts',(370.152873018193,-14.2972478703358,3.14989165171628));
#37252=CARTESIAN_POINT('Ctrl Pts',(370.133018409303,-14.2985020423274,3.14554353782786));
#37253=CARTESIAN_POINT('Ctrl Pts',(370.121169339341,-14.2992476692183,3.14287834102476));
#37254=CARTESIAN_POINT('Ctrl Pts',(370.076453826311,-14.3020516640907,3.13255462980272));
#37255=CARTESIAN_POINT('Ctrl Pts',(370.043692030089,-14.3040859848517,3.1244467358504));
#37256=CARTESIAN_POINT('Ctrl Pts',(369.792393436752,-14.3195773498738,3.05804924326558));
#37257=CARTESIAN_POINT('Ctrl Pts',(369.580386001519,-14.332018490769,2.97740705792136));
#37258=CARTESIAN_POINT('Ctrl Pts',(369.198082779311,-14.3560257450671,2.78384097563209));
#37259=CARTESIAN_POINT('Ctrl Pts',(369.026641659745,-14.3674964530608,2.67569200545997));
#37260=CARTESIAN_POINT('Ctrl Pts',(368.844689098034,-14.3812464190204,2.53539974943799));
#37261=CARTESIAN_POINT('Ctrl Pts',(368.82311799837,-14.3829032746543,2.51832276451449));
#37262=CARTESIAN_POINT('Ctrl Pts',(368.788146039231,-14.3856352015933,2.48990092508703));
#37263=CARTESIAN_POINT('Ctrl Pts',(368.774614308145,-14.3867037578458,2.47871882160117));
#37264=CARTESIAN_POINT('Ctrl Pts',(368.75046320298,-14.3886320367758,2.45842695572304));
#37265=CARTESIAN_POINT('Ctrl Pts',(368.739810450985,-14.3894901023403,2.44935747333377));
#37266=CARTESIAN_POINT('Ctrl Pts',(368.717711302272,-14.3912861304441,2.43029322893714));
#37267=CARTESIAN_POINT('Ctrl Pts',(368.706275888992,-14.3922245842296,2.42028631694347));
#37268=CARTESIAN_POINT('Ctrl Pts',(368.675843627777,-14.3947467544945,2.39327321060066));
#37269=CARTESIAN_POINT('Ctrl Pts',(368.656977417908,-14.39633652132,2.37612209518331));
#37270=CARTESIAN_POINT('Ctrl Pts',(368.615734598434,-14.3998710875583,2.33772494081934));
#37271=CARTESIAN_POINT('Ctrl Pts',(368.59345582189,-14.4018200967631,2.31637795023291));
#37272=CARTESIAN_POINT('Ctrl Pts',(368.52697459957,-14.4077588625314,2.25082047322648));
#37273=CARTESIAN_POINT('Ctrl Pts',(368.483750797434,-14.4117893125636,2.2056426227508));
#37274=CARTESIAN_POINT('Ctrl Pts',(368.33858245214,-14.425927373716,2.04479535131051));
#37275=CARTESIAN_POINT('Ctrl Pts',(368.243648890569,-14.4362747606188,1.92309884255712));
#37276=CARTESIAN_POINT('Ctrl Pts',(368.047198427823,-14.4601204493167,1.63018635058073));
#37277=CARTESIAN_POINT('Ctrl Pts',(367.952068702746,-14.4736262941071,1.45540205072955));
#37278=CARTESIAN_POINT('Ctrl Pts',(367.863255122363,-14.4880636653893,1.24883681004773));
#37279=CARTESIAN_POINT('Ctrl Pts',(367.853177638638,-14.4897355994879,1.22458574715773));
#37280=CARTESIAN_POINT('Ctrl Pts',(367.839588517502,-14.4920357522168,1.19072178319475));
#37281=CARTESIAN_POINT('Ctrl Pts',(367.835824836624,-14.4926779380862,1.18121200266286));
#37282=CARTESIAN_POINT('Ctrl Pts',(367.82942236771,-14.4937791112338,1.16480693090007));
#37283=CARTESIAN_POINT('Ctrl Pts',(367.826761912075,-14.4942393647444,1.15792026003089));
#37284=CARTESIAN_POINT('Ctrl Pts',(367.8212227985,-14.4952032008594,1.14343420822557));
#37285=CARTESIAN_POINT('Ctrl Pts',(367.818349182529,-14.4957064646365,1.13583298806097));
#37286=CARTESIAN_POINT('Ctrl Pts',(367.811345283805,-14.496941314451,1.1170924524523));
#37287=CARTESIAN_POINT('Ctrl Pts',(367.807247736193,-14.4976709748604,1.10594087528126));
#37288=CARTESIAN_POINT('Ctrl Pts',(367.792383530459,-14.5003457860907,1.0647860034953));
#37289=CARTESIAN_POINT('Ctrl Pts',(367.782000123076,-14.5022696567905,1.03464501456254));
#37290=CARTESIAN_POINT('Ctrl Pts',(367.756879105932,-14.5070819782502,0.958051574230242));
#37291=CARTESIAN_POINT('Ctrl Pts',(367.742744331952,-14.5099421570616,0.911408638277277));
#37292=CARTESIAN_POINT('Ctrl Pts',(367.651482169859,-14.5296669372514,0.583647475138517));
#37293=CARTESIAN_POINT('Ctrl Pts',(367.611750993081,-14.5453464830234,0.293528753126043));
#37294=CARTESIAN_POINT('Ctrl Pts',(367.611568484837,-14.5621367793278,0.00201768782053767));
#37295=CARTESIAN_POINT('Ctrl Pts',(367.611568482398,-14.5621370039932,0.00201378720837838));
#37296=CARTESIAN_POINT('Ctrl Pts',(367.611529543686,-14.5657262072406,-0.0603014899340788));
#37297=CARTESIAN_POINT('Ctrl Pts',(367.613298001685,-14.5693556441044,-0.122602711417325));
#37298=CARTESIAN_POINT('Ctrl Pts',(367.619123992365,-14.5753575806756,-0.224029177529986));
#37299=CARTESIAN_POINT('Ctrl Pts',(367.622093417936,-14.5776982320454,-0.263200716430373));
#37300=CARTESIAN_POINT('Ctrl Pts',(367.627485851368,-14.5811558607185,-0.32043338973456));
#37301=CARTESIAN_POINT('Ctrl Pts',(367.629347258197,-14.5822555702037,-0.338544693856912));
#37302=CARTESIAN_POINT('Ctrl Pts',(367.632894712695,-14.5842002783055,-0.370404195808923));
#37303=CARTESIAN_POINT('Ctrl Pts',(367.634516128718,-14.5850432468155,-0.384159221583366));
#37304=CARTESIAN_POINT('Ctrl Pts',(367.637873932442,-14.5867039800211,-0.411147102473858));
#37305=CARTESIAN_POINT('Ctrl Pts',(367.639603956755,-14.587521529145,-0.424380477676149));
#37306=CARTESIAN_POINT('Ctrl Pts',(367.643209043072,-14.5891531316318,-0.450684451132964));
#37307=CARTESIAN_POINT('Ctrl Pts',(367.645082337404,-14.5899671142311,-0.463755031332736));
#37308=CARTESIAN_POINT('Ctrl Pts',(367.649713767579,-14.5919029387403,-0.494714036293463));
#37309=CARTESIAN_POINT('Ctrl Pts',(367.652542361493,-14.5930269887199,-0.512591317510589));
#37310=CARTESIAN_POINT('Ctrl Pts',(367.663120110933,-14.5970352283152,-0.575980746669439));
#37311=CARTESIAN_POINT('Ctrl Pts',(367.671696156822,-14.5999453753308,-0.621347400769385));
#37312=CARTESIAN_POINT('Ctrl Pts',(367.700889455498,-14.6089359498101,-0.759452330405161));
#37313=CARTESIAN_POINT('Ctrl Pts',(367.724633449776,-14.6151108731505,-0.851470184924121));
#37314=CARTESIAN_POINT('Ctrl Pts',(367.82339296904,-14.6374219417203,-1.17447643183663));
#37315=CARTESIAN_POINT('Ctrl Pts',(367.920381600721,-14.6541041518821,-1.39786380971215));
#37316=CARTESIAN_POINT('Ctrl Pts',(368.086491169778,-14.6762588318194,-1.68632334492067));
#37317=CARTESIAN_POINT('Ctrl Pts',(368.134719837601,-14.6821651427856,-1.76250150926248));
#37318=CARTESIAN_POINT('Ctrl Pts',(368.195595639249,-14.6889519677809,-1.85028140904557));
#37319=CARTESIAN_POINT('Ctrl Pts',(368.205215171511,-14.6900062229206,-1.86392471200062));
#37320=CARTESIAN_POINT('Ctrl Pts',(368.220285921368,-14.6916292470805,-1.8849506124113));
#37321=CARTESIAN_POINT('Ctrl Pts',(368.225663229509,-14.6922028227161,-1.89238548162658));
#37322=CARTESIAN_POINT('Ctrl Pts',(368.235700035469,-14.6932630573907,-1.90613866954504));
#37323=CARTESIAN_POINT('Ctrl Pts',(368.240350842862,-14.6937502669214,-1.91246289932247));
#37324=CARTESIAN_POINT('Ctrl Pts',(368.251049560078,-14.6948618280029,-1.92690033023722));
#37325=CARTESIAN_POINT('Ctrl Pts',(368.257112603532,-14.695485119697,-1.93500208383904));
#37326=CARTESIAN_POINT('Ctrl Pts',(368.273149413321,-14.6971167843962,-1.9562222121564));
#37327=CARTESIAN_POINT('Ctrl Pts',(368.283185953523,-14.6981209597262,-1.9692930653197));
#37328=CARTESIAN_POINT('Ctrl Pts',(368.360801338117,-14.7057626398311,-2.06878439063798));
#37329=CARTESIAN_POINT('Ctrl Pts',(368.432660357244,-14.7121285853512,-2.15178977397477));
#37330=CARTESIAN_POINT('Ctrl Pts',(368.648473988236,-14.7298793679245,-2.37676628524619));
#37331=CARTESIAN_POINT('Ctrl Pts',(368.801727361925,-14.7409658535802,-2.50908590259739));
#37332=CARTESIAN_POINT('Ctrl Pts',(369.043461084339,-14.7577911171689,-2.68102602330532));
#37333=CARTESIAN_POINT('Ctrl Pts',(369.122929835695,-14.7632252055085,-2.73243803474336));
#37334=CARTESIAN_POINT('Ctrl Pts',(369.239935230264,-14.7711831019791,-2.80102567857583));
#37335=CARTESIAN_POINT('Ctrl Pts',(369.275721381436,-14.7736112476814,-2.82109511080739));
#37336=CARTESIAN_POINT('Ctrl Pts',(369.340241994816,-14.7779857525509,-2.85567687128589));
#37337=CARTESIAN_POINT('Ctrl Pts',(369.368829465222,-14.7799228371907,-2.87045235737246));
#37338=CARTESIAN_POINT('Ctrl Pts',(369.412702618209,-14.7828962044104,-2.89230204465149));
#37339=CARTESIAN_POINT('Ctrl Pts',(369.42783094632,-14.7839215683452,-2.89968887260062));
#37340=CARTESIAN_POINT('Ctrl Pts',(369.44313006262,-14.7849587739765,-2.90701119875706));
#37341=CARTESIAN_POINT('Ctrl Pts',(369.443243891176,-14.7849664910133,-2.90706567014499));
#37342=CARTESIAN_POINT('Ctrl Pts',(369.44347956101,-14.784982468342,-2.90717843030899));
#37343=CARTESIAN_POINT('Ctrl Pts',(369.443601403232,-14.7849907287,-2.90723671834003));
#37344=CARTESIAN_POINT('Ctrl Pts',(369.44385368473,-14.785007832293,-2.90735738765271));
#37345=CARTESIAN_POINT('Ctrl Pts',(369.443984124403,-14.7850166755574,-2.90741976775063));
#37346=CARTESIAN_POINT('Ctrl Pts',(369.444254229332,-14.7850349875826,-2.90754891755886));
#37347=CARTESIAN_POINT('Ctrl Pts',(369.444393895036,-14.7850444563766,-2.90761568590466));
#37348=CARTESIAN_POINT('Ctrl Pts',(369.444683127018,-14.7850640652319,-2.9077539300466));
#37349=CARTESIAN_POINT('Ctrl Pts',(369.444832694614,-14.7850742053858,-2.90782540465923));
#37350=CARTESIAN_POINT('Ctrl Pts',(369.445142461662,-14.7850952065497,-2.90797340522548));
#37351=CARTESIAN_POINT('Ctrl Pts',(369.445302661015,-14.7851060675567,-2.90804992904742));
#37352=CARTESIAN_POINT('Ctrl Pts',(369.445634474543,-14.7851285635215,-2.90820839563492));
#37353=CARTESIAN_POINT('Ctrl Pts',(369.445806090231,-14.7851401985863,-2.90829033672642));
#37354=CARTESIAN_POINT('Ctrl Pts',(369.446161583289,-14.7851643000955,-2.9084600348383));
#37355=CARTESIAN_POINT('Ctrl Pts',(369.446345461694,-14.7851767666152,-2.90854778959569));
#37356=CARTESIAN_POINT('Ctrl Pts',(369.446726392235,-14.7852025928852,-2.90872954183718));
#37357=CARTESIAN_POINT('Ctrl Pts',(369.446923445436,-14.7852159527137,-2.90882353665617));
#37358=CARTESIAN_POINT('Ctrl Pts',(369.447331708293,-14.785243632247,-2.90901822803156));
#37359=CARTESIAN_POINT('Ctrl Pts',(369.447542919348,-14.7852579520536,-2.90911892160163));
#37360=CARTESIAN_POINT('Ctrl Pts',(369.447980556,-14.7852876233021,-2.90932750369134));
#37361=CARTESIAN_POINT('Ctrl Pts',(369.448206983806,-14.7853029749017,-2.90943538905564));
#37362=CARTESIAN_POINT('Ctrl Pts',(369.448676195715,-14.7853347871718,-2.9096588858121));
#37363=CARTESIAN_POINT('Ctrl Pts',(369.448918981691,-14.7853512479786,-2.90977449324957));
#37364=CARTESIAN_POINT('Ctrl Pts',(369.449422140198,-14.785385362104,-2.91001400506745));
#37365=CARTESIAN_POINT('Ctrl Pts',(369.449682514275,-14.7854030155383,-2.91013790459845));
#37366=CARTESIAN_POINT('Ctrl Pts',(369.450222172062,-14.7854396046585,-2.9103946130254));
#37367=CARTESIAN_POINT('Ctrl Pts',(369.450501458114,-14.7854585405159,-2.91052741659699));
#37368=CARTESIAN_POINT('Ctrl Pts',(369.45095012229,-14.7854889605257,-2.91074068214148));
#37369=CARTESIAN_POINT('Ctrl Pts',(369.451119488603,-14.785500443816,-2.91082116966564));
#37370=CARTESIAN_POINT('Ctrl Pts',(369.451525152882,-14.7855279485492,-2.91101390907347));
#37371=CARTESIAN_POINT('Ctrl Pts',(369.45176145728,-14.7855439704622,-2.91112614686676));
#37372=CARTESIAN_POINT('Ctrl Pts',(369.464636110533,-14.7864169016701,-2.9172393157375));
#37373=CARTESIAN_POINT('Ctrl Pts',(369.477313227918,-14.7872766423694,-2.92315783676663));
#37374=CARTESIAN_POINT('Ctrl Pts',(369.505982921319,-14.7892216200159,-2.93631606601768));
#37375=CARTESIAN_POINT('Ctrl Pts',(369.521996822386,-14.7903084690579,-2.94350797915841));
#37376=CARTESIAN_POINT('Ctrl Pts',(369.563258768175,-14.7931103964096,-2.9616352558956));
#37377=CARTESIAN_POINT('Ctrl Pts',(369.588589140412,-14.7948319315181,-2.97237859050976));
#37378=CARTESIAN_POINT('Ctrl Pts',(369.801060619626,-14.8092875278524,-3.05930086161237));
#37379=CARTESIAN_POINT('Ctrl Pts',(369.994815099907,-14.8226115143557,-3.11803650085941));
#37380=CARTESIAN_POINT('Ctrl Pts',(370.414642241851,-14.8514628291443,-3.20331911012692));
#37381=CARTESIAN_POINT('Ctrl Pts',(370.640664368604,-14.8669854764521,-3.22488589164837));
#37382=CARTESIAN_POINT('Ctrl Pts',(370.900846086614,-14.8837891595983,-3.22224009950534));
#37383=CARTESIAN_POINT('Ctrl Pts',(370.934597928943,-14.8859473316224,-3.22136638429714));
#37384=CARTESIAN_POINT('Ctrl Pts',(370.980467394636,-14.8888453255572,-3.21945731660136));
#37385=CARTESIAN_POINT('Ctrl Pts',(370.992600743006,-14.8896085645721,-3.21888360145778));
#37386=CARTESIAN_POINT('Ctrl Pts',(371.01289985147,-14.8908795556085,-3.2178087191754));
#37387=CARTESIAN_POINT('Ctrl Pts',(371.021067375818,-14.8913893478805,-3.21734503954768));
#37388=CARTESIAN_POINT('Ctrl Pts',(371.036552848112,-14.8923527529241,-3.21640674411154));
#37389=CARTESIAN_POINT('Ctrl Pts',(371.043871065989,-14.8928067129957,-3.2159382441647));
#37390=CARTESIAN_POINT('Ctrl Pts',(371.061197822731,-14.8938784976677,-3.21476961852181));
#37391=CARTESIAN_POINT('Ctrl Pts',(371.071204885147,-14.8944951189018,-3.21404772227204));
#37392=CARTESIAN_POINT('Ctrl Pts',(371.106493513815,-14.8966616417776,-3.21133633790211));
#37393=CARTESIAN_POINT('Ctrl Pts',(371.131755542328,-14.8981982525318,-3.20909513368419));
#37394=CARTESIAN_POINT('Ctrl Pts',(371.374156337586,-14.9128273865256,-3.18470265991466));
#37395=CARTESIAN_POINT('Ctrl Pts',(371.588572828108,-14.9249031331154,-3.14084106498018));
#37396=CARTESIAN_POINT('Ctrl Pts',(371.93967960176,-14.9454832122059,-3.0309513879916));
#37397=CARTESIAN_POINT('Ctrl Pts',(372.079137539878,-14.9538846835172,-2.97639217264208));
#37398=CARTESIAN_POINT('Ctrl Pts',(372.263982497451,-14.9657538279371,-2.88880594163498));
#37399=CARTESIAN_POINT('Ctrl Pts',(372.313057550088,-14.968978471874,-2.86399531935684));
#37400=CARTESIAN_POINT('Ctrl Pts',(372.397380354294,-14.9746666327631,-2.81861951332702));
#37401=CARTESIAN_POINT('Ctrl Pts',(372.432917359687,-14.9771110002828,-2.79861746871052));
#37402=CARTESIAN_POINT('Ctrl Pts',(372.484098876848,-14.980705486509,-2.76851696381506));
#37403=CARTESIAN_POINT('Ctrl Pts',(372.500051401872,-14.9818365219561,-2.7589482284486));
#37404=CARTESIAN_POINT('Ctrl Pts',(372.527963276131,-14.983834799941,-2.74187564456478));
#37405=CARTESIAN_POINT('Ctrl Pts',(372.539957925444,-14.9846998862187,-2.73443025195699));
#37406=CARTESIAN_POINT('Ctrl Pts',(372.563245523905,-14.9863920802445,-2.7197621884444));
#37407=CARTESIAN_POINT('Ctrl Pts',(372.574543104809,-14.9872188844856,-2.71254738524966));
#37408=CARTESIAN_POINT('Ctrl Pts',(372.604839728448,-14.9894521568887,-2.69293233776965));
#37409=CARTESIAN_POINT('Ctrl Pts',(372.623753109014,-14.9908634673373,-2.68040178136115));
#37410=CARTESIAN_POINT('Ctrl Pts',(372.694476070924,-14.9962067746047,-2.63246401506292));
#37411=CARTESIAN_POINT('Ctrl Pts',(372.74537731758,-15.0001878644663,-2.59574772045186));
#37412=CARTESIAN_POINT('Ctrl Pts',(373.063186167333,-15.0259400767039,-2.35208812934773));
#37413=CARTESIAN_POINT('Ctrl Pts',(373.297165870306,-15.049362723905,-2.10581814719845));
#37414=CARTESIAN_POINT('Ctrl Pts',(373.515235068,-15.07474446331,-1.78913401456201));
#37415=CARTESIAN_POINT('Ctrl Pts',(373.540991783389,-15.0778102481464,-1.74992408904023));
#37416=CARTESIAN_POINT('Ctrl Pts',(373.582330977327,-15.0828301131175,-1.68389488407781));
#37417=CARTESIAN_POINT('Ctrl Pts',(373.598398297926,-15.0848081787999,-1.65738878096312));
#37418=CARTESIAN_POINT('Ctrl Pts',(373.620027139034,-15.0875046943282,-1.62051825677079));
#37419=CARTESIAN_POINT('Ctrl Pts',(373.62591750103,-15.0882426627077,-1.61034998121272));
#37420=CARTESIAN_POINT('Ctrl Pts',(373.63577420305,-15.0894833990594,-1.59311816853934));
#37421=CARTESIAN_POINT('Ctrl Pts',(373.639769734243,-15.0899880060545,-1.58607153914489));
#37422=CARTESIAN_POINT('Ctrl Pts',(373.647368963763,-15.0909508281979,-1.5725507652667));
#37423=CARTESIAN_POINT('Ctrl Pts',(373.650976949577,-15.0914093290709,-1.56607917979689));
#37424=CARTESIAN_POINT('Ctrl Pts',(373.65956142729,-15.0925036783252,-1.55055570969226));
#37425=CARTESIAN_POINT('Ctrl Pts',(373.664516817666,-15.0931382002379,-1.54149216348104));
#37426=CARTESIAN_POINT('Ctrl Pts',(373.682241520336,-15.0954185894691,-1.50869959115124));
#37427=CARTESIAN_POINT('Ctrl Pts',(373.694757081233,-15.097049334235,-1.48483372825997));
#37428=CARTESIAN_POINT('Ctrl Pts',(373.782882984625,-15.108703943065,-1.31153618912381));
#37429=CARTESIAN_POINT('Ctrl Pts',(373.847052218332,-15.1181416774105,-1.156550391605));
#37430=CARTESIAN_POINT('Ctrl Pts',(373.94723804733,-15.136273113025,-0.848681079501607));
#37431=CARTESIAN_POINT('Ctrl Pts',(373.984718395765,-15.1449528553108,-0.696782618238089));
#37432=CARTESIAN_POINT('Ctrl Pts',(374.031087543922,-15.1606901858902,-0.425394552490045));
#37433=CARTESIAN_POINT('Ctrl Pts',(374.044619760704,-15.167627509278,-0.307008298993963));
#37434=CARTESIAN_POINT('Ctrl Pts',(374.053152217895,-15.1763988089038,-0.161110782556596));
#37435=CARTESIAN_POINT('Ctrl Pts',(374.054392668747,-15.1780347503003,-0.134050236484528));
#37436=CARTESIAN_POINT('Ctrl Pts',(374.055818003606,-15.1806448840402,-0.0911351358949342));
#37437=CARTESIAN_POINT('Ctrl Pts',(374.056227285777,-15.1816120514834,-0.0752889519820703));
#37438=CARTESIAN_POINT('Ctrl Pts',(374.056777643753,-15.1834396202582,-0.0454547290851735));
#37439=CARTESIAN_POINT('Ctrl Pts',(374.056944580141,-15.1842991912654,-0.0314674935290114));
#37440=CARTESIAN_POINT('Ctrl Pts',(374.057115518403,-15.1862423225575,4.79464644808931E-5));
#37441=CARTESIAN_POINT('Ctrl Pts',(374.057067589397,-15.1873274823166,0.0175758795245109));
#37442=CARTESIAN_POINT('Ctrl Pts',(374.056577958902,-15.1901221470586,0.0625263277847719));
#37443=CARTESIAN_POINT('Ctrl Pts',(374.055929189083,-15.1918380525257,0.0899447401956231));
#37444=CARTESIAN_POINT('Ctrl Pts',(374.047285624018,-15.2067842976116,0.327161352660448));
#37445=CARTESIAN_POINT('Ctrl Pts',(374.019158402656,-15.2206551917808,0.535684977525285));
#37446=CARTESIAN_POINT('Ctrl Pts',(373.9206296805,-15.2495867121422,0.95334347585698));
#37447=CARTESIAN_POINT('Ctrl Pts',(373.848645715502,-15.26459357155,1.161043725027));
#37448=CARTESIAN_POINT('Ctrl Pts',(373.742062090989,-15.2809012068014,1.39005471166277));
#37449=CARTESIAN_POINT('Ctrl Pts',(373.727528603959,-15.2830315919661,1.42005648084333));
#37450=CARTESIAN_POINT('Ctrl Pts',(373.707093814898,-15.2858986397865,1.46062381908723));
#37451=CARTESIAN_POINT('Ctrl Pts',(373.701595242644,-15.2866580966725,1.47138847687503));
#37452=CARTESIAN_POINT('Ctrl Pts',(373.692279606572,-15.2879245438182,1.48937533860907));
#37453=CARTESIAN_POINT('Ctrl Pts',(373.688495454932,-15.2884335439982,1.49661434754555));
#37454=CARTESIAN_POINT('Ctrl Pts',(373.68125704012,-15.289396785489,1.51033398812035));
#37455=CARTESIAN_POINT('Ctrl Pts',(373.677808094293,-15.2898513651982,1.51681730641792));
#37456=CARTESIAN_POINT('Ctrl Pts',(373.669575173422,-15.290926288746,1.53216676074724));
#37457=CARTESIAN_POINT('Ctrl Pts',(373.664771693647,-15.2915454121538,1.54102242617792));
#37458=CARTESIAN_POINT('Ctrl Pts',(373.64773680582,-15.2937135463022,1.57207946848017));
#37459=CARTESIAN_POINT('Ctrl Pts',(373.635284720688,-15.2952493084193,1.59415957664774));
#37460=CARTESIAN_POINT('Ctrl Pts',(373.513707501154,-15.3098065356114,1.80391772552069));
#37461=CARTESIAN_POINT('Ctrl Pts',(373.386125988914,-15.3218226087251,1.98029024685482));
#37462=CARTESIAN_POINT('Ctrl Pts',(373.141814194786,-15.342378645182,2.25481247409797));
#37463=CARTESIAN_POINT('Ctrl Pts',(373.034138701614,-15.3508204547322,2.35997931752947));
#37464=CARTESIAN_POINT('Ctrl Pts',(372.877473715543,-15.3627418466324,2.49292461823461));
#37465=CARTESIAN_POINT('Ctrl Pts',(372.834516845515,-15.3659758919759,2.52752102546892));
#37466=CARTESIAN_POINT('Ctrl Pts',(372.758215635121,-15.3716791764802,2.58580846468359));
#37467=CARTESIAN_POINT('Ctrl Pts',(372.725268236795,-15.3741291221087,2.60999894859004));
#37468=CARTESIAN_POINT('Ctrl Pts',(372.676655439127,-15.3777303140805,2.64428751544775));
#37469=CARTESIAN_POINT('Ctrl Pts',(372.661347632427,-15.378862374457,2.65488726844239));
#37470=CARTESIAN_POINT('Ctrl Pts',(372.634271146596,-15.3808618280139,2.67329105811179));
#37471=CARTESIAN_POINT('Ctrl Pts',(372.622541324314,-15.3817270566629,2.68115157108491));
#37472=CARTESIAN_POINT('Ctrl Pts',(372.599580451992,-15.3834190486863,2.69632065294771));
#37473=CARTESIAN_POINT('Ctrl Pts',(372.588354716294,-15.384245505401,2.70363676932782));
#37474=CARTESIAN_POINT('Ctrl Pts',(372.558023627186,-15.3864766491972,2.72313595018312));
#37475=CARTESIAN_POINT('Ctrl Pts',(372.538835142652,-15.3878861620485,2.73518770220726));
#37476=CARTESIAN_POINT('Ctrl Pts',(372.466205231059,-15.3932148616151,2.77974343487143));
#37477=CARTESIAN_POINT('Ctrl Pts',(372.411951233608,-15.3971827967621,2.81088989862553));
#37478=CARTESIAN_POINT('Ctrl Pts',(372.341222145031,-15.4023427007326,2.84880159784428));
#37479=CARTESIAN_POINT('Ctrl Pts',(372.325552341488,-15.4034850341071,2.85703524452286));
#37480=CARTESIAN_POINT('Ctrl Pts',(372.309820571668,-15.4046310424783,2.8651368711395));
#37481=CARTESIAN_POINT('Origin',(370.834317853224,2.31077344927308,0.));
#37482=CARTESIAN_POINT('',(372.309820641399,-16.9034565314269,2.86513683522929));
#37483=CARTESIAN_POINT('',(372.309820496378,-16.659489044147,2.86513690991276));
#37484=CARTESIAN_POINT('',(372.309820613641,2.31077344927308,2.86513684952399));
#37485=CARTESIAN_POINT('',(367.611567947997,-16.0577322247446,-0.00078157510278719));
#37486=CARTESIAN_POINT('Ctrl Pts',(372.309820641399,-16.9034565314269,2.86513683522934));
#37487=CARTESIAN_POINT('Ctrl Pts',(372.325909722202,-16.9022323513834,2.85685119829489));
#37488=CARTESIAN_POINT('Ctrl Pts',(372.341930769895,-16.9010077354113,2.84842913430061));
#37489=CARTESIAN_POINT('Ctrl Pts',(372.505759160986,-16.8884311056161,2.76053675089465));
#37490=CARTESIAN_POINT('Ctrl Pts',(372.647228207769,-16.8771027798122,2.66976513787703));
#37491=CARTESIAN_POINT('Ctrl Pts',(372.80246186057,-16.8645883578776,2.55210744017415));
#37492=CARTESIAN_POINT('Ctrl Pts',(372.823726159882,-16.8628724789041,2.53556658744123));
#37493=CARTESIAN_POINT('Ctrl Pts',(372.85284972562,-16.8605230212038,2.51232028550546));
#37494=CARTESIAN_POINT('Ctrl Pts',(372.860887248126,-16.859874683756,2.50584130209764));
#37495=CARTESIAN_POINT('Ctrl Pts',(372.874635760793,-16.8587659944343,2.49464931815305));
#37496=CARTESIAN_POINT('Ctrl Pts',(372.880361838071,-16.8583043355179,2.48995509983542));
#37497=CARTESIAN_POINT('Ctrl Pts',(372.892313323745,-16.8573410536013,2.4800882474694));
#37498=CARTESIAN_POINT('Ctrl Pts',(372.898535493,-16.8568397291628,2.47491183869975));
#37499=CARTESIAN_POINT('Ctrl Pts',(372.913733967472,-16.8556154366311,2.4621705838769));
#37500=CARTESIAN_POINT('Ctrl Pts',(372.922688679771,-16.8548943228249,2.45457993575919));
#37501=CARTESIAN_POINT('Ctrl Pts',(372.955098319559,-16.8522843683828,2.42680148232818));
#37502=CARTESIAN_POINT('Ctrl Pts',(372.978304460663,-16.8504154960276,2.4063243357264));
#37503=CARTESIAN_POINT('Ctrl Pts',(373.035868637231,-16.8457687630433,2.35403561752845));
#37504=CARTESIAN_POINT('Ctrl Pts',(373.069835922902,-16.8430167664751,2.32180294956494));
#37505=CARTESIAN_POINT('Ctrl Pts',(373.341360001274,-16.8208157859511,2.05265946845745));
#37506=CARTESIAN_POINT('Ctrl Pts',(373.541299064155,-16.8029432288099,1.78071996647468));
#37507=CARTESIAN_POINT('Ctrl Pts',(373.725373100968,-16.7795282714451,1.42551050641333));
#37508=CARTESIAN_POINT('Ctrl Pts',(373.75333113971,-16.7757013781764,1.36734825183877));
#37509=CARTESIAN_POINT('Ctrl Pts',(373.788830260338,-16.7704333959477,1.28743912752393));
#37510=CARTESIAN_POINT('Ctrl Pts',(373.797913069125,-16.7690449222066,1.26639110291828));
#37511=CARTESIAN_POINT('Ctrl Pts',(373.812541765713,-16.7667391386269,1.23147187965546));
#37512=CARTESIAN_POINT('Ctrl Pts',(373.818217226164,-16.765826244692,1.21765560963807));
#37513=CARTESIAN_POINT('Ctrl Pts',(373.829117726463,-16.7640362766019,1.19058566772046));
#37514=CARTESIAN_POINT('Ctrl Pts',(373.83435133797,-16.7631595166423,1.17733580297789));
#37515=CARTESIAN_POINT('Ctrl Pts',(373.846524403341,-16.7610782894638,1.1459091609273));
#37516=CARTESIAN_POINT('Ctrl Pts',(373.853387378807,-16.759871294863,1.12770354204574));
#37517=CARTESIAN_POINT('Ctrl Pts',(373.875825271191,-16.755809160591,1.06650869819381));
#37518=CARTESIAN_POINT('Ctrl Pts',(373.890649521697,-16.7529293804579,1.02325195564793));
#37519=CARTESIAN_POINT('Ctrl Pts',(373.923962025596,-16.7459560656058,0.918855254082635));
#37520=CARTESIAN_POINT('Ctrl Pts',(373.941562200785,-16.7418357351535,0.857454239297127));
#37521=CARTESIAN_POINT('Ctrl Pts',(374.003524581494,-16.7254431429028,0.614222323204082));
#37522=CARTESIAN_POINT('Ctrl Pts',(374.03383462416,-16.7127939529725,0.4292076850403));
#37523=CARTESIAN_POINT('Ctrl Pts',(374.052274408795,-16.6962283953781,0.184976232893961));
#37524=CARTESIAN_POINT('Ctrl Pts',(374.055075140046,-16.6923227461787,0.127213662083228));
#37525=CARTESIAN_POINT('Ctrl Pts',(374.057610445119,-16.6844200056457,0.00951870105741554));
#37526=CARTESIAN_POINT('Ctrl Pts',(374.05723060713,-16.6804261206773,-0.0503957971463344));
#37527=CARTESIAN_POINT('Ctrl Pts',(374.053034137692,-16.6723548701964,-0.172973011430824));
#37528=CARTESIAN_POINT('Ctrl Pts',(374.049056479242,-16.6682841191934,-0.235607576669509));
#37529=CARTESIAN_POINT('Ctrl Pts',(374.041813555831,-16.6633151407042,-0.31357741551113));
#37530=CARTESIAN_POINT('Ctrl Pts',(374.040262782967,-16.6623336884095,-0.329054110797701));
#37531=CARTESIAN_POINT('Ctrl Pts',(374.037636352438,-16.6607929462501,-0.353481838647011));
#37532=CARTESIAN_POINT('Ctrl Pts',(374.036635105261,-16.6602296732624,-0.362440394593988));
#37533=CARTESIAN_POINT('Ctrl Pts',(374.034780488765,-16.6592278542868,-0.378426467662355));
#37534=CARTESIAN_POINT('Ctrl Pts',(374.033941557743,-16.6587885247435,-0.385455345868134));
#37535=CARTESIAN_POINT('Ctrl Pts',(374.031872864361,-16.6577374339569,-0.402315388999192));
#37536=CARTESIAN_POINT('Ctrl Pts',(374.03062092058,-16.6571269237507,-0.412143699649872));
#37537=CARTESIAN_POINT('Ctrl Pts',(374.026671092672,-16.6552754778802,-0.442050649803302));
#37538=CARTESIAN_POINT('Ctrl Pts',(374.023829132134,-16.6540423092407,-0.462110194509896));
#37539=CARTESIAN_POINT('Ctrl Pts',(373.996214745117,-16.6428908964535,-0.644613825384406));
#37540=CARTESIAN_POINT('Ctrl Pts',(373.959237736352,-16.6335771954796,-0.804989980482481));
#37541=CARTESIAN_POINT('Ctrl Pts',(373.829315695519,-16.6091555115711,-1.2204572388388));
#37542=CARTESIAN_POINT('Ctrl Pts',(373.716174339148,-16.594215009074,-1.46779347140523));
#37543=CARTESIAN_POINT('Ctrl Pts',(373.555299592743,-16.5760459106668,-1.72729839558306));
#37544=CARTESIAN_POINT('Ctrl Pts',(373.536704302207,-16.5739825942352,-1.75624847873965));
#37545=CARTESIAN_POINT('Ctrl Pts',(373.507903350223,-16.5708382231381,-1.79954656094379));
#37546=CARTESIAN_POINT('Ctrl Pts',(373.498037417929,-16.5697697824507,-1.81411832481062));
#37547=CARTESIAN_POINT('Ctrl Pts',(373.480635499177,-16.5678998009398,-1.83937254616221));
#37548=CARTESIAN_POINT('Ctrl Pts',(373.473152872376,-16.5671002912839,-1.85009139791578));
#37549=CARTESIAN_POINT('Ctrl Pts',(373.457339398711,-16.5654199530555,-1.87245306672002));
#37550=CARTESIAN_POINT('Ctrl Pts',(373.448995786434,-16.5645386465747,-1.88408646569699));
#37551=CARTESIAN_POINT('Ctrl Pts',(373.428898112143,-16.5624280861523,-1.91171779454894));
#37552=CARTESIAN_POINT('Ctrl Pts',(373.417073309084,-16.5611961088051,-1.92766331938697));
#37553=CARTESIAN_POINT('Ctrl Pts',(373.376078744505,-16.5569575585351,-1.98188934212332));
#37554=CARTESIAN_POINT('Ctrl Pts',(373.346200349984,-16.5539233328718,-2.0196236565588));
#37555=CARTESIAN_POINT('Ctrl Pts',(373.22974159564,-16.542293448099,-2.16011955613223));
#37556=CARTESIAN_POINT('Ctrl Pts',(373.137618444344,-16.5334798573043,-2.25808995462906));
#37557=CARTESIAN_POINT('Ctrl Pts',(372.896009439958,-16.5113436817431,-2.48482478203979));
#37558=CARTESIAN_POINT('Ctrl Pts',(372.740306805638,-16.4978641595868,-2.60617130714752));
#37559=CARTESIAN_POINT('Ctrl Pts',(372.495855143005,-16.4785027089262,-2.76299522431061));
#37560=CARTESIAN_POINT('Ctrl Pts',(372.415042136443,-16.4723665423346,-2.81001119069164));
#37561=CARTESIAN_POINT('Ctrl Pts',(372.318203714575,-16.4654097092436,-2.86084839102259));
#37562=CARTESIAN_POINT('Ctrl Pts',(372.304059840075,-16.4644032324974,-2.86814038740558));
#37563=CARTESIAN_POINT('Ctrl Pts',(372.280988626841,-16.4627777540035,-2.87981946543494));
#37564=CARTESIAN_POINT('Ctrl Pts',(372.272094160435,-16.4621549915347,-2.88427040642093));
#37565=CARTESIAN_POINT('Ctrl Pts',(372.256158973332,-16.4610463989456,-2.8921526120886));
#37566=CARTESIAN_POINT('Ctrl Pts',(372.249126226424,-16.4605596217961,-2.89559944979315));
#37567=CARTESIAN_POINT('Ctrl Pts',(372.233723147319,-16.4594989209627,-2.90307917661999));
#37568=CARTESIAN_POINT('Ctrl Pts',(372.225347918544,-16.458925646247,-2.90710151960614));
#37569=CARTESIAN_POINT('Ctrl Pts',(372.201371805636,-16.4572940665186,-2.91848910916759));
#37570=CARTESIAN_POINT('Ctrl Pts',(372.185728747011,-16.4562410633533,-2.92576550929154));
#37571=CARTESIAN_POINT('Ctrl Pts',(372.075285116867,-16.4488820900499,-2.97606378893287));
#37572=CARTESIAN_POINT('Ctrl Pts',(371.978497226611,-16.4428215134212,-3.01460006081601));
#37573=CARTESIAN_POINT('Ctrl Pts',(371.675401585834,-16.4245262844205,-3.11857079053734));
#37574=CARTESIAN_POINT('Ctrl Pts',(371.464249767503,-16.4126886525198,-3.16798013063101));
#37575=CARTESIAN_POINT('Ctrl Pts',(371.116237981162,-16.3927453744618,-3.21321657456114));
#37576=CARTESIAN_POINT('Ctrl Pts',(370.981800657999,-16.3849477960543,-3.22218596219761));
#37577=CARTESIAN_POINT('Ctrl Pts',(370.818545452719,-16.3751654088909,-3.22283884775045));
#37578=CARTESIAN_POINT('Ctrl Pts',(370.789885301376,-16.3734367211124,-3.22257112805646));
#37579=CARTESIAN_POINT('Ctrl Pts',(370.744881476628,-16.370702813201,-3.2215502811411));
#37580=CARTESIAN_POINT('Ctrl Pts',(370.72853304133,-16.3697056480773,-3.22105489514798));
#37581=CARTESIAN_POINT('Ctrl Pts',(370.698396849238,-16.3678597907341,-3.21991204055672));
#37582=CARTESIAN_POINT('Ctrl Pts',(370.684608057561,-16.3670122400859,-3.219300395418));
#37583=CARTESIAN_POINT('Ctrl Pts',(370.654065400149,-16.3651280978956,-3.21774893114551));
#37584=CARTESIAN_POINT('Ctrl Pts',(370.637314176059,-16.3640902036087,-3.21676680299875));
#37585=CARTESIAN_POINT('Ctrl Pts',(370.589171527548,-16.3610939258599,-3.2135667356678));
#37586=CARTESIAN_POINT('Ctrl Pts',(370.557804610997,-16.3591253182421,-3.21101980679819));
#37587=CARTESIAN_POINT('Ctrl Pts',(370.487169381023,-16.3546538388649,-3.20424173956248));
#37588=CARTESIAN_POINT('Ctrl Pts',(370.447931989098,-16.3521431032443,-3.19974732322143));
#37589=CARTESIAN_POINT('Ctrl Pts',(370.320135022441,-16.3438762244035,-3.18272406280029));
#37590=CARTESIAN_POINT('Ctrl Pts',(370.23201853106,-16.3380340783113,-3.16723060599847));
#37591=CARTESIAN_POINT('Ctrl Pts',(370.006507465763,-16.3227377422392,-3.11782799692219));
#37592=CARTESIAN_POINT('Ctrl Pts',(369.870498325785,-16.3131693936757,-3.07850108825781));
#37593=CARTESIAN_POINT('Ctrl Pts',(369.582656729771,-16.2924635401514,-2.974321187145));
#37594=CARTESIAN_POINT('Ctrl Pts',(369.432301889864,-16.2813548480603,-2.90647616002652));
#37595=CARTESIAN_POINT('Ctrl Pts',(369.264158619013,-16.2690415811167,-2.81450573788576));
#37596=CARTESIAN_POINT('Ctrl Pts',(369.240697529743,-16.2673264597083,-2.80128844353948));
#37597=CARTESIAN_POINT('Ctrl Pts',(369.208468468072,-16.2649773420076,-2.78259555850076));
#37598=CARTESIAN_POINT('Ctrl Pts',(369.19955777666,-16.2643286069238,-2.77736993651894));
#37599=CARTESIAN_POINT('Ctrl Pts',(369.184301980301,-16.263219416897,-2.76832440798745));
#37600=CARTESIAN_POINT('Ctrl Pts',(369.177944699307,-16.2627576523458,-2.76452534558062));
#37601=CARTESIAN_POINT('Ctrl Pts',(369.164807622842,-16.2618044568689,-2.75661314556102));
#37602=CARTESIAN_POINT('Ctrl Pts',(369.158029838833,-16.2613132540862,-2.75249685523508));
#37603=CARTESIAN_POINT('Ctrl Pts',(369.141582255117,-16.260122497351,-2.74242460843516));
#37604=CARTESIAN_POINT('Ctrl Pts',(369.131928496297,-16.2594246399089,-2.73644240291207));
#37605=CARTESIAN_POINT('Ctrl Pts',(369.111212317908,-16.2579289012428,-2.72345301840999));
#37606=CARTESIAN_POINT('Ctrl Pts',(369.100160531888,-16.2571320649984,-2.71642916841906));
#37607=CARTESIAN_POINT('Ctrl Pts',(369.069251640905,-16.2549057747582,-2.69651982109413));
#37608=CARTESIAN_POINT('Ctrl Pts',(369.049492844587,-16.2534852232699,-2.68348237110937));
#37609=CARTESIAN_POINT('Ctrl Pts',(368.983985918588,-16.2487781135972,-2.63921527155641));
#37610=CARTESIAN_POINT('Ctrl Pts',(368.93889752219,-16.2455422602912,-2.60702281492231));
#37611=CARTESIAN_POINT('Ctrl Pts',(368.799243045708,-16.2354573079859,-2.50177205215575));
#37612=CARTESIAN_POINT('Ctrl Pts',(368.707894629632,-16.2287645624368,-2.42460722287221));
#37613=CARTESIAN_POINT('Ctrl Pts',(368.450036902546,-16.2089234129788,-2.18097843011303));
#37614=CARTESIAN_POINT('Ctrl Pts',(368.297259405153,-16.1958088288278,-2.00119524996881));
#37615=CARTESIAN_POINT('Ctrl Pts',(368.142377486986,-16.1793981642233,-1.77236102539354));
#37616=CARTESIAN_POINT('Ctrl Pts',(368.119995923379,-16.1769349825886,-1.73789032184905));
#37617=CARTESIAN_POINT('Ctrl Pts',(368.088530507135,-16.1733305634356,-1.68733809187866));
#37618=CARTESIAN_POINT('Ctrl Pts',(368.078915503128,-16.1722088668653,-1.67159081517988));
#37619=CARTESIAN_POINT('Ctrl Pts',(368.062174494859,-16.1702191035882,-1.64363577052792));
#37620=CARTESIAN_POINT('Ctrl Pts',(368.054992537633,-16.1693531039936,-1.6314619595809));
#37621=CARTESIAN_POINT('Ctrl Pts',(368.040260998156,-16.167550611066,-1.60611159725536));
#37622=CARTESIAN_POINT('Ctrl Pts',(368.032724016678,-16.1666136902732,-1.59292816367406));
#37623=CARTESIAN_POINT('Ctrl Pts',(368.013478835883,-16.164182528865,-1.55870603339544));
#37624=CARTESIAN_POINT('Ctrl Pts',(368.001912893915,-16.1626832516834,-1.53758881247696));
#37625=CARTESIAN_POINT('Ctrl Pts',(367.952346208536,-16.1560861030596,-1.44463208451442));
#37626=CARTESIAN_POINT('Ctrl Pts',(367.91683684042,-16.1509018547886,-1.37150467360372));
#37627=CARTESIAN_POINT('Ctrl Pts',(367.825785047635,-16.1362280826729,-1.16441504258489));
#37628=CARTESIAN_POINT('Ctrl Pts',(367.776464921742,-16.1265584651244,-1.02793951760935));
#37629=CARTESIAN_POINT('Ctrl Pts',(367.680143790595,-16.1029930879962,-0.692155113000229));
#37630=CARTESIAN_POINT('Ctrl Pts',(367.64260182306,-16.0890276708331,-0.490764710893553));
#37631=CARTESIAN_POINT('Ctrl Pts',(367.620767434018,-16.0731142928088,-0.246701889451502));
#37632=CARTESIAN_POINT('Ctrl Pts',(367.61791261563,-16.0705057516962,-0.206169398443341));
#37633=CARTESIAN_POINT('Ctrl Pts',(367.61513268978,-16.0670833664798,-0.152137864877246));
#37634=CARTESIAN_POINT('Ctrl Pts',(367.614524841718,-16.0662354427632,-0.138679574765838));
#37635=CARTESIAN_POINT('Ctrl Pts',(367.613672552055,-16.0648622698571,-0.116760590996401));
#37636=CARTESIAN_POINT('Ctrl Pts',(367.613377023756,-16.0643342638905,-0.108302209163852));
#37637=CARTESIAN_POINT('Ctrl Pts',(367.612884972192,-16.0633469595842,-0.0924272495048247));
#37638=CARTESIAN_POINT('Ctrl Pts',(367.61268073451,-16.0628872413884,-0.085011057575803));
#37639=CARTESIAN_POINT('Ctrl Pts',(367.612310034364,-16.0619361444319,-0.0696190826078667));
#37640=CARTESIAN_POINT('Ctrl Pts',(367.612147572256,-16.0614449863556,-0.0616432077410594));
#37641=CARTESIAN_POINT('Ctrl Pts',(367.611861842461,-16.0603919769561,-0.0444871727029009));
#37642=CARTESIAN_POINT('Ctrl Pts',(367.611748183298,-16.0598306413629,-0.0353068958615575));
#37643=CARTESIAN_POINT('Ctrl Pts',(367.611605266647,-16.0587566060512,-0.0176782066592246));
#37644=CARTESIAN_POINT('Ctrl Pts',(367.611569996882,-16.0582436059849,-0.00922995489554233));
#37645=CARTESIAN_POINT('Ctrl Pts',(367.611567947997,-16.0577322247446,-0.00078157510278719));
#37646=CARTESIAN_POINT('Ctrl Pts',(367.611567948554,-16.0577323635611,-0.000783868448169546));
#37647=CARTESIAN_POINT('Ctrl Pts',(367.611558543255,-16.0553917611876,0.0378845160265506));
#37648=CARTESIAN_POINT('Ctrl Pts',(367.612245086453,-16.0530852721127,0.076552140657268));
#37649=CARTESIAN_POINT('Ctrl Pts',(367.61924901596,-16.041536127642,0.272363362098293));
#37650=CARTESIAN_POINT('Ctrl Pts',(367.636367475431,-16.032722440087,0.428919686002358));
#37651=CARTESIAN_POINT('Ctrl Pts',(367.696311832866,-16.0142065883644,0.754463912204947));
#37652=CARTESIAN_POINT('Ctrl Pts',(367.741534008391,-16.0045302483034,0.922486301583004));
#37653=CARTESIAN_POINT('Ctrl Pts',(367.820264686816,-15.991020743859,1.14244968281997));
#37654=CARTESIAN_POINT('Ctrl Pts',(367.842025001008,-15.987516969942,1.19828654531898));
#37655=CARTESIAN_POINT('Ctrl Pts',(367.882268797683,-15.9813819831846,1.29360773869993));
#37656=CARTESIAN_POINT('Ctrl Pts',(367.900020506377,-15.9787744610406,1.33338419662031));
#37657=CARTESIAN_POINT('Ctrl Pts',(367.926702488772,-15.9749848335776,1.39005566491259));
#37658=CARTESIAN_POINT('Ctrl Pts',(367.934985851469,-15.9738249330681,1.40725114265235));
#37659=CARTESIAN_POINT('Ctrl Pts',(367.949690306032,-15.971793802957,1.43709521717563));
#37660=CARTESIAN_POINT('Ctrl Pts',(367.956043128462,-15.9709249675335,1.44977699936811));
#37661=CARTESIAN_POINT('Ctrl Pts',(367.968491948276,-15.9692388069575,1.47422352688446));
#37662=CARTESIAN_POINT('Ctrl Pts',(367.97457720096,-15.9684218725892,1.48599344484594));
#37663=CARTESIAN_POINT('Ctrl Pts',(367.990916067982,-15.9662473617425,1.51712352738365));
#37664=CARTESIAN_POINT('Ctrl Pts',(368.001294670479,-15.9648853863186,1.53641697388562));
#37665=CARTESIAN_POINT('Ctrl Pts',(368.039587657036,-15.9599278808336,1.6058948649576));
#37666=CARTESIAN_POINT('Ctrl Pts',(368.068644050648,-15.9562919096499,1.65543436205101));
#37667=CARTESIAN_POINT('Ctrl Pts',(368.234340344584,-15.9362010568114,1.92138858625597));
#37668=CARTESIAN_POINT('Ctrl Pts',(368.395049497262,-15.9188529075266,2.12168455659783));
#37669=CARTESIAN_POINT('Ctrl Pts',(368.687444003093,-15.8911977730566,2.40845922980061));
#37670=CARTESIAN_POINT('Ctrl Pts',(368.804752641828,-15.8809063011847,2.50811063957212));
#37671=CARTESIAN_POINT('Ctrl Pts',(368.939328040708,-15.8702824408994,2.60678031072377));
#37672=CARTESIAN_POINT('Ctrl Pts',(368.949964974113,-15.8694503064739,2.61447972226268));
#37673=CARTESIAN_POINT('Ctrl Pts',(368.96991709048,-15.8679039912597,2.62873679149439));
#37674=CARTESIAN_POINT('Ctrl Pts',(368.979220523612,-15.867188801396,2.635310461769));
#37675=CARTESIAN_POINT('Ctrl Pts',(368.995043066117,-15.8659825908233,2.64636512787702));
#37676=CARTESIAN_POINT('Ctrl Pts',(369.001544124791,-15.8654898633921,2.65087166751089));
#37677=CARTESIAN_POINT('Ctrl Pts',(369.014156817787,-15.864539567564,2.65954621850779));
#37678=CARTESIAN_POINT('Ctrl Pts',(369.020266282239,-15.8640817895662,2.6637171741215));
#37679=CARTESIAN_POINT('Ctrl Pts',(369.034914581061,-15.8629901153259,2.6736438550759));
#37680=CARTESIAN_POINT('Ctrl Pts',(369.043466808301,-15.8623575333972,2.6793798053355));
#37681=CARTESIAN_POINT('Ctrl Pts',(369.074313013917,-15.860092495342,2.69985458281451));
#37682=CARTESIAN_POINT('Ctrl Pts',(369.09676331998,-15.8584748932765,2.71435741049251));
#37683=CARTESIAN_POINT('Ctrl Pts',(369.275571127005,-15.8458120799247,2.82673898134911));
#37684=CARTESIAN_POINT('Ctrl Pts',(369.439910331565,-15.8354819853616,2.911320943536));
#37685=CARTESIAN_POINT('Ctrl Pts',(369.770306512907,-15.8155061306556,3.0469328305337));
#37686=CARTESIAN_POINT('Ctrl Pts',(369.935013743376,-15.8058870282335,3.09954306551405));
#37687=CARTESIAN_POINT('Ctrl Pts',(370.161284180084,-15.7924507460144,3.15225450396176));
#37688=CARTESIAN_POINT('Ctrl Pts',(370.219799101908,-15.7889587599341,3.16418218238292));
#37689=CARTESIAN_POINT('Ctrl Pts',(370.321397456469,-15.7828425807606,3.18196749943756));
#37690=CARTESIAN_POINT('Ctrl Pts',(370.364331130253,-15.7802418760712,3.18859165005315));
#37691=CARTESIAN_POINT('Ctrl Pts',(370.426282439285,-15.7764604032467,3.19687162561534));
#37692=CARTESIAN_POINT('Ctrl Pts',(370.445202503272,-15.7753017049714,3.19922964320208));
#37693=CARTESIAN_POINT('Ctrl Pts',(370.478228966909,-15.7732719748428,3.20304844818476));
#37694=CARTESIAN_POINT('Ctrl Pts',(370.492326282178,-15.7724033273363,3.20458428061597));
#37695=CARTESIAN_POINT('Ctrl Pts',(370.521426418436,-15.7706053857465,3.20756039123727));
#37696=CARTESIAN_POINT('Ctrl Pts',(370.536430102122,-15.7696757335476,3.2089885616552));
#37697=CARTESIAN_POINT('Ctrl Pts',(370.5749026246,-15.7672848663603,3.21237854653832));
#37698=CARTESIAN_POINT('Ctrl Pts',(370.598383634439,-15.765818927103,3.21418841766123));
#37699=CARTESIAN_POINT('Ctrl Pts',(370.69098732607,-15.7600100085974,3.22030593670393));
#37700=CARTESIAN_POINT('Ctrl Pts',(370.760217317485,-15.7556062413676,3.22264206790362));
#37701=CARTESIAN_POINT('Ctrl Pts',(371.159343406374,-15.7298520816828,3.22324310190208));
#37702=CARTESIAN_POINT('Ctrl Pts',(371.487257202047,-15.7069787162743,3.17309562573088));
#37703=CARTESIAN_POINT('Ctrl Pts',(371.846259928825,-15.6821398371778,3.06010812443847));
#37704=CARTESIAN_POINT('Ctrl Pts',(371.890397785148,-15.6790950398932,3.04515748598768));
#37705=CARTESIAN_POINT('Ctrl Pts',(371.963182546608,-15.6741060238483,3.01873034918337));
#37706=CARTESIAN_POINT('Ctrl Pts',(371.992015796015,-15.6721381590867,3.00779056004922));
#37707=CARTESIAN_POINT('Ctrl Pts',(372.031587989533,-15.6694534521488,2.99212285804948));
#37708=CARTESIAN_POINT('Ctrl Pts',(372.042463770167,-15.668717298722,2.9877480533522));
#37709=CARTESIAN_POINT('Ctrl Pts',(372.060805027621,-15.6674789931086,2.98025371896806));
#37710=CARTESIAN_POINT('Ctrl Pts',(372.068283007404,-15.6669750145239,2.97716526611397));
#37711=CARTESIAN_POINT('Ctrl Pts',(372.082585473385,-15.6660129224498,2.97119511054539));
#37712=CARTESIAN_POINT('Ctrl Pts',(372.089411736594,-15.6655545267642,2.96831800570742));
#37713=CARTESIAN_POINT('Ctrl Pts',(372.105739531959,-15.6644598424752,2.96136983962954));
#37714=CARTESIAN_POINT('Ctrl Pts',(372.115231586048,-15.6638248846716,2.95727652207977));
#37715=CARTESIAN_POINT('Ctrl Pts',(372.149479209147,-15.6615385423578,2.94231187670626));
#37716=CARTESIAN_POINT('Ctrl Pts',(372.174118198749,-15.6599023946376,2.93117445996874));
#37717=CARTESIAN_POINT('Ctrl Pts',(372.236039048279,-15.6558055709026,2.90224079126109));
#37718=CARTESIAN_POINT('Ctrl Pts',(372.273114281798,-15.6533665221963,2.88404006384538));
#37719=CARTESIAN_POINT('Ctrl Pts',(372.309820655984,-15.6509557951682,2.86513682771809));
#37720=CARTESIAN_POINT('Ctrl Pts',(372.309820571668,-15.4046310424783,2.86513687113946));
#37721=CARTESIAN_POINT('Ctrl Pts',(372.025277739051,-15.4253590643006,3.01167218233879));
#37722=CARTESIAN_POINT('Ctrl Pts',(371.720480749908,-15.4475437349958,3.11501642052086));
#37723=CARTESIAN_POINT('Ctrl Pts',(371.359227982871,-15.471774267914,3.18006098518721));
#37724=CARTESIAN_POINT('Ctrl Pts',(371.31287769668,-15.4748406834038,3.1873655951699));
#37725=CARTESIAN_POINT('Ctrl Pts',(371.235664752265,-15.4798614659379,3.19781160499005));
#37726=CARTESIAN_POINT('Ctrl Pts',(371.204887598201,-15.4818398289967,3.20152410950472));
#37727=CARTESIAN_POINT('Ctrl Pts',(371.162374312456,-15.4845366789787,3.20603097630842));
#37728=CARTESIAN_POINT('Ctrl Pts',(371.150681339494,-15.485274690602,3.20720592043849));
#37729=CARTESIAN_POINT('Ctrl Pts',(371.130917739862,-15.4865154784946,3.20908268642529));
#37730=CARTESIAN_POINT('Ctrl Pts',(371.122850484533,-15.4870200941273,3.20981808002048));
#37731=CARTESIAN_POINT('Ctrl Pts',(371.107399355604,-15.4879829161681,3.21116784842592));
#37732=CARTESIAN_POINT('Ctrl Pts',(371.100016046143,-15.4884414084109,3.21178718638036));
#37733=CARTESIAN_POINT('Ctrl Pts',(371.082334832843,-15.4895357156332,3.21320896116639));
#37734=CARTESIAN_POINT('Ctrl Pts',(371.072035003531,-15.4901702043731,3.21398736984018));
#37735=CARTESIAN_POINT('Ctrl Pts',(371.03485625716,-15.4924503160593,3.2166174471686));
#37736=CARTESIAN_POINT('Ctrl Pts',(371.007957282404,-15.4940808213809,3.2181816153142));
#37737=CARTESIAN_POINT('Ctrl Pts',(370.813110436838,-15.5057733297517,3.2270616685182));
#37738=CARTESIAN_POINT('Ctrl Pts',(370.644816952915,-15.5152446234542,3.22156483063877));
#37739=CARTESIAN_POINT('Ctrl Pts',(370.330957683941,-15.5329290412395,3.18662007183154));
#37740=CARTESIAN_POINT('Ctrl Pts',(370.185509914545,-15.5411350240599,3.16021605524769));
#37741=CARTESIAN_POINT('Ctrl Pts',(369.920003521484,-15.5567519071712,3.09290928588405));
#37742=CARTESIAN_POINT('Ctrl Pts',(369.799558618616,-15.564090614991,3.05472201469633));
#37743=CARTESIAN_POINT('Ctrl Pts',(369.655977875133,-15.573314931458,2.99973157101965));
#37744=CARTESIAN_POINT('Ctrl Pts',(369.630411240774,-15.5749761358368,2.98956240936314));
#37745=CARTESIAN_POINT('Ctrl Pts',(369.590239987775,-15.5776173351037,2.97298537543862));
#37746=CARTESIAN_POINT('Ctrl Pts',(369.575546992478,-15.5785900112208,2.96679417616491));
#37747=CARTESIAN_POINT('Ctrl Pts',(369.548061419041,-15.5804223151932,2.95497162358561));
#37748=CARTESIAN_POINT('Ctrl Pts',(369.535258317569,-15.5812810651284,2.94936556291936));
#37749=CARTESIAN_POINT('Ctrl Pts',(369.506607139596,-15.5832147886038,2.93659739719836));
#37750=CARTESIAN_POINT('Ctrl Pts',(369.490779851015,-15.5842912969811,2.92938997573834));
#37751=CARTESIAN_POINT('Ctrl Pts',(369.450554468205,-15.5870488500567,2.91067759585452));
#37752=CARTESIAN_POINT('Ctrl Pts',(369.426241445198,-15.588736010971,2.89899395149917));
#37753=CARTESIAN_POINT('Ctrl Pts',(369.261210994774,-15.6003309907493,2.81712261552336));
#37754=CARTESIAN_POINT('Ctrl Pts',(369.125667843278,-15.610585849957,2.73703260199142));
#37755=CARTESIAN_POINT('Ctrl Pts',(368.817334177866,-15.6356315725808,2.52298982554617));
#37756=CARTESIAN_POINT('Ctrl Pts',(368.651243842037,-15.6505984631149,2.38073184346979));
#37757=CARTESIAN_POINT('Ctrl Pts',(368.46388180627,-15.6686073600612,2.1840364852025));
#37758=CARTESIAN_POINT('Ctrl Pts',(368.427934161896,-15.6721197930694,2.14436484273628));
#37759=CARTESIAN_POINT('Ctrl Pts',(368.370704461978,-15.6777831504157,2.07795380187474));
#37760=CARTESIAN_POINT('Ctrl Pts',(368.348830592228,-15.6799659748668,2.05173980739089));
#37761=CARTESIAN_POINT('Ctrl Pts',(368.319710796621,-15.6828913834033,2.01569286317304));
#37762=CARTESIAN_POINT('Ctrl Pts',(368.312098982396,-15.6836579437112,2.00616009994196));
#37763=CARTESIAN_POINT('Ctrl Pts',(368.299466566243,-15.6849329290432,1.99015416829915));
#37764=CARTESIAN_POINT('Ctrl Pts',(368.294416248236,-15.6854434210197,1.98370474162987));
#37765=CARTESIAN_POINT('Ctrl Pts',(368.284896912626,-15.6864069898513,1.97145227540206));
#37766=CARTESIAN_POINT('Ctrl Pts',(368.280423007563,-15.6868604217393,1.96565315515727));
#37767=CARTESIAN_POINT('Ctrl Pts',(368.269889284293,-15.687929513276,1.95190256464055));
#37768=CARTESIAN_POINT('Ctrl Pts',(368.263846577545,-15.6885439841889,1.94393799645155));
#37769=CARTESIAN_POINT('Ctrl Pts',(368.242886760738,-15.6906800021544,1.91604336343282));
#37770=CARTESIAN_POINT('Ctrl Pts',(368.228163164279,-15.6921888085721,1.89596811703243));
#37771=CARTESIAN_POINT('Ctrl Pts',(368.083669887638,-15.7071022282203,1.69409107064014));
#37772=CARTESIAN_POINT('Ctrl Pts',(367.972882826127,-15.7194382937699,1.49940874058233));
#37773=CARTESIAN_POINT('Ctrl Pts',(367.797473221262,-15.7438675047481,1.09960503934842));
#37774=CARTESIAN_POINT('Ctrl Pts',(367.731418556255,-15.7558976998376,0.896413326277192));
#37775=CARTESIAN_POINT('Ctrl Pts',(367.678972346146,-15.770573726751,0.656480483783131));
#37776=CARTESIAN_POINT('Ctrl Pts',(367.672518443659,-15.7725284225183,0.624656923953805));
#37777=CARTESIAN_POINT('Ctrl Pts',(367.663420893998,-15.7755294644004,0.576037204796292));
#37778=CARTESIAN_POINT('Ctrl Pts',(367.660427362353,-15.7765646926789,0.559308074378739));
#37779=CARTESIAN_POINT('Ctrl Pts',(367.655217516292,-15.7784574667457,0.528803615118159));
#37780=CARTESIAN_POINT('Ctrl Pts',(367.652958061819,-15.7793136207491,0.515036002221224));
#37781=CARTESIAN_POINT('Ctrl Pts',(367.6482613794,-15.7811728488783,0.485206776664554));
#37782=CARTESIAN_POINT('Ctrl Pts',(367.645856068077,-15.782176908691,0.469140596973328));
#37783=CARTESIAN_POINT('Ctrl Pts',(367.639616551988,-15.7849307424308,0.425197558401056));
#37784=CARTESIAN_POINT('Ctrl Pts',(367.636025893485,-15.7866881317583,0.397288091169767));
#37785=CARTESIAN_POINT('Ctrl Pts',(367.618558134734,-15.7962699865278,0.245872203411862));
#37786=CARTESIAN_POINT('Ctrl Pts',(367.611470409427,-15.8043047509393,0.121702817941861));
#37787=CARTESIAN_POINT('Ctrl Pts',(367.61168598124,-15.8222767577775,-0.150361365533153));
#37788=CARTESIAN_POINT('Ctrl Pts',(367.621971522796,-15.8322681552496,-0.297976929090117));
#37789=CARTESIAN_POINT('Ctrl Pts',(367.665539758003,-15.853643745467,-0.610944278953389));
#37790=CARTESIAN_POINT('Ctrl Pts',(367.701738994466,-15.8649990219507,-0.775479145063843));
#37791=CARTESIAN_POINT('Ctrl Pts',(367.758450440369,-15.8775383431487,-0.96222819727075));
#37792=CARTESIAN_POINT('Ctrl Pts',(367.766602426614,-15.8792544997248,-0.987909720862183));
#37793=CARTESIAN_POINT('Ctrl Pts',(367.778324066333,-15.8816045791753,-1.02329185690301));
#37794=CARTESIAN_POINT('Ctrl Pts',(367.781619477406,-15.8822532628188,-1.03308125673883));
#37795=CARTESIAN_POINT('Ctrl Pts',(367.787359479625,-15.8833626048898,-1.049865290023));
#37796=CARTESIAN_POINT('Ctrl Pts',(367.789781207601,-15.8838245713511,-1.0568675762433));
#37797=CARTESIAN_POINT('Ctrl Pts',(367.794901190632,-15.8847885829895,-1.07150806527044));
#37798=CARTESIAN_POINT('Ctrl Pts',(367.797604125347,-15.885290328627,-1.07914453132832));
#37799=CARTESIAN_POINT('Ctrl Pts',(367.804298694291,-15.8865158264506,-1.09783403049992));
#37800=CARTESIAN_POINT('Ctrl Pts',(367.808322096293,-15.8872377195161,-1.10887571485367));
#37801=CARTESIAN_POINT('Ctrl Pts',(367.823177396167,-15.8898515546441,-1.14896107542089));
#37802=CARTESIAN_POINT('Ctrl Pts',(367.834368153605,-15.8917234602903,-1.17787111605591));
#37803=CARTESIAN_POINT('Ctrl Pts',(367.86353987318,-15.89637876482,-1.25011869018984));
#37804=CARTESIAN_POINT('Ctrl Pts',(367.882053696358,-15.89913618808,-1.2932344450927));
#37805=CARTESIAN_POINT('Ctrl Pts',(368.041566553706,-15.9214797048832,-1.64341800223679));
#37806=CARTESIAN_POINT('Ctrl Pts',(368.229112338637,-15.9394717597361,-1.92697354739763));
#37807=CARTESIAN_POINT('Ctrl Pts',(368.499548716523,-15.9629361954599,-2.22235961619356));
#37808=CARTESIAN_POINT('Ctrl Pts',(368.54311377023,-15.966648523197,-2.26724772926983));
#37809=CARTESIAN_POINT('Ctrl Pts',(368.604201983852,-15.971782663577,-2.32663150691058));
#37810=CARTESIAN_POINT('Ctrl Pts',(368.62061463122,-15.9731553309329,-2.34225296764824));
#37811=CARTESIAN_POINT('Ctrl Pts',(368.646992930526,-15.9753516226572,-2.36683476067277));
#37812=CARTESIAN_POINT('Ctrl Pts',(368.656852295318,-15.976170381231,-2.37590842361511));
#37813=CARTESIAN_POINT('Ctrl Pts',(368.677217144973,-15.9778573464397,-2.39441714750869));
#37814=CARTESIAN_POINT('Ctrl Pts',(368.687728614372,-15.9787258236816,-2.40384516377056));
#37815=CARTESIAN_POINT('Ctrl Pts',(368.712244216327,-15.980746332422,-2.4255448343693));
#37816=CARTESIAN_POINT('Ctrl Pts',(368.726293313437,-15.9819004817632,-2.43776470978677));
#37817=CARTESIAN_POINT('Ctrl Pts',(368.771519544025,-15.9856045333485,-2.47641908096368));
#37818=CARTESIAN_POINT('Ctrl Pts',(368.803093025258,-15.9881735076257,-2.50238162171343));
#37819=CARTESIAN_POINT('Ctrl Pts',(368.878410791953,-15.9942651626766,-2.56194987869804));
#37820=CARTESIAN_POINT('Ctrl Pts',(368.922539942347,-15.9978064962388,-2.59504609852665));
#37821=CARTESIAN_POINT('Ctrl Pts',(369.090063792928,-16.0111488235541,-2.71409381614047));
#37822=CARTESIAN_POINT('Ctrl Pts',(369.218566235213,-16.0211963058601,-2.792501681698));
#37823=CARTESIAN_POINT('Ctrl Pts',(369.544813190576,-16.0460031779589,-2.96148914426724));
#37824=CARTESIAN_POINT('Ctrl Pts',(369.747174718968,-16.0608317272373,-3.04160709039922));
#37825=CARTESIAN_POINT('Ctrl Pts',(369.980455695816,-16.0763865435603,-3.10768073246277));
#37826=CARTESIAN_POINT('Ctrl Pts',(370.004926514732,-16.0779994653569,-3.1143009197698));
#37827=CARTESIAN_POINT('Ctrl Pts',(370.03922905887,-16.0802318665744,-3.12314790999112));
#37828=CARTESIAN_POINT('Ctrl Pts',(370.04899625515,-16.0808642961358,-3.1256181872605));
#37829=CARTESIAN_POINT('Ctrl Pts',(370.065902776158,-16.0819532518912,-3.12980985998363));
#37830=CARTESIAN_POINT('Ctrl Pts',(370.073036630265,-16.0824109820555,-3.13155271270328));
#37831=CARTESIAN_POINT('Ctrl Pts',(370.088117928119,-16.0833748297816,-3.13518260307879));
#37832=CARTESIAN_POINT('Ctrl Pts',(370.096066703054,-16.0838805987039,-3.13706383815625));
#37833=CARTESIAN_POINT('Ctrl Pts',(370.115795270121,-16.0851305452592,-3.14165385704228));
#37834=CARTESIAN_POINT('Ctrl Pts',(370.127583451163,-16.0858726891269,-3.14432666172176));
#37835=CARTESIAN_POINT('Ctrl Pts',(370.171933471353,-16.0886480488088,-3.15412039216201));
#37836=CARTESIAN_POINT('Ctrl Pts',(370.204591337821,-16.0906578463273,-3.16080262460133));
#37837=CARTESIAN_POINT('Ctrl Pts',(370.45274566944,-16.1057138709211,-3.20757926218942));
#37838=CARTESIAN_POINT('Ctrl Pts',(370.671751067082,-16.117802492749,-3.22610578570191));
#37839=CARTESIAN_POINT('Ctrl Pts',(371.1009010831,-16.1418313442101,-3.21856153531412));
#37840=CARTESIAN_POINT('Ctrl Pts',(371.30994669702,-16.1537094556595,-3.19436478554087));
#37841=CARTESIAN_POINT('Ctrl Pts',(371.54194965591,-16.1679154334896,-3.14422121751639));
#37842=CARTESIAN_POINT('Ctrl Pts',(371.568682479037,-16.1695672960928,-3.13808514214414));
#37843=CARTESIAN_POINT('Ctrl Pts',(371.612365966074,-16.1722926536017,-3.12746957572566));
#37844=CARTESIAN_POINT('Ctrl Pts',(371.629364489063,-16.1733596873915,-3.12319157929255));
#37845=CARTESIAN_POINT('Ctrl Pts',(371.659864022225,-16.1752863105638,-3.11525067342172));
#37846=CARTESIAN_POINT('Ctrl Pts',(371.673377770979,-16.17614425493,-3.11163810236189));
#37847=CARTESIAN_POINT('Ctrl Pts',(371.702153805507,-16.1779805186812,-3.10374444500678));
#37848=CARTESIAN_POINT('Ctrl Pts',(371.717408836428,-16.1789596252393,-3.09943851705888));
#37849=CARTESIAN_POINT('Ctrl Pts',(371.758644542212,-16.1816218660906,-3.08747006962052));
#37850=CARTESIAN_POINT('Ctrl Pts',(371.784560932768,-16.1833119620926,-3.07959238805969));
#37851=CARTESIAN_POINT('Ctrl Pts',(371.923834492422,-16.1924881617337,-3.03533265652999));
#37852=CARTESIAN_POINT('Ctrl Pts',(372.035196464518,-16.2001672931004,-2.99302115859517));
#37853=CARTESIAN_POINT('Ctrl Pts',(372.286656963632,-16.2183016927497,-2.88118401238031));
#37854=CARTESIAN_POINT('Ctrl Pts',(372.424548989944,-16.2288576245951,-2.8074309045405));
#37855=CARTESIAN_POINT('Ctrl Pts',(372.698187026081,-16.2507576231464,-2.63442464190561));
#37856=CARTESIAN_POINT('Ctrl Pts',(372.832646419374,-16.2620696723749,-2.53394850991685));
#37857=CARTESIAN_POINT('Ctrl Pts',(372.978952845682,-16.2745698460313,-2.40569831769175));
#37858=CARTESIAN_POINT('Ctrl Pts',(372.998993015467,-16.2762862448348,-2.38768197186743));
#37859=CARTESIAN_POINT('Ctrl Pts',(373.02639998404,-16.2786365946828,-2.36241406028341));
#37860=CARTESIAN_POINT('Ctrl Pts',(373.033960786732,-16.2792853109311,-2.35537581552413));
#37861=CARTESIAN_POINT('Ctrl Pts',(373.046886597713,-16.2803946940512,-2.3432268371922));
#37862=CARTESIAN_POINT('Ctrl Pts',(373.052268005961,-16.2808566691676,-2.33813378193352));
#37863=CARTESIAN_POINT('Ctrl Pts',(373.063496010433,-16.281820682033,-2.32743376365624));
#37864=CARTESIAN_POINT('Ctrl Pts',(373.069339096466,-16.2823224203379,-2.32182325443305));
#37865=CARTESIAN_POINT('Ctrl Pts',(373.083606420539,-16.2835478725564,-2.30802005801452));
#37866=CARTESIAN_POINT('Ctrl Pts',(373.092007227394,-16.2842697276756,-2.29980311047356));
#37867=CARTESIAN_POINT('Ctrl Pts',(373.122400814623,-16.2868832678142,-2.26974767398716));
#37868=CARTESIAN_POINT('Ctrl Pts',(373.14412399018,-16.2887549223363,-2.24763740686851));
#37869=CARTESIAN_POINT('Ctrl Pts',(373.19791291814,-16.2934094718393,-2.19128640286177));
#37870=CARTESIAN_POINT('Ctrl Pts',(373.229557139794,-16.2961664019762,-2.15665178592457));
#37871=CARTESIAN_POINT('Ctrl Pts',(373.482690714373,-16.3184961462378,-1.86714954484856));
#37872=CARTESIAN_POINT('Ctrl Pts',(373.663628178267,-16.3364766525888,-1.57961056321843));
#37873=CARTESIAN_POINT('Ctrl Pts',(373.821331351251,-16.3599361288771,-1.21152925151641));
#37874=CARTESIAN_POINT('Ctrl Pts',(373.844346112093,-16.3636593570963,-1.15316168393667));
#37875=CARTESIAN_POINT('Ctrl Pts',(373.873343715202,-16.3688062916375,-1.07282522608097));
#37876=CARTESIAN_POINT('Ctrl Pts',(373.880819767758,-16.3701805283311,-1.0514077229525));
#37877=CARTESIAN_POINT('Ctrl Pts',(373.892352637534,-16.372378703109,-1.01721211911853));
#37878=CARTESIAN_POINT('Ctrl Pts',(373.896556988662,-16.3731977600452,-1.00448429863444));
#37879=CARTESIAN_POINT('Ctrl Pts',(373.905026222533,-16.3748848723642,-0.978298005006675));
#37880=CARTESIAN_POINT('Ctrl Pts',(373.909282309256,-16.375753195416,-0.964837012145004));
#37881=CARTESIAN_POINT('Ctrl Pts',(373.918941605234,-16.3777725488329,-0.933573766835426));
#37882=CARTESIAN_POINT('Ctrl Pts',(373.92427933988,-16.378925689385,-0.915751962765309));
#37883=CARTESIAN_POINT('Ctrl Pts',(373.940825948793,-16.3826231847994,-0.858713330257394));
#37884=CARTESIAN_POINT('Ctrl Pts',(373.951444414233,-16.3851865168706,-0.819330756820049));
#37885=CARTESIAN_POINT('Ctrl Pts',(373.974619922245,-16.3912624529728,-0.726392151438716));
#37886=CARTESIAN_POINT('Ctrl Pts',(373.986558577369,-16.3947935798126,-0.672696428392339));
#37887=CARTESIAN_POINT('Ctrl Pts',(374.025849689343,-16.4080786223829,-0.471847747902337));
#37888=CARTESIAN_POINT('Ctrl Pts',(374.04431361308,-16.418076710204,-0.323163328932099));
#37889=CARTESIAN_POINT('Ctrl Pts',(374.064142574974,-16.4429066093382,0.0440956859872955));
#37890=CARTESIAN_POINT('Ctrl Pts',(374.053754847137,-16.4578128503601,0.262585741215501));
#37891=CARTESIAN_POINT('Ctrl Pts',(374.017614573982,-16.4734322616272,0.503367580842284));
#37892=CARTESIAN_POINT('Ctrl Pts',(374.013567032374,-16.4750411104205,0.528329142222957));
#37893=CARTESIAN_POINT('Ctrl Pts',(374.007498328675,-16.4772688285565,0.563155852975093));
#37894=CARTESIAN_POINT('Ctrl Pts',(374.005724226252,-16.4779005791181,0.573062359578017));
#37895=CARTESIAN_POINT('Ctrl Pts',(374.002575834159,-16.4789886869301,0.590180326034277));
#37896=CARTESIAN_POINT('Ctrl Pts',(374.001223268762,-16.4794462438367,0.597395633215517));
#37897=CARTESIAN_POINT('Ctrl Pts',(373.998313051562,-16.480410105544,0.612632612996904));
#37898=CARTESIAN_POINT('Ctrl Pts',(373.996749522974,-16.4809160595897,0.620653099833034));
#37899=CARTESIAN_POINT('Ctrl Pts',(373.992794707616,-16.482167107379,0.640537262129272));
#37900=CARTESIAN_POINT('Ctrl Pts',(373.990367040153,-16.482910159428,0.652393718856743));
#37901=CARTESIAN_POINT('Ctrl Pts',(373.980980545483,-16.4856929606646,0.696957406043927));
#37902=CARTESIAN_POINT('Ctrl Pts',(373.973579337385,-16.487709128971,0.729570598966351));
#37903=CARTESIAN_POINT('Ctrl Pts',(373.913417886548,-16.502876781086,0.976776543161759));
#37904=CARTESIAN_POINT('Ctrl Pts',(373.839212363841,-16.5150558614424,1.18557298503233));
#37905=CARTESIAN_POINT('Ctrl Pts',(373.654800620771,-16.539080145388,1.57298082266496));
#37906=CARTESIAN_POINT('Ctrl Pts',(373.547428172945,-16.5508555038655,1.75168733897278));
#37907=CARTESIAN_POINT('Ctrl Pts',(373.407260112967,-16.5649454219879,1.94083445839598));
#37908=CARTESIAN_POINT('Ctrl Pts',(373.390644912604,-16.5665977522904,1.96266710433325));
#37909=CARTESIAN_POINT('Ctrl Pts',(373.362959355716,-16.5693237252037,1.99809835813762));
#37910=CARTESIAN_POINT('Ctrl Pts',(373.352052977023,-16.5703909016546,2.01182373095153));
#37911=CARTESIAN_POINT('Ctrl Pts',(373.332243703026,-16.5723176798561,2.03633977771281));
#37912=CARTESIAN_POINT('Ctrl Pts',(373.32338144701,-16.5731756354563,2.04716283127113));
#37913=CARTESIAN_POINT('Ctrl Pts',(373.30432820077,-16.5750118116152,2.07012503321343));
#37914=CARTESIAN_POINT('Ctrl Pts',(373.294117588436,-16.5759908185356,2.08224734804377));
#37915=CARTESIAN_POINT('Ctrl Pts',(373.266220519242,-16.5786525065559,2.11487595162464));
#37916=CARTESIAN_POINT('Ctrl Pts',(373.248364652252,-16.5803421444424,2.13523508025426));
#37917=CARTESIAN_POINT('Ctrl Pts',(373.150711199032,-16.5895105300705,2.24378809742133));
#37918=CARTESIAN_POINT('Ctrl Pts',(373.06634310773,-16.5971819105454,2.32772865472945));
#37919=CARTESIAN_POINT('Ctrl Pts',(372.861134771292,-16.6152870729816,2.51046307751723));
#37920=CARTESIAN_POINT('Ctrl Pts',(372.737372936722,-16.6258208207289,2.60552992763899));
#37921=CARTESIAN_POINT('Ctrl Pts',(372.511239339714,-16.6441391148463,2.75449903459483));
#37922=CARTESIAN_POINT('Ctrl Pts',(372.411958976517,-16.6519005815039,2.81253712073997));
#37923=CARTESIAN_POINT('Ctrl Pts',(372.309820496378,-16.659489044147,2.8651369099128));
#37924=CARTESIAN_POINT('Origin',(370.834317853224,2.31077344927308,0.));
#37925=CARTESIAN_POINT('',(372.309820613645,-18.1566220988445,2.86513684952226));
#37926=CARTESIAN_POINT('',(372.30982061364,-17.9078850417037,2.86513684952483));
#37927=CARTESIAN_POINT('',(372.309820613641,2.31077344927308,2.86513684952399));
#37928=CARTESIAN_POINT('Ctrl Pts',(372.309820613645,-18.1566220988445,2.86513684952223));
#37929=CARTESIAN_POINT('Ctrl Pts',(372.311272455587,-18.1565224746897,2.86438917256799));
#37930=CARTESIAN_POINT('Ctrl Pts',(372.312723729234,-18.1564228118652,2.86364039207921));
#37931=CARTESIAN_POINT('Ctrl Pts',(372.326767808063,-18.1554576139208,2.85638086804062));
#37932=CARTESIAN_POINT('Ctrl Pts',(372.339317931448,-18.1545892200256,2.84978828782492));
#37933=CARTESIAN_POINT('Ctrl Pts',(372.36512906347,-18.1527908926273,2.83601164631683));
#37934=CARTESIAN_POINT('Ctrl Pts',(372.378383934423,-18.1518605947356,2.82881688060898));
#37935=CARTESIAN_POINT('Ctrl Pts',(372.412247200125,-18.1494661414153,2.81012693188647));
#37936=CARTESIAN_POINT('Ctrl Pts',(372.432780445712,-18.1479972342059,2.79849811327024));
#37937=CARTESIAN_POINT('Ctrl Pts',(372.513369501142,-18.142163295722,2.75168093150799));
#37938=CARTESIAN_POINT('Ctrl Pts',(372.572402702544,-18.1377368166799,2.71477848919915));
#37939=CARTESIAN_POINT('Ctrl Pts',(372.903756766383,-18.1119825699006,2.49240520076421));
#37940=CARTESIAN_POINT('Ctrl Pts',(373.147485721579,-18.0891386287628,2.26800440197018));
#37941=CARTESIAN_POINT('Ctrl Pts',(373.382019222329,-18.0643288144873,1.97420987794159));
#37942=CARTESIAN_POINT('Ctrl Pts',(373.410286213246,-18.0612851649056,1.93718206565545));
#37943=CARTESIAN_POINT('Ctrl Pts',(373.455912336209,-18.0562978202709,1.87464937232052));
#37944=CARTESIAN_POINT('Ctrl Pts',(373.47372525588,-18.0543304981424,1.84948550355376));
#37945=CARTESIAN_POINT('Ctrl Pts',(373.497809231683,-18.0516464018496,1.81440585998606));
#37946=CARTESIAN_POINT('Ctrl Pts',(373.504390730472,-18.0509103276274,1.80470656563241));
#37947=CARTESIAN_POINT('Ctrl Pts',(373.515425294158,-18.0496721163653,1.78825219267867));
#37948=CARTESIAN_POINT('Ctrl Pts',(373.519906069262,-18.0491681535526,1.78151591444796));
#37949=CARTESIAN_POINT('Ctrl Pts',(373.528441075473,-18.0482060610674,1.76857923310684));
#37950=CARTESIAN_POINT('Ctrl Pts',(373.532499344245,-18.0477476494008,1.76238165122051));
#37951=CARTESIAN_POINT('Ctrl Pts',(373.542169638696,-18.0466528874298,1.74750197171174));
#37952=CARTESIAN_POINT('Ctrl Pts',(373.547761370958,-18.0460178683492,1.73880669312301));
#37953=CARTESIAN_POINT('Ctrl Pts',(373.567829863526,-18.0437310008234,1.70726713642371));
#37954=CARTESIAN_POINT('Ctrl Pts',(373.582061219956,-18.0420943985745,1.68426704681048));
#37955=CARTESIAN_POINT('Ctrl Pts',(373.680851554203,-18.0306056967888,1.52002083554513));
#37956=CARTESIAN_POINT('Ctrl Pts',(373.754778409436,-18.021318990523,1.37264003441066));
#37957=CARTESIAN_POINT('Ctrl Pts',(373.869780397681,-18.0043043085601,1.09152415619711));
#37958=CARTESIAN_POINT('Ctrl Pts',(373.91404932033,-17.9965759599883,0.959536767928402));
#37959=CARTESIAN_POINT('Ctrl Pts',(373.972914253652,-17.9835134164142,0.737281790762283));
#37960=CARTESIAN_POINT('Ctrl Pts',(373.992449289228,-17.9782858701628,0.648518210451095));
#37961=CARTESIAN_POINT('Ctrl Pts',(374.018501010872,-17.9694654434798,0.500615603629913));
#37962=CARTESIAN_POINT('Ctrl Pts',(374.027177755205,-17.9659365810877,0.441908752567425));
#37963=CARTESIAN_POINT('Ctrl Pts',(374.036785426267,-17.9610589387017,0.361637699410192));
#37964=CARTESIAN_POINT('Ctrl Pts',(374.039128103955,-17.9597544427021,0.340252265720417));
#37965=CARTESIAN_POINT('Ctrl Pts',(374.042704875131,-17.9575509014232,0.30427719254953));
#37966=CARTESIAN_POINT('Ctrl Pts',(374.04405399143,-17.9566554900278,0.289699506760121));
#37967=CARTESIAN_POINT('Ctrl Pts',(374.0465225546,-17.954880620755,0.260887665127171));
#37968=CARTESIAN_POINT('Ctrl Pts',(374.047646825911,-17.9540013358557,0.246654252351041));
#37969=CARTESIAN_POINT('Ctrl Pts',(374.05014874386,-17.9518575153502,0.212051944139108));
#37970=CARTESIAN_POINT('Ctrl Pts',(374.051427479241,-17.9505899111106,0.191676726808597));
#37971=CARTESIAN_POINT('Ctrl Pts',(374.054509972385,-17.9469714890389,0.133763252387256));
#37972=CARTESIAN_POINT('Ctrl Pts',(374.055850774254,-17.9446063798233,0.096204673597261));
#37973=CARTESIAN_POINT('Ctrl Pts',(374.060118796779,-17.9297162148921,-0.138349548598383));
#37974=CARTESIAN_POINT('Ctrl Pts',(374.045632434078,-17.9166524107532,-0.335213734643995));
#37975=CARTESIAN_POINT('Ctrl Pts',(373.977994876229,-17.8888800873244,-0.741293296357779));
#37976=CARTESIAN_POINT('Ctrl Pts',(373.921637211871,-17.8741982093691,-0.949047432136426));
#37977=CARTESIAN_POINT('Ctrl Pts',(373.833242583549,-17.8582047356997,-1.18053383136164));
#37978=CARTESIAN_POINT('Ctrl Pts',(373.820978923856,-17.8560929931491,-1.21122479857131));
#37979=CARTESIAN_POINT('Ctrl Pts',(373.803605061511,-17.8532470790033,-1.25283520240953));
#37980=CARTESIAN_POINT('Ctrl Pts',(373.798902997843,-17.8524905226537,-1.26392147729961));
#37981=CARTESIAN_POINT('Ctrl Pts',(373.790912679704,-17.8512278199055,-1.28247069868622));
#37982=CARTESIAN_POINT('Ctrl Pts',(373.787658072661,-17.8507196851463,-1.28994791127096));
#37983=CARTESIAN_POINT('Ctrl Pts',(373.781418381097,-17.8497572653634,-1.30413572164383));
#37984=CARTESIAN_POINT('Ctrl Pts',(373.778438692717,-17.849302647879,-1.31084857510864));
#37985=CARTESIAN_POINT('Ctrl Pts',(373.771310236494,-17.8482266275866,-1.32676114935411));
#37986=CARTESIAN_POINT('Ctrl Pts',(373.767141124425,-17.8476064537096,-1.33595174801758));
#37987=CARTESIAN_POINT('Ctrl Pts',(373.752295274384,-17.8454294343591,-1.3682742401605));
#37988=CARTESIAN_POINT('Ctrl Pts',(373.741387172071,-17.8438859864404,-1.39129964200097));
#37989=CARTESIAN_POINT('Ctrl Pts',(373.636197315612,-17.8294946859269,-1.60670016403932));
#37990=CARTESIAN_POINT('Ctrl Pts',(373.523213188884,-17.8176247779347,-1.78938009521692));
#37991=CARTESIAN_POINT('Ctrl Pts',(373.257455177897,-17.7931791000757,-2.1363891967906));
#37992=CARTESIAN_POINT('Ctrl Pts',(373.104036478827,-17.7806386349199,-2.29872005507313));
#37993=CARTESIAN_POINT('Ctrl Pts',(372.911099012102,-17.7654259002684,-2.46456903345395));
#37994=CARTESIAN_POINT('Ctrl Pts',(372.886780802671,-17.7635185832077,-2.48485738749289));
#37995=CARTESIAN_POINT('Ctrl Pts',(372.84909412177,-17.7605759114643,-2.51536818698017));
#37996=CARTESIAN_POINT('Ctrl Pts',(372.835937584093,-17.7595510163357,-2.52585014690899));
#37997=CARTESIAN_POINT('Ctrl Pts',(372.811836523562,-17.7576775674519,-2.54474517693252));
#37998=CARTESIAN_POINT('Ctrl Pts',(372.800918797294,-17.756830379529,-2.55319188947021));
#37999=CARTESIAN_POINT('Ctrl Pts',(372.776976276307,-17.7549755315757,-2.57147080952233));
#38000=CARTESIAN_POINT('Ctrl Pts',(372.763930443029,-17.7539667908113,-2.58127470653681));
#38001=CARTESIAN_POINT('Ctrl Pts',(372.727900031589,-17.7511857674438,-2.60792564975395));
#38002=CARTESIAN_POINT('Ctrl Pts',(372.704766007083,-17.7494056114818,-2.62456725591072));
#38003=CARTESIAN_POINT('Ctrl Pts',(372.573798457109,-17.7393554033275,-2.7161685379367));
#38004=CARTESIAN_POINT('Ctrl Pts',(372.461695482452,-17.7308492103,-2.78477983918326));
#38005=CARTESIAN_POINT('Ctrl Pts',(372.152216154913,-17.7076472245125,-2.9491132722235));
#38006=CARTESIAN_POINT('Ctrl Pts',(371.948728804061,-17.692641303294,-3.03186442814594));
#38007=CARTESIAN_POINT('Ctrl Pts',(371.637790762505,-17.6709764271891,-3.12274655071335));
#38008=CARTESIAN_POINT('Ctrl Pts',(371.535747746345,-17.6640663585574,-3.1472393293699));
#38009=CARTESIAN_POINT('Ctrl Pts',(371.415703805194,-17.6562990364168,-3.16992216028446));
#38010=CARTESIAN_POINT('Ctrl Pts',(371.398699248294,-17.6552071638666,-3.17299382272355));
#38011=CARTESIAN_POINT('Ctrl Pts',(371.372508792167,-17.6535391992345,-3.17750759298088));
#38012=CARTESIAN_POINT('Ctrl Pts',(371.363340281956,-17.6529578760478,-3.17904691145144));
#38013=CARTESIAN_POINT('Ctrl Pts',(371.346436060333,-17.6518909909958,-3.18180983694083));
#38014=CARTESIAN_POINT('Ctrl Pts',(371.338702562616,-17.6514048118915,-3.18304492014342));
#38015=CARTESIAN_POINT('Ctrl Pts',(371.321144695166,-17.6503052835796,-3.18578341389902));
#38016=CARTESIAN_POINT('Ctrl Pts',(371.311317831575,-17.6496929080889,-3.1872695777252));
#38017=CARTESIAN_POINT('Ctrl Pts',(371.285764027622,-17.6481079433627,-3.19101337179345));
#38018=CARTESIAN_POINT('Ctrl Pts',(371.270026777515,-17.6471391758871,-3.19320023549246));
#38019=CARTESIAN_POINT('Ctrl Pts',(371.162223264578,-17.6405490738872,-3.20736889704702));
#38020=CARTESIAN_POINT('Ctrl Pts',(371.069683910013,-17.6351217352367,-3.21548493149783));
#38021=CARTESIAN_POINT('Ctrl Pts',(370.89497092361,-17.6250931827155,-3.22322303948595));
#38022=CARTESIAN_POINT('Ctrl Pts',(370.812915000222,-17.6204731452029,-3.22372276897205));
#38023=CARTESIAN_POINT('Ctrl Pts',(370.59828778088,-17.6084366279982,-3.21683362490853));
#38024=CARTESIAN_POINT('Ctrl Pts',(370.466039115849,-17.6010634035132,-3.20438743792046));
#38025=CARTESIAN_POINT('Ctrl Pts',(370.238247108365,-17.5880033552765,-3.16865842814046));
#38026=CARTESIAN_POINT('Ctrl Pts',(370.142304174231,-17.5823902094017,-3.14909693923421));
#38027=CARTESIAN_POINT('Ctrl Pts',(370.006711540312,-17.5741925626739,-3.11495526004104));
#38028=CARTESIAN_POINT('Ctrl Pts',(369.966223825611,-17.5717106375951,-3.10391543249087));
#38029=CARTESIAN_POINT('Ctrl Pts',(369.894288036021,-17.5672322257253,-3.08278307605368));
#38030=CARTESIAN_POINT('Ctrl Pts',(369.862757389896,-17.5652453452894,-3.07299165242911));
#38031=CARTESIAN_POINT('Ctrl Pts',(369.815133883546,-17.5622054729207,-3.05739659949721));
#38032=CARTESIAN_POINT('Ctrl Pts',(369.798927037312,-17.5611640629864,-3.05194622682745));
#38033=CARTESIAN_POINT('Ctrl Pts',(369.769580670656,-17.5592654367029,-3.04181636856075));
#38034=CARTESIAN_POINT('Ctrl Pts',(369.756426619538,-17.5584096655022,-3.03718003527179));
#38035=CARTESIAN_POINT('Ctrl Pts',(369.728117436705,-17.5565574994371,-3.02699498839624));
#38036=CARTESIAN_POINT('Ctrl Pts',(369.712973114192,-17.5555601670673,-3.02141754519029));
#38037=CARTESIAN_POINT('Ctrl Pts',(369.671948971665,-17.5528405125514,-3.00595800900626));
#38038=CARTESIAN_POINT('Ctrl Pts',(369.646154111898,-17.5511108769936,-2.99585577348444));
#38039=CARTESIAN_POINT('Ctrl Pts',(369.511670807134,-17.5419878780569,-2.94117703568361));
#38040=CARTESIAN_POINT('Ctrl Pts',(369.405361236193,-17.5344076589766,-2.89101972272695));
#38041=CARTESIAN_POINT('Ctrl Pts',(369.100207979186,-17.5115502347573,-2.7260985344978));
#38042=CARTESIAN_POINT('Ctrl Pts',(368.910612341183,-17.4958394940733,-2.5957833433018));
#38043=CARTESIAN_POINT('Ctrl Pts',(368.680121355113,-17.4755063573029,-2.39813829373268));
#38044=CARTESIAN_POINT('Ctrl Pts',(368.625443682218,-17.4705828018742,-2.34787267731464));
#38045=CARTESIAN_POINT('Ctrl Pts',(368.541914925819,-17.462959462446,-2.2655806277239));
#38046=CARTESIAN_POINT('Ctrl Pts',(368.511887106196,-17.4601967082233,-2.23478916354029));
#38047=CARTESIAN_POINT('Ctrl Pts',(368.473399270228,-17.4566367725319,-2.19370862359015));
#38048=CARTESIAN_POINT('Ctrl Pts',(368.464375436289,-17.4558007154867,-2.18395673846982));
#38049=CARTESIAN_POINT('Ctrl Pts',(368.449729970821,-17.4544419318746,-2.16793199424891));
#38050=CARTESIAN_POINT('Ctrl Pts',(368.444072271429,-17.4539165530998,-2.16169252280414));
#38051=CARTESIAN_POINT('Ctrl Pts',(368.433089187723,-17.4528958689476,-2.14948422688604));
#38052=CARTESIAN_POINT('Ctrl Pts',(368.427761483458,-17.4524003974966,-2.14351766647589));
#38053=CARTESIAN_POINT('Ctrl Pts',(368.414720051287,-17.4511865064303,-2.12880249813699));
#38054=CARTESIAN_POINT('Ctrl Pts',(368.407031400889,-17.4504699357884,-2.12003162411374));
#38055=CARTESIAN_POINT('Ctrl Pts',(368.380832281767,-17.4480242800004,-2.08981545373216));
#38056=CARTESIAN_POINT('Ctrl Pts',(368.362556463019,-17.4463114373808,-2.06816726455138));
#38057=CARTESIAN_POINT('Ctrl Pts',(368.138316755813,-17.4251682794733,-1.7953303082772));
#38058=CARTESIAN_POINT('Ctrl Pts',(367.971161677067,-17.4078836424248,-1.51460813668211));
#38059=CARTESIAN_POINT('Ctrl Pts',(367.804805783727,-17.382611375939,-1.10536121641511));
#38060=CARTESIAN_POINT('Ctrl Pts',(367.766733022571,-17.3757999892202,-0.994829521371667));
#38061=CARTESIAN_POINT('Ctrl Pts',(367.727371254028,-17.3671716546808,-0.856577987980679));
#38062=CARTESIAN_POINT('Ctrl Pts',(367.720321072374,-17.3655448668063,-0.830582326898628));
#38063=CARTESIAN_POINT('Ctrl Pts',(367.709650907161,-17.3629464395477,-0.789191998261899));
#38064=CARTESIAN_POINT('Ctrl Pts',(367.705816875335,-17.3619817232031,-0.773853443073163));
#38065=CARTESIAN_POINT('Ctrl Pts',(367.698805235388,-17.3601569824079,-0.744898434275763));
#38066=CARTESIAN_POINT('Ctrl Pts',(367.695603065259,-17.3592977719579,-0.731288263296041));
#38067=CARTESIAN_POINT('Ctrl Pts',(367.688579399558,-17.3573530286158,-0.70053941658764));
#38068=CARTESIAN_POINT('Ctrl Pts',(367.684809233268,-17.3562658776419,-0.683389586071041));
#38069=CARTESIAN_POINT('Ctrl Pts',(367.675483915894,-17.3534612699564,-0.639253333006067));
#38070=CARTESIAN_POINT('Ctrl Pts',(367.67013443683,-17.3517373288029,-0.612225366257496));
#38071=CARTESIAN_POINT('Ctrl Pts',(367.629312528714,-17.3375790029011,-0.391126490720944));
#38072=CARTESIAN_POINT('Ctrl Pts',(367.611388699999,-17.3245840805187,-0.194274640082018));
#38073=CARTESIAN_POINT('Ctrl Pts',(367.611756317698,-17.2975526701401,0.207397995299695));
#38074=CARTESIAN_POINT('Ctrl Pts',(367.631397625581,-17.2835589428912,0.411367515210719));
#38075=CARTESIAN_POINT('Ctrl Pts',(367.680579773175,-17.2665934771642,0.665599276409641));
#38076=CARTESIAN_POINT('Ctrl Pts',(367.692284086745,-17.2630710855992,0.718826047744092));
#38077=CARTESIAN_POINT('Ctrl Pts',(367.708940487933,-17.2586611938674,0.786359205967593));
#38078=CARTESIAN_POINT('Ctrl Pts',(367.712650277796,-17.2577113791877,0.800959453061964));
#38079=CARTESIAN_POINT('Ctrl Pts',(367.718693296946,-17.2562146856849,0.824062441180066));
#38080=CARTESIAN_POINT('Ctrl Pts',(367.720959225455,-17.2556640927977,0.832582333418417));
#38081=CARTESIAN_POINT('Ctrl Pts',(367.725325752797,-17.2546230601939,0.848733365040112));
#38082=CARTESIAN_POINT('Ctrl Pts',(367.72741948144,-17.2541322640714,0.856365992984681));
#38083=CARTESIAN_POINT('Ctrl Pts',(367.732412322328,-17.2529811997489,0.874307908959234));
#38084=CARTESIAN_POINT('Ctrl Pts',(367.735334727508,-17.2523222807221,0.884610556343805));
#38085=CARTESIAN_POINT('Ctrl Pts',(367.745128867118,-17.2501613579301,0.918494560075191));
#38086=CARTESIAN_POINT('Ctrl Pts',(367.752219016763,-17.2486713882148,0.942012576382163));
#38087=CARTESIAN_POINT('Ctrl Pts',(367.793068157957,-17.2404724321887,1.07210813275743));
#38088=CARTESIAN_POINT('Ctrl Pts',(367.832089524263,-17.2340245788628,1.17696459774762));
#38089=CARTESIAN_POINT('Ctrl Pts',(367.994451570116,-17.2108341043497,1.55227199535719));
#38090=CARTESIAN_POINT('Ctrl Pts',(368.149546398421,-17.1947082962738,1.8073165771048));
#38091=CARTESIAN_POINT('Ctrl Pts',(368.369696370391,-17.1741710836258,2.07710621084808));
#38092=CARTESIAN_POINT('Ctrl Pts',(368.402942043159,-17.1711235540913,2.11592544849935));
#38093=CARTESIAN_POINT('Ctrl Pts',(368.451061991343,-17.1667767712337,2.16948052544261));
#38094=CARTESIAN_POINT('Ctrl Pts',(368.465179273883,-17.165508970542,2.18488823825482));
#38095=CARTESIAN_POINT('Ctrl Pts',(368.488364251498,-17.1634382307613,2.20970358716528));
#38096=CARTESIAN_POINT('Ctrl Pts',(368.497341213578,-17.1626391743246,2.21919544484741));
#38097=CARTESIAN_POINT('Ctrl Pts',(368.516280450613,-17.1609588428651,2.23897863220294));
#38098=CARTESIAN_POINT('Ctrl Pts',(368.52625409672,-17.1600770840736,2.24925863358192));
#38099=CARTESIAN_POINT('Ctrl Pts',(368.550240660873,-17.157963663427,2.27365444860545));
#38100=CARTESIAN_POINT('Ctrl Pts',(368.564316250548,-17.156729258969,2.28770755728963));
#38101=CARTESIAN_POINT('Ctrl Pts',(368.613062650418,-17.1524732593598,2.33548327426032));
#38102=CARTESIAN_POINT('Ctrl Pts',(368.648360640956,-17.1494237035336,2.36855387511503));
#38103=CARTESIAN_POINT('Ctrl Pts',(368.794694906472,-17.1369032868009,2.49959614354931));
#38104=CARTESIAN_POINT('Ctrl Pts',(368.91166430413,-17.1271600299159,2.59064394632193));
#38105=CARTESIAN_POINT('Ctrl Pts',(369.185238553045,-17.1050566465925,2.77483199317565));
#38106=CARTESIAN_POINT('Ctrl Pts',(369.344326446425,-17.0926381768084,2.86340343563949));
#38107=CARTESIAN_POINT('Ctrl Pts',(369.596220774644,-17.0742120008577,2.97693990324591));
#38108=CARTESIAN_POINT('Ctrl Pts',(369.684087726991,-17.0680011140411,3.01198102555866));
#38109=CARTESIAN_POINT('Ctrl Pts',(369.788443786333,-17.0609710397771,3.04836343364431));
#38110=CARTESIAN_POINT('Ctrl Pts',(369.803550462248,-17.0599616954946,3.05350467448696));
#38111=CARTESIAN_POINT('Ctrl Pts',(369.828146749709,-17.0583325213329,3.06167216697092));
#38112=CARTESIAN_POINT('Ctrl Pts',(369.837613092478,-17.0577089034025,3.0647669362743));
#38113=CARTESIAN_POINT('Ctrl Pts',(369.854550052235,-17.0565993984479,3.07021725158917));
#38114=CARTESIAN_POINT('Ctrl Pts',(369.862015044824,-17.0561125577271,3.07258948912748));
#38115=CARTESIAN_POINT('Ctrl Pts',(369.878343644799,-17.0550524288006,3.07771294987256));
#38116=CARTESIAN_POINT('Ctrl Pts',(369.887210511191,-17.0544797841385,3.08045311223727));
#38117=CARTESIAN_POINT('Ctrl Pts',(369.912546848122,-17.0528518171205,3.08816316151229));
#38118=CARTESIAN_POINT('Ctrl Pts',(369.929044727598,-17.0518017598808,3.09303962079563));
#38119=CARTESIAN_POINT('Ctrl Pts',(370.044350253084,-17.04452726393,3.12612012043599));
#38120=CARTESIAN_POINT('Ctrl Pts',(370.144428580246,-17.0385418272147,3.14971951048712));
#38121=CARTESIAN_POINT('Ctrl Pts',(370.388709111282,-17.0243477330293,3.1951174534242));
#38122=CARTESIAN_POINT('Ctrl Pts',(370.533590594242,-17.0162661444774,3.21199457798821));
#38123=CARTESIAN_POINT('Ctrl Pts',(370.883060434138,-16.9966680405207,3.22884336333444));
#38124=CARTESIAN_POINT('Ctrl Pts',(371.087444345024,-16.9850959737636,3.2192727689767));
#38125=CARTESIAN_POINT('Ctrl Pts',(371.316663332644,-16.9712379720792,3.18656731558649));
#38126=CARTESIAN_POINT('Ctrl Pts',(371.343739220006,-16.9695876342822,3.18235105223757));
#38127=CARTESIAN_POINT('Ctrl Pts',(371.388027066876,-16.9668646948732,3.17487486494676));
#38128=CARTESIAN_POINT('Ctrl Pts',(371.405272371843,-16.9657985413286,3.17181891352475));
#38129=CARTESIAN_POINT('Ctrl Pts',(371.43623459049,-16.9638734507462,3.16607156899831));
#38130=CARTESIAN_POINT('Ctrl Pts',(371.449960613528,-16.9630161555497,3.16343119422142));
#38131=CARTESIAN_POINT('Ctrl Pts',(371.479203946042,-16.9611812253746,3.15760833501188));
#38132=CARTESIAN_POINT('Ctrl Pts',(371.494715791472,-16.9602028039494,3.15440057996654));
#38133=CARTESIAN_POINT('Ctrl Pts',(371.53667114559,-16.957542305202,3.14540143720601));
#38134=CARTESIAN_POINT('Ctrl Pts',(371.56306589521,-16.9558532742018,3.13939111420503));
#38135=CARTESIAN_POINT('Ctrl Pts',(371.705059756929,-16.9466820864274,3.10517066284102));
#38136=CARTESIAN_POINT('Ctrl Pts',(371.819092226175,-16.9390070957941,3.07091028896699));
#38137=CARTESIAN_POINT('Ctrl Pts',(372.060678684937,-16.9220784159541,2.9834857840475));
#38138=CARTESIAN_POINT('Ctrl Pts',(372.187224989695,-16.9127845441374,2.92827176954826));
#38139=CARTESIAN_POINT('Ctrl Pts',(372.309820641399,-16.9034565314269,2.86513683522936));
#38140=CARTESIAN_POINT('',(367.611567912033,-17.0672029561653,-0.000615672028770192));
#38141=CARTESIAN_POINT('Ctrl Pts',(372.309820496378,-16.659489044147,2.86513690991278));
#38142=CARTESIAN_POINT('Ctrl Pts',(372.262650708085,-16.6629935624819,2.88942864517458));
#38143=CARTESIAN_POINT('Ctrl Pts',(372.214871312371,-16.6664605937869,2.91256053053015));
#38144=CARTESIAN_POINT('Ctrl Pts',(372.141992305273,-16.671602854912,2.94564610246232));
#38145=CARTESIAN_POINT('Ctrl Pts',(372.117320350931,-16.6733189975538,2.95647562724856));
#38146=CARTESIAN_POINT('Ctrl Pts',(372.083005338726,-16.6756690614488,2.97102740022174));
#38147=CARTESIAN_POINT('Ctrl Pts',(372.073476620043,-16.6763177432156,2.97501425320145));
#38148=CARTESIAN_POINT('Ctrl Pts',(372.057080114797,-16.6774270829223,2.98178216997762));
#38149=CARTESIAN_POINT('Ctrl Pts',(372.050221672257,-16.6778890488854,2.98458545915616));
#38150=CARTESIAN_POINT('Ctrl Pts',(372.035844558692,-16.6788530604544,2.99040411298314));
#38151=CARTESIAN_POINT('Ctrl Pts',(372.028324103031,-16.6793548065152,2.99341481590983));
#38152=CARTESIAN_POINT('Ctrl Pts',(372.009866088416,-16.6805803069624,3.0007235810072));
#38153=CARTESIAN_POINT('Ctrl Pts',(371.998916083265,-16.6813022022125,3.00499028873532));
#38154=CARTESIAN_POINT('Ctrl Pts',(371.958999122469,-16.6839160543264,3.02029310874339));
#38155=CARTESIAN_POINT('Ctrl Pts',(371.929895653298,-16.6857879744324,3.03097143922983));
#38156=CARTESIAN_POINT('Ctrl Pts',(371.856368790584,-16.6904433224381,3.05675162136396));
#38157=CARTESIAN_POINT('Ctrl Pts',(371.811760227619,-16.6932007740934,3.07130679575183));
#38158=CARTESIAN_POINT('Ctrl Pts',(371.443406119834,-16.7155450849012,3.1826566025822));
#38159=CARTESIAN_POINT('Ctrl Pts',(371.106594318805,-16.7335378055608,3.22896227462198));
#38160=CARTESIAN_POINT('Ctrl Pts',(370.706189162994,-16.7570025275489,3.22080903927003));
#38161=CARTESIAN_POINT('Ctrl Pts',(370.643723679882,-16.7607142270674,3.21771672472883));
#38162=CARTESIAN_POINT('Ctrl Pts',(370.558803700995,-16.7658476300432,3.21103142973763));
#38163=CARTESIAN_POINT('Ctrl Pts',(370.536236670781,-16.7672202068724,3.20901518527397));
#38164=CARTESIAN_POINT('Ctrl Pts',(370.500360748185,-16.7694163899799,3.20542816889744));
#38165=CARTESIAN_POINT('Ctrl Pts',(370.487036892193,-16.7702351313492,3.20401201926006));
#38166=CARTESIAN_POINT('Ctrl Pts',(370.459690769202,-16.7719220881224,3.20093290988067));
#38167=CARTESIAN_POINT('Ctrl Pts',(370.44566984396,-16.7727905743016,3.19926079906817));
#38168=CARTESIAN_POINT('Ctrl Pts',(370.413185603054,-16.7748111498907,3.19517009347095));
#38169=CARTESIAN_POINT('Ctrl Pts',(370.394731501116,-16.7759653575872,3.19268352864213));
#38170=CARTESIAN_POINT('Ctrl Pts',(370.335835132856,-16.7796697886667,3.18422733541922));
#38171=CARTESIAN_POINT('Ctrl Pts',(370.295485767457,-16.7822390895788,3.177648262919));
#38172=CARTESIAN_POINT('Ctrl Pts',(370.201007904746,-16.7883316549126,3.16039223939409));
#38173=CARTESIAN_POINT('Ctrl Pts',(370.147008117449,-16.791873579666,3.14908960577615));
#38174=CARTESIAN_POINT('Ctrl Pts',(369.946950222638,-16.80521923053,3.10182502334244));
#38175=CARTESIAN_POINT('Ctrl Pts',(369.803188308791,-16.8152695799673,3.05704156139889));
#38176=CARTESIAN_POINT('Ctrl Pts',(369.460642174878,-16.840094972195,2.92341508949743));
#38177=CARTESIAN_POINT('Ctrl Pts',(369.26668564817,-16.8549393966478,2.82416070148185));
#38178=CARTESIAN_POINT('Ctrl Pts',(369.063066496116,-16.8704934669863,2.69247446804024));
#38179=CARTESIAN_POINT('Ctrl Pts',(369.042107199391,-16.8720935828904,2.67856887046183));
#38180=CARTESIAN_POINT('Ctrl Pts',(369.013010656927,-16.8743112548417,2.65877010694048));
#38181=CARTESIAN_POINT('Ctrl Pts',(369.00473551571,-16.8749415449182,2.6530825206512));
#38182=CARTESIAN_POINT('Ctrl Pts',(368.990461450957,-16.8760278299444,2.64317326987093));
#38183=CARTESIAN_POINT('Ctrl Pts',(368.984450164862,-16.8764850152884,2.6389696672845));
#38184=CARTESIAN_POINT('Ctrl Pts',(368.971925758133,-16.8774368647073,2.63014771338083));
#38185=CARTESIAN_POINT('Ctrl Pts',(368.965415352056,-16.8779312566451,2.62552561473488));
#38186=CARTESIAN_POINT('Ctrl Pts',(368.949377502307,-16.8791483489555,2.61404957514139));
#38187=CARTESIAN_POINT('Ctrl Pts',(368.939870086883,-16.8798691521744,2.60716761607293));
#38188=CARTESIAN_POINT('Ctrl Pts',(368.919403109872,-16.8814198309935,2.59218148776407));
#38189=CARTESIAN_POINT('Ctrl Pts',(368.908456890568,-16.882248530284,2.58405938529645));
#38190=CARTESIAN_POINT('Ctrl Pts',(368.877524678459,-16.8845895054829,2.56080193004355));
#38191=CARTESIAN_POINT('Ctrl Pts',(368.857662877341,-16.8860917153746,2.54550215868964));
#38192=CARTESIAN_POINT('Ctrl Pts',(368.790781951608,-16.8911545437106,2.49272810742424));
#38193=CARTESIAN_POINT('Ctrl Pts',(368.74463159088,-16.8946557137532,2.45416881047839));
#38194=CARTESIAN_POINT('Ctrl Pts',(368.473097825576,-16.9154859910744,2.21408147750278));
#38195=CARTESIAN_POINT('Ctrl Pts',(368.275914163258,-16.9317540681465,1.98295407454614));
#38196=CARTESIAN_POINT('Ctrl Pts',(368.074281504201,-16.9536608277038,1.66545987109065));
#38197=CARTESIAN_POINT('Ctrl Pts',(368.03689325041,-16.9580202953467,1.60186503628977));
#38198=CARTESIAN_POINT('Ctrl Pts',(367.990227832369,-16.9639084551325,1.51586616965014));
#38199=CARTESIAN_POINT('Ctrl Pts',(367.978972649988,-16.9653667830668,1.494557463995));
#38200=CARTESIAN_POINT('Ctrl Pts',(367.961010735384,-16.9677585880796,1.45960773681184));
#38201=CARTESIAN_POINT('Ctrl Pts',(367.954159544919,-16.9686869629579,1.44604171637026));
#38202=CARTESIAN_POINT('Ctrl Pts',(367.941117647913,-16.970485911897,1.41975709571559));
#38203=CARTESIAN_POINT('Ctrl Pts',(367.934914208457,-16.9713560152189,1.40704517817393));
#38204=CARTESIAN_POINT('Ctrl Pts',(367.920667614035,-16.9733884946347,1.37735715012612));
#38205=CARTESIAN_POINT('Ctrl Pts',(367.912688868128,-16.9745530678839,1.36035086827977));
#38206=CARTESIAN_POINT('Ctrl Pts',(367.887439612811,-16.9783253268818,1.30528650333673));
#38207=CARTESIAN_POINT('Ctrl Pts',(367.870761162794,-16.9809530857138,1.26696317971802));
#38208=CARTESIAN_POINT('Ctrl Pts',(367.83319658768,-16.9872090820167,1.17584493234048));
#38209=CARTESIAN_POINT('Ctrl Pts',(367.812951534621,-16.9908573621093,1.12280234002851));
#38210=CARTESIAN_POINT('Ctrl Pts',(367.741722098781,-17.0048111140382,0.920276643044859));
#38211=CARTESIAN_POINT('Ctrl Pts',(367.700352129991,-17.0153885726118,0.76766326205813));
#38212=CARTESIAN_POINT('Ctrl Pts',(367.631209677124,-17.0399686176423,0.410581857261768));
#38213=CARTESIAN_POINT('Ctrl Pts',(367.611528588751,-17.053991323043,0.205222988379962));
#38214=CARTESIAN_POINT('Ctrl Pts',(367.611567912033,-17.0672029561653,-0.000615672028770192));
#38215=CARTESIAN_POINT('Ctrl Pts',(367.611567912602,-17.0672031470406,-0.00061864588800962));
#38216=CARTESIAN_POINT('Ctrl Pts',(367.611570957118,-17.0682211099538,-0.0164786273153796));
#38217=CARTESIAN_POINT('Ctrl Pts',(367.611691078271,-17.0692338931669,-0.0323387716768588));
#38218=CARTESIAN_POINT('Ctrl Pts',(367.612138722679,-17.0711344453491,-0.0622672202399708));
#38219=CARTESIAN_POINT('Ctrl Pts',(367.612441307727,-17.072023403668,-0.076335432346843));
#38220=CARTESIAN_POINT('Ctrl Pts',(367.613056974207,-17.0734023779987,-0.0982748725629377));
#38221=CARTESIAN_POINT('Ctrl Pts',(367.613306783411,-17.0738957229655,-0.106147503405766));
#38222=CARTESIAN_POINT('Ctrl Pts',(367.613851155909,-17.0748563448645,-0.121524541521579));
#38223=CARTESIAN_POINT('Ctrl Pts',(367.614143093733,-17.0753237617378,-0.12902901098511));
#38224=CARTESIAN_POINT('Ctrl Pts',(367.614827398663,-17.0763258391311,-0.145167017576318));
#38225=CARTESIAN_POINT('Ctrl Pts',(367.615228262234,-17.076860022709,-0.153800062710141));
#38226=CARTESIAN_POINT('Ctrl Pts',(367.616382604606,-17.0782706427935,-0.17667388015715));
#38227=CARTESIAN_POINT('Ctrl Pts',(367.617195895314,-17.0791438146921,-0.190911627513823));
#38228=CARTESIAN_POINT('Ctrl Pts',(367.621107655103,-17.0828857601728,-0.2522396163173));
#38229=CARTESIAN_POINT('Ctrl Pts',(367.625145896418,-17.0857063948571,-0.299266566907833));
#38230=CARTESIAN_POINT('Ctrl Pts',(367.662099032802,-17.1059737394695,-0.641279429069706));
#38231=CARTESIAN_POINT('Ctrl Pts',(367.734595054949,-17.1218983053493,-0.930576127672779));
#38232=CARTESIAN_POINT('Ctrl Pts',(367.89059535041,-17.1457207982213,-1.31720314357685));
#38233=CARTESIAN_POINT('Ctrl Pts',(367.941690097384,-17.152711835624,-1.42591245093985));
#38234=CARTESIAN_POINT('Ctrl Pts',(368.011625526135,-17.1615437755249,-1.55539788589501));
#38235=CARTESIAN_POINT('Ctrl Pts',(368.024827587978,-17.1631832237465,-1.57911967181968));
#38236=CARTESIAN_POINT('Ctrl Pts',(368.046216795702,-17.1657976701473,-1.61643488371139));
#38237=CARTESIAN_POINT('Ctrl Pts',(368.054207536525,-17.1667656029413,-1.63013982625584));
#38238=CARTESIAN_POINT('Ctrl Pts',(368.069432953017,-17.1685938218349,-1.65581541066522));
#38239=CARTESIAN_POINT('Ctrl Pts',(368.076645026661,-17.1694532709602,-1.6677990758605));
#38240=CARTESIAN_POINT('Ctrl Pts',(368.093060422651,-17.1713950574803,-1.6946774941438));
#38241=CARTESIAN_POINT('Ctrl Pts',(368.102307522788,-17.1724789851461,-1.70954486482611));
#38242=CARTESIAN_POINT('Ctrl Pts',(368.126314836691,-17.175268356208,-1.74745124779751));
#38243=CARTESIAN_POINT('Ctrl Pts',(368.141247911939,-17.1769801591818,-1.77037860870688));
#38244=CARTESIAN_POINT('Ctrl Pts',(368.271494725808,-17.1917189099354,-1.96489013794532));
#38245=CARTESIAN_POINT('Ctrl Pts',(368.402759537296,-17.205365686685,-2.12517111702655));
#38246=CARTESIAN_POINT('Ctrl Pts',(368.651990502347,-17.2291920824747,-2.37595113128453));
#38247=CARTESIAN_POINT('Ctrl Pts',(368.762543333597,-17.2391926531057,-2.47294309358282));
#38248=CARTESIAN_POINT('Ctrl Pts',(368.932572722941,-17.2534719468017,-2.60268491932549));
#38249=CARTESIAN_POINT('Ctrl Pts',(368.987074884175,-17.2578984733887,-2.64164680296096));
#38250=CARTESIAN_POINT('Ctrl Pts',(369.065175067175,-17.2639946059058,-2.69387803304517));
#38251=CARTESIAN_POINT('Ctrl Pts',(369.087783503371,-17.2657313259898,-2.70859057811791));
#38252=CARTESIAN_POINT('Ctrl Pts',(369.122693706617,-17.2683673846775,-2.73068966860798));
#38253=CARTESIAN_POINT('Ctrl Pts',(369.134863997648,-17.2692779991825,-2.73828046322356));
#38254=CARTESIAN_POINT('Ctrl Pts',(369.155069719111,-17.2707755590437,-2.75069647539726));
#38255=CARTESIAN_POINT('Ctrl Pts',(369.163076108545,-17.2713652836882,-2.75556825928215));
#38256=CARTESIAN_POINT('Ctrl Pts',(369.178590250877,-17.2725007510968,-2.76491592356747));
#38257=CARTESIAN_POINT('Ctrl Pts',(369.186095176108,-17.2730467745846,-2.7693963184189));
#38258=CARTESIAN_POINT('Ctrl Pts',(369.200112346615,-17.2740604111612,-2.77768732061275));
#38259=CARTESIAN_POINT('Ctrl Pts',(369.206619690619,-17.2745284981946,-2.78150556022892));
#38260=CARTESIAN_POINT('Ctrl Pts',(369.221869653992,-17.2756197465412,-2.79038176201841));
#38261=CARTESIAN_POINT('Ctrl Pts',(369.230622697484,-17.2762417359791,-2.79542151148647));
#38262=CARTESIAN_POINT('Ctrl Pts',(369.253981461589,-17.2778904370138,-2.80872498806493));
#38263=CARTESIAN_POINT('Ctrl Pts',(369.26862849445,-17.2789126976185,-2.81691604923042));
#38264=CARTESIAN_POINT('Ctrl Pts',(369.395504761955,-17.2876744336074,-2.88657371442765));
#38265=CARTESIAN_POINT('Ctrl Pts',(369.511252215524,-17.2950431499279,-2.94142753055836));
#38266=CARTESIAN_POINT('Ctrl Pts',(369.755685715311,-17.3099559672069,-3.0399080259698));
#38267=CARTESIAN_POINT('Ctrl Pts',(369.884475764445,-17.3174721576643,-3.08257839165419));
#38268=CARTESIAN_POINT('Ctrl Pts',(370.180477252832,-17.3346536825963,-3.16032910483207));
#38269=CARTESIAN_POINT('Ctrl Pts',(370.34854102955,-17.3443548904515,-3.19048568180492));
#38270=CARTESIAN_POINT('Ctrl Pts',(370.558603406045,-17.3568949861004,-3.21119108833059));
#38271=CARTESIAN_POINT('Ctrl Pts',(370.599086902747,-17.3593294714796,-3.21441018537751));
#38272=CARTESIAN_POINT('Ctrl Pts',(370.658156874634,-17.3629120748944,-3.21798536042964));
#38273=CARTESIAN_POINT('Ctrl Pts',(370.676703688881,-17.3640412909574,-3.21894706746407));
#38274=CARTESIAN_POINT('Ctrl Pts',(370.70935749729,-17.3660374839419,-3.22035737973027));
#38275=CARTESIAN_POINT('Ctrl Pts',(370.723461178377,-17.3669023192771,-3.22087372173741));
#38276=CARTESIAN_POINT('Ctrl Pts',(370.750976167829,-17.3685948790892,-3.22170012218377));
#38277=CARTESIAN_POINT('Ctrl Pts',(370.764386933254,-17.3694223056793,-3.22201911408936));
#38278=CARTESIAN_POINT('Ctrl Pts',(370.80053399765,-17.371659387394,-3.22265313777134));
#38279=CARTESIAN_POINT('Ctrl Pts',(370.823271955808,-17.3730739144129,-3.22281127912992));
#38280=CARTESIAN_POINT('Ctrl Pts',(370.909124649413,-17.3784434197128,-3.22249982387998));
#38281=CARTESIAN_POINT('Ctrl Pts',(370.972215863131,-17.3824481121993,-3.22041680755756));
#38282=CARTESIAN_POINT('Ctrl Pts',(371.3718192139,-17.4082000183046,-3.19545975670053));
#38283=CARTESIAN_POINT('Ctrl Pts',(371.702956587845,-17.4315913740504,-3.12173925962892));
#38284=CARTESIAN_POINT('Ctrl Pts',(372.060220880805,-17.4569422422504,-2.98085186165981));
#38285=CARTESIAN_POINT('Ctrl Pts',(372.103461516991,-17.4600068931505,-2.96269992769949));
#38286=CARTESIAN_POINT('Ctrl Pts',(372.174593463969,-17.4650251082468,-2.93099622797123));
#38287=CARTESIAN_POINT('Ctrl Pts',(372.202712074826,-17.4670026391745,-2.91797447221289));
#38288=CARTESIAN_POINT('Ctrl Pts',(372.241229225719,-17.4696985532576,-2.89945788155222));
#38289=CARTESIAN_POINT('Ctrl Pts',(372.25179104359,-17.4704364438616,-2.89430913718401));
#38290=CARTESIAN_POINT('Ctrl Pts',(372.269586213686,-17.4716770875192,-2.88551345664637));
#38291=CARTESIAN_POINT('Ctrl Pts',(372.276834344788,-17.4721816789811,-2.88189683224231));
#38292=CARTESIAN_POINT('Ctrl Pts',(372.290686401712,-17.4731445013185,-2.87491967099586));
#38293=CARTESIAN_POINT('Ctrl Pts',(372.297292455,-17.473603017721,-2.87156364736597));
#38294=CARTESIAN_POINT('Ctrl Pts',(372.313080913513,-17.4746974426093,-2.8634741300774));
#38295=CARTESIAN_POINT('Ctrl Pts',(372.32225231543,-17.4753320242106,-2.85871917561391));
#38296=CARTESIAN_POINT('Ctrl Pts',(372.355269753859,-17.477612913445,-2.84139919359176));
#38297=CARTESIAN_POINT('Ctrl Pts',(372.378981538499,-17.4792440896457,-2.82857884255323));
#38298=CARTESIAN_POINT('Ctrl Pts',(372.548405847168,-17.490869591487,-2.73420948188425));
#38299=CARTESIAN_POINT('Ctrl Pts',(372.687764411577,-17.5002813403914,-2.64173211187344));
#38300=CARTESIAN_POINT('Ctrl Pts',(372.942702201732,-17.5184052891386,-2.44240742459958));
#38301=CARTESIAN_POINT('Ctrl Pts',(373.058868420832,-17.5271031772986,-2.33709461935308));
#38302=CARTESIAN_POINT('Ctrl Pts',(373.249167487908,-17.5428664953261,-2.1374817241649));
#38303=CARTESIAN_POINT('Ctrl Pts',(373.326561631098,-17.5498108484044,-2.04671523926428));
#38304=CARTESIAN_POINT('Ctrl Pts',(373.415156990239,-17.5585900845478,-1.93031632678799));
#38305=CARTESIAN_POINT('Ctrl Pts',(373.43129505862,-17.5602264871636,-1.9085494751868));
#38306=CARTESIAN_POINT('Ctrl Pts',(373.456436743717,-17.5628371881133,-1.87372927866225));
#38307=CARTESIAN_POINT('Ctrl Pts',(373.465622017144,-17.5638044562273,-1.86080822990685));
#38308=CARTESIAN_POINT('Ctrl Pts',(373.482731740458,-17.5656321103684,-1.83635974401741));
#38309=CARTESIAN_POINT('Ctrl Pts',(373.490677222235,-17.5664916651961,-1.82484742387543));
#38310=CARTESIAN_POINT('Ctrl Pts',(373.508408103083,-17.5684346188864,-1.79879571891066));
#38311=CARTESIAN_POINT('Ctrl Pts',(373.518150294236,-17.5695196160096,-1.78422759532211));
#38312=CARTESIAN_POINT('Ctrl Pts',(373.542827532757,-17.5723135818269,-1.74666670538541));
#38313=CARTESIAN_POINT('Ctrl Pts',(373.557588625952,-17.5740289455973,-1.72356186068839));
#38314=CARTESIAN_POINT('Ctrl Pts',(373.68123918879,-17.5887860097614,-1.52446286166184));
#38315=CARTESIAN_POINT('Ctrl Pts',(373.773217809876,-17.6024488708771,-1.33857669212179));
#38316=CARTESIAN_POINT('Ctrl Pts',(373.925633105795,-17.6313549520017,-0.937649155496241));
#38317=CARTESIAN_POINT('Ctrl Pts',(373.982875888344,-17.6465623976405,-0.722501540273425));
#38318=CARTESIAN_POINT('Ctrl Pts',(374.022776003527,-17.6630631548155,-0.470079244576507));
#38319=CARTESIAN_POINT('Ctrl Pts',(374.027490475314,-17.6652044765469,-0.436908095776338));
#38320=CARTESIAN_POINT('Ctrl Pts',(374.033203981388,-17.6680837102208,-0.391652616151649));
#38321=CARTESIAN_POINT('Ctrl Pts',(374.034653209938,-17.6688446606219,-0.379628566137522));
#38322=CARTESIAN_POINT('Ctrl Pts',(374.036966895449,-17.6701129014934,-0.35947666703041));
#38323=CARTESIAN_POINT('Ctrl Pts',(374.037868265382,-17.6706222138474,-0.351353273828388));
#38324=CARTESIAN_POINT('Ctrl Pts',(374.039520386064,-17.6715855169474,-0.335928790195689));
#38325=CARTESIAN_POINT('Ctrl Pts',(374.040277113279,-17.6720398496192,-0.328628443722183));
#38326=CARTESIAN_POINT('Ctrl Pts',(374.042011723599,-17.6731135243446,-0.3113177741166));
#38327=CARTESIAN_POINT('Ctrl Pts',(374.042967704247,-17.6737316527555,-0.301305264299879));
#38328=CARTESIAN_POINT('Ctrl Pts',(374.046158364721,-17.6758924354209,-0.266148983439942));
#38329=CARTESIAN_POINT('Ctrl Pts',(374.048144560642,-17.6774219602216,-0.240982855618438));
#38330=CARTESIAN_POINT('Ctrl Pts',(374.064485526612,-17.692076590735,0.00251039764335815));
#38331=CARTESIAN_POINT('Ctrl Pts',(374.056868616474,-17.7041795515152,0.221771927720396));
#38332=CARTESIAN_POINT('Ctrl Pts',(374.006773978729,-17.7247707915569,0.586438806639206));
#38333=CARTESIAN_POINT('Ctrl Pts',(373.976220623224,-17.7331540235787,0.732687411003659));
#38334=CARTESIAN_POINT('Ctrl Pts',(373.920717203207,-17.7449995364376,0.929124077846322));
#38335=CARTESIAN_POINT('Ctrl Pts',(373.904439967954,-17.7482199173833,0.981571301054406));
#38336=CARTESIAN_POINT('Ctrl Pts',(373.873767628938,-17.7539012191369,1.07215758850318));
#38337=CARTESIAN_POINT('Ctrl Pts',(373.859973838216,-17.7563430556571,1.11048749201427));
#38338=CARTESIAN_POINT('Ctrl Pts',(373.838830925856,-17.7599344988351,1.16591788336398));
#38339=CARTESIAN_POINT('Ctrl Pts',(373.8320540067,-17.7610650687459,1.18323338612762));
#38340=CARTESIAN_POINT('Ctrl Pts',(373.81986928966,-17.7630628130109,1.21358949282197));
#38341=CARTESIAN_POINT('Ctrl Pts',(373.814524896591,-17.7639278348604,1.22665512893726));
#38342=CARTESIAN_POINT('Ctrl Pts',(373.803937549914,-17.7656201216009,1.25206077161786));
#38343=CARTESIAN_POINT('Ctrl Pts',(373.798703082882,-17.7664470844208,1.26440401783152));
#38344=CARTESIAN_POINT('Ctrl Pts',(373.784398860316,-17.7686813277719,1.29755729202507));
#38345=CARTESIAN_POINT('Ctrl Pts',(373.775186129058,-17.7700934581313,1.31830444751966));
#38346=CARTESIAN_POINT('Ctrl Pts',(373.739645163729,-17.7754434363473,1.39611612572322));
#38347=CARTESIAN_POINT('Ctrl Pts',(373.711870267672,-17.7794305350366,1.4525006832974));
#38348=CARTESIAN_POINT('Ctrl Pts',(373.52448889745,-17.8051826665246,1.80639845349481));
#38349=CARTESIAN_POINT('Ctrl Pts',(373.320661075031,-17.8285973427458,2.07800650840981));
#38350=CARTESIAN_POINT('Ctrl Pts',(373.044782431174,-17.8539712184178,2.34566911183202));
#38351=CARTESIAN_POINT('Ctrl Pts',(373.010410543838,-17.8570367148681,2.3775908566064));
#38352=CARTESIAN_POINT('Ctrl Pts',(372.95218938131,-17.8620561602466,2.4293410982708));
#38353=CARTESIAN_POINT('Ctrl Pts',(372.928729540129,-17.8640340899359,2.44959544254447));
#38354=CARTESIAN_POINT('Ctrl Pts',(372.895976042751,-17.8667304525125,2.47705897141263));
#38355=CARTESIAN_POINT('Ctrl Pts',(372.886930502134,-17.8674684011147,2.48455971187591));
#38356=CARTESIAN_POINT('Ctrl Pts',(372.871580342513,-17.8687091138961,2.49714731797277));
#38357=CARTESIAN_POINT('Ctrl Pts',(372.865297253062,-17.8692137169407,2.50226015043363));
#38358=CARTESIAN_POINT('Ctrl Pts',(372.853230241241,-17.8701765391318,2.51200422578053));
#38359=CARTESIAN_POINT('Ctrl Pts',(372.847449555383,-17.8706350439528,2.51663926958221));
#38360=CARTESIAN_POINT('Ctrl Pts',(372.833571569182,-17.8717294124365,2.52768843928296));
#38361=CARTESIAN_POINT('Ctrl Pts',(372.82545925588,-17.8723639495244,2.5340836979523));
#38362=CARTESIAN_POINT('Ctrl Pts',(372.796073368577,-17.8746444658048,2.5570215226785));
#38363=CARTESIAN_POINT('Ctrl Pts',(372.774622596909,-17.8762753201882,2.57333662368372));
#38364=CARTESIAN_POINT('Ctrl Pts',(372.612968721112,-17.888336173369,2.69311711966996));
#38365=CARTESIAN_POINT('Ctrl Pts',(372.464767953331,-17.8981305986617,2.78534127973496));
#38366=CARTESIAN_POINT('Ctrl Pts',(372.30982061364,-17.9078850417037,2.86513684952479));
#38367=CARTESIAN_POINT('Origin',(370.834317853224,2.31077344927308,0.));
#38368=CARTESIAN_POINT('',(372.309820886087,-19.4026365087528,2.86513670921869));
#38369=CARTESIAN_POINT('',(372.309820613636,-19.1541342831958,2.86513684952678));
#38370=CARTESIAN_POINT('',(372.309820613641,2.31077344927308,2.86513684952399));
#38371=CARTESIAN_POINT('',(367.611567987131,-18.5635425847965,-0.000929030908117072));
#38372=CARTESIAN_POINT('Ctrl Pts',(372.309820886087,-19.4026365087528,2.86513670921864));
#38373=CARTESIAN_POINT('Ctrl Pts',(372.451012724632,-19.3937337882005,2.79242500044792));
#38374=CARTESIAN_POINT('Ctrl Pts',(372.586752355134,-19.3849172730876,2.70931674540583));
#38375=CARTESIAN_POINT('Ctrl Pts',(372.815210811217,-19.3688610084774,2.54502313882603));
#38376=CARTESIAN_POINT('Ctrl Pts',(372.910361849359,-19.3617482119209,2.46801867475545));
#38377=CARTESIAN_POINT('Ctrl Pts',(373.021643049223,-19.3527361787373,2.36696242610841));
#38378=CARTESIAN_POINT('Ctrl Pts',(373.042138607321,-19.3510455136871,2.34785648676577));
#38379=CARTESIAN_POINT('Ctrl Pts',(373.074094496837,-19.3483587261884,2.31727877877292));
#38380=CARTESIAN_POINT('Ctrl Pts',(373.085722132557,-19.3473702012269,2.30598332774414));
#38381=CARTESIAN_POINT('Ctrl Pts',(373.107191031656,-19.3455243189301,2.2848105989877));
#38382=CARTESIAN_POINT('Ctrl Pts',(373.117054408305,-19.3446679781463,2.27495621252225));
#38383=CARTESIAN_POINT('Ctrl Pts',(373.138807804842,-19.3427606244533,2.25293873228251));
#38384=CARTESIAN_POINT('Ctrl Pts',(373.150666038243,-19.3417082534954,2.24074495124684));
#38385=CARTESIAN_POINT('Ctrl Pts',(373.184952854174,-19.3386279334484,2.20492491418085));
#38386=CARTESIAN_POINT('Ctrl Pts',(373.207119888148,-19.3365888506403,2.18105230629932));
#38387=CARTESIAN_POINT('Ctrl Pts',(373.374045670421,-19.320858601998,1.99572591721334));
#38388=CARTESIAN_POINT('Ctrl Pts',(373.502512692134,-19.3064876522737,1.82039679920618));
#38389=CARTESIAN_POINT('Ctrl Pts',(373.723426328483,-19.2770668591204,1.44469973170487));
#38390=CARTESIAN_POINT('Ctrl Pts',(373.814927445316,-19.2620962467399,1.24502418872069));
#38391=CARTESIAN_POINT('Ctrl Pts',(373.893612733978,-19.2464190764061,1.01364323459907));
#38392=CARTESIAN_POINT('Ctrl Pts',(373.901477011672,-19.244809285654,0.989592119636126));
#38393=CARTESIAN_POINT('Ctrl Pts',(373.912059238191,-19.2425834688701,0.955890125530128));
#38394=CARTESIAN_POINT('Ctrl Pts',(373.915016437398,-19.2419545122697,0.946316122941213));
#38395=CARTESIAN_POINT('Ctrl Pts',(373.920058452308,-19.240870113285,0.929718340331362));
#38396=CARTESIAN_POINT('Ctrl Pts',(373.922164038936,-19.2404134876832,0.922701020433811));
#38397=CARTESIAN_POINT('Ctrl Pts',(373.926568669735,-19.2394503017213,0.907837702013906));
#38398=CARTESIAN_POINT('Ctrl Pts',(373.928861822364,-19.2389440987316,0.899990017253865));
#38399=CARTESIAN_POINT('Ctrl Pts',(373.934486774089,-19.2376902726851,0.880464476330244));
#38400=CARTESIAN_POINT('Ctrl Pts',(373.9377825179,-19.2369447150209,0.868776218601778));
#38401=CARTESIAN_POINT('Ctrl Pts',(373.949995254367,-19.2341388635721,0.824507645660303));
#38402=CARTESIAN_POINT('Ctrl Pts',(373.958466258092,-19.2321026690729,0.791805200823067));
#38403=CARTESIAN_POINT('Ctrl Pts',(374.019849171622,-19.2165686833898,0.538492662821227));
#38404=CARTESIAN_POINT('Ctrl Pts',(374.049853280193,-19.2040927502311,0.312957572843277));
#38405=CARTESIAN_POINT('Ctrl Pts',(374.061302742344,-19.1800861437778,-0.115356820233256));
#38406=CARTESIAN_POINT('Ctrl Pts',(374.047777092144,-19.1686545390522,-0.316865296403728));
#38407=CARTESIAN_POINT('Ctrl Pts',(374.011122748232,-19.1549482976994,-0.542941502003293));
#38408=CARTESIAN_POINT('Ctrl Pts',(374.00637102757,-19.1532910734376,-0.570046843804094));
#38409=CARTESIAN_POINT('Ctrl Pts',(373.998021505317,-19.1505590735351,-0.614332758561281));
#38410=CARTESIAN_POINT('Ctrl Pts',(373.994629364478,-19.14949082033,-0.631551003009051));
#38411=CARTESIAN_POINT('Ctrl Pts',(373.98828245973,-19.1475634457108,-0.662435120398092));
#38412=CARTESIAN_POINT('Ctrl Pts',(373.985379052945,-19.146705982806,-0.6761111844239));
#38413=CARTESIAN_POINT('Ctrl Pts',(373.979001449076,-19.1448723303964,-0.705218280905172));
#38414=CARTESIAN_POINT('Ctrl Pts',(373.975502462,-19.1438953663188,-0.720643449346488));
#38415=CARTESIAN_POINT('Ctrl Pts',(373.965731718371,-19.1412429513149,-0.762293808155959));
#38416=CARTESIAN_POINT('Ctrl Pts',(373.959244249751,-19.1395606184977,-0.788466606828006));
#38417=CARTESIAN_POINT('Ctrl Pts',(373.922779956108,-19.13050262772,-0.928051814776708));
#38418=CARTESIAN_POINT('Ctrl Pts',(373.886959379672,-19.1229398109753,-1.03983293588876));
#38419=CARTESIAN_POINT('Ctrl Pts',(373.754895207958,-19.0985562013961,-1.38576945027254));
#38420=CARTESIAN_POINT('Ctrl Pts',(373.637153655961,-19.0811581811182,-1.61065830930062));
#38421=CARTESIAN_POINT('Ctrl Pts',(373.44450385867,-19.0584512783996,-1.89231031788687));
#38422=CARTESIAN_POINT('Ctrl Pts',(373.39169191851,-19.0526656454684,-1.96309707654296));
#38423=CARTESIAN_POINT('Ctrl Pts',(373.326144741747,-19.0460539147674,-2.04381077121446));
#38424=CARTESIAN_POINT('Ctrl Pts',(373.316165237461,-19.0450617888305,-2.05591762849249));
#38425=CARTESIAN_POINT('Ctrl Pts',(373.299758726256,-19.043454818925,-2.07552799275485));
#38426=CARTESIAN_POINT('Ctrl Pts',(373.293385063146,-19.0428363497616,-2.08307551718272));
#38427=CARTESIAN_POINT('Ctrl Pts',(373.281898610934,-19.0417323109011,-2.09655128159395));
#38428=CARTESIAN_POINT('Ctrl Pts',(373.276798847984,-19.0412458277008,-2.10249029391497));
#38429=CARTESIAN_POINT('Ctrl Pts',(373.265563755886,-19.0401821437575,-2.11547825488287));
#38430=CARTESIAN_POINT('Ctrl Pts',(373.259419392365,-19.0396056198209,-2.12251912031126));
#38431=CARTESIAN_POINT('Ctrl Pts',(373.241676882191,-19.0379553595244,-2.14267275191081));
#38432=CARTESIAN_POINT('Ctrl Pts',(373.230002200027,-19.0368871168533,-2.15571810726184));
#38433=CARTESIAN_POINT('Ctrl Pts',(373.143088779976,-19.0290577347666,-2.25125749716476));
#38434=CARTESIAN_POINT('Ctrl Pts',(373.063706306622,-19.0225792061031,-2.32989615295844));
#38435=CARTESIAN_POINT('Ctrl Pts',(372.808883642388,-19.0031350986898,-2.55735412958696));
#38436=CARTESIAN_POINT('Ctrl Pts',(372.621485887732,-18.9905755990178,-2.69165490894473));
#38437=CARTESIAN_POINT('Ctrl Pts',(372.321198736284,-18.970837643492,-2.86156501591225));
#38438=CARTESIAN_POINT('Ctrl Pts',(372.218053772718,-18.9641281173776,-2.91284051630096));
#38439=CARTESIAN_POINT('Ctrl Pts',(372.087115555339,-18.9555733123906,-2.96940629667062));
#38440=CARTESIAN_POINT('Ctrl Pts',(372.061698465615,-18.9539112481575,-2.98000211379355));
#38441=CARTESIAN_POINT('Ctrl Pts',(372.02120966583,-18.9512599228766,-2.99627512649834));
#38442=CARTESIAN_POINT('Ctrl Pts',(372.006225461719,-18.9502779229291,-3.00216744219175));
#38443=CARTESIAN_POINT('Ctrl Pts',(371.978177691622,-18.9484380422996,-3.01295483478988));
#38444=CARTESIAN_POINT('Ctrl Pts',(371.965125229587,-18.9475811235609,-3.01787786933896));
#38445=CARTESIAN_POINT('Ctrl Pts',(371.935958556905,-18.9456645265899,-3.02866296352277));
#38446=CARTESIAN_POINT('Ctrl Pts',(371.919828785115,-18.9446034248848,-3.03448143595878));
#38447=CARTESIAN_POINT('Ctrl Pts',(371.872285082879,-18.9414718888481,-3.05120423971157));
#38448=CARTESIAN_POINT('Ctrl Pts',(371.840748675907,-18.9393897481342,-3.06175115716176));
#38449=CARTESIAN_POINT('Ctrl Pts',(371.768692498686,-18.9346196367783,-3.08461582866832));
#38450=CARTESIAN_POINT('Ctrl Pts',(371.728082439077,-18.9319221939621,-3.09662645229191));
#38451=CARTESIAN_POINT('Ctrl Pts',(371.59157180186,-18.9228230751304,-3.1340911978803));
#38452=CARTESIAN_POINT('Ctrl Pts',(371.494741135868,-18.916315005331,-3.1559149669713));
#38453=CARTESIAN_POINT('Ctrl Pts',(371.21833626417,-18.8976325265469,-3.20493309143997));
#38454=CARTESIAN_POINT('Ctrl Pts',(371.037252906775,-18.8852520378186,-3.22147140152816));
#38455=CARTESIAN_POINT('Ctrl Pts',(370.733215797561,-18.8648209650685,-3.22349381551713));
#38456=CARTESIAN_POINT('Ctrl Pts',(370.61071602129,-18.8566933440213,-3.21731918924799));
#38457=CARTESIAN_POINT('Ctrl Pts',(370.472258998816,-18.8478264833585,-3.20239122272093));
#38458=CARTESIAN_POINT('Ctrl Pts',(370.455677750087,-18.846769915271,-3.20047306770233));
#38459=CARTESIAN_POINT('Ctrl Pts',(370.429117818178,-18.8450868107117,-3.19719125135016));
#38460=CARTESIAN_POINT('Ctrl Pts',(370.419129569491,-18.8444559706803,-3.19590952024229));
#38461=CARTESIAN_POINT('Ctrl Pts',(370.401359706475,-18.8433376245148,-3.19354450839424));
#38462=CARTESIAN_POINT('Ctrl Pts',(370.393575852172,-18.8428491144423,-3.19247956566053));
#38463=CARTESIAN_POINT('Ctrl Pts',(370.376802560894,-18.8417994218955,-3.19012222243118));
#38464=CARTESIAN_POINT('Ctrl Pts',(370.367814661835,-18.8412387777074,-3.18882028561105));
#38465=CARTESIAN_POINT('Ctrl Pts',(370.342733350662,-18.8396790742257,-3.18507883441596));
#38466=CARTESIAN_POINT('Ctrl Pts',(370.32665248204,-18.8386846082506,-3.18255532566717));
#38467=CARTESIAN_POINT('Ctrl Pts',(370.229873136762,-18.8327292903931,-3.16661590043902));
#38468=CARTESIAN_POINT('Ctrl Pts',(370.14968326247,-18.8279190792379,-3.15025198162497));
#38469=CARTESIAN_POINT('Ctrl Pts',(369.845512685463,-18.8098557518665,-3.07601556310163));
#38470=CARTESIAN_POINT('Ctrl Pts',(369.627374552892,-18.7972409607748,-2.99715007174537));
#38471=CARTESIAN_POINT('Ctrl Pts',(369.291045897363,-18.7760218895102,-2.83282257705658));
#38472=CARTESIAN_POINT('Ctrl Pts',(369.166880637706,-18.7677595215318,-2.76156080301757));
#38473=CARTESIAN_POINT('Ctrl Pts',(369.025851502575,-18.7576093992297,-2.6676331572469));
#38474=CARTESIAN_POINT('Ctrl Pts',(369.004018422764,-18.7560153103336,-2.6527007247544));
#38475=CARTESIAN_POINT('Ctrl Pts',(368.9682753094,-18.7533664469392,-2.62760337206058));
#38476=CARTESIAN_POINT('Ctrl Pts',(368.954258317529,-18.7523175272013,-2.61759247793402));
#38477=CARTESIAN_POINT('Ctrl Pts',(368.929308441917,-18.7504318771016,-2.59946956482081));
#38478=CARTESIAN_POINT('Ctrl Pts',(368.918345362037,-18.7495967877095,-2.59139967577723));
#38479=CARTESIAN_POINT('Ctrl Pts',(368.906962012131,-18.7487227603054,-2.58290870354206));
#38480=CARTESIAN_POINT('Ctrl Pts',(368.906490250812,-18.7486865254295,-2.58255661010685));
#38481=CARTESIAN_POINT('Ctrl Pts',(368.905613988974,-18.7486191986383,-2.58190224863651));
#38482=CARTESIAN_POINT('Ctrl Pts',(368.905209462892,-18.7485881080562,-2.58160001468823));
#38483=CARTESIAN_POINT('Ctrl Pts',(368.9044546884,-18.7485300813512,-2.58103582285306));
#38484=CARTESIAN_POINT('Ctrl Pts',(368.904104422185,-18.7485031461553,-2.58077388866856));
#38485=CARTESIAN_POINT('Ctrl Pts',(368.903448392035,-18.7484526850307,-2.58028309148791));
#38486=CARTESIAN_POINT('Ctrl Pts',(368.903142615232,-18.7484291597506,-2.58005424527035));
#38487=CARTESIAN_POINT('Ctrl Pts',(368.902568042002,-18.7483849444246,-2.57962406992362));
#38488=CARTESIAN_POINT('Ctrl Pts',(368.9022992368,-18.7483642548975,-2.57942275346145));
#38489=CARTESIAN_POINT('Ctrl Pts',(368.901792714676,-18.748325260987,-2.57904327990657));
#38490=CARTESIAN_POINT('Ctrl Pts',(368.90155499064,-18.7483069569418,-2.57886513175161));
#38491=CARTESIAN_POINT('Ctrl Pts',(368.901105939673,-18.7482723753281,-2.57852852021724));
#38492=CARTESIAN_POINT('Ctrl Pts',(368.900894607248,-18.7482560980041,-2.57837006346816));
#38493=CARTESIAN_POINT('Ctrl Pts',(368.900494552842,-18.7482252800931,-2.57807002640754));
#38494=CARTESIAN_POINT('Ctrl Pts',(368.900305826744,-18.7482107396987,-2.57792845121671));
#38495=CARTESIAN_POINT('Ctrl Pts',(368.899947889935,-18.7481831586558,-2.57765987911257));
#38496=CARTESIAN_POINT('Ctrl Pts',(368.899778676684,-18.7481701182055,-2.57753288663675));
#38497=CARTESIAN_POINT('Ctrl Pts',(368.899457211003,-18.7481453413187,-2.5772915810855));
#38498=CARTESIAN_POINT('Ctrl Pts',(368.899304956129,-18.7481336050015,-2.57717727112944));
#38499=CARTESIAN_POINT('Ctrl Pts',(368.89901527509,-18.7481112729191,-2.57695974417649));
#38500=CARTESIAN_POINT('Ctrl Pts',(368.898877847376,-18.7481006772771,-2.57685652992174));
#38501=CARTESIAN_POINT('Ctrl Pts',(368.898616029925,-18.7480804891817,-2.57665986074643));
#38502=CARTESIAN_POINT('Ctrl Pts',(368.898491637807,-18.7480708967376,-2.57656640714193));
#38503=CARTESIAN_POINT('Ctrl Pts',(368.898108635053,-18.7480413589492,-2.57627862053249));
#38504=CARTESIAN_POINT('Ctrl Pts',(368.897850047608,-18.7480214124823,-2.57608425812408));
#38505=CARTESIAN_POINT('Ctrl Pts',(368.89733741382,-18.7479818623205,-2.57569882573889));
#38506=CARTESIAN_POINT('Ctrl Pts',(368.897083366226,-18.7479622586594,-2.57550775691557));
#38507=CARTESIAN_POINT('Ctrl Pts',(368.896579405829,-18.747923363138,-2.5751286122862));
#38508=CARTESIAN_POINT('Ctrl Pts',(368.896329492229,-18.7479040713328,-2.5749405377555));
#38509=CARTESIAN_POINT('Ctrl Pts',(368.895833420362,-18.7478657705733,-2.57456710167071));
#38510=CARTESIAN_POINT('Ctrl Pts',(368.895587261517,-18.7478467616786,-2.57438174135701));
#38511=CARTESIAN_POINT('Ctrl Pts',(368.88109967745,-18.7467277978641,-2.56346917505674));
#38512=CARTESIAN_POINT('Ctrl Pts',(368.866947726395,-18.7456232277403,-2.55262418252919));
#38513=CARTESIAN_POINT('Ctrl Pts',(368.83742363808,-18.7432941879183,-2.52960777178642));
#38514=CARTESIAN_POINT('Ctrl Pts',(368.822071171902,-18.7420687941547,-2.51741241193527));
#38515=CARTESIAN_POINT('Ctrl Pts',(368.781567216631,-18.7387972120977,-2.48463050636741));
#38516=CARTESIAN_POINT('Ctrl Pts',(368.756614762325,-18.7367414637005,-2.46380268530472));
#38517=CARTESIAN_POINT('Ctrl Pts',(368.61527695233,-18.724860872279,-2.3421539067914));
#38518=CARTESIAN_POINT('Ctrl Pts',(368.505935845111,-18.7147194559581,-2.23348462200715));
#38519=CARTESIAN_POINT('Ctrl Pts',(368.30260347148,-18.6939576492595,-2.00018232824538));
#38520=CARTESIAN_POINT('Ctrl Pts',(368.209040508131,-18.6833611218842,-1.87569309738877));
#38521=CARTESIAN_POINT('Ctrl Pts',(368.09206976599,-18.6688697463246,-1.69406445937904));
#38522=CARTESIAN_POINT('Ctrl Pts',(368.060744999295,-18.6648401083185,-1.64227684914999));
#38523=CARTESIAN_POINT('Ctrl Pts',(368.001643120891,-18.6569691725492,-1.53804698891253));
#38524=CARTESIAN_POINT('Ctrl Pts',(367.973817935267,-18.6531271520189,-1.48565672741149));
#38525=CARTESIAN_POINT('Ctrl Pts',(367.940584569664,-18.648384611323,-1.41868389269732));
#38526=CARTESIAN_POINT('Ctrl Pts',(367.93381589388,-18.6474099657379,-1.40479347587154));
#38527=CARTESIAN_POINT('Ctrl Pts',(367.923305677577,-18.6458832307948,-1.38282497376202));
#38528=CARTESIAN_POINT('Ctrl Pts',(367.919497357666,-18.645327177658,-1.37477935611536));
#38529=CARTESIAN_POINT('Ctrl Pts',(367.912375506448,-18.6442820383655,-1.35957080279077));
#38530=CARTESIAN_POINT('Ctrl Pts',(367.909054980676,-18.6437925478035,-1.35241153994755));
#38531=CARTESIAN_POINT('Ctrl Pts',(367.90135947377,-18.6426528381987,-1.33565859392353));
#38532=CARTESIAN_POINT('Ctrl Pts',(367.897005239223,-18.642003887901,-1.32605556068822));
#38533=CARTESIAN_POINT('Ctrl Pts',(367.883044313809,-18.639909234041,-1.29485929749686));
#38534=CARTESIAN_POINT('Ctrl Pts',(367.873627746383,-18.638474570192,-1.27318116163881));
#38535=CARTESIAN_POINT('Ctrl Pts',(367.824298493661,-18.6308284758156,-1.15611126230261));
#38536=CARTESIAN_POINT('Ctrl Pts',(367.788752120352,-18.6248410324956,-1.05893498910157));
#38537=CARTESIAN_POINT('Ctrl Pts',(367.716819209143,-18.6111043507131,-0.828471602173698));
#38538=CARTESIAN_POINT('Ctrl Pts',(367.684204119844,-18.603446239682,-0.694225362277117));
#38539=CARTESIAN_POINT('Ctrl Pts',(367.627921477791,-18.5852416036501,-0.374248736269292));
#38540=CARTESIAN_POINT('Ctrl Pts',(367.611621845575,-18.5746522845756,-0.187760588864271));
#38541=CARTESIAN_POINT('Ctrl Pts',(367.611567987131,-18.5635425847965,-0.000929030908117072));
#38542=CARTESIAN_POINT('Ctrl Pts',(367.611567986386,-18.5635424308017,-0.000926441180962114));
#38543=CARTESIAN_POINT('Ctrl Pts',(367.611561433042,-18.5621868546136,0.0218702425262871));
#38544=CARTESIAN_POINT('Ctrl Pts',(367.611796764245,-18.5608243144971,0.0446660322138806));
#38545=CARTESIAN_POINT('Ctrl Pts',(367.61269974216,-18.5582319726971,0.0877961717655694));
#38546=CARTESIAN_POINT('Ctrl Pts',(367.613318130634,-18.557003728493,0.108130382418844));
#38547=CARTESIAN_POINT('Ctrl Pts',(367.614679704908,-18.5549312730263,0.142262623923747));
#38548=CARTESIAN_POINT('Ctrl Pts',(367.615319194447,-18.5540902943665,0.156064364308312));
#38549=CARTESIAN_POINT('Ctrl Pts',(367.61675120443,-18.5524310824112,0.183195869062681));
#38550=CARTESIAN_POINT('Ctrl Pts',(367.617537861165,-18.5516130484395,0.196525672863026));
#38551=CARTESIAN_POINT('Ctrl Pts',(367.619385569006,-18.5498691035744,0.224841430668591));
#38552=CARTESIAN_POINT('Ctrl Pts',(367.620468613133,-18.5489425221585,0.239825584186962));
#38553=CARTESIAN_POINT('Ctrl Pts',(367.623500696627,-18.5465687318471,0.278055582785385));
#38554=CARTESIAN_POINT('Ctrl Pts',(367.625597407924,-18.5451169289521,0.301288529800636));
#38555=CARTESIAN_POINT('Ctrl Pts',(367.634766644662,-18.5394181927076,0.391890462042314));
#38556=CARTESIAN_POINT('Ctrl Pts',(367.643709849647,-18.535113288941,0.459048509102686));
#38557=CARTESIAN_POINT('Ctrl Pts',(367.702634207896,-18.5118308696448,0.815320799879443));
#38558=CARTESIAN_POINT('Ctrl Pts',(367.789806455443,-18.4916843078721,1.096852948199));
#38559=CARTESIAN_POINT('Ctrl Pts',(367.943811114952,-18.4673246458672,1.42692731569131));
#38560=CARTESIAN_POINT('Ctrl Pts',(367.97592467792,-18.4626269686303,1.49021490732091));
#38561=CARTESIAN_POINT('Ctrl Pts',(368.023604689163,-18.4561974305674,1.57695742094196));
#38562=CARTESIAN_POINT('Ctrl Pts',(368.037426676502,-18.454390931036,1.60134414030576));
#38563=CARTESIAN_POINT('Ctrl Pts',(368.062136589854,-18.4512633521572,1.64364467950337));
#38564=CARTESIAN_POINT('Ctrl Pts',(368.072884228646,-18.449934882808,1.66163810144827));
#38565=CARTESIAN_POINT('Ctrl Pts',(368.089041425074,-18.4479856094687,1.68809827325241));
#38566=CARTESIAN_POINT('Ctrl Pts',(368.094316023043,-18.4473565693565,1.69664622832731));
#38567=CARTESIAN_POINT('Ctrl Pts',(368.1037781462,-18.4462412448989,1.71182122852219));
#38568=CARTESIAN_POINT('Ctrl Pts',(368.107949970904,-18.4457539646683,1.71845779250366));
#38569=CARTESIAN_POINT('Ctrl Pts',(368.117079464797,-18.4446972959236,1.73286411596574));
#38570=CARTESIAN_POINT('Ctrl Pts',(368.122046262031,-18.4441285174633,1.7406278535319));
#38571=CARTESIAN_POINT('Ctrl Pts',(368.135965458597,-18.4425510721127,1.76218109323868));
#38572=CARTESIAN_POINT('Ctrl Pts',(368.144990314941,-18.4415470612145,1.7759237790307));
#38573=CARTESIAN_POINT('Ctrl Pts',(368.195802701521,-18.4359938776332,1.85202316421997));
#38574=CARTESIAN_POINT('Ctrl Pts',(368.23965709356,-18.4315699553687,1.91297920298884));
#38575=CARTESIAN_POINT('Ctrl Pts',(368.401466650583,-18.416271043705,2.12207277266602));
#38576=CARTESIAN_POINT('Ctrl Pts',(368.530303687065,-18.4058363291721,2.26130186850869));
#38577=CARTESIAN_POINT('Ctrl Pts',(368.76506159713,-18.3880595930074,2.47397106897141));
#38578=CARTESIAN_POINT('Ctrl Pts',(368.864481723045,-18.3808423235635,2.55383952574365));
#38579=CARTESIAN_POINT('Ctrl Pts',(369.008987276482,-18.3705178542385,2.65645788274047));
#38580=CARTESIAN_POINT('Ctrl Pts',(369.050273954255,-18.3675862744025,2.68435973652801));
#38581=CARTESIAN_POINT('Ctrl Pts',(369.114335635373,-18.3630536493607,2.72552227684239));
#38582=CARTESIAN_POINT('Ctrl Pts',(369.136654906391,-18.361477398524,2.73948005466697));
#38583=CARTESIAN_POINT('Ctrl Pts',(369.178400984181,-18.3585329351248,2.76488066665537));
#38584=CARTESIAN_POINT('Ctrl Pts',(369.197781820261,-18.3571674309792,2.77639614451246));
#38585=CARTESIAN_POINT('Ctrl Pts',(369.229977469707,-18.3549006999941,2.79507154085188));
#38586=CARTESIAN_POINT('Ctrl Pts',(369.242723427475,-18.3540037472758,2.8023490427497));
#38587=CARTESIAN_POINT('Ctrl Pts',(369.267507338053,-18.3522602727361,2.81627617472115));
#38588=CARTESIAN_POINT('Ctrl Pts',(369.279539035871,-18.3514141529309,2.82293632633563));
#38589=CARTESIAN_POINT('Ctrl Pts',(369.307936984545,-18.3494175477101,2.83841940127925));
#38590=CARTESIAN_POINT('Ctrl Pts',(369.32433755661,-18.3482648086236,2.84717802998766));
#38591=CARTESIAN_POINT('Ctrl Pts',(369.377943257472,-18.344497671982,2.87521240007685));
#38592=CARTESIAN_POINT('Ctrl Pts',(369.415447475562,-18.3418629653338,2.89390391937879));
#38593=CARTESIAN_POINT('Ctrl Pts',(369.632398845651,-18.3266205429553,2.9967979491953));
#38594=CARTESIAN_POINT('Ctrl Pts',(369.818919170711,-18.3134720320422,3.06502033581282));
#38595=CARTESIAN_POINT('Ctrl Pts',(370.173215382734,-18.2887448091165,3.15870080076113));
#38596=CARTESIAN_POINT('Ctrl Pts',(370.33906170517,-18.277275715564,3.18891391318488));
#38597=CARTESIAN_POINT('Ctrl Pts',(370.553584288714,-18.2630369163046,3.21084803578277));
#38598=CARTESIAN_POINT('Ctrl Pts',(370.600758455413,-18.2599434255684,3.21462391396209));
#38599=CARTESIAN_POINT('Ctrl Pts',(370.679137643247,-18.2548835773616,3.21916284300575));
#38600=CARTESIAN_POINT('Ctrl Pts',(370.710300239197,-18.2528927647022,3.22051395074741));
#38601=CARTESIAN_POINT('Ctrl Pts',(370.753248562283,-18.2501822523067,3.22175169337876));
#38602=CARTESIAN_POINT('Ctrl Pts',(370.765020262515,-18.2494427652063,3.22202638998329));
#38603=CARTESIAN_POINT('Ctrl Pts',(370.784892882518,-18.2482004856959,3.22238116259231));
#38604=CARTESIAN_POINT('Ctrl Pts',(370.792993010989,-18.247695840565,3.22249522066432));
#38605=CARTESIAN_POINT('Ctrl Pts',(370.808489848256,-18.2467337532987,3.22265499026134));
#38606=CARTESIAN_POINT('Ctrl Pts',(370.815886377183,-18.2462760205163,3.22270578169746));
#38607=CARTESIAN_POINT('Ctrl Pts',(370.833577585122,-18.2451845671903,3.22276635704575));
#38608=CARTESIAN_POINT('Ctrl Pts',(370.843872339146,-18.2445521597513,3.22275228005189));
#38609=CARTESIAN_POINT('Ctrl Pts',(370.880897287609,-18.2422869478081,3.22252423631014));
#38610=CARTESIAN_POINT('Ctrl Pts',(370.907625469464,-18.2406690065501,3.22202703215624));
#38611=CARTESIAN_POINT('Ctrl Pts',(371.12069639972,-18.2278873277165,3.21541056377437));
#38612=CARTESIAN_POINT('Ctrl Pts',(371.306218928516,-18.217454329542,3.19346284536564));
#38613=CARTESIAN_POINT('Ctrl Pts',(371.656424393001,-18.1974514474449,3.12082644107492));
#38614=CARTESIAN_POINT('Ctrl Pts',(371.820985622986,-18.1879091679197,3.07276729050772));
#38615=CARTESIAN_POINT('Ctrl Pts',(372.036481249505,-18.1745712257921,2.99072772526386));
#38616=CARTESIAN_POINT('Ctrl Pts',(372.091421869898,-18.1710951728397,2.96805290603718));
#38617=CARTESIAN_POINT('Ctrl Pts',(372.185238398458,-18.1650044255871,2.92626118903604));
#38618=CARTESIAN_POINT('Ctrl Pts',(372.224414434892,-18.162412947782,2.90785523919848));
#38619=CARTESIAN_POINT('Ctrl Pts',(372.278808144101,-18.1587413231323,2.88094920614493));
#38620=CARTESIAN_POINT('Ctrl Pts',(372.294346657032,-18.1576839085395,2.87310570647248));
#38621=CARTESIAN_POINT('Ctrl Pts',(372.309820613645,-18.1566220988445,2.86513684952223));
#38622=CARTESIAN_POINT('Ctrl Pts',(372.30982061364,-17.9078850417037,2.86513684952479));
#38623=CARTESIAN_POINT('Ctrl Pts',(372.309665113799,-17.9078948309285,2.86521692962436));
#38624=CARTESIAN_POINT('Ctrl Pts',(372.309509607163,-17.9079046201015,2.86529699720688));
#38625=CARTESIAN_POINT('Ctrl Pts',(372.149417046826,-17.9179819848434,2.94770930247267));
#38626=CARTESIAN_POINT('Ctrl Pts',(371.982871800774,-17.9279809453626,3.01650382468275));
#38627=CARTESIAN_POINT('Ctrl Pts',(371.753260760495,-17.9419028595915,3.08956185831615));
#38628=CARTESIAN_POINT('Ctrl Pts',(371.694542374156,-17.9454722331597,3.10642264911262));
#38629=CARTESIAN_POINT('Ctrl Pts',(371.592564343319,-17.9517121204166,3.13259221355794));
#38630=CARTESIAN_POINT('Ctrl Pts',(371.549526047059,-17.9543578076374,3.14269767417157));
#38631=CARTESIAN_POINT('Ctrl Pts',(371.487509907703,-17.9581935631353,3.15591929908358));
#38632=CARTESIAN_POINT('Ctrl Pts',(371.468689690302,-17.9593606681352,3.1597561345731));
#38633=CARTESIAN_POINT('Ctrl Pts',(371.435886103649,-17.9614007117614,3.16613884521319));
#38634=CARTESIAN_POINT('Ctrl Pts',(371.421917974562,-17.9622712005717,3.16876089888251));
#38635=CARTESIAN_POINT('Ctrl Pts',(371.39313609342,-17.9640688050595,3.17396689533857));
#38636=CARTESIAN_POINT('Ctrl Pts',(371.378320707143,-17.964996250804,3.17653971500232));
#38637=CARTESIAN_POINT('Ctrl Pts',(371.340448066994,-17.9673727748034,3.18284390426041));
#38638=CARTESIAN_POINT('Ctrl Pts',(371.317367569864,-17.9688264610973,3.18642841396283));
#38639=CARTESIAN_POINT('Ctrl Pts',(371.227210481178,-17.9745268940078,3.19942819398872));
#38640=CARTESIAN_POINT('Ctrl Pts',(371.159886665819,-17.9788315789448,3.20697820851767));
#38641=CARTESIAN_POINT('Ctrl Pts',(370.815643716397,-18.001098327878,3.23463218450161));
#38642=CARTESIAN_POINT('Ctrl Pts',(370.537223214437,-18.020088317223,3.22100630659121));
#38643=CARTESIAN_POINT('Ctrl Pts',(370.146169707613,-18.046764492343,3.15070108530287));
#38644=CARTESIAN_POINT('Ctrl Pts',(370.029537896644,-18.0546979102241,3.12294743593051));
#38645=CARTESIAN_POINT('Ctrl Pts',(369.897695638997,-18.0634488910075,3.08369447031538));
#38646=CARTESIAN_POINT('Ctrl Pts',(369.880721713374,-18.0645712465194,3.07848780958138));
#38647=CARTESIAN_POINT('Ctrl Pts',(369.85482649867,-18.0662760110946,3.07030985909656));
#38648=CARTESIAN_POINT('Ctrl Pts',(369.845874053369,-18.0668640028922,3.06743945405717));
#38649=CARTESIAN_POINT('Ctrl Pts',(369.829487334403,-18.0679375815943,3.06210622289666));
#38650=CARTESIAN_POINT('Ctrl Pts',(369.822049468652,-18.0684238373718,3.05965547275575));
#38651=CARTESIAN_POINT('Ctrl Pts',(369.805297842416,-18.0695166868434,3.0540680997207));
#38652=CARTESIAN_POINT('Ctrl Pts',(369.795989460649,-18.070122363661,3.05091597647042));
#38653=CARTESIAN_POINT('Ctrl Pts',(369.772030001172,-18.0716776090082,3.04268016254921));
#38654=CARTESIAN_POINT('Ctrl Pts',(369.757400747259,-18.0726235924178,3.0375331472809));
#38655=CARTESIAN_POINT('Ctrl Pts',(369.662971002363,-18.0787097385326,3.00354192872578));
#38656=CARTESIAN_POINT('Ctrl Pts',(369.58429179907,-18.0836880693738,2.97165863517123));
#38657=CARTESIAN_POINT('Ctrl Pts',(369.301497498598,-18.101553134999,2.84383836348255));
#38658=CARTESIAN_POINT('Ctrl Pts',(369.106343100387,-18.1138663872354,2.72966475108411));
#38659=CARTESIAN_POINT('Ctrl Pts',(368.846833302129,-18.1321226613698,2.53877252164653));
#38660=CARTESIAN_POINT('Ctrl Pts',(368.771591027677,-18.1376693027145,2.47802678712066));
#38661=CARTESIAN_POINT('Ctrl Pts',(368.66801894127,-18.1457782277218,2.38641969792796));
#38662=CARTESIAN_POINT('Ctrl Pts',(368.637380281222,-18.1482405403667,2.35824405694403));
#38663=CARTESIAN_POINT('Ctrl Pts',(368.583582762035,-18.1526868667367,2.30681283219935));
#38664=CARTESIAN_POINT('Ctrl Pts',(368.560216953395,-18.1546614824959,2.28378170403739));
#38665=CARTESIAN_POINT('Ctrl Pts',(368.525238962124,-18.1576868485972,2.24823562316858));
#38666=CARTESIAN_POINT('Ctrl Pts',(368.51336744887,-18.1587261971525,2.23597807361711));
#38667=CARTESIAN_POINT('Ctrl Pts',(368.491965269601,-18.1606232678165,2.21352584863382));
#38668=CARTESIAN_POINT('Ctrl Pts',(368.482402358576,-18.1614795652237,2.20336238619958));
#38669=CARTESIAN_POINT('Ctrl Pts',(368.461889109813,-18.1633353932994,2.18127519986581));
#38670=CARTESIAN_POINT('Ctrl Pts',(368.450962043675,-18.1643358817287,2.16933047503538));
#38671=CARTESIAN_POINT('Ctrl Pts',(368.421455852697,-18.1670705190176,2.1365842831454));
#38672=CARTESIAN_POINT('Ctrl Pts',(368.403056359257,-18.1688121087645,2.11562352556677));
#38673=CARTESIAN_POINT('Ctrl Pts',(368.306814269867,-18.1781198292555,2.00307053172437));
#38674=CARTESIAN_POINT('Ctrl Pts',(368.233878107522,-18.1858820255865,1.90742579353446));
#38675=CARTESIAN_POINT('Ctrl Pts',(368.038700649009,-18.2088312948118,1.6194154133175));
#38676=CARTESIAN_POINT('Ctrl Pts',(367.931289971958,-18.2244287289647,1.41788424658226));
#38677=CARTESIAN_POINT('Ctrl Pts',(367.818581118882,-18.2445786758436,1.13878095402693));
#38678=CARTESIAN_POINT('Ctrl Pts',(367.793459975509,-18.2494373953493,1.06989477207599));
#38679=CARTESIAN_POINT('Ctrl Pts',(367.757477377276,-18.2569732341094,0.959681058240468));
#38680=CARTESIAN_POINT('Ctrl Pts',(367.74505088434,-18.2597116941447,0.91889338381017));
#38681=CARTESIAN_POINT('Ctrl Pts',(367.729827255088,-18.263245777266,0.865119224278525));
#38682=CARTESIAN_POINT('Ctrl Pts',(367.726296365582,-18.264079579731,0.852347108118338));
#38683=CARTESIAN_POINT('Ctrl Pts',(367.720651109441,-18.2654358849767,0.831425190664511));
#38684=CARTESIAN_POINT('Ctrl Pts',(367.718489765131,-18.2659610186009,0.823288387078938));
#38685=CARTESIAN_POINT('Ctrl Pts',(367.714333907342,-18.2669822266133,0.807392051567859));
#38686=CARTESIAN_POINT('Ctrl Pts',(367.712336411367,-18.267478460698,0.799633432242072));
#38687=CARTESIAN_POINT('Ctrl Pts',(367.70749135303,-18.2686957545412,0.780519474099676));
#38688=CARTESIAN_POINT('Ctrl Pts',(367.704676656848,-18.2694149447895,0.769155773254699));
#38689=CARTESIAN_POINT('Ctrl Pts',(367.696714052944,-18.2714856751083,0.736241051033128));
#38690=CARTESIAN_POINT('Ctrl Pts',(367.691726280864,-18.2728285961033,0.714651497305161));
#38691=CARTESIAN_POINT('Ctrl Pts',(367.637064029954,-18.2881130404458,0.466399380181343));
#38692=CARTESIAN_POINT('Ctrl Pts',(367.611779436814,-18.3008908155179,0.23502725988353));
#38693=CARTESIAN_POINT('Ctrl Pts',(367.611379681676,-18.3255973486856,-0.20626324314669));
#38694=CARTESIAN_POINT('Ctrl Pts',(367.631555742899,-18.337433932554,-0.414938720819074));
#38695=CARTESIAN_POINT('Ctrl Pts',(367.677080944046,-18.3515927856995,-0.647089576842867));
#38696=CARTESIAN_POINT('Ctrl Pts',(367.682702210047,-18.3532446356701,-0.673935151891065));
#38697=CARTESIAN_POINT('Ctrl Pts',(367.692476436401,-18.3559699765553,-0.717814267250105));
#38698=CARTESIAN_POINT('Ctrl Pts',(367.69642702409,-18.357037006491,-0.734891785432829));
#38699=CARTESIAN_POINT('Ctrl Pts',(367.703780437963,-18.3589636254771,-0.765538194276729));
#38700=CARTESIAN_POINT('Ctrl Pts',(367.707132691253,-18.3598215695404,-0.779118853732655));
#38701=CARTESIAN_POINT('Ctrl Pts',(367.714472005468,-18.3616578356588,-0.808041278383915));
#38702=CARTESIAN_POINT('Ctrl Pts',(367.718484043535,-18.3626369449096,-0.823376267203227));
#38703=CARTESIAN_POINT('Ctrl Pts',(367.729658053295,-18.3652992007026,-0.864834548370007));
#38704=CARTESIAN_POINT('Ctrl Pts',(367.737036386613,-18.3669893090864,-0.890897701181946));
#38705=CARTESIAN_POINT('Ctrl Pts',(367.77861296461,-18.3761657200652,-1.03099913954588));
#38706=CARTESIAN_POINT('Ctrl Pts',(367.818778224723,-18.3838450610775,-1.1431564164714));
#38707=CARTESIAN_POINT('Ctrl Pts',(367.92576857589,-18.4019802522657,-1.39672974376027));
#38708=CARTESIAN_POINT('Ctrl Pts',(367.996863543076,-18.4125367849318,-1.53602052723518));
#38709=CARTESIAN_POINT('Ctrl Pts',(368.164581427382,-18.4344365281345,-1.81292713735376));
#38710=CARTESIAN_POINT('Ctrl Pts',(368.262449119488,-18.4457477161982,-1.94928172049029));
#38711=CARTESIAN_POINT('Ctrl Pts',(368.387856699903,-18.4582471133576,-2.09801608158198));
#38712=CARTESIAN_POINT('Ctrl Pts',(368.405484750028,-18.4599635201717,-2.11839881049245));
#38713=CARTESIAN_POINT('Ctrl Pts',(368.43022149595,-18.4623138789628,-2.14628631961244));
#38714=CARTESIAN_POINT('Ctrl Pts',(368.437113180321,-18.4629625962881,-2.15398097109664));
#38715=CARTESIAN_POINT('Ctrl Pts',(368.449011575299,-18.4640719807624,-2.16713784060525));
#38716=CARTESIAN_POINT('Ctrl Pts',(368.454000295682,-18.4645339561658,-2.17261611601515));
#38717=CARTESIAN_POINT('Ctrl Pts',(368.464482605557,-18.4654979690725,-2.18404763675884));
#38718=CARTESIAN_POINT('Ctrl Pts',(368.469979807997,-18.465999707135,-2.18999744072849));
#38719=CARTESIAN_POINT('Ctrl Pts',(368.483506308833,-18.4672251578462,-2.20452732564601));
#38720=CARTESIAN_POINT('Ctrl Pts',(368.491560313153,-18.4679470117112,-2.21308444600156));
#38721=CARTESIAN_POINT('Ctrl Pts',(368.52102611119,-18.4705605420995,-2.2440497876282));
#38722=CARTESIAN_POINT('Ctrl Pts',(368.542714810309,-18.4724321883214,-2.26619367841296));
#38723=CARTESIAN_POINT('Ctrl Pts',(368.598021606244,-18.477086712869,-2.32105510469655));
#38724=CARTESIAN_POINT('Ctrl Pts',(368.632041603794,-18.4798436267073,-2.35335876140487));
#38725=CARTESIAN_POINT('Ctrl Pts',(368.916620752167,-18.5021729162937,-2.61200285310076));
#38726=CARTESIAN_POINT('Ctrl Pts',(369.200622905637,-18.5201530414036,-2.7984285062356));
#38727=CARTESIAN_POINT('Ctrl Pts',(369.565603648433,-18.5436123541569,-2.96317697938668));
#38728=CARTESIAN_POINT('Ctrl Pts',(369.623523868706,-18.5473359423497,-2.98731161669759));
#38729=CARTESIAN_POINT('Ctrl Pts',(369.703294904873,-18.5524832993742,-3.01785010980724));
#38730=CARTESIAN_POINT('Ctrl Pts',(369.72456561599,-18.5538575878478,-3.02573662544653));
#38731=CARTESIAN_POINT('Ctrl Pts',(369.758534281309,-18.5560558247618,-3.03792477658731));
#38732=CARTESIAN_POINT('Ctrl Pts',(369.771179124183,-18.5568748915467,-3.0423729679479));
#38733=CARTESIAN_POINT('Ctrl Pts',(369.797197935718,-18.5585620087448,-3.05134382698736));
#38734=CARTESIAN_POINT('Ctrl Pts',(369.810574591674,-18.5594303267327,-3.05585775162006));
#38735=CARTESIAN_POINT('Ctrl Pts',(369.8416458933,-18.5614496421438,-3.06611578874955));
#38736=CARTESIAN_POINT('Ctrl Pts',(369.859361342558,-18.5626027495016,-3.07179482210187));
#38737=CARTESIAN_POINT('Ctrl Pts',(369.916068229302,-18.5663000293194,-3.0894333660342));
#38738=CARTESIAN_POINT('Ctrl Pts',(369.955236696981,-18.5688631758737,-3.10080585829091));
#38739=CARTESIAN_POINT('Ctrl Pts',(370.047705068625,-18.5749385952949,-3.12576109332134));
#38740=CARTESIAN_POINT('Ctrl Pts',(370.101156486561,-18.5784693867073,-3.13872839241657));
#38741=CARTESIAN_POINT('Ctrl Pts',(370.301185206125,-18.5917525497531,-3.18186712662266));
#38742=CARTESIAN_POINT('Ctrl Pts',(370.44946400873,-18.6017490176813,-3.20318402681224));
#38743=CARTESIAN_POINT('Ctrl Pts',(370.816286029456,-18.6265796853989,-3.23007780540514));
#38744=CARTESIAN_POINT('Ctrl Pts',(371.034971459471,-18.641488490177,-3.22389199146721));
#38745=CARTESIAN_POINT('Ctrl Pts',(371.276436450036,-18.657110023523,-3.19237967185828));
#38746=CARTESIAN_POINT('Ctrl Pts',(371.301468994018,-18.6587187303267,-3.1888127455819));
#38747=CARTESIAN_POINT('Ctrl Pts',(371.336403339736,-18.6609462851765,-3.18341467630133));
#38748=CARTESIAN_POINT('Ctrl Pts',(371.346341737351,-18.6615780120427,-3.18183129431249));
#38749=CARTESIAN_POINT('Ctrl Pts',(371.36351657664,-18.6626660902676,-3.17901245055126));
#38750=CARTESIAN_POINT('Ctrl Pts',(371.370756447126,-18.6631236411341,-3.17779878015446));
#38751=CARTESIAN_POINT('Ctrl Pts',(371.386046544524,-18.6640875033625,-3.17518185094773));
#38752=CARTESIAN_POINT('Ctrl Pts',(371.394095698605,-18.6645934638954,-3.17377269220271));
#38753=CARTESIAN_POINT('Ctrl Pts',(371.414052800967,-18.6658445502377,-3.17020053419664));
#38754=CARTESIAN_POINT('Ctrl Pts',(371.425954229934,-18.666587634076,-3.16800101723802));
#38755=CARTESIAN_POINT('Ctrl Pts',(371.470694266014,-18.6693706961138,-3.15947163921331));
#38756=CARTESIAN_POINT('Ctrl Pts',(371.503447330943,-18.6713870877218,-3.15269756240237));
#38757=CARTESIAN_POINT('Ctrl Pts',(371.751828510616,-18.6865586707859,-3.09728130408462));
#38758=CARTESIAN_POINT('Ctrl Pts',(371.962070051936,-18.6987409357764,-3.02707402774668));
#38759=CARTESIAN_POINT('Ctrl Pts',(372.352928981711,-18.7227647890337,-2.85011954174657));
#38760=CARTESIAN_POINT('Ctrl Pts',(372.533598432476,-18.7345362428666,-2.74623216680772));
#38761=CARTESIAN_POINT('Ctrl Pts',(372.725346998694,-18.748621901833,-2.60976611878067));
#38762=CARTESIAN_POINT('Ctrl Pts',(372.747497224853,-18.7502744011564,-2.59357187017878));
#38763=CARTESIAN_POINT('Ctrl Pts',(372.783456926749,-18.7530005964673,-2.56657004566426));
#38764=CARTESIAN_POINT('Ctrl Pts',(372.797390028108,-18.7540678244717,-2.5559289005277));
#38765=CARTESIAN_POINT('Ctrl Pts',(372.822282936842,-18.7559946587017,-2.53659379284251));
#38766=CARTESIAN_POINT('Ctrl Pts',(372.833274344976,-18.7568526183678,-2.52794109462594));
#38767=CARTESIAN_POINT('Ctrl Pts',(372.856598039331,-18.758688762904,-2.50933289959637));
#38768=CARTESIAN_POINT('Ctrl Pts',(372.868913878038,-18.7596677338427,-2.49935746814898));
#38769=CARTESIAN_POINT('Ctrl Pts',(372.90207007223,-18.7623292222263,-2.47209455469661));
#38770=CARTESIAN_POINT('Ctrl Pts',(372.922766586904,-18.764018694681,-2.45463491001722));
#38771=CARTESIAN_POINT('Ctrl Pts',(373.033142588268,-18.7731842611679,-2.35911486843591));
#38772=CARTESIAN_POINT('Ctrl Pts',(373.118660443868,-18.7808528455383,-2.27640646205571));
#38773=CARTESIAN_POINT('Ctrl Pts',(373.305207014915,-18.7989474736678,-2.07486939361421));
#38774=CARTESIAN_POINT('Ctrl Pts',(373.402574731008,-18.809473232447,-1.95305556505446));
#38775=CARTESIAN_POINT('Ctrl Pts',(373.585977416438,-18.8313858387925,-1.68605348148778));
#38776=CARTESIAN_POINT('Ctrl Pts',(373.670217151245,-18.842740940469,-1.5401599097305));
#38777=CARTESIAN_POINT('Ctrl Pts',(373.754294437162,-18.8552801028434,-1.36403086282793));
#38778=CARTESIAN_POINT('Ctrl Pts',(373.76559610371,-18.8569962599118,-1.3395713395968));
#38779=CARTESIAN_POINT('Ctrl Pts',(373.780804619568,-18.859346339912,-1.30554202755263));
#38780=CARTESIAN_POINT('Ctrl Pts',(373.784973832728,-18.8599950236202,-1.29609164312704));
#38781=CARTESIAN_POINT('Ctrl Pts',(373.792055556113,-18.8611043657702,-1.27982816758715));
#38782=CARTESIAN_POINT('Ctrl Pts',(373.794990108312,-18.8615663322498,-1.27302484587574));
#38783=CARTESIAN_POINT('Ctrl Pts',(373.801083928449,-18.8625303438933,-1.25876218471752));
#38784=CARTESIAN_POINT('Ctrl Pts',(373.804238569916,-18.8630320895178,-1.25130097144065));
#38785=CARTESIAN_POINT('Ctrl Pts',(373.81190061876,-18.8642575872455,-1.23298683544353));
#38786=CARTESIAN_POINT('Ctrl Pts',(373.816376916963,-18.8649794802337,-1.2221208664844));
#38787=CARTESIAN_POINT('Ctrl Pts',(373.832443764382,-18.8675933147685,-1.18250557092711));
#38788=CARTESIAN_POINT('Ctrl Pts',(373.843679227197,-18.8694652199086,-1.1536128841999));
#38789=CARTESIAN_POINT('Ctrl Pts',(373.870867137919,-18.874120522916,-1.08059566270273));
#38790=CARTESIAN_POINT('Ctrl Pts',(373.886276581807,-18.8768779451818,-1.03627549390567));
#38791=CARTESIAN_POINT('Ctrl Pts',(374.004679216291,-18.899221434189,-0.670142569164643));
#38792=CARTESIAN_POINT('Ctrl Pts',(374.057448020884,-18.9172134657338,-0.334296922208163));
#38793=CARTESIAN_POINT('Ctrl Pts',(374.056995052279,-18.9406778914367,0.0661883945450329));
#38794=CARTESIAN_POINT('Ctrl Pts',(374.055103692997,-18.9443902411663,0.12871300483197));
#38795=CARTESIAN_POINT('Ctrl Pts',(374.050050778173,-18.9495244073616,0.213758549730239));
#38796=CARTESIAN_POINT('Ctrl Pts',(374.048468449479,-18.950897077887,0.236361728238311));
#38797=CARTESIAN_POINT('Ctrl Pts',(374.045571318633,-18.9530933734128,0.272301823266245));
#38798=CARTESIAN_POINT('Ctrl Pts',(374.044411427091,-18.9539121325887,0.285650731774019));
#38799=CARTESIAN_POINT('Ctrl Pts',(374.041858333086,-18.9555990980942,0.313051132780387));
#38800=CARTESIAN_POINT('Ctrl Pts',(374.040455961039,-18.9564675750236,0.32710146013089));
#38801=CARTESIAN_POINT('Ctrl Pts',(374.036990322945,-18.9584880814232,0.35965721796383));
#38802=CARTESIAN_POINT('Ctrl Pts',(374.034858936996,-18.9596422287215,0.378154744137123));
#38803=CARTESIAN_POINT('Ctrl Pts',(374.027536839797,-18.9633462670263,0.437196544117848));
#38804=CARTESIAN_POINT('Ctrl Pts',(374.021735194516,-18.9659152298723,0.477659669921169));
#38805=CARTESIAN_POINT('Ctrl Pts',(374.006300666022,-18.972006853065,0.572437432523947));
#38806=CARTESIAN_POINT('Ctrl Pts',(373.996040010534,-18.9755481659373,0.626635459845248));
#38807=CARTESIAN_POINT('Ctrl Pts',(373.952642131851,-18.9888903769495,0.827514792632508));
#38808=CARTESIAN_POINT('Ctrl Pts',(373.910646173259,-18.9989377589264,0.972071278230671));
#38809=CARTESIAN_POINT('Ctrl Pts',(373.783738820259,-19.0237446769951,1.31687400168511));
#38810=CARTESIAN_POINT('Ctrl Pts',(373.68836220749,-19.0385733831318,1.51250972265325));
#38811=CARTESIAN_POINT('Ctrl Pts',(373.560684429104,-19.0541283304377,1.71862893220527));
#38812=CARTESIAN_POINT('Ctrl Pts',(373.547081764963,-19.055741244464,1.7400207367515));
#38813=CARTESIAN_POINT('Ctrl Pts',(373.527721860386,-19.0579736367487,1.76968751828831));
#38814=CARTESIAN_POINT('Ctrl Pts',(373.522176469462,-19.0586060650166,1.77809873844025));
#38815=CARTESIAN_POINT('Ctrl Pts',(373.512520851668,-19.0596950191552,1.79259593588793));
#38816=CARTESIAN_POINT('Ctrl Pts',(373.508429135349,-19.0601527489896,1.79869406615128));
#38817=CARTESIAN_POINT('Ctrl Pts',(373.499742239819,-19.0611165967424,1.81154550655377));
#38818=CARTESIAN_POINT('Ctrl Pts',(373.495142164213,-19.0616223660171,1.81829543021478));
#38819=CARTESIAN_POINT('Ctrl Pts',(373.483671561335,-19.0628723146617,1.83499007896691));
#38820=CARTESIAN_POINT('Ctrl Pts',(373.476770574373,-19.0636144602543,1.84491389713835));
#38821=CARTESIAN_POINT('Ctrl Pts',(373.450630588182,-19.0663898340582,1.88205637645325));
#38822=CARTESIAN_POINT('Ctrl Pts',(373.431024813298,-19.0683996436644,1.90901589648941));
#38823=CARTESIAN_POINT('Ctrl Pts',(373.279349867431,-19.0834558791109,2.11091970121108));
#38824=CARTESIAN_POINT('Ctrl Pts',(373.130143250801,-19.0955446718493,2.27230581699969));
#38825=CARTESIAN_POINT('Ctrl Pts',(372.808198637967,-19.1195735167413,2.55616863627562));
#38826=CARTESIAN_POINT('Ctrl Pts',(372.637536906503,-19.131451436681,2.67928884237165));
#38827=CARTESIAN_POINT('Ctrl Pts',(372.432425920222,-19.1456571967526,2.79873550709));
#38828=CARTESIAN_POINT('Ctrl Pts',(372.408549803685,-19.1473090589213,2.81223461481011));
#38829=CARTESIAN_POINT('Ctrl Pts',(372.369137319987,-19.1500344158585,2.8338585034132));
#38830=CARTESIAN_POINT('Ctrl Pts',(372.353701512038,-19.1511014495157,2.84216433222546));
#38831=CARTESIAN_POINT('Ctrl Pts',(372.328763936574,-19.1528250819395,2.85532174488835));
#38832=CARTESIAN_POINT('Ctrl Pts',(372.319304375368,-19.153478853133,2.86025285363061));
#38833=CARTESIAN_POINT('Ctrl Pts',(372.309820613636,-19.1541342831958,2.86513684952685));
#38834=CARTESIAN_POINT('Origin',(370.834317853224,2.31077344927308,0.));
#38835=CARTESIAN_POINT('',(372.309820629953,-20.6514935740585,2.86513684112382));
#38836=CARTESIAN_POINT('',(372.309820109182,-20.4075893673376,2.8651371093129));
#38837=CARTESIAN_POINT('',(372.309820613641,2.31077344927308,2.86513684952399));
#38838=CARTESIAN_POINT('Ctrl Pts',(372.309820629953,-20.6514935740584,2.86513684112379));
#38839=CARTESIAN_POINT('Ctrl Pts',(372.324583288222,-20.6503904433452,2.85753429210912));
#38840=CARTESIAN_POINT('Ctrl Pts',(372.339291174212,-20.64929025969,2.84981559336732));
#38841=CARTESIAN_POINT('Ctrl Pts',(372.395235037442,-20.6451027812944,2.81990206143058));
#38842=CARTESIAN_POINT('Ctrl Pts',(372.436043231241,-20.6420424298463,2.79692444492251));
#38843=CARTESIAN_POINT('Ctrl Pts',(372.50296861048,-20.6370307707822,2.75729578544244));
#38844=CARTESIAN_POINT('Ctrl Pts',(372.529371715499,-20.6350555600094,2.74114355089575));
#38845=CARTESIAN_POINT('Ctrl Pts',(372.565463786448,-20.6323625883558,2.71834308507967));
#38846=CARTESIAN_POINT('Ctrl Pts',(372.575354284503,-20.6316253643962,2.71201908645424));
#38847=CARTESIAN_POINT('Ctrl Pts',(372.592005262767,-20.6303857832336,2.70124379535853));
#38848=CARTESIAN_POINT('Ctrl Pts',(372.598783874991,-20.6298815911851,2.69682085699796));
#38849=CARTESIAN_POINT('Ctrl Pts',(372.611731474634,-20.628919503314,2.68830303380777));
#38850=CARTESIAN_POINT('Ctrl Pts',(372.617903088859,-20.6284613225708,2.6842123785172));
#38851=CARTESIAN_POINT('Ctrl Pts',(372.632645542387,-20.6273676840638,2.67436752374572));
#38852=CARTESIAN_POINT('Ctrl Pts',(372.641203001412,-20.6267335513693,2.66859329941169));
#38853=CARTESIAN_POINT('Ctrl Pts',(372.671987988741,-20.6244542021076,2.64760487159186));
#38854=CARTESIAN_POINT('Ctrl Pts',(372.694053005574,-20.6228240976427,2.63215279832257));
#38855=CARTESIAN_POINT('Ctrl Pts',(372.852746208518,-20.6111063275073,2.51802843755481));
#38856=CARTESIAN_POINT('Ctrl Pts',(372.981658347962,-20.6016124942679,2.40903775557397));
#38857=CARTESIAN_POINT('Ctrl Pts',(373.212009111439,-20.5834632775565,2.18103062259949));
#38858=CARTESIAN_POINT('Ctrl Pts',(373.314485233728,-20.5748212028382,2.06375335691227));
#38859=CARTESIAN_POINT('Ctrl Pts',(373.479586857849,-20.5591386133118,1.84466338293518));
#38860=CARTESIAN_POINT('Ctrl Pts',(373.545776542936,-20.5522167406175,1.74591476204762));
#38861=CARTESIAN_POINT('Ctrl Pts',(373.620161257533,-20.5434636516853,1.62047099395734));
#38862=CARTESIAN_POINT('Ctrl Pts',(373.633668206809,-20.5418295046034,1.59702449753135));
#38863=CARTESIAN_POINT('Ctrl Pts',(373.654610207764,-20.539222026732,1.55958950508434));
#38864=CARTESIAN_POINT('Ctrl Pts',(373.662240300058,-20.5382557035163,1.54571116646521));
#38865=CARTESIAN_POINT('Ctrl Pts',(373.676411466993,-20.5364296071305,1.51947913406856));
#38866=CARTESIAN_POINT('Ctrl Pts',(373.68297508463,-20.5355706619534,1.50713798853662));
#38867=CARTESIAN_POINT('Ctrl Pts',(373.697583134365,-20.5336287872889,1.47923506137128));
#38868=CARTESIAN_POINT('Ctrl Pts',(373.705581334097,-20.5325442593025,1.46364969886281));
#38869=CARTESIAN_POINT('Ctrl Pts',(373.725769468597,-20.5297509313047,1.42350857973443));
#38870=CARTESIAN_POINT('Ctrl Pts',(373.737773660644,-20.5280357343837,1.39886147290829));
#38871=CARTESIAN_POINT('Ctrl Pts',(373.839337072564,-20.5130371168941,1.18338986790783));
#38872=CARTESIAN_POINT('Ctrl Pts',(373.910272372336,-20.4991075794542,0.984391604116014));
#38873=CARTESIAN_POINT('Ctrl Pts',(374.000455015869,-20.4739811563885,0.622824594982));
#38874=CARTESIAN_POINT('Ctrl Pts',(374.027745360789,-20.462948082131,0.462987970792784));
#38875=CARTESIAN_POINT('Ctrl Pts',(374.050544783541,-20.4467955758357,0.220575524284215));
#38876=CARTESIAN_POINT('Ctrl Pts',(374.055097362522,-20.4414673146229,0.139107810831596));
#38877=CARTESIAN_POINT('Ctrl Pts',(374.056844418894,-20.4352547762159,0.0412869601068374));
#38878=CARTESIAN_POINT('Ctrl Pts',(374.05701174876,-20.4342280325143,0.0250232089321368));
#38879=CARTESIAN_POINT('Ctrl Pts',(374.057080624951,-20.4326383995095,-0.000320171998430622));
#38880=CARTESIAN_POINT('Ctrl Pts',(374.057066935641,-20.432071001271,-0.00939903622049846));
#38881=CARTESIAN_POINT('Ctrl Pts',(374.05696983288,-20.4310165860551,-0.0263345968753181));
#38882=CARTESIAN_POINT('Ctrl Pts',(374.056896055615,-20.4305290674782,-0.0341909936959644));
#38883=CARTESIAN_POINT('Ctrl Pts',(374.056662107682,-20.4294200938858,-0.0521205993707929));
#38884=CARTESIAN_POINT('Ctrl Pts',(374.056483435635,-20.4287996723389,-0.0621933839278968));
#38885=CARTESIAN_POINT('Ctrl Pts',(374.055882932423,-20.4271571080255,-0.0889667388121332));
#38886=CARTESIAN_POINT('Ctrl Pts',(374.055378469183,-20.4261393677661,-0.105665393491946));
#38887=CARTESIAN_POINT('Ctrl Pts',(374.050054104149,-20.4176494938012,-0.245799076200485));
#38888=CARTESIAN_POINT('Ctrl Pts',(374.03827014266,-20.4105226904863,-0.36888150311233));
#38889=CARTESIAN_POINT('Ctrl Pts',(373.990329562263,-20.3926913286214,-0.679875734584698));
#38890=CARTESIAN_POINT('Ctrl Pts',(373.944470335683,-20.382179002354,-0.865791504826672));
#38891=CARTESIAN_POINT('Ctrl Pts',(373.83705695062,-20.3634010670208,-1.17863396699224));
#38892=CARTESIAN_POINT('Ctrl Pts',(373.783174619783,-20.3553183756282,-1.30761503569664));
#38893=CARTESIAN_POINT('Ctrl Pts',(373.708566707221,-20.3452554309117,-1.45794591329469));
#38894=CARTESIAN_POINT('Ctrl Pts',(373.695699934448,-20.3435536084455,-1.4830392002752));
#38895=CARTESIAN_POINT('Ctrl Pts',(373.67497940397,-20.3408629295831,-1.52217549880286));
#38896=CARTESIAN_POINT('Ctrl Pts',(373.667346766217,-20.3398818787172,-1.5363344227502));
#38897=CARTESIAN_POINT('Ctrl Pts',(373.652896706246,-20.3380428590516,-1.56266613556717));
#38898=CARTESIAN_POINT('Ctrl Pts',(373.64610558809,-20.3371858442013,-1.57485298561577));
#38899=CARTESIAN_POINT('Ctrl Pts',(373.630781533879,-20.3352678448751,-1.60193732210998));
#38900=CARTESIAN_POINT('Ctrl Pts',(373.622208301866,-20.3342054270773,-1.61681140808226));
#38901=CARTESIAN_POINT('Ctrl Pts',(373.60021940518,-20.3315066862081,-1.65426600255352));
#38902=CARTESIAN_POINT('Ctrl Pts',(373.586645979849,-20.3298646790583,-1.67675198526912));
#38903=CARTESIAN_POINT('Ctrl Pts',(373.500103992828,-20.3195395445211,-1.81623639875334));
#38904=CARTESIAN_POINT('Ctrl Pts',(373.419973531792,-20.3105927746075,-1.9286021818012));
#38905=CARTESIAN_POINT('Ctrl Pts',(373.198073387264,-20.2872801811893,-2.20098828315791));
#38906=CARTESIAN_POINT('Ctrl Pts',(373.047132238567,-20.2726627443467,-2.35268630125291));
#38907=CARTESIAN_POINT('Ctrl Pts',(372.828364666454,-20.2537219734903,-2.53274125151364));
#38908=CARTESIAN_POINT('Ctrl Pts',(372.772974775291,-20.2490970432678,-2.57538569581566));
#38909=CARTESIAN_POINT('Ctrl Pts',(372.693713943368,-20.2427568278717,-2.63240073959923));
#38910=CARTESIAN_POINT('Ctrl Pts',(372.670979839837,-20.2409689473225,-2.64831273262103));
#38911=CARTESIAN_POINT('Ctrl Pts',(372.630854178683,-20.2378703786869,-2.67563210694264));
#38912=CARTESIAN_POINT('Ctrl Pts',(372.613552694506,-20.2365524781537,-2.68716828138095));
#38913=CARTESIAN_POINT('Ctrl Pts',(372.587756552771,-20.2346156582034,-2.7040100842197));
#38914=CARTESIAN_POINT('Ctrl Pts',(372.579347262632,-20.2339886496511,-2.70944462487207));
#38915=CARTESIAN_POINT('Ctrl Pts',(372.564311214331,-20.2328755128736,-2.7190626957432));
#38916=CARTESIAN_POINT('Ctrl Pts',(372.557694395383,-20.2323884045542,-2.72326132991864));
#38917=CARTESIAN_POINT('Ctrl Pts',(372.543242262024,-20.2313304719903,-2.73235801173618));
#38918=CARTESIAN_POINT('Ctrl Pts',(372.535401176276,-20.230760270171,-2.73724651288528));
#38919=CARTESIAN_POINT('Ctrl Pts',(372.513461790462,-20.2291750622415,-2.75079387286468));
#38920=CARTESIAN_POINT('Ctrl Pts',(372.499317448713,-20.2281647859198,-2.75937813041033));
#38921=CARTESIAN_POINT('Ctrl Pts',(372.419144689466,-20.2225004318338,-2.8071943727758));
#38922=CARTESIAN_POINT('Ctrl Pts',(372.351791083465,-20.2179775971129,-2.84416830470394));
#38923=CARTESIAN_POINT('Ctrl Pts',(372.262992842847,-20.2122307012515,-2.88886064756223));
#38924=CARTESIAN_POINT('Ctrl Pts',(372.242703963854,-20.2109318217702,-2.89880607574419));
#38925=CARTESIAN_POINT('Ctrl Pts',(372.152136628291,-20.2051894355994,-2.94202605078323));
#38926=CARTESIAN_POINT('Ctrl Pts',(372.080769921292,-20.200811677939,-2.9729651324264));
#38927=CARTESIAN_POINT('Ctrl Pts',(371.832996847688,-20.1859001877882,-3.06988801276916));
#38928=CARTESIAN_POINT('Ctrl Pts',(371.651977109528,-20.1754685757687,-3.12297961441169));
#38929=CARTESIAN_POINT('Ctrl Pts',(371.404535398339,-20.1609166793302,-3.17255024325987));
#38930=CARTESIAN_POINT('Ctrl Pts',(371.34135098151,-20.1571787823768,-3.18325930020289));
#38931=CARTESIAN_POINT('Ctrl Pts',(371.232490240739,-20.1506715972725,-3.19838669300094));
#38932=CARTESIAN_POINT('Ctrl Pts',(371.186960858635,-20.1479302173056,-3.20372615604336));
#38933=CARTESIAN_POINT('Ctrl Pts',(371.121947881511,-20.1439808191757,-3.20994794684186));
#38934=CARTESIAN_POINT('Ctrl Pts',(371.102544953445,-20.1427977389029,-3.21162747708565));
#38935=CARTESIAN_POINT('Ctrl Pts',(371.068921453156,-20.1407394726026,-3.21423113024819));
#38936=CARTESIAN_POINT('Ctrl Pts',(371.054707632188,-20.1398668716245,-3.21523699636672));
#38937=CARTESIAN_POINT('Ctrl Pts',(371.025588030514,-20.1380738748322,-3.2171036969262));
#38938=CARTESIAN_POINT('Ctrl Pts',(371.010682022249,-20.1371532108741,-3.21795527399319));
#38939=CARTESIAN_POINT('Ctrl Pts',(370.972904651007,-20.1348124512563,-3.2198502200869));
#38940=CARTESIAN_POINT('Ctrl Pts',(370.950027386388,-20.1333880101405,-3.22075348339693));
#38941=CARTESIAN_POINT('Ctrl Pts',(370.862856605748,-20.1279329819469,-3.22326531046257));
#38942=CARTESIAN_POINT('Ctrl Pts',(370.798533274687,-20.1238506028816,-3.22319286401706));
#38943=CARTESIAN_POINT('Ctrl Pts',(370.452629574746,-20.1015777275565,-3.21244814636443));
#38944=CARTESIAN_POINT('Ctrl Pts',(370.17339313524,-20.0823066110808,-3.16680231692582));
#38945=CARTESIAN_POINT('Ctrl Pts',(369.825493601141,-20.057908035134,-3.06187307237525));
#38946=CARTESIAN_POINT('Ctrl Pts',(369.748190429484,-20.0524724400234,-3.03531250696704));
#38947=CARTESIAN_POINT('Ctrl Pts',(369.629179937456,-20.0441609566835,-2.98929181104623));
#38948=CARTESIAN_POINT('Ctrl Pts',(369.58673964208,-20.0412088073997,-2.97182974545993));
#38949=CARTESIAN_POINT('Ctrl Pts',(369.532224073778,-20.0374452087341,-2.94802547686855));
#38950=CARTESIAN_POINT('Ctrl Pts',(369.519798107862,-20.0365893079822,-2.94250578200464));
#38951=CARTESIAN_POINT('Ctrl Pts',(369.499669342575,-20.0352064603573,-2.93341149719189));
#38952=CARTESIAN_POINT('Ctrl Pts',(369.491945234246,-20.034676685613,-2.92988488077386));
#38953=CARTESIAN_POINT('Ctrl Pts',(369.477008568169,-20.0336540439749,-2.9229937401109));
#38954=CARTESIAN_POINT('Ctrl Pts',(369.469794439684,-20.0331609671482,-2.91963298297711));
#38955=CARTESIAN_POINT('Ctrl Pts',(369.453857423651,-20.0320734047485,-2.91213663041633));
#38956=CARTESIAN_POINT('Ctrl Pts',(369.445140444403,-20.0314796853285,-2.9079884601214));
#38957=CARTESIAN_POINT('Ctrl Pts',(369.414272193598,-20.029380817066,-2.89312863421641));
#38958=CARTESIAN_POINT('Ctrl Pts',(369.39222446503,-20.0278882790643,-2.882202233137));
#38959=CARTESIAN_POINT('Ctrl Pts',(369.160005631377,-20.0122155176577,-2.76378742624917));
#38960=CARTESIAN_POINT('Ctrl Pts',(368.962095480527,-19.999236407559,-2.63375365515045));
#38961=CARTESIAN_POINT('Ctrl Pts',(368.621799398861,-19.9745009324386,-2.35225682265025));
#38962=CARTESIAN_POINT('Ctrl Pts',(368.476362989442,-19.962856822136,-2.20644138951225));
#38963=CARTESIAN_POINT('Ctrl Pts',(368.326596185414,-19.9487476522049,-2.02444152885311));
#38964=CARTESIAN_POINT('Ctrl Pts',(368.307716960025,-19.9469254568871,-2.00082965282536));
#38965=CARTESIAN_POINT('Ctrl Pts',(368.27903925908,-19.9440870192184,-1.96390981840097));
#38966=CARTESIAN_POINT('Ctrl Pts',(368.269005965348,-19.9430800944763,-1.95078583411237));
#38967=CARTESIAN_POINT('Ctrl Pts',(368.251526324454,-19.9413009462858,-1.92755365391943));
#38968=CARTESIAN_POINT('Ctrl Pts',(368.24403725733,-19.9405304179593,-1.91747792615612));
#38969=CARTESIAN_POINT('Ctrl Pts',(368.227071474119,-19.9387657040422,-1.8943715272601));
#38970=CARTESIAN_POINT('Ctrl Pts',(368.217633283635,-19.9377700528415,-1.88131310867088));
#38971=CARTESIAN_POINT('Ctrl Pts',(368.192302682442,-19.9350594124727,-1.8457070060361));
#38972=CARTESIAN_POINT('Ctrl Pts',(368.176601492659,-19.9333371906028,-1.82302555811161));
#38973=CARTESIAN_POINT('Ctrl Pts',(368.096537895935,-19.9243306158851,-1.70413523511091));
#38974=CARTESIAN_POINT('Ctrl Pts',(368.037108747733,-19.9168651079502,-1.60472176121304));
#38975=CARTESIAN_POINT('Ctrl Pts',(367.875961596529,-19.8941001017526,-1.29889422203756));
#38976=CARTESIAN_POINT('Ctrl Pts',(367.790851163987,-19.8783552716304,-1.0845698119118));
#38977=CARTESIAN_POINT('Ctrl Pts',(367.699573020366,-19.8555214847328,-0.756172554428587));
#38978=CARTESIAN_POINT('Ctrl Pts',(367.675401654138,-19.8481967618234,-0.647823872396063));
#38979=CARTESIAN_POINT('Ctrl Pts',(367.653944128462,-19.8400291793497,-0.521196874538539));
#38980=CARTESIAN_POINT('Ctrl Pts',(367.651163459427,-19.8389242235019,-0.503935857255061));
#38981=CARTESIAN_POINT('Ctrl Pts',(367.647112956313,-19.8372405672459,-0.477419878440386));
#38982=CARTESIAN_POINT('Ctrl Pts',(367.645742711021,-19.8366564851984,-0.468180908321821));
#38983=CARTESIAN_POINT('Ctrl Pts',(367.643297812703,-19.8355870139964,-0.451187265802331));
#38984=CARTESIAN_POINT('Ctrl Pts',(367.642211249176,-19.8351009850683,-0.443434638433489));
#38985=CARTESIAN_POINT('Ctrl Pts',(367.639816647838,-19.8340048924913,-0.425884155100602));
#38986=CARTESIAN_POINT('Ctrl Pts',(367.638525430672,-19.8333957760794,-0.41608420154635));
#38987=CARTESIAN_POINT('Ctrl Pts',(367.635298956339,-19.8318249115421,-0.390694800896339));
#38988=CARTESIAN_POINT('Ctrl Pts',(367.633432530947,-19.830866873789,-0.375096662570071));
#38989=CARTESIAN_POINT('Ctrl Pts',(367.621818520877,-19.8245547031182,-0.27162794779574));
#38990=CARTESIAN_POINT('Ctrl Pts',(367.615575338699,-19.8193763009762,-0.183393693137639));
#38991=CARTESIAN_POINT('Ctrl Pts',(367.612059119699,-19.812522347707,-0.064170820373583));
#38992=CARTESIAN_POINT('Ctrl Pts',(367.61159246942,-19.8107618795412,-0.0333228726335784));
#38993=CARTESIAN_POINT('Ctrl Pts',(367.611365393164,-19.7939561659989,0.262665895764635));
#38994=CARTESIAN_POINT('Ctrl Pts',(367.643879954345,-19.7795271327586,0.526807229265741));
#38995=CARTESIAN_POINT('Ctrl Pts',(367.727498015159,-19.7595540549841,0.860211327451352));
#38996=CARTESIAN_POINT('Ctrl Pts',(367.749395193941,-19.7549171119708,0.935704950494251));
#38997=CARTESIAN_POINT('Ctrl Pts',(367.781754144639,-19.7487086465045,1.03372130521205));
#38998=CARTESIAN_POINT('Ctrl Pts',(367.789748227104,-19.7472178308891,1.05703390297856));
#38999=CARTESIAN_POINT('Ctrl Pts',(367.803140493652,-19.7447865904906,1.09467610087256));
#39000=CARTESIAN_POINT('Ctrl Pts',(367.808374903739,-19.7438516044097,1.10906321045882));
#39001=CARTESIAN_POINT('Ctrl Pts',(367.818623883133,-19.7420494110642,1.13662044129997));
#39002=CARTESIAN_POINT('Ctrl Pts',(367.82362272606,-19.7411827458648,1.14979606455863));
#39003=CARTESIAN_POINT('Ctrl Pts',(367.835377841904,-19.7391725523392,1.18017712122158));
#39004=CARTESIAN_POINT('Ctrl Pts',(367.84219599776,-19.7380269675883,1.19735792818893));
#39005=CARTESIAN_POINT('Ctrl Pts',(367.864300968917,-19.7343755915541,1.25169135355113));
#39006=CARTESIAN_POINT('Ctrl Pts',(367.880134398117,-19.7318514714104,1.28861608597521));
#39007=CARTESIAN_POINT('Ctrl Pts',(367.965273786669,-19.7187233157166,1.47734575648011));
#39008=CARTESIAN_POINT('Ctrl Pts',(368.0455947568,-19.7077453239286,1.6238760508442));
#39009=CARTESIAN_POINT('Ctrl Pts',(368.205904771585,-19.6880831628653,1.86908292525594));
#39010=CARTESIAN_POINT('Ctrl Pts',(368.281061349241,-19.6795146878501,1.97050917442894));
#39011=CARTESIAN_POINT('Ctrl Pts',(368.452653694803,-19.6614781278235,2.17572537289477));
#39012=CARTESIAN_POINT('Ctrl Pts',(368.550390997389,-19.6520451176192,2.27811153420839));
#39013=CARTESIAN_POINT('Ctrl Pts',(368.668218219015,-19.6418564832114,2.38630979085417));
#39014=CARTESIAN_POINT('Ctrl Pts',(368.681997526511,-19.6406819886341,2.39874535793091));
#39015=CARTESIAN_POINT('Ctrl Pts',(368.703130056975,-19.6389074733238,2.41748835592149));
#39016=CARTESIAN_POINT('Ctrl Pts',(368.710405290203,-19.6383013140247,2.42388258879763));
#39017=CARTESIAN_POINT('Ctrl Pts',(368.723607269034,-19.6372100758334,2.43538078420053));
#39018=CARTESIAN_POINT('Ctrl Pts',(368.729523824179,-19.6367241802063,2.44049602190619));
#39019=CARTESIAN_POINT('Ctrl Pts',(368.7426786172,-19.6356507974017,2.45178575303565));
#39020=CARTESIAN_POINT('Ctrl Pts',(368.749925593552,-19.6350640731383,2.45794975247521));
#39021=CARTESIAN_POINT('Ctrl Pts',(368.771201559347,-19.6333545932458,2.47588450354414));
#39022=CARTESIAN_POINT('Ctrl Pts',(368.785303971363,-19.6322379607947,2.48756810250515));
#39023=CARTESIAN_POINT('Ctrl Pts',(368.912946411962,-19.6222702335846,2.59149558261916));
#39024=CARTESIAN_POINT('Ctrl Pts',(369.032559796952,-19.6139059631413,2.67604116914777));
#39025=CARTESIAN_POINT('Ctrl Pts',(369.358668816137,-19.5923961636063,2.8747275213872));
#39026=CARTESIAN_POINT('Ctrl Pts',(369.572636943486,-19.5794631856752,2.97485406524251));
#39027=CARTESIAN_POINT('Ctrl Pts',(369.870788610753,-19.5611693233384,3.07636746945026));
#39028=CARTESIAN_POINT('Ctrl Pts',(369.946887712082,-19.556484341736,3.09917596190114));
#39029=CARTESIAN_POINT('Ctrl Pts',(370.047690384361,-19.5502204166709,3.12537146155126));
#39030=CARTESIAN_POINT('Ctrl Pts',(370.071703779854,-19.548724045934,3.13131749755412));
#39031=CARTESIAN_POINT('Ctrl Pts',(370.110704966837,-19.5462859811946,3.14049947741603));
#39032=CARTESIAN_POINT('Ctrl Pts',(370.125651853903,-19.5453497836919,3.14390602049039));
#39033=CARTESIAN_POINT('Ctrl Pts',(370.154377861132,-19.5435467851678,3.15023770190342));
#39034=CARTESIAN_POINT('Ctrl Pts',(370.168152997817,-19.5426805379087,3.1531794028812));
#39035=CARTESIAN_POINT('Ctrl Pts',(370.200004517233,-19.5406735690553,3.15976330883456));
#39036=CARTESIAN_POINT('Ctrl Pts',(370.218093623182,-19.5395308124168,3.16334083711164));
#39037=CARTESIAN_POINT('Ctrl Pts',(370.27544858307,-19.5358976308321,3.17417345409311));
#39038=CARTESIAN_POINT('Ctrl Pts',(370.314817868995,-19.5333891342309,3.1808538970289));
#39039=CARTESIAN_POINT('Ctrl Pts',(370.517265537148,-19.5204097959917,3.21134797236672));
#39040=CARTESIAN_POINT('Ctrl Pts',(370.681850536276,-19.5095746299259,3.22335504829115));
#39041=CARTESIAN_POINT('Ctrl Pts',(371.005336752247,-19.4878740285333,3.2221210794355));
#39042=CARTESIAN_POINT('Ctrl Pts',(371.163796609833,-19.4770561089891,3.20979035701147));
#39043=CARTESIAN_POINT('Ctrl Pts',(371.431353970829,-19.458913215028,3.16894223643924));
#39044=CARTESIAN_POINT('Ctrl Pts',(371.541063953601,-19.4515146343037,3.14629341435928));
#39045=CARTESIAN_POINT('Ctrl Pts',(371.665391850588,-19.4433339887412,3.11379308502182));
#39046=CARTESIAN_POINT('Ctrl Pts',(371.681368822718,-19.442286697041,3.10948485238336));
#39047=CARTESIAN_POINT('Ctrl Pts',(371.706973835975,-19.4406154671804,3.10236839437006));
#39048=CARTESIAN_POINT('Ctrl Pts',(371.716622951791,-19.4399873184542,3.09963801725236));
#39049=CARTESIAN_POINT('Ctrl Pts',(371.733804595024,-19.4388719425498,3.09468945414974));
#39050=CARTESIAN_POINT('Ctrl Pts',(371.741341938866,-19.4383837318602,3.09248872738467));
#39051=CARTESIAN_POINT('Ctrl Pts',(371.757607141006,-19.4373325908181,3.0876750882068));
#39052=CARTESIAN_POINT('Ctrl Pts',(371.766331991843,-19.4367702142016,3.08505270772787));
#39053=CARTESIAN_POINT('Ctrl Pts',(371.790740739503,-19.4352007158312,3.07760330496356));
#39054=CARTESIAN_POINT('Ctrl Pts',(371.806399314343,-19.4341982812127,3.07269336236137));
#39055=CARTESIAN_POINT('Ctrl Pts',(371.902341188907,-19.4280795719444,3.0418027544764));
#39056=CARTESIAN_POINT('Ctrl Pts',(371.981623171483,-19.4231237218335,3.01279454187252));
#39057=CARTESIAN_POINT('Ctrl Pts',(372.144736803546,-19.4129626901145,2.94573874203487));
#39058=CARTESIAN_POINT('Ctrl Pts',(372.228190025311,-19.4077836670407,2.90717539528309));
#39059=CARTESIAN_POINT('Ctrl Pts',(372.309820886087,-19.4026365087528,2.86513670921865));
#39060=CARTESIAN_POINT('',(367.611568037796,-19.5613959703564,-0.00109071397770461));
#39061=CARTESIAN_POINT('Ctrl Pts',(372.309820613636,-19.1541342831958,2.86513684952685));
#39062=CARTESIAN_POINT('Ctrl Pts',(372.306868563801,-19.154338301629,2.86665711117884));
#39063=CARTESIAN_POINT('Ctrl Pts',(372.303914169137,-19.1545424807628,2.86817280799209));
#39064=CARTESIAN_POINT('Ctrl Pts',(372.286842891529,-19.1557222807326,2.87689760560397));
#39065=CARTESIAN_POINT('Ctrl Pts',(372.272675520473,-19.1567013873833,2.88400693944335));
#39066=CARTESIAN_POINT('Ctrl Pts',(372.234157867628,-19.1593636287487,2.90298108729884));
#39067=CARTESIAN_POINT('Ctrl Pts',(372.209709935956,-19.1610537251766,2.91464368421585));
#39068=CARTESIAN_POINT('Ctrl Pts',(372.077029171251,-19.170229932089,2.97589641095051));
#39069=CARTESIAN_POINT('Ctrl Pts',(371.966270420312,-19.1779090706688,3.01976298846185));
#39070=CARTESIAN_POINT('Ctrl Pts',(371.705181375476,-19.1960434975514,3.10678403213363));
#39071=CARTESIAN_POINT('Ctrl Pts',(371.553629055342,-19.2065994500682,3.14532905088503));
#39072=CARTESIAN_POINT('Ctrl Pts',(371.234911433396,-19.2284994398373,3.20214398956842));
#39073=CARTESIAN_POINT('Ctrl Pts',(371.067871282371,-19.2398114594399,3.21864331106934));
#39074=CARTESIAN_POINT('Ctrl Pts',(370.873352244017,-19.2523116063804,3.22262625248144));
#39075=CARTESIAN_POINT('Ctrl Pts',(370.84640504265,-19.2540280054567,3.22283999864873));
#39076=CARTESIAN_POINT('Ctrl Pts',(370.809127970701,-19.2563783556098,3.22266810737568));
#39077=CARTESIAN_POINT('Ctrl Pts',(370.798798731968,-19.2570270718949,3.22257081525373));
#39078=CARTESIAN_POINT('Ctrl Pts',(370.781061466026,-19.2581364550607,3.22231845366809));
#39079=CARTESIAN_POINT('Ctrl Pts',(370.773653253057,-19.2585984301872,3.22218749742093));
#39080=CARTESIAN_POINT('Ctrl Pts',(370.758146765737,-19.2595624430543,3.22185988928937));
#39081=CARTESIAN_POINT('Ctrl Pts',(370.750048691387,-19.260064181351,3.22165825172853));
#39082=CARTESIAN_POINT('Ctrl Pts',(370.730205278945,-19.2612896335181,3.22108929076979));
#39083=CARTESIAN_POINT('Ctrl Pts',(370.718460878824,-19.2620114885945,3.22068825232257));
#39084=CARTESIAN_POINT('Ctrl Pts',(370.675749817811,-19.2646250284017,3.21899585580073));
#39085=CARTESIAN_POINT('Ctrl Pts',(370.644798918115,-19.2664966826415,3.21732200378132));
#39086=CARTESIAN_POINT('Ctrl Pts',(370.567079628982,-19.2711512312952,3.21199337808265));
#39087=CARTESIAN_POINT('Ctrl Pts',(370.520356822767,-19.2739081608776,3.20776349441411));
#39088=CARTESIAN_POINT('Ctrl Pts',(370.138209401912,-19.2962378896698,3.16473681101626));
#39089=CARTESIAN_POINT('Ctrl Pts',(369.810690838872,-19.3142183830495,3.0744680851715));
#39090=CARTESIAN_POINT('Ctrl Pts',(369.446006032172,-19.3376778537739,2.90906223356186));
#39091=CARTESIAN_POINT('Ctrl Pts',(369.389648081856,-19.3414010942409,2.88148941811556));
#39092=CARTESIAN_POINT('Ctrl Pts',(369.314056166936,-19.3465480431571,2.84173126140242));
#39093=CARTESIAN_POINT('Ctrl Pts',(369.294091585639,-19.3479222816126,2.83096011295208));
#39094=CARTESIAN_POINT('Ctrl Pts',(369.262513704432,-19.3501204585051,2.81349052874243));
#39095=CARTESIAN_POINT('Ctrl Pts',(369.250825385868,-19.3509395157766,2.80692871922191));
#39096=CARTESIAN_POINT('Ctrl Pts',(369.227155683611,-19.3526093862186,2.79344568118483));
#39097=CARTESIAN_POINT('Ctrl Pts',(369.215177269395,-19.3534603533395,2.7865198318835));
#39098=CARTESIAN_POINT('Ctrl Pts',(369.187673174213,-19.3554281337958,2.77037990221073));
#39099=CARTESIAN_POINT('Ctrl Pts',(369.172179690717,-19.3565468800844,2.76111213263311));
#39100=CARTESIAN_POINT('Ctrl Pts',(369.139744408855,-19.3589109716653,2.74133831938517));
#39101=CARTESIAN_POINT('Ctrl Pts',(369.122820633625,-19.3601573102741,2.73080430977802));
#39102=CARTESIAN_POINT('Ctrl Pts',(369.077890326319,-19.3635010200687,2.70225623105007));
#39103=CARTESIAN_POINT('Ctrl Pts',(369.050064021607,-19.3656085054049,2.68396433053046));
#39104=CARTESIAN_POINT('Ctrl Pts',(368.879690998772,-19.3787435614883,2.56814747924556));
#39105=CARTESIAN_POINT('Ctrl Pts',(368.744911698469,-19.3901742471553,2.45973866842112));
#39106=CARTESIAN_POINT('Ctrl Pts',(368.466698470098,-19.415961837233,2.19652714471642));
#39107=CARTESIAN_POINT('Ctrl Pts',(368.328429068574,-19.4303616533602,2.03737099911767));
#39108=CARTESIAN_POINT('Ctrl Pts',(368.179494482557,-19.447138021473,1.82762972744126));
#39109=CARTESIAN_POINT('Ctrl Pts',(368.153174945853,-19.4501592887267,1.78879590508509));
#39110=CARTESIAN_POINT('Ctrl Pts',(368.119978809347,-19.4540320448328,1.73743604769735));
#39111=CARTESIAN_POINT('Ctrl Pts',(368.112325789226,-19.4549294039006,1.72542159660882));
#39112=CARTESIAN_POINT('Ctrl Pts',(368.100159844046,-19.4563627899728,1.70603990841662));
#39113=CARTESIAN_POINT('Ctrl Pts',(368.095596544341,-19.4569020230972,1.69870473734099));
#39114=CARTESIAN_POINT('Ctrl Pts',(368.086871297713,-19.4579360016838,1.68455298847506));
#39115=CARTESIAN_POINT('Ctrl Pts',(368.08270515164,-19.4584310055976,1.67773921928313));
#39116=CARTESIAN_POINT('Ctrl Pts',(368.072792092752,-19.459612108242,1.66139007581286));
#39117=CARTESIAN_POINT('Ctrl Pts',(368.067069116106,-19.4602966600066,1.6518401693799));
#39118=CARTESIAN_POINT('Ctrl Pts',(368.047620411075,-19.4626329618374,1.6190014439291));
#39119=CARTESIAN_POINT('Ctrl Pts',(368.034137851771,-19.4642698374452,1.59556898258199));
#39120=CARTESIAN_POINT('Ctrl Pts',(368.001899206718,-19.468233904188,1.53787119067329));
#39121=CARTESIAN_POINT('Ctrl Pts',(367.983467789884,-19.4705439558542,1.50342853917158));
#39122=CARTESIAN_POINT('Ctrl Pts',(367.91124321529,-19.4798137931502,1.36235610529661));
#39123=CARTESIAN_POINT('Ctrl Pts',(367.86276681526,-19.4865572697705,1.25310337091742));
#39124=CARTESIAN_POINT('Ctrl Pts',(367.738655482965,-19.5062050327462,0.925390214173588));
#39125=CARTESIAN_POINT('Ctrl Pts',(367.680312770581,-19.5189718213504,0.701224908475511));
#39126=CARTESIAN_POINT('Ctrl Pts',(367.637213578117,-19.5361834239919,0.410597412293125));
#39127=CARTESIAN_POINT('Ctrl Pts',(367.629816262804,-19.5399128189062,0.348187819863735));
#39128=CARTESIAN_POINT('Ctrl Pts',(367.622238257198,-19.5450658167484,0.263014439344415));
#39129=CARTESIAN_POINT('Ctrl Pts',(367.620466919147,-19.5464397530616,0.240403951145996));
#39130=CARTESIAN_POINT('Ctrl Pts',(367.618028679303,-19.5486375673944,0.204404405759115));
#39131=CARTESIAN_POINT('Ctrl Pts',(367.617206395823,-19.5494565672057,0.191026368648337));
#39132=CARTESIAN_POINT('Ctrl Pts',(367.615724633287,-19.5511044386181,0.164185626947726));
#39133=CARTESIAN_POINT('Ctrl Pts',(367.615066113935,-19.5519333231276,0.150723142999138));
#39134=CARTESIAN_POINT('Ctrl Pts',(367.613908855636,-19.5536096990944,0.123575763942133));
#39135=CARTESIAN_POINT('Ctrl Pts',(367.613412851242,-19.5544572586867,0.109891037489478));
#39136=CARTESIAN_POINT('Ctrl Pts',(367.612530157003,-19.5562933996043,0.0803346467455371));
#39137=CARTESIAN_POINT('Ctrl Pts',(367.612173507387,-19.557282899167,0.0644625091245308));
#39138=CARTESIAN_POINT('Ctrl Pts',(367.61168447067,-19.5593120843888,0.032029723451429));
#39139=CARTESIAN_POINT('Ctrl Pts',(367.611562433136,-19.5603520594605,0.0154694610957346));
#39140=CARTESIAN_POINT('Ctrl Pts',(367.611568037796,-19.5613959703564,-0.00109071397770461));
#39141=CARTESIAN_POINT('Ctrl Pts',(367.61156803705,-19.5613958313854,-0.00108850939768229));
#39142=CARTESIAN_POINT('Ctrl Pts',(367.611585009097,-19.5645634070565,-0.0513376498611552));
#39143=CARTESIAN_POINT('Ctrl Pts',(367.612777200739,-19.5677668500842,-0.10157770103759));
#39144=CARTESIAN_POINT('Ctrl Pts',(367.626998441497,-19.5872241200623,-0.403227078336578));
#39145=CARTESIAN_POINT('Ctrl Pts',(367.66827534513,-19.6043279925662,-0.652401396010281));
#39146=CARTESIAN_POINT('Ctrl Pts',(367.7786981762,-19.6311772852115,-1.03475273693346));
#39147=CARTESIAN_POINT('Ctrl Pts',(367.828824469343,-19.6409513883906,-1.17240952248012));
#39148=CARTESIAN_POINT('Ctrl Pts',(367.895565317816,-19.651433745654,-1.32294626623134));
#39149=CARTESIAN_POINT('Ctrl Pts',(367.903134556563,-19.6525926603946,-1.33963345938175));
#39150=CARTESIAN_POINT('Ctrl Pts',(367.914852287953,-19.6543411352039,-1.36489157306516));
#39151=CARTESIAN_POINT('Ctrl Pts',(367.918896975249,-19.6549367151184,-1.37350984807355));
#39152=CARTESIAN_POINT('Ctrl Pts',(367.926336632082,-19.6560176775914,-1.38918106995364));
#39153=CARTESIAN_POINT('Ctrl Pts',(367.929719120598,-19.6565037901847,-1.39623960441441));
#39154=CARTESIAN_POINT('Ctrl Pts',(367.937348660056,-19.6575883984911,-1.41201311537138));
#39155=CARTESIAN_POINT('Ctrl Pts',(367.941609331193,-19.6581860431998,-1.42072128034461));
#39156=CARTESIAN_POINT('Ctrl Pts',(367.954150849471,-19.6599223661703,-1.44606392042762));
#39157=CARTESIAN_POINT('Ctrl Pts',(367.962536500583,-19.6610547756491,-1.46264648198441));
#39158=CARTESIAN_POINT('Ctrl Pts',(368.036875327732,-19.6708570192796,-1.60654667233671));
#39159=CARTESIAN_POINT('Ctrl Pts',(368.111122418866,-19.6790616618526,-1.72942007047729));
#39160=CARTESIAN_POINT('Ctrl Pts',(368.35406351278,-19.7029510255846,-2.07680744285875));
#39161=CARTESIAN_POINT('Ctrl Pts',(368.544113137892,-19.7182955623904,-2.284676478965));
#39162=CARTESIAN_POINT('Ctrl Pts',(368.783521402744,-19.7368044940429,-2.48624352627725));
#39163=CARTESIAN_POINT('Ctrl Pts',(368.808687217269,-19.7387395349292,-2.50678945455595));
#39164=CARTESIAN_POINT('Ctrl Pts',(368.849531102628,-19.7418662105282,-2.5391186427375));
#39165=CARTESIAN_POINT('Ctrl Pts',(368.865013959996,-19.7430483310722,-2.5511456402404));
#39166=CARTESIAN_POINT('Ctrl Pts',(368.894571255231,-19.7452997871051,-2.57367617952947));
#39167=CARTESIAN_POINT('Ctrl Pts',(368.908623734446,-19.7463679930637,-2.58420743816429));
#39168=CARTESIAN_POINT('Ctrl Pts',(368.923020921186,-19.747460375822,-2.59481438719899));
#39169=CARTESIAN_POINT('Ctrl Pts',(368.923280502528,-19.7474800708206,-2.59500557045182));
#39170=CARTESIAN_POINT('Ctrl Pts',(368.923802633112,-19.7475196846589,-2.59539000200284));
#39171=CARTESIAN_POINT('Ctrl Pts',(368.924065183248,-19.7475396035514,-2.59558324960454));
#39172=CARTESIAN_POINT('Ctrl Pts',(368.924443840134,-19.7475683301349,-2.5958618679334));
#39173=CARTESIAN_POINT('Ctrl Pts',(368.924559923217,-19.7475771365773,-2.59594727065917));
#39174=CARTESIAN_POINT('Ctrl Pts',(368.924800958579,-19.7475954220328,-2.59612457629137));
#39175=CARTESIAN_POINT('Ctrl Pts',(368.924925911978,-19.7476049011099,-2.59621647812081));
#39176=CARTESIAN_POINT('Ctrl Pts',(368.925185691327,-19.7476246078851,-2.59640751403123));
#39177=CARTESIAN_POINT('Ctrl Pts',(368.925320517877,-19.7476348356036,-2.59650664627378));
#39178=CARTESIAN_POINT('Ctrl Pts',(368.925601203812,-19.7476561276013,-2.59671298905518));
#39179=CARTESIAN_POINT('Ctrl Pts',(368.925747065573,-19.7476671920303,-2.59682019858774));
#39180=CARTESIAN_POINT('Ctrl Pts',(368.926051182247,-19.747690260543,-2.59704368725327));
#39181=CARTESIAN_POINT('Ctrl Pts',(368.926209438383,-19.7477022646824,-2.59715996393718));
#39182=CARTESIAN_POINT('Ctrl Pts',(368.926539942212,-19.7477273337446,-2.59740275090876));
#39183=CARTESIAN_POINT('Ctrl Pts',(368.926712191508,-19.7477403987438,-2.59752925826852));
#39184=CARTESIAN_POINT('Ctrl Pts',(368.937671468353,-19.7485716344314,-2.60557654887377));
#39185=CARTESIAN_POINT('Ctrl Pts',(368.94850758579,-19.7493923913792,-2.61342998528496));
#39186=CARTESIAN_POINT('Ctrl Pts',(368.97216676901,-19.7511821096357,-2.6303531296322));
#39187=CARTESIAN_POINT('Ctrl Pts',(368.98500780431,-19.7521520344117,-2.63939700993301));
#39188=CARTESIAN_POINT('Ctrl Pts',(369.019627670078,-19.7547634145558,-2.66340294915108));
#39189=CARTESIAN_POINT('Ctrl Pts',(369.0415248915,-19.7564113849455,-2.6781913785143));
#39190=CARTESIAN_POINT('Ctrl Pts',(369.143440881046,-19.7640661878629,-2.74521102102542));
#39191=CARTESIAN_POINT('Ctrl Pts',(369.225568902198,-19.7701937221241,-2.79413175576221));
#39192=CARTESIAN_POINT('Ctrl Pts',(369.527797089775,-19.7926043616879,-2.95641298873467));
#39193=CARTESIAN_POINT('Ctrl Pts',(369.758600723709,-19.8095442447405,-3.04797974859762));
#39194=CARTESIAN_POINT('Ctrl Pts',(370.109681646012,-19.8339313546563,-3.14237161758454));
#39195=CARTESIAN_POINT('Ctrl Pts',(370.223360936712,-19.841611452251,-3.16643877024317));
#39196=CARTESIAN_POINT('Ctrl Pts',(370.355541697904,-19.8501205690991,-3.18703662900512));
#39197=CARTESIAN_POINT('Ctrl Pts',(370.373003618394,-19.851236254454,-3.18961099367103));
#39198=CARTESIAN_POINT('Ctrl Pts',(370.39977619719,-19.8529330309967,-3.19333353771929));
#39199=CARTESIAN_POINT('Ctrl Pts',(370.409071869014,-19.8535196267109,-3.19458469790623));
#39200=CARTESIAN_POINT('Ctrl Pts',(370.426139965871,-19.8545918716988,-3.19680617528343));
#39201=CARTESIAN_POINT('Ctrl Pts',(370.433910469346,-19.8550781785161,-3.19778874215249));
#39202=CARTESIAN_POINT('Ctrl Pts',(370.451464628769,-19.8561726547757,-3.19994344609137));
#39203=CARTESIAN_POINT('Ctrl Pts',(370.461250115588,-19.8567798945841,-3.20109904857294));
#39204=CARTESIAN_POINT('Ctrl Pts',(370.486534691424,-19.8583418772711,-3.20396747517877));
#39205=CARTESIAN_POINT('Ctrl Pts',(370.5020413892,-19.8592929828154,-3.20561274691841));
#39206=CARTESIAN_POINT('Ctrl Pts',(370.603799126536,-19.8654930779212,-3.21566298835883));
#39207=CARTESIAN_POINT('Ctrl Pts',(370.690355141666,-19.8705732047546,-3.22069943406989));
#39208=CARTESIAN_POINT('Ctrl Pts',(371.063649729496,-19.8920464373321,-3.22733777508927));
#39209=CARTESIAN_POINT('Ctrl Pts',(371.349684506944,-19.9075115236879,-3.19416930597227));
#39210=CARTESIAN_POINT('Ctrl Pts',(371.71432318891,-19.9292753464472,-3.10156718149705));
#39211=CARTESIAN_POINT('Ctrl Pts',(371.800110644108,-19.9345406849459,-3.07593409277145));
#39212=CARTESIAN_POINT('Ctrl Pts',(371.908227008078,-19.9414178771559,-3.03866010010499));
#39213=CARTESIAN_POINT('Ctrl Pts',(371.931643750064,-19.9429220731663,-3.03028247859762));
#39214=CARTESIAN_POINT('Ctrl Pts',(371.969368109949,-19.9453702030028,-3.01629153130544));
#39215=CARTESIAN_POINT('Ctrl Pts',(371.983736922314,-19.9463085617691,-3.01084530952918));
#39216=CARTESIAN_POINT('Ctrl Pts',(372.011204387882,-19.9481138993346,-3.00020901717105));
#39217=CARTESIAN_POINT('Ctrl Pts',(372.024309058994,-19.9489803094843,-2.99503538916531));
#39218=CARTESIAN_POINT('Ctrl Pts',(372.054163799418,-19.9509659881961,-2.9830220864592));
#39219=CARTESIAN_POINT('Ctrl Pts',(372.070890922978,-19.9520871066675,-2.97612700040191));
#39220=CARTESIAN_POINT('Ctrl Pts',(372.123555899257,-19.9556445835641,-2.9538973367222));
#39221=CARTESIAN_POINT('Ctrl Pts',(372.159272326135,-19.9580982242592,-2.93805031346501));
#39222=CARTESIAN_POINT('Ctrl Pts',(372.433251001694,-19.9772472490339,-2.81047691871032));
#39223=CARTESIAN_POINT('Ctrl Pts',(372.657266714198,-19.9949613950613,-2.67061301510547));
#39224=CARTESIAN_POINT('Ctrl Pts',(372.955891055772,-20.0209421681235,-2.4289324677483));
#39225=CARTESIAN_POINT('Ctrl Pts',(373.045670720648,-20.029108080863,-2.34748967144073));
#39226=CARTESIAN_POINT('Ctrl Pts',(373.158292218291,-20.0396443879272,-2.23311711524096));
#39227=CARTESIAN_POINT('Ctrl Pts',(373.185411852564,-20.0422058564334,-2.20454670814433));
#39228=CARTESIAN_POINT('Ctrl Pts',(373.230365388343,-20.0464831161929,-2.15541499266873));
#39229=CARTESIAN_POINT('Ctrl Pts',(373.248474554539,-20.0482151911012,-2.13511243647799));
#39230=CARTESIAN_POINT('Ctrl Pts',(373.273648468843,-20.0506328592559,-2.10615960508946));
#39231=CARTESIAN_POINT('Ctrl Pts',(373.280928112895,-20.051333181227,-2.09769882975));
#39232=CARTESIAN_POINT('Ctrl Pts',(373.293344167969,-20.0525294442645,-2.08311569631408));
#39233=CARTESIAN_POINT('Ctrl Pts',(373.298501995548,-20.0530269298298,-2.07701178116447));
#39234=CARTESIAN_POINT('Ctrl Pts',(373.308492631924,-20.0539915173376,-2.0650989859083));
#39235=CARTESIAN_POINT('Ctrl Pts',(373.31332774562,-20.0544588028548,-2.0592922602964));
#39236=CARTESIAN_POINT('Ctrl Pts',(373.326501800481,-20.055733430506,-2.04335725019007));
#39237=CARTESIAN_POINT('Ctrl Pts',(373.334799496513,-20.0565378408961,-2.03319483672731));
#39238=CARTESIAN_POINT('Ctrl Pts',(373.366790327903,-20.0596466179166,-1.99352273093183));
#39239=CARTESIAN_POINT('Ctrl Pts',(373.390026032369,-20.0619207088804,-1.96364602190412));
#39240=CARTESIAN_POINT('Ctrl Pts',(373.543470241788,-20.0771022234632,-1.75900670530429));
#39241=CARTESIAN_POINT('Ctrl Pts',(373.656202001614,-20.0891068632888,-1.57181541419065));
#39242=CARTESIAN_POINT('Ctrl Pts',(373.835241957669,-20.1126175572737,-1.19217400150092));
#39243=CARTESIAN_POINT('Ctrl Pts',(373.903964903389,-20.1240487436974,-1.00203633652997));
#39244=CARTESIAN_POINT('Ctrl Pts',(373.962489932576,-20.138023789715,-0.775683997800598));
#39245=CARTESIAN_POINT('Ctrl Pts',(373.970054333592,-20.1399549687382,-0.744515168821039));
#39246=CARTESIAN_POINT('Ctrl Pts',(373.980895132226,-20.1429272757765,-0.696746032019548));
#39247=CARTESIAN_POINT('Ctrl Pts',(373.984508224294,-20.1439576168608,-0.680223650647294));
#39248=CARTESIAN_POINT('Ctrl Pts',(373.990584454607,-20.1457624449378,-0.651350364426154));
#39249=CARTESIAN_POINT('Ctrl Pts',(373.993105578386,-20.1465350601005,-0.639011937670078));
#39250=CARTESIAN_POINT('Ctrl Pts',(373.998630227968,-20.1482834177722,-0.61114236534025));
#39251=CARTESIAN_POINT('Ctrl Pts',(374.001591831354,-20.1492604753915,-0.595603331819884));
#39252=CARTESIAN_POINT('Ctrl Pts',(374.009287361599,-20.1519113522302,-0.553544815837882));
#39253=CARTESIAN_POINT('Ctrl Pts',(374.013803291285,-20.1535920322722,-0.526987211053909));
#39254=CARTESIAN_POINT('Ctrl Pts',(374.033834216395,-20.1616918993334,-0.399539619430839));
#39255=CARTESIAN_POINT('Ctrl Pts',(374.044881567072,-20.1682498748797,-0.298016500369266));
#39256=CARTESIAN_POINT('Ctrl Pts',(374.052182099146,-20.1761072188326,-0.178290132968703));
#39257=CARTESIAN_POINT('Ctrl Pts',(374.053122306004,-20.1772829238742,-0.160423048926655));
#39258=CARTESIAN_POINT('Ctrl Pts',(374.064047482659,-20.1935617809217,0.0863312633924986));
#39259=CARTESIAN_POINT('Ctrl Pts',(374.049744285065,-20.2092512515646,0.315631722763584));
#39260=CARTESIAN_POINT('Ctrl Pts',(373.99880818053,-20.2295533026651,0.614500249161861));
#39261=CARTESIAN_POINT('Ctrl Pts',(373.983840463085,-20.2344675414593,0.687108649114254));
#39262=CARTESIAN_POINT('Ctrl Pts',(373.959583204317,-20.2411624303431,0.787189303701725));
#39263=CARTESIAN_POINT('Ctrl Pts',(373.952408095704,-20.2430239041147,0.815146536385452));
#39264=CARTESIAN_POINT('Ctrl Pts',(373.93924937225,-20.2462371288764,0.863699936251745));
#39265=CARTESIAN_POINT('Ctrl Pts',(373.933434039182,-20.2475968030059,0.88433943766575));
#39266=CARTESIAN_POINT('Ctrl Pts',(373.924565255301,-20.2495830654088,0.914653711071972));
#39267=CARTESIAN_POINT('Ctrl Pts',(373.921671569227,-20.2502183283875,0.924374088810376));
#39268=CARTESIAN_POINT('Ctrl Pts',(373.916456119987,-20.2513407275249,0.94159594525245));
#39269=CARTESIAN_POINT('Ctrl Pts',(373.914152775887,-20.2518289056371,0.949102772740537));
#39270=CARTESIAN_POINT('Ctrl Pts',(373.909103105037,-20.2528830239978,0.965348184213942));
#39271=CARTESIAN_POINT('Ctrl Pts',(373.906346953022,-20.253448386996,0.974083505853382));
#39272=CARTESIAN_POINT('Ctrl Pts',(373.89862162327,-20.2550061329951,0.998209153985737));
#39273=CARTESIAN_POINT('Ctrl Pts',(373.89357370679,-20.2559940490821,1.0135742486666));
#39274=CARTESIAN_POINT('Ctrl Pts',(373.865786598802,-20.2612779666433,1.09605486608285));
#39275=CARTESIAN_POINT('Ctrl Pts',(373.840952392484,-20.2654626067173,1.16244973322412));
#39276=CARTESIAN_POINT('Ctrl Pts',(373.727204371436,-20.2827778366572,1.43845409343994));
#39277=CARTESIAN_POINT('Ctrl Pts',(373.618399207126,-20.2952104635624,1.63916107061131));
#39278=CARTESIAN_POINT('Ctrl Pts',(373.399719065697,-20.317000973493,1.95699615120404));
#39279=CARTESIAN_POINT('Ctrl Pts',(373.300643129428,-20.3260984230423,2.0804681736899));
#39280=CARTESIAN_POINT('Ctrl Pts',(373.173155089046,-20.3373085061491,2.21738557800843));
#39281=CARTESIAN_POINT('Ctrl Pts',(373.153109544783,-20.3390576450781,2.23833943479634));
#39282=CARTESIAN_POINT('Ctrl Pts',(373.121383707644,-20.3418068997686,2.27061927087443));
#39283=CARTESIAN_POINT('Ctrl Pts',(373.109895474686,-20.3427986333407,2.28213246094062));
#39284=CARTESIAN_POINT('Ctrl Pts',(373.089388160715,-20.3445625464153,2.30237551450739));
#39285=CARTESIAN_POINT('Ctrl Pts',(373.080404241571,-20.345333151517,2.31114063409223));
#39286=CARTESIAN_POINT('Ctrl Pts',(373.059580003881,-20.3471146207233,2.33122160263012));
#39287=CARTESIAN_POINT('Ctrl Pts',(373.047704245605,-20.3481270768203,2.34250004523115));
#39288=CARTESIAN_POINT('Ctrl Pts',(373.014763623252,-20.3509261840192,2.37330971176742));
#39289=CARTESIAN_POINT('Ctrl Pts',(372.993523188709,-20.3527208692228,2.39265019954587));
#39290=CARTESIAN_POINT('Ctrl Pts',(372.870477583172,-20.3630624541511,2.50171657938173));
#39291=CARTESIAN_POINT('Ctrl Pts',(372.763357000183,-20.3718623029062,2.58521409458497));
#39292=CARTESIAN_POINT('Ctrl Pts',(372.541704365468,-20.3896579703631,2.7365231665723));
#39293=CARTESIAN_POINT('Ctrl Pts',(372.427652359241,-20.398622957923,2.80445528357387));
#39294=CARTESIAN_POINT('Ctrl Pts',(372.309820109182,-20.4075893673377,2.8651371093129));
#39295=CARTESIAN_POINT('Origin',(370.834317853224,2.31077344927308,0.));
#39296=CARTESIAN_POINT('',(372.30982061585,-21.9062759889522,2.86513684838664));
#39297=CARTESIAN_POINT('',(372.309820475366,-21.6596622257337,2.86513692073375));
#39298=CARTESIAN_POINT('',(372.309820613641,2.31077344927308,2.86513684952399));
#39299=CARTESIAN_POINT('',(367.611568348902,-21.0592932850034,0.00244209184973706));
#39300=CARTESIAN_POINT('Ctrl Pts',(372.30982061585,-21.9062759889522,2.86513684838664));
#39301=CARTESIAN_POINT('Ctrl Pts',(372.382893739272,-21.9009851307799,2.82750527921983));
#39302=CARTESIAN_POINT('Ctrl Pts',(372.454498104907,-21.8956052014087,2.78709322077374));
#39303=CARTESIAN_POINT('Ctrl Pts',(372.643036039748,-21.8809245436686,2.67096329734966));
#39304=CARTESIAN_POINT('Ctrl Pts',(372.756730764924,-21.8715042487675,2.59033412028013));
#39305=CARTESIAN_POINT('Ctrl Pts',(372.992754913673,-21.8509453041641,2.39883245921991));
#39306=CARTESIAN_POINT('Ctrl Pts',(373.112529794808,-21.8398349848028,2.28539020326298));
#39307=CARTESIAN_POINT('Ctrl Pts',(373.241267734201,-21.8275119410745,2.14323148975206));
#39308=CARTESIAN_POINT('Ctrl Pts',(373.259168824634,-21.825789189413,2.12295709471688));
#39309=CARTESIAN_POINT('Ctrl Pts',(373.283557373645,-21.8234320747738,2.09462411971231));
#39310=CARTESIAN_POINT('Ctrl Pts',(373.290263880839,-21.8227828268609,2.08675670540548));
#39311=CARTESIAN_POINT('Ctrl Pts',(373.301711062041,-21.8216729911173,2.07319637109261));
#39312=CARTESIAN_POINT('Ctrl Pts',(373.306470127899,-21.821211090369,2.06751918333684));
#39313=CARTESIAN_POINT('Ctrl Pts',(373.316385616803,-21.8202477730655,2.05560760685672));
#39314=CARTESIAN_POINT('Ctrl Pts',(373.32153819584,-21.8197466524052,2.04937014357779));
#39315=CARTESIAN_POINT('Ctrl Pts',(373.334098144096,-21.8185236280619,2.03404853617821));
#39316=CARTESIAN_POINT('Ctrl Pts',(373.341479639451,-21.8178035696857,2.02494314431389));
#39317=CARTESIAN_POINT('Ctrl Pts',(373.36809420745,-21.8152018021794,1.99174429399388));
#39318=CARTESIAN_POINT('Ctrl Pts',(373.387031673304,-21.8133398976859,1.9674146125055));
#39319=CARTESIAN_POINT('Ctrl Pts',(373.433696964172,-21.8087140916263,1.9056535049467));
#39320=CARTESIAN_POINT('Ctrl Pts',(373.460968504656,-21.8059757569823,1.86788485355934));
#39321=CARTESIAN_POINT('Ctrl Pts',(373.674415499764,-21.7841374308493,1.55835553292629));
#39322=CARTESIAN_POINT('Ctrl Pts',(373.818745390186,-21.7665685501627,1.26010196384501));
#39323=CARTESIAN_POINT('Ctrl Pts',(373.935770583654,-21.743276557568,0.87860648371622));
#39324=CARTESIAN_POINT('Ctrl Pts',(373.954014280031,-21.7391577740338,0.81145027923866));
#39325=CARTESIAN_POINT('Ctrl Pts',(373.975514623449,-21.7335486833004,0.720803071599567));
#39326=CARTESIAN_POINT('Ctrl Pts',(373.980707263015,-21.7321203770548,0.697787828764224));
#39327=CARTESIAN_POINT('Ctrl Pts',(373.988803968052,-21.729765840041,0.659971473455969));
#39328=CARTESIAN_POINT('Ctrl Pts',(373.99185771668,-21.728844413903,0.645203063365475));
#39329=CARTESIAN_POINT('Ctrl Pts',(373.997580810329,-21.7270503467114,0.616511155613441));
#39330=CARTESIAN_POINT('Ctrl Pts',(374.000262160511,-21.7261781116167,0.602590386367526));
#39331=CARTESIAN_POINT('Ctrl Pts',(374.006329523518,-21.7241274254506,0.569931657583617));
#39332=CARTESIAN_POINT('Ctrl Pts',(374.009641460587,-21.7229466497956,0.551180636789482));
#39333=CARTESIAN_POINT('Ctrl Pts',(374.019939258384,-21.7190636850927,0.489702182951094));
#39334=CARTESIAN_POINT('Ctrl Pts',(374.026230077136,-21.7163397283381,0.446864663107874));
#39335=CARTESIAN_POINT('Ctrl Pts',(374.039106885686,-21.7098118446127,0.344933548992318));
#39336=CARTESIAN_POINT('Ctrl Pts',(374.044924051041,-21.7059854387018,0.285760423490181));
#39337=CARTESIAN_POINT('Ctrl Pts',(374.061138257654,-21.6909603051318,0.0555898186995252));
#39338=CARTESIAN_POINT('Ctrl Pts',(374.059531536481,-21.6794413151913,-0.11595420880175));
#39339=CARTESIAN_POINT('Ctrl Pts',(374.027741857847,-21.6552554987378,-0.472081490288715));
#39340=CARTESIAN_POINT('Ctrl Pts',(373.995122248821,-21.6426216504934,-0.655854882085085));
#39341=CARTESIAN_POINT('Ctrl Pts',(373.939868985894,-21.6289359167833,-0.861617495075068));
#39342=CARTESIAN_POINT('Ctrl Pts',(373.93261301436,-21.6272329183293,-0.887355479899007));
#39343=CARTESIAN_POINT('Ctrl Pts',(373.922120499917,-21.624897879142,-0.922875061892184));
#39344=CARTESIAN_POINT('Ctrl Pts',(373.919156382567,-21.6242513141715,-0.932735128224145));
#39345=CARTESIAN_POINT('Ctrl Pts',(373.913981590629,-21.6231448559065,-0.949654432522006));
#39346=CARTESIAN_POINT('Ctrl Pts',(373.911793792372,-21.6226836669908,-0.95672050426103));
#39347=CARTESIAN_POINT('Ctrl Pts',(373.907159147995,-21.6217204478724,-0.971508908189923));
#39348=CARTESIAN_POINT('Ctrl Pts',(373.904707487191,-21.6212187214428,-0.979229635483536));
#39349=CARTESIAN_POINT('Ctrl Pts',(373.898621306252,-21.6199919345615,-0.998148544096804));
#39350=CARTESIAN_POINT('Ctrl Pts',(373.894954439373,-21.6192687460855,-1.00933634920738));
#39351=CARTESIAN_POINT('Ctrl Pts',(373.881353361476,-21.6166426321991,-1.05007822699854));
#39352=CARTESIAN_POINT('Ctrl Pts',(373.871051368315,-21.6147600002147,-1.07950886690085));
#39353=CARTESIAN_POINT('Ctrl Pts',(373.844051325317,-21.6100718599456,-1.153195077101));
#39354=CARTESIAN_POINT('Ctrl Pts',(373.826802764311,-21.6072928093812,-1.19724223146323));
#39355=CARTESIAN_POINT('Ctrl Pts',(373.743840534152,-21.5947860480074,-1.39609232393525));
#39356=CARTESIAN_POINT('Ctrl Pts',(373.667038647829,-21.5854568700873,-1.54599383128619));
#39357=CARTESIAN_POINT('Ctrl Pts',(373.474834770935,-21.5649387033559,-1.85827679800381));
#39358=CARTESIAN_POINT('Ctrl Pts',(373.355403183912,-21.5537459110768,-2.01733453960356));
#39359=CARTESIAN_POINT('Ctrl Pts',(373.194022509707,-21.5394817795497,-2.1953724807785));
#39360=CARTESIAN_POINT('Ctrl Pts',(373.165337585478,-21.5369761814856,-2.22580618226301));
#39361=CARTESIAN_POINT('Ctrl Pts',(373.123066223026,-21.5333209376364,-2.26894107782471));
#39362=CARTESIAN_POINT('Ctrl Pts',(373.109948608228,-21.5321916293128,-2.28209714065851));
#39363=CARTESIAN_POINT('Ctrl Pts',(373.086637466069,-21.5301930227709,-2.30507576610511));
#39364=CARTESIAN_POINT('Ctrl Pts',(373.07649151796,-21.5293258519542,-2.314946041049));
#39365=CARTESIAN_POINT('Ctrl Pts',(373.05536479639,-21.527525521149,-2.33522954834881));
#39366=CARTESIAN_POINT('Ctrl Pts',(373.044375059447,-21.5265919654709,-2.34563289966435));
#39367=CARTESIAN_POINT('Ctrl Pts',(373.015889384619,-21.5241794408812,-2.37222074242629));
#39368=CARTESIAN_POINT('Ctrl Pts',(372.998286686673,-21.5226955807195,-2.38828901857445));
#39369=CARTESIAN_POINT('Ctrl Pts',(372.921664932002,-21.5162649514294,-2.45668913343389));
#39370=CARTESIAN_POINT('Ctrl Pts',(372.860917992413,-21.5112371224128,-2.50703599290373));
#39371=CARTESIAN_POINT('Ctrl Pts',(372.688807686359,-21.4971721451186,-2.63933487575649));
#39372=CARTESIAN_POINT('Ctrl Pts',(372.573931444021,-21.4879731843749,-2.71642388056084));
#39373=CARTESIAN_POINT('Ctrl Pts',(372.265505218993,-21.4639351193716,-2.89579112272621));
#39374=CARTESIAN_POINT('Ctrl Pts',(372.065839911069,-21.4489636306048,-2.98617912766259));
#39375=CARTESIAN_POINT('Ctrl Pts',(371.823438085971,-21.4324033428029,-3.06743059300092));
#39376=CARTESIAN_POINT('Ctrl Pts',(371.788119572725,-21.4300299111857,-3.07859575624792));
#39377=CARTESIAN_POINT('Ctrl Pts',(371.740151602604,-21.4268666415602,-3.09285496532919));
#39378=CARTESIAN_POINT('Ctrl Pts',(371.727665915429,-21.4260487326176,-3.09648443743946));
#39379=CARTESIAN_POINT('Ctrl Pts',(371.70791578232,-21.4247639375077,-3.10209621234038));
#39380=CARTESIAN_POINT('Ctrl Pts',(371.700665929133,-21.4242942225412,-3.10412874514725));
#39381=CARTESIAN_POINT('Ctrl Pts',(371.685700193208,-21.4233286217651,-3.10826794920499));
#39382=CARTESIAN_POINT('Ctrl Pts',(371.677983541762,-21.4228329515048,-3.11037131866956));
#39383=CARTESIAN_POINT('Ctrl Pts',(371.659416643566,-21.4216454903862,-3.11535801908702));
#39384=CARTESIAN_POINT('Ctrl Pts',(371.648558882816,-21.4209552947868,-3.11821345570626));
#39385=CARTESIAN_POINT('Ctrl Pts',(371.610921949337,-21.4185767153969,-3.12790144183443));
#39386=CARTESIAN_POINT('Ctrl Pts',(371.584069128766,-21.4169039483204,-3.13444644125051));
#39387=CARTESIAN_POINT('Ctrl Pts',(371.517929230512,-21.4128358232616,-3.14966847619807));
#39388=CARTESIAN_POINT('Ctrl Pts',(371.478556738527,-21.4104588124242,-3.15795702530659));
#39389=CARTESIAN_POINT('Ctrl Pts',(371.315701905379,-21.4007722869956,-3.18906785778866));
#39390=CARTESIAN_POINT('Ctrl Pts',(371.191085156325,-21.3936997307683,-3.20540264040855));
#39391=CARTESIAN_POINT('Ctrl Pts',(370.810274280389,-21.3723146336441,-3.23282918036115));
#39392=CARTESIAN_POINT('Ctrl Pts',(370.553470253751,-21.3581235225349,-3.22069446487603));
#39393=CARTESIAN_POINT('Ctrl Pts',(370.261634682643,-21.3405327747065,-3.17170779038807));
#39394=CARTESIAN_POINT('Ctrl Pts',(370.222575659103,-21.3381497694521,-3.16440635836082));
#39395=CARTESIAN_POINT('Ctrl Pts',(370.16583240598,-21.334641606644,-3.15270934337757));
#39396=CARTESIAN_POINT('Ctrl Pts',(370.148033716792,-21.3335345274922,-3.14888282728821));
#39397=CARTESIAN_POINT('Ctrl Pts',(370.116512346005,-21.3315616330043,-3.14182614687594));
#39398=CARTESIAN_POINT('Ctrl Pts',(370.102776540251,-21.3306977695544,-3.13865633366134));
#39399=CARTESIAN_POINT('Ctrl Pts',(370.074182053584,-21.3288905632669,-3.13185967997858));
#39400=CARTESIAN_POINT('Ctrl Pts',(370.059327540076,-21.3279467293159,-3.12821698266401));
#39401=CARTESIAN_POINT('Ctrl Pts',(370.020673401817,-21.3254773557378,-3.11844580493747));
#39402=CARTESIAN_POINT('Ctrl Pts',(369.996917305815,-21.323946476853,-3.11215067133646));
#39403=CARTESIAN_POINT('Ctrl Pts',(369.889954933388,-21.316992183378,-3.08249333949358));
#39404=CARTESIAN_POINT('Ctrl Pts',(369.807643391858,-21.3114703644308,-3.05606344806941));
#39405=CARTESIAN_POINT('Ctrl Pts',(369.575826971805,-21.2954197566551,-2.97120554285046));
#39406=CARTESIAN_POINT('Ctrl Pts',(369.429499346165,-21.284664937349,-2.90488153345523));
#39407=CARTESIAN_POINT('Ctrl Pts',(369.11149405211,-21.2601675761501,-2.73107902149694));
#39408=CARTESIAN_POINT('Ctrl Pts',(368.943740585815,-21.2464177428291,-2.61775577757414));
#39409=CARTESIAN_POINT('Ctrl Pts',(368.767527892904,-21.23177269076,-2.47288862052929));
#39410=CARTESIAN_POINT('Ctrl Pts',(368.74756646452,-21.2301109829521,-2.4560675096459));
#39411=CARTESIAN_POINT('Ctrl Pts',(368.720093728711,-21.2278228102019,-2.43234000342293));
#39412=CARTESIAN_POINT('Ctrl Pts',(368.712408119311,-21.2271825544836,-2.42563818996595));
#39413=CARTESIAN_POINT('Ctrl Pts',(368.69922169994,-21.226084022486,-2.41402906234032));
#39414=CARTESIAN_POINT('Ctrl Pts',(368.693705733471,-21.2256244910883,-2.40913919335098));
#39415=CARTESIAN_POINT('Ctrl Pts',(368.682144539781,-21.2246614106808,-2.39881921366845));
#39416=CARTESIAN_POINT('Ctrl Pts',(368.676102995784,-21.2241581842561,-2.39338509692603));
#39417=CARTESIAN_POINT('Ctrl Pts',(368.661773560249,-21.2229645668032,-2.38039799008005));
#39418=CARTESIAN_POINT('Ctrl Pts',(368.653504318056,-21.2222757065406,-2.37282439922897));
#39419=CARTESIAN_POINT('Ctrl Pts',(368.624143689053,-21.2198289604591,-2.3456505968525));
#39420=CARTESIAN_POINT('Ctrl Pts',(368.603274947239,-21.218088224308,-2.32581044810955));
#39421=CARTESIAN_POINT('Ctrl Pts',(368.551816569861,-21.2137831490516,-2.2755583292685));
#39422=CARTESIAN_POINT('Ctrl Pts',(368.52156562114,-21.211240699703,-2.2448062901687));
#39423=CARTESIAN_POINT('Ctrl Pts',(368.394585416592,-21.2004690777782,-2.11043009073927));
#39424=CARTESIAN_POINT('Ctrl Pts',(368.304126810216,-21.192534540594,-2.00108687043521));
#39425=CARTESIAN_POINT('Ctrl Pts',(368.084885354961,-21.171584562775,-1.6973371141667));
#39426=CARTESIAN_POINT('Ctrl Pts',(367.969490619708,-21.1585948572441,-1.49435027826096));
#39427=CARTESIAN_POINT('Ctrl Pts',(367.860599430131,-21.1423225627907,-1.24290540008052));
#39428=CARTESIAN_POINT('Ctrl Pts',(367.844953337446,-21.1398532728638,-1.2047882193159));
#39429=CARTESIAN_POINT('Ctrl Pts',(367.823358438197,-21.136241530456,-1.1491658145845));
#39430=CARTESIAN_POINT('Ctrl Pts',(367.816822325723,-21.135118732656,-1.13189195061084));
#39431=CARTESIAN_POINT('Ctrl Pts',(367.80554584632,-21.1331276924466,-1.10129812426441));
#39432=CARTESIAN_POINT('Ctrl Pts',(367.800743940264,-21.1322615258602,-1.08800125591406));
#39433=CARTESIAN_POINT('Ctrl Pts',(367.790968401941,-21.1304593578306,-1.06036411310029));
#39434=CARTESIAN_POINT('Ctrl Pts',(367.786008287192,-21.1295229335788,-1.04601946064155));
#39435=CARTESIAN_POINT('Ctrl Pts',(367.773453935209,-21.1270945200379,-1.0088645146689));
#39436=CARTESIAN_POINT('Ctrl Pts',(367.766013386807,-21.1255975157025,-0.986003643311825));
#39437=CARTESIAN_POINT('Ctrl Pts',(367.734650087054,-21.1190252202562,-0.885846593204056));
#39438=CARTESIAN_POINT('Ctrl Pts',(367.713389119955,-21.1138643575451,-0.807753937092196));
#39439=CARTESIAN_POINT('Ctrl Pts',(367.63939699187,-21.0926491166726,-0.48910608461047));
#39440=CARTESIAN_POINT('Ctrl Pts',(367.611382556567,-21.0758721219843,-0.243702563233693));
#39441=CARTESIAN_POINT('Ctrl Pts',(367.611568775535,-21.05929280343,0.00243818631688326));
#39442=CARTESIAN_POINT('Ctrl Pts',(367.611568778454,-21.0592925437503,0.00244204158639814));
#39443=CARTESIAN_POINT('Ctrl Pts',(367.611670430483,-21.050256619999,0.136591675607924));
#39444=CARTESIAN_POINT('Ctrl Pts',(367.62014819537,-21.0413230654388,0.270622973866999));
#39445=CARTESIAN_POINT('Ctrl Pts',(367.638663870236,-21.0319058275821,0.417250911136126));
#39446=CARTESIAN_POINT('Ctrl Pts',(367.640454036196,-21.0310429050257,0.430739636842257));
#39447=CARTESIAN_POINT('Ctrl Pts',(367.643579511215,-21.0296122624237,0.453198214792116));
#39448=CARTESIAN_POINT('Ctrl Pts',(367.644867327215,-21.0290421005523,0.462174356468439));
#39449=CARTESIAN_POINT('Ctrl Pts',(367.6472756725,-21.0280100508083,0.478471047067952));
#39450=CARTESIAN_POINT('Ctrl Pts',(367.648383576089,-21.0275474804427,0.485793360354128));
#39451=CARTESIAN_POINT('Ctrl Pts',(367.650717386335,-21.0265977187514,0.500866454061022));
#39452=CARTESIAN_POINT('Ctrl Pts',(367.65194634415,-21.0261107391561,0.508616473974502));
#39453=CARTESIAN_POINT('Ctrl Pts',(367.654828402712,-21.0249980982769,0.526371758319217));
#39454=CARTESIAN_POINT('Ctrl Pts',(367.656500428208,-21.024373509503,0.536373762997258));
#39455=CARTESIAN_POINT('Ctrl Pts',(367.661027934047,-21.0227353673763,0.562692666414876));
#39456=CARTESIAN_POINT('Ctrl Pts',(367.663962092744,-21.021726069586,0.578995963941172));
#39457=CARTESIAN_POINT('Ctrl Pts',(367.68778355975,-21.013916876501,0.705743217318074));
#39458=CARTESIAN_POINT('Ctrl Pts',(367.714312587374,-21.0074021149789,0.815060843580679));
#39459=CARTESIAN_POINT('Ctrl Pts',(367.782839169424,-20.9937891359949,1.04436530684944));
#39460=CARTESIAN_POINT('Ctrl Pts',(367.82632540199,-20.9867338571666,1.16370290727211));
#39461=CARTESIAN_POINT('Ctrl Pts',(367.929724673882,-20.9721630238219,1.40258692280196));
#39462=CARTESIAN_POINT('Ctrl Pts',(367.990259540533,-20.9646549665396,1.52159144867606));
#39463=CARTESIAN_POINT('Ctrl Pts',(368.102808468552,-20.9518257330537,1.71253146110584));
#39464=CARTESIAN_POINT('Ctrl Pts',(368.150728051799,-20.9466312456677,1.78668723258931));
#39465=CARTESIAN_POINT('Ctrl Pts',(368.215899938985,-20.939835450195,1.87899375779051));
#39466=CARTESIAN_POINT('Ctrl Pts',(368.230404543994,-20.9383386375002,1.89904326999987));
#39467=CARTESIAN_POINT('Ctrl Pts',(368.254267323612,-20.9359000297585,1.93124102367045));
#39468=CARTESIAN_POINT('Ctrl Pts',(368.263484005647,-20.9349637358191,1.94349323185903));
#39469=CARTESIAN_POINT('Ctrl Pts',(368.281335083599,-20.9331606726499,1.96687440764748));
#39470=CARTESIAN_POINT('Ctrl Pts',(368.289955721355,-20.9322944581095,1.97801347047114));
#39471=CARTESIAN_POINT('Ctrl Pts',(368.309836724503,-20.9303068393581,2.00335747225589));
#39472=CARTESIAN_POINT('Ctrl Pts',(368.321144391136,-20.9291835658514,2.01752453736189));
#39473=CARTESIAN_POINT('Ctrl Pts',(368.357345939766,-20.925609548994,2.06210384959962));
#39474=CARTESIAN_POINT('Ctrl Pts',(368.382676164423,-20.9231412833028,2.09215557668116));
#39475=CARTESIAN_POINT('Ctrl Pts',(368.58026508161,-20.9041225305542,2.31805794850113));
#39476=CARTESIAN_POINT('Ctrl Pts',(368.775150148223,-20.8865738677939,2.4927745435859));
#39477=CARTESIAN_POINT('Ctrl Pts',(369.089422744843,-20.8606466927883,2.71228561740984));
#39478=CARTESIAN_POINT('Ctrl Pts',(369.193876847071,-20.8523760208687,2.77670831094918));
#39479=CARTESIAN_POINT('Ctrl Pts',(369.336650652102,-20.8417200867529,2.85388931128534));
#39480=CARTESIAN_POINT('Ctrl Pts',(369.371894699906,-20.839139731914,2.87210899074695));
#39481=CARTESIAN_POINT('Ctrl Pts',(369.431832853633,-20.8348456873779,2.9017049800208));
#39482=CARTESIAN_POINT('Ctrl Pts',(369.456350127994,-20.8331152513396,2.91342771089651));
#39483=CARTESIAN_POINT('Ctrl Pts',(369.49062373296,-20.8307351075431,2.92928588543748));
#39484=CARTESIAN_POINT('Ctrl Pts',(369.500255817856,-20.8300704288418,2.93368508545387));
#39485=CARTESIAN_POINT('Ctrl Pts',(369.517288916468,-20.8289026962187,2.94136326596961));
#39486=CARTESIAN_POINT('Ctrl Pts',(369.52468090525,-20.8283984600167,2.94466197588536));
#39487=CARTESIAN_POINT('Ctrl Pts',(369.53885744033,-20.8274363726568,2.95092437904478));
#39488=CARTESIAN_POINT('Ctrl Pts',(369.545639852613,-20.8269782360171,2.95389258192722));
#39489=CARTESIAN_POINT('Ctrl Pts',(369.561901299952,-20.8258848123245,2.96094244905693));
#39490=CARTESIAN_POINT('Ctrl Pts',(369.571389899842,-20.8252508491641,2.96500203422523));
#39491=CARTESIAN_POINT('Ctrl Pts',(369.605693814825,-20.8229729183033,2.97948400672942));
#39492=CARTESIAN_POINT('Ctrl Pts',(369.630620727352,-20.8213440375405,2.98964133477149));
#39493=CARTESIAN_POINT('Ctrl Pts',(369.805844891081,-20.8100577578687,3.05849550205809));
#39494=CARTESIAN_POINT('Ctrl Pts',(369.960255472456,-20.8009436427681,3.10615176418349));
#39495=CARTESIAN_POINT('Ctrl Pts',(370.300729940333,-20.7813725874012,3.18381565404969));
#39496=CARTESIAN_POINT('Ctrl Pts',(370.487148977787,-20.7709650589865,3.20949655035878));
#39497=CARTESIAN_POINT('Ctrl Pts',(370.738651487676,-20.7564438916969,3.22196527997086));
#39498=CARTESIAN_POINT('Ctrl Pts',(370.802640332434,-20.752710726408,3.22322945611918));
#39499=CARTESIAN_POINT('Ctrl Pts',(370.912411778464,-20.7462110384625,3.22212908513293));
#39500=CARTESIAN_POINT('Ctrl Pts',(370.958185007214,-20.743472334966,3.22069419776701));
#39501=CARTESIAN_POINT('Ctrl Pts',(371.023351284055,-20.7395261251584,3.21726015717407));
#39502=CARTESIAN_POINT('Ctrl Pts',(371.042782067425,-20.738343500531,3.21605957696625));
#39503=CARTESIAN_POINT('Ctrl Pts',(371.076412864168,-20.7362857701199,3.21367555545438));
#39504=CARTESIAN_POINT('Ctrl Pts',(371.090618249888,-20.7354132456086,3.21257383828616));
#39505=CARTESIAN_POINT('Ctrl Pts',(371.119695797588,-20.7336201697358,3.2101246050641));
#39506=CARTESIAN_POINT('Ctrl Pts',(371.134566814587,-20.7326993486106,3.20876784769503));
#39507=CARTESIAN_POINT('Ctrl Pts',(371.172224359961,-20.7303577092353,3.20506808986542));
#39508=CARTESIAN_POINT('Ctrl Pts',(371.194996036016,-20.7289325389667,3.20258543569505));
#39509=CARTESIAN_POINT('Ctrl Pts',(371.281677495565,-20.7234715341142,3.19219889111599));
#39510=CARTESIAN_POINT('Ctrl Pts',(371.345368152211,-20.7193837624055,3.18262329706301));
#39511=CARTESIAN_POINT('Ctrl Pts',(371.722731983278,-20.6947005614426,3.11426923387221));
#39512=CARTESIAN_POINT('Ctrl Pts',(372.026377772473,-20.6726736702049,3.01110568884279));
#39513=CARTESIAN_POINT('Ctrl Pts',(372.309820629953,-20.6514935740584,2.86513684112378));
#39514=CARTESIAN_POINT('Ctrl Pts',(372.309820109182,-20.4075893673377,2.8651371093129));
#39515=CARTESIAN_POINT('Ctrl Pts',(372.236449403773,-20.4131724889653,2.90292191235081));
#39516=CARTESIAN_POINT('Ctrl Pts',(372.161612953962,-20.4187542681293,2.93789577972557));
#39517=CARTESIAN_POINT('Ctrl Pts',(372.020771392189,-20.4289722133308,2.99722782015865));
#39518=CARTESIAN_POINT('Ctrl Pts',(371.95519343297,-20.4336194577636,3.02236426609869));
#39519=CARTESIAN_POINT('Ctrl Pts',(371.849736759986,-20.4408671198182,3.05888127804711));
#39520=CARTESIAN_POINT('Ctrl Pts',(371.810371161769,-20.4435237400848,3.07166901593224));
#39521=CARTESIAN_POINT('Ctrl Pts',(371.758224777912,-20.4469691961886,3.08750472081901));
#39522=CARTESIAN_POINT('Ctrl Pts',(371.745658090238,-20.4477939288932,3.09123735626392));
#39523=CARTESIAN_POINT('Ctrl Pts',(371.72501383467,-20.4491392410567,3.09723240715502));
#39524=CARTESIAN_POINT('Ctrl Pts',(371.716949732103,-20.4496623725934,3.09954010870645));
#39525=CARTESIAN_POINT('Ctrl Pts',(371.701145527495,-20.4506828424217,3.10399611253002));
#39526=CARTESIAN_POINT('Ctrl Pts',(371.69340627628,-20.4511803197094,3.1061469969777));
#39527=CARTESIAN_POINT('Ctrl Pts',(371.676086654923,-20.4522887753341,3.11089076482974));
#39528=CARTESIAN_POINT('Ctrl Pts',(371.666502104897,-20.4528988818066,3.11346839449123));
#39529=CARTESIAN_POINT('Ctrl Pts',(371.633241857372,-20.455005117194,3.12224870853292));
#39530=CARTESIAN_POINT('Ctrl Pts',(371.609506856374,-20.4564889669916,3.12822611930707));
#39531=CARTESIAN_POINT('Ctrl Pts',(371.364224522508,-20.4716478690781,3.18703467440204));
#39532=CARTESIAN_POINT('Ctrl Pts',(371.137705945806,-20.4842078716369,3.21651620159829));
#39533=CARTESIAN_POINT('Ctrl Pts',(370.766279165288,-20.505002342164,3.22523484205441));
#39534=CARTESIAN_POINT('Ctrl Pts',(370.622555644941,-20.5130913865835,3.21899386683575));
#39535=CARTESIAN_POINT('Ctrl Pts',(370.399384112381,-20.5261329373996,3.19428957090933));
#39536=CARTESIAN_POINT('Ctrl Pts',(370.319400195146,-20.5309030228467,3.18237512441352));
#39537=CARTESIAN_POINT('Ctrl Pts',(370.216320540462,-20.5372148381288,3.16303257245616));
#39538=CARTESIAN_POINT('Ctrl Pts',(370.19273871102,-20.5386700068387,3.15833372039807));
#39539=CARTESIAN_POINT('Ctrl Pts',(370.154352735759,-20.5410579356198,3.15023739207248));
#39540=CARTESIAN_POINT('Ctrl Pts',(370.139515867155,-20.5419856254667,3.14699831190856));
#39541=CARTESIAN_POINT('Ctrl Pts',(370.110900722152,-20.543784168412,3.14053903276191));
#39542=CARTESIAN_POINT('Ctrl Pts',(370.097119647786,-20.5446545576779,3.13733271388021));
#39543=CARTESIAN_POINT('Ctrl Pts',(370.065378860911,-20.5466691750322,3.12972719018952));
#39544=CARTESIAN_POINT('Ctrl Pts',(370.047435137408,-20.5478154393323,3.12526399326896));
#39545=CARTESIAN_POINT('Ctrl Pts',(369.989563077295,-20.5515367178166,3.1103393089887));
#39546=CARTESIAN_POINT('Ctrl Pts',(369.949798330844,-20.5541313479689,3.09926543057856));
#39547=CARTESIAN_POINT('Ctrl Pts',(369.688723175139,-20.5714236508928,3.02112639715902));
#39548=CARTESIAN_POINT('Ctrl Pts',(369.475005077592,-20.5868816049001,2.93118153154803));
#39549=CARTESIAN_POINT('Ctrl Pts',(369.165913419395,-20.6107811429149,2.75997644837197));
#39550=CARTESIAN_POINT('Ctrl Pts',(369.062490420558,-20.6190603475817,2.69474914675987));
#39551=CARTESIAN_POINT('Ctrl Pts',(368.895026045517,-20.632716565347,2.57531341287178));
#39552=CARTESIAN_POINT('Ctrl Pts',(368.828938371322,-20.6381766613465,2.52419246057124));
#39553=CARTESIAN_POINT('Ctrl Pts',(368.75235390224,-20.6445212095048,2.46004304285685));
#39554=CARTESIAN_POINT('Ctrl Pts',(368.73988171435,-20.6455549995162,2.44943319002243));
#39555=CARTESIAN_POINT('Ctrl Pts',(368.720599432734,-20.6471533825058,2.43277515035024));
#39556=CARTESIAN_POINT('Ctrl Pts',(368.713733399541,-20.647722558541,2.42679254838276));
#39557=CARTESIAN_POINT('Ctrl Pts',(368.700988921186,-20.6487789336027,2.41559247476848));
#39558=CARTESIAN_POINT('Ctrl Pts',(368.695104239349,-20.6492666462905,2.41038263607563));
#39559=CARTESIAN_POINT('Ctrl Pts',(368.681611122912,-20.6503848706486,2.3983485459287));
#39560=CARTESIAN_POINT('Ctrl Pts',(368.674016046234,-20.6510142731382,2.39150959100153));
#39561=CARTESIAN_POINT('Ctrl Pts',(368.654007394432,-20.6526727140554,2.37331978349067));
#39562=CARTESIAN_POINT('Ctrl Pts',(368.641649748008,-20.653697329528,2.36190751285045));
#39563=CARTESIAN_POINT('Ctrl Pts',(368.534295856988,-20.6626073761054,2.26119759097805));
#39564=CARTESIAN_POINT('Ctrl Pts',(368.444698779682,-20.6701077911428,2.16629740969664));
#39565=CARTESIAN_POINT('Ctrl Pts',(368.24170244363,-20.6880123158001,1.92331429889627));
#39566=CARTESIAN_POINT('Ctrl Pts',(368.134925767335,-20.6982667568535,1.77033230655128));
#39567=CARTESIAN_POINT('Ctrl Pts',(367.996436053644,-20.7140239887933,1.52998602980585));
#39568=CARTESIAN_POINT('Ctrl Pts',(367.954292124961,-20.7192692009857,1.4490964019836));
#39569=CARTESIAN_POINT('Ctrl Pts',(367.890408320602,-20.7281170015069,1.31265146894373));
#39570=CARTESIAN_POINT('Ctrl Pts',(367.866679033928,-20.7316550586823,1.25808441033854));
#39571=CARTESIAN_POINT('Ctrl Pts',(367.836433102605,-20.7365440122689,1.18290690545401));
#39572=CARTESIAN_POINT('Ctrl Pts',(367.828592408877,-20.7378503711747,1.16283973251491));
#39573=CARTESIAN_POINT('Ctrl Pts',(367.815757742447,-20.7400566375981,1.1289938711139));
#39574=CARTESIAN_POINT('Ctrl Pts',(367.810655419908,-20.7409528976578,1.11525682315256));
#39575=CARTESIAN_POINT('Ctrl Pts',(367.8007642724,-20.7427291241415,1.08805989106883));
#39576=CARTESIAN_POINT('Ctrl Pts',(367.795970906776,-20.7436089150044,1.07460200857527));
#39577=CARTESIAN_POINT('Ctrl Pts',(367.784544510618,-20.7457534041116,1.04183348526444));
#39578=CARTESIAN_POINT('Ctrl Pts',(367.778005279433,-20.7470211690814,1.02249101355206));
#39579=CARTESIAN_POINT('Ctrl Pts',(367.759958909582,-20.7506386124121,0.967391135818501));
#39580=CARTESIAN_POINT('Ctrl Pts',(367.748892823107,-20.7530025609021,0.93149380908082));
#39581=CARTESIAN_POINT('Ctrl Pts',(367.678401948528,-20.7691059141394,0.687773792393171));
#39582=CARTESIAN_POINT('Ctrl Pts',(367.639398211184,-20.7835044470568,0.474654693217188));
#39583=CARTESIAN_POINT('Ctrl Pts',(367.614988883063,-20.8040106317177,0.172232679670542));
#39584=CARTESIAN_POINT('Ctrl Pts',(367.611504123752,-20.8099302381019,0.0849412129632191));
#39585=CARTESIAN_POINT('Ctrl Pts',(367.611664143858,-20.8244823436421,-0.131334013137009));
#39586=CARTESIAN_POINT('Ctrl Pts',(367.619498885925,-20.8330526939712,-0.260176677917461));
#39587=CARTESIAN_POINT('Ctrl Pts',(367.637059308486,-20.8423358011356,-0.404892037900025));
#39588=CARTESIAN_POINT('Ctrl Pts',(367.639213326537,-20.8433993001567,-0.421552909710437));
#39589=CARTESIAN_POINT('Ctrl Pts',(367.642871577308,-20.845091512285,-0.448207926447213));
#39590=CARTESIAN_POINT('Ctrl Pts',(367.644292679191,-20.8457245970961,-0.458212912194987));
#39591=CARTESIAN_POINT('Ctrl Pts',(367.646903514384,-20.8468457447733,-0.475992915680618));
#39592=CARTESIAN_POINT('Ctrl Pts',(367.648074678532,-20.8473348264556,-0.483770461822187));
#39593=CARTESIAN_POINT('Ctrl Pts',(367.650657789762,-20.8483844177657,-0.50050817679968));
#39594=CARTESIAN_POINT('Ctrl Pts',(367.652079094575,-20.8489443980657,-0.509466703914104));
#39595=CARTESIAN_POINT('Ctrl Pts',(367.656145279662,-20.8504991640164,-0.534414926739518));
#39596=CARTESIAN_POINT('Ctrl Pts',(367.658873021496,-20.8514894075788,-0.550391103699132));
#39597=CARTESIAN_POINT('Ctrl Pts',(367.675838695875,-20.8573517055304,-0.645430537034827));
#39598=CARTESIAN_POINT('Ctrl Pts',(367.692909538148,-20.8620785845905,-0.723966327732457));
#39599=CARTESIAN_POINT('Ctrl Pts',(367.753466689018,-20.8761320040982,-0.959719535726872));
#39600=CARTESIAN_POINT('Ctrl Pts',(367.805963794626,-20.8851725494863,-1.11435345873297));
#39601=CARTESIAN_POINT('Ctrl Pts',(367.952696805268,-20.9061091157299,-1.45837945728222));
#39602=CARTESIAN_POINT('Ctrl Pts',(368.054286687824,-20.9180379973265,-1.64378262616659));
#39603=CARTESIAN_POINT('Ctrl Pts',(368.188723632344,-20.9323017221405,-1.8405708770611));
#39604=CARTESIAN_POINT('Ctrl Pts',(368.204484444029,-20.9339536948737,-1.86302069367058));
#39605=CARTESIAN_POINT('Ctrl Pts',(368.230783847336,-20.9366791972889,-1.89948295937156));
#39606=CARTESIAN_POINT('Ctrl Pts',(368.241153813833,-20.9377462646679,-1.91361570820506));
#39607=CARTESIAN_POINT('Ctrl Pts',(368.260005433912,-20.9396729243354,-1.93887307593593));
#39608=CARTESIAN_POINT('Ctrl Pts',(368.268445256511,-20.9405308713393,-1.95002847274029));
#39609=CARTESIAN_POINT('Ctrl Pts',(368.286602922103,-20.9423671144386,-1.97370652275852));
#39610=CARTESIAN_POINT('Ctrl Pts',(368.296341035147,-20.9433461975165,-1.98621309652278));
#39611=CARTESIAN_POINT('Ctrl Pts',(368.322968211011,-20.9460083081062,-2.01989458665303));
#39612=CARTESIAN_POINT('Ctrl Pts',(368.340032306862,-20.947698296167,-2.04092888359619));
#39613=CARTESIAN_POINT('Ctrl Pts',(368.43350445921,-20.9568726538298,-2.15322533921771));
#39614=CARTESIAN_POINT('Ctrl Pts',(368.514650339832,-20.9645499580092,-2.24040648040338));
#39615=CARTESIAN_POINT('Ctrl Pts',(368.712941883156,-20.9826774605727,-2.43110076573428));
#39616=CARTESIAN_POINT('Ctrl Pts',(368.833166472407,-20.993228157677,-2.53098266361671));
#39617=CARTESIAN_POINT('Ctrl Pts',(369.09656126622,-21.0151303726708,-2.71927181700343));
#39618=CARTESIAN_POINT('Ctrl Pts',(369.240395242531,-21.0264499172951,-2.80600401173764));
#39619=CARTESIAN_POINT('Ctrl Pts',(369.414427222154,-21.0389568559812,-2.89322556837779));
#39620=CARTESIAN_POINT('Ctrl Pts',(369.438667530525,-21.0406731912015,-2.90499636499687));
#39621=CARTESIAN_POINT('Ctrl Pts',(369.472401161234,-21.0430234700713,-2.92085726829929));
#39622=CARTESIAN_POINT('Ctrl Pts',(369.481770031706,-21.0436721777599,-2.92520745504079));
#39623=CARTESIAN_POINT('Ctrl Pts',(369.497894864518,-21.0447815501,-2.93260056167912));
#39624=CARTESIAN_POINT('Ctrl Pts',(369.504640634475,-21.0452435229423,-2.93566533441154));
#39625=CARTESIAN_POINT('Ctrl Pts',(369.518783580922,-21.0462075354752,-2.94203207999242));
#39626=CARTESIAN_POINT('Ctrl Pts',(369.52618271919,-21.0467092756968,-2.94532946445713));
#39627=CARTESIAN_POINT('Ctrl Pts',(369.544345745921,-21.0479347398582,-2.95334177052092));
#39628=CARTESIAN_POINT('Ctrl Pts',(369.555123274173,-21.0486566049195,-2.95802584335908));
#39629=CARTESIAN_POINT('Ctrl Pts',(369.594419237341,-21.0512702223882,-2.97484951436676));
#39630=CARTESIAN_POINT('Ctrl Pts',(369.623087795619,-21.0531419427455,-2.98663692464109));
#39631=CARTESIAN_POINT('Ctrl Pts',(369.695560182531,-21.0577966901896,-3.01521954617209));
#39632=CARTESIAN_POINT('Ctrl Pts',(369.73956997722,-21.0605537496065,-3.03147579037329));
#39633=CARTESIAN_POINT('Ctrl Pts',(370.103192032219,-21.0828871011326,-3.15683737291466));
#39634=CARTESIAN_POINT('Ctrl Pts',(370.437785774692,-21.1008706321102,-3.21604877209414));
#39635=CARTESIAN_POINT('Ctrl Pts',(370.838172825026,-21.1243314065514,-3.22335721264079));
#39636=CARTESIAN_POINT('Ctrl Pts',(370.900860905433,-21.1280517794558,-3.22267246688889));
#39637=CARTESIAN_POINT('Ctrl Pts',(370.986145765926,-21.1331953627915,-3.21925148555618));
#39638=CARTESIAN_POINT('Ctrl Pts',(371.008794598007,-21.1345691886592,-3.21810342710667));
#39639=CARTESIAN_POINT('Ctrl Pts',(371.044806860208,-21.1367668704605,-3.21589669917595));
#39640=CARTESIAN_POINT('Ctrl Pts',(371.058179321594,-21.1375858492668,-3.21499350486038));
#39641=CARTESIAN_POINT('Ctrl Pts',(371.085625750943,-21.1392729229095,-3.21296766769742));
#39642=CARTESIAN_POINT('Ctrl Pts',(371.099698735474,-21.1401412861844,-3.2118359034023));
#39643=CARTESIAN_POINT('Ctrl Pts',(371.132301692281,-21.1421609413787,-3.20899820138306));
#39644=CARTESIAN_POINT('Ctrl Pts',(371.150825088617,-21.1433143454845,-3.20722418478793));
#39645=CARTESIAN_POINT('Ctrl Pts',(371.209920565754,-21.14701355302,-3.20104758036026));
#39646=CARTESIAN_POINT('Ctrl Pts',(371.250423528438,-21.1495783583976,-3.1960348607383));
#39647=CARTESIAN_POINT('Ctrl Pts',(371.3453049054,-21.1556583981561,-3.18245805948559));
#39648=CARTESIAN_POINT('Ctrl Pts',(371.399579405198,-21.1591921892299,-3.17326738077384));
#39649=CARTESIAN_POINT('Ctrl Pts',(371.600641249979,-21.1724921674109,-3.13389841893385));
#39650=CARTESIAN_POINT('Ctrl Pts',(371.745490944,-21.182503129386,-3.0948870706698));
#39651=CARTESIAN_POINT('Ctrl Pts',(372.093012864535,-21.2073269502911,-2.97477314321546));
#39652=CARTESIAN_POINT('Ctrl Pts',(372.291202952998,-21.2222128514161,-2.88289574145071));
#39653=CARTESIAN_POINT('Ctrl Pts',(372.500376836419,-21.2378154055712,-2.75880504297725));
#39654=CARTESIAN_POINT('Ctrl Pts',(372.52198652861,-21.2394253638472,-2.7456387844639));
#39655=CARTESIAN_POINT('Ctrl Pts',(372.551974207059,-21.2416543578093,-2.726880186768));
#39656=CARTESIAN_POINT('Ctrl Pts',(372.560483819027,-21.2422862934715,-2.72150141791122));
#39657=CARTESIAN_POINT('Ctrl Pts',(372.575155610684,-21.2433746324087,-2.71213114799151));
#39658=CARTESIAN_POINT('Ctrl Pts',(372.581329554162,-21.243832236518,-2.70815833751388));
#39659=CARTESIAN_POINT('Ctrl Pts',(372.59434570188,-21.2447960942692,-2.69971966909606));
#39660=CARTESIAN_POINT('Ctrl Pts',(372.601184598619,-21.2453019977332,-2.69524882456415));
#39661=CARTESIAN_POINT('Ctrl Pts',(372.618107410608,-21.2465527447182,-2.68409365324746));
#39662=CARTESIAN_POINT('Ctrl Pts',(372.628170948985,-21.2472955487117,-2.67737838305814));
#39663=CARTESIAN_POINT('Ctrl Pts',(372.665882107389,-21.2500763154891,-2.65190613231603));
#39664=CARTESIAN_POINT('Ctrl Pts',(372.693276374765,-21.2520907419033,-2.63277556327152));
#39665=CARTESIAN_POINT('Ctrl Pts',(372.899156264197,-21.2672277725459,-2.48418499539591));
#39666=CARTESIAN_POINT('Ctrl Pts',(373.064252047781,-21.2793820431779,-2.33712451788103));
#39667=CARTESIAN_POINT('Ctrl Pts',(373.353765251096,-21.3034079003868,-2.02039636753664));
#39668=CARTESIAN_POINT('Ctrl Pts',(373.47918593318,-21.3152118239945,-1.85317939726525));
#39669=CARTESIAN_POINT('Ctrl Pts',(373.601825034779,-21.3293337978134,-1.65159739813631));
#39670=CARTESIAN_POINT('Ctrl Pts',(373.615781711854,-21.3309858033637,-1.62798301549597));
#39671=CARTESIAN_POINT('Ctrl Pts',(373.63816052682,-21.3337113489871,-1.5889905916598));
#39672=CARTESIAN_POINT('Ctrl Pts',(373.64676179006,-21.3347784264039,-1.57371659517667));
#39673=CARTESIAN_POINT('Ctrl Pts',(373.662002024521,-21.3367050970169,-1.5461291875673));
#39674=CARTESIAN_POINT('Ctrl Pts',(373.6686862832,-21.337563044849,-1.5338412012516));
#39675=CARTESIAN_POINT('Ctrl Pts',(373.682773574452,-21.3393992819088,-1.50753733253041));
#39676=CARTESIAN_POINT('Ctrl Pts',(373.690153602984,-21.3403783580614,-1.49350961189458));
#39677=CARTESIAN_POINT('Ctrl Pts',(373.709863151346,-21.3430404300869,-1.45536606315369));
#39678=CARTESIAN_POINT('Ctrl Pts',(373.721992411232,-21.3447303861658,-1.43114873944816));
#39679=CARTESIAN_POINT('Ctrl Pts',(373.785767105788,-21.3539041972888,-1.2997036919467));
#39680=CARTESIAN_POINT('Ctrl Pts',(373.831742132378,-21.3615809592628,-1.18984214288387));
#39681=CARTESIAN_POINT('Ctrl Pts',(373.923728905526,-21.3797064154961,-0.930601627656953));
#39682=CARTESIAN_POINT('Ctrl Pts',(373.965165288329,-21.3902555595844,-0.779915080146005));
#39683=CARTESIAN_POINT('Ctrl Pts',(374.028141953759,-21.4121584291594,-0.462315219347082));
#39684=CARTESIAN_POINT('Ctrl Pts',(374.047874504023,-21.4234801947338,-0.295486099095809));
#39685=CARTESIAN_POINT('Ctrl Pts',(374.055599306909,-21.4359891401719,-0.100942438561298));
#39686=CARTESIAN_POINT('Ctrl Pts',(374.056330712701,-21.4377054586117,-0.0740055626245434));
#39687=CARTESIAN_POINT('Ctrl Pts',(374.056875053357,-21.4400557187606,-0.0367334839249444));
#39688=CARTESIAN_POINT('Ctrl Pts',(374.056976238577,-21.4407044241994,-0.0264044523672441));
#39689=CARTESIAN_POINT('Ctrl Pts',(374.057064719241,-21.4418137937143,-0.00866582622766637));
#39690=CARTESIAN_POINT('Ctrl Pts',(374.057076125694,-21.4422757659688,-0.00125650916390129));
#39691=CARTESIAN_POINT('Ctrl Pts',(374.057046514133,-21.4432397784107,0.0142534064147461));
#39692=CARTESIAN_POINT('Ctrl Pts',(374.057000506907,-21.4437415191223,0.0223539007758042));
#39693=CARTESIAN_POINT('Ctrl Pts',(374.056812912081,-21.4449669864023,0.042204831239696));
#39694=CARTESIAN_POINT('Ctrl Pts',(374.05663759566,-21.4456888540699,0.0539549773240474));
#39695=CARTESIAN_POINT('Ctrl Pts',(374.055766103616,-21.4483024919377,0.0966922906082021));
#39696=CARTESIAN_POINT('Ctrl Pts',(374.054687163395,-21.4501742296776,0.127671047637771));
#39697=CARTESIAN_POINT('Ctrl Pts',(374.050852459734,-21.4548290294194,0.205482665572566));
#39698=CARTESIAN_POINT('Ctrl Pts',(374.047520731281,-21.4575861230028,0.252280995407905));
#39699=CARTESIAN_POINT('Ctrl Pts',(374.011835407342,-21.4799204293363,0.635263878207513));
#39700=CARTESIAN_POINT('Ctrl Pts',(373.927843709714,-21.4979047608619,0.964528905658023));
#39701=CARTESIAN_POINT('Ctrl Pts',(373.769441908256,-21.5213658788122,1.33232568326378));
#39702=CARTESIAN_POINT('Ctrl Pts',(373.742980822224,-21.5250854957027,1.38914502608119));
#39703=CARTESIAN_POINT('Ctrl Pts',(373.704713072962,-21.5302281916624,1.46542247897418));
#39704=CARTESIAN_POINT('Ctrl Pts',(373.694331252966,-21.5316019086747,1.48558240174572));
#39705=CARTESIAN_POINT('Ctrl Pts',(373.677476210964,-21.5337994598229,1.51748072318112));
#39706=CARTESIAN_POINT('Ctrl Pts',(373.671140885479,-21.5346184178957,1.52929142662923));
#39707=CARTESIAN_POINT('Ctrl Pts',(373.657980876679,-21.5363054812106,1.553461949206));
#39708=CARTESIAN_POINT('Ctrl Pts',(373.651148282713,-21.5371738550963,1.56581710907888));
#39709=CARTESIAN_POINT('Ctrl Pts',(373.635122181286,-21.539193590141,1.59435221385653));
#39710=CARTESIAN_POINT('Ctrl Pts',(373.625869344799,-21.5403470640137,1.61049809454227));
#39711=CARTESIAN_POINT('Ctrl Pts',(373.595877003629,-21.5440467250904,1.66179859367238));
#39712=CARTESIAN_POINT('Ctrl Pts',(373.574609932803,-21.5466119208011,1.6966386121425));
#39713=CARTESIAN_POINT('Ctrl Pts',(373.523117347707,-21.5526930479246,1.77749979454535));
#39714=CARTESIAN_POINT('Ctrl Pts',(373.492363533691,-21.5562275450168,1.82316779960588));
#39715=CARTESIAN_POINT('Ctrl Pts',(373.373573195683,-21.5695314832925,1.99016777537936));
#39716=CARTESIAN_POINT('Ctrl Pts',(373.27828293745,-21.5795458593314,2.10608918660309));
#39717=CARTESIAN_POINT('Ctrl Pts',(373.025590365263,-21.6043680783881,2.37315832507954));
#39718=CARTESIAN_POINT('Ctrl Pts',(372.860235300926,-21.6192485973552,2.51579566290711));
#39719=CARTESIAN_POINT('Ctrl Pts',(372.661009056787,-21.6348466845178,2.6551755634908));
#39720=CARTESIAN_POINT('Ctrl Pts',(372.640101685127,-21.6364569312988,2.66943868081069));
#39721=CARTESIAN_POINT('Ctrl Pts',(372.610644886824,-21.6386862569657,2.68902978557585));
#39722=CARTESIAN_POINT('Ctrl Pts',(372.602235833935,-21.639318240708,2.69456581619799));
#39723=CARTESIAN_POINT('Ctrl Pts',(372.587649792265,-21.640406639658,2.70407074168204));
#39724=CARTESIAN_POINT('Ctrl Pts',(372.581484985815,-21.6408642560052,2.70805806396937));
#39725=CARTESIAN_POINT('Ctrl Pts',(372.568431032926,-21.6418281126203,2.71643807146547));
#39726=CARTESIAN_POINT('Ctrl Pts',(372.56153870847,-21.6423340028603,2.72082569009355));
#39727=CARTESIAN_POINT('Ctrl Pts',(372.544400418106,-21.6435846714673,2.73164447171057));
#39728=CARTESIAN_POINT('Ctrl Pts',(372.53413466586,-21.6443274108694,2.73804432265444));
#39729=CARTESIAN_POINT('Ctrl Pts',(372.495389120594,-21.6471076486376,2.76189708060224));
#39730=CARTESIAN_POINT('Ctrl Pts',(372.466673517353,-21.6491216221936,2.77896535142017));
#39731=CARTESIAN_POINT('Ctrl Pts',(372.39558244711,-21.6540075646915,2.81973889580822));
#39732=CARTESIAN_POINT('Ctrl Pts',(372.35294581336,-21.6568525731455,2.84292801726746));
#39733=CARTESIAN_POINT('Ctrl Pts',(372.309820475366,-21.6596622257337,2.86513692073371));
#39734=CARTESIAN_POINT('Origin',(370.834317853224,2.31077344927308,0.));
#39735=CARTESIAN_POINT('',(372.309820652883,-23.1546465340815,2.86513682931516));
#39736=CARTESIAN_POINT('',(372.309820613641,-22.9071794904733,2.86513684952399));
#39737=CARTESIAN_POINT('',(372.309820613641,2.31077344927308,2.86513684952399));
#39738=CARTESIAN_POINT('Ctrl Pts',(372.309820652881,-23.1546465340816,2.86513682931627));
#39739=CARTESIAN_POINT('Ctrl Pts',(372.375818427643,-23.1504575899474,2.83114895814868));
#39740=CARTESIAN_POINT('Ctrl Pts',(372.440695164174,-23.1462298331336,2.79485332831167));
#39741=CARTESIAN_POINT('Ctrl Pts',(372.557946972649,-23.1383172123807,2.72381177552407));
#39742=CARTESIAN_POINT('Ctrl Pts',(372.610603706517,-23.1346570443842,2.6897687278091));
#39743=CARTESIAN_POINT('Ctrl Pts',(372.699363577078,-23.1282731428272,2.62864122470886));
#39744=CARTESIAN_POINT('Ctrl Pts',(372.735952986043,-23.1255758729175,2.60229394204416));
#39745=CARTESIAN_POINT('Ctrl Pts',(372.787437630317,-23.1216790267826,2.56355516601944));
#39746=CARTESIAN_POINT('Ctrl Pts',(372.802793534755,-23.1205034687938,2.55178279225814));
#39747=CARTESIAN_POINT('Ctrl Pts',(372.82925555013,-23.1184540105637,2.53111508787315));
#39748=CARTESIAN_POINT('Ctrl Pts',(372.84041058973,-23.1175826328585,2.52228307786803));
#39749=CARTESIAN_POINT('Ctrl Pts',(372.86318364494,-23.1157881871445,2.50400585935424));
#39750=CARTESIAN_POINT('Ctrl Pts',(372.8747950368,-23.1148648237785,2.49455298514946));
#39751=CARTESIAN_POINT('Ctrl Pts',(372.904144886064,-23.1125090853678,2.47031714470044));
#39752=CARTESIAN_POINT('Ctrl Pts',(372.921790878424,-23.1110722532151,2.45542400936769));
#39753=CARTESIAN_POINT('Ctrl Pts',(372.989068402243,-23.1055135279536,2.39739269569842));
#39754=CARTESIAN_POINT('Ctrl Pts',(373.0375324728,-23.1013372878133,2.35293136202504));
#39755=CARTESIAN_POINT('Ctrl Pts',(373.323772203477,-23.0755829695132,2.07373143717664));
#39756=CARTESIAN_POINT('Ctrl Pts',(373.525152884969,-23.052413081836,1.80473668543287));
#39757=CARTESIAN_POINT('Ctrl Pts',(373.703512244996,-23.0272813886519,1.46834187313638));
#39758=CARTESIAN_POINT('Ctrl Pts',(373.724516971627,-23.0242251842694,1.42655312337029));
#39759=CARTESIAN_POINT('Ctrl Pts',(373.757886841314,-23.019219553762,1.3563988761391));
#39760=CARTESIAN_POINT('Ctrl Pts',(373.770766007287,-23.017246292843,1.32828684473065));
#39761=CARTESIAN_POINT('Ctrl Pts',(373.787972682978,-23.0145555127484,1.28925498367497));
#39762=CARTESIAN_POINT('Ctrl Pts',(373.792647639179,-23.0138185706774,1.27849135851359));
#39763=CARTESIAN_POINT('Ctrl Pts',(373.800447197861,-23.0125793267435,1.26026178548212));
#39764=CARTESIAN_POINT('Ctrl Pts',(373.803602632893,-23.0120751922324,1.25280922704203));
#39765=CARTESIAN_POINT('Ctrl Pts',(373.809591347453,-23.0111131293128,1.23851525048463));
#39766=CARTESIAN_POINT('Ctrl Pts',(373.812429157636,-23.0106549165748,1.23167587143866));
#39767=CARTESIAN_POINT('Ctrl Pts',(373.819167917302,-23.0095610636028,1.21527539534458));
#39768=CARTESIAN_POINT('Ctrl Pts',(373.823046564516,-23.0089267498693,1.2057051416493));
#39769=CARTESIAN_POINT('Ctrl Pts',(373.836885267025,-23.0066457452285,1.17108211402457));
#39770=CARTESIAN_POINT('Ctrl Pts',(373.846577172637,-23.0050141972727,1.14592246363119));
#39771=CARTESIAN_POINT('Ctrl Pts',(373.915157645971,-22.9931914684596,0.961006218298169));
#39772=CARTESIAN_POINT('Ctrl Pts',(373.961626460669,-22.9836065499557,0.79690769540356));
#39773=CARTESIAN_POINT('Ctrl Pts',(374.025069682204,-22.9654332471019,0.478568227592113));
#39774=CARTESIAN_POINT('Ctrl Pts',(374.04432023341,-22.9568573415195,0.325280366040332));
#39775=CARTESIAN_POINT('Ctrl Pts',(374.058803532347,-22.9412698440434,0.0530398975333145));
#39776=CARTESIAN_POINT('Ctrl Pts',(374.058576340274,-22.9343739858897,-0.0653747579176822));
#39777=CARTESIAN_POINT('Ctrl Pts',(374.050300461851,-22.9256503207824,-0.210485047580604));
#39778=CARTESIAN_POINT('Ctrl Pts',(374.048422121928,-22.9240179561323,-0.237448471477331));
#39779=CARTESIAN_POINT('Ctrl Pts',(374.044906226568,-22.9214127076359,-0.280161489643905));
#39780=CARTESIAN_POINT('Ctrl Pts',(374.043491340748,-22.920446811544,-0.295928498657462));
#39781=CARTESIAN_POINT('Ctrl Pts',(374.040608501147,-22.9186211403665,-0.325596727179447));
#39782=CARTESIAN_POINT('Ctrl Pts',(374.039166151481,-22.9177621900321,-0.339500107667311));
#39783=CARTESIAN_POINT('Ctrl Pts',(374.03571157404,-22.9158197903486,-0.370813931734146));
#39784=CARTESIAN_POINT('Ctrl Pts',(374.033647689189,-22.9147347381789,-0.38821812028866));
#39785=CARTESIAN_POINT('Ctrl Pts',(374.027987994458,-22.9119390419953,-0.432829937472582));
#39786=CARTESIAN_POINT('Ctrl Pts',(374.024186473679,-22.9102219817883,-0.460009603363318));
#39787=CARTESIAN_POINT('Ctrl Pts',(373.988638411203,-22.8954139474487,-0.692482710099291));
#39788=CARTESIAN_POINT('Ctrl Pts',(373.937463810628,-22.8816968156054,-0.894274997482535));
#39789=CARTESIAN_POINT('Ctrl Pts',(373.816782650418,-22.8576410161071,-1.2301603058513));
#39790=CARTESIAN_POINT('Ctrl Pts',(373.756624185978,-22.8474794350743,-1.36693720205042));
#39791=CARTESIAN_POINT('Ctrl Pts',(373.657105453504,-22.8332101838817,-1.5563337026695));
#39792=CARTESIAN_POINT('Ctrl Pts',(373.625287475591,-22.8289384670155,-1.61269773980359));
#39793=CARTESIAN_POINT('Ctrl Pts',(373.578155401195,-22.8230342560931,-1.69061149148152));
#39794=CARTESIAN_POINT('Ctrl Pts',(373.564242233459,-22.8213387867928,-1.71298706281995));
#39795=CARTESIAN_POINT('Ctrl Pts',(373.539302933239,-22.8183847488793,-1.75201944196714));
#39796=CARTESIAN_POINT('Ctrl Pts',(373.528393580486,-22.8171198176635,-1.76874883198107));
#39797=CARTESIAN_POINT('Ctrl Pts',(373.511872204583,-22.8152455968796,-1.79357667339913));
#39798=CARTESIAN_POINT('Ctrl Pts',(373.50637765528,-22.8146289362175,-1.80175220496754));
#39799=CARTESIAN_POINT('Ctrl Pts',(373.49687378055,-22.8135738345459,-1.81575425496961));
#39800=CARTESIAN_POINT('Ctrl Pts',(373.492882677434,-22.8131341944013,-1.82159289066328));
#39801=CARTESIAN_POINT('Ctrl Pts',(373.483738390691,-22.8121347447722,-1.83487611313049));
#39802=CARTESIAN_POINT('Ctrl Pts',(373.478573039406,-22.8115757696153,-1.84231214780079));
#39803=CARTESIAN_POINT('Ctrl Pts',(373.464349945175,-22.8100515033805,-1.8626046500728));
#39804=CARTESIAN_POINT('Ctrl Pts',(373.455229189856,-22.8090903767888,-1.8754169338235));
#39805=CARTESIAN_POINT('Ctrl Pts',(373.408123192149,-22.8042062133094,-1.94057372394504));
#39806=CARTESIAN_POINT('Ctrl Pts',(373.368659580733,-22.8003755574656,-1.99183673121851));
#39807=CARTESIAN_POINT('Ctrl Pts',(373.179167820705,-22.7829637510526,-2.22322682239339));
#39808=CARTESIAN_POINT('Ctrl Pts',(373.011307588369,-22.7701791185087,-2.38784271349591));
#39809=CARTESIAN_POINT('Ctrl Pts',(372.702586041308,-22.7479934127432,-2.63073698966304));
#39810=CARTESIAN_POINT('Ctrl Pts',(372.571074792703,-22.7388810476321,-2.71935089694838));
#39811=CARTESIAN_POINT('Ctrl Pts',(372.408421633394,-22.7276549040944,-2.81232208191326));
#39812=CARTESIAN_POINT('Ctrl Pts',(372.383057360193,-22.7259059833655,-2.82636941317432));
#39813=CARTESIAN_POINT('Ctrl Pts',(372.343181470897,-22.7231574342356,-2.84775568106284));
#39814=CARTESIAN_POINT('Ctrl Pts',(372.328797603426,-22.7221661884842,-2.85533047069488));
#39815=CARTESIAN_POINT('Ctrl Pts',(372.30321567839,-22.720403320069,-2.86855609233045));
#39816=CARTESIAN_POINT('Ctrl Pts',(372.292040707712,-22.7196332712365,-2.8742510238464));
#39817=CARTESIAN_POINT('Ctrl Pts',(372.266211612292,-22.7178533473739,-2.88722453959774));
#39818=CARTESIAN_POINT('Ctrl Pts',(372.251534826704,-22.71684188463,-2.89445699805788));
#39819=CARTESIAN_POINT('Ctrl Pts',(372.210975743188,-22.7140462255332,-2.9140613511023));
#39820=CARTESIAN_POINT('Ctrl Pts',(372.184982832316,-22.7122540200032,-2.92619967411106));
#39821=CARTESIAN_POINT('Ctrl Pts',(372.03561852144,-22.7019495045231,-2.9935365966455));
#39822=CARTESIAN_POINT('Ctrl Pts',(371.909048766829,-22.6931863669261,-3.04127109375586));
#39823=CARTESIAN_POINT('Ctrl Pts',(371.573536129836,-22.669918818181,-3.14424200773115));
#39824=CARTESIAN_POINT('Ctrl Pts',(371.361365461458,-22.6551387111873,-3.18667728991171));
#39825=CARTESIAN_POINT('Ctrl Pts',(371.076616937972,-22.6360103027534,-3.21439709733479));
#39826=CARTESIAN_POINT('Ctrl Pts',(371.006454044967,-22.6313577770401,-3.21891719321225));
#39827=CARTESIAN_POINT('Ctrl Pts',(370.908354709285,-22.6249836439428,-3.22201986193785));
#39828=CARTESIAN_POINT('Ctrl Pts',(370.880502680639,-22.623188672298,-3.2225394518304));
#39829=CARTESIAN_POINT('Ctrl Pts',(370.831790410131,-22.6200790425069,-3.22281649543114));
#39830=CARTESIAN_POINT('Ctrl Pts',(370.810933063276,-22.6187571049461,-3.22273265346978));
#39831=CARTESIAN_POINT('Ctrl Pts',(370.780053632795,-22.6168155135291,-3.22230871445646));
#39832=CARTESIAN_POINT('Ctrl Pts',(370.770030426685,-22.6161877149443,-3.22212432876341));
#39833=CARTESIAN_POINT('Ctrl Pts',(370.752172616245,-22.6150737179957,-3.22171245610256));
#39834=CARTESIAN_POINT('Ctrl Pts',(370.744337824636,-22.6145865334719,-3.22150315667842));
#39835=CARTESIAN_POINT('Ctrl Pts',(370.727276768108,-22.6135290643111,-3.22098509491697));
#39836=CARTESIAN_POINT('Ctrl Pts',(370.718051039864,-22.612959397355,-3.22066527423341));
#39837=CARTESIAN_POINT('Ctrl Pts',(370.692333841999,-22.6113771207536,-3.21966310812248));
#39838=CARTESIAN_POINT('Ctrl Pts',(370.675845785337,-22.6103692128702,-3.21889369494802));
#39839=CARTESIAN_POINT('Ctrl Pts',(370.583254402348,-22.6047422436662,-3.21385975027898));
#39840=CARTESIAN_POINT('Ctrl Pts',(370.507309001395,-22.6002524158567,-3.20702268835355));
#39841=CARTESIAN_POINT('Ctrl Pts',(370.406620101294,-22.5943837805416,-3.19434339418074));
#39842=CARTESIAN_POINT('Ctrl Pts',(370.38160615894,-22.5929328169873,-3.19089442892033));
#39843=CARTESIAN_POINT('Ctrl Pts',(370.118439190809,-22.577717848968,-3.15145156950783));
#39844=CARTESIAN_POINT('Ctrl Pts',(369.884993756802,-22.5645969140588,-3.08916200989525));
#39845=CARTESIAN_POINT('Ctrl Pts',(369.551343008246,-22.544106370614,-2.95869407315529));
#39846=CARTESIAN_POINT('Ctrl Pts',(369.4444532531,-22.5372642585771,-2.91001152634442));
#39847=CARTESIAN_POINT('Ctrl Pts',(369.316567139063,-22.528601226433,-2.84311056161835));
#39848=CARTESIAN_POINT('Ctrl Pts',(369.29282879917,-22.5269723726417,-2.83031028776976));
#39849=CARTESIAN_POINT('Ctrl Pts',(369.255426819647,-22.5243714032571,-2.80953214587484));
#39850=CARTESIAN_POINT('Ctrl Pts',(369.241656142435,-22.5234062343577,-2.80174881737241));
#39851=CARTESIAN_POINT('Ctrl Pts',(369.215823303253,-22.5215811106365,-2.78689583881151));
#39852=CARTESIAN_POINT('Ctrl Pts',(369.203748724746,-22.5207219737441,-2.77984843690317));
#39853=CARTESIAN_POINT('Ctrl Pts',(369.176623228777,-22.518778035624,-2.76377893751879));
#39854=CARTESIAN_POINT('Ctrl Pts',(369.161599469324,-22.5176916218334,-2.75471208514711));
#39855=CARTESIAN_POINT('Ctrl Pts',(369.123211731119,-22.5148901899874,-2.7311152257372));
#39856=CARTESIAN_POINT('Ctrl Pts',(369.099958795823,-22.5131687122187,-2.71640812875586));
#39857=CARTESIAN_POINT('Ctrl Pts',(368.90747694444,-22.4987090372795,-2.59118756795139));
#39858=CARTESIAN_POINT('Ctrl Pts',(368.748830111933,-22.4853805015065,-2.46529592096053));
#39859=CARTESIAN_POINT('Ctrl Pts',(368.439693774064,-22.4565270836035,-2.16867212810489));
#39860=CARTESIAN_POINT('Ctrl Pts',(368.293313226137,-22.4410072626153,-1.99516127724561));
#39861=CARTESIAN_POINT('Ctrl Pts',(368.147390020781,-22.4242069970067,-1.77979643637953));
#39862=CARTESIAN_POINT('Ctrl Pts',(368.128898570412,-22.4220495410153,-1.75156023204495));
#39863=CARTESIAN_POINT('Ctrl Pts',(368.104362843625,-22.4191526926294,-1.71277861331031));
#39864=CARTESIAN_POINT('Ctrl Pts',(368.097930317653,-22.4183898949876,-1.70248295112186));
#39865=CARTESIAN_POINT('Ctrl Pts',(368.087263688831,-22.4171196971502,-1.68519370053065));
#39866=CARTESIAN_POINT('Ctrl Pts',(368.082997792968,-22.4166102586024,-1.67821998582673));
#39867=CARTESIAN_POINT('Ctrl Pts',(368.074958850116,-22.4156475845874,-1.66496520646447));
#39868=CARTESIAN_POINT('Ctrl Pts',(368.071180622507,-22.4151940019205,-1.65868740078578));
#39869=CARTESIAN_POINT('Ctrl Pts',(368.062284800896,-22.4141232066181,-1.64379158544372));
#39870=CARTESIAN_POINT('Ctrl Pts',(368.057185900619,-22.4135071945503,-1.63516242116217));
#39871=CARTESIAN_POINT('Ctrl Pts',(368.039474953511,-22.4113590235147,-1.60486734382766));
#39872=CARTESIAN_POINT('Ctrl Pts',(368.027075158065,-22.4098398026188,-1.58307756077528));
#39873=CARTESIAN_POINT('Ctrl Pts',(367.907781650956,-22.3950489428594,-1.3676365184546));
#39874=CARTESIAN_POINT('Ctrl Pts',(367.820824017495,-22.3828236105416,-1.16358333373568));
#39875=CARTESIAN_POINT('Ctrl Pts',(367.691924192908,-22.3584158248751,-0.746798412283902));
#39876=CARTESIAN_POINT('Ctrl Pts',(367.649119630298,-22.3462892245306,-0.535576541975873));
#39877=CARTESIAN_POINT('Ctrl Pts',(367.624416628219,-22.3315008076421,-0.289325118867448));
#39878=CARTESIAN_POINT('Ctrl Pts',(367.621660915153,-22.3295433778472,-0.256924465194356));
#39879=CARTESIAN_POINT('Ctrl Pts',(367.618212063996,-22.3265394617365,-0.207533134624308));
#39880=CARTESIAN_POINT('Ctrl Pts',(367.617162288861,-22.3255041358149,-0.190568903346805));
#39881=CARTESIAN_POINT('Ctrl Pts',(367.615495769845,-22.323611878576,-0.159675719927475));
#39882=CARTESIAN_POINT('Ctrl Pts',(367.614835127737,-22.3227563439161,-0.145749478905231));
#39883=CARTESIAN_POINT('Ctrl Pts',(367.613601405335,-22.3208992680427,-0.11561243796431));
#39884=CARTESIAN_POINT('Ctrl Pts',(367.613060312588,-22.3198967486611,-0.0994007798438235));
#39885=CARTESIAN_POINT('Ctrl Pts',(367.611917262764,-22.3171492188841,-0.0551320548488592));
#39886=CARTESIAN_POINT('Ctrl Pts',(367.61155937483,-22.3153966428901,-0.0270706258412181));
#39887=CARTESIAN_POINT('Ctrl Pts',(367.611612283881,-22.3045829565581,0.144955229369807));
#39888=CARTESIAN_POINT('Ctrl Pts',(367.621302827077,-22.2952341305359,0.288734706018177));
#39889=CARTESIAN_POINT('Ctrl Pts',(367.668697853027,-22.2717071754967,0.639635700406626));
#39890=CARTESIAN_POINT('Ctrl Pts',(367.717129037138,-22.2573193439216,0.844635775710463));
#39891=CARTESIAN_POINT('Ctrl Pts',(367.794265431603,-22.2413995174392,1.07004133787955));
#39892=CARTESIAN_POINT('Ctrl Pts',(367.803711225707,-22.2395293705156,1.09650842504543));
#39893=CARTESIAN_POINT('Ctrl Pts',(367.839622605778,-22.232707118368,1.19312128143747));
#39894=CARTESIAN_POINT('Ctrl Pts',(367.868189489768,-22.2278184363116,1.26246681312823));
#39895=CARTESIAN_POINT('Ctrl Pts',(367.905938017425,-22.2220108502679,1.34572627218807));
#39896=CARTESIAN_POINT('Ctrl Pts',(367.912838908949,-22.2209728885945,1.36064266692296));
#39897=CARTESIAN_POINT('Ctrl Pts',(367.923786854749,-22.2193633906209,1.38383950884999));
#39898=CARTESIAN_POINT('Ctrl Pts',(367.927755717288,-22.218787280989,1.3921562535321));
#39899=CARTESIAN_POINT('Ctrl Pts',(367.935166745954,-22.217725186406,1.40751620618379));
#39900=CARTESIAN_POINT('Ctrl Pts',(367.938598923244,-22.2172386271057,1.4145638529164));
#39901=CARTESIAN_POINT('Ctrl Pts',(367.94648827149,-22.2161321737461,1.43061482901119));
#39902=CARTESIAN_POINT('Ctrl Pts',(367.950961845366,-22.2155133060001,1.43960988479592));
#39903=CARTESIAN_POINT('Ctrl Pts',(367.964901739796,-22.2136105332993,1.46731330447654));
#39904=CARTESIAN_POINT('Ctrl Pts',(367.974508836153,-22.2123350374289,1.48595074080188));
#39905=CARTESIAN_POINT('Ctrl Pts',(367.99738965047,-22.2093763805,1.52929475126235));
#39906=CARTESIAN_POINT('Ctrl Pts',(368.010805505982,-22.2077010518569,1.55392477219541));
#39907=CARTESIAN_POINT('Ctrl Pts',(368.059316331355,-22.2018369392941,1.64028217133379));
#39908=CARTESIAN_POINT('Ctrl Pts',(368.096129599397,-22.197730103909,1.70102480492215));
#39909=CARTESIAN_POINT('Ctrl Pts',(368.254939960526,-22.1811378152163,1.94452995984583));
#39910=CARTESIAN_POINT('Ctrl Pts',(368.393462738948,-22.1691209599349,2.11580246317889));
#39911=CARTESIAN_POINT('Ctrl Pts',(368.64040486064,-22.1491868929606,2.36430183950861));
#39912=CARTESIAN_POINT('Ctrl Pts',(368.738009099589,-22.1416117265743,2.4512570863769));
#39913=CARTESIAN_POINT('Ctrl Pts',(368.862973301372,-22.1320796498359,2.54965257543158));
#39914=CARTESIAN_POINT('Ctrl Pts',(368.885566281338,-22.1303627967389,2.56696217932471));
#39915=CARTESIAN_POINT('Ctrl Pts',(368.921462920414,-22.1276435501531,2.59371733483017));
#39916=CARTESIAN_POINT('Ctrl Pts',(368.934614438044,-22.1266490679695,2.60336523101493));
#39917=CARTESIAN_POINT('Ctrl Pts',(368.959030464327,-22.1248057593544,2.62099319469931));
#39918=CARTESIAN_POINT('Ctrl Pts',(368.970274148213,-22.1239580523437,2.62900155458907));
#39919=CARTESIAN_POINT('Ctrl Pts',(368.99534035114,-22.122070553859,2.6466134193754));
#39920=CARTESIAN_POINT('Ctrl Pts',(369.009187278973,-22.1210294354912,2.65618132184698));
#39921=CARTESIAN_POINT('Ctrl Pts',(369.049340282527,-22.1180145410628,2.68346388750705));
#39922=CARTESIAN_POINT('Ctrl Pts',(369.075833135174,-22.1160303426408,2.70089887711048));
#39923=CARTESIAN_POINT('Ctrl Pts',(369.297491488857,-22.09946532088,2.84212885786059));
#39924=CARTESIAN_POINT('Ctrl Pts',(369.505161956313,-22.0841020747728,2.94496841624281));
#39925=CARTESIAN_POINT('Ctrl Pts',(369.91455574407,-22.0546224190185,3.09552057882965));
#39926=CARTESIAN_POINT('Ctrl Pts',(370.113449153496,-22.0406456606377,3.14778838051105));
#39927=CARTESIAN_POINT('Ctrl Pts',(370.341597952414,-22.0258073034496,3.1849676061297));
#39928=CARTESIAN_POINT('Ctrl Pts',(370.367271750704,-22.02415470334,3.18883357826953));
#39929=CARTESIAN_POINT('Ctrl Pts',(370.403067826214,-22.0218769940768,3.19378215793963));
#39930=CARTESIAN_POINT('Ctrl Pts',(370.413151967347,-22.0212382523578,3.19512759702493));
#39931=CARTESIAN_POINT('Ctrl Pts',(370.430547459083,-22.0201416176846,3.19736473940421));
#39932=CARTESIAN_POINT('Ctrl Pts',(370.437855736055,-22.0196824793025,3.19827916233054));
#39933=CARTESIAN_POINT('Ctrl Pts',(370.453239805592,-22.0187194094488,3.20015049893188));
#39934=CARTESIAN_POINT('Ctrl Pts',(370.461316189459,-22.0182158051448,3.20110191265379));
#39935=CARTESIAN_POINT('Ctrl Pts',(370.481250456995,-22.0169775249502,3.20337374119091));
#39936=CARTESIAN_POINT('Ctrl Pts',(370.493112381309,-22.0162448028569,3.20465891294888));
#39937=CARTESIAN_POINT('Ctrl Pts',(370.537078155534,-22.0135433401442,3.20917547031835));
#39938=CARTESIAN_POINT('Ctrl Pts',(370.569224035159,-22.0115964460134,3.21199067333927));
#39939=CARTESIAN_POINT('Ctrl Pts',(370.803393819919,-21.9975846718547,3.22895860734334));
#39940=CARTESIAN_POINT('Ctrl Pts',(371.006335553882,-21.9863442066119,3.22452483097958));
#39941=CARTESIAN_POINT('Ctrl Pts',(371.416293280266,-21.9632631396498,3.17672679826232));
#39942=CARTESIAN_POINT('Ctrl Pts',(371.622141640787,-21.9514553842187,3.13202951747999));
#39943=CARTESIAN_POINT('Ctrl Pts',(371.857966820673,-21.9367480102533,3.05608821134147));
#39944=CARTESIAN_POINT('Ctrl Pts',(371.893564299402,-21.934496363534,3.04393317186487));
#39945=CARTESIAN_POINT('Ctrl Pts',(371.948149643752,-21.9309907019908,3.0242211304565));
#39946=CARTESIAN_POINT('Ctrl Pts',(371.967292738687,-21.9297510888913,3.01710168585497));
#39947=CARTESIAN_POINT('Ctrl Pts',(371.999702433401,-21.927634477982,3.00469636487816));
#39948=CARTESIAN_POINT('Ctrl Pts',(372.013004084916,-21.9267606018636,2.99950332917185));
#39949=CARTESIAN_POINT('Ctrl Pts',(372.039870571419,-21.9249848593066,2.98880820319062));
#39950=CARTESIAN_POINT('Ctrl Pts',(372.053433297567,-21.9240828625618,2.98330175374703));
#39951=CARTESIAN_POINT('Ctrl Pts',(372.086826013824,-21.9218480528061,2.96947861699129));
#39952=CARTESIAN_POINT('Ctrl Pts',(372.106610952183,-21.9205116628002,2.96105558602107));
#39953=CARTESIAN_POINT('Ctrl Pts',(372.180601611237,-21.9154667081681,2.92867711883052));
#39954=CARTESIAN_POINT('Ctrl Pts',(372.234224708035,-21.911714342546,2.90342722946176));
#39955=CARTESIAN_POINT('Ctrl Pts',(372.294701480411,-21.9073686153834,2.87288520306915));
#39956=CARTESIAN_POINT('Ctrl Pts',(372.3022688911,-21.9068227714453,2.8690258740493));
#39957=CARTESIAN_POINT('Ctrl Pts',(372.30982061585,-21.9062759889522,2.86513684838664));
#39958=CARTESIAN_POINT('',(367.611568766713,-22.0642265507751,0.00242649832743659));
#39959=CARTESIAN_POINT('Ctrl Pts',(372.309820475366,-21.6596622257337,2.86513692073373));
#39960=CARTESIAN_POINT('Ctrl Pts',(372.15720255111,-21.6696054137955,2.94373286698527));
#39961=CARTESIAN_POINT('Ctrl Pts',(371.998464664616,-21.6791174589537,3.01005219247402));
#39962=CARTESIAN_POINT('Ctrl Pts',(371.636719776143,-21.7004247473343,3.12823047273937));
#39963=CARTESIAN_POINT('Ctrl Pts',(371.432535462295,-21.7122360244881,3.17360910930486));
#39964=CARTESIAN_POINT('Ctrl Pts',(371.198185196885,-21.7263662855851,3.20226021354722));
#39965=CARTESIAN_POINT('Ctrl Pts',(371.170918071698,-21.7280182410862,3.20524104274543));
#39966=CARTESIAN_POINT('Ctrl Pts',(371.12616871568,-21.7307437208177,3.20955571750068));
#39967=CARTESIAN_POINT('Ctrl Pts',(371.108707434098,-21.7318107829302,3.2110956336877));
#39968=CARTESIAN_POINT('Ctrl Pts',(371.07729088784,-21.7337374368571,3.21360814988941));
#39969=CARTESIAN_POINT('Ctrl Pts',(371.063340117727,-21.7345953834297,3.21463248742269));
#39970=CARTESIAN_POINT('Ctrl Pts',(371.033567836235,-21.7364316297104,3.21662373527376));
#39971=CARTESIAN_POINT('Ctrl Pts',(371.017745022203,-21.7374107164302,3.21756480422641));
#39972=CARTESIAN_POINT('Ctrl Pts',(370.974867390853,-21.7400728472851,3.21979766576227));
#39973=CARTESIAN_POINT('Ctrl Pts',(370.947802656645,-21.7417628521499,3.22086514905843));
#39974=CARTESIAN_POINT('Ctrl Pts',(370.801742683221,-21.7509374969785,3.22478281290298));
#39975=CARTESIAN_POINT('Ctrl Pts',(370.682685366382,-21.7586150860404,3.22137970072268));
#39976=CARTESIAN_POINT('Ctrl Pts',(370.408531303646,-21.7767436642974,3.19831148923421));
#39977=CARTESIAN_POINT('Ctrl Pts',(370.254129888967,-21.7872951779175,3.17393535632644));
#39978=CARTESIAN_POINT('Ctrl Pts',(369.938826625605,-21.8091971328656,3.10037537880386));
#39979=CARTESIAN_POINT('Ctrl Pts',(369.778743908101,-21.8205155936598,3.04959117024204));
#39980=CARTESIAN_POINT('Ctrl Pts',(369.598359065231,-21.8330214872617,2.97644913027678));
#39981=CARTESIAN_POINT('Ctrl Pts',(369.57351646754,-21.8347377708286,2.96601138345266));
#39982=CARTESIAN_POINT('Ctrl Pts',(369.539334873628,-21.8370879920982,2.95114271732617));
#39983=CARTESIAN_POINT('Ctrl Pts',(369.529882678033,-21.8377366928928,2.94697694867391));
#39984=CARTESIAN_POINT('Ctrl Pts',(369.513685020318,-21.8388460565771,2.93974512149232));
#39985=CARTESIAN_POINT('Ctrl Pts',(369.506929871898,-21.8393080276134,2.93670114385904));
#39986=CARTESIAN_POINT('Ctrl Pts',(369.49281133788,-21.8402720401648,2.93028043898301));
#39987=CARTESIAN_POINT('Ctrl Pts',(369.485450104011,-21.8407737821897,2.92689920884158));
#39988=CARTESIAN_POINT('Ctrl Pts',(369.468492659415,-21.8419277316657,2.91903259752636));
#39989=CARTESIAN_POINT('Ctrl Pts',(369.45890556076,-21.8425787442681,2.91452754293065));
#39990=CARTESIAN_POINT('Ctrl Pts',(369.424775032174,-21.8448920300211,2.8982834175181));
#39991=CARTESIAN_POINT('Ctrl Pts',(369.400357482516,-21.8465389339236,2.88628056483274));
#39992=CARTESIAN_POINT('Ctrl Pts',(369.340679306922,-21.8505512477435,2.85600044460679));
#39993=CARTESIAN_POINT('Ctrl Pts',(369.305598226387,-21.8528986613721,2.83737752672048));
#39994=CARTESIAN_POINT('Ctrl Pts',(369.163484569218,-21.8623982678518,2.75853480965307));
#39995=CARTESIAN_POINT('Ctrl Pts',(369.059585121429,-21.8693229051471,2.69286581003269));
#39996=CARTESIAN_POINT('Ctrl Pts',(368.747824252617,-21.8907998418315,2.46991876110876));
#39997=CARTESIAN_POINT('Ctrl Pts',(368.555137462499,-21.9052073193631,2.2933113135743));
#39998=CARTESIAN_POINT('Ctrl Pts',(368.360225706862,-21.9230317259545,2.06555886163211));
#39999=CARTESIAN_POINT('Ctrl Pts',(368.335195661523,-21.9253916888148,2.03520353475155));
#40000=CARTESIAN_POINT('Ctrl Pts',(368.299444921123,-21.928872625577,1.99019243067548));
#40001=CARTESIAN_POINT('Ctrl Pts',(368.288281822289,-21.9299759351463,1.97589149533118));
#40002=CARTESIAN_POINT('Ctrl Pts',(368.268660770095,-21.9319450354443,1.95031279403572));
#40003=CARTESIAN_POINT('Ctrl Pts',(368.260154884994,-21.9328089074328,1.93907226936395));
#40004=CARTESIAN_POINT('Ctrl Pts',(368.242545577739,-21.9346191225584,1.91548151313104));
#40005=CARTESIAN_POINT('Ctrl Pts',(368.233456078819,-21.9355659783712,1.90312137620516));
#40006=CARTESIAN_POINT('Ctrl Pts',(368.209928759807,-21.9380499912831,1.87064495639728));
#40007=CARTESIAN_POINT('Ctrl Pts',(368.195634126757,-21.9395925983478,1.85042665438473));
#40008=CARTESIAN_POINT('Ctrl Pts',(368.1314320321,-21.9466773620323,1.75736249585734));
#40009=CARTESIAN_POINT('Ctrl Pts',(368.08430257063,-21.9523224934432,1.6826551156313));
#40010=CARTESIAN_POINT('Ctrl Pts',(367.971273251686,-21.9670814143888,1.48602779920037));
#40011=CARTESIAN_POINT('Ctrl Pts',(367.910063524424,-21.9763319528122,1.36162881281598));
#40012=CARTESIAN_POINT('Ctrl Pts',(367.806771086688,-21.9945387165853,1.11235280351233));
#40013=CARTESIAN_POINT('Ctrl Pts',(367.763956825202,-22.0034674198314,0.988054720714536));
#40014=CARTESIAN_POINT('Ctrl Pts',(367.719479566163,-22.0145941420502,0.827724497566529));
#40015=CARTESIAN_POINT('Ctrl Pts',(367.710663772789,-22.0169259591233,0.793807730461049));
#40016=CARTESIAN_POINT('Ctrl Pts',(367.685633394994,-22.0239416283017,0.690625496999164));
#40017=CARTESIAN_POINT('Ctrl Pts',(367.671155987291,-22.0285729763092,0.620955764132295));
#40018=CARTESIAN_POINT('Ctrl Pts',(367.65622806814,-22.0341194728747,0.534906541002544));
#40019=CARTESIAN_POINT('Ctrl Pts',(367.65358086441,-22.0351417551776,0.518933447614696));
#40020=CARTESIAN_POINT('Ctrl Pts',(367.649624001201,-22.0367324567524,0.493889263945372));
#40021=CARTESIAN_POINT('Ctrl Pts',(367.648232508244,-22.0373052803712,0.484831636289578));
#40022=CARTESIAN_POINT('Ctrl Pts',(367.645720503549,-22.0383648473461,0.468002302179814));
#40023=CARTESIAN_POINT('Ctrl Pts',(367.644589763945,-22.0388521349285,0.460232475466851));
#40024=CARTESIAN_POINT('Ctrl Pts',(367.642410505258,-22.0398122952688,0.44486388903691));
#40025=CARTESIAN_POINT('Ctrl Pts',(367.641360720088,-22.0402852380351,0.437265533234733));
#40026=CARTESIAN_POINT('Ctrl Pts',(367.639007558378,-22.0413701111036,0.419772884890152));
#40027=CARTESIAN_POINT('Ctrl Pts',(367.637722984271,-22.0419810181206,0.409876084887379));
#40028=CARTESIAN_POINT('Ctrl Pts',(367.634520268729,-22.0435545488452,0.384270000244196));
#40029=CARTESIAN_POINT('Ctrl Pts',(367.632671806503,-22.0445135623278,0.368552070056182));
#40030=CARTESIAN_POINT('Ctrl Pts',(367.618127851558,-22.0525175341208,0.236502619217367));
#40031=CARTESIAN_POINT('Ctrl Pts',(367.611660397471,-22.0592628964552,0.119562495099769));
#40032=CARTESIAN_POINT('Ctrl Pts',(367.611568839302,-22.0658953423866,0.0025210645287454));
#40033=CARTESIAN_POINT('Ctrl Pts',(367.611568766713,-22.0642265507751,0.00242649832743659));
#40034=CARTESIAN_POINT('Ctrl Pts',(367.61149490218,-22.0703030074805,-0.0956765390764883));
#40035=CARTESIAN_POINT('Ctrl Pts',(367.615904730246,-22.076379464186,-0.193948280684805));
#40036=CARTESIAN_POINT('Ctrl Pts',(367.624817916114,-22.0824559208914,-0.291937863578686));
#40037=CARTESIAN_POINT('Ctrl Pts',(367.634068124722,-22.0887621387753,-0.393632599514726));
#40038=CARTESIAN_POINT('Ctrl Pts',(367.648169083226,-22.0950683566592,-0.495022935142761));
#40039=CARTESIAN_POINT('Ctrl Pts',(367.667083341441,-22.1013745745431,-0.595603147969471));
#40040=CARTESIAN_POINT('Ctrl Pts',(367.685274214606,-22.107439608042,-0.692336621399258));
#40041=CARTESIAN_POINT('Ctrl Pts',(367.707916867878,-22.1135046415409,-0.788320316617951));
#40042=CARTESIAN_POINT('Ctrl Pts',(367.734925204045,-22.1195696750397,-0.883109714992833));
#40043=CARTESIAN_POINT('Ctrl Pts',(367.761923563297,-22.1256324681073,-0.977864098039831));
#40044=CARTESIAN_POINT('Ctrl Pts',(367.793284280533,-22.1316952611748,-1.07142462983612));
#40045=CARTESIAN_POINT('Ctrl Pts',(367.8288706626,-22.1377580542424,-1.16335925099373));
#40046=CARTESIAN_POINT('Ctrl Pts',(367.864454056667,-22.1438203382491,-1.25528615288583));
#40047=CARTESIAN_POINT('Ctrl Pts',(367.904262248197,-22.1498826222559,-1.34558699777065));
#40048=CARTESIAN_POINT('Ctrl Pts',(367.94810981923,-22.1559449062627,-1.43384823011757));
#40049=CARTESIAN_POINT('Ctrl Pts',(367.991966225147,-22.162008411764,-1.52212724629151));
#40050=CARTESIAN_POINT('Ctrl Pts',(368.03986342594,-22.1680719172652,-1.60836543339431));
#40051=CARTESIAN_POINT('Ctrl Pts',(368.091569889003,-22.1741354227665,-1.69217350388752));
#40052=CARTESIAN_POINT('Ctrl Pts',(368.143331202225,-22.1802053604279,-1.77607047789136));
#40053=CARTESIAN_POINT('Ctrl Pts',(368.198909603746,-22.1862752980892,-1.85753181076433));
#40054=CARTESIAN_POINT('Ctrl Pts',(368.258030269901,-22.1923452357506,-1.93619726539244));
#40055=CARTESIAN_POINT('Ctrl Pts',(368.317188279368,-22.1984190074618,-2.01491240871425));
#40056=CARTESIAN_POINT('Ctrl Pts',(368.379892718554,-22.204492779173,-2.09082781700198));
#40057=CARTESIAN_POINT('Ctrl Pts',(368.445829956663,-22.2105665508842,-2.16361806483572));
#40058=CARTESIAN_POINT('Ctrl Pts',(368.51186647817,-22.2166494680298,-2.23651791482009));
#40059=CARTESIAN_POINT('Ctrl Pts',(368.581145192527,-22.2227323851755,-2.30628290284342));
#40060=CARTESIAN_POINT('Ctrl Pts',(368.65331761671,-22.2288153023212,-2.37262629396778));
#40061=CARTESIAN_POINT('Ctrl Pts',(368.673052085238,-22.2304785849159,-2.39076690070184));
#40062=CARTESIAN_POINT('Ctrl Pts',(368.693002731649,-22.2321418675107,-2.4086519303531));
#40063=CARTESIAN_POINT('Ctrl Pts',(368.713162052515,-22.2338051501055,-2.42627608313987));
#40064=CARTESIAN_POINT('Ctrl Pts',(368.7879867928,-22.2399787057032,-2.49169111690126));
#40065=CARTESIAN_POINT('Ctrl Pts',(368.865971414356,-22.2461522613009,-2.55375612836349));
#40066=CARTESIAN_POINT('Ctrl Pts',(368.946783406865,-22.2523258168986,-2.61215069938684));
#40067=CARTESIAN_POINT('Ctrl Pts',(369.027486316182,-22.2584910391893,-2.67046644713183));
#40068=CARTESIAN_POINT('Ctrl Pts',(369.111008661803,-22.2646562614799,-2.72512135014984));
#40069=CARTESIAN_POINT('Ctrl Pts',(369.196983264425,-22.2708214837706,-2.77583374985307));
#40070=CARTESIAN_POINT('Ctrl Pts',(369.282867184459,-22.2769802032302,-2.82649266013559));
#40071=CARTESIAN_POINT('Ctrl Pts',(369.371197847217,-22.2831389226898,-2.8732171151454));
#40072=CARTESIAN_POINT('Ctrl Pts',(369.461578149132,-22.2892976421493,-2.91576804072415));
#40073=CARTESIAN_POINT('Ctrl Pts',(369.551892819251,-22.295451889309,-2.95828806694153));
#40074=CARTESIAN_POINT('Ctrl Pts',(369.644253777684,-22.3016061364688,-2.9966404049843));
#40075=CARTESIAN_POINT('Ctrl Pts',(369.738239120822,-22.3077603836285,-3.03063177817354));
#40076=CARTESIAN_POINT('Ctrl Pts',(369.832189133076,-22.3139123172893,-3.06461037335698));
#40077=CARTESIAN_POINT('Ctrl Pts',(369.927761908852,-22.3200642509501,-3.09423111367641));
#40078=CARTESIAN_POINT('Ctrl Pts',(370.024516181735,-22.3262161846108,-3.11934910123139));
#40079=CARTESIAN_POINT('Ctrl Pts',(370.121259931609,-22.3323674491864,-3.14446435695037));
#40080=CARTESIAN_POINT('Ctrl Pts',(370.219184502878,-22.338518713762,-3.1650777244909));
#40081=CARTESIAN_POINT('Ctrl Pts',(370.317835081649,-22.3446699783376,-3.18109464008319));
#40082=CARTESIAN_POINT('Ctrl Pts',(370.416501286305,-22.3508222172506,-3.19711409269532));
#40083=CARTESIAN_POINT('Ctrl Pts',(370.515893298302,-22.3569744561636,-3.20853557764327));
#40084=CARTESIAN_POINT('Ctrl Pts',(370.615548765499,-22.3631266950766,-3.21531610401774));
#40085=CARTESIAN_POINT('Ctrl Pts',(370.715310527321,-22.3692854960975,-3.22210386264477));
#40086=CARTESIAN_POINT('Ctrl Pts',(370.815335871493,-22.3754442971184,-3.22424074843573));
#40087=CARTESIAN_POINT('Ctrl Pts',(370.915160130291,-22.3816030981393,-3.22173588128178));
#40088=CARTESIAN_POINT('Ctrl Pts',(371.015040260087,-22.3877653462017,-3.21922961216972));
#40089=CARTESIAN_POINT('Ctrl Pts',(371.114718647339,-22.3939275942641,-3.21207644735806));
#40090=CARTESIAN_POINT('Ctrl Pts',(371.213735526934,-22.4000898423265,-3.20033744961007));
#40091=CARTESIAN_POINT('Ctrl Pts',(371.312916739533,-22.4062623175416,-3.18857896927706));
#40092=CARTESIAN_POINT('Ctrl Pts',(371.411433823139,-22.4124347927566,-3.17221952512817));
#40093=CARTESIAN_POINT('Ctrl Pts',(371.508836858696,-22.4186072679716,-3.15137139571912));
#40094=CARTESIAN_POINT('Ctrl Pts',(371.580973515862,-22.4231786011534,-3.1359312777072));
#40095=CARTESIAN_POINT('Ctrl Pts',(371.652499354296,-22.4277499343352,-3.11803024189166));
#40096=CARTESIAN_POINT('Ctrl Pts',(371.723237922332,-22.432321267517,-3.09773121384613));
#40097=CARTESIAN_POINT('Ctrl Pts',(371.818769919459,-22.4384948246092,-3.07031750244726));
#40098=CARTESIAN_POINT('Ctrl Pts',(371.913199866761,-22.4446683817013,-3.03843243676399));
#40099=CARTESIAN_POINT('Ctrl Pts',(372.006078257194,-22.4508419387934,-3.00218172637621));
#40100=CARTESIAN_POINT('Ctrl Pts',(372.098831277111,-22.4570071626011,-2.96597994847164));
#40101=CARTESIAN_POINT('Ctrl Pts',(372.190036502055,-22.4631723864089,-2.92542439530771));
#40102=CARTESIAN_POINT('Ctrl Pts',(372.279258200579,-22.4693376102166,-2.88067092099817));
#40103=CARTESIAN_POINT('Ctrl Pts',(372.368385791926,-22.4754963312137,-2.8359646507122));
#40104=CARTESIAN_POINT('Ctrl Pts',(372.455533630333,-22.4816550522108,-2.78706945586543));
#40105=CARTESIAN_POINT('Ctrl Pts',(372.54028554618,-22.4878137732079,-2.73418942158186));
#40106=CARTESIAN_POINT('Ctrl Pts',(372.624975917764,-22.4939680219291,-2.6813477871705));
#40107=CARTESIAN_POINT('Ctrl Pts',(372.7072734587,-22.5001222706504,-2.62452729563315));
#40108=CARTESIAN_POINT('Ctrl Pts',(372.786787039032,-22.5062765193716,-2.56397769900044));
#40109=CARTESIAN_POINT('Ctrl Pts',(372.866270728882,-22.5124284546081,-2.50345086397094));
#40110=CARTESIAN_POINT('Ctrl Pts',(372.942972192604,-22.5185803898446,-2.43919797207752));
#40111=CARTESIAN_POINT('Ctrl Pts',(373.016530456563,-22.5247323250811,-2.37151127265513));
#40112=CARTESIAN_POINT('Ctrl Pts',(373.090080720462,-22.5308835912447,-2.30383193471127));
#40113=CARTESIAN_POINT('Ctrl Pts',(373.160488144793,-22.5370348574083,-2.23271982573149));
#40114=CARTESIAN_POINT('Ctrl Pts',(373.227426707879,-22.5431861235718,-2.15850586570228));
#40115=CARTESIAN_POINT('Ctrl Pts',(373.294375873894,-22.5493383640831,-2.08428015033702));
#40116=CARTESIAN_POINT('Ctrl Pts',(373.357854796475,-22.5554906045944,-2.00695193042528));
#40117=CARTESIAN_POINT('Ctrl Pts',(373.417576704477,-22.5616428451056,-1.92688641853166));
#40118=CARTESIAN_POINT('Ctrl Pts',(373.477362313167,-22.5678016477307,-1.84673550701894));
#40119=CARTESIAN_POINT('Ctrl Pts',(373.533382645166,-22.5739604503557,-1.76384182205795));
#40120=CARTESIAN_POINT('Ctrl Pts',(373.585393463147,-22.5801192529807,-1.67860077176959));
#40121=CARTESIAN_POINT('Ctrl Pts',(373.637433391291,-22.5862815026529,-1.59331201254414));
#40122=CARTESIAN_POINT('Ctrl Pts',(373.685459127654,-22.5924437523252,-1.50567365227615));
#40123=CARTESIAN_POINT('Ctrl Pts',(373.729272740669,-22.5986060019974,-1.41610513810223));
#40124=CARTESIAN_POINT('Ctrl Pts',(373.773159068715,-22.6047784788148,-1.32638797201701));
#40125=CARTESIAN_POINT('Ctrl Pts',(373.812819137771,-22.6109509556321,-1.23473465216716));
#40126=CARTESIAN_POINT('Ctrl Pts',(373.848103390945,-22.6171234324495,-1.14158411653432));
#40127=CARTESIAN_POINT('Ctrl Pts',(373.874234801161,-22.6216947499426,-1.07259711413171));
#40128=CARTESIAN_POINT('Ctrl Pts',(373.897967168603,-22.6262660674357,-1.00278930654557));
#40129=CARTESIAN_POINT('Ctrl Pts',(373.919257714423,-22.6308373849288,-0.932343078103629));
#40130=CARTESIAN_POINT('Ctrl Pts',(373.948010513183,-22.6370109313029,-0.837205722445122));
#40131=CARTESIAN_POINT('Ctrl Pts',(373.972408582359,-22.643184477677,-0.740570465601611));
#40132=CARTESIAN_POINT('Ctrl Pts',(373.99229706809,-22.6493580240511,-0.642872336453218));
#40133=CARTESIAN_POINT('Ctrl Pts',(374.012158707525,-22.6555232371186,-0.545306084256246));
#40134=CARTESIAN_POINT('Ctrl Pts',(374.027522776871,-22.661688450186,-0.446680233157299));
#40135=CARTESIAN_POINT('Ctrl Pts',(374.038284026963,-22.6678536632534,-0.347445420230547));
#40136=CARTESIAN_POINT('Ctrl Pts',(374.04903392652,-22.674012373502,-0.248315276194083));
#40137=CARTESIAN_POINT('Ctrl Pts',(374.055190612357,-22.6801710837505,-0.148577876587435));
#40138=CARTESIAN_POINT('Ctrl Pts',(374.056699968837,-22.6863297939991,-0.0486935671092582));
#40139=CARTESIAN_POINT('Ctrl Pts',(374.058208229274,-22.6924840320034,0.0511182098073811));
#40140=CARTESIAN_POINT('Ctrl Pts',(374.055075863433,-22.6986382700078,0.151076251681782));
#40141=CARTESIAN_POINT('Ctrl Pts',(374.047300704171,-22.7047925080121,0.250716497300676));
#40142=CARTESIAN_POINT('Ctrl Pts',(374.039528467698,-22.7109444325545,0.350319286793416));
#40143=CARTESIAN_POINT('Ctrl Pts',(374.027116939493,-22.7170963570968,0.449604085043901));
#40144=CARTESIAN_POINT('Ctrl Pts',(374.010116011264,-22.7232482816392,0.548109133190833));
#40145=CARTESIAN_POINT('Ctrl Pts',(373.99311693193,-22.729399537144,0.646603468659849));
#40146=CARTESIAN_POINT('Ctrl Pts',(373.971529518756,-22.7355507926487,0.744317794796839));
#40147=CARTESIAN_POINT('Ctrl Pts',(373.945455106497,-22.7417020481534,0.84079875939419));
#40148=CARTESIAN_POINT('Ctrl Pts',(373.919376563894,-22.7478542780537,0.93729500715171));
#40149=CARTESIAN_POINT('Ctrl Pts',(373.888809723702,-22.754006507954,1.03255708615276));
#40150=CARTESIAN_POINT('Ctrl Pts',(373.853906015083,-22.7601587378543,1.1261460363838));
#40151=CARTESIAN_POINT('Ctrl Pts',(373.818965076553,-22.7663175300076,1.21983481291871));
#40152=CARTESIAN_POINT('Ctrl Pts',(373.779678184323,-22.7724763221609,1.31184648945386));
#40153=CARTESIAN_POINT('Ctrl Pts',(373.736245199107,-22.7786351143142,1.40176147818316));
#40154=CARTESIAN_POINT('Ctrl Pts',(373.692787904219,-22.784797353576,1.49172679280622));
#40155=CARTESIAN_POINT('Ctrl Pts',(373.645180101722,-22.7909595928378,1.57959270082742));
#40156=CARTESIAN_POINT('Ctrl Pts',(373.593666955272,-22.7971218320996,1.66496549379406));
#40157=CARTESIAN_POINT('Ctrl Pts',(373.542068313422,-22.8032942987141,1.75047997838042));
#40158=CARTESIAN_POINT('Ctrl Pts',(373.486551622581,-22.8094667653285,1.83349272205318));
#40159=CARTESIAN_POINT('Ctrl Pts',(373.427404649069,-22.815639231943,1.91364009983924));
#40160=CARTESIAN_POINT('Ctrl Pts',(373.383599493119,-22.8202106554088,1.9729984773599));
#40161=CARTESIAN_POINT('Ctrl Pts',(373.337803971307,-22.8247820788746,2.03078581500396));
#40162=CARTESIAN_POINT('Ctrl Pts',(373.290148161389,-22.8293535023404,2.08686728375234));
#40163=CARTESIAN_POINT('Ctrl Pts',(373.222538649734,-22.8358390013515,2.16643031544849));
#40164=CARTESIAN_POINT('Ctrl Pts',(373.150934271423,-22.8423245003625,2.24285075309167));
#40165=CARTESIAN_POINT('Ctrl Pts',(373.075662772314,-22.8488099993736,2.31570518766263));
#40166=CARTESIAN_POINT('Ctrl Pts',(373.004120718376,-22.8549741641048,2.38494993433884));
#40167=CARTESIAN_POINT('Ctrl Pts',(372.929266562978,-22.8611383288359,2.45097319270896));
#40168=CARTESIAN_POINT('Ctrl Pts',(372.85142373199,-22.8673024935671,2.51344413829839));
#40169=CARTESIAN_POINT('Ctrl Pts',(372.773652963371,-22.8734609518727,2.57585725191674));
#40170=CARTESIAN_POINT('Ctrl Pts',(372.69289935254,-22.8796194101784,2.63472431588723));
#40171=CARTESIAN_POINT('Ctrl Pts',(372.609522090141,-22.8857778684841,2.6897523082492));
#40172=CARTESIAN_POINT('Ctrl Pts',(372.52620826623,-22.8919316410604,2.74473843197019));
#40173=CARTESIAN_POINT('Ctrl Pts',(372.440275122555,-22.8980854136366,2.79589105555995));
#40174=CARTESIAN_POINT('Ctrl Pts',(372.352112829219,-22.9042391862129,2.84295901717621));
#40175=CARTESIAN_POINT('Ctrl Pts',(372.338071363139,-22.905219287633,2.8504554554098));
#40176=CARTESIAN_POINT('Ctrl Pts',(372.323973410745,-22.9061993890532,2.8578483700235));
#40177=CARTESIAN_POINT('Ctrl Pts',(372.309820613641,-22.9071794904733,2.86513684952399));
#40178=CARTESIAN_POINT('Origin',(370.834317853224,2.31077344927308,0.));
#40179=CARTESIAN_POINT('',(372.309820613641,-24.4036702759163,2.86513684952401));
#40180=CARTESIAN_POINT('',(372.309820613613,-24.1556143901908,2.8651368495388));
#40181=CARTESIAN_POINT('',(372.309820613641,2.31077344927308,2.86513684952399));
#40182=CARTESIAN_POINT('',(367.611569215287,-23.5607734493238,-0.00296296689770666));
#40183=CARTESIAN_POINT('Ctrl Pts',(367.611569215287,-23.5607734493238,-0.00296296689770666));
#40184=CARTESIAN_POINT('Ctrl Pts',(367.611692406337,-23.5690424041229,-0.136954943290668));
#40185=CARTESIAN_POINT('Ctrl Pts',(367.620176327635,-23.577311358922,-0.270574321379934));
#40186=CARTESIAN_POINT('Ctrl Pts',(367.636856717719,-23.5855803137211,-0.402939014537645));
#40187=CARTESIAN_POINT('Ctrl Pts',(367.653537107804,-23.5938492685202,-0.535303707695356));
#40188=CARTESIAN_POINT('Ctrl Pts',(367.678413783074,-23.6021182233193,-0.66641417607396));
#40189=CARTESIAN_POINT('Ctrl Pts',(367.711269345869,-23.6103871781184,-0.795415352636087));
#40190=CARTESIAN_POINT('Ctrl Pts',(367.735803278768,-23.6165617788534,-0.891743217399455));
#40191=CARTESIAN_POINT('Ctrl Pts',(367.764841010137,-23.6227363795885,-0.987103344829856));
#40192=CARTESIAN_POINT('Ctrl Pts',(367.798290303457,-23.6289109803235,-1.08104314417068));
#40193=CARTESIAN_POINT('Ctrl Pts',(367.831694437508,-23.6350772448446,-1.17485611713065));
#40194=CARTESIAN_POINT('Ctrl Pts',(367.869498150779,-23.6412435093657,-1.2672521681585));
#40195=CARTESIAN_POINT('Ctrl Pts',(367.911558672564,-23.6474097738868,-1.35779097594902));
#40196=CARTESIAN_POINT('Ctrl Pts',(367.953574809394,-23.6535695313708,-1.448234241393));
#40197=CARTESIAN_POINT('Ctrl Pts',(367.999838642044,-23.6597292888548,-1.53682376866967));
#40198=CARTESIAN_POINT('Ctrl Pts',(368.050158604511,-23.6658890463388,-1.62313734486777));
#40199=CARTESIAN_POINT('Ctrl Pts',(368.10044194652,-23.6720443210465,-1.70938810618064));
#40200=CARTESIAN_POINT('Ctrl Pts',(368.154775331463,-23.6781995957541,-1.79336583575048));
#40201=CARTESIAN_POINT('Ctrl Pts',(368.212920796576,-23.6843548704617,-1.87467198034734));
#40202=CARTESIAN_POINT('Ctrl Pts',(368.271044343581,-23.6905078249199,-1.95594747634661));
#40203=CARTESIAN_POINT('Ctrl Pts',(368.332976863224,-23.6966607793781,-2.03455303583693));
#40204=CARTESIAN_POINT('Ctrl Pts',(368.398437009064,-23.7028137338363,-2.11011897189568));
#40205=CARTESIAN_POINT('Ctrl Pts',(368.463889952418,-23.7089660112937,-2.18567659354284));
#40206=CARTESIAN_POINT('Ctrl Pts',(368.532869466085,-23.7151182887511,-2.25819492869112));
#40207=CARTESIAN_POINT('Ctrl Pts',(368.605054499426,-23.7212705662085,-2.32733806352102));
#40208=CARTESIAN_POINT('Ctrl Pts',(368.677250858103,-23.727423808916,-2.39649204643378));
#40209=CARTESIAN_POINT('Ctrl Pts',(368.75265342196,-23.7335770516235,-2.46226947697302));
#40210=CARTESIAN_POINT('Ctrl Pts',(368.830905681368,-23.739730294331,-2.52437264130288));
#40211=CARTESIAN_POINT('Ctrl Pts',(368.909241136097,-23.7458900789711,-2.58654183174805));
#40212=CARTESIAN_POINT('Ctrl Pts',(368.99043199569,-23.7520498636111,-2.64502868519833));
#40213=CARTESIAN_POINT('Ctrl Pts',(369.074090287861,-23.7582096482512,-2.69957709292313));
#40214=CARTESIAN_POINT('Ctrl Pts',(369.157795263888,-23.7643728702374,-2.75415594030923));
#40215=CARTESIAN_POINT('Ctrl Pts',(369.243970040455,-23.7705360922235,-2.80479174516912));
#40216=CARTESIAN_POINT('Ctrl Pts',(369.332201218711,-23.7766993142097,-2.85127395716686));
#40217=CARTESIAN_POINT('Ctrl Pts',(369.420578436674,-23.7828727375233,-2.89783310623801));
#40218=CARTESIAN_POINT('Ctrl Pts',(369.511018461915,-23.7890461608368,-2.94022474592278));
#40219=CARTESIAN_POINT('Ctrl Pts',(369.603086953579,-23.7952195841504,-2.97828609006258));
#40220=CARTESIAN_POINT('Ctrl Pts',(369.67111180803,-23.799780821277,-3.00640773459576));
#40221=CARTESIAN_POINT('Ctrl Pts',(369.740025219121,-23.8043420584035,-3.03216648065162));
#40222=CARTESIAN_POINT('Ctrl Pts',(369.809647408009,-23.8089032955301,-3.05551436606063));
#40223=CARTESIAN_POINT('Ctrl Pts',(369.903886288049,-23.8150772737584,-3.08711748867723));
#40224=CARTESIAN_POINT('Ctrl Pts',(369.999753264778,-23.8212512519868,-3.11441194208328));
#40225=CARTESIAN_POINT('Ctrl Pts',(370.096818059282,-23.8274252302152,-3.13722992725036));
#40226=CARTESIAN_POINT('Ctrl Pts',(370.193752031933,-23.8335908872878,-3.16001715882533));
#40227=CARTESIAN_POINT('Ctrl Pts',(370.291880194628,-23.8397565443605,-3.17833981576138));
#40228=CARTESIAN_POINT('Ctrl Pts',(370.390755187851,-23.8459222014331,-3.19207921649617));
#40229=CARTESIAN_POINT('Ctrl Pts',(370.489526082069,-23.8520813670892,-3.20580415191577));
#40230=CARTESIAN_POINT('Ctrl Pts',(370.589041815961,-23.8582405327454,-3.21495536528608));
#40231=CARTESIAN_POINT('Ctrl Pts',(370.688843799736,-23.8643996984015,-3.21946499627839));
#40232=CARTESIAN_POINT('Ctrl Pts',(370.788573560222,-23.8705544068796,-3.22397136380465));
#40233=CARTESIAN_POINT('Ctrl Pts',(370.888588726393,-23.8767091153578,-3.2238428076631));
#40234=CARTESIAN_POINT('Ctrl Pts',(370.988425442236,-23.8828638238359,-3.21906328199818));
#40235=CARTESIAN_POINT('Ctrl Pts',(371.088224778161,-23.8890162279264,-3.21428554583794));
#40236=CARTESIAN_POINT('Ctrl Pts',(371.187845363413,-23.895168632017,-3.20486032107226));
#40237=CARTESIAN_POINT('Ctrl Pts',(371.286824087747,-23.9013210361075,-3.19082366642503));
#40238=CARTESIAN_POINT('Ctrl Pts',(371.38579218459,-23.9074727796055,-3.17678851891385));
#40239=CARTESIAN_POINT('Ctrl Pts',(371.484118127764,-23.9136245231034,-3.15814298692393));
#40240=CARTESIAN_POINT('Ctrl Pts',(371.581345671679,-23.9197762666014,-3.13497480068882));
#40241=CARTESIAN_POINT('Ctrl Pts',(371.678588739431,-23.9259289923175,-3.11180291530516));
#40242=CARTESIAN_POINT('Ctrl Pts',(371.774732637287,-23.9320817180336,-3.0841070419717));
#40243=CARTESIAN_POINT('Ctrl Pts',(371.869334006427,-23.9382344437497,-3.05202541357524));
#40244=CARTESIAN_POINT('Ctrl Pts',(371.964036410521,-23.9443937406219,-3.01990952176504));
#40245=CARTESIAN_POINT('Ctrl Pts',(372.057192584349,-23.950553037494,-2.98339866125467));
#40246=CARTESIAN_POINT('Ctrl Pts',(372.148377081947,-23.9567123343662,-2.94268005496815));
#40247=CARTESIAN_POINT('Ctrl Pts',(372.239612696557,-23.9628750840714,-2.90193862228546));
#40248=CARTESIAN_POINT('Ctrl Pts',(372.328874046053,-23.9690378337767,-2.85698494148562));
#40249=CARTESIAN_POINT('Ctrl Pts',(372.415760194849,-23.9752005834819,-2.80805229342594));
#40250=CARTESIAN_POINT('Ctrl Pts',(372.502790590456,-23.9813735644726,-2.7590384082704));
#40251=CARTESIAN_POINT('Ctrl Pts',(372.587437541014,-23.9875465454632,-2.70603259178947));
#40252=CARTESIAN_POINT('Ctrl Pts',(372.669328903666,-23.9937195264539,-2.64931161007049));
#40253=CARTESIAN_POINT('Ctrl Pts',(372.729910243236,-23.9982861552832,-2.60735073723878));
#40254=CARTESIAN_POINT('Ctrl Pts',(372.788984151554,-24.0028527841124,-2.56335756968843));
#40255=CARTESIAN_POINT('Ctrl Pts',(372.846412402545,-24.0074194129417,-2.51745766341643));
#40256=CARTESIAN_POINT('Ctrl Pts',(372.923980424882,-24.0135875333515,-2.45546091279952));
#40257=CARTESIAN_POINT('Ctrl Pts',(372.998817689026,-24.0197556537614,-2.38976601714212));
#40258=CARTESIAN_POINT('Ctrl Pts',(373.070550216883,-24.0259237741713,-2.32064266491488));
#40259=CARTESIAN_POINT('Ctrl Pts',(373.142185663187,-24.0320835467545,-2.25161286302785));
#40260=CARTESIAN_POINT('Ctrl Pts',(373.210724414209,-24.0382433193377,-2.17916412599214));
#40261=CARTESIAN_POINT('Ctrl Pts',(373.275824448159,-24.0444030919209,-2.10360716612856));
#40262=CARTESIAN_POINT('Ctrl Pts',(373.340855678201,-24.0505563542704,-2.02813006204793));
#40263=CARTESIAN_POINT('Ctrl Pts',(373.402455134041,-24.05670961662,-1.94955159369536));
#40264=CARTESIAN_POINT('Ctrl Pts',(373.460317367959,-24.0628628789695,-1.86821950292517));
#40265=CARTESIAN_POINT('Ctrl Pts',(373.51813765047,-24.069011680067,-1.78694637973033));
#40266=CARTESIAN_POINT('Ctrl Pts',(373.572225846467,-24.0751604811644,-1.70292395656945));
#40267=CARTESIAN_POINT('Ctrl Pts',(373.622317162364,-24.0813092822619,-1.61653252820172));
#40268=CARTESIAN_POINT('Ctrl Pts',(373.672389699844,-24.0874557782741,-1.53017348657084));
#40269=CARTESIAN_POINT('Ctrl Pts',(373.718468116397,-24.0936022742864,-1.44144758023228));
#40270=CARTESIAN_POINT('Ctrl Pts',(373.760331787587,-24.0997487702986,-1.35076275430425));
#40271=CARTESIAN_POINT('Ctrl Pts',(373.802191001744,-24.1058946119217,-1.26008758317269));
#40272=CARTESIAN_POINT('Ctrl Pts',(373.839836180324,-24.1120404535448,-1.16745430204368));
#40273=CARTESIAN_POINT('Ctrl Pts',(373.873093830474,-24.1181862951678,-1.07329312053637));
#40274=CARTESIAN_POINT('Ctrl Pts',(373.906356866755,-24.1243331321203,-0.979116689467482));
#40275=CARTESIAN_POINT('Ctrl Pts',(373.935230818367,-24.1304799690728,-0.88341227674254));
#40276=CARTESIAN_POINT('Ctrl Pts',(373.95959161304,-24.1366268060252,-0.786626651406925));
#40277=CARTESIAN_POINT('Ctrl Pts',(373.983978674557,-24.1427802707583,-0.689736667700208));
#40278=CARTESIAN_POINT('Ctrl Pts',(374.003842755604,-24.1489337354914,-0.591763566115745));
#40279=CARTESIAN_POINT('Ctrl Pts',(374.019110660718,-24.1550872002244,-0.493165627184254));
#40280=CARTESIAN_POINT('Ctrl Pts',(374.034387188387,-24.1612441401292,-0.394512005027022));
#40281=CARTESIAN_POINT('Ctrl Pts',(374.045062324706,-24.167401080034,-0.295233275307133));
#40282=CARTESIAN_POINT('Ctrl Pts',(374.051114866669,-24.1735580199387,-0.195792075397338));
#40283=CARTESIAN_POINT('Ctrl Pts',(374.057177561605,-24.1797252879408,-0.0961840656103151));
#40284=CARTESIAN_POINT('Ctrl Pts',(374.05860216773,-24.1858925559429,0.00358652363811422));
#40285=CARTESIAN_POINT('Ctrl Pts',(374.055419632907,-24.1920598239449,0.103057689769968));
#40286=CARTESIAN_POINT('Ctrl Pts',(374.053032843013,-24.1966850594144,0.177657588076881));
#40287=CARTESIAN_POINT('Ctrl Pts',(374.048055867032,-24.2013102948839,0.252089099841304));
#40288=CARTESIAN_POINT('Ctrl Pts',(374.040520715247,-24.2059355303535,0.32616065068505));
#40289=CARTESIAN_POINT('Ctrl Pts',(374.030446123188,-24.2121195279502,0.425195239394674));
#40290=CARTESIAN_POINT('Ctrl Pts',(374.015761345737,-24.218303525547,0.523933314390892));
#40291=CARTESIAN_POINT('Ctrl Pts',(373.996491531801,-24.2244875231438,0.621912525210338));
#40292=CARTESIAN_POINT('Ctrl Pts',(373.977247756659,-24.2306631644669,0.719759339293816));
#40293=CARTESIAN_POINT('Ctrl Pts',(373.953431343539,-24.2368388057901,0.816848906757136));
#40294=CARTESIAN_POINT('Ctrl Pts',(373.925119226506,-24.2430144471132,0.912723634742711));
#40295=CARTESIAN_POINT('Ctrl Pts',(373.89683708831,-24.2491835492381,1.00849684390231));
#40296=CARTESIAN_POINT('Ctrl Pts',(373.864068833032,-24.2553526513629,1.10305735860655));
#40297=CARTESIAN_POINT('Ctrl Pts',(373.826942315829,-24.2615217534878,1.19595835559579));
#40298=CARTESIAN_POINT('Ctrl Pts',(373.789843372054,-24.267686273893,1.28879035610646));
#40299=CARTESIAN_POINT('Ctrl Pts',(373.748392762907,-24.2738507942982,1.37996488928198));
#40300=CARTESIAN_POINT('Ctrl Pts',(373.702767705487,-24.2800153147034,1.46905173753502));
#40301=CARTESIAN_POINT('Ctrl Pts',(373.657160253058,-24.2861774564523,1.55810421052689));
#40302=CARTESIAN_POINT('Ctrl Pts',(373.607381750357,-24.2923395982011,1.64507021490609));
#40303=CARTESIAN_POINT('Ctrl Pts',(373.553656571141,-24.29850173995,1.72954170222534));
#40304=CARTESIAN_POINT('Ctrl Pts',(373.499937898263,-24.3046631354385,1.81400295970507));
#40305=CARTESIAN_POINT('Ctrl Pts',(373.442273731442,-24.310824530927,1.89596993588171));
#40306=CARTESIAN_POINT('Ctrl Pts',(373.380932693877,-24.3169859264155,1.97506212962201));
#40307=CARTESIAN_POINT('Ctrl Pts',(373.319582844735,-24.323148206982,2.05416568487398));
#40308=CARTESIAN_POINT('Ctrl Pts',(373.254555340926,-24.3293104875486,2.13039329566615));
#40309=CARTESIAN_POINT('Ctrl Pts',(373.186159521633,-24.3354727681152,2.20339699764539));
#40310=CARTESIAN_POINT('Ctrl Pts',(373.11769382624,-24.3416413443317,2.27647528333577));
#40311=CARTESIAN_POINT('Ctrl Pts',(373.045853240098,-24.3478099205483,2.34632276702677));
#40312=CARTESIAN_POINT('Ctrl Pts',(372.970984357664,-24.3539784967648,2.41262798858518));
#40313=CARTESIAN_POINT('Ctrl Pts',(372.896074773403,-24.360150426475,2.47896925640998));
#40314=CARTESIAN_POINT('Ctrl Pts',(372.818133950538,-24.3663223561853,2.54176415499762));
#40315=CARTESIAN_POINT('Ctrl Pts',(372.737540397211,-24.3724942858955,2.60074249216659));
#40316=CARTESIAN_POINT('Ctrl Pts',(372.656818848318,-24.3786760176259,2.65981449645049));
#40317=CARTESIAN_POINT('Ctrl Pts',(372.573436514892,-24.3848577493563,2.7150575937841));
#40318=CARTESIAN_POINT('Ctrl Pts',(372.487799670703,-24.3910394810866,2.76624573054627));
#40319=CARTESIAN_POINT('Ctrl Pts',(372.429473975143,-24.3952497460299,2.80110903861588));
#40320=CARTESIAN_POINT('Ctrl Pts',(372.370103013157,-24.3994600109731,2.83409231253986));
#40321=CARTESIAN_POINT('Ctrl Pts',(372.309820613641,-24.4036702759164,2.86513684952406));
#40322=CARTESIAN_POINT('Ctrl Pts',(367.611569202942,-23.5610139381901,-0.0029495098797409));
#40323=CARTESIAN_POINT('Ctrl Pts',(367.611380133205,-23.5494540715678,0.203635402400345));
#40324=CARTESIAN_POINT('Ctrl Pts',(367.631054003286,-23.5377943915509,0.409741458807204));
#40325=CARTESIAN_POINT('Ctrl Pts',(367.675072507174,-23.5239887098281,0.63711280560356));
#40326=CARTESIAN_POINT('Ctrl Pts',(367.680115170967,-23.5224883651973,0.66162623187756));
#40327=CARTESIAN_POINT('Ctrl Pts',(367.688962196206,-23.5199820626771,0.702231206944551));
#40328=CARTESIAN_POINT('Ctrl Pts',(367.692605866632,-23.5189811692298,0.718356913272546));
#40329=CARTESIAN_POINT('Ctrl Pts',(367.699991077294,-23.5170114587375,0.749910137940433));
#40330=CARTESIAN_POINT('Ctrl Pts',(367.703722856242,-23.516042977234,0.765339469820808));
#40331=CARTESIAN_POINT('Ctrl Pts',(367.710951352093,-23.5142156201992,0.794288523311939));
#40332=CARTESIAN_POINT('Ctrl Pts',(367.714422259156,-23.5133575956715,0.807814354310493));
#40333=CARTESIAN_POINT('Ctrl Pts',(367.722425264666,-23.5114215825672,0.838180291735856));
#40334=CARTESIAN_POINT('Ctrl Pts',(367.727006342797,-23.5103420288793,0.855006925232355));
#40335=CARTESIAN_POINT('Ctrl Pts',(367.739073921332,-23.507569007301,0.897953703212452));
#40336=CARTESIAN_POINT('Ctrl Pts',(367.746754487406,-23.5058692900971,0.924017445948775));
#40337=CARTESIAN_POINT('Ctrl Pts',(367.80321028937,-23.4938126983858,1.10703040359618));
#40338=CARTESIAN_POINT('Ctrl Pts',(367.863592127225,-23.4830748265927,1.26012048479625));
#40339=CARTESIAN_POINT('Ctrl Pts',(367.994739098085,-23.4630061701277,1.53015545340408));
#40340=CARTESIAN_POINT('Ctrl Pts',(368.06177485662,-23.4537776085564,1.6485103184398));
#40341=CARTESIAN_POINT('Ctrl Pts',(368.217519064277,-23.4345500723545,1.88697208611006));
#40342=CARTESIAN_POINT('Ctrl Pts',(368.307516678658,-23.4245847290635,2.00588765010823));
#40343=CARTESIAN_POINT('Ctrl Pts',(368.418109840132,-23.4138573885052,2.13270456257474));
#40344=CARTESIAN_POINT('Ctrl Pts',(368.43092318024,-23.4126353810892,2.1471339040296));
#40345=CARTESIAN_POINT('Ctrl Pts',(368.450499814581,-23.4108007664504,2.16878467438934));
#40346=CARTESIAN_POINT('Ctrl Pts',(368.457167767995,-23.4101814558805,2.17609119377525));
#40347=CARTESIAN_POINT('Ctrl Pts',(368.468662404547,-23.4091235420553,2.1885707465838));
#40348=CARTESIAN_POINT('Ctrl Pts',(368.473472583463,-23.4086837190848,2.19375869917104));
#40349=CARTESIAN_POINT('Ctrl Pts',(368.484454792367,-23.4076861133738,2.20552545384239));
#40350=CARTESIAN_POINT('Ctrl Pts',(368.490637378892,-23.4071291485305,2.21209420486772));
#40351=CARTESIAN_POINT('Ctrl Pts',(368.507573736009,-23.4056157594886,2.22993769692907));
#40352=CARTESIAN_POINT('Ctrl Pts',(368.51838197718,-23.4046634020596,2.24116071704021));
#40353=CARTESIAN_POINT('Ctrl Pts',(368.573339388843,-23.3998854571837,2.29740504253139));
#40354=CARTESIAN_POINT('Ctrl Pts',(368.618724775936,-23.3961476035813,2.34120525214784));
#40355=CARTESIAN_POINT('Ctrl Pts',(368.818820475119,-23.3803814053289,2.52327792289411));
#40356=CARTESIAN_POINT('Ctrl Pts',(368.985407988201,-23.3689802148214,2.64777410432298));
#40357=CARTESIAN_POINT('Ctrl Pts',(369.269128081034,-23.3503442157055,2.81988629963155));
#40358=CARTESIAN_POINT('Ctrl Pts',(369.379072471157,-23.3432929817804,2.8781652479805));
#40359=CARTESIAN_POINT('Ctrl Pts',(369.558878684482,-23.3317650861883,2.9605349853177));
#40360=CARTESIAN_POINT('Ctrl Pts',(369.626677412875,-23.3274203636305,2.98883184898583));
#40361=CARTESIAN_POINT('Ctrl Pts',(369.716631397185,-23.321629636725,3.02281501693162));
#40362=CARTESIAN_POINT('Ctrl Pts',(369.737966668181,-23.3202543651,3.03061836581827));
#40363=CARTESIAN_POINT('Ctrl Pts',(369.773688825696,-23.3179478787091,3.04325712489756));
#40364=CARTESIAN_POINT('Ctrl Pts',(369.788030784401,-23.3170208351351,3.04821771196498));
#40365=CARTESIAN_POINT('Ctrl Pts',(369.815804401445,-23.3152233857138,3.05760492940643));
#40366=CARTESIAN_POINT('Ctrl Pts',(369.829231235774,-23.314353441857,3.06204481304255));
#40367=CARTESIAN_POINT('Ctrl Pts',(369.860274585425,-23.3123396275133,3.07208381377094));
#40368=CARTESIAN_POINT('Ctrl Pts',(369.877910788305,-23.3111937212452,3.07761998137172));
#40369=CARTESIAN_POINT('Ctrl Pts',(369.935081857265,-23.3074726460979,3.09502764046936));
#40370=CARTESIAN_POINT('Ctrl Pts',(369.97479616449,-23.3048778588671,3.10629098515518));
#40371=CARTESIAN_POINT('Ctrl Pts',(370.239521699351,-23.2875090406947,3.17590430315866));
#40372=CARTESIAN_POINT('Ctrl Pts',(370.470026884013,-23.2719661716621,3.21051502441555));
#40373=CARTESIAN_POINT('Ctrl Pts',(370.843961392244,-23.2466524399666,3.22585701486366));
#40374=CARTESIAN_POINT('Ctrl Pts',(370.985954778114,-23.2370366717919,3.22230611145));
#40375=CARTESIAN_POINT('Ctrl Pts',(371.170232003222,-23.2248548909977,3.20548614410348));
#40376=CARTESIAN_POINT('Ctrl Pts',(371.213125284679,-23.2220412807141,3.20070070850935));
#40377=CARTESIAN_POINT('Ctrl Pts',(371.28479040941,-23.2173906603054,3.19124435789764));
#40378=CARTESIAN_POINT('Ctrl Pts',(371.313617538054,-23.215533687009,3.18704220651699));
#40379=CARTESIAN_POINT('Ctrl Pts',(371.353706562784,-23.212974075198,3.1806421330473));
#40380=CARTESIAN_POINT('Ctrl Pts',(371.365018730542,-23.212254356973,3.17877422889665));
#40381=CARTESIAN_POINT('Ctrl Pts',(371.384249077559,-23.2110354670183,3.17549333124718));
#40382=CARTESIAN_POINT('Ctrl Pts',(371.392172320108,-23.2105345989786,3.17411100112082));
#40383=CARTESIAN_POINT('Ctrl Pts',(371.407443141196,-23.2095719308206,3.17138782671641));
#40384=CARTESIAN_POINT('Ctrl Pts',(371.414791302006,-23.2091098916934,3.17005109124221));
#40385=CARTESIAN_POINT('Ctrl Pts',(371.43461298449,-23.2078665838393,3.16637401143913));
#40386=CARTESIAN_POINT('Ctrl Pts',(371.447077589814,-23.2070880039969,3.16398548393497));
#40387=CARTESIAN_POINT('Ctrl Pts',(371.493643353979,-23.2041904546128,3.15477682561962));
#40388=CARTESIAN_POINT('Ctrl Pts',(371.527648852348,-23.2020967710002,3.14747824194551));
#40389=CARTESIAN_POINT('Ctrl Pts',(371.821610133719,-23.1841397458632,3.07938980133958));
#40390=CARTESIAN_POINT('Ctrl Pts',(372.072938453568,-23.1696816819013,2.98712763432748));
#40391=CARTESIAN_POINT('Ctrl Pts',(372.309820652881,-23.1546465340816,2.86513682931627));
#40392=CARTESIAN_POINT('',(367.61156800787,-23.3142265506821,0.000998384406030673));
#40393=CARTESIAN_POINT('Ctrl Pts',(372.309820613641,-22.9071794904733,2.86513684952399));
#40394=CARTESIAN_POINT('Ctrl Pts',(372.220989734859,-22.9133311557454,2.91088342769398));
#40395=CARTESIAN_POINT('Ctrl Pts',(372.129996352699,-22.9194828210175,2.95251196963913));
#40396=CARTESIAN_POINT('Ctrl Pts',(372.037260366095,-22.9256344862896,2.98982388665753));
#40397=CARTESIAN_POINT('Ctrl Pts',(371.944529271348,-22.9317858270591,3.02713383545884));
#40398=CARTESIAN_POINT('Ctrl Pts',(371.85005615787,-22.9379371678286,3.06012745032107));
#40399=CARTESIAN_POINT('Ctrl Pts',(371.75428056199,-22.9440885085982,3.08865442822273));
#40400=CARTESIAN_POINT('Ctrl Pts',(371.658484431469,-22.9502411682378,3.11718752241366));
#40401=CARTESIAN_POINT('Ctrl Pts',(371.561385679857,-22.9563938278775,3.14125195325109));
#40402=CARTESIAN_POINT('Ctrl Pts',(371.46343766846,-22.9625464875172,3.16074766796994));
#40403=CARTESIAN_POINT('Ctrl Pts',(371.365382213966,-22.9687058962556,3.18026476831898));
#40404=CARTESIAN_POINT('Ctrl Pts',(371.266476066421,-22.9748653049941,3.19520306302124));
#40405=CARTESIAN_POINT('Ctrl Pts',(371.167181258783,-22.9810247137325,3.20551392380996));
#40406=CARTESIAN_POINT('Ctrl Pts',(371.067825889607,-22.9871878791957,3.21583107336247));
#40407=CARTESIAN_POINT('Ctrl Pts',(370.96808182146,-22.993351044659,3.22151514481994));
#40408=CARTESIAN_POINT('Ctrl Pts',(370.868412603373,-22.9995142101222,3.2225696440127));
#40409=CARTESIAN_POINT('Ctrl Pts',(370.76858417089,-23.0056872207983,3.22362582769196));
#40410=CARTESIAN_POINT('Ctrl Pts',(370.668831260545,-23.0118602314744,3.22003768913998));
#40411=CARTESIAN_POINT('Ctrl Pts',(370.569613789268,-23.0180332421505,3.21186072565816));
#40412=CARTESIAN_POINT('Ctrl Pts',(370.51691446294,-23.0213120346843,3.20751753426901));
#40413=CARTESIAN_POINT('Ctrl Pts',(370.46436605609,-23.0245908272182,3.2018806167265));
#40414=CARTESIAN_POINT('Ctrl Pts',(370.412036183166,-23.027869619752,3.19496412399772));
#40415=CARTESIAN_POINT('Ctrl Pts',(370.313505351796,-23.0340431901468,3.18194120342392));
#40416=CARTESIAN_POINT('Ctrl Pts',(370.215405000158,-23.0402167605415,3.16433326267595));
#40417=CARTESIAN_POINT('Ctrl Pts',(370.11819531248,-23.0463903309363,3.14217855462378));
#40418=CARTESIAN_POINT('Ctrl Pts',(370.021116839483,-23.0525555681794,3.12005375123481));
#40419=CARTESIAN_POINT('Ctrl Pts',(369.924927060452,-23.0587208054224,3.09339447487113));
#40420=CARTESIAN_POINT('Ctrl Pts',(369.830079930798,-23.0648860426655,3.06229060633737));
#40421=CARTESIAN_POINT('Ctrl Pts',(369.735332839819,-23.0710447772114,3.0312195441709));
#40422=CARTESIAN_POINT('Ctrl Pts',(369.641925993033,-23.0772035117573,2.99571334445778));
#40423=CARTESIAN_POINT('Ctrl Pts',(369.550301111884,-23.0833622463032,2.95591247679277));
#40424=CARTESIAN_POINT('Ctrl Pts',(369.458742764106,-23.0895165086865,2.91614051051173));
#40425=CARTESIAN_POINT('Ctrl Pts',(369.368964206311,-23.0956707710697,2.87208024906491));
#40426=CARTESIAN_POINT('Ctrl Pts',(369.281389129887,-23.101825033453,2.82392102275079));
#40427=CARTESIAN_POINT('Ctrl Pts',(369.193846973397,-23.1079769824166,2.77577989974461));
#40428=CARTESIAN_POINT('Ctrl Pts',(369.108507032422,-23.1141289313801,2.72354308251434));
#40429=CARTESIAN_POINT('Ctrl Pts',(369.025769440113,-23.1202808803436,2.66744638182932));
#40430=CARTESIAN_POINT('Ctrl Pts',(368.943040845521,-23.1264321602824,2.61135578166257));
#40431=CARTESIAN_POINT('Ctrl Pts',(368.862914396256,-23.1325834402213,2.55140637626594));
#40432=CARTESIAN_POINT('Ctrl Pts',(368.785761359651,-23.1387347201601,2.48787737944211));
#40433=CARTESIAN_POINT('Ctrl Pts',(368.708596101796,-23.1448869744783,2.42433831945346));
#40434=CARTESIAN_POINT('Ctrl Pts',(368.634405527312,-23.1510392287965,2.35721881777673));
#40435=CARTESIAN_POINT('Ctrl Pts',(368.56352714042,-23.1571914831147,2.2868377951104));
#40436=CARTESIAN_POINT('Ctrl Pts',(368.492573153698,-23.1633502995092,2.21638170310869));
#40437=CARTESIAN_POINT('Ctrl Pts',(368.424938717774,-23.1695091159038,2.14265744997855));
#40438=CARTESIAN_POINT('Ctrl Pts',(368.360923722094,-23.1756679322983,2.06602009539862));
#40439=CARTESIAN_POINT('Ctrl Pts',(368.296872897655,-23.1818301957406,1.98933984741162));
#40440=CARTESIAN_POINT('Ctrl Pts',(368.236445810301,-23.1879924591828,1.90974359673948));
#40441=CARTESIAN_POINT('Ctrl Pts',(368.179900095961,-23.1941547226251,1.82761700922941));
#40442=CARTESIAN_POINT('Ctrl Pts',(368.123260537344,-23.2003272130696,1.74535412297017));
#40443=CARTESIAN_POINT('Ctrl Pts',(368.070515447642,-23.2064997035142,1.66055288074536));
#40444=CARTESIAN_POINT('Ctrl Pts',(368.021877492127,-23.2126721939587,1.57362536131473));
#40445=CARTESIAN_POINT('Ctrl Pts',(367.985857525235,-23.2172433750271,1.5092491691267));
#40446=CARTESIAN_POINT('Ctrl Pts',(367.952089158342,-23.2218145560954,1.44370736284903));
#40447=CARTESIAN_POINT('Ctrl Pts',(367.920641598016,-23.2263857371637,1.3771740058318));
#40448=CARTESIAN_POINT('Ctrl Pts',(367.874660085628,-23.2330695567271,1.27989128029524));
#40449=CARTESIAN_POINT('Ctrl Pts',(367.833500582128,-23.2397533762904,1.18018949652149));
#40450=CARTESIAN_POINT('Ctrl Pts',(367.797403084392,-23.2464371958538,1.07854821373587));
#40451=CARTESIAN_POINT('Ctrl Pts',(367.761433795259,-23.253097276288,0.97726793344535));
#40452=CARTESIAN_POINT('Ctrl Pts',(367.730490777906,-23.2597573567222,0.874062186934083));
#40453=CARTESIAN_POINT('Ctrl Pts',(367.704765965764,-23.2664174371564,0.769430013840498));
#40454=CARTESIAN_POINT('Ctrl Pts',(367.679099449172,-23.2730624250395,0.665034949959054));
#40455=CARTESIAN_POINT('Ctrl Pts',(367.658627659573,-23.2797074129225,0.55922020650824));
#40456=CARTESIAN_POINT('Ctrl Pts',(367.643493542549,-23.2863524008056,0.452501691604395));
#40457=CARTESIAN_POINT('Ctrl Pts',(367.628409460502,-23.2929754196625,0.34613599929171));
#40458=CARTESIAN_POINT('Ctrl Pts',(367.618627926109,-23.2995984385194,0.238872805855995));
#40459=CARTESIAN_POINT('Ctrl Pts',(367.61424114798,-23.3062214573763,0.131238617972967));
#40460=CARTESIAN_POINT('Ctrl Pts',(367.612473748099,-23.3088898218116,0.0878736140116947));
#40461=CARTESIAN_POINT('Ctrl Pts',(367.611581468412,-23.3115581862468,0.0444485422163019));
#40462=CARTESIAN_POINT('Ctrl Pts',(367.61156800787,-23.3142265506821,0.000998384406030673));
#40463=CARTESIAN_POINT('Ctrl Pts',(372.309820613613,-24.1556143901908,2.86513684953878));
#40464=CARTESIAN_POINT('Ctrl Pts',(372.442467835282,-24.1456807417415,2.79682550805366));
#40465=CARTESIAN_POINT('Ctrl Pts',(372.570225783518,-24.1359684629225,2.71937755021739));
#40466=CARTESIAN_POINT('Ctrl Pts',(372.71400207142,-24.1248961996909,2.61794165651371));
#40467=CARTESIAN_POINT('Ctrl Pts',(372.735639693992,-24.1232254189926,2.60226951022979));
#40468=CARTESIAN_POINT('Ctrl Pts',(372.770977497378,-24.1204887407584,2.57599822448064));
#40469=CARTESIAN_POINT('Ctrl Pts',(372.784791237552,-24.1194168924612,2.5655547208309));
#40470=CARTESIAN_POINT('Ctrl Pts',(372.809601410106,-24.117487797431,2.54648145323391));
#40471=CARTESIAN_POINT('Ctrl Pts',(372.820627069685,-24.1166290541856,2.53789058631565));
#40472=CARTESIAN_POINT('Ctrl Pts',(372.844161623111,-24.1147927314224,2.51930583980846));
#40473=CARTESIAN_POINT('Ctrl Pts',(372.856652674699,-24.1138160601309,2.50928989519937));
#40474=CARTESIAN_POINT('Ctrl Pts',(372.890624974238,-24.1111537696733,2.48163076886942));
#40475=CARTESIAN_POINT('Ctrl Pts',(372.911953723628,-24.1094756626206,2.46380184110973));
#40476=CARTESIAN_POINT('Ctrl Pts',(373.032637829351,-24.0999367694206,2.36023897619377));
#40477=CARTESIAN_POINT('Ctrl Pts',(373.126919786398,-24.0923196815813,2.26877080163027));
#40478=CARTESIAN_POINT('Ctrl Pts',(373.312543629323,-24.0766404502101,2.06526205475736));
#40479=CARTESIAN_POINT('Ctrl Pts',(373.402459820053,-24.0686272142593,1.95232133653624));
#40480=CARTESIAN_POINT('Ctrl Pts',(373.579077853419,-24.051241220845,1.6970658514811));
#40481=CARTESIAN_POINT('Ctrl Pts',(373.66292007332,-24.0418725320143,1.5532984449698));
#40482=CARTESIAN_POINT('Ctrl Pts',(373.747049322534,-24.0302942232591,1.37943514783926));
#40483=CARTESIAN_POINT('Ctrl Pts',(373.758498583684,-24.0286610656654,1.35499553021274));
#40484=CARTESIAN_POINT('Ctrl Pts',(373.773906126548,-24.0263778251464,1.32100158323732));
#40485=CARTESIAN_POINT('Ctrl Pts',(373.778127734967,-24.0257429094197,1.31156691517234));
#40486=CARTESIAN_POINT('Ctrl Pts',(373.785298629911,-24.0246479901468,1.29533198794876));
#40487=CARTESIAN_POINT('Ctrl Pts',(373.788270006115,-24.0241893149638,1.28854149300396));
#40488=CARTESIAN_POINT('Ctrl Pts',(373.794438023941,-24.0232265726319,1.2743122425177));
#40489=CARTESIAN_POINT('Ctrl Pts',(373.797630078186,-24.0227222222388,1.26687164650172));
#40490=CARTESIAN_POINT('Ctrl Pts',(373.805382162072,-24.0214823997838,1.24861214142649));
#40491=CARTESIAN_POINT('Ctrl Pts',(373.809911147423,-24.0207450925936,1.23778024888221));
#40492=CARTESIAN_POINT('Ctrl Pts',(373.82616188849,-24.0180523914571,1.1983089949849));
#40493=CARTESIAN_POINT('Ctrl Pts',(373.837529756581,-24.0160775364631,1.16952694618834));
#40494=CARTESIAN_POINT('Ctrl Pts',(373.865048833878,-24.0110672133875,1.09680387408566));
#40495=CARTESIAN_POINT('Ctrl Pts',(373.880659988586,-24.0080078539166,1.05266716711442));
#40496=CARTESIAN_POINT('Ctrl Pts',(374.000151315765,-23.9827952290267,0.689883826976194));
#40497=CARTESIAN_POINT('Ctrl Pts',(374.054718573656,-23.9595432569405,0.35712651679104));
#40498=CARTESIAN_POINT('Ctrl Pts',(374.05743309452,-23.9337913500727,-0.0428874854631862));
#40499=CARTESIAN_POINT('Ctrl Pts',(374.055920631198,-23.9296795236787,-0.107646196950578));
#40500=CARTESIAN_POINT('Ctrl Pts',(374.051230006456,-23.9241917417428,-0.195245715194762));
#40501=CARTESIAN_POINT('Ctrl Pts',(374.049757396586,-23.9227631724972,-0.218158836000152));
#40502=CARTESIAN_POINT('Ctrl Pts',(374.046922111944,-23.9204173294058,-0.255958618483742));
#40503=CARTESIAN_POINT('Ctrl Pts',(374.045700525348,-23.9194956710875,-0.270854726207899));
#40504=CARTESIAN_POINT('Ctrl Pts',(374.043112353225,-23.9177019446455,-0.299930540435097));
#40505=CARTESIAN_POINT('Ctrl Pts',(374.041755293547,-23.9168295995274,-0.314110727311317));
#40506=CARTESIAN_POINT('Ctrl Pts',(374.038324221398,-23.9147738206573,-0.347618452159981));
#40507=CARTESIAN_POINT('Ctrl Pts',(374.036169263463,-23.9135929545013,-0.366937280676859));
#40508=CARTESIAN_POINT('Ctrl Pts',(374.028374357827,-23.9096597447962,-0.43150916286562));
#40509=CARTESIAN_POINT('Ctrl Pts',(374.021948598906,-23.9069320677534,-0.476663039213774));
#40510=CARTESIAN_POINT('Ctrl Pts',(374.004265634068,-23.9004635370716,-0.584464019033404));
#40511=CARTESIAN_POINT('Ctrl Pts',(373.992106726697,-23.896750150491,-0.646944564977889));
#40512=CARTESIAN_POINT('Ctrl Pts',(373.937211133331,-23.8823588087427,-0.890348639634534));
#40513=CARTESIAN_POINT('Ctrl Pts',(373.880707345235,-23.8720535919357,-1.06779326105677));
#40514=CARTESIAN_POINT('Ctrl Pts',(373.746134394167,-23.8524512054304,-1.3908096630725));
#40515=CARTESIAN_POINT('Ctrl Pts',(373.671586221931,-23.8431975132892,-1.53717998803959));
#40516=CARTESIAN_POINT('Ctrl Pts',(373.572202271709,-23.8317503433501,-1.70024511841311));
#40517=CARTESIAN_POINT('Ctrl Pts',(373.557882142189,-23.8301187725732,-1.7230908297668));
#40518=CARTESIAN_POINT('Ctrl Pts',(373.537682871047,-23.8278376384181,-1.75443489866671));
#40519=CARTESIAN_POINT('Ctrl Pts',(373.532046530819,-23.8272032277156,-1.76308939324761));
#40520=CARTESIAN_POINT('Ctrl Pts',(373.522297322871,-23.826109207318,-1.77790291682286));
#40521=CARTESIAN_POINT('Ctrl Pts',(373.51820460441,-23.8256509253845,-1.78407519883241));
#40522=CARTESIAN_POINT('Ctrl Pts',(373.509591685067,-23.8246884292966,-1.79696774644401));
#40523=CARTESIAN_POINT('Ctrl Pts',(373.505067393653,-23.8241839290119,-1.80368512895664));
#40524=CARTESIAN_POINT('Ctrl Pts',(373.493920415644,-23.8229437308169,-1.82010156471624));
#40525=CARTESIAN_POINT('Ctrl Pts',(373.487269975296,-23.8222061971507,-1.82978155086282));
#40526=CARTESIAN_POINT('Ctrl Pts',(373.462902857343,-23.8195131249983,-1.86483678270179));
#40527=CARTESIAN_POINT('Ctrl Pts',(373.444874432871,-23.8175381322536,-1.88999193913474));
#40528=CARTESIAN_POINT('Ctrl Pts',(373.398672438488,-23.8125277723452,-1.95253541258379));
#40529=CARTESIAN_POINT('Ctrl Pts',(373.370041794885,-23.8094685289126,-1.98957599084985));
#40530=CARTESIAN_POINT('Ctrl Pts',(373.130001478492,-23.7842646622101,-2.28652524659589));
#40531=CARTESIAN_POINT('Ctrl Pts',(372.880034100536,-23.7610223940301,-2.51266487245713));
#40532=CARTESIAN_POINT('Ctrl Pts',(372.545373553593,-23.7352702109003,-2.73177844891641));
#40533=CARTESIAN_POINT('Ctrl Pts',(372.49004191261,-23.7311514395181,-2.76566518484465));
#40534=CARTESIAN_POINT('Ctrl Pts',(372.413768032092,-23.7256552974136,-2.80926733451301));
#40535=CARTESIAN_POINT('Ctrl Pts',(372.393692448891,-23.7242251688583,-2.82046037706913));
#40536=CARTESIAN_POINT('Ctrl Pts',(372.360356214305,-23.721876973729,-2.83858208254149));
#40537=CARTESIAN_POINT('Ctrl Pts',(372.347164260939,-23.7209545151969,-2.84563474070548));
#40538=CARTESIAN_POINT('Ctrl Pts',(372.321306187646,-23.7191593699215,-2.85922829586009));
#40539=CARTESIAN_POINT('Ctrl Pts',(372.30864484895,-23.7182864050242,-2.8657774991294));
#40540=CARTESIAN_POINT('Ctrl Pts',(372.278607366622,-23.7162293667329,-2.88106292777026));
#40541=CARTESIAN_POINT('Ctrl Pts',(372.261194650089,-23.7150478605854,-2.88972635806348));
#40542=CARTESIAN_POINT('Ctrl Pts',(372.202684712001,-23.7111133253847,-2.91817926264425));
#40543=CARTESIAN_POINT('Ctrl Pts',(372.161244859663,-23.7083849498742,-2.93725434720373));
#40544=CARTESIAN_POINT('Ctrl Pts',(372.061044129988,-23.7019149054048,-2.98082391284935));
#40545=CARTESIAN_POINT('Ctrl Pts',(372.001934482439,-23.6982006830013,-3.00447011650423));
#40546=CARTESIAN_POINT('Ctrl Pts',(371.767534707402,-23.6838030078993,-3.09027577786004));
#40547=CARTESIAN_POINT('Ctrl Pts',(371.587703263998,-23.673492175786,-3.13896678149078));
#40548=CARTESIAN_POINT('Ctrl Pts',(371.243614258785,-23.6539039780741,-3.20083920080511));
#40549=CARTESIAN_POINT('Ctrl Pts',(371.080605450578,-23.64467062926,-3.21748732348361));
#40550=CARTESIAN_POINT('Ctrl Pts',(370.89010909125,-23.633247361395,-3.22237982570473));
#40551=CARTESIAN_POINT('Ctrl Pts',(370.863151363411,-23.6316159203847,-3.22273376565086));
#40552=CARTESIAN_POINT('Ctrl Pts',(370.825860245988,-23.6293346263441,-3.22275546777749));
#40553=CARTESIAN_POINT('Ctrl Pts',(370.815527305335,-23.6286999045171,-3.2227117843164));
#40554=CARTESIAN_POINT('Ctrl Pts',(370.79778355667,-23.6276052191003,-3.22255143332531));
#40555=CARTESIAN_POINT('Ctrl Pts',(370.790372537335,-23.6271465824796,-3.22245889063775));
#40556=CARTESIAN_POINT('Ctrl Pts',(370.774861384072,-23.6261835678811,-3.22221168256888));
#40557=CARTESIAN_POINT('Ctrl Pts',(370.766761461282,-23.6256789045941,-3.22205203679152));
#40558=CARTESIAN_POINT('Ctrl Pts',(370.746913032961,-23.6244380336093,-3.2215859577276));
#40559=CARTESIAN_POINT('Ctrl Pts',(370.735165501581,-23.6236999866931,-3.22124579731949));
#40560=CARTESIAN_POINT('Ctrl Pts',(370.692438942622,-23.6210031222292,-3.21977466916652));
#40561=CARTESIAN_POINT('Ctrl Pts',(370.661475889779,-23.619024782242,-3.21826102669073));
#40562=CARTESIAN_POINT('Ctrl Pts',(370.583717254512,-23.614004141467,-3.21333442906917));
#40563=CARTESIAN_POINT('Ctrl Pts',(370.536966327229,-23.6109378491655,-3.20934579561924));
#40564=CARTESIAN_POINT('Ctrl Pts',(370.154452293196,-23.5855423839119,-3.16828165909862));
#40565=CARTESIAN_POINT('Ctrl Pts',(369.826308807702,-23.5621059305944,-3.07964705438672));
#40566=CARTESIAN_POINT('Ctrl Pts',(369.460755538353,-23.5363545674471,-2.91605196249271));
#40567=CARTESIAN_POINT('Ctrl Pts',(369.40439804049,-23.5323848797017,-2.88883413915596));
#40568=CARTESIAN_POINT('Ctrl Pts',(369.3287539288,-23.5270541988766,-2.84954530041571));
#40569=CARTESIAN_POINT('Ctrl Pts',(369.308752740665,-23.5256444144833,-2.83888750730262));
#40570=CARTESIAN_POINT('Ctrl Pts',(369.27710628605,-23.5234129267838,-2.82159339091499));
#40571=CARTESIAN_POINT('Ctrl Pts',(369.265387407107,-23.5225863955767,-2.81509402906771));
#40572=CARTESIAN_POINT('Ctrl Pts',(369.241649314295,-23.5209116082893,-2.80173446214553));
#40573=CARTESIAN_POINT('Ctrl Pts',(369.229633061403,-23.5200635433797,-2.79486954965636));
#40574=CARTESIAN_POINT('Ctrl Pts',(369.202033903474,-23.5181148306078,-2.77886541645274));
#40575=CARTESIAN_POINT('Ctrl Pts',(369.186482786133,-23.5170161644153,-2.76967209388485));
#40576=CARTESIAN_POINT('Ctrl Pts',(369.153920839204,-23.5147138866712,-2.75005118011403));
#40577=CARTESIAN_POINT('Ctrl Pts',(369.136927845903,-23.5135113461233,-2.73959537304416));
#40578=CARTESIAN_POINT('Ctrl Pts',(369.091800528143,-23.5103140547179,-2.71124740986724));
#40579=CARTESIAN_POINT('Ctrl Pts',(369.063844496158,-23.5083294094359,-2.6930750744508));
#40580=CARTESIAN_POINT('Ctrl Pts',(368.890462271229,-23.495983641918,-2.57650399326839));
#40581=CARTESIAN_POINT('Ctrl Pts',(368.75299306793,-23.486050932814,-2.46678813542396));
#40582=CARTESIAN_POINT('Ctrl Pts',(368.467561371951,-23.4640905314945,-2.19804938935714));
#40583=CARTESIAN_POINT('Ctrl Pts',(368.325351303357,-23.4521715428843,-2.03421299416523));
#40584=CARTESIAN_POINT('Ctrl Pts',(368.177802589493,-23.4369987957076,-1.82499733314741));
#40585=CARTESIAN_POINT('Ctrl Pts',(368.155559316862,-23.4346197714901,-1.79218888359884));
#40586=CARTESIAN_POINT('Ctrl Pts',(368.126635994491,-23.4313884781567,-1.74778574327806));
#40587=CARTESIAN_POINT('Ctrl Pts',(368.119413912504,-23.4305695885449,-1.73654617871157));
#40588=CARTESIAN_POINT('Ctrl Pts',(368.108191409367,-23.4292774861578,-1.71883972315113));
#40589=CARTESIAN_POINT('Ctrl Pts',(368.104143541894,-23.4288073452721,-1.71240287570564));
#40590=CARTESIAN_POINT('Ctrl Pts',(368.09590252233,-23.4278416395556,-1.69919465407191));
#40591=CARTESIAN_POINT('Ctrl Pts',(368.091711683448,-23.4273459212298,-1.69242204809366));
#40592=CARTESIAN_POINT('Ctrl Pts',(368.081791256619,-23.4261614934845,-1.6762565298239));
#40593=CARTESIAN_POINT('Ctrl Pts',(368.076084613433,-23.4254713180545,-1.66684972490288));
#40594=CARTESIAN_POINT('Ctrl Pts',(368.056927707008,-23.4231247347265,-1.63490380828036));
#40595=CARTESIAN_POINT('Ctrl Pts',(368.04370506277,-23.421454706823,-1.61223033024187));
#40596=CARTESIAN_POINT('Ctrl Pts',(368.012234155429,-23.417359647458,-1.55671847845611));
#40597=CARTESIAN_POINT('Ctrl Pts',(367.994280613696,-23.414919985841,-1.52371816552844));
#40598=CARTESIAN_POINT('Ctrl Pts',(367.925134837549,-23.4051203823547,-1.39115239105593));
#40599=CARTESIAN_POINT('Ctrl Pts',(367.878571310424,-23.397593111491,-1.28926725537856));
#40600=CARTESIAN_POINT('Ctrl Pts',(367.749651634282,-23.3739040249761,-0.963271993030066));
#40601=CARTESIAN_POINT('Ctrl Pts',(367.686800329966,-23.3577465822787,-0.732273755138728));
#40602=CARTESIAN_POINT('Ctrl Pts',(367.640064499905,-23.3382158920887,-0.432493266754107));
#40603=CARTESIAN_POINT('Ctrl Pts',(367.632024075438,-23.3341073263439,-0.368266801160347));
#40604=CARTESIAN_POINT('Ctrl Pts',(367.623760271491,-23.3286242171115,-0.281004642953406));
#40605=CARTESIAN_POINT('Ctrl Pts',(367.621841707968,-23.3271971591267,-0.258148513109521));
#40606=CARTESIAN_POINT('Ctrl Pts',(367.619076172366,-23.3248528204618,-0.220367577383022));
#40607=CARTESIAN_POINT('Ctrl Pts',(367.618088768468,-23.3239311734424,-0.205454184320089));
#40608=CARTESIAN_POINT('Ctrl Pts',(367.616417549739,-23.3221941933596,-0.1772361669251));
#40609=CARTESIAN_POINT('Ctrl Pts',(367.615712417976,-23.3213782110927,-0.163933165152991));
#40610=CARTESIAN_POINT('Ctrl Pts',(367.614440904176,-23.319717079721,-0.136757959450048));
#40611=CARTESIAN_POINT('Ctrl Pts',(367.61388163701,-23.3188721689367,-0.122885691443705));
#40612=CARTESIAN_POINT('Ctrl Pts',(367.61281983492,-23.3169680356372,-0.0915127688218745));
#40613=CARTESIAN_POINT('Ctrl Pts',(367.612370226851,-23.3159104699517,-0.0740106754883971));
#40614=CARTESIAN_POINT('Ctrl Pts',(367.611728139963,-23.313707335571,-0.0373953607415123));
#40615=CARTESIAN_POINT('Ctrl Pts',(367.611563030695,-23.3125626383311,-0.0182823692621725));
#40616=CARTESIAN_POINT('Ctrl Pts',(367.611567960415,-23.3114228970708,0.00083120270546652));
#40617=CARTESIAN_POINT('Origin',(370.834317853224,0.,0.));
#40618=CARTESIAN_POINT('',(366.90131859535,-0.404163522081287,0.00241610556833531));
#40619=CARTESIAN_POINT('',(372.583015783242,-7.58132545439985E-5,3.52286027959531));
#40620=CARTESIAN_POINT('Ctrl Pts',(366.901318595351,-0.404163522034968,
0.00241610647972434));
#40621=CARTESIAN_POINT('Ctrl Pts',(366.90139983104,-0.397442828341541,0.134653616887458));
#40622=CARTESIAN_POINT('Ctrl Pts',(366.908149810272,-0.390722134648114,
0.266692292879821));
#40623=CARTESIAN_POINT('Ctrl Pts',(366.921511751991,-0.384001440954687,
0.39804197537121));
#40624=CARTESIAN_POINT('Ctrl Pts',(366.933209419728,-0.378117831862511,
0.513031620996121));
#40625=CARTESIAN_POINT('Ctrl Pts',(366.94999952768,-0.372234222770335,0.627693708269049));
#40626=CARTESIAN_POINT('Ctrl Pts',(366.971856973827,-0.36635061367816,0.741542281418));
#40627=CARTESIAN_POINT('Ctrl Pts',(366.993686185506,-0.360474604768403,
0.855243790084839));
#40628=CARTESIAN_POINT('Ctrl Pts',(367.020569640122,-0.354598595858646,
0.968133473973612));
#40629=CARTESIAN_POINT('Ctrl Pts',(367.052430428212,-0.348722586948889,
1.07972982941867));
#40630=CARTESIAN_POINT('Ctrl Pts',(367.084258493025,-0.342852613114828,
1.19121156753371));
#40631=CARTESIAN_POINT('Ctrl Pts',(367.121053609894,-0.336982639280766,
1.30140222607469));
#40632=CARTESIAN_POINT('Ctrl Pts',(367.162687831609,-0.331112665446705,
1.40983048072249));
#40633=CARTESIAN_POINT('Ctrl Pts',(367.205725225613,-0.325044859534052,
1.5219130254236));
#40634=CARTESIAN_POINT('Ctrl Pts',(367.253933585446,-0.318977053621399,
1.63211183191873));
#40635=CARTESIAN_POINT('Ctrl Pts',(367.307115391484,-0.312909247708746,
1.73992292757268));
#40636=CARTESIAN_POINT('Ctrl Pts',(367.358503086155,-0.307046141868695,
1.84409696900549));
#40637=CARTESIAN_POINT('Ctrl Pts',(367.414533876438,-0.301183036028645,
1.94604140494679));
#40638=CARTESIAN_POINT('Ctrl Pts',(367.474980931379,-0.295319930188594,
2.04532257737789));
#40639=CARTESIAN_POINT('Ctrl Pts',(367.53541824693,-0.289457769027829,2.14458775336109));
#40640=CARTESIAN_POINT('Ctrl Pts',(367.600270198113,-0.283595607867065,
2.24119016769621));
#40641=CARTESIAN_POINT('Ctrl Pts',(367.669265030756,-0.2777334467063,2.33472260257821));
#40642=CARTESIAN_POINT('Ctrl Pts',(367.738265281955,-0.271870825156812,
2.42826238309215));
#40643=CARTESIAN_POINT('Ctrl Pts',(367.811408816996,-0.266008203607325,
2.51873137362716));
#40644=CARTESIAN_POINT('Ctrl Pts',(367.888382183185,-0.260145582057837,
2.60575363915912));
#40645=CARTESIAN_POINT('Ctrl Pts',(367.96538004165,-0.254281095071549,2.69280359444305));
#40646=CARTESIAN_POINT('Ctrl Pts',(368.046209881964,-0.24841660808526,2.77640433567425));
#40647=CARTESIAN_POINT('Ctrl Pts',(368.130520310688,-0.242552121098972,
2.85621565169292));
#40648=CARTESIAN_POINT('Ctrl Pts',(368.214923611673,-0.236681174079493,
2.93611488396953));
#40649=CARTESIAN_POINT('Ctrl Pts',(368.302814854683,-0.230810227060013,
3.01221607612009));
#40650=CARTESIAN_POINT('Ctrl Pts',(368.393808309786,-0.224939280040534,
3.08421824266495));
#40651=CARTESIAN_POINT('Ctrl Pts',(368.484861606446,-0.21906447201135,3.15626776120651));
#40652=CARTESIAN_POINT('Ctrl Pts',(368.57902084509,-0.213189663982166,3.2242126453513));
#40653=CARTESIAN_POINT('Ctrl Pts',(368.675871377948,-0.207314855952981,
3.28779528154807));
#40654=CARTESIAN_POINT('Ctrl Pts',(368.7728599454,-0.201431674952421,3.35146853782812));
#40655=CARTESIAN_POINT('Ctrl Pts',(368.872547109993,-0.19554849395186,3.41076692797266));
#40656=CARTESIAN_POINT('Ctrl Pts',(368.974493672812,-0.1896653129513,3.46547875739509));
#40657=CARTESIAN_POINT('Ctrl Pts',(368.998637955345,-0.188271983148544,
3.47843630918389));
#40658=CARTESIAN_POINT('Ctrl Pts',(369.02290888086,-0.186878653345788,3.4911368154074));
#40659=CARTESIAN_POINT('Ctrl Pts',(369.047300464512,-0.185485323543031,
3.50357786447521));
#40660=CARTESIAN_POINT('Ctrl Pts',(369.149105904895,-0.179669852264471,
3.55550423781901));
#40661=CARTESIAN_POINT('Ctrl Pts',(369.253360637276,-0.17385438098591,3.60308333242703));
#40662=CARTESIAN_POINT('Ctrl Pts',(369.359652963928,-0.168038909707349,
3.64607356813824));
#40663=CARTESIAN_POINT('Ctrl Pts',(369.465809271562,-0.162230880308276,
3.68900879056884));
#40664=CARTESIAN_POINT('Ctrl Pts',(369.573997602747,-0.156422850909202,
3.72736667042392));
#40665=CARTESIAN_POINT('Ctrl Pts',(369.683781476545,-0.150614821510128,
3.76095134852051));
#40666=CARTESIAN_POINT('Ctrl Pts',(369.793455633911,-0.144812596572471,
3.79450246257071));
#40667=CARTESIAN_POINT('Ctrl Pts',(369.90472176221,-0.139010371634813,3.82328973690433));
#40668=CARTESIAN_POINT('Ctrl Pts',(370.017123934124,-0.133208146697156,
3.84716559282111));
#40669=CARTESIAN_POINT('Ctrl Pts',(370.12944833016,-0.127409936567555,3.87102492801012));
#40670=CARTESIAN_POINT('Ctrl Pts',(370.242906795218,-0.121611726437954,
3.88997951496179));
#40671=CARTESIAN_POINT('Ctrl Pts',(370.357029515543,-0.115813516308353,
3.90393197209095));
#40672=CARTESIAN_POINT('Ctrl Pts',(370.471111671465,-0.110017367126275,
3.91787946988243));
#40673=CARTESIAN_POINT('Ctrl Pts',(370.585857195012,-0.104221217944197,
3.92682832001067));
#40674=CARTESIAN_POINT('Ctrl Pts',(370.700788087664,-0.0984250687621187,
3.93073260368975));
#40675=CARTESIAN_POINT('Ctrl Pts',(370.815707265729,-0.0926295103654732,
3.934636489416));
#40676=CARTESIAN_POINT('Ctrl Pts',(370.930811353533,-0.0868339519688277,
3.93349681685789));
#40677=CARTESIAN_POINT('Ctrl Pts',(371.045620097053,-0.0810383935721821,
3.92731974274477));
#40678=CARTESIAN_POINT('Ctrl Pts',(371.160446245561,-0.0752419565697322,
3.92114173218812));
#40679=CARTESIAN_POINT('Ctrl Pts',(371.274976539408,-0.0694455195672822,
3.90992482587317));
#40680=CARTESIAN_POINT('Ctrl Pts',(371.388734429562,-0.0636490825648323,
3.89372716813622));
#40681=CARTESIAN_POINT('Ctrl Pts',(371.502604957337,-0.057846906207729,
3.87751347225338));
#40682=CARTESIAN_POINT('Ctrl Pts',(371.615701135977,-0.0520447298506258,
3.8563092379738));
#40683=CARTESIAN_POINT('Ctrl Pts',(371.727555213591,-0.0462425534935225,
3.83022401669202));
#40684=CARTESIAN_POINT('Ctrl Pts',(371.839468999384,-0.0404372799102038,
3.80412487100908));
#40685=CARTESIAN_POINT('Ctrl Pts',(371.950138958083,-0.0346320063268851,
3.77313966492761));
#40686=CARTESIAN_POINT('Ctrl Pts',(372.059112930347,-0.0288267327435663,
3.73742772760287));
#40687=CARTESIAN_POINT('Ctrl Pts',(372.168252435842,-0.0230126408555866,
3.70166154326654));
#40688=CARTESIAN_POINT('Ctrl Pts',(372.275690416357,-0.0171985489676068,
3.66115443970971));
#40689=CARTESIAN_POINT('Ctrl Pts',(372.380994919605,-0.011384457079627,
3.61611380522396));
#40690=CARTESIAN_POINT('Ctrl Pts',(372.449268758601,-0.00761490913793266,
3.58691185343346));
#40691=CARTESIAN_POINT('Ctrl Pts',(372.516646252166,-0.00384536119623833,
3.55580517448111));
#40692=CARTESIAN_POINT('Ctrl Pts',(372.583015783242,-7.58132545439984E-5,
3.52286027959531));
#40693=CARTESIAN_POINT('',(369.085623377893,-2.77555756156289E-16,3.52286199445083));
#40694=CARTESIAN_POINT('Origin',(370.834317853224,0.,0.));
#40695=CARTESIAN_POINT('',(366.899343652645,-0.220836477965047,0.00293853132396546));
#40696=CARTESIAN_POINT('Ctrl Pts',(369.085623377893,-1.52655665885959E-15,
3.52286199445085));
#40697=CARTESIAN_POINT('Ctrl Pts',(367.913859775743,-0.0661720391372309,
2.94121657640649));
#40698=CARTESIAN_POINT('Ctrl Pts',(366.970282437321,-0.139784198458912,
1.59707612697616));
#40699=CARTESIAN_POINT('Ctrl Pts',(366.896697454669,-0.213396357780595,
0.149413139069871));
#40700=CARTESIAN_POINT('Ctrl Pts',(366.897788092871,-0.220836477965047,
0.00293969297354404));
#40701=CARTESIAN_POINT('',(366.901318304758,-1.47083647792631,0.00188461231299786));
#40702=CARTESIAN_POINT('Ctrl Pts',(366.901318949881,-0.220836477965047,
0.00293705622590823));
#40703=CARTESIAN_POINT('Ctrl Pts',(366.901234427765,-0.226590815698461,
-0.110246132556759));
#40704=CARTESIAN_POINT('Ctrl Pts',(366.906039797176,-0.232345153431876,
-0.223646287279866));
#40705=CARTESIAN_POINT('Ctrl Pts',(366.915764765303,-0.23809949116529,-0.336794740378594));
#40706=CARTESIAN_POINT('Ctrl Pts',(366.925477985005,-0.243846877265747,
-0.44980650241884));
#40707=CARTESIAN_POINT('Ctrl Pts',(366.940098957755,-0.249594263366204,
-0.562566741970477));
#40708=CARTESIAN_POINT('Ctrl Pts',(366.959605392163,-0.255341649466661,
-0.674605324692005));
#40709=CARTESIAN_POINT('Ctrl Pts',(366.979642603147,-0.261245423856523,
-0.789692514553013));
#40710=CARTESIAN_POINT('Ctrl Pts',(367.004834999942,-0.267149198246385,
-0.904017749906057));
#40711=CARTESIAN_POINT('Ctrl Pts',(367.035101201619,-0.273052972636247,
-1.01707513693258));
#40712=CARTESIAN_POINT('Ctrl Pts',(367.064521882916,-0.278791818449364,
-1.1269741387124));
#40713=CARTESIAN_POINT('Ctrl Pts',(367.098736520101,-0.284530664262481,
-1.23567474535294));
#40714=CARTESIAN_POINT('Ctrl Pts',(367.137618511887,-0.290269510075598,
-1.34272222732676));
#40715=CARTESIAN_POINT('Ctrl Pts',(367.176490656075,-0.29600690241781,-1.44974259750745));
#40716=CARTESIAN_POINT('Ctrl Pts',(367.220027659705,-0.301744294760022,
-1.55511027016918));
#40717=CARTESIAN_POINT('Ctrl Pts',(367.268053469544,-0.307481687102234,
-1.65838697103408));
#40718=CARTESIAN_POINT('Ctrl Pts',(367.316079741298,-0.31321913462706,-1.76166466522104));
#40719=CARTESIAN_POINT('Ctrl Pts',(367.368594722556,-0.318956582151886,
-1.86285095747377));
#40720=CARTESIAN_POINT('Ctrl Pts',(367.42537515651,-0.324694029676713,-1.96152968127402));
#40721=CARTESIAN_POINT('Ctrl Pts',(367.485032850718,-0.330722213438933,
-2.06520879605726));
#40722=CARTESIAN_POINT('Ctrl Pts',(367.549399382709,-0.336750397201152,
-2.16611907350112));
#40723=CARTESIAN_POINT('Ctrl Pts',(367.618163464101,-0.342778580963372,
-2.26381093409381));
#40724=CARTESIAN_POINT('Ctrl Pts',(367.68370180763,-0.348523981327521,-2.35692004847437));
#40725=CARTESIAN_POINT('Ctrl Pts',(367.753234155057,-0.35426938169167,-2.44710554481106));
#40726=CARTESIAN_POINT('Ctrl Pts',(367.826449722831,-0.360014782055818,
-2.53401229479408));
#40727=CARTESIAN_POINT('Ctrl Pts',(367.89971427732,-0.36576402652439,-2.62097719192105));
#40728=CARTESIAN_POINT('Ctrl Pts',(367.976666662431,-0.371513270992961,
-2.70465866445914));
#40729=CARTESIAN_POINT('Ctrl Pts',(368.056959715535,-0.377262515461532,
-2.78473890607607));
#40730=CARTESIAN_POINT('Ctrl Pts',(368.137368011638,-0.383020011704652,
-2.86493408524752));
#40731=CARTESIAN_POINT('Ctrl Pts',(368.221126219979,-0.388777507947771,
-2.9415174392729));
#40732=CARTESIAN_POINT('Ctrl Pts',(368.307854884267,-0.394535004190891,
-3.01421198101424));
#40733=CARTESIAN_POINT('Ctrl Pts',(368.320393985063,-0.39536741440171,-3.02472204932538));
#40734=CARTESIAN_POINT('Ctrl Pts',(368.332995130104,-0.39619982461253,-3.03515090546895));
#40735=CARTESIAN_POINT('Ctrl Pts',(368.345657126446,-0.39703223482335,-3.04549778968796));
#40736=CARTESIAN_POINT('Ctrl Pts',(368.43501691424,-0.402906821877936,-3.11851908531629));
#40737=CARTESIAN_POINT('Ctrl Pts',(368.527743429137,-0.408781408932522,
-3.18772681551179));
#40738=CARTESIAN_POINT('Ctrl Pts',(368.623477395761,-0.414655995987109,
-3.25279471710768));
#40739=CARTESIAN_POINT('Ctrl Pts',(368.719086275458,-0.420522907249488,
-3.31777760035463));
#40740=CARTESIAN_POINT('Ctrl Pts',(368.817694453855,-0.426389818511866,
-3.37863118196099));
#40741=CARTESIAN_POINT('Ctrl Pts',(368.91890901952,-0.432256729774245,-3.43506884934927));
#40742=CARTESIAN_POINT('Ctrl Pts',(369.020018356643,-0.438117541454837,
-3.49144784085979));
#40743=CARTESIAN_POINT('Ctrl Pts',(369.123728332576,-0.443978353135429,
-3.54341985015297));
#40744=CARTESIAN_POINT('Ctrl Pts',(369.229616995135,-0.44983916481602,-3.59074144934557));
#40745=CARTESIAN_POINT('Ctrl Pts',(369.339307084574,-0.455910380958478,
-3.63976190462764));
#40746=CARTESIAN_POINT('Ctrl Pts',(369.451334858364,-0.461981597100936,
-3.6837915195401));
#40747=CARTESIAN_POINT('Ctrl Pts',(369.565202912687,-0.468052813243394,
-3.72261148492628));
#40748=CARTESIAN_POINT('Ctrl Pts',(369.67499397438,-0.473906652320662,-3.76004151953938));
#40749=CARTESIAN_POINT('Ctrl Pts',(369.786495371136,-0.47976049139793,-3.79262842019649));
#40750=CARTESIAN_POINT('Ctrl Pts',(369.899241547008,-0.485614330475199,
-3.82022529460672));
#40751=CARTESIAN_POINT('Ctrl Pts',(370.011969085537,-0.491467201892101,
-3.8478176071557));
#40752=CARTESIAN_POINT('Ctrl Pts',(370.125940592961,-0.497320073309003,
-3.87042143549834));
#40753=CARTESIAN_POINT('Ctrl Pts',(370.24067733466,-0.503172944725905,-3.88794032036495));
#40754=CARTESIAN_POINT('Ctrl Pts',(370.355422840317,-0.509026263203728,
-3.90546054337966));
#40755=CARTESIAN_POINT('Ctrl Pts',(370.470933288102,-0.514879581681551,
-3.91789498858037));
#40756=CARTESIAN_POINT('Ctrl Pts',(370.586722485398,-0.520732900159374,
-3.92519878908458));
#40757=CARTESIAN_POINT('Ctrl Pts',(370.702548511644,-0.526588080396118,
-3.93250491270102));
#40758=CARTESIAN_POINT('Ctrl Pts',(370.818653051683,-0.532443260632862,
-3.93467712077262));
#40759=CARTESIAN_POINT('Ctrl Pts',(370.934548270486,-0.538298440869606,
-3.93172263307771));
#40760=CARTESIAN_POINT('Ctrl Pts',(371.050572154818,-0.544160121459632,
-3.92876486534478));
#40761=CARTESIAN_POINT('Ctrl Pts',(371.166385840931,-0.550021802049658,
-3.92066905220891));
#40762=CARTESIAN_POINT('Ctrl Pts',(371.281504887398,-0.555883482639684,
-3.90749443460466));
#40763=CARTESIAN_POINT('Ctrl Pts',(371.39670000685,-0.561749036746287,-3.89431111094779));
#40764=CARTESIAN_POINT('Ctrl Pts',(371.511199165663,-0.56761459085289,-3.87604236462034));
#40765=CARTESIAN_POINT('Ctrl Pts',(371.624528107544,-0.573480144959494,
-3.85279856130163));
#40766=CARTESIAN_POINT('Ctrl Pts',(371.738020524004,-0.57935416000267,-3.82952122929286));
#40767=CARTESIAN_POINT('Ctrl Pts',(371.850338955568,-0.585228175045846,
-3.80125461822108));
#40768=CARTESIAN_POINT('Ctrl Pts',(371.961024224051,-0.591102190089022,
-3.76815893427253));
#40769=CARTESIAN_POINT('Ctrl Pts',(371.988950872021,-0.592584244137683,
-3.75980866754208));
#40770=CARTESIAN_POINT('Ctrl Pts',(372.016773656166,-0.594066298186344,
-3.7511512266878));
#40771=CARTESIAN_POINT('Ctrl Pts',(372.044485418052,-0.595548352235006,
-3.74218966182081));
#40772=CARTESIAN_POINT('Ctrl Pts',(372.154481444827,-0.601431054947578,
-3.70661860960474));
#40773=CARTESIAN_POINT('Ctrl Pts',(372.263084729786,-0.607313757660151,
-3.66613649502488));
#40774=CARTESIAN_POINT('Ctrl Pts',(372.36982554564,-0.613196460372723,-3.6208707691011));
#40775=CARTESIAN_POINT('Ctrl Pts',(372.476431606303,-0.619071736453563,
-3.57566218899838));
#40776=CARTESIAN_POINT('Ctrl Pts',(372.581179498504,-0.624947012534402,
-3.52568216769427));
#40777=CARTESIAN_POINT('Ctrl Pts',(372.683614836949,-0.630822288615242,
-3.47110784418825));
#40778=CARTESIAN_POINT('Ctrl Pts',(372.785947967316,-0.636691702454758,
-3.41658797392835));
#40779=CARTESIAN_POINT('Ctrl Pts',(372.885972772728,-0.642561116294274,
-3.35748311290708));
#40780=CARTESIAN_POINT('Ctrl Pts',(372.983255643082,-0.648430530133791,
-3.29401812006566));
#40781=CARTESIAN_POINT('Ctrl Pts',(373.08383132835,-0.654498610946827,-3.22840497437678));
#40782=CARTESIAN_POINT('Ctrl Pts',(373.181475754103,-0.660566691759863,
-3.15813147174083));
#40783=CARTESIAN_POINT('Ctrl Pts',(373.275737999055,-0.666634772572899,
-3.08349747389725));
#40784=CARTESIAN_POINT('Ctrl Pts',(373.366814166754,-0.672497751393524,
-3.01138611576976));
#40785=CARTESIAN_POINT('Ctrl Pts',(373.454732750234,-0.678360730214148,
-2.93520454944456));
#40786=CARTESIAN_POINT('Ctrl Pts',(373.539117912785,-0.684223709034772,
-2.85526629892858));
#40787=CARTESIAN_POINT('Ctrl Pts',(373.623491786546,-0.69008590352393,-2.77533874230853));
#40788=CARTESIAN_POINT('Ctrl Pts',(373.70433288055,-0.695948098013087,-2.69165578387076));
#40789=CARTESIAN_POINT('Ctrl Pts',(373.781300729666,-0.701810292502244,
-2.60456924000078));
#40790=CARTESIAN_POINT('Ctrl Pts',(373.858276728288,-0.707673107692014,
-2.51747347523727));
#40791=CARTESIAN_POINT('Ctrl Pts',(373.93137839401,-0.713535922881785,-2.42697371697525));
#40792=CARTESIAN_POINT('Ctrl Pts',(374.000304680523,-0.719398738071556,
-2.3334558940266));
#40793=CARTESIAN_POINT('Ctrl Pts',(374.069254783761,-0.725263579092993,
-2.23990575701705));
#40794=CARTESIAN_POINT('Ctrl Pts',(374.134026394532,-0.73112842011443,-2.14333581259028));
#40795=CARTESIAN_POINT('Ctrl Pts',(374.19436142697,-0.736993261135867,-2.04416148641085));
#40796=CARTESIAN_POINT('Ctrl Pts',(374.25476533676,-0.742864797350716,-1.94487394466549));
#40797=CARTESIAN_POINT('Ctrl Pts',(374.310722345107,-0.748736333565566,
-1.84297643876841));
#40798=CARTESIAN_POINT('Ctrl Pts',(374.362019974693,-0.754607869780415,
-1.73890964175274));
#40799=CARTESIAN_POINT('Ctrl Pts',(374.413352542805,-0.760483405065387,
-1.63477196542995));
#40800=CARTESIAN_POINT('Ctrl Pts',(374.460019247498,-0.766358940350359,
-1.52846243173027));
#40801=CARTESIAN_POINT('Ctrl Pts',(374.501856133221,-0.772234475635331,
-1.42044076425583));
#40802=CARTESIAN_POINT('Ctrl Pts',(374.543754029754,-0.778118579224664,
-1.31226156857679));
#40803=CARTESIAN_POINT('Ctrl Pts',(374.580807919275,-0.784002682813997,
-1.20236564459075));
#40804=CARTESIAN_POINT('Ctrl Pts',(374.612903924456,-0.789886786403331,
-1.0912269710248));
#40805=CARTESIAN_POINT('Ctrl Pts',(374.620499923914,-0.791279347484441,
-1.06492434241461));
#40806=CARTESIAN_POINT('Ctrl Pts',(374.62781845736,-0.792671908565551,-1.03855214562892));
#40807=CARTESIAN_POINT('Ctrl Pts',(374.634858437725,-0.794064469646662,
-1.01211672526561));
#40808=CARTESIAN_POINT('Ctrl Pts',(374.664527507088,-0.799933234780828,
-0.900708130382654));
#40809=CARTESIAN_POINT('Ctrl Pts',(374.689343901236,-0.805801999914994,
-0.787805313291286));
#40810=CARTESIAN_POINT('Ctrl Pts',(374.709158397564,-0.81167076504916,-0.673869242462348));
#40811=CARTESIAN_POINT('Ctrl Pts',(374.728947086403,-0.817531886380949,
-0.560081568236297));
#40812=CARTESIAN_POINT('Ctrl Pts',(374.743746762255,-0.823393007712738,
-0.445263720451045));
#40813=CARTESIAN_POINT('Ctrl Pts',(374.753458183173,-0.829254129044527,
-0.329891003466261));
#40814=CARTESIAN_POINT('Ctrl Pts',(374.76315956181,-0.835109189571829,-0.214637589843619));
#40815=CARTESIAN_POINT('Ctrl Pts',(374.767783116298,-0.84096425009913,-0.0988308582322655));
#40816=CARTESIAN_POINT('Ctrl Pts',(374.767280916993,-0.846819310626432,
0.0170452055034932));
#40817=CARTESIAN_POINT('Ctrl Pts',(374.766759991466,-0.852892697144427,
0.137242105257054));
#40818=CARTESIAN_POINT('Ctrl Pts',(374.760723519815,-0.858966083662422,
0.257513161864049));
#40819=CARTESIAN_POINT('Ctrl Pts',(374.749177157538,-0.865039470180417,
0.377313698964833));
#40820=CARTESIAN_POINT('Ctrl Pts',(374.738058864704,-0.870887692172542,
0.492672755014569));
#40821=CARTESIAN_POINT('Ctrl Pts',(374.721832007549,-0.876735914164666,
0.607595110489041));
#40822=CARTESIAN_POINT('Ctrl Pts',(374.700554655476,-0.882584136156791,
0.721596832665063));
#40823=CARTESIAN_POINT('Ctrl Pts',(374.679280607887,-0.888431449889361,
0.835580849775604));
#40824=CARTESIAN_POINT('Ctrl Pts',(374.652957700854,-0.894278763621932,
0.948644111060452));
#40825=CARTESIAN_POINT('Ctrl Pts',(374.6216953827,-0.900126077354503,1.06031148688492));
#40826=CARTESIAN_POINT('Ctrl Pts',(374.590430323825,-0.905973903712251,
1.17198865241984));
#40827=CARTESIAN_POINT('Ctrl Pts',(374.554225104672,-0.91182173007,1.28226929059222));
#40828=CARTESIAN_POINT('Ctrl Pts',(374.513239244379,-0.917669556427749,
1.3906927761732));
#40829=CARTESIAN_POINT('Ctrl Pts',(374.472239832407,-0.923519316327171,
1.49915211119891));
#40830=CARTESIAN_POINT('Ctrl Pts',(374.426456782632,-0.929369076226593,
1.60575268567303));
#40831=CARTESIAN_POINT('Ctrl Pts',(374.376097729164,-0.935218836126015,
1.71005389107764));
#40832=CARTESIAN_POINT('Ctrl Pts',(374.32568156061,-0.941075230572934,1.8144733904487));
#40833=CARTESIAN_POINT('Ctrl Pts',(374.270679209817,-0.946931625019853,
1.91658794271533));
#40834=CARTESIAN_POINT('Ctrl Pts',(374.21134428671,-0.952788019466772,2.01598151468107));
#40835=CARTESIAN_POINT('Ctrl Pts',(374.151969390969,-0.958648359237997,
2.11544204591309));
#40836=CARTESIAN_POINT('Ctrl Pts',(374.088256338433,-0.964508699009221,
2.212177602151));
#40837=CARTESIAN_POINT('Ctrl Pts',(374.020501076916,-0.970369038780445,
2.30580256419781));
#40838=CARTESIAN_POINT('Ctrl Pts',(373.952646309136,-0.976237985123354,
2.3995650250892));
#40839=CARTESIAN_POINT('Ctrl Pts',(373.880737741167,-0.982106931466264,
2.49020745178429));
#40840=CARTESIAN_POINT('Ctrl Pts',(373.805110467789,-0.987975877809173,
2.57737855994104));
#40841=CARTESIAN_POINT('Ctrl Pts',(373.785331698605,-0.989510780892221,
2.60017638340796));
#40842=CARTESIAN_POINT('Ctrl Pts',(373.765298765781,-0.991045683975268,
2.62273698068117));
#40843=CARTESIAN_POINT('Ctrl Pts',(373.7450180497,-0.992580587058316,2.6450545110137));
#40844=CARTESIAN_POINT('Ctrl Pts',(373.667402471763,-0.998454757841746,
2.73046510539298));
#40845=CARTESIAN_POINT('Ctrl Pts',(373.585895108387,-1.00432892862518,2.81259870524487));
#40846=CARTESIAN_POINT('Ctrl Pts',(373.500803564184,-1.0102030994086,2.89107989395727));
#40847=CARTESIAN_POINT('Ctrl Pts',(373.415821930156,-1.0160696827033,2.96945971089188));
#40848=CARTESIAN_POINT('Ctrl Pts',(373.327265622912,-1.02193626599799,3.04419622120281));
#40849=CARTESIAN_POINT('Ctrl Pts',(373.23548132504,-1.02780284929268,3.11494831122668));
#40850=CARTESIAN_POINT('Ctrl Pts',(373.143791077077,-1.0336634211929,3.1856279027106));
#40851=CARTESIAN_POINT('Ctrl Pts',(373.048879742946,-1.03952399309311,3.25233094422102));
#40852=CARTESIAN_POINT('Ctrl Pts',(372.951129053949,-1.04538456499333,3.31475479341772));
#40853=CARTESIAN_POINT('Ctrl Pts',(372.849862898589,-1.05145590413819,3.37942362875561));
#40854=CARTESIAN_POINT('Ctrl Pts',(372.745549649257,-1.05752724328305,3.43949938190571));
#40855=CARTESIAN_POINT('Ctrl Pts',(372.638649337469,-1.06359858242791,3.49469267532374));
#40856=CARTESIAN_POINT('Ctrl Pts',(372.535578934053,-1.06945240422199,3.5479085633163));
#40857=CARTESIAN_POINT('Ctrl Pts',(372.430104058848,-1.07530622601607,3.59658563003629));
#40858=CARTESIAN_POINT('Ctrl Pts',(372.322663715453,-1.08116004781016,3.64051034806745));
#40859=CARTESIAN_POINT('Ctrl Pts',(372.215239617031,-1.08701298450677,3.68442842468413));
#40860=CARTESIAN_POINT('Ctrl Pts',(372.10585102357,-1.09286592120338,3.72359542510701));
#40861=CARTESIAN_POINT('Ctrl Pts',(371.994957353933,-1.0987188579,3.75784578573875));
#40862=CARTESIAN_POINT('Ctrl Pts',(371.884053645702,-1.10457232443071,3.79209924686686));
#40863=CARTESIAN_POINT('Ctrl Pts',(371.771644985145,-1.11042579096142,3.82143506153576));
#40864=CARTESIAN_POINT('Ctrl Pts',(371.65820571613,-1.11627925749214,3.84573761317069));
#40865=CARTESIAN_POINT('Ctrl Pts',(371.544728757109,-1.12213466882724,3.87004823928745));
#40866=CARTESIAN_POINT('Ctrl Pts',(371.430220912433,-1.12799008016235,3.8893221906019));
#40867=CARTESIAN_POINT('Ctrl Pts',(371.31516576963,-1.13384549149745,3.90349513657796));
#40868=CARTESIAN_POINT('Ctrl Pts',(371.199980493832,-1.13970752558923,3.91768411284928));
#40869=CARTESIAN_POINT('Ctrl Pts',(371.084247094577,-1.145569559681,3.92676051768643));
#40870=CARTESIAN_POINT('Ctrl Pts',(370.968453420699,-1.15143159377278,3.93071197743338));
#40871=CARTESIAN_POINT('Ctrl Pts',(370.852581812872,-1.15729757325678,3.93466609667673));
#40872=CARTESIAN_POINT('Ctrl Pts',(370.736650261674,-1.16316355274079,3.93348840664086));
#40873=CARTESIAN_POINT('Ctrl Pts',(370.621144014598,-1.16902953222479,3.92721859775153));
#40874=CARTESIAN_POINT('Ctrl Pts',(370.50546915118,-1.17490407488202,3.92093963617768));
#40875=CARTESIAN_POINT('Ctrl Pts',(370.390221240461,-1.18077861753925,3.90955376079433));
#40876=CARTESIAN_POINT('Ctrl Pts',(370.275877907201,-1.18665316019649,3.89315217101589));
#40877=CARTESIAN_POINT('Ctrl Pts',(370.247047880572,-1.18813434162098,3.88901674609357));
#40878=CARTESIAN_POINT('Ctrl Pts',(370.218275294763,-1.18961552304547,3.88456271075643));
#40879=CARTESIAN_POINT('Ctrl Pts',(370.189567661076,-1.19109670446997,3.87979202918465));
#40880=CARTESIAN_POINT('Ctrl Pts',(370.075708923278,-1.1969712899297,3.86087079770612));
#40881=CARTESIAN_POINT('Ctrl Pts',(369.962494838753,-1.20284587538942,3.8369018660354));
#40882=CARTESIAN_POINT('Ctrl Pts',(369.850407688153,-1.20872046084915,3.80794036023027));
#40883=CARTESIAN_POINT('Ctrl Pts',(369.738464919095,-1.21458747914623,3.77901616027875));
#40884=CARTESIAN_POINT('Ctrl Pts',(369.627646593364,-1.2204544974433,3.74511227789214));
#40885=CARTESIAN_POINT('Ctrl Pts',(369.518427331906,-1.22632151574038,3.70633527030471));
#40886=CARTESIAN_POINT('Ctrl Pts',(369.409319610662,-1.23218254234268,3.66759786375174));
#40887=CARTESIAN_POINT('Ctrl Pts',(369.301808092295,-1.23804356894498,3.62399736847882));
#40888=CARTESIAN_POINT('Ctrl Pts',(369.196354052403,-1.24390459554727,3.57569064478454));
#40889=CARTESIAN_POINT('Ctrl Pts',(369.087118914978,-1.24997577164454,3.52565186384557));
#40890=CARTESIAN_POINT('Ctrl Pts',(368.980092005545,-1.2560469477418,3.47056314614565));
#40891=CARTESIAN_POINT('Ctrl Pts',(368.875765726678,-1.26211812383907,3.41065427265807));
#40892=CARTESIAN_POINT('Ctrl Pts',(368.775165822266,-1.26797244685032,3.35288525212275));
#40893=CARTESIAN_POINT('Ctrl Pts',(368.677077312013,-1.27382676986157,3.29063474660381));
#40894=CARTESIAN_POINT('Ctrl Pts',(368.581917608772,-1.27968109287282,3.22415603511867));
#40895=CARTESIAN_POINT('Ctrl Pts',(368.486772025745,-1.28553454719394,3.15768718803637));
#40896=CARTESIAN_POINT('Ctrl Pts',(368.394554724071,-1.29138800151506,3.08699161896017));
#40897=CARTESIAN_POINT('Ctrl Pts',(368.305653866951,-1.29724145583618,3.0123657554363));
#40898=CARTESIAN_POINT('Ctrl Pts',(368.216744721041,-1.30309545591186,2.93773293407125));
#40899=CARTESIAN_POINT('Ctrl Pts',(368.131152950724,-1.30894945598755,2.85916935532755));
#40900=CARTESIAN_POINT('Ctrl Pts',(368.04923282857,-1.31480345606323,2.77701105605485));
#40901=CARTESIAN_POINT('Ctrl Pts',(367.967285274941,-1.32065941638826,2.69482524555043));
#40902=CARTESIAN_POINT('Ctrl Pts',(367.889012105708,-1.32651537671329,2.60904261325329));
#40903=CARTESIAN_POINT('Ctrl Pts',(367.814729499569,-1.33237133703832,2.52003475660019));
#40904=CARTESIAN_POINT('Ctrl Pts',(367.740362627206,-1.33823394036761,2.43092592939101));
#40905=CARTESIAN_POINT('Ctrl Pts',(367.669995618135,-1.34409654369689,2.33858489253369));
#40906=CARTESIAN_POINT('Ctrl Pts',(367.603903294895,-1.34995914702618,2.24341498197191));
#40907=CARTESIAN_POINT('Ctrl Pts',(367.537766352001,-1.35582570826346,2.14818082115663));
#40908=CARTESIAN_POINT('Ctrl Pts',(367.475910061212,-1.36169226950075,2.05011433221244));
#40909=CARTESIAN_POINT('Ctrl Pts',(367.41856407928,-1.36755883073803,1.9496448794047));
#40910=CARTESIAN_POINT('Ctrl Pts',(367.361134255697,-1.37343396907469,1.84902853705703));
#40911=CARTESIAN_POINT('Ctrl Pts',(367.308228089329,-1.37930910741135,1.7460025853227));
#40912=CARTESIAN_POINT('Ctrl Pts',(367.260027817216,-1.38518424574801,1.64101789706739));
#40913=CARTESIAN_POINT('Ctrl Pts',(367.24791697758,-1.38666043779255,1.61463935877258));
#40914=CARTESIAN_POINT('Ctrl Pts',(367.236102986169,-1.38813662983709,1.58813724181436));
#40915=CARTESIAN_POINT('Ctrl Pts',(367.224588238786,-1.38961282188163,1.56151884735705));
#40916=CARTESIAN_POINT('Ctrl Pts',(367.171790801604,-1.39638145988535,1.4394681446803));
#40917=CARTESIAN_POINT('Ctrl Pts',(367.125132255917,-1.40315009788907,1.3146085025099));
#40918=CARTESIAN_POINT('Ctrl Pts',(367.084888280074,-1.4099187358928,1.1875465784499));
#40919=CARTESIAN_POINT('Ctrl Pts',(367.046449861813,-1.41638369700041,1.06618532425741));
#40920=CARTESIAN_POINT('Ctrl Pts',(367.013863146076,-1.42284865810803,0.942815388015679));
#40921=CARTESIAN_POINT('Ctrl Pts',(366.987321294167,-1.42931361921565,0.817989287584305));
#40922=CARTESIAN_POINT('Ctrl Pts',(366.960853551685,-1.43576052903715,0.693511723148201));
#40923=CARTESIAN_POINT('Ctrl Pts',(366.940397090558,-1.44220743885865,0.567586355194118));
#40924=CARTESIAN_POINT('Ctrl Pts',(366.926095588808,-1.44865434868014,0.440780820727839));
#40925=CARTESIAN_POINT('Ctrl Pts',(366.91185314515,-1.4550746359692,0.314498930076723));
#40926=CARTESIAN_POINT('Ctrl Pts',(366.903715033871,-1.46149492325826,0.187344380357386));
#40927=CARTESIAN_POINT('Ctrl Pts',(366.901773925552,-1.46791521054732,0.0598937136168328));
#40928=CARTESIAN_POINT('Ctrl Pts',(366.901479520429,-1.46888896634032,0.0405634532293221));
#40929=CARTESIAN_POINT('Ctrl Pts',(366.901327572947,-1.46986272213331,0.0212264068426718));
#40930=CARTESIAN_POINT('Ctrl Pts',(366.901318304758,-1.47083647792631,0.00188461231300882));
#40931=CARTESIAN_POINT('',(366.901319334106,-2.72083647799451,-0.00341300743396218));
#40932=CARTESIAN_POINT('Ctrl Pts',(366.901318304757,-1.47083647796505,0.00188461154355254));
#40933=CARTESIAN_POINT('Ctrl Pts',(366.901261719524,-1.47678156820664,-0.116203223969871));
#40934=CARTESIAN_POINT('Ctrl Pts',(366.906527842602,-1.48272665844822,-0.234278390804712));
#40935=CARTESIAN_POINT('Ctrl Pts',(366.917086804898,-1.48867174868981,-0.351837908745937));
#40936=CARTESIAN_POINT('Ctrl Pts',(366.92764953488,-1.49461896027934,-0.469439374686569));
#40937=CARTESIAN_POINT('Ctrl Pts',(366.943508829284,-1.50056617186887,-0.586524432214348));
#40938=CARTESIAN_POINT('Ctrl Pts',(366.964583027599,-1.50651338345841,-0.702596170888543));
#40939=CARTESIAN_POINT('Ctrl Pts',(366.985669182943,-1.51246396936283,-0.818733766072115));
#40940=CARTESIAN_POINT('Ctrl Pts',(367.011976063052,-1.51841455526725,-0.933856509621635));
#40941=CARTESIAN_POINT('Ctrl Pts',(367.043371192066,-1.52436514117167,-1.04747907485301));
#40942=CARTESIAN_POINT('Ctrl Pts',(367.074812871969,-1.53032455026213,-1.16127011307985));
#40943=CARTESIAN_POINT('Ctrl Pts',(367.111357763594,-1.5362839593526,-1.27355614956378));
#40944=CARTESIAN_POINT('Ctrl Pts',(367.152823750657,-1.54224336844306,-1.38386783067174));
#40945=CARTESIAN_POINT('Ctrl Pts',(367.19432364179,-1.54820765015872,-1.49426970654022));
#40946=CARTESIAN_POINT('Ctrl Pts',(367.240752491767,-1.55417193187437,-1.60269364785085));
#40947=CARTESIAN_POINT('Ctrl Pts',(367.291881092043,-1.56013621359003,-1.70869271463069));
#40948=CARTESIAN_POINT('Ctrl Pts',(367.343101685845,-1.56611122658532,-1.81488250104475));
#40949=CARTESIAN_POINT('Ctrl Pts',(367.39903873536,-1.57208623958061,-1.91863835015954));
#40950=CARTESIAN_POINT('Ctrl Pts',(367.459418063913,-1.57806125257591,-2.01953965351184));
#40951=CARTESIAN_POINT('Ctrl Pts',(367.49333041214,-1.58141714814836,-2.07621136911178));
#40952=CARTESIAN_POINT('Ctrl Pts',(367.528643336201,-1.58477304372082,-2.13198314630219));
#40953=CARTESIAN_POINT('Ctrl Pts',(367.565302654357,-1.58812893929328,-2.18678499848034));
#40954=CARTESIAN_POINT('Ctrl Pts',(367.629467027507,-1.59400272382044,-2.28270403542105));
#40955=CARTESIAN_POINT('Ctrl Pts',(367.697963489202,-1.5998765083476,-2.37595634573234));
#40956=CARTESIAN_POINT('Ctrl Pts',(367.77054320877,-1.60575029287476,-2.46612528635486));
#40957=CARTESIAN_POINT('Ctrl Pts',(367.843029224813,-1.6116164940947,-2.55617781501576));
#40958=CARTESIAN_POINT('Ctrl Pts',(367.919587758434,-1.61748269531463,-2.64315457153911));
#40959=CARTESIAN_POINT('Ctrl Pts',(367.999926268157,-1.62334889653457,-2.72666707584575));
#40960=CARTESIAN_POINT('Ctrl Pts',(368.080182514416,-1.62920909099594,-2.81009406664348));
#40961=CARTESIAN_POINT('Ctrl Pts',(368.16421075322,-1.63506928545731,-2.89006356505874));
#40962=CARTESIAN_POINT('Ctrl Pts',(368.251678103068,-1.64092947991869,-2.96621997176746));
#40963=CARTESIAN_POINT('Ctrl Pts',(368.34229906722,-1.64700096228478,-3.04512217944073));
#40964=CARTESIAN_POINT('Ctrl Pts',(368.436611531206,-1.65307244465088,-3.11993079519123));
#40965=CARTESIAN_POINT('Ctrl Pts',(368.534203108104,-1.65914392701697,-3.1902917044186));
#40966=CARTESIAN_POINT('Ctrl Pts',(368.628290220622,-1.6649973855088,-3.2581259888283));
#40967=CARTESIAN_POINT('Ctrl Pts',(368.725424630104,-1.67085084400064,-3.32182624026368));
#40968=CARTESIAN_POINT('Ctrl Pts',(368.825203662947,-1.67670430249247,-3.38111655676455));
#40969=CARTESIAN_POINT('Ctrl Pts',(368.924967708685,-1.68255688177761,-3.44039796768529));
#40970=CARTESIAN_POINT('Ctrl Pts',(369.027375232877,-1.68840946106274,-3.49527054975938));
#40971=CARTESIAN_POINT('Ctrl Pts',(369.1319962977,-1.69426204034787,-3.5455028305727));
#40972=CARTESIAN_POINT('Ctrl Pts',(369.23662694669,-1.70011515577833,-3.59573971308408));
#40973=CARTESIAN_POINT('Ctrl Pts',(369.343471166969,-1.70596827120879,-3.64133527046977));
#40974=CARTESIAN_POINT('Ctrl Pts',(369.452076895114,-1.71182138663925,-3.68210523121274));
#40975=CARTESIAN_POINT('Ctrl Pts',(369.560718834498,-1.71767645361093,-3.72288878544448));
#40976=CARTESIAN_POINT('Ctrl Pts',(369.671123063043,-1.72353152058261,-3.75884339859797));
#40977=CARTESIAN_POINT('Ctrl Pts',(369.782820814395,-1.72938658755429,-3.78983416224704));
#40978=CARTESIAN_POINT('Ctrl Pts',(369.89464513393,-1.73524828908372,-3.82086004249034));
#40979=CARTESIAN_POINT('Ctrl Pts',(370.00776550347,-1.74110999061315,-3.84691073616757));
#40980=CARTESIAN_POINT('Ctrl Pts',(370.1217012825,-1.74697169214257,-3.86790209585631));
#40981=CARTESIAN_POINT('Ctrl Pts',(370.235713875457,-1.75283734555011,-3.8889076076295));
#40982=CARTESIAN_POINT('Ctrl Pts',(370.35054256436,-1.75870299895765,-3.90484693682024));
#40983=CARTESIAN_POINT('Ctrl Pts',(370.465701608604,-1.76456865236519,-3.9156878149569));
#40984=CARTESIAN_POINT('Ctrl Pts',(370.581029008395,-1.77044288100274,-3.92654454180078));
#40985=CARTESIAN_POINT('Ctrl Pts',(370.696687316357,-1.77631710964028,-3.93228792160872));
#40986=CARTESIAN_POINT('Ctrl Pts',(370.812190739785,-1.78219133827782,-3.9329377557814));
#40987=CARTESIAN_POINT('Ctrl Pts',(370.841381507179,-1.78367591108686,-3.93310198604936));
#40988=CARTESIAN_POINT('Ctrl Pts',(370.870562409818,-1.7851604838959,-3.93294114670895));
#40989=CARTESIAN_POINT('Ctrl Pts',(370.89972567556,-1.78664505670494,-3.93245607944669));
#40990=CARTESIAN_POINT('Ctrl Pts',(371.015111361698,-1.79251883139494,-3.93053689044455));
#40991=CARTESIAN_POINT('Ctrl Pts',(371.13060461455,-1.79839260608493,-3.9235317516989));
#40992=CARTESIAN_POINT('Ctrl Pts',(371.245720432017,-1.80426638077492,-3.91142389906314));
#40993=CARTESIAN_POINT('Ctrl Pts',(371.360687659088,-1.81013257365272,-3.89933167512777));
#40994=CARTESIAN_POINT('Ctrl Pts',(371.475278012522,-1.81599876653052,-3.88214987859083));
#40995=CARTESIAN_POINT('Ctrl Pts',(371.589006460754,-1.82186495940832,-3.85991374329322));
#40996=CARTESIAN_POINT('Ctrl Pts',(371.702618484437,-1.82772514702643,-3.83770037127148));
#40997=CARTESIAN_POINT('Ctrl Pts',(371.815369954917,-1.83358533464455,-3.81044303113285));
#40998=CARTESIAN_POINT('Ctrl Pts',(371.926781602886,-1.83944552226266,-3.77822867964279));
#40999=CARTESIAN_POINT('Ctrl Pts',(372.042210365337,-1.84551700775657,-3.74485279127307));
#41000=CARTESIAN_POINT('Ctrl Pts',(372.156200414314,-1.85158849325049,-3.7061557285506));
#41001=CARTESIAN_POINT('Ctrl Pts',(372.268230626626,-1.8576599787444,-3.66229206348618));
#41002=CARTESIAN_POINT('Ctrl Pts',(372.376237778867,-1.86351343420555,-3.62000356422606));
#41003=CARTESIAN_POINT('Ctrl Pts',(372.482423013211,-1.86936688966669,-3.57291331431962));
#41004=CARTESIAN_POINT('Ctrl Pts',(372.586336197593,-1.87522034512784,-3.52121012167621));
#41005=CARTESIAN_POINT('Ctrl Pts',(372.690233799147,-1.88107292280444,-3.46951468244678));
#41006=CARTESIAN_POINT('Ctrl Pts',(372.791859658437,-1.88692550048104,-3.41320785994075));
#41007=CARTESIAN_POINT('Ctrl Pts',(372.890786198693,-1.89277807815764,-3.35252545763399));
#41008=CARTESIAN_POINT('Ctrl Pts',(372.989721825639,-1.89863119341051,-3.29183748147225));
#41009=CARTESIAN_POINT('Ctrl Pts',(373.085957288494,-1.90448430866338,-3.22677334257692));
#41010=CARTESIAN_POINT('Ctrl Pts',(373.179092680216,-1.91033742391624,-3.15761302421715));
#41011=CARTESIAN_POINT('Ctrl Pts',(373.272259147994,-1.91619249215109,-3.08842962945288));
#41012=CARTESIAN_POINT('Ctrl Pts',(373.362323156304,-1.92204756038593,-3.01514758366029));
#41013=CARTESIAN_POINT('Ctrl Pts',(373.448917224356,-1.92790262862077,-2.93808766521248));
#41014=CARTESIAN_POINT('Ctrl Pts',(373.535609446504,-1.93376433355642,-2.86094039959762));
#41015=CARTESIAN_POINT('Ctrl Pts',(373.618823569234,-1.93962603849207,-2.78000698909683));
#41016=CARTESIAN_POINT('Ctrl Pts',(373.698228330228,-1.94548774342772,-2.69564570737847));
#41017=CARTESIAN_POINT('Ctrl Pts',(373.777686641789,-1.95135340149696,-2.61122753241484));
#41018=CARTESIAN_POINT('Ctrl Pts',(373.853330207195,-1.95721905956621,-2.5233771953031));
#41019=CARTESIAN_POINT('Ctrl Pts',(373.924868594353,-1.96308471763545,-2.43248537847783));
#41020=CARTESIAN_POINT('Ctrl Pts',(373.996511588308,-1.96895895274604,-2.34146065535941));
#41021=CARTESIAN_POINT('Ctrl Pts',(374.064037183986,-1.97483318785662,-2.24738591097531));
#41022=CARTESIAN_POINT('Ctrl Pts',(374.12719867635,-1.98070742296721,-2.1506800981757));
#41023=CARTESIAN_POINT('Ctrl Pts',(374.143161354266,-1.98219200668367,-2.12623983109978));
#41024=CARTESIAN_POINT('Ctrl Pts',(374.158845522861,-1.98367659040014,-2.10163163060495));
#41025=CARTESIAN_POINT('Ctrl Pts',(374.174247676138,-1.9851611741166,-2.07686248413491));
#41026=CARTESIAN_POINT('Ctrl Pts',(374.235184917553,-1.99103479676543,-1.97886557221579));
#41027=CARTESIAN_POINT('Ctrl Pts',(374.291907025266,-1.99690841941426,-1.87802119648227));
#41028=CARTESIAN_POINT('Ctrl Pts',(374.344136978532,-2.0027820420631,-1.7747277840912));
#41029=CARTESIAN_POINT('Ctrl Pts',(374.396299489111,-2.00864808031137,-1.67156775081926));
#41030=CARTESIAN_POINT('Ctrl Pts',(374.443981195916,-2.01451411855964,-1.56596533510407));
#41031=CARTESIAN_POINT('Ctrl Pts',(374.486948754576,-2.02038015680791,-1.45834718036902));
#41032=CARTESIAN_POINT('Ctrl Pts',(374.529872308428,-2.02624018741016,-1.35083924172044));
#41033=CARTESIAN_POINT('Ctrl Pts',(374.568091165031,-2.03210021801241,-1.24132005173336));
#41034=CARTESIAN_POINT('Ctrl Pts',(374.601418565507,-2.03796024861466,-1.13023945406255));
#41035=CARTESIAN_POINT('Ctrl Pts',(374.635948890338,-2.0440317920694,-1.01514949608916));
#41036=CARTESIAN_POINT('Ctrl Pts',(374.665227779516,-2.05010333552413,-0.898383689086442));
#41037=CARTESIAN_POINT('Ctrl Pts',(374.689102584017,-2.05617487897886,-0.780463759087138));
#41038=CARTESIAN_POINT('Ctrl Pts',(374.712119175849,-2.06202817245776,-0.666782623072344));
#41039=CARTESIAN_POINT('Ctrl Pts',(374.730113419204,-2.06788146593666,-0.552029348212954));
#41040=CARTESIAN_POINT('Ctrl Pts',(374.742999937441,-2.07373475941556,-0.436684513719917));
#41041=CARTESIAN_POINT('Ctrl Pts',(374.755884519722,-2.07958717354782,-0.321357007606787));
#41042=CARTESIAN_POINT('Ctrl Pts',(374.763662856782,-2.08543958768007,-0.205438529059168));
#41043=CARTESIAN_POINT('Ctrl Pts',(374.7663012899,-2.09129200181233,-0.0894161825815296));
#41044=CARTESIAN_POINT('Ctrl Pts',(374.768939964745,-2.09714495212982,0.0266167936069241));
#41045=CARTESIAN_POINT('Ctrl Pts',(374.766437790135,-2.10299790244732,0.142753243570707));
#41046=CARTESIAN_POINT('Ctrl Pts',(374.758813231973,-2.10885085276482,0.258505361991111));
#41047=CARTESIAN_POINT('Ctrl Pts',(374.751186131278,-2.11470575484346,0.374296079831456));
#41048=CARTESIAN_POINT('Ctrl Pts',(374.738433277609,-2.1205606569221,0.48970179924492));
#41049=CARTESIAN_POINT('Ctrl Pts',(374.720624996025,-2.12641555900074,0.604239846263571));
#41050=CARTESIAN_POINT('Ctrl Pts',(374.70279653121,-2.13227709680322,0.718907706358394));
#41051=CARTESIAN_POINT('Ctrl Pts',(374.679901265995,-2.13813863460571,0.832705522798185));
#41052=CARTESIAN_POINT('Ctrl Pts',(374.652060667602,-2.14400017240819,0.9451607287999));
#41053=CARTESIAN_POINT('Ctrl Pts',(374.624201296653,-2.14986566256999,1.05769176189599));
#41054=CARTESIAN_POINT('Ctrl Pts',(374.591390069302,-2.15573115273178,1.1688779866112));
#41055=CARTESIAN_POINT('Ctrl Pts',(374.553797820794,-2.16159664289357,1.27826357643707));
#41056=CARTESIAN_POINT('Ctrl Pts',(374.51615060056,-2.16747071025231,1.38780912250208));
#41057=CARTESIAN_POINT('Ctrl Pts',(374.473708557019,-2.17334477761104,1.49554839575386));
#41058=CARTESIAN_POINT('Ctrl Pts',(374.426689986348,-2.17921884496978,1.60104698780224));
#41059=CARTESIAN_POINT('Ctrl Pts',(374.414794209437,-2.1807049938226,1.62773830779771));
#41060=CARTESIAN_POINT('Ctrl Pts',(374.402605714179,-2.18219114267543,1.65428633429488));
#41061=CARTESIAN_POINT('Ctrl Pts',(374.390128484359,-2.18367729152825,1.68068431167408));
#41062=CARTESIAN_POINT('Ctrl Pts',(374.340814742886,-2.18955099597836,1.78501700816801));
#41063=CARTESIAN_POINT('Ctrl Pts',(374.286823069956,-2.19542470042848,1.88735121811656));
#41064=CARTESIAN_POINT('Ctrl Pts',(374.228338108275,-2.20129840487859,1.98723816094113));
#41065=CARTESIAN_POINT('Ctrl Pts',(374.169928655086,-2.2071645259338,2.08699614219802));
#41066=CARTESIAN_POINT('Ctrl Pts',(374.107037656623,-2.213030646989,2.18431278648332));
#41067=CARTESIAN_POINT('Ctrl Pts',(374.039897142691,-2.2188967680442,2.27876071998403));
#41068=CARTESIAN_POINT('Ctrl Pts',(373.972825378801,-2.22475688235252,2.37311194139425));
#41069=CARTESIAN_POINT('Ctrl Pts',(373.901512992663,-2.23061699666084,2.46459996018473));
#41070=CARTESIAN_POINT('Ctrl Pts',(373.82623676315,-2.23647711096916,2.55282397286396));
#41071=CARTESIAN_POINT('Ctrl Pts',(373.748245014519,-2.24254862338461,2.64423058374904));
#41072=CARTESIAN_POINT('Ctrl Pts',(373.665998267915,-2.24862013580006,2.73213286109561));
#41073=CARTESIAN_POINT('Ctrl Pts',(373.579852176448,-2.2546916482155,2.81611972046616));
#41074=CARTESIAN_POINT('Ctrl Pts',(373.496801088157,-2.26054502711049,2.8970891522086));
#41075=CARTESIAN_POINT('Ctrl Pts',(373.410126341169,-2.26639840600548,2.97441935289265));
#41076=CARTESIAN_POINT('Ctrl Pts',(373.320185499786,-2.27225178490047,3.04777805028148));
#41077=CARTESIAN_POINT('Ctrl Pts',(373.230258162648,-2.27810428493482,3.12112573316519));
#41078=CARTESIAN_POINT('Ctrl Pts',(373.137066026264,-2.28395678496917,3.19050283737361));
#41079=CARTESIAN_POINT('Ctrl Pts',(373.041000174379,-2.28980928500352,3.25561701271872));
#41080=CARTESIAN_POINT('Ctrl Pts',(372.944925514806,-2.29566232161761,3.32073715798223));
#41081=CARTESIAN_POINT('Ctrl Pts',(372.845976957976,-2.30151535823171,3.38159336561159));
#41082=CARTESIAN_POINT('Ctrl Pts',(372.744574433297,-2.3073683948458,3.43793670655639));
#41083=CARTESIAN_POINT('Ctrl Pts',(372.643138089548,-2.31322338352427,3.49429883874342));
#41084=CARTESIAN_POINT('Ctrl Pts',(372.53924651148,-2.31907837220274,3.54614491086618));
#41085=CARTESIAN_POINT('Ctrl Pts',(372.433343429567,-2.32493336088122,3.59327235346863));
#41086=CARTESIAN_POINT('Ctrl Pts',(372.327320322671,-2.33079498529589,3.64045320783567));
#41087=CARTESIAN_POINT('Ctrl Pts',(372.219281539386,-2.33665660971056,3.68290459063861));
#41088=CARTESIAN_POINT('Ctrl Pts',(372.109690041444,-2.34251823412524,3.7204723868772));
#41089=CARTESIAN_POINT('Ctrl Pts',(372.00002464635,-2.34838381101207,3.75806551494505));
#41090=CARTESIAN_POINT('Ctrl Pts',(371.88880484719,-2.35424938789891,3.79076838312668));
#41091=CARTESIAN_POINT('Ctrl Pts',(371.776506301536,-2.36011496478575,3.81847743582001));
#41092=CARTESIAN_POINT('Ctrl Pts',(371.664043552036,-2.36598911836679,3.84622700491544));
#41093=CARTESIAN_POINT('Ctrl Pts',(371.550499311584,-2.37186327194783,3.86896810474756));
#41094=CARTESIAN_POINT('Ctrl Pts',(371.436356968969,-2.37773742552887,3.88664867245714));
#41095=CARTESIAN_POINT('Ctrl Pts',(371.407495143563,-2.37922275333255,3.89111934869017));
#41096=CARTESIAN_POINT('Ctrl Pts',(371.378595087753,-2.38070808113623,3.89526672833392));
#41097=CARTESIAN_POINT('Ctrl Pts',(371.349664624851,-2.38219340893991,3.899090497151));
#41098=CARTESIAN_POINT('Ctrl Pts',(371.235259727832,-2.38806710598372,3.91421150918715));
#41099=CARTESIAN_POINT('Ctrl Pts',(371.119998224111,-2.39394080302752,3.92431823209095));
#41100=CARTESIAN_POINT('Ctrl Pts',(371.004357323081,-2.39981450007133,3.9293225343169));
#41101=CARTESIAN_POINT('Ctrl Pts',(370.888865721855,-2.4056806137964,3.93432037566845));
#41102=CARTESIAN_POINT('Ctrl Pts',(370.77299610641,-2.41154672752147,3.93422887912462));
#41103=CARTESIAN_POINT('Ctrl Pts',(370.657233386885,-2.41741284124654,3.92901133770078));
#41104=CARTESIAN_POINT('Ctrl Pts',(370.541589203678,-2.42327294830962,3.92379913882726));
#41105=CARTESIAN_POINT('Ctrl Pts',(370.426052108943,-2.42913305537271,3.91347135398659));
#41106=CARTESIAN_POINT('Ctrl Pts',(370.311108944468,-2.43499316243579,3.89804328321253));
#41107=CARTESIAN_POINT('Ctrl Pts',(370.192019112406,-2.44106467759895,3.88205863231204));
#41108=CARTESIAN_POINT('Ctrl Pts',(370.073567323926,-2.44713619276211,3.86059873453573));
#41109=CARTESIAN_POINT('Ctrl Pts',(369.956291821024,-2.45320770792527,3.83373959558801));
#41110=CARTESIAN_POINT('Ctrl Pts',(369.843229905495,-2.45906107983606,3.80784547768828));
#41111=CARTESIAN_POINT('Ctrl Pts',(369.731261641927,-2.46491445174686,3.77693352036053));
#41112=CARTESIAN_POINT('Ctrl Pts',(369.620860079267,-2.47076782365766,3.74112405980109));
#41113=CARTESIAN_POINT('Ctrl Pts',(369.510475090904,-2.47662031681705,3.70531997522223));
#41114=CARTESIAN_POINT('Ctrl Pts',(369.401656728655,-2.48247280997644,3.66461997679757));
#41115=CARTESIAN_POINT('Ctrl Pts',(369.294862665814,-2.48832530313584,3.61919420948306));
#41116=CARTESIAN_POINT('Ctrl Pts',(369.188058809529,-2.49417833299227,3.5737642764439));
#41117=CARTESIAN_POINT('Ctrl Pts',(369.08328000188,-2.50003136284871,3.52360787473349));
#41118=CARTESIAN_POINT('Ctrl Pts',(368.980963066482,-2.50588439270515,3.46894292753008));
#41119=CARTESIAN_POINT('Ctrl Pts',(368.878612004814,-2.5117393747514,3.41425974765814));
#41120=CARTESIAN_POINT('Ctrl Pts',(368.778724812357,-2.51759435679765,3.35506522671987));
#41121=CARTESIAN_POINT('Ctrl Pts',(368.681712259107,-2.52344933884391,3.29162242005026));
#41122=CARTESIAN_POINT('Ctrl Pts',(368.58458975315,-2.52931095684717,3.22810770816659));
#41123=CARTESIAN_POINT('Ctrl Pts',(368.490348735288,-2.53517257485043,3.16033532645054));
#41124=CARTESIAN_POINT('Ctrl Pts',(368.39936968424,-2.54103419285368,3.08861075798817));
#41125=CARTESIAN_POINT('Ctrl Pts',(368.3083292844,-2.54689976345022,3.01683782437362));
#41126=CARTESIAN_POINT('Ctrl Pts',(368.220555543304,-2.55276533404675,2.94110766656594));
#41127=CARTESIAN_POINT('Ctrl Pts',(368.136393336658,-2.55863090464328,2.86176384471411));
#41128=CARTESIAN_POINT('Ctrl Pts',(368.052108063965,-2.56450505216076,2.78230400248942));
#41129=CARTESIAN_POINT('Ctrl Pts',(367.971445151871,-2.57037919967823,2.69922024582023));
#41130=CARTESIAN_POINT('Ctrl Pts',(367.894710397421,-2.57625334719571,2.61289054607839));
#41131=CARTESIAN_POINT('Ctrl Pts',(367.875306514429,-2.57773874024766,2.59106039356829));
#41132=CARTESIAN_POINT('Ctrl Pts',(367.856153596938,-2.57922413329961,2.56902283554765));
#41133=CARTESIAN_POINT('Ctrl Pts',(367.837256150676,-2.58070952635156,2.54678427651789));
#41134=CARTESIAN_POINT('Ctrl Pts',(367.762976104771,-2.58654814933545,2.45937134449326));
#41135=CARTESIAN_POINT('Ctrl Pts',(367.692389725622,-2.59238677231935,2.3685483759452));
#41136=CARTESIAN_POINT('Ctrl Pts',(367.625829426242,-2.59822539530325,2.27466283521863));
#41137=CARTESIAN_POINT('Ctrl Pts',(367.559413871114,-2.60405132142248,2.18098146112644));
#41138=CARTESIAN_POINT('Ctrl Pts',(367.497007195303,-2.60987724754172,2.08425112139886));
#41139=CARTESIAN_POINT('Ctrl Pts',(367.43890221528,-2.61570317366095,1.9848530539077));
#41140=CARTESIAN_POINT('Ctrl Pts',(367.380853286225,-2.62152347980066,1.88555087076066));
#41141=CARTESIAN_POINT('Ctrl Pts',(367.327098015095,-2.62734378594036,1.78358643416845));
#41142=CARTESIAN_POINT('Ctrl Pts',(367.277886848885,-2.63316409208007,1.67937116545977));
#41143=CARTESIAN_POINT('Ctrl Pts',(367.228710852137,-2.63898023865493,1.57523037568008));
#41144=CARTESIAN_POINT('Ctrl Pts',(367.184072681692,-2.64479638522979,1.46884232958704));
#41145=CARTESIAN_POINT('Ctrl Pts',(367.144177225176,-2.65061253180465,1.36064365108106));
#41146=CARTESIAN_POINT('Ctrl Pts',(367.104035865337,-2.65646452731802,1.2517780692015));
#41147=CARTESIAN_POINT('Ctrl Pts',(367.068696089812,-2.66231652283139,1.14107983564306));
#41148=CARTESIAN_POINT('Ctrl Pts',(367.038317611231,-2.66816851834475,1.02901465625417));
#41149=CARTESIAN_POINT('Ctrl Pts',(367.00814066676,-2.67398169108727,0.917692929379906));
#41150=CARTESIAN_POINT('Ctrl Pts',(366.982859474865,-2.67979486382978,0.805022755356134));
#41151=CARTESIAN_POINT('Ctrl Pts',(366.962580390979,-2.6856080365723,0.691475251508002));
#41152=CARTESIAN_POINT('Ctrl Pts',(366.942098158934,-2.69147944347109,0.576790271899731));
#41153=CARTESIAN_POINT('Ctrl Pts',(366.926718911473,-2.69735085036988,0.461210711058661));
#41154=CARTESIAN_POINT('Ctrl Pts',(366.916498975035,-2.70322225726867,0.345230702143492));
#41155=CARTESIAN_POINT('Ctrl Pts',(366.906279038596,-2.70909366416747,0.22925069322832));
#41156=CARTESIAN_POINT('Ctrl Pts',(366.901218424583,-2.71496507106626,0.112870675986645));
#41157=CARTESIAN_POINT('Ctrl Pts',(366.901319334106,-2.72083647796505,-0.00341300685045548));
#41158=CARTESIAN_POINT('',(366.901317853728,-3.97083647799244,6.29929319774584E-5));
#41159=CARTESIAN_POINT('Ctrl Pts',(366.901319334107,-2.72083647799451,-0.00341300743396402));
#41160=CARTESIAN_POINT('Ctrl Pts',(366.901441265661,-2.7279310477181,-0.143921527762734));
#41161=CARTESIAN_POINT('Ctrl Pts',(366.909096556454,-2.73502561744168,-0.284100586580425));
#41162=CARTESIAN_POINT('Ctrl Pts',(366.924157040721,-2.74212018716526,-0.423239199940604));
#41163=CARTESIAN_POINT('Ctrl Pts',(366.939429079127,-2.74931441408195,-0.564332288935045));
#41164=CARTESIAN_POINT('Ctrl Pts',(366.96231575338,-2.75650864099864,-0.704355514953356));
#41165=CARTESIAN_POINT('Ctrl Pts',(366.992634451626,-2.76370286791533,-0.842589842028374));
#41166=CARTESIAN_POINT('Ctrl Pts',(367.01444037844,-2.76887712653129,-0.942011248410526));
#41167=CARTESIAN_POINT('Ctrl Pts',(367.040089742119,-2.77405138514725,-1.04050775981355));
#41168=CARTESIAN_POINT('Ctrl Pts',(367.069499460836,-2.77922564376321,-1.13781873439388));
#41169=CARTESIAN_POINT('Ctrl Pts',(367.102884652554,-2.78509933529881,-1.24828376719106));
#41170=CARTESIAN_POINT('Ctrl Pts',(367.141191364605,-2.79097302683441,-1.35746218040211));
#41171=CARTESIAN_POINT('Ctrl Pts',(367.184303170996,-2.79684671837001,-1.46488286887288));
#41172=CARTESIAN_POINT('Ctrl Pts',(367.227359316144,-2.80271282643851,-1.57216486751786));
#41173=CARTESIAN_POINT('Ctrl Pts',(367.275208065812,-2.80857893450702,-1.67769327456226));
#41174=CARTESIAN_POINT('Ctrl Pts',(367.327682967674,-2.81444504257553,-1.78101116769307));
#41175=CARTESIAN_POINT('Ctrl Pts',(367.38010413606,-2.82030514384128,-1.88422326492003));
#41176=CARTESIAN_POINT('Ctrl Pts',(367.437141848167,-2.82616524510703,-1.98522898441801));
#41177=CARTESIAN_POINT('Ctrl Pts',(367.498581472885,-2.83202534637278,-2.08359108293439));
#41178=CARTESIAN_POINT('Ctrl Pts',(367.562237666942,-2.8380968636562,-2.18550181008616));
#41179=CARTESIAN_POINT('Ctrl Pts',(367.63061921938,-2.84416838093962,-2.28457414684417));
#41180=CARTESIAN_POINT('Ctrl Pts',(367.703435001426,-2.85023989822305,-2.3803490433799));
#41181=CARTESIAN_POINT('Ctrl Pts',(367.773634490001,-2.85609326402086,-2.47268271839094));
#41182=CARTESIAN_POINT('Ctrl Pts',(367.847954774005,-2.86194662981867,-2.56195147426968));
#41183=CARTESIAN_POINT('Ctrl Pts',(367.926091211913,-2.86779999561648,-2.64777393347103));
#41184=CARTESIAN_POINT('Ctrl Pts',(368.004215917966,-2.87365248255626,-2.7335835067944));
#41185=CARTESIAN_POINT('Ctrl Pts',(368.086155360562,-2.87950496949605,-2.81594750690446));
#41186=CARTESIAN_POINT('Ctrl Pts',(368.171565856825,-2.88535745643583,-2.89451909747916));
#41187=CARTESIAN_POINT('Ctrl Pts',(368.256984184116,-2.89121047997231,-2.97309789204371));
#41188=CARTESIAN_POINT('Ctrl Pts',(368.345873893653,-2.8970635035088,-3.0478833061231));
#41189=CARTESIAN_POINT('Ctrl Pts',(368.43785636777,-2.90291652704529,-3.11856719484054));
#41190=CARTESIAN_POINT('Ctrl Pts',(368.529869519808,-2.90877150267747,-3.18927465799169));
#41191=CARTESIAN_POINT('Ctrl Pts',(368.624977160095,-2.91462647830966,-3.25587762409626));
#41192=CARTESIAN_POINT('Ctrl Pts',(368.722770292194,-2.92048145394185,-3.31811029013596));
#41193=CARTESIAN_POINT('Ctrl Pts',(368.820674260018,-2.9263430654232,-3.38041348876383));
#41194=CARTESIAN_POINT('Ctrl Pts',(368.921269445856,-2.93220467690455,-3.43833627917756));
#41195=CARTESIAN_POINT('Ctrl Pts',(369.024120685343,-2.9380662883859,-3.49165794621909));
#41196=CARTESIAN_POINT('Ctrl Pts',(369.127041278082,-2.94393185238961,-3.54501556840394));
#41197=CARTESIAN_POINT('Ctrl Pts',(369.232220579747,-2.94979741639331,-3.59376571601081));
#41198=CARTESIAN_POINT('Ctrl Pts',(369.33920341154,-2.95566298039701,-3.63773580765107));
#41199=CARTESIAN_POINT('Ctrl Pts',(369.446342678002,-2.96153712126816,-3.68177019415657));
#41200=CARTESIAN_POINT('Ctrl Pts',(369.555290350564,-2.9674112621393,-3.72101043576224));
#41201=CARTESIAN_POINT('Ctrl Pts',(369.665576008652,-2.97328540301044,-3.7553337402616));
#41202=CARTESIAN_POINT('Ctrl Pts',(369.693465045456,-2.97477085573192,-3.76401341737478));
#41203=CARTESIAN_POINT('Ctrl Pts',(369.721439595303,-2.9762563084534,-3.77237892036187));
#41204=CARTESIAN_POINT('Ctrl Pts',(369.749491964837,-2.97774176117488,-3.78042878413089));
#41205=CARTESIAN_POINT('Ctrl Pts',(369.860414998906,-2.98361545119011,-3.81225908324459));
#41206=CARTESIAN_POINT('Ctrl Pts',(369.972924879248,-2.98948914120535,-3.83925630424393));
#41207=CARTESIAN_POINT('Ctrl Pts',(370.08656261712,-2.99536283122058,-3.86126289015381));
#41208=CARTESIAN_POINT('Ctrl Pts',(370.200053638318,-3.0012289377668,-3.8832410635561));
#41209=CARTESIAN_POINT('Ctrl Pts',(370.314669219303,-3.00709504431303,-3.90024133777752));
#41210=CARTESIAN_POINT('Ctrl Pts',(370.429935169522,-3.01296115085926,-3.91215588200705));
#41211=CARTESIAN_POINT('Ctrl Pts',(370.545083089184,-3.01882125060272,-3.92405822592678));
#41212=CARTESIAN_POINT('Ctrl Pts',(370.6608796449,-3.02468135034618,-3.93088515619367));
#41213=CARTESIAN_POINT('Ctrl Pts',(370.776841064394,-3.03054145008965,-3.93257999521253));
#41214=CARTESIAN_POINT('Ctrl Pts',(370.896986089165,-3.03661296794368,-3.93433597989082));
#41215=CARTESIAN_POINT('Ctrl Pts',(371.01730765464,-3.04268448579772,-3.93058248923657));
#41216=CARTESIAN_POINT('Ctrl Pts',(371.137262193632,-3.04875600365176,-3.92131530568698));
#41217=CARTESIAN_POINT('Ctrl Pts',(371.252906688351,-3.05460936793719,-3.91238109804404));
#41218=CARTESIAN_POINT('Ctrl Pts',(371.368209630447,-3.06046273222263,-3.89832263430311));
#41219=CARTESIAN_POINT('Ctrl Pts',(371.482685396514,-3.06631609650807,-3.87918915867836));
#41220=CARTESIAN_POINT('Ctrl Pts',(371.597143974651,-3.07216858194181,-3.86005855584379));
#41221=CARTESIAN_POINT('Ctrl Pts',(371.710775216324,-3.07802106737556,-3.8358545243301));
#41222=CARTESIAN_POINT('Ctrl Pts',(371.8231013587,-3.0838735528093,-3.80667784023));
#41223=CARTESIAN_POINT('Ctrl Pts',(371.935437800075,-3.08972657484777,-3.77749848096794));
#41224=CARTESIAN_POINT('Ctrl Pts',(372.046468504377,-3.09557959688623,-3.74334566663788));
#41225=CARTESIAN_POINT('Ctrl Pts',(372.155729283017,-3.10143261892469,-3.70437050431128));
#41226=CARTESIAN_POINT('Ctrl Pts',(372.265026502415,-3.10728759306855,-3.66538234295201));
#41227=CARTESIAN_POINT('Ctrl Pts',(372.372552233433,-3.11314256721241,-3.62156877418964));
#41228=CARTESIAN_POINT('Ctrl Pts',(372.47786139906,-3.11899754135627,-3.57312938653809));
#41229=CARTESIAN_POINT('Ctrl Pts',(372.58328991928,-3.12485915137134,-3.52463509897922));
#41230=CARTESIAN_POINT('Ctrl Pts',(372.686496484367,-3.13072076138641,-3.47150470100279));
#41231=CARTESIAN_POINT('Ctrl Pts',(372.787059719113,-3.13658237140148,-3.4139842127936));
#41232=CARTESIAN_POINT('Ctrl Pts',(372.887690764503,-3.14244793394998,-3.35642493803053));
#41233=CARTESIAN_POINT('Ctrl Pts',(372.985674582027,-3.14831349649848,-3.29446989871987));
#41234=CARTESIAN_POINT('Ctrl Pts',(373.08061939366,-3.15417905904698,-3.22840802709887));
#41235=CARTESIAN_POINT('Ctrl Pts',(373.175703037956,-3.16005319849043,-3.16224955677507));
#41236=CARTESIAN_POINT('Ctrl Pts',(373.267738480606,-3.16592733793389,-3.09197251904274));
#41237=CARTESIAN_POINT('Ctrl Pts',(373.356367519119,-3.17180147737734,-3.01790564510519));
#41238=CARTESIAN_POINT('Ctrl Pts',(373.37878025198,-3.17328694444707,-2.99917542883248));
#41239=CARTESIAN_POINT('Ctrl Pts',(373.40097533511,-3.1747724115168,-2.98020303382209));
#41240=CARTESIAN_POINT('Ctrl Pts',(373.422947366583,-3.17625787858653,-2.96099413078909));
#41241=CARTESIAN_POINT('Ctrl Pts',(373.509827023923,-3.18213156715133,-2.88504016561103));
#41242=CARTESIAN_POINT('Ctrl Pts',(373.593505655049,-3.18800525571613,-2.8051327049278));
#41243=CARTESIAN_POINT('Ctrl Pts',(373.673602041439,-3.19387894428093,-2.72157202707445));
#41244=CARTESIAN_POINT('Ctrl Pts',(373.753595015685,-3.19974504934853,-2.63811923409786));
#41245=CARTESIAN_POINT('Ctrl Pts',(373.830014659571,-3.20561115441613,-2.55102289936201));
#41246=CARTESIAN_POINT('Ctrl Pts',(373.902513298785,-3.21147725948372,-2.46062303245315));
#41247=CARTESIAN_POINT('Ctrl Pts',(373.974937700166,-3.21733735772231,-2.37031573404369));
#41248=CARTESIAN_POINT('Ctrl Pts',(374.043448826235,-3.22319745596089,-2.27671195247972));
#41249=CARTESIAN_POINT('Ctrl Pts',(374.107736792764,-3.22905755419947,-2.18018747961318));
#41250=CARTESIAN_POINT('Ctrl Pts',(374.174344135562,-3.23512907260775,-2.08018060430173));
#41251=CARTESIAN_POINT('Ctrl Pts',(374.236417527231,-3.24120059101603,-1.97703863982467));
#41252=CARTESIAN_POINT('Ctrl Pts',(374.293658750397,-3.24727210942431,-1.87121606372578));
#41253=CARTESIAN_POINT('Ctrl Pts',(374.348843239589,-3.25312547214878,-1.76919579783982));
#41254=CARTESIAN_POINT('Ctrl Pts',(374.399536619953,-3.25897883487324,-1.6646846337297));
#41255=CARTESIAN_POINT('Ctrl Pts',(374.44551701066,-3.26483219759771,-1.55811734003903));
#41256=CARTESIAN_POINT('Ctrl Pts',(374.491490497511,-3.27068468145237,-1.45156604719793));
#41257=CARTESIAN_POINT('Ctrl Pts',(374.532752238139,-3.27653716530704,-1.34295961787381));
#41258=CARTESIAN_POINT('Ctrl Pts',(374.56912791564,-3.2823896491617,-1.23275415135092));
#41259=CARTESIAN_POINT('Ctrl Pts',(374.605506928266,-3.28824266960461,-1.12253858057844));
#41260=CARTESIAN_POINT('Ctrl Pts',(374.636998857715,-3.29409569004751,-1.0107240735106));
#41261=CARTESIAN_POINT('Ctrl Pts',(374.663479039322,-3.29994871049042,-0.897782607807121));
#41262=CARTESIAN_POINT('Ctrl Pts',(374.689968052559,-3.30580368302387,-0.784803474036556));
#41263=CARTESIAN_POINT('Ctrl Pts',(374.711441899971,-3.31165865555731,-0.670697036266607));
#41264=CARTESIAN_POINT('Ctrl Pts',(374.727827016793,-3.31751362809076,-0.555945494812407));
#41265=CARTESIAN_POINT('Ctrl Pts',(374.744230704035,-3.32337523648144,-0.44106389726611));
#41266=CARTESIAN_POINT('Ctrl Pts',(374.755534090831,-3.32923684487212,-0.325536145945799));
#41267=CARTESIAN_POINT('Ctrl Pts',(374.761715478285,-3.33509845326281,-0.209849695415509));
#41268=CARTESIAN_POINT('Ctrl Pts',(374.767901033892,-3.34096401417679,-0.0940852367072996));
#41269=CARTESIAN_POINT('Ctrl Pts',(374.768957709119,-3.34682957509076,0.0218377221899005));
#41270=CARTESIAN_POINT('Ctrl Pts',(374.764915909321,-3.35269513600474,0.137433334413964));
#41271=CARTESIAN_POINT('Ctrl Pts',(374.760868199417,-3.35856927381135,0.253197975852862));
#41272=CARTESIAN_POINT('Ctrl Pts',(374.751707168292,-3.36444341161797,0.368633905063984));
#41273=CARTESIAN_POINT('Ctrl Pts',(374.737514866301,-3.37031754942459,0.483261913567972));
#41274=CARTESIAN_POINT('Ctrl Pts',(374.733925843954,-3.37180303161579,0.51224963412393));
#41275=CARTESIAN_POINT('Ctrl Pts',(374.730015320347,-3.37328851380699,0.541185748295071));
#41276=CARTESIAN_POINT('Ctrl Pts',(374.725785132249,-3.37477399599819,0.570062642416895));
#41277=CARTESIAN_POINT('Ctrl Pts',(374.709058703409,-3.38064768567527,0.684243691448876));
#41278=CARTESIAN_POINT('Ctrl Pts',(374.687274812471,-3.38652137535235,0.797878119513533));
#41279=CARTESIAN_POINT('Ctrl Pts',(374.660479123692,-3.39239506502944,0.910482801800082));
#41280=CARTESIAN_POINT('Ctrl Pts',(374.633718030649,-3.39826117122451,1.02294210092382));
#41281=CARTESIAN_POINT('Ctrl Pts',(374.601958102632,-3.40412727741957,1.13437389995395));
#41282=CARTESIAN_POINT('Ctrl Pts',(374.565296575013,-3.40999338361464,1.24430172287687));
#41283=CARTESIAN_POINT('Ctrl Pts',(374.528672588315,-3.41585348299443,1.35411698116069));
#41284=CARTESIAN_POINT('Ctrl Pts',(374.487157115496,-3.42171358237422,1.46243093703371));
#41285=CARTESIAN_POINT('Ctrl Pts',(374.440897946408,-3.427573681754,1.56877947189834));
#41286=CARTESIAN_POINT('Ctrl Pts',(374.392969855275,-3.43364519973966,1.6789648118273));
#41287=CARTESIAN_POINT('Ctrl Pts',(374.339949427173,-3.43971671772532,1.78703979826832));
#41288=CARTESIAN_POINT('Ctrl Pts',(374.2820568967,-3.44578823571098,1.89250746051153));
#41289=CARTESIAN_POINT('Ctrl Pts',(374.226244487294,-3.45164159960368,1.99418559231968));
#41290=CARTESIAN_POINT('Ctrl Pts',(374.165904282349,-3.45749496349637,2.09344014831928));
#41291=CARTESIAN_POINT('Ctrl Pts',(374.101281337829,-3.46334832738907,2.18984898800324));
#41292=CARTESIAN_POINT('Ctrl Pts',(374.036668096214,-3.46920081241996,2.28624335224225));
#41293=CARTESIAN_POINT('Ctrl Pts',(373.967773623597,-3.47505329745085,2.37979250665876));
#41294=CARTESIAN_POINT('Ctrl Pts',(373.894886685096,-3.48090578248174,2.4701027155506));
#41295=CARTESIAN_POINT('Ctrl Pts',(373.821993063834,-3.48675880410763,2.56042120468677));
#41296=CARTESIAN_POINT('Ctrl Pts',(373.74510650849,-3.49261182573351,2.64749983643588));
#41297=CARTESIAN_POINT('Ctrl Pts',(373.66455604385,-3.4984648473594,2.73097799044945));
#41298=CARTESIAN_POINT('Ctrl Pts',(373.583978714072,-3.50431982108134,2.81448398604389));
#41299=CARTESIAN_POINT('Ctrl Pts',(373.499735331858,-3.51017479480327,2.8943868189638));
#41300=CARTESIAN_POINT('Ctrl Pts',(373.412191213912,-3.51602976852521,2.97036326671578));
#41301=CARTESIAN_POINT('Ctrl Pts',(373.324547875972,-3.52189137810657,3.04642582399623));
#41302=CARTESIAN_POINT('Ctrl Pts',(373.233596647768,-3.52775298768792,3.11855284312599));
#41303=CARTESIAN_POINT('Ctrl Pts',(373.139735378167,-3.53361459726928,3.18646183653393));
#41304=CARTESIAN_POINT('Ctrl Pts',(373.045810817228,-3.53948015937665,3.25441662147055));
#41305=CARTESIAN_POINT('Ctrl Pts',(372.948972651852,-3.54534572148402,3.31814749059889));
#41306=CARTESIAN_POINT('Ctrl Pts',(372.849645626147,-3.5512112835914,3.37741661150713));
#41307=CARTESIAN_POINT('Ctrl Pts',(372.75017336002,-3.55708542258622,3.43677239837674));
#41308=CARTESIAN_POINT('Ctrl Pts',(372.64820533279,-3.56295956158103,3.49165322137719));
#41309=CARTESIAN_POINT('Ctrl Pts',(372.544188707529,-3.56883370057585,3.54186824452851));
#41310=CARTESIAN_POINT('Ctrl Pts',(372.517884652632,-3.57031917152052,3.55456677923165));
#41311=CARTESIAN_POINT('Ctrl Pts',(372.491449676109,-3.57180464246518,3.56696718210122));
#41312=CARTESIAN_POINT('Ctrl Pts',(372.464891171338,-3.57329011340984,3.57906686920676));
#41313=CARTESIAN_POINT('Ctrl Pts',(372.359876388396,-3.5791638028427,3.62691015052314));
#41314=CARTESIAN_POINT('Ctrl Pts',(372.252579237115,-3.58503749227556,3.67020727878392));
#41315=CARTESIAN_POINT('Ctrl Pts',(372.143430446049,-3.59091118170843,3.70873471945731));
#41316=CARTESIAN_POINT('Ctrl Pts',(372.034422576298,-3.59677728765789,3.74721241759496));
#41317=CARTESIAN_POINT('Ctrl Pts',(371.923568206989,-3.60264339360736,3.78093253835325));
#41318=CARTESIAN_POINT('Ctrl Pts',(371.811320436833,-3.60850949955683,3.80971848718799));
#41319=CARTESIAN_POINT('Ctrl Pts',(371.699187606936,-3.61436959868993,3.8384749595847));
#41320=CARTESIAN_POINT('Ctrl Pts',(371.585664612081,-3.62022969782304,3.86230720793486));
#41321=CARTESIAN_POINT('Ctrl Pts',(371.471221573008,-3.62608979695614,3.88108781808982));
#41322=CARTESIAN_POINT('Ctrl Pts',(371.352649691404,-3.63216131503386,3.90054598961159));
#41323=CARTESIAN_POINT('Ctrl Pts',(371.233090551928,-3.63823283311159,3.91458098755772));
#41324=CARTESIAN_POINT('Ctrl Pts',(371.113081154288,-3.64430435118931,3.92310846421301));
#41325=CARTESIAN_POINT('Ctrl Pts',(370.99738378895,-3.65015771483424,3.93132954190695));
#41326=CARTESIAN_POINT('Ctrl Pts',(370.8812684123,-3.65601107847918,3.93443203439467));
#41327=CARTESIAN_POINT('Ctrl Pts',(370.765222599452,-3.66186444212412,3.93239301773184));
#41328=CARTESIAN_POINT('Ctrl Pts',(370.64919421047,-3.66771692690728,3.93035430722012));
#41329=CARTESIAN_POINT('Ctrl Pts',(370.533235777493,-3.67356941169044,3.92317562979895));
#41330=CARTESIAN_POINT('Ctrl Pts',(370.417834702004,-3.67942189647361,3.91088618918392));
#41331=CARTESIAN_POINT('Ctrl Pts',(370.302423045765,-3.68527491785206,3.89859562179005));
#41332=CARTESIAN_POINT('Ctrl Pts',(370.187569259445,-3.69112793923052,3.8811934034429));
#41333=CARTESIAN_POINT('Ctrl Pts',(370.073754742584,-3.69698096060898,3.85876052052131));
#41334=CARTESIAN_POINT('Ctrl Pts',(369.959902266366,-3.70283593408407,3.83632015579633));
#41335=CARTESIAN_POINT('Ctrl Pts',(369.847090153966,-3.70869090755916,3.80884587006832));
#41336=CARTESIAN_POINT('Ctrl Pts',(369.735788053409,-3.71454588103425,3.77646941983088));
#41337=CARTESIAN_POINT('Ctrl Pts',(369.624359806195,-3.72040749037086,3.74405627503945));
#41338=CARTESIAN_POINT('Ctrl Pts',(369.514445383608,-3.72626909970748,3.70672999180798));
#41339=CARTESIAN_POINT('Ctrl Pts',(369.406497839792,-3.73213070904409,3.66467174645196));
#41340=CARTESIAN_POINT('Ctrl Pts',(369.298477506141,-3.73799627090767,3.62258514090692));
#41341=CARTESIAN_POINT('Ctrl Pts',(369.192427069188,-3.74386183277124,3.57576038611358));
#41342=CARTESIAN_POINT('Ctrl Pts',(369.088776639164,-3.74972739463482,3.52442546665648));
#41343=CARTESIAN_POINT('Ctrl Pts',(368.984974646777,-3.75560153338908,3.47301548295103));
#41344=CARTESIAN_POINT('Ctrl Pts',(368.88358002556,-3.76147567214334,3.41708237147469));
#41345=CARTESIAN_POINT('Ctrl Pts',(368.7849955478,-3.7673498108976,3.35689843285317));
#41346=CARTESIAN_POINT('Ctrl Pts',(368.760065150951,-3.76883528420557,3.34167890227506));
#41347=CARTESIAN_POINT('Ctrl Pts',(368.735314303328,-3.77032075751353,3.32618773625792));
#41348=CARTESIAN_POINT('Ctrl Pts',(368.710749184282,-3.7718062308215,3.31042974676844));
#41349=CARTESIAN_POINT('Ctrl Pts',(368.613616589462,-3.77767992012328,3.2481213001706));
#41350=CARTESIAN_POINT('Ctrl Pts',(368.519066868909,-3.78355360942506,3.18143044890821));
#41351=CARTESIAN_POINT('Ctrl Pts',(368.427521362484,-3.78942729872684,3.11059795733275));
#41352=CARTESIAN_POINT('Ctrl Pts',(368.336094049932,-3.79529340454241,3.03985691717658));
#41353=CARTESIAN_POINT('Ctrl Pts',(368.247663561768,-3.80115951035798,2.96498512114459));
#41354=CARTESIAN_POINT('Ctrl Pts',(368.162623920894,-3.80702561617355,2.88626757802382));
#41355=CARTESIAN_POINT('Ctrl Pts',(368.077671359549,-3.81288571517012,2.80763064068279));
#41356=CARTESIAN_POINT('Ctrl Pts',(367.996103040416,-3.8187458141667,2.72515606823728));
#41357=CARTESIAN_POINT('Ctrl Pts',(367.918280887532,-3.82460591316327,2.63916983438361));
#41358=CARTESIAN_POINT('Ctrl Pts',(367.837651087206,-3.83067743129119,2.55008141149203));
#41359=CARTESIAN_POINT('Ctrl Pts',(367.761043220298,-3.8367489494191,2.45722343393455));
#41360=CARTESIAN_POINT('Ctrl Pts',(367.688819277542,-3.84282046754701,2.36100142108893));
#41361=CARTESIAN_POINT('Ctrl Pts',(367.619190400276,-3.84867383104969,2.26823674407078));
#41362=CARTESIAN_POINT('Ctrl Pts',(367.553636102176,-3.85452719455238,2.17234597521138));
#41363=CARTESIAN_POINT('Ctrl Pts',(367.492439965521,-3.86038055805506,2.07372640039124));
#41364=CARTESIAN_POINT('Ctrl Pts',(367.431253017268,-3.8662330426941,1.97512163298217));
#41365=CARTESIAN_POINT('Ctrl Pts',(367.374423147118,-3.87208552733313,1.87378922524824));
#41366=CARTESIAN_POINT('Ctrl Pts',(367.322190039943,-3.87793801197217,1.77015457606821));
#41367=CARTESIAN_POINT('Ctrl Pts',(367.269952143699,-3.88379103320477,1.66651042499457));
#41368=CARTESIAN_POINT('Ctrl Pts',(367.222312034212,-3.88964405443738,1.56056398181326));
#41369=CARTESIAN_POINT('Ctrl Pts',(367.179462629267,-3.89549707566998,1.45276367379992));
#41370=CARTESIAN_POINT('Ctrl Pts',(367.136598933222,-3.90135204899762,1.34492741231271));
#41371=CARTESIAN_POINT('Ctrl Pts',(367.098529271382,-3.90720702232526,1.23523644025223));
#41372=CARTESIAN_POINT('Ctrl Pts',(367.065397528396,-3.9130619956529,1.1241568329647));
#41373=CARTESIAN_POINT('Ctrl Pts',(367.032228234837,-3.91892360484046,1.01295133121557));
#41374=CARTESIAN_POINT('Ctrl Pts',(367.004008148557,-3.92478521402803,0.900354449080872));
#41375=CARTESIAN_POINT('Ctrl Pts',(366.980830630642,-3.93064682321559,0.786845108896487));
#41376=CARTESIAN_POINT('Ctrl Pts',(366.957637483957,-3.93651238492899,0.67325922853615));
#41377=CARTESIAN_POINT('Ctrl Pts',(366.939493740771,-3.94237794664238,0.558760072016698));
#41378=CARTESIAN_POINT('Ctrl Pts',(366.926440990701,-3.94824350835577,0.443832656930772));
#41379=CARTESIAN_POINT('Ctrl Pts',(366.913369154308,-3.95411764695937,0.328737189769056));
#41380=CARTESIAN_POINT('Ctrl Pts',(366.905403196255,-3.95999178556298,0.213212624846767));
#41381=CARTESIAN_POINT('Ctrl Pts',(366.902532646884,-3.96586592416658,0.0977450316198287));
#41382=CARTESIAN_POINT('Ctrl Pts',(366.901806731355,-3.96735139885544,0.0685451439943927));
#41383=CARTESIAN_POINT('Ctrl Pts',(366.901406409168,-3.96883687354429,0.0393488768402862));
#41384=CARTESIAN_POINT('Ctrl Pts',(366.901330986672,-3.97032234823315,0.0101640313479354));
#41385=CARTESIAN_POINT('Ctrl Pts',(366.901322285313,-3.97049372481045,0.00679702754295266));
#41386=CARTESIAN_POINT('Ctrl Pts',(366.901317907657,-3.97066510138775,0.00343001255941355));
#41387=CARTESIAN_POINT('Ctrl Pts',(366.901317853728,-3.97083647796505,6.29934700403027E-5));
#41388=CARTESIAN_POINT('',(366.901319301027,-5.22083647793354,0.00337467329664299));
#41389=CARTESIAN_POINT('Ctrl Pts',(366.901317853728,-3.97083647799244,6.29929319748385E-5));
#41390=CARTESIAN_POINT('Ctrl Pts',(366.901316006288,-3.97670742792183,-0.115282994231212));
#41391=CARTESIAN_POINT('Ctrl Pts',(366.906392714759,-3.98257837785123,-0.230822054784923));
#41392=CARTESIAN_POINT('Ctrl Pts',(366.916573017939,-3.98844932778063,-0.346069943216802));
#41393=CARTESIAN_POINT('Ctrl Pts',(366.926740174846,-3.99431269629403,-0.461169006978742));
#41394=CARTESIAN_POINT('Ctrl Pts',(366.941997784334,-4.00017606480742,-0.575977238150028));
#41395=CARTESIAN_POINT('Ctrl Pts',(366.962318895233,-4.00603943332082,-0.690009470453848));
#41396=CARTESIAN_POINT('Ctrl Pts',(366.98261920661,-4.01189680042706,-0.803924985916004));
#41397=CARTESIAN_POINT('Ctrl Pts',(367.007972638632,-4.01775416753331,-0.917065677602088));
#41398=CARTESIAN_POINT('Ctrl Pts',(367.038300426437,-4.02361153463955,-1.0289512600367));
#41399=CARTESIAN_POINT('Ctrl Pts',(367.069631422851,-4.02966265676477,-1.14453788984538));
#41400=CARTESIAN_POINT('Ctrl Pts',(367.106271543185,-4.03571377888999,-1.25878448561143));
#41401=CARTESIAN_POINT('Ctrl Pts',(367.148076468894,-4.04176490101521,-1.37117229276752));
#41402=CARTESIAN_POINT('Ctrl Pts',(367.188496474471,-4.04761556061815,-1.47983689903133));
#41403=CARTESIAN_POINT('Ctrl Pts',(367.233744340121,-4.05346622022109,-1.58676350770212));
#41404=CARTESIAN_POINT('Ctrl Pts',(367.283639118081,-4.05931687982403,-1.69149919296599));
#41405=CARTESIAN_POINT('Ctrl Pts',(367.333526485669,-4.06516667048694,-1.79621932288472));
#41406=CARTESIAN_POINT('Ctrl Pts',(367.38805921546,-4.07101646114985,-1.89874880311661));
#41407=CARTESIAN_POINT('Ctrl Pts',(367.447008987533,-4.07686625181276,-1.99865646082808));
#41408=CARTESIAN_POINT('Ctrl Pts',(367.505964297075,-4.08271659197805,-2.09857350340442));
#41409=CARTESIAN_POINT('Ctrl Pts',(367.569337263499,-4.08856693214333,-2.19586787767364));
#41410=CARTESIAN_POINT('Ctrl Pts',(367.636854926471,-4.09441727230861,-2.29013533050827));
#41411=CARTESIAN_POINT('Ctrl Pts',(367.704395301767,-4.10026958047482,-2.38443449405184));
#41412=CARTESIAN_POINT('Ctrl Pts',(367.776082905224,-4.10612188864103,-2.47570437546677));
#41413=CARTESIAN_POINT('Ctrl Pts',(367.851603443936,-4.11197419680724,-2.56357245901625));
#41414=CARTESIAN_POINT('Ctrl Pts',(367.927209624855,-4.11783314163933,-2.65154018720096));
#41415=CARTESIAN_POINT('Ctrl Pts',(368.006657146676,-4.12369208647142,-2.73609810417007));
#41416=CARTESIAN_POINT('Ctrl Pts',(368.08959362769,-4.12955103130351,-2.81690928603809));
#41417=CARTESIAN_POINT('Ctrl Pts',(368.172586341101,-4.13541394860355,-2.89777525931286));
#41418=CARTESIAN_POINT('Ctrl Pts',(368.259072416014,-4.14127686590358,-2.97488916474135));
#41419=CARTESIAN_POINT('Ctrl Pts',(368.348666392974,-4.14713978320362,-3.0479543661541));
#41420=CARTESIAN_POINT('Ctrl Pts',(368.438390871182,-4.15301124034136,-3.12112599324715));
#41421=CARTESIAN_POINT('Ctrl Pts',(368.531231955111,-4.15888269747911,-3.19023690154316));
#41422=CARTESIAN_POINT('Ctrl Pts',(368.626775215789,-4.16475415461685,-3.25503371778361));
#41423=CARTESIAN_POINT('Ctrl Pts',(368.648929193589,-4.16611559162617,-3.27005840103452));
#41424=CARTESIAN_POINT('Ctrl Pts',(368.671228352797,-4.16747702863549,-3.28485133119991));
#41425=CARTESIAN_POINT('Ctrl Pts',(368.693667350086,-4.16883846564481,-3.29940970832898));
#41426=CARTESIAN_POINT('Ctrl Pts',(368.79047660343,-4.1747121550369,-3.362219360721));
#41427=CARTESIAN_POINT('Ctrl Pts',(368.890213818182,-4.18058584442899,-3.42086923500305));
#41428=CARTESIAN_POINT('Ctrl Pts',(368.992485948426,-4.18645953382108,-3.47507470919244));
#41429=CARTESIAN_POINT('Ctrl Pts',(369.094626035744,-4.19232563972848,-3.52921019902339));
#41430=CARTESIAN_POINT('Ctrl Pts',(369.199294168293,-4.19819174563587,-3.57891250832711));
#41431=CARTESIAN_POINT('Ctrl Pts',(369.306068251032,-4.20405785154327,-3.6239401420828));
#41432=CARTESIAN_POINT('Ctrl Pts',(369.412732998472,-4.20991795063308,-3.66892166811612));
#41433=CARTESIAN_POINT('Ctrl Pts',(369.521499028297,-4.21577804972288,-3.70923788037747));
#41434=CARTESIAN_POINT('Ctrl Pts',(369.63192015551,-4.22163814881268,-3.74469341555927));
#41435=CARTESIAN_POINT('Ctrl Pts',(369.746325025037,-4.22770966690618,-3.78142810554859));
#41436=CARTESIAN_POINT('Ctrl Pts',(369.862506271927,-4.23378118499967,-3.81294456082516));
#41437=CARTESIAN_POINT('Ctrl Pts',(369.979945211424,-4.23985270309316,-3.83908014880446));
#41438=CARTESIAN_POINT('Ctrl Pts',(370.093164476022,-4.24570606669193,-3.86427666423187));
#41439=CARTESIAN_POINT('Ctrl Pts',(370.207552170995,-4.2515594302907,-3.8844722379831));
#41440=CARTESIAN_POINT('Ctrl Pts',(370.322629435589,-4.25741279388947,-3.89957227952731));
#41441=CARTESIAN_POINT('Ctrl Pts',(370.43768942172,-4.26326527862549,-3.91467005385136));
#41442=CARTESIAN_POINT('Ctrl Pts',(370.553438362077,-4.26911776336151,-3.92467376349243));
#41443=CARTESIAN_POINT('Ctrl Pts',(370.669389878806,-4.27497024809754,-3.92954040102077));
#41444=CARTESIAN_POINT('Ctrl Pts',(370.785352026734,-4.28082326942793,-3.93440748475452));
#41445=CARTESIAN_POINT('Ctrl Pts',(370.901516375152,-4.28667629075833,-3.93413654274441));
#41446=CARTESIAN_POINT('Ctrl Pts',(371.017394844555,-4.29252931208872,-3.92873666911454));
#41447=CARTESIAN_POINT('Ctrl Pts',(371.133311961667,-4.29838428551486,-3.92333499452244));
#41448=CARTESIAN_POINT('Ctrl Pts',(371.248942597698,-4.30423925894099,-3.91280100608419));
#41449=CARTESIAN_POINT('Ctrl Pts',(371.363802807532,-4.31009423236713,-3.89719574606688));
#41450=CARTESIAN_POINT('Ctrl Pts',(371.478793196663,-4.31595584165372,-3.88157279949143));
#41451=CARTESIAN_POINT('Ctrl Pts',(371.593011007171,-4.32181745094032,-3.8608671650547));
#41452=CARTESIAN_POINT('Ctrl Pts',(371.705981416894,-4.32767906022691,-3.83519121189154));
#41453=CARTESIAN_POINT('Ctrl Pts',(371.819028003395,-4.33354462203976,-3.8094979452443));
#41454=CARTESIAN_POINT('Ctrl Pts',(371.930825116793,-4.33941018385262,-3.77882779527807));
#41455=CARTESIAN_POINT('Ctrl Pts',(372.040913723662,-4.34527574566547,-3.74334281163796));
#41456=CARTESIAN_POINT('Ctrl Pts',(372.151163307077,-4.35114988436842,-3.7078059402479));
#41457=CARTESIAN_POINT('Ctrl Pts',(372.25969901233,-4.35702402307136,-3.66744032764205));
#41458=CARTESIAN_POINT('Ctrl Pts',(372.366082308297,-4.36289816177431,-3.6224558871262));
#41459=CARTESIAN_POINT('Ctrl Pts',(372.392984906742,-4.36438363553503,-3.61108005665875));
#41460=CARTESIAN_POINT('Ctrl Pts',(372.419749985999,-4.36586910929575,-3.59940907819492));
#41461=CARTESIAN_POINT('Ctrl Pts',(372.446370724537,-4.36735458305647,-3.58744679961806));
#41462=CARTESIAN_POINT('Ctrl Pts',(372.55163138508,-4.37322827243772,-3.54014693440975));
#41463=CARTESIAN_POINT('Ctrl Pts',(372.65498382718,-4.37910196181898,-3.48813162499369));
#41464=CARTESIAN_POINT('Ctrl Pts',(372.755975806822,-4.38497565120024,-3.43157685465061));
#41465=CARTESIAN_POINT('Ctrl Pts',(372.856837396328,-4.39084175709653,-3.37509510183072));
#41466=CARTESIAN_POINT('Ctrl Pts',(372.955344226832,-4.39670786299282,-3.31408574345218));
#41467=CARTESIAN_POINT('Ctrl Pts',(373.051064546437,-4.40257396888911,-3.24877255253882));
#41468=CARTESIAN_POINT('Ctrl Pts',(373.146686849652,-4.40843406796754,-3.1835262415027));
#41469=CARTESIAN_POINT('Ctrl Pts',(373.239527978279,-4.41429416704596,-3.11398509543468));
#41470=CARTESIAN_POINT('Ctrl Pts',(373.329181885871,-4.42015426612438,-3.04041813877719));
#41471=CARTESIAN_POINT('Ctrl Pts',(373.422070302121,-4.42622578422203,-2.96419705398699));
#41472=CARTESIAN_POINT('Ctrl Pts',(373.511536785862,-4.43229730231969,-2.88365441067687));
#41473=CARTESIAN_POINT('Ctrl Pts',(373.597163491713,-4.43836882041735,-2.79913789904727));
#41474=CARTESIAN_POINT('Ctrl Pts',(373.679713561403,-4.4442221840042,-2.71765813340982));
#41475=CARTESIAN_POINT('Ctrl Pts',(373.7586947178,-4.45007554759105,-2.63248546851936));
#41476=CARTESIAN_POINT('Ctrl Pts',(373.833767880766,-4.45592891117791,-2.54397101639923));
#41477=CARTESIAN_POINT('Ctrl Pts',(373.908829771748,-4.46178139590183,-2.45546985442746));
#41478=CARTESIAN_POINT('Ctrl Pts',(373.979984568861,-4.46763388062576,-2.36362821790459));
#41479=CARTESIAN_POINT('Ctrl Pts',(374.046932462564,-4.47348636534969,-2.26883149922001));
#41480=CARTESIAN_POINT('Ctrl Pts',(374.113886494489,-4.47933938666779,-2.17402608895058));
#41481=CARTESIAN_POINT('Ctrl Pts',(374.176632617891,-4.4851924079859,-2.07626539540355));
#41482=CARTESIAN_POINT('Ctrl Pts',(374.234913882091,-4.49104542930401,-1.97596448562587));
#41483=CARTESIAN_POINT('Ctrl Pts',(374.293214584218,-4.49690040271769,-1.87563012355893));
#41484=CARTESIAN_POINT('Ctrl Pts',(374.347047258646,-4.50275537613138,-1.77275421764517));
#41485=CARTESIAN_POINT('Ctrl Pts',(374.396200848422,-4.50861034954506,-1.66777652235462));
#41486=CARTESIAN_POINT('Ctrl Pts',(374.445410147478,-4.51447195881902,-1.5626798483311));
#41487=CARTESIAN_POINT('Ctrl Pts',(374.489929601841,-4.52033356809298,-1.45547700475608));
#41488=CARTESIAN_POINT('Ctrl Pts',(374.529596230563,-4.52619517736695,-1.34662790479401));
#41489=CARTESIAN_POINT('Ctrl Pts',(374.569289606785,-4.53206073916705,-1.23770540708521));
#41490=CARTESIAN_POINT('Ctrl Pts',(374.604123517665,-4.53792630096715,-1.127134835646));
#41491=CARTESIAN_POINT('Ctrl Pts',(374.633985288407,-4.54379186276726,-1.01538976851875));
#41492=CARTESIAN_POINT('Ctrl Pts',(374.663890724381,-4.54966600145736,-0.903481302695676));
#41493=CARTESIAN_POINT('Ctrl Pts',(374.688809421587,-4.55554014014746,-0.790395315599256));
#41494=CARTESIAN_POINT('Ctrl Pts',(374.708680039928,-4.56141427883755,-0.676614104371761));
#41495=CARTESIAN_POINT('Ctrl Pts',(374.713704995249,-4.56289975271441,-0.647840691643158));
#41496=CARTESIAN_POINT('Ctrl Pts',(374.718407384881,-4.56438522659127,-0.61902283482409));
#41497=CARTESIAN_POINT('Ctrl Pts',(374.722786744215,-4.56587070046812,-0.590168352076625));
#41498=CARTESIAN_POINT('Ctrl Pts',(374.74010310156,-4.5717443898632,-0.47607528591433));
#41499=CARTESIAN_POINT('Ctrl Pts',(374.752422570739,-4.57761807925828,-0.361029423535447));
#41500=CARTESIAN_POINT('Ctrl Pts',(374.759647866103,-4.58349176865336,-0.245506191346751));
#41501=CARTESIAN_POINT('Ctrl Pts',(374.766863832933,-4.58935787456369,-0.130132110502376));
#41502=CARTESIAN_POINT('Ctrl Pts',(374.768998680004,-4.59522398047402,-0.0142822940982282));
#41503=CARTESIAN_POINT('Ctrl Pts',(374.766006388738,-4.60109008638435,0.101559143872355));
#41504=CARTESIAN_POINT('Ctrl Pts',(374.763017161541,-4.60695018547703,0.217281961687449));
#41505=CARTESIAN_POINT('Ctrl Pts',(374.754911249543,-4.6128102845697,0.332996007581691));
#41506=CARTESIAN_POINT('Ctrl Pts',(374.741694594454,-4.61867038366237,0.448214236826252));
#41507=CARTESIAN_POINT('Ctrl Pts',(374.728001112617,-4.62474190175476,0.567589276798935));
#41508=CARTESIAN_POINT('Ctrl Pts',(374.708821129095,-4.63081341984716,0.686431597997449));
#41509=CARTESIAN_POINT('Ctrl Pts',(374.684220292739,-4.63688493793955,0.804201595508767));
#41510=CARTESIAN_POINT('Ctrl Pts',(374.660503384068,-4.642738301541,0.917740023013324));
#41511=CARTESIAN_POINT('Ctrl Pts',(374.631748561313,-4.64859166514245,1.03028142046676));
#41512=CARTESIAN_POINT('Ctrl Pts',(374.598067048097,-4.6544450287439,1.14135051500074));
#41513=CARTESIAN_POINT('Ctrl Pts',(374.564390592047,-4.66029751348253,1.25240293288441));
#41514=CARTESIAN_POINT('Ctrl Pts',(374.525789036252,-4.66614999822116,1.36198309214184));
#41515=CARTESIAN_POINT('Ctrl Pts',(374.482423699357,-4.67200248295978,1.46963013558091));
#41516=CARTESIAN_POINT('Ctrl Pts',(374.439054386444,-4.67785550429271,1.57728704880895));
#41517=CARTESIAN_POINT('Ctrl Pts',(374.39092057855,-4.68370852562563,1.68301011064146));
#41518=CARTESIAN_POINT('Ctrl Pts',(374.338231764369,-4.68956154695855,1.78635839161207));
#41519=CARTESIAN_POINT('Ctrl Pts',(374.285525377451,-4.69541652038709,1.88974114122974));
#41520=CARTESIAN_POINT('Ctrl Pts',(374.228261150967,-4.70127149381563,1.9907471671861));
#41521=CARTESIAN_POINT('Ctrl Pts',(374.166694198068,-4.70712646724417,2.08896072158416));
#41522=CARTESIAN_POINT('Ctrl Pts',(374.105057466936,-4.71298807653309,2.18728558843171));
#41523=CARTESIAN_POINT('Ctrl Pts',(374.039108495572,-4.71884968582201,2.28281131650771));
#41524=CARTESIAN_POINT('Ctrl Pts',(373.969145399099,-4.72471129511092,2.37515162834309));
#41525=CARTESIAN_POINT('Ctrl Pts',(373.899135125997,-4.73057685692604,2.46755420592903));
#41526=CARTESIAN_POINT('Ctrl Pts',(373.825105601212,-4.73644241874116,2.55676677308016));
#41527=CARTESIAN_POINT('Ctrl Pts',(373.747393694012,-4.74230798055627,2.64243791711714));
#41528=CARTESIAN_POINT('Ctrl Pts',(373.669568152944,-4.74818211926135,2.72823433337842));
#41529=CARTESIAN_POINT('Ctrl Pts',(373.588049772981,-4.75405625796643,2.81047869938095));
#41530=CARTESIAN_POINT('Ctrl Pts',(373.503210579151,-4.75993039667151,2.88885801269218));
#41531=CARTESIAN_POINT('Ctrl Pts',(373.481756132711,-4.7614158704076,2.90867886085772));
#41532=CARTESIAN_POINT('Ctrl Pts',(373.460089473667,-4.76290134414369,2.92825274815523));
#41533=CARTESIAN_POINT('Ctrl Pts',(373.438216919809,-4.76438681787978,2.94757504587028));
#41534=CARTESIAN_POINT('Ctrl Pts',(373.351730983092,-4.77026050727015,3.02397705307453));
#41535=CARTESIAN_POINT('Ctrl Pts',(373.261735543641,-4.77613419666053,3.09669665584062));
#41536=CARTESIAN_POINT('Ctrl Pts',(373.168577366521,-4.7820078860509,3.16539437109851));
#41537=CARTESIAN_POINT('Ctrl Pts',(373.075539465359,-4.78787399195645,3.23400339115201));
#41538=CARTESIAN_POINT('Ctrl Pts',(372.979347276529,-4.793740097862,3.29860060718047));
#41539=CARTESIAN_POINT('Ctrl Pts',(372.880382657707,-4.79960620376755,3.35888490661022));
#41540=CARTESIAN_POINT('Ctrl Pts',(372.781519377394,-4.8054663028554,3.41910747568559));
#41541=CARTESIAN_POINT('Ctrl Pts',(372.679889664702,-4.81132640194326,3.47502569903849));
#41542=CARTESIAN_POINT('Ctrl Pts',(372.575906008195,-4.81718650103112,3.52638053795451));
#41543=CARTESIAN_POINT('Ctrl Pts',(372.468170858581,-4.8232580191253,3.57958814230175));
#41544=CARTESIAN_POINT('Ctrl Pts',(372.357909071984,-4.82932953721947,3.6278966043136));
#41545=CARTESIAN_POINT('Ctrl Pts',(372.245609671513,-4.83540105531365,3.67106856427793));
#41546=CARTESIAN_POINT('Ctrl Pts',(372.137345278253,-4.84125441891024,3.71268932121693));
#41547=CARTESIAN_POINT('Ctrl Pts',(372.027187596029,-4.84710778250683,3.74953617995246));
#41548=CARTESIAN_POINT('Ctrl Pts',(371.915596295746,-4.85296114610342,3.78144495262564));
#41549=CARTESIAN_POINT('Ctrl Pts',(371.80402175052,-4.85881363083717,3.81334893430402));
#41550=CARTESIAN_POINT('Ctrl Pts',(371.691014412357,-4.86466611557092,3.84031619062209));
#41551=CARTESIAN_POINT('Ctrl Pts',(371.577048995543,-4.87051860030466,3.86223244383732));
#41552=CARTESIAN_POINT('Ctrl Pts',(371.46307312963,-4.87637162163269,3.88415070647875));
#41553=CARTESIAN_POINT('Ctrl Pts',(371.348139416176,-4.88222464296072,3.90101696737458));
#41554=CARTESIAN_POINT('Ctrl Pts',(371.232731937483,-4.88807766428875,3.91276822945902));
#41555=CARTESIAN_POINT('Ctrl Pts',(371.117285968168,-4.89393263771242,3.92452341081629));
#41556=CARTESIAN_POINT('Ctrl Pts',(371.001366330216,-4.89978761113609,3.93116015932585));
#41557=CARTESIAN_POINT('Ctrl Pts',(370.885460679113,-4.90564258455976,3.93266746768146));
#41558=CARTESIAN_POINT('Ctrl Pts',(370.769423663841,-4.9115041938438,3.9341764843775));
#41559=CARTESIAN_POINT('Ctrl Pts',(370.653401080399,-4.91736580312783,3.93054445202538));
#41560=CARTESIAN_POINT('Ctrl Pts',(370.537879131819,-4.92322741241187,3.92181247441175));
#41561=CARTESIAN_POINT('Ctrl Pts',(370.42227928594,-4.92909297422208,3.91307460876149));
#41562=CARTESIAN_POINT('Ctrl Pts',(370.307181156296,-4.9349585360323,3.89922999939365));
#41563=CARTESIAN_POINT('Ctrl Pts',(370.193062657751,-4.94082409784251,3.88037121604094));
#41564=CARTESIAN_POINT('Ctrl Pts',(370.078777289972,-4.94669823654274,3.86148485652147));
#41565=CARTESIAN_POINT('Ctrl Pts',(369.965474814808,-4.95257237524297,3.83756977527947));
#41566=CARTESIAN_POINT('Ctrl Pts',(369.853619928964,-4.9584465139432,3.80876890626776));
#41567=CARTESIAN_POINT('Ctrl Pts',(369.82533365435,-4.95993198772594,3.80148563666511));
#41568=CARTESIAN_POINT('Ctrl Pts',(369.797139860427,-4.96141746150869,3.79389016329038));
#41569=CARTESIAN_POINT('Ctrl Pts',(369.769045861673,-4.96290293529143,3.78598528576341));
#41570=CARTESIAN_POINT('Ctrl Pts',(369.657959806633,-4.96877662468105,3.75472872923864));
#41571=CARTESIAN_POINT('Ctrl Pts',(369.548065570126,-4.97465031407066,3.71852684355877));
#41572=CARTESIAN_POINT('Ctrl Pts',(369.43983640708,-4.98052400346028,3.67748698112731));
#41573=CARTESIAN_POINT('Ctrl Pts',(369.331746978052,-4.98639010936504,3.63650010501407));
#41574=CARTESIAN_POINT('Ctrl Pts',(369.225318730081,-4.99225621526981,3.5906878191036));
#41575=CARTESIAN_POINT('Ctrl Pts',(369.121011699104,-4.99812232117457,3.54020776540811));
#41576=CARTESIAN_POINT('Ctrl Pts',(369.016811477197,-5.00398242026166,3.48977940264416));
#41577=CARTESIAN_POINT('Ctrl Pts',(368.914728521473,-5.00984251934875,3.4346929582895));
#41578=CARTESIAN_POINT('Ctrl Pts',(368.815204118168,-5.01570261843584,3.37515462237046));
#41579=CARTESIAN_POINT('Ctrl Pts',(368.712089101421,-5.02177413653031,3.31346827910653));
#41580=CARTESIAN_POINT('Ctrl Pts',(368.611721158483,-5.02784565462478,3.24700291130161));
#41581=CARTESIAN_POINT('Ctrl Pts',(368.514564848662,-5.03391717271925,3.17604077395487));
#41582=CARTESIAN_POINT('Ctrl Pts',(368.420899442719,-5.03977053631499,3.10762836293033));
#41583=CARTESIAN_POINT('Ctrl Pts',(368.330219210943,-5.04562389991074,3.03503703071258));
#41584=CARTESIAN_POINT('Ctrl Pts',(368.242911313649,-5.05147726350649,2.95856403456943));
#41585=CARTESIAN_POINT('Ctrl Pts',(368.155616525342,-5.05732974823937,2.88210252058951));
#41586=CARTESIAN_POINT('Ctrl Pts',(368.071693375414,-5.06318223297226,2.80176077368999));
#41587=CARTESIAN_POINT('Ctrl Pts',(367.99149523948,-5.06903471770514,2.71787574896006));
#41588=CARTESIAN_POINT('Ctrl Pts',(367.911289750453,-5.07488773903229,2.63398303309974));
#41589=CARTESIAN_POINT('Ctrl Pts',(367.834810239874,-5.08074076035944,2.54654669223868));
#41590=CARTESIAN_POINT('Ctrl Pts',(367.762372070291,-5.08659378168659,2.45593935322555));
#41591=CARTESIAN_POINT('Ctrl Pts',(367.68990974118,-5.09244875510936,2.36530179491538));
#41592=CARTESIAN_POINT('Ctrl Pts',(367.621491691082,-5.09830372853214,2.27149145800506));
#41593=CARTESIAN_POINT('Ctrl Pts',(367.5573915322,-5.10415870195491,2.17491215606009));
#41594=CARTESIAN_POINT('Ctrl Pts',(367.49321872402,-5.11002031123802,2.07822339388147));
#41595=CARTESIAN_POINT('Ctrl Pts',(367.43337380333,-5.11588192052113,1.97875974729758));
#41596=CARTESIAN_POINT('Ctrl Pts',(367.378085805582,-5.12174352980424,1.87695205928416));
#41597=CARTESIAN_POINT('Ctrl Pts',(367.322760526731,-5.12760909161352,1.77507572159938));
#41598=CARTESIAN_POINT('Ctrl Pts',(367.27199846984,-5.13347465342279,1.67085256566387));
#41599=CARTESIAN_POINT('Ctrl Pts',(367.225980930032,-5.13934021523207,1.5647343700214));
#41600=CARTESIAN_POINT('Ctrl Pts',(367.179896101293,-5.14521435393135,1.45846100354941));
#41601=CARTESIAN_POINT('Ctrl Pts',(367.138569782313,-5.15108849263063,1.35028745158122));
#41602=CARTESIAN_POINT('Ctrl Pts',(367.102133781073,-5.15696263132991,1.24068168825928));
#41603=CARTESIAN_POINT('Ctrl Pts',(367.092919711119,-5.15844810512097,1.21296417985523));
#41604=CARTESIAN_POINT('Ctrl Pts',(367.08401812311,-5.15993357891203,1.18515513506516));
#41605=CARTESIAN_POINT('Ctrl Pts',(367.075430629752,-5.16141905270309,1.15726221800515));
#41606=CARTESIAN_POINT('Ctrl Pts',(367.034031316038,-5.16858035029366,1.02279368618848));
#41607=CARTESIAN_POINT('Ctrl Pts',(366.99982432457,-5.17574164788424,0.886013496256454));
#41608=CARTESIAN_POINT('Ctrl Pts',(366.973028253342,-5.18290294547481,0.747617299051116));
#41609=CARTESIAN_POINT('Ctrl Pts',(366.946571909388,-5.18997345034808,0.610975723358209));
#41610=CARTESIAN_POINT('Ctrl Pts',(366.927339781937,-5.19704395522134,0.47275885287306));
#41611=CARTESIAN_POINT('Ctrl Pts',(366.915496348917,-5.20411446009461,0.333657035566035));
#41612=CARTESIAN_POINT('Ctrl Pts',(366.906159623003,-5.20968846604092,0.223996640628183));
#41613=CARTESIAN_POINT('Ctrl Pts',(366.901414039019,-5.21526247198723,0.11378665995732));
#41614=CARTESIAN_POINT('Ctrl Pts',(366.901319301027,-5.22083647793354,0.00337467329664173));
#41615=CARTESIAN_POINT('',(366.901318344487,-6.47083647800501,-0.00196577584637884));
#41616=CARTESIAN_POINT('Ctrl Pts',(366.901319301027,-5.22083647796505,0.00337467267254136));
#41617=CARTESIAN_POINT('Ctrl Pts',(366.901220385248,-5.22665628935448,-0.111906319793344));
#41618=CARTESIAN_POINT('Ctrl Pts',(366.906194278261,-5.23247610074391,-0.227277537418665));
#41619=CARTESIAN_POINT('Ctrl Pts',(366.916237979017,-5.23829591213334,-0.342255897440759));
#41620=CARTESIAN_POINT('Ctrl Pts',(366.92627823891,-5.24411372971836,-0.45719486712096));
#41621=CARTESIAN_POINT('Ctrl Pts',(366.94138481826,-5.24993154730338,-0.571740830287758));
#41622=CARTESIAN_POINT('Ctrl Pts',(366.961502674584,-5.25574936488841,-0.685413446100535));
#41623=CARTESIAN_POINT('Ctrl Pts',(366.981618648936,-5.26156663823225,-0.799075428145822));
#41624=CARTESIAN_POINT('Ctrl Pts',(367.006744895332,-5.26738391157609,-0.91186381321898));
#41625=CARTESIAN_POINT('Ctrl Pts',(367.036774959491,-5.27320118491992,-1.02330687980761));
#41626=CARTESIAN_POINT('Ctrl Pts',(367.066809693356,-5.27901936285557,-1.13476727590416));
#41627=CARTESIAN_POINT('Ctrl Pts',(367.101749651619,-5.28483754079121,-1.24488153367752));
#41628=CARTESIAN_POINT('Ctrl Pts',(367.141438277983,-5.29065571872685,-1.35319231551333));
#41629=CARTESIAN_POINT('Ctrl Pts',(367.181168991503,-5.2964800664544,-1.46161795375153));
#41630=CARTESIAN_POINT('Ctrl Pts',(367.225658286707,-5.30230441418196,-1.56823590254402));
#41631=CARTESIAN_POINT('Ctrl Pts',(367.274701058985,-5.30812876190951,-1.67260792721126));
#41632=CARTESIAN_POINT('Ctrl Pts',(367.3237696694,-5.31395617818903,-1.77703494017874));
#41633=CARTESIAN_POINT('Ctrl Pts',(367.377396339998,-5.31978359446856,-1.87921330207371));
#41634=CARTESIAN_POINT('Ctrl Pts',(367.435330423078,-5.32561101074808,-1.97873026198886));
#41635=CARTESIAN_POINT('Ctrl Pts',(367.493362906729,-5.33144832484695,-2.07841625065439));
#41636=CARTESIAN_POINT('Ctrl Pts',(367.555717193792,-5.33728563894582,-2.17543145344911));
#41637=CARTESIAN_POINT('Ctrl Pts',(367.622099516669,-5.34312295304469,-2.26939250864676));
#41638=CARTESIAN_POINT('Ctrl Pts',(367.685829398993,-5.34872702540138,-2.35959915902038));
#41639=CARTESIAN_POINT('Ctrl Pts',(367.753271360859,-5.35433109775806,-2.44699082150734));
#41640=CARTESIAN_POINT('Ctrl Pts',(367.824132815498,-5.35993517011475,-2.53125957551776));
#41641=CARTESIAN_POINT('Ctrl Pts',(367.898403479368,-5.36580885950525,-2.6195825761642));
#41642=CARTESIAN_POINT('Ctrl Pts',(367.976688413826,-5.37168254889576,-2.70478110188886));
#41643=CARTESIAN_POINT('Ctrl Pts',(368.058694720451,-5.37755623828626,-2.7864682350268));
#41644=CARTESIAN_POINT('Ctrl Pts',(368.140595149229,-5.38342234419195,-2.8680499024016));
#41645=CARTESIAN_POINT('Ctrl Pts',(368.226207105284,-5.38928845009763,-2.94612890400528));
#41646=CARTESIAN_POINT('Ctrl Pts',(368.315197321775,-5.39515455600332,-3.02035109681528));
#41647=CARTESIAN_POINT('Ctrl Pts',(368.404096413419,-5.40101465509129,-3.09449728704539));
#41648=CARTESIAN_POINT('Ctrl Pts',(368.496366569283,-5.40687475417926,-3.1647942609626));
#41649=CARTESIAN_POINT('Ctrl Pts',(368.591638020787,-5.41273485326723,-3.2309249711469));
#41650=CARTESIAN_POINT('Ctrl Pts',(368.690346648913,-5.41880637136136,-3.29944152648743));
#41651=CARTESIAN_POINT('Ctrl Pts',(368.792276901224,-5.42487788945549,-3.3634852049364));
#41652=CARTESIAN_POINT('Ctrl Pts',(368.896980114067,-5.43094940754962,-3.42274911210829));
#41653=CARTESIAN_POINT('Ctrl Pts',(368.997921256795,-5.43680277114631,-3.47988361973216));
#41654=CARTESIAN_POINT('Ctrl Pts',(369.101439129703,-5.44265613474301,-3.53257570586139));
#41655=CARTESIAN_POINT('Ctrl Pts',(369.207103307448,-5.4485094983397,-3.58059517706402));
#41656=CARTESIAN_POINT('Ctrl Pts',(369.312751620072,-5.45436198307355,-3.62860743830468));
#41657=CARTESIAN_POINT('Ctrl Pts',(369.420545220731,-5.4602144678074,-3.67194830873207));
#41658=CARTESIAN_POINT('Ctrl Pts',(369.530031443503,-5.46606695254125,-3.71043474021793));
#41659=CARTESIAN_POINT('Ctrl Pts',(369.63952770469,-5.47191997386937,-3.74892470039278));
#41660=CARTESIAN_POINT('Ctrl Pts',(369.750716506707,-5.47777299519749,-3.78255919981777));
#41661=CARTESIAN_POINT('Ctrl Pts',(369.863128354181,-5.4836260165256,-3.81120452835425));
#41662=CARTESIAN_POINT('Ctrl Pts',(369.975577693176,-5.48948098994937,-3.83985941066103));
#41663=CARTESIAN_POINT('Ctrl Pts',(370.089250488604,-5.49533596337313,-3.86352171135541));
#41664=CARTESIAN_POINT('Ctrl Pts',(370.203666042502,-5.5011909367969,-3.88210861435288));
#41665=CARTESIAN_POINT('Ctrl Pts',(370.318211271734,-5.507052546081,-3.9007165832175));
#41666=CARTESIAN_POINT('Ctrl Pts',(370.433500531635,-5.51291415536509,-3.91423760683375));
#41667=CARTESIAN_POINT('Ctrl Pts',(370.549046874426,-5.51877576464919,-3.92264062445891));
#41668=CARTESIAN_POINT('Ctrl Pts',(370.664671130964,-5.52464132645946,-3.93104930830056));
#41669=CARTESIAN_POINT('Ctrl Pts',(370.780552403619,-5.53050688826974,-3.93433310255362));
#41670=CARTESIAN_POINT('Ctrl Pts',(370.896204350897,-5.53637245008002,-3.93251307199427));
#41671=CARTESIAN_POINT('Ctrl Pts',(371.012025409687,-5.54224658878028,-3.93069038010385));
#41672=CARTESIAN_POINT('Ctrl Pts',(371.12761606305,-5.54812072748055,-3.92374899371211));
#41673=CARTESIAN_POINT('Ctrl Pts',(371.242495614349,-5.55399486618082,-3.91176174061286));
#41674=CARTESIAN_POINT('Ctrl Pts',(371.271546777462,-5.55548033996268,-3.90873035999623));
#41675=CARTESIAN_POINT('Ctrl Pts',(371.300552521484,-5.55696581374454,-3.90537654957443));
#41676=CARTESIAN_POINT('Ctrl Pts',(371.329505198997,-5.5584512875264,-3.90170199945949));
#41677=CARTESIAN_POINT('Ctrl Pts',(371.443986542801,-5.56432497691687,-3.88717251648342));
#41678=CARTESIAN_POINT('Ctrl Pts',(371.558018540075,-5.57019866630734,-3.86757600285981));
#41679=CARTESIAN_POINT('Ctrl Pts',(371.67111727785,-5.57607235569782,-3.84294883168461));
#41680=CARTESIAN_POINT('Ctrl Pts',(371.784069994528,-5.58193846160348,-3.81835345650102));
#41681=CARTESIAN_POINT('Ctrl Pts',(371.896091447911,-5.58780456750914,-3.78874042739306));
#41682=CARTESIAN_POINT('Ctrl Pts',(372.006703381712,-5.5936706734148,-3.75419780680135));
#41683=CARTESIAN_POINT('Ctrl Pts',(372.117202050302,-5.59953077250276,-3.71969055741302));
#41684=CARTESIAN_POINT('Ctrl Pts',(372.226293678196,-5.60539087159071,-3.68026387953297));
#41685=CARTESIAN_POINT('Ctrl Pts',(372.333511392892,-5.61125097067867,-3.63605661818084));
#41686=CARTESIAN_POINT('Ctrl Pts',(372.444597278135,-5.61732248877281,-3.59025445969113));
#41687=CARTESIAN_POINT('Ctrl Pts',(372.553671042936,-5.62339400686695,-3.53932035601467));
#41688=CARTESIAN_POINT('Ctrl Pts',(372.660231576705,-5.62946552496109,-3.4834649523722));
#41689=CARTESIAN_POINT('Ctrl Pts',(372.762963305331,-5.63531888855774,-3.42961647802234));
#41690=CARTESIAN_POINT('Ctrl Pts',(372.863358902254,-5.64117225215439,-3.37119447813759));
#41691=CARTESIAN_POINT('Ctrl Pts',(372.960991596452,-5.64702561575104,-3.3084358524636));
#41692=CARTESIAN_POINT('Ctrl Pts',(373.058609631429,-5.65287810048484,-3.24568664978606));
#41693=CARTESIAN_POINT('Ctrl Pts',(373.153465241097,-5.65873058521864,-3.17860233934789));
#41694=CARTESIAN_POINT('Ctrl Pts',(373.245159214173,-5.66458306995244,-3.10746406774643));
#41695=CARTESIAN_POINT('Ctrl Pts',(373.336861594356,-5.67043609128049,-3.0363192737209));
#41696=CARTESIAN_POINT('Ctrl Pts',(373.42540143525,-5.67628911260855,-2.96112003290217));
#41697=CARTESIAN_POINT('Ctrl Pts',(373.51041186127,-5.68214213393659,-2.88218838039787));
#41698=CARTESIAN_POINT('Ctrl Pts',(373.595450639909,-5.68799710736029,-2.80323040266316));
#41699=CARTESIAN_POINT('Ctrl Pts',(373.676957360409,-5.69385208078399,-2.72053781891182));
#41700=CARTESIAN_POINT('Ctrl Pts',(373.754601840828,-5.69970705420768,-2.6344696680252));
#41701=CARTESIAN_POINT('Ctrl Pts',(373.832334321293,-5.70556866349174,-2.54830396994421));
#41702=CARTESIAN_POINT('Ctrl Pts',(373.906195547849,-5.71143027277579,-2.45875537565285));
#41703=CARTESIAN_POINT('Ctrl Pts',(373.975895440889,-5.71729188205984,-2.36621623286639));
#41704=CARTESIAN_POINT('Ctrl Pts',(374.045642333079,-5.72315744387009,-2.27361469025631));
#41705=CARTESIAN_POINT('Ctrl Pts',(374.111222071213,-5.72902300568033,-2.17801892359745));
#41706=CARTESIAN_POINT('Ctrl Pts',(374.172388705838,-5.73488856749057,-2.0798490288792));
#41707=CARTESIAN_POINT('Ctrl Pts',(374.233644781085,-5.7407627061908,-1.98153558569724));
#41708=CARTESIAN_POINT('Ctrl Pts',(374.290474672201,-5.74663684489102,-1.88064086103138));
#41709=CARTESIAN_POINT('Ctrl Pts',(374.342678986736,-5.75251098359125,-1.77760826867542));
#41710=CARTESIAN_POINT('Ctrl Pts',(374.355880605649,-5.75399645737352,-1.75155300807049));
#41711=CARTESIAN_POINT('Ctrl Pts',(374.368786662145,-5.75548193115579,-1.7253611212195));
#41712=CARTESIAN_POINT('Ctrl Pts',(374.381394430701,-5.75696740493806,-1.69903995053452));
#41713=CARTESIAN_POINT('Ctrl Pts',(374.431246617451,-5.76284109432869,-1.5949638080628));
#41714=CARTESIAN_POINT('Ctrl Pts',(374.476597343558,-5.76871478371933,-1.48851836949951));
#41715=CARTESIAN_POINT('Ctrl Pts',(374.517214839797,-5.77458847310996,-1.38012998891218));
#41716=CARTESIAN_POINT('Ctrl Pts',(374.557779895031,-5.78045457901578,-1.27188154790683));
#41717=CARTESIAN_POINT('Ctrl Pts',(374.593623729609,-5.7863206849216,-1.16169553684183));
#41718=CARTESIAN_POINT('Ctrl Pts',(374.624561075807,-5.79218679082742,-1.05002157771301));
#41719=CARTESIAN_POINT('Ctrl Pts',(374.655466742557,-5.79804688991551,-0.938461971295911));
#41720=CARTESIAN_POINT('Ctrl Pts',(374.681475804798,-5.8039069890036,-0.8254178432435));
#41721=CARTESIAN_POINT('Ctrl Pts',(374.702451839065,-5.80976708809169,-0.711356779387259));
#41722=CARTESIAN_POINT('Ctrl Pts',(374.724184640795,-5.81583860618577,-0.593180652563559));
#41723=CARTESIAN_POINT('Ctrl Pts',(374.740514239084,-5.82191012427986,-0.473913250040106));
#41724=CARTESIAN_POINT('Ctrl Pts',(374.751345983948,-5.82798164237394,-0.35408985175764));
#41725=CARTESIAN_POINT('Ctrl Pts',(374.761788535562,-5.83383500597076,-0.238571803934091));
#41726=CARTESIAN_POINT('Ctrl Pts',(374.767121478564,-5.83968836956758,-0.122537474222565));
#41727=CARTESIAN_POINT('Ctrl Pts',(374.767312525039,-5.8455417331644,-0.00647390726555887));
#41728=CARTESIAN_POINT('Ctrl Pts',(374.767503542829,-5.85139421789838,0.109572233137454));
#41729=CARTESIAN_POINT('Ctrl Pts',(374.762554198516,-5.85724670263235,0.22564718902378));
#41730=CARTESIAN_POINT('Ctrl Pts',(374.752484325558,-5.86309918736633,0.341263087776295));
#41731=CARTESIAN_POINT('Ctrl Pts',(374.742413529328,-5.86895220869458,0.456889586954512));
#41732=CARTESIAN_POINT('Ctrl Pts',(374.727221307014,-5.87480523002283,0.572056533719801));
#41733=CARTESIAN_POINT('Ctrl Pts',(374.7069793805,-5.88065825135108,0.686281061344037));
#41734=CARTESIAN_POINT('Ctrl Pts',(374.686730702912,-5.88651322477496,0.800543685053763));
#41735=CARTESIAN_POINT('Ctrl Pts',(374.661429044272,-5.89236819819884,0.913862858034044));
#41736=CARTESIAN_POINT('Ctrl Pts',(374.631197112997,-5.89822317162272,1.02576648741553));
#41737=CARTESIAN_POINT('Ctrl Pts',(374.600930917711,-5.90408478090695,1.13779694518774));
#41738=CARTESIAN_POINT('Ctrl Pts',(374.56572340463,-5.90994639019118,1.24840825813228));
#41739=CARTESIAN_POINT('Ctrl Pts',(374.525747011703,-5.91580799947541,1.35714397465026));
#41740=CARTESIAN_POINT('Ctrl Pts',(374.485743662401,-5.92167356128584,1.46595301246082));
#41741=CARTESIAN_POINT('Ctrl Pts',(374.440965189286,-5.92753912309628,1.5728835553525));
#41742=CARTESIAN_POINT('Ctrl Pts',(374.391631270778,-5.93340468490672,1.67750119203868));
#41743=CARTESIAN_POINT('Ctrl Pts',(374.342225213981,-5.93927882360712,1.78227180536844));
#41744=CARTESIAN_POINT('Ctrl Pts',(374.288250609583,-5.94515296230752,1.88472239868276));
#41745=CARTESIAN_POINT('Ctrl Pts',(374.229971969129,-5.95102710100793,1.98444504210553));
#41746=CARTESIAN_POINT('Ctrl Pts',(374.215234252371,-5.95251257478852,2.00966327063081));
#41747=CARTESIAN_POINT('Ctrl Pts',(374.20022150031,-5.95399804856911,2.03470720212601));
#41748=CARTESIAN_POINT('Ctrl Pts',(374.1849384053,-5.95548352234971,2.05957056592035));
#41749=CARTESIAN_POINT('Ctrl Pts',(374.124507750657,-5.96135721174026,2.15788241634833));
#41750=CARTESIAN_POINT('Ctrl Pts',(374.059645873288,-5.96723090113082,2.25369607201985));
#41751=CARTESIAN_POINT('Ctrl Pts',(373.99058539756,-5.97310459052138,2.34658564484079));
#41752=CARTESIAN_POINT('Ctrl Pts',(373.921614085394,-5.97897069642712,2.43935528849655));
#41753=CARTESIAN_POINT('Ctrl Pts',(373.84845519928,-5.98483680233285,2.52920802854297));
#41754=CARTESIAN_POINT('Ctrl Pts',(373.771386124717,-5.99070290823859,2.61574443870009));
#41755=CARTESIAN_POINT('Ctrl Pts',(373.694395967904,-5.99656300732661,2.70219223667548));
#41756=CARTESIAN_POINT('Ctrl Pts',(373.613503860036,-6.00242310641462,2.78533015275468));
#41757=CARTESIAN_POINT('Ctrl Pts',(373.529028760698,-6.00828320550263,2.86479006650444));
#41758=CARTESIAN_POINT('Ctrl Pts',(373.441505992494,-6.01435472359674,2.94711671266566));
#41759=CARTESIAN_POINT('Ctrl Pts',(373.350137088781,-6.02042624169086,3.02549459551221));
#41760=CARTESIAN_POINT('Ctrl Pts',(373.255320538837,-6.02649775978497,3.09955399957096));
#41761=CARTESIAN_POINT('Ctrl Pts',(373.163910823308,-6.03235112338171,3.17095239005482));
#41762=CARTESIAN_POINT('Ctrl Pts',(373.06929730463,-6.03820448697844,3.23833701764739));
#41763=CARTESIAN_POINT('Ctrl Pts',(372.971871746654,-6.04405785057518,3.30141671902837));
#41764=CARTESIAN_POINT('Ctrl Pts',(372.874460816798,-6.04991033530907,3.36448694920454));
#41765=CARTESIAN_POINT('Ctrl Pts',(372.774239033879,-6.05576282004297,3.42325331391514));
#41766=CARTESIAN_POINT('Ctrl Pts',(372.671627112992,-6.06161530477687,3.47746799898576));
#41767=CARTESIAN_POINT('Ctrl Pts',(372.56900578397,-6.06746832610504,3.53168765481516));
#41768=CARTESIAN_POINT('Ctrl Pts',(372.463994246656,-6.07332134743322,3.58135460838357));
#41769=CARTESIAN_POINT('Ctrl Pts',(372.357037138867,-6.07917436876139,3.62626736150693));
#41770=CARTESIAN_POINT('Ctrl Pts',(372.250044358818,-6.08502934218518,3.67119509390058));
#41771=CARTESIAN_POINT('Ctrl Pts',(372.141105098732,-6.09088431560897,3.71136531305037));
#41772=CARTESIAN_POINT('Ctrl Pts',(372.030682583354,-6.09673928903277,3.74662520576861));
#41773=CARTESIAN_POINT('Ctrl Pts',(371.920134918237,-6.10260089831691,3.78192506104642));
#41774=CARTESIAN_POINT('Ctrl Pts',(371.808101036282,-6.10846250760106,3.81230335629673));
#41775=CARTESIAN_POINT('Ctrl Pts',(371.695057977601,-6.1143241168852,3.83765754572866));
#41776=CARTESIAN_POINT('Ctrl Pts',(371.581938693155,-6.12018967869554,3.86302883167673));
#41777=CARTESIAN_POINT('Ctrl Pts',(371.467809282695,-6.12605524050587,3.88336919365227));
#41778=CARTESIAN_POINT('Ctrl Pts',(371.353153875195,-6.1319208023162,3.89862773066437));
#41779=CARTESIAN_POINT('Ctrl Pts',(371.238330813369,-6.13779494101652,3.91390857939995));
#41780=CARTESIAN_POINT('Ctrl Pts',(371.12298062946,-6.14366907971683,3.9240927368195));
#41781=CARTESIAN_POINT('Ctrl Pts',(371.007589504371,-6.14954321841715,3.92918133138555));
#41782=CARTESIAN_POINT('Ctrl Pts',(370.978408972608,-6.15102869219855,3.93046815387949));
#41783=CARTESIAN_POINT('Ctrl Pts',(370.949225804753,-6.15251416597996,3.93142937397184));
#41784=CARTESIAN_POINT('Ctrl Pts',(370.92004781387,-6.15399963976136,3.93206553529409));
#41785=CARTESIAN_POINT('Ctrl Pts',(370.804675561844,-6.15987332915193,3.93458097114762));
#41786=CARTESIAN_POINT('Ctrl Pts',(370.68900035449,-6.16574701854249,3.93201852063393));
#41787=CARTESIAN_POINT('Ctrl Pts',(370.573506176798,-6.17162070793306,3.92434278184764));
#41788=CARTESIAN_POINT('Ctrl Pts',(370.458161112939,-6.1774868138388,3.91667695316123));
#41789=CARTESIAN_POINT('Ctrl Pts',(370.342997022408,-6.18335291974455,3.90391099203652));
#41790=CARTESIAN_POINT('Ctrl Pts',(370.228499919559,-6.18921902565029,3.88606145489872));
#41791=CARTESIAN_POINT('Ctrl Pts',(370.114120060284,-6.19507912473834,3.86823019545951));
#41792=CARTESIAN_POINT('Ctrl Pts',(370.00040623596,-6.20093922382639,3.84532577747242));
#41793=CARTESIAN_POINT('Ctrl Pts',(369.887840692103,-6.20679932291444,3.81741666359283));
#41794=CARTESIAN_POINT('Ctrl Pts',(369.771214040227,-6.21287084100855,3.78850065255539));
#41795=CARTESIAN_POINT('Ctrl Pts',(369.65582053851,-6.21894235910265,3.75421204151894));
#41796=CARTESIAN_POINT('Ctrl Pts',(369.542186886595,-6.22501387719676,3.71468525787553));
#41797=CARTESIAN_POINT('Ctrl Pts',(369.432636182606,-6.23086724079351,3.67657870315747));
#41798=CARTESIAN_POINT('Ctrl Pts',(369.324721462914,-6.23672060439025,3.63360406847479));
#41799=CARTESIAN_POINT('Ctrl Pts',(369.21889977325,-6.242573967987,3.58593271365957));
#41800=CARTESIAN_POINT('Ctrl Pts',(369.113093972357,-6.2484264527209,3.53826851653782));
#41801=CARTESIAN_POINT('Ctrl Pts',(369.009380953208,-6.25427893745481,3.48590917112673));
#41802=CARTESIAN_POINT('Ctrl Pts',(368.908197029654,-6.26013142218871,3.4290738652016));
#41803=CARTESIAN_POINT('Ctrl Pts',(368.807003828892,-6.26598444351687,3.37223334824221));
#41804=CARTESIAN_POINT('Ctrl Pts',(368.708340544919,-6.27183746484502,3.31091625730278));
#41805=CARTESIAN_POINT('Ctrl Pts',(368.612617540628,-6.27769048617318,3.24538699094737));
#41806=CARTESIAN_POINT('Ctrl Pts',(368.516862610866,-6.28354545959698,3.1798358693162));
#41807=CARTESIAN_POINT('Ctrl Pts',(368.424050251476,-6.28940043302078,3.11007001205794));
#41808=CARTESIAN_POINT('Ctrl Pts',(368.334559991117,-6.29525540644457,3.03639582907697));
#41809=CARTESIAN_POINT('Ctrl Pts',(368.244968305043,-6.30111701572871,2.96263814587257));
#41810=CARTESIAN_POINT('Ctrl Pts',(368.158706552196,-6.30697862501285,2.88496355849596));
#41811=CARTESIAN_POINT('Ctrl Pts',(368.076119510592,-6.31284023429699,2.80371733644894));
#41812=CARTESIAN_POINT('Ctrl Pts',(367.99347677994,-6.31870579610733,2.72241632947761));
#41813=CARTESIAN_POINT('Ctrl Pts',(367.914513975261,-6.32457135791766,2.63753919395571));
#41814=CARTESIAN_POINT('Ctrl Pts',(367.839536319979,-6.33043691972799,2.54946515334727));
#41815=CARTESIAN_POINT('Ctrl Pts',(367.764449028975,-6.33631105842832,2.46126232688987));
#41816=CARTESIAN_POINT('Ctrl Pts',(367.693358769784,-6.34218519712865,2.36985359077362));
#41817=CARTESIAN_POINT('Ctrl Pts',(367.626528157443,-6.34805933582898,2.27564809837513));
#41818=CARTESIAN_POINT('Ctrl Pts',(367.609627786598,-6.34954480961033,2.2518250672626));
#41819=CARTESIAN_POINT('Ctrl Pts',(367.592999592957,-6.35103028339168,2.22782330886293));
#41820=CARTESIAN_POINT('Ctrl Pts',(367.576647355237,-6.35251575717303,2.20364968326253));
#41821=CARTESIAN_POINT('Ctrl Pts',(367.510968455758,-6.35848217503169,2.10655611399077));
#41822=CARTESIAN_POINT('Ctrl Pts',(367.449530811241,-6.36444859289036,2.00637148061744));
#41823=CARTESIAN_POINT('Ctrl Pts',(367.392633063595,-6.37041501074903,1.90349541865323));
#41824=CARTESIAN_POINT('Ctrl Pts',(367.335814919807,-6.37637308117918,1.80076328736784));
#41825=CARTESIAN_POINT('Ctrl Pts',(367.283524226256,-6.38233115160934,1.69534756210725));
#41826=CARTESIAN_POINT('Ctrl Pts',(367.236017055976,-6.3882892220395,1.58767766644368));
#41827=CARTESIAN_POINT('Ctrl Pts',(367.188566178526,-6.39424023255341,1.48013535242832));
#41828=CARTESIAN_POINT('Ctrl Pts',(367.145887704166,-6.40019124306732,1.37034454303869));
#41829=CARTESIAN_POINT('Ctrl Pts',(367.108192119715,-6.40614225358123,1.25875971419715));
#41830=CARTESIAN_POINT('Ctrl Pts',(367.070540033329,-6.41208639704585,1.14730364643201));
#41831=CARTESIAN_POINT('Ctrl Pts',(367.037859510265,-6.41803054051047,1.03405805614495));
#41832=CARTESIAN_POINT('Ctrl Pts',(367.010312890166,-6.42397468397509,0.919497168298037));
#41833=CARTESIAN_POINT('Ctrl Pts',(366.982784981765,-6.42991478973863,0.805014098664051));
#41834=CARTESIAN_POINT('Ctrl Pts',(366.960384129132,-6.43585489550216,0.689217893220492));
#41835=CARTESIAN_POINT('Ctrl Pts',(366.943222766006,-6.44179500126569,0.572597609344167));
#41836=CARTESIAN_POINT('Ctrl Pts',(366.926069341682,-6.44773235915183,0.456031273706099));
#41837=CARTESIAN_POINT('Ctrl Pts',(366.914150640268,-6.45366971703798,0.33864200960788));
#41838=CARTESIAN_POINT('Ctrl Pts',(366.907527853233,-6.45960707492412,0.220928259789999));
#41839=CARTESIAN_POINT('Ctrl Pts',(366.903352598499,-6.4633502092711,0.14671707217018));
#41840=CARTESIAN_POINT('Ctrl Pts',(366.901281186748,-6.46709334361807,0.0723770988410905));
#41841=CARTESIAN_POINT('Ctrl Pts',(366.901318344487,-6.47083647796505,-0.00196577505274522));
#41842=CARTESIAN_POINT('',(366.901318562436,-7.72083647791836,-0.00236191956902979));
#41843=CARTESIAN_POINT('Ctrl Pts',(366.901318344487,-6.47083647800501,-0.00196577584638068));
#41844=CARTESIAN_POINT('Ctrl Pts',(366.90138468552,-6.47751942771998,-0.134696701814077));
#41845=CARTESIAN_POINT('Ctrl Pts',(366.908174895024,-6.48420237743496,-0.267198358871215));
#41846=CARTESIAN_POINT('Ctrl Pts',(366.921591070369,-6.49088532714993,-0.398820915615153));
#41847=CARTESIAN_POINT('Ctrl Pts',(366.934591876209,-6.49736137039203,-0.526368391724456));
#41848=CARTESIAN_POINT('Ctrl Pts',(366.953814296689,-6.50383741363414,-0.653090193759929));
#41849=CARTESIAN_POINT('Ctrl Pts',(366.979118129333,-6.51031345687624,-0.778411259497541));
#41850=CARTESIAN_POINT('Ctrl Pts',(367.005634629937,-6.51709985982765,-0.909738247073178));
#41851=CARTESIAN_POINT('Ctrl Pts',(367.038829661962,-6.52388626277905,-1.03952658214836));
#41852=CARTESIAN_POINT('Ctrl Pts',(367.078485202183,-6.53067266573046,-1.16713756574511));
#41853=CARTESIAN_POINT('Ctrl Pts',(367.118140742404,-6.53745906868187,-1.29474854934185));
#41854=CARTESIAN_POINT('Ctrl Pts',(367.164256593428,-6.54424547163327,-1.42018191676854));
#41855=CARTESIAN_POINT('Ctrl Pts',(367.216559571197,-6.55103187458468,-1.5428266308395));
#41856=CARTESIAN_POINT('Ctrl Pts',(367.26182824266,-6.55690556397525,-1.64897667247503));
#41857=CARTESIAN_POINT('Ctrl Pts',(367.311848152075,-6.56277925336581,-1.75330944973659));
#41858=CARTESIAN_POINT('Ctrl Pts',(367.366452037994,-6.56865294275637,-1.85536942077916));
#41859=CARTESIAN_POINT('Ctrl Pts',(367.420985425167,-6.57451904866213,-1.95729762281101));
#41860=CARTESIAN_POINT('Ctrl Pts',(367.480090826079,-6.58038515456788,-2.05695849323852));
#41861=CARTESIAN_POINT('Ctrl Pts',(367.543552804627,-6.58625126047363,-2.15391606032704));
#41862=CARTESIAN_POINT('Ctrl Pts',(367.606949798918,-6.59211135956167,-2.25077434410206));
#41863=CARTESIAN_POINT('Ctrl Pts',(367.674694272473,-6.59797145864971,-2.34493448698793));
#41864=CARTESIAN_POINT('Ctrl Pts',(367.746525052225,-6.60383155773775,-2.43598534849786));
#41865=CARTESIAN_POINT('Ctrl Pts',(367.820947322637,-6.60990307583185,-2.53032111737081));
#41866=CARTESIAN_POINT('Ctrl Pts',(367.899756102272,-6.61597459392596,-2.62131861919165));
#41867=CARTESIAN_POINT('Ctrl Pts',(367.98261179353,-6.62204611202007,-2.70855340525223));
#41868=CARTESIAN_POINT('Ctrl Pts',(368.062490413584,-6.62789947561682,-2.7926537757333));
#41869=CARTESIAN_POINT('Ctrl Pts',(368.146129823731,-6.63375283921357,-2.87325684653535));
#41870=CARTESIAN_POINT('Ctrl Pts',(368.233185491794,-6.63960620281031,-2.95001685390454));
#41871=CARTESIAN_POINT('Ctrl Pts',(368.320228088741,-6.64545868754421,-3.02676533601691));
#41872=CARTESIAN_POINT('Ctrl Pts',(368.410685613885,-6.65131117227811,-3.09967162887043));
#41873=CARTESIAN_POINT('Ctrl Pts',(368.504178506474,-6.65716365701201,-3.1684285733985));
#41874=CARTESIAN_POINT('Ctrl Pts',(368.597679971106,-6.66301667834019,-3.23719182201525));
#41875=CARTESIAN_POINT('Ctrl Pts',(368.694217023573,-6.66886969966836,-3.30180472124366));
#41876=CARTESIAN_POINT('Ctrl Pts',(368.793379610461,-6.67472272099653,-3.36200239280498));
#41877=CARTESIAN_POINT('Ctrl Pts',(368.892575269986,-6.68057769442036,-3.42222014145235));
#41878=CARTESIAN_POINT('Ctrl Pts',(368.994397852182,-6.68643266784418,-3.47801952002925));
#41879=CARTESIAN_POINT('Ctrl Pts',(369.098411738974,-6.69228764126801,-3.52918106116823));
#41880=CARTESIAN_POINT('Ctrl Pts',(369.202543512145,-6.69814925055216,-3.58040058734258));
#41881=CARTESIAN_POINT('Ctrl Pts',(369.30887117602,-6.70401085983632,-3.62697160218351));
#41882=CARTESIAN_POINT('Ctrl Pts',(369.416938033824,-6.70987246912047,-3.66872231813177));
#41883=CARTESIAN_POINT('Ctrl Pts',(369.525077761904,-6.71573803093081,-3.71050118689439));
#41884=CARTESIAN_POINT('Ctrl Pts',(369.634958628495,-6.72160359274114,-3.74745315320668));
#41885=CARTESIAN_POINT('Ctrl Pts',(369.746109307894,-6.72746915455148,-3.77945646381478));
#41886=CARTESIAN_POINT('Ctrl Pts',(369.857422516848,-6.73334329325182,-3.81150657111234));
#41887=CARTESIAN_POINT('Ctrl Pts',(369.970008844132,-6.73921743195215,-3.83859348490398));
#41888=CARTESIAN_POINT('Ctrl Pts',(370.083387260216,-6.74509157065248,-3.86064660963485));
#41889=CARTESIAN_POINT('Ctrl Pts',(370.112058810727,-6.74657704443377,-3.86622348485934));
#41890=CARTESIAN_POINT('Ctrl Pts',(370.140780994845,-6.74806251821505,-3.87147870792583));
#41891=CARTESIAN_POINT('Ctrl Pts',(370.169546004779,-6.74954799199634,-3.87641166409289));
#41892=CARTESIAN_POINT('Ctrl Pts',(370.283285295097,-6.7554216813869,-3.89591699139492));
#41893=CARTESIAN_POINT('Ctrl Pts',(370.398073215185,-6.76129537077747,-3.91044465986015));
#41894=CARTESIAN_POINT('Ctrl Pts',(370.513436295632,-6.76716906016804,-3.91988826702975));
#41895=CARTESIAN_POINT('Ctrl Pts',(370.628650431505,-6.77303516607379,-3.9293196816153));
#41896=CARTESIAN_POINT('Ctrl Pts',(370.744437842971,-6.77890127197954,-3.93368005515114));
#41897=CARTESIAN_POINT('Ctrl Pts',(370.860315389599,-6.7847673778853,-3.9329140758606));
#41898=CARTESIAN_POINT('Ctrl Pts',(370.976074279097,-6.79062747697333,-3.93214888092309));
#41899=CARTESIAN_POINT('Ctrl Pts',(371.09192270949,-6.79648757606136,-3.92626777720643));
#41900=CARTESIAN_POINT('Ctrl Pts',(371.207373611798,-6.80234767514939,-3.9152673473206));
#41901=CARTESIAN_POINT('Ctrl Pts',(371.326989719275,-6.8084191932435,-3.90387004702048));
#41902=CARTESIAN_POINT('Ctrl Pts',(371.446178623122,-6.81449071133761,-3.88697702227996));
#41903=CARTESIAN_POINT('Ctrl Pts',(371.56439955667,-6.82056222943172,-3.86464354194443));
#41904=CARTESIAN_POINT('Ctrl Pts',(371.678372717596,-6.82641559302847,-3.84311252140584));
#41905=CARTESIAN_POINT('Ctrl Pts',(371.791445830236,-6.83226895662522,-3.81652536002251));
#41906=CARTESIAN_POINT('Ctrl Pts',(371.903141572424,-6.83812232022197,-3.7849841290653));
#41907=CARTESIAN_POINT('Ctrl Pts',(372.014820543872,-6.84397480495587,-3.75344763391778));
#41908=CARTESIAN_POINT('Ctrl Pts',(372.12512215859,-6.84982728968977,-3.71695866046873));
#41909=CARTESIAN_POINT('Ctrl Pts',(372.233582544911,-6.85567977442367,-3.67566964274513));
#41910=CARTESIAN_POINT('Ctrl Pts',(372.342052875593,-6.86153279575184,-3.63437683937295));
#41911=CARTESIAN_POINT('Ctrl Pts',(372.448681256152,-6.86738581708002,-3.58828326384426));
#41912=CARTESIAN_POINT('Ctrl Pts',(372.553022813437,-6.87323883840819,-3.53758989422734));
#41913=CARTESIAN_POINT('Ctrl Pts',(372.657399170646,-6.87909381183201,-3.48687961739263));
#41914=CARTESIAN_POINT('Ctrl Pts',(372.759486816577,-6.88494878525584,-3.4315666763854));
#41915=CARTESIAN_POINT('Ctrl Pts',(372.858865178378,-6.89080375867967,-3.37189814914575));
#41916=CARTESIAN_POINT('Ctrl Pts',(372.958356172787,-6.89666536796382,-3.31216199529465));
#41917=CARTESIAN_POINT('Ctrl Pts',(373.05513139988,-6.90252697724797,-3.24806061504836));
#41918=CARTESIAN_POINT('Ctrl Pts',(373.148798925558,-6.90838858653212,-3.17988464661986));
#41919=CARTESIAN_POINT('Ctrl Pts',(373.242529611936,-6.91425414834247,-3.11166270663513));
#41920=CARTESIAN_POINT('Ctrl Pts',(373.333148102055,-6.92011971015281,-3.03936096456918));
#41921=CARTESIAN_POINT('Ctrl Pts',(373.420296575553,-6.92598527196315,-2.96330947551237));
#41922=CARTESIAN_POINT('Ctrl Pts',(373.507572481494,-6.93185941066348,-2.88714678052573));
#41923=CARTESIAN_POINT('Ctrl Pts',(373.59136794654,-6.93773354936381,-2.80722367981111));
#41924=CARTESIAN_POINT('Ctrl Pts',(373.671362878008,-6.94360768806415,-2.72390611573636));
#41925=CARTESIAN_POINT('Ctrl Pts',(373.69159229025,-6.94509316184543,-2.70283646395128));
#41926=CARTESIAN_POINT('Ctrl Pts',(373.711578864619,-6.94657863562671,-2.68154989365513));
#41927=CARTESIAN_POINT('Ctrl Pts',(373.731317851865,-6.94806410940799,-2.66005263253818));
#41928=CARTESIAN_POINT('Ctrl Pts',(373.809367482516,-6.95393779879856,-2.57505063779416));
#41929=CARTESIAN_POINT('Ctrl Pts',(373.883802819557,-6.95981148818913,-2.48646903502814));
#41930=CARTESIAN_POINT('Ctrl Pts',(373.954277779898,-6.96568517757969,-2.39464800251529));
#41931=CARTESIAN_POINT('Ctrl Pts',(374.024661750443,-6.97155128348545,-2.30294551958161));
#41932=CARTESIAN_POINT('Ctrl Pts',(374.091095263553,-6.97741738939121,-2.20801224908474));
#41933=CARTESIAN_POINT('Ctrl Pts',(374.153269925284,-6.98328349529696,-2.11022419267893));
#41934=CARTESIAN_POINT('Ctrl Pts',(374.215380920954,-6.989143594385,-2.01253626999715));
#41935=CARTESIAN_POINT('Ctrl Pts',(374.273241519302,-6.99500369347304,-1.91199972259126));
#41936=CARTESIAN_POINT('Ctrl Pts',(374.326584803942,-7.00086379256108,-1.80902198574878));
#41937=CARTESIAN_POINT('Ctrl Pts',(374.381852592596,-7.00693531065518,-1.70232904709086));
#41938=CARTESIAN_POINT('Ctrl Pts',(374.432270689726,-7.01300682874929,-1.59301580650699));
#41939=CARTESIAN_POINT('Ctrl Pts',(374.477592383421,-7.0190783468434,-1.48156663623885));
#41940=CARTESIAN_POINT('Ctrl Pts',(374.521285632442,-7.02493171044015,-1.37412192372638));
#41941=CARTESIAN_POINT('Ctrl Pts',(374.560242241898,-7.0307850740369,-1.26469254681109));
#41942=CARTESIAN_POINT('Ctrl Pts',(374.594289222193,-7.03663843763365,-1.15373493686026));
#41943=CARTESIAN_POINT('Ctrl Pts',(374.628331090449,-7.04249092236755,-1.04279398682117));
#41944=CARTESIAN_POINT('Ctrl Pts',(374.657464674142,-7.04834340710146,-0.930325654860274));
#41945=CARTESIAN_POINT('Ctrl Pts',(374.681566595537,-7.05419589183536,-0.816802371915838));
#41946=CARTESIAN_POINT('Ctrl Pts',(374.705670726756,-7.06004891316354,-0.703268680410562));
#41947=CARTESIAN_POINT('Ctrl Pts',(374.724742192778,-7.06590193449171,-0.588680249801158));
#41948=CARTESIAN_POINT('Ctrl Pts',(374.738708707085,-7.07175495581989,-0.473519862611013));
#41949=CARTESIAN_POINT('Ctrl Pts',(374.752679879494,-7.07760992924371,-0.358321067207775));
#41950=CARTESIAN_POINT('Ctrl Pts',(374.76154266493,-7.08346490266754,-0.242550345827211));
#41951=CARTESIAN_POINT('Ctrl Pts',(374.76527668838,-7.08931987609136,-0.126695052439334));
#41952=CARTESIAN_POINT('Ctrl Pts',(374.769014943865,-7.09518148537551,-0.0107084519574659));
#41953=CARTESIAN_POINT('Ctrl Pts',(374.767612822065,-7.10104309465967,0.105362498684048));
#41954=CARTESIAN_POINT('Ctrl Pts',(374.761102077346,-7.10690470394382,0.22103089644694));
#41955=CARTESIAN_POINT('Ctrl Pts',(374.754586942385,-7.11277026575416,0.336777290259909));
#41956=CARTESIAN_POINT('Ctrl Pts',(374.742956366527,-7.11863582756451,0.452120180645069));
#41957=CARTESIAN_POINT('Ctrl Pts',(374.726293719834,-7.12450138937485,0.566579962341262));
#41958=CARTESIAN_POINT('Ctrl Pts',(374.709606708265,-7.13037552807518,0.681207112311389));
#41959=CARTESIAN_POINT('Ctrl Pts',(374.687873018142,-7.13624966677552,0.794948172196397));
#41960=CARTESIAN_POINT('Ctrl Pts',(374.661226628422,-7.14212380547585,0.907335784765218));
#41961=CARTESIAN_POINT('Ctrl Pts',(374.654488191467,-7.14360927925711,0.935756777242086));
#41962=CARTESIAN_POINT('Ctrl Pts',(374.647435831465,-7.14509475303838,0.964091304736905));
#41963=CARTESIAN_POINT('Ctrl Pts',(374.640072206979,-7.14658022681965,0.992332000327942));
#41964=CARTESIAN_POINT('Ctrl Pts',(374.610955810874,-7.15245391621022,1.10399810724093));
#41965=CARTESIAN_POINT('Ctrl Pts',(374.576872099117,-7.15832760560079,1.21456763442592));
#41966=CARTESIAN_POINT('Ctrl Pts',(374.537919311246,-7.16420129499136,1.32356535166729));
#41967=CARTESIAN_POINT('Ctrl Pts',(374.499016815084,-7.17006740089712,1.43242234261573));
#41968=CARTESIAN_POINT('Ctrl Pts',(374.455257882231,-7.17593350680287,1.53971117384656));
#41969=CARTESIAN_POINT('Ctrl Pts',(374.406791286539,-7.18179961270863,1.64496886543727));
#41970=CARTESIAN_POINT('Ctrl Pts',(374.358374320023,-7.18765971179667,1.75011877449274));
#41971=CARTESIAN_POINT('Ctrl Pts',(374.305259450984,-7.19351981088471,1.85324130788152));
#41972=CARTESIAN_POINT('Ctrl Pts',(374.24764435258,-7.19937990997275,1.95389129912461));
#41973=CARTESIAN_POINT('Ctrl Pts',(374.187950632866,-7.20545142806686,2.05817251243229));
#41974=CARTESIAN_POINT('Ctrl Pts',(374.123425988981,-7.21152294616097,2.1597989824911));
#41975=CARTESIAN_POINT('Ctrl Pts',(374.054343697848,-7.21759446425507,2.2583008125483));
#41976=CARTESIAN_POINT('Ctrl Pts',(373.987743588644,-7.22344782785183,2.35326339313092));
#41977=CARTESIAN_POINT('Ctrl Pts',(373.91690797301,-7.22930119144858,2.44532164376667));
#41978=CARTESIAN_POINT('Ctrl Pts',(373.8421266145,-7.23515455504533,2.53408276415575));
#41979=CARTESIAN_POINT('Ctrl Pts',(373.76735648416,-7.24100703977924,2.62283055736129));
#41980=CARTESIAN_POINT('Ctrl Pts',(373.688642055061,-7.24685952451315,2.70828188879879));
#41981=CARTESIAN_POINT('Ctrl Pts',(373.606313430384,-7.25271200924705,2.79007697388538));
#41982=CARTESIAN_POINT('Ctrl Pts',(373.523977257278,-7.25856503057523,2.87187955848303));
#41983=CARTESIAN_POINT('Ctrl Pts',(373.438026522958,-7.26441805190341,2.95002493912412));
#41984=CARTESIAN_POINT('Ctrl Pts',(373.348827726156,-7.27027107323158,3.02419065188158));
#41985=CARTESIAN_POINT('Ctrl Pts',(373.259599179833,-7.27612604665541,3.09838110033653));
#41986=CARTESIAN_POINT('Ctrl Pts',(373.167120734459,-7.28198102007923,3.16858897764277));
#41987=CARTESIAN_POINT('Ctrl Pts',(373.071790871911,-7.28783599350305,3.23453296329564));
#41988=CARTESIAN_POINT('Ctrl Pts',(372.976352965209,-7.29369760278721,3.30055168798608));
#41989=CARTESIAN_POINT('Ctrl Pts',(372.878057530989,-7.29955921207137,3.36229664032892));
#41990=CARTESIAN_POINT('Ctrl Pts',(372.777330932039,-7.30542082135552,3.41953054900116));
#41991=CARTESIAN_POINT('Ctrl Pts',(372.676536412404,-7.31128638316587,3.47680305091834));
#41992=CARTESIAN_POINT('Ctrl Pts',(372.573307830703,-7.31715194497621,3.52955826466241));
#41993=CARTESIAN_POINT('Ctrl Pts',(372.468093398704,-7.32301750678656,3.57760624817654));
#41994=CARTESIAN_POINT('Ctrl Pts',(372.362725117399,-7.32889164548689,3.62572448962713));
#41995=CARTESIAN_POINT('Ctrl Pts',(372.255365572104,-7.33476578418723,3.66912160962422));
#41996=CARTESIAN_POINT('Ctrl Pts',(372.146480118032,-7.34063992288757,3.70765683293566));
#41997=CARTESIAN_POINT('Ctrl Pts',(372.118944764266,-7.34212539666881,3.71740176181865));
#41998=CARTESIAN_POINT('Ctrl Pts',(372.091311887034,-7.34361087045006,3.72683602521229));
#41999=CARTESIAN_POINT('Ctrl Pts',(372.063589118049,-7.3450963442313,3.7359578634502));
#42000=CARTESIAN_POINT('Ctrl Pts',(371.953970936889,-7.35097003362186,3.77202638593574));
#42001=CARTESIAN_POINT('Ctrl Pts',(371.842581391219,-7.35684372301243,3.80332636779904));
#42002=CARTESIAN_POINT('Ctrl Pts',(371.729873077309,-7.36271741240299,3.82968273367564));
#42003=CARTESIAN_POINT('Ctrl Pts',(371.617310280421,-7.36858351830874,3.8560050710078));
#42004=CARTESIAN_POINT('Ctrl Pts',(371.503432499929,-7.37444962421448,3.87739639218139));
#42005=CARTESIAN_POINT('Ctrl Pts',(371.388709433216,-7.38031573012023,3.89373072721186));
#42006=CARTESIAN_POINT('Ctrl Pts',(371.274103841462,-7.38617582920826,3.91004833609135));
#42007=CARTESIAN_POINT('Ctrl Pts',(371.15865509175,-7.39203592829629,3.92131920098413));
#42008=CARTESIAN_POINT('Ctrl Pts',(371.042844421464,-7.39789602738432,3.92746809921326));
#42009=CARTESIAN_POINT('Ctrl Pts',(370.922855566402,-7.40396754547843,3.93383883566263));
#42010=CARTESIAN_POINT('Ctrl Pts',(370.802478622983,-7.41003906357254,3.93471094705704));
#42011=CARTESIAN_POINT('Ctrl Pts',(370.682256595156,-7.41611058166665,3.93005933464048));
#42012=CARTESIAN_POINT('Ctrl Pts',(370.566354240868,-7.4219639452634,3.92557485837552));
#42013=CARTESIAN_POINT('Ctrl Pts',(370.450596309506,-7.42781730886014,3.91595678793313));
#42014=CARTESIAN_POINT('Ctrl Pts',(370.335469957822,-7.43367067245688,3.90123567312369));
#42015=CARTESIAN_POINT('Ctrl Pts',(370.220360891973,-7.43952315719078,3.88651676864012));
#42016=CARTESIAN_POINT('Ctrl Pts',(370.105883626943,-7.44537564192467,3.86669639568048));
#42017=CARTESIAN_POINT('Ctrl Pts',(369.992519444617,-7.45122812665857,3.84185689989449));
#42018=CARTESIAN_POINT('Ctrl Pts',(369.879144868317,-7.45708114798674,3.81701512666023));
#42019=CARTESIAN_POINT('Ctrl Pts',(369.766883981189,-7.46293416931491,3.78715340422476));
#42020=CARTESIAN_POINT('Ctrl Pts',(369.656206434648,-7.46878719064308,3.75240489358781));
#42021=CARTESIAN_POINT('Ctrl Pts',(369.545491975009,-7.4746421640669,3.71764479365149));
#42022=CARTESIAN_POINT('Ctrl Pts',(369.436362299972,-7.48049713749072,3.67799478834188));
#42023=CARTESIAN_POINT('Ctrl Pts',(369.329269826182,-7.48635211091454,3.63363721858656));
#42024=CARTESIAN_POINT('Ctrl Pts',(369.222055976828,-7.49221372019868,3.58922937522347));
#42025=CARTESIAN_POINT('Ctrl Pts',(369.11688431907,-7.49807532948283,3.54010347642571));
#42026=CARTESIAN_POINT('Ctrl Pts',(369.014185369185,-7.50393693876697,3.48648917114978));
#42027=CARTESIAN_POINT('Ctrl Pts',(368.911417168643,-7.50980250057731,3.43283871335409));
#42028=CARTESIAN_POINT('Ctrl Pts',(368.811125352605,-7.51566806238764,3.37469402922101));
#42029=CARTESIAN_POINT('Ctrl Pts',(368.713712510734,-7.52153362419797,3.31232878522059));
#42030=CARTESIAN_POINT('Ctrl Pts',(368.616157227395,-7.52740776289829,3.24987234793736));
#42031=CARTESIAN_POINT('Ctrl Pts',(368.521489656313,-7.53328190159861,3.18318327105412));
#42032=CARTESIAN_POINT('Ctrl Pts',(368.430080365508,-7.53915604029894,3.11257628061743));
#42033=CARTESIAN_POINT('Ctrl Pts',(368.406964448131,-7.54064151408028,3.094720925403));
#42034=CARTESIAN_POINT('Ctrl Pts',(368.384056717002,-7.54212698786162,3.07661520573756));
#42035=CARTESIAN_POINT('Ctrl Pts',(368.361362788011,-7.54361246164296,3.05826458067907));
#42036=CARTESIAN_POINT('Ctrl Pts',(368.272792509054,-7.5494099957431,2.9866454273343));
#42037=CARTESIAN_POINT('Ctrl Pts',(368.187169953114,-7.55520752984324,2.91104090485572));
#42038=CARTESIAN_POINT('Ctrl Pts',(368.104882304396,-7.56100506394338,2.83172572555944));
#42039=CARTESIAN_POINT('Ctrl Pts',(368.022701404712,-7.56679507709507,2.7525134392111));
#42040=CARTESIAN_POINT('Ctrl Pts',(367.943847116321,-7.57258509024677,2.66960035561438));
#42041=CARTESIAN_POINT('Ctrl Pts',(367.868675111064,-7.57837510339846,2.58330256181359));
#42042=CARTESIAN_POINT('Ctrl Pts',(367.791609172166,-7.58431099400346,2.49483052383489));
#42043=CARTESIAN_POINT('Ctrl Pts',(367.718413913144,-7.59024688460845,2.40280120236307));
#42044=CARTESIAN_POINT('Ctrl Pts',(367.649434223809,-7.59618277521345,2.30759729309164));
#42045=CARTESIAN_POINT('Ctrl Pts',(367.582267264402,-7.60196267545875,2.21489526484194));
#42046=CARTESIAN_POINT('Ctrl Pts',(367.519097337803,-7.60774257570405,2.11918379009273));
#42047=CARTESIAN_POINT('Ctrl Pts',(367.460202815846,-7.61352247594935,2.02085049287173));
#42048=CARTESIAN_POINT('Ctrl Pts',(367.401329349346,-7.619300309815,1.92255235091569));
#42049=CARTESIAN_POINT('Ctrl Pts',(367.346728467926,-7.62507814368065,1.821634613281));
#42050=CARTESIAN_POINT('Ctrl Pts',(367.296634832238,-7.63085597754629,1.71851326530402));
#42051=CARTESIAN_POINT('Ctrl Pts',(367.246546243089,-7.63663322934065,1.61540230599123));
#42052=CARTESIAN_POINT('Ctrl Pts',(367.200964181829,-7.64241048113501,1.51008856014474));
#42053=CARTESIAN_POINT('Ctrl Pts',(367.16007661686,-7.64818773292937,1.40301116781184));
#42054=CARTESIAN_POINT('Ctrl Pts',(367.117229971858,-7.65424179501179,1.29080328699221));
#42055=CARTESIAN_POINT('Ctrl Pts',(367.079539067204,-7.6602958570942,1.17665902241042));
#42056=CARTESIAN_POINT('Ctrl Pts',(367.04716232087,-7.66634991917662,1.06110412955548));
#42057=CARTESIAN_POINT('Ctrl Pts',(367.016232762133,-7.67213337458751,0.950714351380221));
#42058=CARTESIAN_POINT('Ctrl Pts',(366.990152592752,-7.67791682999841,0.83903776885068));
#42059=CARTESIAN_POINT('Ctrl Pts',(366.969007692485,-7.6837002854093,0.726544122050305));
#42060=CARTESIAN_POINT('Ctrl Pts',(366.947850984632,-7.68948697037646,0.613987657343232));
#42061=CARTESIAN_POINT('Ctrl Pts',(366.931635090475,-7.69527365534362,0.500613639997401));
#42062=CARTESIAN_POINT('Ctrl Pts',(366.920394058982,-7.70106034031079,0.386897315662876));
#42063=CARTESIAN_POINT('Ctrl Pts',(366.909138803071,-7.70685434775759,0.273037094524837));
#42064=CARTESIAN_POINT('Ctrl Pts',(366.902870989076,-7.7126483552044,0.158834124779586));
#42065=CARTESIAN_POINT('Ctrl Pts',(366.90157260312,-7.7184423626512,0.0447637999302818));
#42066=CARTESIAN_POINT('Ctrl Pts',(366.90139376975,-7.71924040107359,0.0290523078551138));
#42067=CARTESIAN_POINT('Ctrl Pts',(366.901309130825,-7.72003843949597,0.0133433237785408));
#42068=CARTESIAN_POINT('Ctrl Pts',(366.901318562436,-7.72083647791836,-0.00236191956903193));
#42069=CARTESIAN_POINT('',(366.901319333012,-8.9708364780123,0.00341174547326769));
#42070=CARTESIAN_POINT('Ctrl Pts',(366.901318562437,-7.72083647796505,-0.0023619204878646));
#42071=CARTESIAN_POINT('Ctrl Pts',(366.901402442653,-7.7279338449949,-0.142036744660448));
#42072=CARTESIAN_POINT('Ctrl Pts',(366.908926347075,-7.73503121202476,-0.281485965734132));
#42073=CARTESIAN_POINT('Ctrl Pts',(366.923821666102,-7.74212857905462,-0.420129230717656));
#42074=CARTESIAN_POINT('Ctrl Pts',(366.936148839964,-7.74800226844519,-0.534868608177298));
#42075=CARTESIAN_POINT('Ctrl Pts',(366.95355074276,-7.75387595783576,-0.649256079205153));
#42076=CARTESIAN_POINT('Ctrl Pts',(366.976000305937,-7.75974964722634,-0.762807121295737));
#42077=CARTESIAN_POINT('Ctrl Pts',(366.99842088462,-7.76561575313211,-0.876211558323485));
#42078=CARTESIAN_POINT('Ctrl Pts',(367.025876084103,-7.77148185903788,-0.988781312399423));
#42079=CARTESIAN_POINT('Ctrl Pts',(367.058287047345,-7.77734796494365,-1.10003652350796));
#42080=CARTESIAN_POINT('Ctrl Pts',(367.090664822173,-7.7832080640317,-1.21117781069763));
#42081=CARTESIAN_POINT('Ctrl Pts',(367.127988152016,-7.78906816311975,-1.32100683807669));
#42082=CARTESIAN_POINT('Ctrl Pts',(367.170127187901,-7.7949282622078,-1.42905415158391));
#42083=CARTESIAN_POINT('Ctrl Pts',(367.213786504066,-7.8009997803019,-1.54099956566681));
#42084=CARTESIAN_POINT('Ctrl Pts',(367.262615478618,-7.807071298396,-1.65103183515777));
#42085=CARTESIAN_POINT('Ctrl Pts',(367.316413133483,-7.81314281649011,-1.75864589466598));
#42086=CARTESIAN_POINT('Ctrl Pts',(367.368277795615,-7.81899618008686,-1.86239329501314));
#42087=CARTESIAN_POINT('Ctrl Pts',(367.424760025071,-7.82484954368361,-1.96389286992876));
#42088=CARTESIAN_POINT('Ctrl Pts',(367.485631165751,-7.83070290728036,-2.0627133754206));
#42089=CARTESIAN_POINT('Ctrl Pts',(367.546493166833,-7.83655539201427,-2.16151904334619));
#42090=CARTESIAN_POINT('Ctrl Pts',(367.611742552217,-7.84240787674818,-2.25764609000768));
#42091=CARTESIAN_POINT('Ctrl Pts',(367.681105897591,-7.84826036148209,-2.35068997591156));
#42092=CARTESIAN_POINT('Ctrl Pts',(367.750475602651,-7.85411338281026,-2.44374239269048));
#42093=CARTESIAN_POINT('Ctrl Pts',(367.823959770586,-7.85996640413844,-2.53371075551181));
#42094=CARTESIAN_POINT('Ctrl Pts',(367.901243474826,-7.86581942546662,-2.62022206898342));
#42095=CARTESIAN_POINT('Ctrl Pts',(367.978552954675,-7.87167439889044,-2.70676223564876));
#42096=CARTESIAN_POINT('Ctrl Pts',(368.059664215542,-7.87752937231427,-2.78984275234909));
#42097=CARTESIAN_POINT('Ctrl Pts',(368.144224628892,-7.88338434573809,-2.86912659957709));
#42098=CARTESIAN_POINT('Ctrl Pts',(368.228880880608,-7.88924595502225,-2.94850030486232));
#42099=CARTESIAN_POINT('Ctrl Pts',(368.31699378572,-7.89510756430641,-3.02406846933119));
#42100=CARTESIAN_POINT('Ctrl Pts',(368.408176642485,-7.90096917359057,-3.09553352841674));
#42101=CARTESIAN_POINT('Ctrl Pts',(368.499420984519,-7.90683473540091,-3.1670467769164));
#42102=CARTESIAN_POINT('Ctrl Pts',(368.593739064917,-7.91270029721125,-3.23445117118938));
#42103=CARTESIAN_POINT('Ctrl Pts',(368.690715590874,-7.91856585902159,-3.29749273552617));
#42104=CARTESIAN_POINT('Ctrl Pts',(368.787833920297,-7.92443999772192,-3.36062648209201));
#42105=CARTESIAN_POINT('Ctrl Pts',(368.887618098713,-7.93031413642226,-3.41938445795903));
#42106=CARTESIAN_POINT('Ctrl Pts',(368.989628625279,-7.93618827512259,-3.47355878780037));
#42107=CARTESIAN_POINT('Ctrl Pts',(369.015425422113,-7.93767374890381,-3.48725859141413));
#42108=CARTESIAN_POINT('Ctrl Pts',(369.041364498861,-7.93915922268503,-3.50066551228921));
#42109=CARTESIAN_POINT('Ctrl Pts',(369.067438566835,-7.94064469646626,-3.51377668432853));
#42110=CARTESIAN_POINT('Ctrl Pts',(369.170537644293,-7.94651838585683,-3.56561937120658));
#42111=CARTESIAN_POINT('Ctrl Pts',(369.276092070835,-7.95239207524741,-3.61300695171539));
#42112=CARTESIAN_POINT('Ctrl Pts',(369.383680024278,-7.95826576463798,-3.65569950751313));
#42113=CARTESIAN_POINT('Ctrl Pts',(369.491129071567,-7.96413187054375,-3.69833694321054));
#42114=CARTESIAN_POINT('Ctrl Pts',(369.600606044041,-7.96999797644951,-3.73629125797482));
#42115=CARTESIAN_POINT('Ctrl Pts',(369.711664962412,-7.97586408235528,-3.76936857931826));
#42116=CARTESIAN_POINT('Ctrl Pts',(369.822610157866,-7.98172418144332,-3.80241202990603));
#42117=CARTESIAN_POINT('Ctrl Pts',(369.935133683513,-7.98758428053137,-3.83058830328234));
#42118=CARTESIAN_POINT('Ctrl Pts',(370.048770661061,-7.99344437961942,-3.85375201704581));
#42119=CARTESIAN_POINT('Ctrl Pts',(370.16650740151,-7.99951589771352,-3.87775142475692));
#42120=CARTESIAN_POINT('Ctrl Pts',(370.285439032527,-8.00558741580763,-3.89636959407894));
#42121=CARTESIAN_POINT('Ctrl Pts',(370.405032191574,-8.01165893390173,-3.90950160771183));
#42122=CARTESIAN_POINT('Ctrl Pts',(370.52032827284,-8.01751229749849,-3.92216177760008));
#42123=CARTESIAN_POINT('Ctrl Pts',(370.63623871592,-8.02336566109525,-3.92972320188565));
#42124=CARTESIAN_POINT('Ctrl Pts',(370.752277186458,-8.02921902469201,-3.93214424061436));
#42125=CARTESIAN_POINT('Ctrl Pts',(370.86829823421,-8.03507150942593,-3.93456491583224));
#42126=CARTESIAN_POINT('Ctrl Pts',(370.984446858253,-8.04092399415985,-3.93184673152891));
#42127=CARTESIAN_POINT('Ctrl Pts',(371.100234894955,-8.04677647889376,-3.92400014359292));
#42128=CARTESIAN_POINT('Ctrl Pts',(371.216033547865,-8.05262950022194,-3.91615283623018));
#42129=CARTESIAN_POINT('Ctrl Pts',(371.331471135489,-8.05848252155013,-3.90317621844472));
#42130=CARTESIAN_POINT('Ctrl Pts',(371.446063502186,-8.06433554287831,-3.88513272115326));
#42131=CARTESIAN_POINT('Ctrl Pts',(371.56069408765,-8.07019051630214,-3.86708320600699));
#42132=CARTESIAN_POINT('Ctrl Pts',(371.67447848375,-8.07604548972597,-3.84396351528625));
#42133=CARTESIAN_POINT('Ctrl Pts',(371.786942327064,-8.08190046314981,-3.81588726403724));
#42134=CARTESIAN_POINT('Ctrl Pts',(371.899533633699,-8.08776207243397,-3.78777919196371));
#42135=CARTESIAN_POINT('Ctrl Pts',(372.010800999204,-8.09362368171813,-3.75470344704641));
#42136=CARTESIAN_POINT('Ctrl Pts',(372.120284743048,-8.0994852910023,-3.71682366521157));
#42137=CARTESIAN_POINT('Ctrl Pts',(372.229842312584,-8.10535085281265,-3.67891834076162));
#42138=CARTESIAN_POINT('Ctrl Pts',(372.337613482471,-8.11121641462301,-3.63620268088925));
#42139=CARTESIAN_POINT('Ctrl Pts',(372.44315970075,-8.11708197643337,-3.58888797674841));
#42140=CARTESIAN_POINT('Ctrl Pts',(372.548860253486,-8.12295611513371,-3.54150408690548));
#42141=CARTESIAN_POINT('Ctrl Pts',(372.652328993861,-8.12883025383405,-3.48950791632073));
#42142=CARTESIAN_POINT('Ctrl Pts',(372.753152985018,-8.13470439253439,-3.43315608980911));
#42143=CARTESIAN_POINT('Ctrl Pts',(372.778649726416,-8.13618986631557,-3.41890563283574));
#42144=CARTESIAN_POINT('Ctrl Pts',(372.803977487445,-8.13767534009675,-3.40437684241504));
#42145=CARTESIAN_POINT('Ctrl Pts',(372.829129908435,-8.13916081387793,-3.38957428955091));
#42146=CARTESIAN_POINT('Ctrl Pts',(372.928584715504,-8.14503450326849,-3.33104373935702));
#42147=CARTESIAN_POINT('Ctrl Pts',(373.025626929823,-8.15090819265906,-3.26803478452432));
#42148=CARTESIAN_POINT('Ctrl Pts',(373.119826272309,-8.15678188204962,-3.20077182352833));
#42149=CARTESIAN_POINT('Ctrl Pts',(373.213903994593,-8.16264798795536,-3.1335957053341));
#42150=CARTESIAN_POINT('Ctrl Pts',(373.30514581114,-8.1685140938611,-3.06217674129362));
#42151=CARTESIAN_POINT('Ctrl Pts',(373.39314703976,-8.17438019976685,-2.98678459118341));
#42152=CARTESIAN_POINT('Ctrl Pts',(373.481058156244,-8.18024029885488,-2.91146964167446));
#42153=CARTESIAN_POINT('Ctrl Pts',(373.565734973332,-8.18610039794291,-2.83218986585995));
#42154=CARTESIAN_POINT('Ctrl Pts',(373.646803310109,-8.19196049703093,-2.74925709143605));
#42155=CARTESIAN_POINT('Ctrl Pts',(373.73079640753,-8.19803201512504,-2.66333229171069));
#42156=CARTESIAN_POINT('Ctrl Pts',(373.810915369646,-8.20410353321915,-2.57348619555379));
#42157=CARTESIAN_POINT('Ctrl Pts',(373.886782892722,-8.21017505131326,-2.48011011502372));
#42158=CARTESIAN_POINT('Ctrl Pts',(373.959924435062,-8.21602841491001,-2.39008911169156));
#42159=CARTESIAN_POINT('Ctrl Pts',(374.029114512845,-8.22188177850675,-2.29678777682011));
#42160=CARTESIAN_POINT('Ctrl Pts',(374.094054489208,-8.22773514210349,-2.2005922075712));
#42161=CARTESIAN_POINT('Ctrl Pts',(374.158984715053,-8.23358762683738,-2.1044110817633));
#42162=CARTESIAN_POINT('Ctrl Pts',(374.219665877236,-8.23944011157128,-2.0053369279751));
#42163=CARTESIAN_POINT('Ctrl Pts',(374.275842123777,-8.24529259630518,-1.90378562217344));
#42164=CARTESIAN_POINT('Ctrl Pts',(374.332023520925,-8.25114561763334,-1.80222500548052));
#42165=CARTESIAN_POINT('Ctrl Pts',(374.383698981349,-8.25699863896151,-1.69818714681505));
#42166=CARTESIAN_POINT('Ctrl Pts',(374.43065850086,-8.26285166028968,-1.59211273035663));
#42167=CARTESIAN_POINT('Ctrl Pts',(374.477633682277,-8.26870663371349,-1.48600293603182));
#42168=CARTESIAN_POINT('Ctrl Pts',(374.519889628069,-8.2745616071373,-1.37785561086923));
#42169=CARTESIAN_POINT('Ctrl Pts',(374.557264652929,-8.28041658056112,-1.26813095797046));
#42170=CARTESIAN_POINT('Ctrl Pts',(374.59468203758,-8.28627818984526,-1.15828194627123));
#42171=CARTESIAN_POINT('Ctrl Pts',(374.627207326679,-8.29213979912941,-1.046852429996));
#42172=CARTESIAN_POINT('Ctrl Pts',(374.654728827592,-8.29800140841355,-0.934317390895616));
#42173=CARTESIAN_POINT('Ctrl Pts',(374.682268886454,-8.30386697022389,-0.821706468591917));
#42174=CARTESIAN_POINT('Ctrl Pts',(374.704798358474,-8.30973253203422,-0.707988943347631));
#42175=CARTESIAN_POINT('Ctrl Pts',(374.722257050076,-8.31559809384455,-0.59364787676059));
#42176=CARTESIAN_POINT('Ctrl Pts',(374.739741270567,-8.32147223254488,-0.479139615490211));
#42177=CARTESIAN_POINT('Ctrl Pts',(374.75213986865,-8.3273463712452,-0.364006402403479));
#42178=CARTESIAN_POINT('Ctrl Pts',(374.759444631172,-8.33322050994552,-0.248734350333146));
#42179=CARTESIAN_POINT('Ctrl Pts',(374.761291886363,-8.33470598372688,-0.219583930193503));
#42180=CARTESIAN_POINT('Ctrl Pts',(374.762813649909,-8.33619145750822,-0.190424618374459));
#42181=CARTESIAN_POINT('Ctrl Pts',(374.764010315222,-8.33767693128958,-0.161264236942478));
#42182=CARTESIAN_POINT('Ctrl Pts',(374.768742031421,-8.34355062068014,-0.0459616141751332));
#42183=CARTESIAN_POINT('Ctrl Pts',(374.768402619582,-8.34942431007071,0.069741473720703));
#42184=CARTESIAN_POINT('Ctrl Pts',(374.762947385123,-8.35529799946127,0.185361811307516));
#42185=CARTESIAN_POINT('Ctrl Pts',(374.757499193884,-8.36116410536702,0.300832872176412));
#42186=CARTESIAN_POINT('Ctrl Pts',(374.746948334513,-8.36703021127278,0.416220986286223));
#42187=CARTESIAN_POINT('Ctrl Pts',(374.731302022173,-8.37289631717853,0.531039910890018));
#42188=CARTESIAN_POINT('Ctrl Pts',(374.715671731458,-8.37875641626656,0.645741262377757));
#42189=CARTESIAN_POINT('Ctrl Pts',(374.694956421622,-8.3846165153546,0.759874176753556));
#42190=CARTESIAN_POINT('Ctrl Pts',(374.669215276891,-8.39047661444263,0.872955182096241));
#42191=CARTESIAN_POINT('Ctrl Pts',(374.642545450384,-8.39654813253674,0.99011589213267));
#42192=CARTESIAN_POINT('Ctrl Pts',(374.610480322117,-8.40261965063085,1.10614690796203));
#42193=CARTESIAN_POINT('Ctrl Pts',(374.573144174743,-8.40869116872496,1.22051904430707));
#42194=CARTESIAN_POINT('Ctrl Pts',(374.537149544982,-8.4145445323217,1.33078169838924));
#42195=CARTESIAN_POINT('Ctrl Pts',(374.496256300368,-8.42039789591845,1.43950220472217));
#42196=CARTESIAN_POINT('Ctrl Pts',(374.450626987493,-8.4262512595152,1.54622030946448));
#42197=CARTESIAN_POINT('Ctrl Pts',(374.405004525706,-8.4321037442491,1.65292239084248));
#42198=CARTESIAN_POINT('Ctrl Pts',(374.354647571982,-8.437956228983,1.75762228866674));
#42199=CARTESIAN_POINT('Ctrl Pts',(374.299766890365,-8.4438087137169,1.8598795581918));
#42200=CARTESIAN_POINT('Ctrl Pts',(374.244881176926,-8.44966173504508,1.96214620333555));
#42201=CARTESIAN_POINT('Ctrl Pts',(374.185471106465,-8.45551475637325,2.06196941092536));
#42202=CARTESIAN_POINT('Ctrl Pts',(374.121793144086,-8.46136777770143,2.15893381370774));
#42203=CARTESIAN_POINT('Ctrl Pts',(374.058093943877,-8.46722275112525,2.25593055599101));
#42204=CARTESIAN_POINT('Ctrl Pts',(373.990124247999,-8.47307772454907,2.3500662523921));
#42205=CARTESIAN_POINT('Ctrl Pts',(373.918183117588,-8.47893269797289,2.44095555700047));
#42206=CARTESIAN_POINT('Ctrl Pts',(373.846160451145,-8.48479430725704,2.5319478729613));
#42207=CARTESIAN_POINT('Ctrl Pts',(373.770157622778,-8.49065591654119,2.61968612920407));
#42208=CARTESIAN_POINT('Ctrl Pts',(373.690513213738,-8.49651752582534,2.70381897740561));
#42209=CARTESIAN_POINT('Ctrl Pts',(373.610815099888,-8.50238308763569,2.78800855700461));
#42210=CARTESIAN_POINT('Ctrl Pts',(373.52747081212,-8.50824864944603,2.86858760113921));
#42211=CARTESIAN_POINT('Ctrl Pts',(373.440853639376,-8.51411421125637,2.94524365639019));
#42212=CARTESIAN_POINT('Ctrl Pts',(373.354109811082,-8.5199883499567,3.02201180159505));
#42213=CARTESIAN_POINT('Ctrl Pts',(373.264083866595,-8.52586248865703,3.09484525070521));
#42214=CARTESIAN_POINT('Ctrl Pts',(373.171179837916,-8.53173662735736,3.16347357575554));
#42215=CARTESIAN_POINT('Ctrl Pts',(373.147685925732,-8.53322210113865,3.18082855879511));
#42216=CARTESIAN_POINT('Ctrl Pts',(373.124008089684,-8.53470757491995,3.19791484891524));
#42217=CARTESIAN_POINT('Ctrl Pts',(373.100153115988,-8.53619304870124,3.2147285362866));
#42218=CARTESIAN_POINT('Ctrl Pts',(373.005828525628,-8.54206673809182,3.2812112829856));
#42219=CARTESIAN_POINT('Ctrl Pts',(372.908418314537,-8.5479404274824,3.34364981695572));
#42220=CARTESIAN_POINT('Ctrl Pts',(372.808304303081,-8.55381411687297,3.40174462530341));
#42221=CARTESIAN_POINT('Ctrl Pts',(372.708319548219,-8.55968022277874,3.45976442779571));
#42222=CARTESIAN_POINT('Ctrl Pts',(372.605638289244,-8.5655463286845,3.51345145198771));
#42223=CARTESIAN_POINT('Ctrl Pts',(372.50067303116,-8.57141243459026,3.56254816402041));
#42224=CARTESIAN_POINT('Ctrl Pts',(372.395815256163,-8.57727253367831,3.61159460164546));
#42225=CARTESIAN_POINT('Ctrl Pts',(372.288678506103,-8.58313263276635,3.65605990263535));
#42226=CARTESIAN_POINT('Ctrl Pts',(372.179701130561,-8.5889927318544,3.69573170523268));
#42227=CARTESIAN_POINT('Ctrl Pts',(372.066792099926,-8.5950642499485,3.73683477596177));
#42228=CARTESIAN_POINT('Ctrl Pts',(371.951907515801,-8.60113576804261,3.77279171431096));
#42229=CARTESIAN_POINT('Ctrl Pts',(371.835559431533,-8.60720728613671,3.80342007959487));
#42230=CARTESIAN_POINT('Ctrl Pts',(371.723391826915,-8.61306064973347,3.83294794323661));
#42231=CARTESIAN_POINT('Ctrl Pts',(371.60986451545,-8.61891401333023,3.85752344941456));
#42232=CARTESIAN_POINT('Ctrl Pts',(371.495452370106,-8.62476737692699,3.87703367932076));
#42233=CARTESIAN_POINT('Ctrl Pts',(371.38105740336,-8.6306198616609,3.89654097983159));
#42234=CARTESIAN_POINT('Ctrl Pts',(371.265778274057,-8.63647234639481,3.91098444686756));
#42235=CARTESIAN_POINT('Ctrl Pts',(371.150099348566,-8.64232483112872,3.92030241782435));
#42236=CARTESIAN_POINT('Ctrl Pts',(371.034409816871,-8.6481778524569,3.92962124311395));
#42237=CARTESIAN_POINT('Ctrl Pts',(370.918320827953,-8.65403087378508,3.93381360495592));
#42238=CARTESIAN_POINT('Ctrl Pts',(370.802320450348,-8.65988389511326,3.93286983845248));
#42239=CARTESIAN_POINT('Ctrl Pts',(370.686281384377,-8.66573886853708,3.93192575718468));
#42240=CARTESIAN_POINT('Ctrl Pts',(370.570331401394,-8.67159384196091,3.92584214471076));
#42241=CARTESIAN_POINT('Ctrl Pts',(370.454956434475,-8.67744881538473,3.91466140476607));
#42242=CARTESIAN_POINT('Ctrl Pts',(370.339450704851,-8.68331042466889,3.90346799288874));
#42243=CARTESIAN_POINT('Ctrl Pts',(370.224521703509,-8.68917203395306,3.88716596299029));
#42244=CARTESIAN_POINT('Ctrl Pts',(370.110648219318,-8.69503364323723,3.86584935828623));
#42245=CARTESIAN_POINT('Ctrl Pts',(369.9966979494,-8.70089920504758,3.84451837963907));
#42246=CARTESIAN_POINT('Ctrl Pts',(369.883805015206,-8.70676476685793,3.81816618682113));
#42247=CARTESIAN_POINT('Ctrl Pts',(369.772434337282,-8.71263032866828,3.78693707348965));
#42248=CARTESIAN_POINT('Ctrl Pts',(369.660900808111,-8.71850446736863,3.75566229553502));
#42249=CARTESIAN_POINT('Ctrl Pts',(369.55089436854,-8.72437860606897,3.71949649341231));
#42250=CARTESIAN_POINT('Ctrl Pts',(369.442861290902,-8.73025274476931,3.67863257681035));
#42251=CARTESIAN_POINT('Ctrl Pts',(369.415541489222,-8.73173821855051,3.6682987594108));
#42252=CARTESIAN_POINT('Ctrl Pts',(369.388347765434,-8.7332236923317,3.65766472835756));
#42253=CARTESIAN_POINT('Ctrl Pts',(369.361287083872,-8.73470916611289,3.64673406660575));
#42254=CARTESIAN_POINT('Ctrl Pts',(369.254286852561,-8.74058285550345,3.60351330244529));
#42255=CARTESIAN_POINT('Ctrl Pts',(369.149012260597,-8.74645654489401,3.55550726078663));
#42256=CARTESIAN_POINT('Ctrl Pts',(369.045921979465,-8.75233023428457,3.50287441949075));
#42257=CARTESIAN_POINT('Ctrl Pts',(368.942964797571,-8.75819634019032,3.45030953213762));
#42258=CARTESIAN_POINT('Ctrl Pts',(368.842186682757,-8.76406244609607,3.39312991089222));
#42259=CARTESIAN_POINT('Ctrl Pts',(368.744027665632,-8.76992855200182,3.33154257539275));
#42260=CARTESIAN_POINT('Ctrl Pts',(368.645969162089,-8.77578865108985,3.27001830454031));
#42261=CARTESIAN_POINT('Ctrl Pts',(368.550524769553,-8.78164875017787,3.20409551531753));
#42262=CARTESIAN_POINT('Ctrl Pts',(368.458110570752,-8.7875088492659,3.13402743298867));
#42263=CARTESIAN_POINT('Ctrl Pts',(368.362362278488,-8.79358036736001,3.06143145410011));
#42264=CARTESIAN_POINT('Ctrl Pts',(368.269867355309,-8.79965188545412,2.98438563480252));
#42265=CARTESIAN_POINT('Ctrl Pts',(368.181056696544,-8.80572340354823,2.90322135471163));
#42266=CARTESIAN_POINT('Ctrl Pts',(368.095437075725,-8.81157676714497,2.82497337206943));
#42267=CARTESIAN_POINT('Ctrl Pts',(368.01324184973,-8.81743013074171,2.7428980970104));
#42268=CARTESIAN_POINT('Ctrl Pts',(367.934823338273,-8.82328349433845,2.65733335465643));
#42269=CARTESIAN_POINT('Ctrl Pts',(367.856416601092,-8.82913597907235,2.57178145956058));
#42270=CARTESIAN_POINT('Ctrl Pts',(367.781785729985,-8.83498846380625,2.48274144344072));
#42271=CARTESIAN_POINT('Ctrl Pts',(367.711245120138,-8.84084094854014,2.39058689527376));
#42272=CARTESIAN_POINT('Ctrl Pts',(367.640698042664,-8.84669396986833,2.29842389777182));
#42273=CARTESIAN_POINT('Ctrl Pts',(367.574242223094,-8.85254699119651,2.2031461286382));
#42274=CARTESIAN_POINT('Ctrl Pts',(367.512150369513,-8.85840001252469,2.1051584762604));
#42275=CARTESIAN_POINT('Ctrl Pts',(367.450037807099,-8.86425498594849,2.00713814310867));
#42276=CARTESIAN_POINT('Ctrl Pts',(367.392292325824,-8.87010995937229,1.90640647834122));
#42277=CARTESIAN_POINT('Ctrl Pts',(367.339141722438,-8.87596493279609,1.80339480280505));
#42278=CARTESIAN_POINT('Ctrl Pts',(367.28593087967,-8.88182654208024,1.70026637676576));
#42279=CARTESIAN_POINT('Ctrl Pts',(367.237325498601,-8.88768815136438,1.59485314960982));
#42280=CARTESIAN_POINT('Ctrl Pts',(367.193506109978,-8.89354976064853,1.48760843310357));
#42281=CARTESIAN_POINT('Ctrl Pts',(367.149657173619,-8.89941532245886,1.38029140069752));
#42282=CARTESIAN_POINT('Ctrl Pts',(367.110600794683,-8.90528088426918,1.27114080783832));
#42283=CARTESIAN_POINT('Ctrl Pts',(367.076467759926,-8.91114644607951,1.16062555387311));
#42284=CARTESIAN_POINT('Ctrl Pts',(367.042284814301,-8.91702058477984,1.04994869950075));
#42285=CARTESIAN_POINT('Ctrl Pts',(367.013039684462,-8.92289472348017,0.937903599782908));
#42286=CARTESIAN_POINT('Ctrl Pts',(366.988812195358,-8.9287688621805,0.824969839038923));
#42287=CARTESIAN_POINT('Ctrl Pts',(366.982685458881,-8.93025433596185,0.796410734602832));
#42288=CARTESIAN_POINT('Ctrl Pts',(366.976879342316,-8.9317398097432,0.767794825732123));
#42289=CARTESIAN_POINT('Ctrl Pts',(366.971394610312,-8.93322528352455,0.739129906964237));
#42290=CARTESIAN_POINT('Ctrl Pts',(366.939445662096,-8.9418782723808,0.57215474673101));
#42291=CARTESIAN_POINT('Ctrl Pts',(366.918315437461,-8.95053126123704,0.40304846186944));
#42292=CARTESIAN_POINT('Ctrl Pts',(366.908222919179,-8.95918425009329,0.232954005898987));
#42293=CARTESIAN_POINT('Ctrl Pts',(366.903692680176,-8.96306832605054,0.156603533493056));
#42294=CARTESIAN_POINT('Ctrl Pts',(366.901385817882,-8.9669524020078,0.08005428134596));
#42295=CARTESIAN_POINT('Ctrl Pts',(366.901319333012,-8.97083647796505,0.00341174640567556));
#42296=CARTESIAN_POINT('',(366.901317864546,-10.2208364779364,0.000298426845041825));
#42297=CARTESIAN_POINT('Ctrl Pts',(366.901319333012,-8.9708364780123,0.00341174547327817));
#42298=CARTESIAN_POINT('Ctrl Pts',(366.901220434153,-8.97661419535868,-0.110597071159494));
#42299=CARTESIAN_POINT('Ctrl Pts',(366.906083007808,-8.98239191270507,-0.224772387134529));
#42300=CARTESIAN_POINT('Ctrl Pts',(366.915923782789,-8.98816963005145,-0.338639792082648));
#42301=CARTESIAN_POINT('Ctrl Pts',(366.926112765496,-8.99415178717165,-0.45653630145333));
#42302=CARTESIAN_POINT('Ctrl Pts',(366.941638841141,-9.00013394429185,-0.57410224769329));
#42303=CARTESIAN_POINT('Ctrl Pts',(366.962461634196,-9.00611610141205,-0.690809973273278));
#42304=CARTESIAN_POINT('Ctrl Pts',(366.982542839518,-9.0118852086149,-0.803361243115248));
#42305=CARTESIAN_POINT('Ctrl Pts',(367.007549840669,-9.01765431581776,-0.915113919845186));
#42306=CARTESIAN_POINT('Ctrl Pts',(367.037393713836,-9.02342342302062,-1.0256003508848));
#42307=CARTESIAN_POINT('Ctrl Pts',(367.067229917836,-9.02919104769962,-1.1360583895296));
#42308=CARTESIAN_POINT('Ctrl Pts',(367.101900412987,-9.03495867237862,-1.24525041765691));
#42309=CARTESIAN_POINT('Ctrl Pts',(367.141265616119,-9.04072629705762,-1.35272102593688));
#42310=CARTESIAN_POINT('Ctrl Pts',(367.180630876692,-9.04649393015267,-1.46019179103654));
#42311=CARTESIAN_POINT('Ctrl Pts',(367.224690711424,-9.05226156324771,-1.56594073115193));
#42312=CARTESIAN_POINT('Ctrl Pts',(367.273256621578,-9.05802919634276,-1.66953044430808));
#42313=CARTESIAN_POINT('Ctrl Pts',(367.321835155203,-9.06379832858696,-1.77314708296887));
#42314=CARTESIAN_POINT('Ctrl Pts',(367.37492190967,-9.06956746083117,-1.8746029939876));
#42315=CARTESIAN_POINT('Ctrl Pts',(367.432281886025,-9.07533659307538,-1.97348429886904));
#42316=CARTESIAN_POINT('Ctrl Pts',(367.489703183547,-9.08111189285922,-2.07247131364609));
#42317=CARTESIAN_POINT('Ctrl Pts',(367.551406604029,-9.08688719264307,-2.16887786140994));
#42318=CARTESIAN_POINT('Ctrl Pts',(367.617113228884,-9.09266249242691,-2.262318148521));
#42319=CARTESIAN_POINT('Ctrl Pts',(367.682861813838,-9.09844148030378,-2.3558181063823));
#42320=CARTESIAN_POINT('Ctrl Pts',(367.752618429645,-9.10422046818064,-2.44634769830393));
#42321=CARTESIAN_POINT('Ctrl Pts',(367.8260644028,-9.10999945605751,-2.53355485001079));
#42322=CARTESIAN_POINT('Ctrl Pts',(367.899616566023,-9.11578679934301,-2.62088808805033));
#42323=CARTESIAN_POINT('Ctrl Pts',(367.976868439654,-9.12157414262851,-2.70488899160559));
#42324=CARTESIAN_POINT('Ctrl Pts',(368.057465231478,-9.127361485914,-2.78524299067516));
#42325=CARTESIAN_POINT('Ctrl Pts',(368.077797364424,-9.12882145758807,-2.80551387435225));
#42326=CARTESIAN_POINT('Ctrl Pts',(368.098342209705,-9.13028142926214,-2.8255528739549));
#42327=CARTESIAN_POINT('Ctrl Pts',(368.11909376202,-9.13174140093621,-2.84535536173312));
#42328=CARTESIAN_POINT('Ctrl Pts',(368.202580431545,-9.13761509032677,-2.92502379944022));
#42329=CARTESIAN_POINT('Ctrl Pts',(368.289715492768,-9.14348877971733,-3.00114738878479));
#42330=CARTESIAN_POINT('Ctrl Pts',(368.380165479798,-9.1493624691079,-3.07337357443067));
#42331=CARTESIAN_POINT('Ctrl Pts',(368.470498687398,-9.15522857501364,-3.14550650928551));
#42332=CARTESIAN_POINT('Ctrl Pts',(368.564137989628,-9.16109468091939,-3.21375179182564));
#42333=CARTESIAN_POINT('Ctrl Pts',(368.660713379682,-9.16696078682514,-3.27779386060144));
#42334=CARTESIAN_POINT('Ctrl Pts',(368.757189877765,-9.17282088591317,-3.3417703511146));
#42335=CARTESIAN_POINT('Ctrl Pts',(368.856596141189,-9.1786809850012,-3.4015519619796));
#42336=CARTESIAN_POINT('Ctrl Pts',(368.958529938369,-9.18454108408922,-3.45686399768413));
#42337=CARTESIAN_POINT('Ctrl Pts',(369.064141274403,-9.19061260218333,-3.51417156545006));
#42338=CARTESIAN_POINT('Ctrl Pts',(369.172465609875,-9.19668412027744,-3.56668068303703));
#42339=CARTESIAN_POINT('Ctrl Pts',(369.283023402244,-9.20275563837155,-3.6141353774254));
#42340=CARTESIAN_POINT('Ctrl Pts',(369.389608764777,-9.20860900196829,-3.65988498671947));
#42341=CARTESIAN_POINT('Ctrl Pts',(369.498269434401,-9.21446236556504,-3.70093696388293));
#42342=CARTESIAN_POINT('Ctrl Pts',(369.608552387805,-9.22031572916178,-3.73710958145271));
#42343=CARTESIAN_POINT('Ctrl Pts',(369.718818782594,-9.22616821389568,-3.77327676782572));
#42344=CARTESIAN_POINT('Ctrl Pts',(369.83070658437,-9.23202069862958,-3.80456592260076));
#42345=CARTESIAN_POINT('Ctrl Pts',(369.943745819968,-9.23787318336348,-3.83084461360448));
#42346=CARTESIAN_POINT('Ctrl Pts',(370.056795419746,-9.24372620469165,-3.85712571401131));
#42347=CARTESIAN_POINT('Ctrl Pts',(370.170996260775,-9.24957922601982,-3.87839534386206));
#42348=CARTESIAN_POINT('Ctrl Pts',(370.285867038557,-9.25543224734799,-3.89457195387263));
#42349=CARTESIAN_POINT('Ctrl Pts',(370.400776127962,-9.26128722077182,-3.91075395909506));
#42350=CARTESIAN_POINT('Ctrl Pts',(370.516355189526,-9.26714219419565,-3.92183950926494));
#42351=CARTESIAN_POINT('Ctrl Pts',(370.63211735073,-9.27299716761947,-3.92779886918755));
#42352=CARTESIAN_POINT('Ctrl Pts',(370.748010713473,-9.27885877690362,-3.93376498327918));
#42353=CARTESIAN_POINT('Ctrl Pts',(370.864087177224,-9.28472038618776,-3.93459328970434));
#42354=CARTESIAN_POINT('Ctrl Pts',(370.979859318703,-9.29058199547191,-3.93030618168944));
#42355=CARTESIAN_POINT('Ctrl Pts',(371.095709526187,-9.29644755728224,-3.92601618284613));
#42356=CARTESIAN_POINT('Ctrl Pts',(371.211254592026,-9.30231311909258,-3.91660393457928));
#42357=CARTESIAN_POINT('Ctrl Pts',(371.326013397635,-9.30817868090291,-3.90214357649817));
#42358=CARTESIAN_POINT('Ctrl Pts',(371.440940008765,-9.31405281960324,-3.88766207382687));
#42359=CARTESIAN_POINT('Ctrl Pts',(371.55507765949,-9.31992695830357,-3.86811779903549));
#42360=CARTESIAN_POINT('Ctrl Pts',(371.667956504604,-9.3258010970039,-3.8436357266169));
#42361=CARTESIAN_POINT('Ctrl Pts',(371.696501721773,-9.32728657078522,-3.83744461017491));
#42362=CARTESIAN_POINT('Ctrl Pts',(371.72496652159,-9.32877204456654,-3.8309379673117));
#42363=CARTESIAN_POINT('Ctrl Pts',(371.753343487414,-9.33025751834786,-3.82411831455329));
#42364=CARTESIAN_POINT('Ctrl Pts',(371.865548418386,-9.33613120773843,-3.79715282882194));
#42365=CARTESIAN_POINT('Ctrl Pts',(371.976752413301,-9.342004897129,-3.76519987490544));
#42366=CARTESIAN_POINT('Ctrl Pts',(372.086478442113,-9.34787858651956,-3.728348543207));
#42367=CARTESIAN_POINT('Ctrl Pts',(372.196062804313,-9.35374469242532,-3.69154479003982));
#42368=CARTESIAN_POINT('Ctrl Pts',(372.30417260711,-9.35961079833107,-3.64985536631478));
#42369=CARTESIAN_POINT('Ctrl Pts',(372.41034209753,-9.36547690423682,-3.60342012279424));
#42370=CARTESIAN_POINT('Ctrl Pts',(372.516402871746,-9.37133700332487,-3.5570324283714));
#42371=CARTESIAN_POINT('Ctrl Pts',(372.62052690933,-9.37719710241292,-3.50590874498824));
#42372=CARTESIAN_POINT('Ctrl Pts',(372.722265327923,-9.38305720150097,-3.45023815595081));
#42373=CARTESIAN_POINT('Ctrl Pts',(372.827674236555,-9.38912871959508,-3.392559099066));
#42374=CARTESIAN_POINT('Ctrl Pts',(372.930521712646,-9.39520023768918,-3.32999900198444));
#42375=CARTESIAN_POINT('Ctrl Pts',(373.030332695486,-9.40127175578329,-3.26282206265745));
#42376=CARTESIAN_POINT('Ctrl Pts',(373.126557389946,-9.40712511938004,-3.19805884444691));
#42377=CARTESIAN_POINT('Ctrl Pts',(373.219959670976,-9.4129784829768,-3.12900509834453));
#42378=CARTESIAN_POINT('Ctrl Pts',(373.310141243316,-9.41883184657355,-3.05594298720925));
#42379=CARTESIAN_POINT('Ctrl Pts',(373.400309275196,-9.42468433130745,-2.98289184610411));
#42380=CARTESIAN_POINT('Ctrl Pts',(373.487257238995,-9.43053681604136,-2.90583379665994));
#42381=CARTESIAN_POINT('Ctrl Pts',(373.570619073994,-9.43638930077526,-2.82509196827481));
#42382=CARTESIAN_POINT('Ctrl Pts',(373.653988552155,-9.44224232210342,-2.74434273694828));
#42383=CARTESIAN_POINT('Ctrl Pts',(373.733770951112,-9.44809534343159,-2.65990934271192));
#42384=CARTESIAN_POINT('Ctrl Pts',(373.809636824618,-9.45394836475975,-2.57215202086995));
#42385=CARTESIAN_POINT('Ctrl Pts',(373.885528000857,-9.45980333818357,-2.4843654302663));
#42386=CARTESIAN_POINT('Ctrl Pts',(373.957499784203,-9.46565831160738,-2.39325302004316));
#42387=CARTESIAN_POINT('Ctrl Pts',(374.025263249713,-9.4715132850312,-2.2992077932684));
#42388=CARTESIAN_POINT('Ctrl Pts',(374.093103516408,-9.47737489431535,-2.20505597830862));
#42389=CARTESIAN_POINT('Ctrl Pts',(374.1567257038,-9.4832365035995,-2.10796504773429));
#42390=CARTESIAN_POINT('Ctrl Pts',(374.215884392299,-9.48909811288366,-2.00835672673192));
#42391=CARTESIAN_POINT('Ctrl Pts',(374.275082971936,-9.49496367469401,-1.90868123910711));
#42392=CARTESIAN_POINT('Ctrl Pts',(374.329811864999,-9.50082923650436,-1.80648534427119));
#42393=CARTESIAN_POINT('Ctrl Pts',(374.379872552623,-9.5066947983147,-1.70221352173318));
#42394=CARTESIAN_POINT('Ctrl Pts',(374.43000644125,-9.51256893701503,-1.59778922821634));
#42395=CARTESIAN_POINT('Ctrl Pts',(374.475458339797,-9.51844307571537,-1.49128332740049));
#42396=CARTESIAN_POINT('Ctrl Pts',(374.516078557755,-9.5243172144157,-1.38315838376092));
#42397=CARTESIAN_POINT('Ctrl Pts',(374.526350747747,-9.52580268819698,-1.35581535066756));
#42398=CARTESIAN_POINT('Ctrl Pts',(374.5363142034,-9.52728816197824,-1.32836884303156));
#42399=CARTESIAN_POINT('Ctrl Pts',(374.545967018738,-9.52877363575952,-1.30082645734895));
#42400=CARTESIAN_POINT('Ctrl Pts',(374.584135069736,-9.53464732515008,-1.19192152707408));
#42401=CARTESIAN_POINT('Ctrl Pts',(374.617569495124,-9.54052101454064,-1.08115393728371));
#42402=CARTESIAN_POINT('Ctrl Pts',(374.646086555742,-9.5463947039312,-0.968972836823832));
#42403=CARTESIAN_POINT('Ctrl Pts',(374.674566798156,-9.55226080983695,-0.856936572703568));
#42404=CARTESIAN_POINT('Ctrl Pts',(374.698142200584,-9.5581269157427,-0.743490823943879));
#42405=CARTESIAN_POINT('Ctrl Pts',(374.716677791602,-9.56399302164845,-0.629102780851182));
#42406=CARTESIAN_POINT('Ctrl Pts',(374.735194402412,-9.56985312073649,-0.514831869657354));
#42407=CARTESIAN_POINT('Ctrl Pts',(374.748681401187,-9.57571321982452,-0.399620988792879));
#42408=CARTESIAN_POINT('Ctrl Pts',(374.757054332714,-9.58157331891256,-0.28394984148724));
#42409=CARTESIAN_POINT('Ctrl Pts',(374.765729340509,-9.58764483700666,-0.164105543074864));
#42410=CARTESIAN_POINT('Ctrl Pts',(374.768914194981,-9.59371635510078,-0.0437675782129017));
#42411=CARTESIAN_POINT('Ctrl Pts',(374.766573368814,-9.59978787319488,0.0765216316346329));
#42412=CARTESIAN_POINT('Ctrl Pts',(374.764316650403,-9.60564123679164,0.192488754039612));
#42413=CARTESIAN_POINT('Ctrl Pts',(374.75692451057,-9.61149460038838,0.308410116268769));
#42414=CARTESIAN_POINT('Ctrl Pts',(374.744418133333,-9.61734796398514,0.423798064520112));
#42415=CARTESIAN_POINT('Ctrl Pts',(374.731913633886,-9.62320044871903,0.539168687659114));
#42416=CARTESIAN_POINT('Ctrl Pts',(374.714296468386,-9.62905293345293,0.654005645440778));
#42417=CARTESIAN_POINT('Ctrl Pts',(374.691639720005,-9.63490541818682,0.767826162651834));
#42418=CARTESIAN_POINT('Ctrl Pts',(374.668980894304,-9.64075843951499,0.881657115676215));
#42419=CARTESIAN_POINT('Ctrl Pts',(374.641281647847,-9.64661146084317,0.99447103765158));
#42420=CARTESIAN_POINT('Ctrl Pts',(374.608666093242,-9.65246448217134,1.10579580532458));
#42421=CARTESIAN_POINT('Ctrl Pts',(374.576039660719,-9.65831945559515,1.21715770195731));
#42422=CARTESIAN_POINT('Ctrl Pts',(374.538493775707,-9.66417442901895,1.32702906043275));
#42423=CARTESIAN_POINT('Ctrl Pts',(374.496202052808,-9.67002940244276,1.43495404415433));
#42424=CARTESIAN_POINT('Ctrl Pts',(374.453862397674,-9.67589101172692,1.54300134698282));
#42425=CARTESIAN_POINT('Ctrl Pts',(374.406766319716,-9.68175262101108,1.64909748720203));
#42426=CARTESIAN_POINT('Ctrl Pts',(374.355135153625,-9.68761423029524,1.75280761556911));
#42427=CARTESIAN_POINT('Ctrl Pts',(374.303469172259,-9.69347979210557,1.85658767643717));
#42428=CARTESIAN_POINT('Ctrl Pts',(374.247262213333,-9.6993453539159,1.95797816132318));
#42429=CARTESIAN_POINT('Ctrl Pts',(374.186780157501,-9.70521091572624,2.05657129669788));
#42430=CARTESIAN_POINT('Ctrl Pts',(374.126209662069,-9.71108505442656,2.15530859941809));
#42431=CARTESIAN_POINT('Ctrl Pts',(374.061351824335,-9.71695919312688,2.25124004824819));
#42432=CARTESIAN_POINT('Ctrl Pts',(373.992514192211,-9.72283333182721,2.34398909647804));
#42433=CARTESIAN_POINT('Ctrl Pts',(373.975106278829,-9.72431880560853,2.36744381663647));
#42434=CARTESIAN_POINT('Ctrl Pts',(373.957444047156,-9.72580427938985,2.39069519944109));
#42435=CARTESIAN_POINT('Ctrl Pts',(373.939532847338,-9.72728975317117,2.41373752515246));
#42436=CARTESIAN_POINT('Ctrl Pts',(373.868710443291,-9.73316344256175,2.50484883641686));
#42437=CARTESIAN_POINT('Ctrl Pts',(373.793756688372,-9.73903713195232,2.59299221037434));
#42438=CARTESIAN_POINT('Ctrl Pts',(373.714949399135,-9.7449108213429,2.67776976170557));
#42439=CARTESIAN_POINT('Ctrl Pts',(373.636243857511,-9.75077692724865,2.76243785725346));
#42440=CARTESIAN_POINT('Ctrl Pts',(373.553694954478,-9.75664303315441,2.84374847230078));
#42441=CARTESIAN_POINT('Ctrl Pts',(373.467622104424,-9.76250913906017,2.92133492099278));
#42442=CARTESIAN_POINT('Ctrl Pts',(373.381637391872,-9.76836923814823,2.99884192214994));
#42443=CARTESIAN_POINT('Ctrl Pts',(373.292136214908,-9.77422933723629,3.07263206734381));
#42444=CARTESIAN_POINT('Ctrl Pts',(373.199475887948,-9.78008943632435,3.1423743365141));
#42445=CARTESIAN_POINT('Ctrl Pts',(373.103472587783,-9.78616095441845,3.21463274764817));
#42446=CARTESIAN_POINT('Ctrl Pts',(373.004078191493,-9.79223247251256,3.28254536114066));
#42447=CARTESIAN_POINT('Ctrl Pts',(372.901729240396,-9.79830399060666,3.34578827127365));
#42448=CARTESIAN_POINT('Ctrl Pts',(372.803057768906,-9.80415735420342,3.40675881310319));
#42449=CARTESIAN_POINT('Ctrl Pts',(372.701640789256,-9.81001071780017,3.46338921298782));
#42450=CARTESIAN_POINT('Ctrl Pts',(372.597899564819,-9.81586408139693,3.51543291025817));
#42451=CARTESIAN_POINT('Ctrl Pts',(372.494173916778,-9.82171656613084,3.56746879334252));
#42452=CARTESIAN_POINT('Ctrl Pts',(372.38812508703,-9.82756905086475,3.61491915795601));
#42453=CARTESIAN_POINT('Ctrl Pts',(372.280198374458,-9.83342153559866,3.65758369942712));
#42454=CARTESIAN_POINT('Ctrl Pts',(372.172261766456,-9.83927455692684,3.70025215266382));
#42455=CARTESIAN_POINT('Ctrl Pts',(372.062447317594,-9.84512757825502,3.73813375858133));
#42456=CARTESIAN_POINT('Ctrl Pts',(371.951219039372,-9.8509805995832,3.77107686747186));
#42457=CARTESIAN_POINT('Ctrl Pts',(371.839953664371,-9.85683557300702,3.80403096352541));
#42458=CARTESIAN_POINT('Ctrl Pts',(371.727273918296,-9.86269054643084,3.83204317013627));
#42459=CARTESIAN_POINT('Ctrl Pts',(371.613656962345,-9.86854551985467,3.85501226366336));
#42460=CARTESIAN_POINT('Ctrl Pts',(371.499911236167,-9.87440712913882,3.87800738970768));
#42461=CARTESIAN_POINT('Ctrl Pts',(371.385226585191,-9.88026873842297,3.89594791252142));
#42462=CARTESIAN_POINT('Ctrl Pts',(371.270088404287,-9.88613034770712,3.90878408547029));
#42463=CARTESIAN_POINT('Ctrl Pts',(371.154872584862,-9.89199590951749,3.9216289139449));
#42464=CARTESIAN_POINT('Ctrl Pts',(371.039203037761,-9.89786147132785,3.92936251147408));
#42465=CARTESIAN_POINT('Ctrl Pts',(370.923566554713,-9.90372703313821,3.93198724174972));
#42466=CARTESIAN_POINT('Ctrl Pts',(370.807760982765,-9.90960117183855,3.93461581002477));
#42467=CARTESIAN_POINT('Ctrl Pts',(370.69198898282,-9.9154753105389,3.93212061084011));
#42468=CARTESIAN_POINT('Ctrl Pts',(370.576733694681,-9.92134944923924,3.92455594956524));
#42469=CARTESIAN_POINT('Ctrl Pts',(370.547587513869,-9.92283492302045,3.92264297022295));
#42470=CARTESIAN_POINT('Ctrl Pts',(370.518474330667,-9.92432039680165,3.92040605411119));
#42471=CARTESIAN_POINT('Ctrl Pts',(370.489401851781,-9.92580587058285,3.91784659627567));
#42472=CARTESIAN_POINT('Ctrl Pts',(370.374446803131,-9.93167955997341,3.90772628279431));
#42473=CARTESIAN_POINT('Ctrl Pts',(370.259746090888,-9.93755324936398,3.89252541571314));
#42474=CARTESIAN_POINT('Ctrl Pts',(370.145784668205,-9.94342693875455,3.87226174904637));
#42475=CARTESIAN_POINT('Ctrl Pts',(370.031970380425,-9.94929304466028,3.85202424467705));
#42476=CARTESIAN_POINT('Ctrl Pts',(369.918893887083,-9.955159150566,3.82673701144358));
#42477=CARTESIAN_POINT('Ctrl Pts',(369.807036474757,-9.96102525647173,3.79646967187357));
#42478=CARTESIAN_POINT('Ctrl Pts',(369.695293602997,-9.96688535555974,3.76623332567367));
#42479=CARTESIAN_POINT('Ctrl Pts',(369.584767725666,-9.97274545464776,3.7310271238657));
#42480=CARTESIAN_POINT('Ctrl Pts',(369.475930705063,-9.97860555373578,3.6909718714331));
#42481=CARTESIAN_POINT('Ctrl Pts',(369.363167093052,-9.98467707182989,3.64947151687319));
#42482=CARTESIAN_POINT('Ctrl Pts',(369.252216943441,-9.99074858992401,3.60276569939484));
#42483=CARTESIAN_POINT('Ctrl Pts',(369.143589089944,-9.99682010801812,3.55104565572135));
#42484=CARTESIAN_POINT('Ctrl Pts',(369.038864322037,-10.0026734716149,3.50118395455078));
#42485=CARTESIAN_POINT('Ctrl Pts',(368.936298243377,-10.0085268352116,3.44666234910111));
#42486=CARTESIAN_POINT('Ctrl Pts',(368.836326411713,-10.0143801988084,3.38770116740654));
#42487=CARTESIAN_POINT('Ctrl Pts',(368.736369590482,-10.0202326835422,3.32874883853505));
#42488=CARTESIAN_POINT('Ctrl Pts',(368.639006597507,-10.0260851682761,3.26535846866901));
#42489=CARTESIAN_POINT('Ctrl Pts',(368.544647151135,-10.03193765301,3.19779565888662));
#42490=CARTESIAN_POINT('Ctrl Pts',(368.450279053268,-10.0377906743382,3.13022665450154));
#42491=CARTESIAN_POINT('Ctrl Pts',(368.358915385376,-10.0436436956664,3.05848469024652));
#42492=CARTESIAN_POINT('Ctrl Pts',(368.270935124946,-10.0494967169946,2.98287746787704));
#42493=CARTESIAN_POINT('Ctrl Pts',(368.182925521401,-10.0553516904184,2.90724502903869));
#42494=CARTESIAN_POINT('Ctrl Pts',(368.098301882323,-10.0612066638422,2.82774503781916));
#42495=CARTESIAN_POINT('Ctrl Pts',(368.017407940355,-10.0670616372661,2.74472358221788));
#42496=CARTESIAN_POINT('Ctrl Pts',(367.936422315496,-10.0729232465502,2.66160803246076));
#42497=CARTESIAN_POINT('Ctrl Pts',(367.859175113332,-10.0787848558343,2.57496334834159));
#42498=CARTESIAN_POINT('Ctrl Pts',(367.785971273526,-10.0846464651185,2.48517044285603));
#42499=CARTESIAN_POINT('Ctrl Pts',(367.712718071834,-10.0905120269288,2.39531698935458));
#42500=CARTESIAN_POINT('Ctrl Pts',(367.643513907526,-10.0963775887392,2.30231141801826));
#42501=CARTESIAN_POINT('Ctrl Pts',(367.578620688798,-10.1022431505495,2.20656406513605));
#42502=CARTESIAN_POINT('Ctrl Pts',(367.513632580269,-10.1081172892499,2.11067670614044));
#42503=CARTESIAN_POINT('Ctrl Pts',(367.452968213445,-10.1139914279502,2.01203991489076));
#42504=CARTESIAN_POINT('Ctrl Pts',(367.396843869782,-10.1198655666505,1.91108911701175));
#42505=CARTESIAN_POINT('Ctrl Pts',(367.382650939506,-10.1213510404318,1.88556030826137));
#42506=CARTESIAN_POINT('Ctrl Pts',(367.368748104157,-10.1228365142132,1.85988361845735));
#42507=CARTESIAN_POINT('Ctrl Pts',(367.355138369347,-10.1243219879945,1.83406627987422));
#42508=CARTESIAN_POINT('Ctrl Pts',(367.298199692195,-10.1305367242282,1.72605498303068));
#42509=CARTESIAN_POINT('Ctrl Pts',(367.246223172796,-10.1367514604618,1.61525459220924));
#42510=CARTESIAN_POINT('Ctrl Pts',(367.199474743866,-10.1429661966954,1.50213333973738));
#42511=CARTESIAN_POINT('Ctrl Pts',(367.150661820684,-10.1494553867988,1.38401645039109));
#42512=CARTESIAN_POINT('Ctrl Pts',(367.107549552707,-10.1559445769023,1.2633692950333));
#42513=CARTESIAN_POINT('Ctrl Pts',(367.070388455924,-10.1624337670057,1.1407561054578));
#42514=CARTESIAN_POINT('Ctrl Pts',(367.034959130744,-10.1686205495883,1.02385690331095));
#42515=CARTESIAN_POINT('Ctrl Pts',(367.00493902324,-10.174807332171,0.905171141912029));
#42516=CARTESIAN_POINT('Ctrl Pts',(366.980497169477,-10.1809941147536,0.785210250520267));
#42517=CARTESIAN_POINT('Ctrl Pts',(366.956093310278,-10.187171280058,0.665435836874832));
#42518=CARTESIAN_POINT('Ctrl Pts',(366.937250502295,-10.1933484453624,0.544390574405071));
#42519=CARTESIAN_POINT('Ctrl Pts',(366.92408797741,-10.1995256106668,0.422600660547639));
#42520=CARTESIAN_POINT('Ctrl Pts',(366.91095107282,-10.2056907523818,0.30104780557353));
#42521=CARTESIAN_POINT('Ctrl Pts',(366.903472449916,-10.2118558940969,0.178753527193132));
#42522=CARTESIAN_POINT('Ctrl Pts',(366.901720164552,-10.2180210358119,0.0562531692756094));
#42523=CARTESIAN_POINT('Ctrl Pts',(366.901453425184,-10.2189595165201,0.0376057110399778));
#42524=CARTESIAN_POINT('Ctrl Pts',(366.901319280049,-10.2198979972282,0.0189534950297947));
#42525=CARTESIAN_POINT('Ctrl Pts',(366.901317864546,-10.2208364779364,0.000298426845041434));
#42526=CARTESIAN_POINT('',(366.901319464936,-11.4708364779244,-0.00356057907672602));
#42527=CARTESIAN_POINT('Ctrl Pts',(366.901317864546,-10.2208364779651,0.000298426274699534));
#42528=CARTESIAN_POINT('Ctrl Pts',(366.901308669822,-10.2269326063234,-0.120880079791976));
#42529=CARTESIAN_POINT('Ctrl Pts',(366.90690418874,-10.2330287346816,-0.241964705586346));
#42530=CARTESIAN_POINT('Ctrl Pts',(366.918052542601,-10.2391248630399,-0.36242932664784));
#42531=CARTESIAN_POINT('Ctrl Pts',(366.929214108592,-10.2452282160379,-0.483036712663392));
#42532=CARTESIAN_POINT('Ctrl Pts',(366.945941599533,-10.2513315690359,-0.60302226985431));
#42533=CARTESIAN_POINT('Ctrl Pts',(366.968131703025,-10.2574349220339,-0.721868168026967));
#42534=CARTESIAN_POINT('Ctrl Pts',(366.990371034528,-10.2635518151187,-0.840977721895112));
#42535=CARTESIAN_POINT('Ctrl Pts',(367.018097133237,-10.2696687082035,-0.958942208026564));
#42536=CARTESIAN_POINT('Ctrl Pts',(367.051155958216,-10.2757856012883,-1.07525581893695));
#42537=CARTESIAN_POINT('Ctrl Pts',(367.084254289864,-10.2819098043146,-1.19170842944621));
#42538=CARTESIAN_POINT('Ctrl Pts',(367.12269794591,-10.2880340073408,-1.30650588769926));
#42539=CARTESIAN_POINT('Ctrl Pts',(367.166284231668,-10.2941582103671,-1.41916114347041));
#42540=CARTESIAN_POINT('Ctrl Pts',(367.209966847428,-10.3002959484877,-1.53206537849831));
#42541=CARTESIAN_POINT('Ctrl Pts',(367.258814666438,-10.3064336866083,-1.64281761691705));
#42542=CARTESIAN_POINT('Ctrl Pts',(367.312577893879,-10.312571424729,-1.75095307154533));
#42543=CARTESIAN_POINT('Ctrl Pts',(367.342554728856,-10.3159936516214,-1.81124630230529));
#42544=CARTESIAN_POINT('Ctrl Pts',(367.374058892957,-10.3194158785138,-1.870726494836));
#42545=CARTESIAN_POINT('Ctrl Pts',(367.407041277237,-10.3228381054062,-1.92931704799599));
#42546=CARTESIAN_POINT('Ctrl Pts',(367.463650113153,-10.3287117947967,-2.0298780923987));
#42547=CARTESIAN_POINT('Ctrl Pts',(367.524782882167,-10.3345854841873,-2.12811303680054));
#42548=CARTESIAN_POINT('Ctrl Pts',(367.590223494545,-10.3404591735779,-2.2235873699918));
#42549=CARTESIAN_POINT('Ctrl Pts',(367.655579616944,-10.3463252794836,-2.31893843684947));
#42550=CARTESIAN_POINT('Ctrl Pts',(367.725232290604,-10.3521913853894,-2.41153564287257));
#42551=CARTESIAN_POINT('Ctrl Pts',(367.79891968103,-10.3580574912951,-2.50096919937823));
#42552=CARTESIAN_POINT('Ctrl Pts',(367.872531616506,-10.3639175903831,-2.59031117706125));
#42553=CARTESIAN_POINT('Ctrl Pts',(367.9501697897,-10.3697776894712,-2.67649563197347));
#42554=CARTESIAN_POINT('Ctrl Pts',(368.031529619935,-10.3756377885592,-2.75914246086288));
#42555=CARTESIAN_POINT('Ctrl Pts',(368.115824727233,-10.3817093066533,-2.8447709987913));
#42556=CARTESIAN_POINT('Ctrl Pts',(368.20411484412,-10.3877808247474,-2.92660145977786));
#42557=CARTESIAN_POINT('Ctrl Pts',(368.29601598023,-10.3938523428415,-3.00424909113004));
#42558=CARTESIAN_POINT('Ctrl Pts',(368.384615035074,-10.3997057064382,-3.07910678103308));
#42559=CARTESIAN_POINT('Ctrl Pts',(368.47656973873,-10.405559070035,-3.15007676361596));
#42560=CARTESIAN_POINT('Ctrl Pts',(368.571499803274,-10.4114124336317,-3.21685303873542));
#42561=CARTESIAN_POINT('Ctrl Pts',(368.666415614389,-10.4172649183656,-3.2836192876219));
#42562=CARTESIAN_POINT('Ctrl Pts',(368.764305560277,-10.4231174030995,-3.34619284343195));
#42563=CARTESIAN_POINT('Ctrl Pts',(368.864758757646,-10.4289698878334,-3.40430991083745));
#42564=CARTESIAN_POINT('Ctrl Pts',(368.965221165224,-10.4348229091615,-3.46243230679768));
#42565=CARTESIAN_POINT('Ctrl Pts',(369.068246933843,-10.4406759304897,-3.51609719518931));
#42566=CARTESIAN_POINT('Ctrl Pts',(369.173399495664,-10.4465289518179,-3.56508614335217));
#42567=CARTESIAN_POINT('Ctrl Pts',(369.278587127895,-10.4523839252417,-3.61409143027528));
#42568=CARTESIAN_POINT('Ctrl Pts',(369.385902589497,-10.4582388986655,-3.65841750156267));
#42569=CARTESIAN_POINT('Ctrl Pts',(369.49488886892,-10.4640938720893,-3.69789385948342));
#42570=CARTESIAN_POINT('Ctrl Pts',(369.603998670291,-10.4699554813734,-3.73741495878536));
#42571=CARTESIAN_POINT('Ctrl Pts',(369.714782680444,-10.4758170906575,-3.77207523320338));
#42572=CARTESIAN_POINT('Ctrl Pts',(369.826768151356,-10.4816786999417,-3.80175388449402));
#42573=CARTESIAN_POINT('Ctrl Pts',(369.938829134893,-10.487544261752,-3.83145254831726));
#42574=CARTESIAN_POINT('Ctrl Pts',(370.052092789734,-10.4934098235623,-3.85616281236528));
#42575=CARTESIAN_POINT('Ctrl Pts',(370.166077300005,-10.4992753853727,-3.87581521270471));
#42576=CARTESIAN_POINT('Ctrl Pts',(370.280228483586,-10.505149524073,-3.89549634967348));
#42577=CARTESIAN_POINT('Ctrl Pts',(370.395102217982,-10.5110236627733,-3.91010481078231));
#42578=CARTESIAN_POINT('Ctrl Pts',(370.510212637904,-10.5168978014736,-3.91962304429937));
#42579=CARTESIAN_POINT('Ctrl Pts',(370.539322183913,-10.518383275255,-3.92203005016969));
#42580=CARTESIAN_POINT('Ctrl Pts',(370.568446873907,-10.5198687490364,-3.92411179532515));
#42581=CARTESIAN_POINT('Ctrl Pts',(370.597578879703,-10.5213542228178,-3.92586852281327));
#42582=CARTESIAN_POINT('Ctrl Pts',(370.712769302795,-10.5272279122084,-3.93281477237919));
#42583=CARTESIAN_POINT('Ctrl Pts',(370.828457552963,-10.5331016015989,-3.93469852452861));
#42584=CARTESIAN_POINT('Ctrl Pts',(370.944161362727,-10.5389752909895,-3.93146580850197));
#42585=CARTESIAN_POINT('Ctrl Pts',(371.059715788002,-10.5448413968953,-3.92823726621543));
#42586=CARTESIAN_POINT('Ctrl Pts',(371.175285323712,-10.5507075028011,-3.919905404038));
#42587=CARTESIAN_POINT('Ctrl Pts',(371.290383678238,-10.5565736087068,-3.90646809320824));
#42588=CARTESIAN_POINT('Ctrl Pts',(371.405364173516,-10.5624337077949,-3.8930445420136));
#42589=CARTESIAN_POINT('Ctrl Pts',(371.519874039392,-10.5682938068829,-3.87452598854464));
#42590=CARTESIAN_POINT('Ctrl Pts',(371.633428756039,-10.5741539059709,-3.8509623167465));
#42591=CARTESIAN_POINT('Ctrl Pts',(371.751080267803,-10.580225424065,-3.82654852142728));
#42592=CARTESIAN_POINT('Ctrl Pts',(371.867705958403,-10.5862969421592,-3.79671871456764));
#42593=CARTESIAN_POINT('Ctrl Pts',(371.982774352302,-10.5923684602533,-3.76158698819061));
#42594=CARTESIAN_POINT('Ctrl Pts',(372.093708246849,-10.59822182385,-3.72771757281882));
#42595=CARTESIAN_POINT('Ctrl Pts',(372.203194399564,-10.6040751874468,-3.68892081630316));
#42596=CARTESIAN_POINT('Ctrl Pts',(372.310769518424,-10.6099285510435,-3.64535039198271));
#42597=CARTESIAN_POINT('Ctrl Pts',(372.418328485242,-10.6157810357774,-3.60178650961494));
#42598=CARTESIAN_POINT('Ctrl Pts',(372.523976605915,-10.6216335205113,-3.55345053966426));
#42599=CARTESIAN_POINT('Ctrl Pts',(372.627269467417,-10.6274860052452,-3.5005447446308));
#42600=CARTESIAN_POINT('Ctrl Pts',(372.730571799488,-10.6333390265734,-3.44763409884617));
#42601=CARTESIAN_POINT('Ctrl Pts',(372.831518075371,-10.6391920479016,-3.39015298341494));
#42602=CARTESIAN_POINT('Ctrl Pts',(372.929688076808,-10.6450450692298,-3.32834983529612));
#42603=CARTESIAN_POINT('Ctrl Pts',(373.027890819837,-10.6509000426536,-3.26652607463396));
#42604=CARTESIAN_POINT('Ctrl Pts',(373.123315097789,-10.6567550160774,-3.20037763495378));
#42605=CARTESIAN_POINT('Ctrl Pts',(373.215569889773,-10.6626099895012,-3.13019611820589));
#42606=CARTESIAN_POINT('Ctrl Pts',(373.307929240714,-10.6684715987854,-3.05993505972314));
#42607=CARTESIAN_POINT('Ctrl Pts',(373.397111606866,-10.6743332080695,-2.98563205106249));
#42608=CARTESIAN_POINT('Ctrl Pts',(373.482759199316,-10.6801948173537,-2.90761886022049));
#42609=CARTESIAN_POINT('Ctrl Pts',(373.568464544566,-10.686060379164,-2.8295530645113));
#42610=CARTESIAN_POINT('Ctrl Pts',(373.650630077893,-10.6919259409744,-2.74777239570561));
#42611=CARTESIAN_POINT('Ctrl Pts',(373.728936231239,-10.6977915027847,-2.66264407040357));
#42612=CARTESIAN_POINT('Ctrl Pts',(373.807356887388,-10.703665641485,-2.5773912666105));
#42613=CARTESIAN_POINT('Ctrl Pts',(373.881906635875,-10.7095397801854,-2.48878135186763));
#42614=CARTESIAN_POINT('Ctrl Pts',(373.952307335647,-10.7154139188857,-2.39721308762895));
#42615=CARTESIAN_POINT('Ctrl Pts',(373.970110523319,-10.716899392667,-2.37405696846678));
#42616=CARTESIAN_POINT('Ctrl Pts',(373.987648601557,-10.7183848664482,-2.35071179676868));
#42617=CARTESIAN_POINT('Ctrl Pts',(374.004917530866,-10.7198703402294,-2.32718428237531));
#42618=CARTESIAN_POINT('Ctrl Pts',(374.073200342821,-10.72574402962,-2.23415449388353));
#42619=CARTESIAN_POINT('Ctrl Pts',(374.137498975262,-10.7316177190106,-2.13796194939481));
#42620=CARTESIAN_POINT('Ctrl Pts',(374.19750663435,-10.7374914084011,-2.03898264399467));
#42621=CARTESIAN_POINT('Ctrl Pts',(374.257436817912,-10.7433575143069,-1.94013113017638));
#42622=CARTESIAN_POINT('Ctrl Pts',(374.313086833233,-10.7492236202127,-1.83850036069155));
#42623=CARTESIAN_POINT('Ctrl Pts',(374.364191268188,-10.7550897261184,-1.73449781617942));
#42624=CARTESIAN_POINT('Ctrl Pts',(374.415243372852,-10.7609498252065,-1.6306017689479));
#42625=CARTESIAN_POINT('Ctrl Pts',(374.461758974449,-10.7668099242945,-1.52433914610418));
#42626=CARTESIAN_POINT('Ctrl Pts',(374.503517328043,-10.7726700233826,-1.41614413602247));
#42627=CARTESIAN_POINT('Ctrl Pts',(374.546782227767,-10.7787415414767,-1.30404569680955));
#42628=CARTESIAN_POINT('Ctrl Pts',(374.584939903085,-10.7848130595708,-1.18987319180289));
#42629=CARTESIAN_POINT('Ctrl Pts',(374.617798108474,-10.7908845776649,-1.07413507443666));
#42630=CARTESIAN_POINT('Ctrl Pts',(374.649475692284,-10.7967379412616,-0.962555520122967));
#42631=CARTESIAN_POINT('Ctrl Pts',(374.676227958048,-10.8025913048584,-0.849521356133328));
#42632=CARTESIAN_POINT('Ctrl Pts',(374.697932883667,-10.8084446684551,-0.735505198168392));
#42633=CARTESIAN_POINT('Ctrl Pts',(374.719634550365,-10.814297153189,-0.621506159345897));
#42634=CARTESIAN_POINT('Ctrl Pts',(374.736290306551,-10.8201496379229,-0.506525825467728));
#42635=CARTESIAN_POINT('Ctrl Pts',(374.747829194461,-10.8260021226568,-0.391047288712072));
#42636=CARTESIAN_POINT('Ctrl Pts',(374.759369140333,-10.831855143985,-0.27555816412495));
#42637=CARTESIAN_POINT('Ctrl Pts',(374.765791244227,-10.8377081653132,-0.15957115697606));
#42638=CARTESIAN_POINT('Ctrl Pts',(374.767076465356,-10.8435611866414,-0.0435740600023058));
#42639=CARTESIAN_POINT('Ctrl Pts',(374.768362115131,-10.8494161600652,0.0724617242429357));
#42640=CARTESIAN_POINT('Ctrl Pts',(374.764507470846,-10.855271133489,0.188507192107884));
#42641=CARTESIAN_POINT('Ctrl Pts',(374.755545591765,-10.8611261069128,0.304075685480253));
#42642=CARTESIAN_POINT('Ctrl Pts',(374.746573555545,-10.8669877161969,0.419775160896118));
#42643=CARTESIAN_POINT('Ctrl Pts',(374.732482763201,-10.8728493254811,0.534996170696944));
#42644=CARTESIAN_POINT('Ctrl Pts',(374.713358041213,-10.8787109347653,0.649258207466544));
#42645=CARTESIAN_POINT('Ctrl Pts',(374.694220423285,-10.8845764965756,0.763597291966407));
#42646=CARTESIAN_POINT('Ctrl Pts',(374.670042202632,-10.8904420583859,0.876975712766699));
#42647=CARTESIAN_POINT('Ctrl Pts',(374.640958713361,-10.8963076201963,0.988925862710946));
#42648=CARTESIAN_POINT('Ctrl Pts',(374.611832696895,-10.9021817588966,1.10103971123219));
#42649=CARTESIAN_POINT('Ctrl Pts',(374.577787217894,-10.9080558975969,1.21172072744426));
#42650=CARTESIAN_POINT('Ctrl Pts',(374.539006575828,-10.9139300362973,1.32051901486169));
#42651=CARTESIAN_POINT('Ctrl Pts',(374.529199584548,-10.9154155100785,1.3480323256042));
#42652=CARTESIAN_POINT('Ctrl Pts',(374.519090012593,-10.9169009838598,1.37542534998755));
#42653=CARTESIAN_POINT('Ctrl Pts',(374.508681308446,-10.9183864576411,1.40269105612236));
#42654=CARTESIAN_POINT('Ctrl Pts',(374.467524408952,-10.9242601470317,1.51050197198515));
#42655=CARTESIAN_POINT('Ctrl Pts',(374.421549959167,-10.9301338364222,1.61667951064537));
#42656=CARTESIAN_POINT('Ctrl Pts',(374.370907594853,-10.9360075258128,1.72076204031954));
#42657=CARTESIAN_POINT('Ctrl Pts',(374.320330614589,-10.9418736317185,1.82471018966963));
#42658=CARTESIAN_POINT('Ctrl Pts',(374.265097884067,-10.9477397376243,1.92656834098959));
#42659=CARTESIAN_POINT('Ctrl Pts',(374.205407930028,-10.95360584353,2.0258925672578));
#42660=CARTESIAN_POINT('Ctrl Pts',(374.145779097742,-10.959465942618,2.1251150867839));
#42661=CARTESIAN_POINT('Ctrl Pts',(374.081702331938,-10.9653260417061,2.22180849033149));
#42662=CARTESIAN_POINT('Ctrl Pts',(374.013422816585,-10.9711861407941,2.31555190655123));
#42663=CARTESIAN_POINT('Ctrl Pts',(373.942679932089,-10.9772576588882,2.41267737136529));
#42664=CARTESIAN_POINT('Ctrl Pts',(373.867425518904,-10.9833291769823,2.50663556622539));
#42665=CARTESIAN_POINT('Ctrl Pts',(373.787982616316,-10.9894006950764,2.59698930826947));
#42666=CARTESIAN_POINT('Ctrl Pts',(373.711394160708,-10.9952540586732,2.68409656815289));
#42667=CARTESIAN_POINT('Ctrl Pts',(373.630913323417,-11.0011074222699,2.76785360237273));
#42668=CARTESIAN_POINT('Ctrl Pts',(373.546871097785,-11.0069607858667,2.84790166533533));
#42669=CARTESIAN_POINT('Ctrl Pts',(373.462841490811,-11.0128132706006,2.92793770935062));
#42670=CARTESIAN_POINT('Ctrl Pts',(373.37525185782,-11.0186657553344,3.00426560454857));
#42671=CARTESIAN_POINT('Ctrl Pts',(373.284469678083,-11.0245182400683,3.07656383570034));
#42672=CARTESIAN_POINT('Ctrl Pts',(373.193679174839,-11.0303712613965,3.14886869562922));
#42673=CARTESIAN_POINT('Ctrl Pts',(373.09969586616,-11.0362242827247,3.2171428996557));
#42674=CARTESIAN_POINT('Ctrl Pts',(373.002919325918,-11.0420773040529,3.28110601057466));
#42675=CARTESIAN_POINT('Ctrl Pts',(372.906110508831,-11.0479322774767,3.34509045442614));
#42676=CARTESIAN_POINT('Ctrl Pts',(372.806506952223,-11.0537872509004,3.40476071842432));
#42677=CARTESIAN_POINT('Ctrl Pts',(372.704535520467,-11.0596422243242,3.45988076053695));
#42678=CARTESIAN_POINT('Ctrl Pts',(372.602448517189,-11.0655038336084,3.51506327413752));
#42679=CARTESIAN_POINT('Ctrl Pts',(372.497988645944,-11.0713654428925,3.56568507603903));
#42680=CARTESIAN_POINT('Ctrl Pts',(372.391605666124,-11.0772270521767,3.61155695895714));
#42681=CARTESIAN_POINT('Ctrl Pts',(372.28515095148,-11.083092613987,3.65745977362282));
#42682=CARTESIAN_POINT('Ctrl Pts',(372.176770931402,-11.0889581757973,3.69860614533514));
#42683=CARTESIAN_POINT('Ctrl Pts',(372.066931905761,-11.0948237376077,3.73485630212038));
#42684=CARTESIAN_POINT('Ctrl Pts',(371.956932268524,-11.100697876308,3.77115946552583));
#42685=CARTESIAN_POINT('Ctrl Pts',(371.845469764092,-11.1065720150084,3.80255201393653));
#42686=CARTESIAN_POINT('Ctrl Pts',(371.733022354505,-11.1124461537087,3.82894492247894));
#42687=CARTESIAN_POINT('Ctrl Pts',(371.704586240337,-11.11393162749,3.83561925818212));
#42688=CARTESIAN_POINT('Ctrl Pts',(371.676087171879,-11.1154171012714,3.84197412459062));
#42689=CARTESIAN_POINT('Ctrl Pts',(371.647532927538,-11.1169025750527,3.8480086074369));
#42690=CARTESIAN_POINT('Ctrl Pts',(371.534627022264,-11.1227762644433,3.87186946470481));
#42691=CARTESIAN_POINT('Ctrl Pts',(371.420482016839,-11.1286499538339,3.89079662734259));
#42692=CARTESIAN_POINT('Ctrl Pts',(371.305566943042,-11.1345236432244,3.90466558047495));
#42693=CARTESIAN_POINT('Ctrl Pts',(371.190800235401,-11.1403897491302,3.91851662748592));
#42694=CARTESIAN_POINT('Ctrl Pts',(371.075265843009,-11.146255855036,3.92732240321006));
#42695=CARTESIAN_POINT('Ctrl Pts',(370.959444424461,-11.1521219609418,3.93100907416535));
#42696=CARTESIAN_POINT('Ctrl Pts',(370.843741605572,-11.1579820600298,3.93469197001653));
#42697=CARTESIAN_POINT('Ctrl Pts',(370.727752755621,-11.1638421591178,3.93326617460275));
#42698=CARTESIAN_POINT('Ctrl Pts',(370.611964452668,-11.1697022582059,3.92670955957546));
#42699=CARTESIAN_POINT('Ctrl Pts',(370.4919987719,-11.1757737763,3.91991639683599));
#42700=CARTESIAN_POINT('Ctrl Pts',(370.372248830317,-11.1818452943941,3.90761515397088));
#42701=CARTESIAN_POINT('Ctrl Pts',(370.253257118779,-11.1879168124882,3.88984028243908));
#42702=CARTESIAN_POINT('Ctrl Pts',(370.138540874531,-11.1937701760849,3.87270407624671));
#42703=CARTESIAN_POINT('Ctrl Pts',(370.024529754068,-11.1996235396817,3.85048088198586));
#42704=CARTESIAN_POINT('Ctrl Pts',(369.911704648765,-11.2054769032785,3.82325435656048));
#42705=CARTESIAN_POINT('Ctrl Pts',(369.798896483773,-11.2113293880124,3.79603191910633));
#42706=CARTESIAN_POINT('Ctrl Pts',(369.687274381367,-11.2171818727463,3.76380774111228));
#42707=CARTESIAN_POINT('Ctrl Pts',(369.577307727326,-11.2230343574802,3.72671632182953));
#42708=CARTESIAN_POINT('Ctrl Pts',(369.467330990819,-11.2288873788083,3.68962150176155));
#42709=CARTESIAN_POINT('Ctrl Pts',(369.359010395903,-11.2347404001365,3.6476586853312));
#42710=CARTESIAN_POINT('Ctrl Pts',(369.252798208958,-11.2405934214647,3.60101160992311));
#42711=CARTESIAN_POINT('Ctrl Pts',(369.146550598198,-11.2464483948885,3.55434897681455));
#42712=CARTESIAN_POINT('Ctrl Pts',(369.042413171748,-11.2523033683124,3.50299914422488));
#42713=CARTESIAN_POINT('Ctrl Pts',(368.940815684815,-11.2581583417362,3.44719284900503));
#42714=CARTESIAN_POINT('Ctrl Pts',(368.839103050181,-11.2640199510204,3.39132330451753));
#42715=CARTESIAN_POINT('Ctrl Pts',(368.739936463082,-11.2698815603045,3.33098741526696));
#42716=CARTESIAN_POINT('Ctrl Pts',(368.64371873473,-11.2757431695887,3.26646054653273));
#42717=CARTESIAN_POINT('Ctrl Pts',(368.547436126058,-11.281608731399,3.20189016685768));
#42718=CARTESIAN_POINT('Ctrl Pts',(368.454106667338,-11.2874742932093,3.13312342495507));
#42719=CARTESIAN_POINT('Ctrl Pts',(368.364100595649,-11.2933398550196,3.06047638454874));
#42720=CARTESIAN_POINT('Ctrl Pts',(368.273962913008,-11.2992139937199,2.9877231163509));
#42721=CARTESIAN_POINT('Ctrl Pts',(368.187158624461,-11.3050881324203,2.91107849827512));
#42722=CARTESIAN_POINT('Ctrl Pts',(368.104021646077,-11.3109622711206,2.83089590434556));
#42723=CARTESIAN_POINT('Ctrl Pts',(368.082997661466,-11.3124477449019,2.81061903533164));
#42724=CARTESIAN_POINT('Ctrl Pts',(368.06220800129,-11.3139332186832,2.79011607799069));
#42725=CARTESIAN_POINT('Ctrl Pts',(368.041657650564,-11.3154186924644,2.7693930729458));
#42726=CARTESIAN_POINT('Ctrl Pts',(367.961508675604,-11.3212122286667,2.68857072423641));
#42727=CARTESIAN_POINT('Ctrl Pts',(367.884719897014,-11.327005764869,2.60411321589936));
#42728=CARTESIAN_POINT('Ctrl Pts',(367.811645983487,-11.3327993010713,2.51633538462223));
#42729=CARTESIAN_POINT('Ctrl Pts',(367.738687843669,-11.3385836583596,2.42869662301526));
#42730=CARTESIAN_POINT('Ctrl Pts',(367.669433128666,-11.3443680156479,2.33774832840426));
#42731=CARTESIAN_POINT('Ctrl Pts',(367.604200404663,-11.3501523729361,2.24384274593864));
#42732=CARTESIAN_POINT('Ctrl Pts',(367.539026703765,-11.3559314964904,2.15002213001591));
#42733=CARTESIAN_POINT('Ctrl Pts',(367.477868005425,-11.3617106200446,2.05324988897528));
#42734=CARTESIAN_POINT('Ctrl Pts',(367.421003061589,-11.3674897435988,1.95391175164293));
#42735=CARTESIAN_POINT('Ctrl Pts',(367.364174919228,-11.3732651270585,1.85463790330231));
#42736=CARTESIAN_POINT('Ctrl Pts',(367.311635219995,-11.3790405105182,1.75280182649306));
#42737=CARTESIAN_POINT('Ctrl Pts',(367.263619271642,-11.3848158939779,1.64881795219631));
#42738=CARTESIAN_POINT('Ctrl Pts',(367.215622031528,-11.3905890272007,1.54487459267253));
#42739=CARTESIAN_POINT('Ctrl Pts',(367.17214521611,-11.3963621604235,1.43878548518357));
#42740=CARTESIAN_POINT('Ctrl Pts',(367.133377649361,-11.4021352936463,1.33098858275673));
#42741=CARTESIAN_POINT('Ctrl Pts',(367.094601015693,-11.4079097770835,1.22316646890099));
#42742=CARTESIAN_POINT('Ctrl Pts',(367.060535985716,-11.4136842605208,1.11363615900919));
#42743=CARTESIAN_POINT('Ctrl Pts',(367.031322638993,-11.4194587439581,1.00285412724623));
#42744=CARTESIAN_POINT('Ctrl Pts',(367.002107164036,-11.4252336480747,0.892064024853437));
#42745=CARTESIAN_POINT('Ctrl Pts',(366.977744175852,-11.4310085521914,0.780022433116942));
#42746=CARTESIAN_POINT('Ctrl Pts',(366.958323041382,-11.436783456308,0.667198035500687));
#42747=CARTESIAN_POINT('Ctrl Pts',(366.938882937663,-11.4425640009601,0.554263438651138));
#42748=CARTESIAN_POINT('Ctrl Pts',(366.924394394745,-11.4483445456121,0.440544929953996));
#42749=CARTESIAN_POINT('Ctrl Pts',(366.914895097852,-11.4541250902642,0.326518398678384));
#42750=CARTESIAN_POINT('Ctrl Pts',(366.90574103352,-11.4596955528176,0.216635928980348));
#42751=CARTESIAN_POINT('Ctrl Pts',(366.901219855256,-11.465266015371,0.106467790374153));
#42752=CARTESIAN_POINT('Ctrl Pts',(366.901319464936,-11.4708364779244,-0.00356057907674602));
#42753=CARTESIAN_POINT('',(366.901318279586,-12.7208364780083,0.00183132834481399));
#42754=CARTESIAN_POINT('Ctrl Pts',(366.901319464937,-11.470836477965,-0.00356057987879464));
#42755=CARTESIAN_POINT('Ctrl Pts',(366.901464067762,-11.4789230860767,-0.163288124293369));
#42756=CARTESIAN_POINT('Ctrl Pts',(366.911342487007,-11.4870096941884,-0.322591275985424));
#42757=CARTESIAN_POINT('Ctrl Pts',(366.930779443932,-11.4950963023001,-0.480496500694793));
#42758=CARTESIAN_POINT('Ctrl Pts',(366.945872845072,-11.5013758048254,-0.603114815275443));
#42759=CARTESIAN_POINT('Ctrl Pts',(366.966729094728,-11.5076553073508,-0.724891027394278));
#42760=CARTESIAN_POINT('Ctrl Pts',(366.993247465156,-11.5139348098761,-0.845379958307364));
#42761=CARTESIAN_POINT('Ctrl Pts',(367.018052084696,-11.5198084992667,-0.958082286609465));
#42762=CARTESIAN_POINT('Ctrl Pts',(367.047862483551,-11.5256821886572,-1.06987969207649));
#42763=CARTESIAN_POINT('Ctrl Pts',(367.082598753345,-11.5315558780478,-1.18029352095419));
#42764=CARTESIAN_POINT('Ctrl Pts',(367.117290175353,-11.5374219839536,-1.29056479520598));
#42765=CARTESIAN_POINT('Ctrl Pts',(367.156894697966,-11.5432880898593,-1.39945565478516));
#42766=CARTESIAN_POINT('Ctrl Pts',(367.201281445146,-11.5491541957651,-1.50649774562716));
#42767=CARTESIAN_POINT('Ctrl Pts',(367.245622740862,-11.5550142948531,-1.61343022673162));
#42768=CARTESIAN_POINT('Ctrl Pts',(367.294736363421,-11.5608743939411,-1.71851732529604));
#42769=CARTESIAN_POINT('Ctrl Pts',(367.348441889177,-11.5667344930292,-1.82130660880631));
#42770=CARTESIAN_POINT('Ctrl Pts',(367.404084987781,-11.5728060111233,-1.9278042951658));
#42771=CARTESIAN_POINT('Ctrl Pts',(367.464657440499,-11.5788775292174,-2.03183480538736));
#42772=CARTESIAN_POINT('Ctrl Pts',(367.529904225892,-11.5849490473115,-2.13291809020064));
#42773=CARTESIAN_POINT('Ctrl Pts',(367.592806642143,-11.5908024109082,-2.23036937180685));
#42774=CARTESIAN_POINT('Ctrl Pts',(367.660053023659,-11.596655774505,-2.32508119855194));
#42775=CARTESIAN_POINT('Ctrl Pts',(367.731368912453,-11.6025091381017,-2.41664992726858));
#42776=CARTESIAN_POINT('Ctrl Pts',(367.802674093406,-11.6083616228356,-2.50820490724874));
#42777=CARTESIAN_POINT('Ctrl Pts',(367.878047312904,-11.6142141075695,-2.59661740170169));
#42778=CARTESIAN_POINT('Ctrl Pts',(367.957172534633,-11.6200665923034,-2.6815152089275));
#42779=CARTESIAN_POINT('Ctrl Pts',(368.036305011083,-11.6259196136316,-2.76642080014239));
#42780=CARTESIAN_POINT('Ctrl Pts',(368.119189891923,-11.6317726349598,-2.8478107612795));
#42781=CARTESIAN_POINT('Ctrl Pts',(368.205473338279,-11.637625656288,-2.92534878540034));
#42782=CARTESIAN_POINT('Ctrl Pts',(368.291785561831,-11.6434806297118,-3.0029126699497));
#42783=CARTESIAN_POINT('Ctrl Pts',(368.381498297658,-11.6493356031356,-3.07662178692343));
#42784=CARTESIAN_POINT('Ctrl Pts',(368.474224166602,-11.6551905765595,-3.14617971361588));
#42785=CARTESIAN_POINT('Ctrl Pts',(368.567055128408,-11.6610521858436,-3.21581647528381));
#42786=CARTESIAN_POINT('Ctrl Pts',(368.662905708786,-11.6669137951278,-3.2812924080347));
#42787=CARTESIAN_POINT('Ctrl Pts',(368.761358975856,-11.6727754044119,-3.34235403461983));
#42788=CARTESIAN_POINT('Ctrl Pts',(368.859878630686,-11.6786409662223,-3.40345683550811));
#42789=CARTESIAN_POINT('Ctrl Pts',(368.961004107323,-11.6845065280326,-3.46013920165616));
#42790=CARTESIAN_POINT('Ctrl Pts',(369.06429482262,-11.690372089843,-3.5121941106853));
#42791=CARTESIAN_POINT('Ctrl Pts',(369.167736574278,-11.6962462285433,-3.56432513675877));
#42792=CARTESIAN_POINT('Ctrl Pts',(369.273349508,-11.7021203672436,-3.61181503274357));
#42793=CARTESIAN_POINT('Ctrl Pts',(369.380674020833,-11.7079945059439,-3.65450524812225));
#42794=CARTESIAN_POINT('Ctrl Pts',(369.407814638043,-11.7094799797252,-3.66530090666838));
#42795=CARTESIAN_POINT('Ctrl Pts',(369.435064642667,-11.7109654535065,-3.67578987601305));
#42796=CARTESIAN_POINT('Ctrl Pts',(369.462416476234,-11.7124509272877,-3.68597010457407));
#42797=CARTESIAN_POINT('Ctrl Pts',(369.570567947274,-11.7183246166783,-3.72622359221322));
#42798=CARTESIAN_POINT('Ctrl Pts',(369.680672685131,-11.7241983060688,-3.76178011693693));
#42799=CARTESIAN_POINT('Ctrl Pts',(369.792285154209,-11.7300719954594,-3.79244734362707));
#42800=CARTESIAN_POINT('Ctrl Pts',(369.903753521104,-11.7359381013651,-3.82307497604649));
#42801=CARTESIAN_POINT('Ctrl Pts',(370.016725353285,-11.7418042072709,-3.84882575554942));
#42802=CARTESIAN_POINT('Ctrl Pts',(370.130736140009,-11.7476703131766,-3.86955575910594));
#42803=CARTESIAN_POINT('Ctrl Pts',(370.244630181141,-11.7535304122646,-3.89026453540292));
#42804=CARTESIAN_POINT('Ctrl Pts',(370.359560656613,-11.7593905113527,-3.9059626885785));
#42805=CARTESIAN_POINT('Ctrl Pts',(370.475049574461,-11.7652506104407,-3.91655656206763));
#42806=CARTESIAN_POINT('Ctrl Pts',(370.594705068994,-11.7713221285348,-3.92753263834379));
#42807=CARTESIAN_POINT('Ctrl Pts',(370.714959625805,-11.7773936466289,-3.93302906002744));
#42808=CARTESIAN_POINT('Ctrl Pts',(370.83527160618,-11.783465164723,-3.9329998843574));
#42809=CARTESIAN_POINT('Ctrl Pts',(370.951260680948,-11.7893185283198,-3.9329717569925));
#42810=CARTESIAN_POINT('Ctrl Pts',(371.067302675186,-11.7951718919165,-3.92780827699223));
#42811=CARTESIAN_POINT('Ctrl Pts',(371.182909618086,-11.8010252555132,-3.9175212547567));
#42812=CARTESIAN_POINT('Ctrl Pts',(371.298499202993,-11.8068777402471,-3.90723577708294));
#42813=CARTESIAN_POINT('Ctrl Pts',(371.413653455037,-11.812730224981,-3.89182832340498));
#42814=CARTESIAN_POINT('Ctrl Pts',(371.527888283919,-11.8185827097149,-3.87136268743516));
#42815=CARTESIAN_POINT('Ctrl Pts',(371.642133586601,-11.8244357310431,-3.85089517504131));
#42816=CARTESIAN_POINT('Ctrl Pts',(371.755458891851,-11.8302887523712,-3.82536863129001));
#42817=CARTESIAN_POINT('Ctrl Pts',(371.867389778888,-11.8361417736994,-3.79489807457389));
#42818=CARTESIAN_POINT('Ctrl Pts',(371.979357997038,-11.8419967471232,-3.76441735533867));
#42819=CARTESIAN_POINT('Ctrl Pts',(372.089930473792,-11.847851720547,-3.72898945278846));
#42820=CARTESIAN_POINT('Ctrl Pts',(372.198648120898,-11.8537066939708,-3.68877919110236));
#42821=CARTESIAN_POINT('Ctrl Pts',(372.307488985492,-11.859568303255,-3.64852335624944));
#42822=CARTESIAN_POINT('Ctrl Pts',(372.414470436844,-11.8654299125391,-3.60347448728542));
#42823=CARTESIAN_POINT('Ctrl Pts',(372.519153453294,-11.8712915218232,-3.5538455229139));
#42824=CARTESIAN_POINT('Ctrl Pts',(372.623907058272,-11.8771570836336,-3.50418309336718));
#42825=CARTESIAN_POINT('Ctrl Pts',(372.726358778034,-11.8830226454439,-3.44993461159245));
#42826=CARTESIAN_POINT('Ctrl Pts',(372.826095805739,-11.8888882072542,-3.39135807426401));
#42827=CARTESIAN_POINT('Ctrl Pts',(372.92597867344,-11.8947623459546,-3.33269588367121));
#42828=CARTESIAN_POINT('Ctrl Pts',(373.023138581555,-11.9006364846549,-3.2696932309884));
#42829=CARTESIAN_POINT('Ctrl Pts',(373.117193143708,-11.9065106233552,-3.20265037244101));
#42830=CARTESIAN_POINT('Ctrl Pts',(373.140978007027,-11.9079960971366,-3.18569632799576));
#42831=CARTESIAN_POINT('Ctrl Pts',(373.16456445696,-11.909481570918,-3.1684841053142));
#42832=CARTESIAN_POINT('Ctrl Pts',(373.187946672029,-11.9109670446994,-3.15101894365791));
#42833=CARTESIAN_POINT('Ctrl Pts',(373.28040193465,-11.91684073409,-3.08196021235674));
#42834=CARTESIAN_POINT('Ctrl Pts',(373.369969186994,-11.9227144234806,-3.00871386735199));
#42835=CARTESIAN_POINT('Ctrl Pts',(373.456245279269,-11.9285881128711,-2.93155002900421));
#42836=CARTESIAN_POINT('Ctrl Pts',(373.542409981003,-11.9344542187769,-2.85448581642098));
#42837=CARTESIAN_POINT('Ctrl Pts',(373.625291667792,-11.9403203246826,-2.77351444181067));
#42838=CARTESIAN_POINT('Ctrl Pts',(373.704517584294,-11.9461864305884,-2.68894821515114));
#42839=CARTESIAN_POINT('Ctrl Pts',(373.783662374467,-11.9520465296764,-2.60446858323037));
#42840=CARTESIAN_POINT('Ctrl Pts',(373.859158559626,-11.9579066287645,-2.51640172094925));
#42841=CARTESIAN_POINT('Ctrl Pts',(373.930668315433,-11.9637667278525,-2.42509851659249));
#42842=CARTESIAN_POINT('Ctrl Pts',(374.004757980089,-11.9698382459466,-2.33050130091862));
#42843=CARTESIAN_POINT('Ctrl Pts',(374.074567805351,-11.9759097640407,-2.23243011563941));
#42844=CARTESIAN_POINT('Ctrl Pts',(374.139765557656,-11.9819812821348,-2.13131519800962));
#42845=CARTESIAN_POINT('Ctrl Pts',(374.202620702615,-11.9878346457316,-2.03383342017918));
#42846=CARTESIAN_POINT('Ctrl Pts',(374.261189258605,-11.9936880093283,-1.93352325019779));
#42847=CARTESIAN_POINT('Ctrl Pts',(374.315216616381,-11.9995413729251,-1.83080113629325));
#42848=CARTESIAN_POINT('Ctrl Pts',(374.369235862131,-12.005393857659,-1.72809444576845));
#42849=CARTESIAN_POINT('Ctrl Pts',(374.418715073166,-12.0112463423929,-1.62297689695675));
#42850=CARTESIAN_POINT('Ctrl Pts',(374.463445425888,-12.0170988271268,-1.51588985791451));
#42851=CARTESIAN_POINT('Ctrl Pts',(374.508179879783,-12.022951848455,-1.40879300042859));
#42852=CARTESIAN_POINT('Ctrl Pts',(374.54816445057,-12.0288048697832,-1.29972667498969));
#42853=CARTESIAN_POINT('Ctrl Pts',(374.583238601092,-12.0346578911113,-1.18915189366549));
#42854=CARTESIAN_POINT('Ctrl Pts',(374.618324449519,-12.0405128645352,-1.07854023351634));
#42855=CARTESIAN_POINT('Ctrl Pts',(374.6484964963,-12.046367837959,-0.966419510687292));
#42856=CARTESIAN_POINT('Ctrl Pts',(374.673644368378,-12.0522228113828,-0.853264853394234));
#42857=CARTESIAN_POINT('Ctrl Pts',(374.698820742338,-12.058084420667,-0.739981949831268));
#42858=CARTESIAN_POINT('Ctrl Pts',(374.718961486519,-12.0639460299511,-0.6256631764289));
#42859=CARTESIAN_POINT('Ctrl Pts',(374.734007537168,-12.0698076392353,-0.510792882628788));
#42860=CARTESIAN_POINT('Ctrl Pts',(374.749063733479,-12.0756732010456,-0.395845130945944));
#42861=CARTESIAN_POINT('Ctrl Pts',(374.759018360247,-12.081538762856,-0.280345528941752));
#42862=CARTESIAN_POINT('Ctrl Pts',(374.763864427585,-12.0874043246663,-0.164780823896794));
#42863=CARTESIAN_POINT('Ctrl Pts',(374.768717581063,-12.0932784633667,-0.0490471349089849));
#42864=CARTESIAN_POINT('Ctrl Pts',(374.768447267897,-12.099152602067,0.0667514355525111));
#42865=CARTESIAN_POINT('Ctrl Pts',(374.763098500457,-12.1050267407673,0.182130793459123));
#42866=CARTESIAN_POINT('Ctrl Pts',(374.761745884491,-12.1065122145486,0.211308349490523));
#42867=CARTESIAN_POINT('Ctrl Pts',(374.760068757544,-12.1079976883298,0.240459138075285));
#42868=CARTESIAN_POINT('Ctrl Pts',(374.758068366329,-12.109483162111,0.269575427124148));
#42869=CARTESIAN_POINT('Ctrl Pts',(374.750158649708,-12.1153568515016,0.384703704876508));
#42870=CARTESIAN_POINT('Ctrl Pts',(374.737164430592,-12.1212305408922,0.499675310147675));
#42871=CARTESIAN_POINT('Ctrl Pts',(374.719094141903,-12.1271042302827,0.614005038186375));
#42872=CARTESIAN_POINT('Ctrl Pts',(374.701047183654,-12.1329703361885,0.728187155805334));
#42873=CARTESIAN_POINT('Ctrl Pts',(374.677937252867,-12.1388364420943,0.841728639899625));
#42874=CARTESIAN_POINT('Ctrl Pts',(374.64982471185,-12.144702548,0.954146955020592));
#42875=CARTESIAN_POINT('Ctrl Pts',(374.621740957718,-12.1505626470881,1.06645015521903));
#42876=CARTESIAN_POINT('Ctrl Pts',(374.588664882284,-12.1564227461761,1.1776320756891));
#42877=CARTESIAN_POINT('Ctrl Pts',(374.550708201941,-12.1622828452641,1.28721862011283));
#42878=CARTESIAN_POINT('Ctrl Pts',(374.511382131164,-12.1683543633583,1.40075879705231));
#42879=CARTESIAN_POINT('Ctrl Pts',(374.466816714825,-12.1744258814524,1.51258586332731));
#42880=CARTESIAN_POINT('Ctrl Pts',(374.417193377692,-12.1804973995465,1.62218740476106));
#42881=CARTESIAN_POINT('Ctrl Pts',(374.36935304672,-12.1863507631432,1.72785087521986));
#42882=CARTESIAN_POINT('Ctrl Pts',(374.316812194979,-12.19220412674,1.83144558961505));
#42883=CARTESIAN_POINT('Ctrl Pts',(374.259782741088,-12.1980574903367,1.93253183725646));
#42884=CARTESIAN_POINT('Ctrl Pts',(374.202761849978,-12.2039099750707,2.03360290713796));
#42885=CARTESIAN_POINT('Ctrl Pts',(374.141253899732,-12.2097624598046,2.13216589942927));
#42886=CARTESIAN_POINT('Ctrl Pts',(374.075516570133,-12.2156149445385,2.22780606820031));
#42887=CARTESIAN_POINT('Ctrl Pts',(374.009773213302,-12.2214679658667,2.32345500589072));
#42888=CARTESIAN_POINT('Ctrl Pts',(373.939799940288,-12.2273209871948,2.41618024684152));
#42889=CARTESIAN_POINT('Ctrl Pts',(373.865897114426,-12.233174008523,2.5055969713922));
#42890=CARTESIAN_POINT('Ctrl Pts',(373.791969640545,-12.2390289819469,2.59504351814734));
#42891=CARTESIAN_POINT('Ctrl Pts',(373.714110270844,-12.2448839553707,2.68117903605044));
#42892=CARTESIAN_POINT('Ctrl Pts',(373.632658425007,-12.2507389287945,2.76365320623102));
#42893=CARTESIAN_POINT('Ctrl Pts',(373.551114263966,-12.2566005380787,2.84622085029007));
#42894=CARTESIAN_POINT('Ctrl Pts',(373.465969790572,-12.2624621473628,2.92511857002222));
#42895=CARTESIAN_POINT('Ctrl Pts',(373.377599988441,-12.268323756647,3.0000341632531));
#42896=CARTESIAN_POINT('Ctrl Pts',(373.289170597903,-12.2741893184573,3.07500027261867));
#42897=CARTESIAN_POINT('Ctrl Pts',(373.19751187384,-12.2800548802677,3.14597865637191));
#42898=CARTESIAN_POINT('Ctrl Pts',(373.103029044526,-12.285920442078,3.21269957052663));
#42899=CARTESIAN_POINT('Ctrl Pts',(373.008408058142,-12.2917945807784,3.27951804702221));
#42900=CARTESIAN_POINT('Ctrl Pts',(372.91095507135,-12.2976687194787,3.34206640715571));
#42901=CARTESIAN_POINT('Ctrl Pts',(372.811101273794,-12.303542858179,3.40012004319834));
#42902=CARTESIAN_POINT('Ctrl Pts',(372.785849878519,-12.3050283319603,3.41480086002022));
#42903=CARTESIAN_POINT('Ctrl Pts',(372.76044505565,-12.3065138057415,3.42919447683105));
#42904=CARTESIAN_POINT('Ctrl Pts',(372.734893978377,-12.3079992795227,3.44329774961413));
#42905=CARTESIAN_POINT('Ctrl Pts',(372.633862850537,-12.3138729689133,3.49906328702403));
#42906=CARTESIAN_POINT('Ctrl Pts',(372.530207018652,-12.3197466583038,3.55047134344603));
#42907=CARTESIAN_POINT('Ctrl Pts',(372.424338775647,-12.3256203476944,3.59726597101978));
#42908=CARTESIAN_POINT('Ctrl Pts',(372.31860721849,-12.3314864536001,3.64400018233316));
#42909=CARTESIAN_POINT('Ctrl Pts',(372.210669305144,-12.3373525595059,3.68613264456589));
#42910=CARTESIAN_POINT('Ctrl Pts',(372.100963236915,-12.3432186654116,3.72345249358361));
#42911=CARTESIAN_POINT('Ctrl Pts',(371.991369506302,-12.3490787644997,3.76073412755138));
#42912=CARTESIAN_POINT('Ctrl Pts',(371.880011610985,-12.3549388635877,3.79321281834832));
#42913=CARTESIAN_POINT('Ctrl Pts',(371.767348500337,-12.3607989626757,3.82072543001294));
#42914=CARTESIAN_POINT('Ctrl Pts',(371.650620761683,-12.3668704807698,3.84923063394015));
#42915=CARTESIAN_POINT('Ctrl Pts',(371.532492264303,-12.3729419988639,3.87240448109277));
#42916=CARTESIAN_POINT('Ctrl Pts',(371.413491945943,-12.379013516958,3.89012163952794));
#42917=CARTESIAN_POINT('Ctrl Pts',(371.298767404124,-12.3848668805548,3.90720220630131));
#42918=CARTESIAN_POINT('Ctrl Pts',(371.183233057243,-12.3907202441515,3.91921139624767));
#42919=CARTESIAN_POINT('Ctrl Pts',(371.067373280744,-12.3965736077483,3.92608891490036));
#42920=CARTESIAN_POINT('Ctrl Pts',(370.951530900201,-12.4024260924821,3.93296540091676));
#42921=CARTESIAN_POINT('Ctrl Pts',(370.835363599504,-12.408278577216,3.93471172321431));
#42922=CARTESIAN_POINT('Ctrl Pts',(370.719359583573,-12.4141310619499,3.93131957442268));
#42923=CARTESIAN_POINT('Ctrl Pts',(370.603344931632,-12.4199840832781,3.92792711461654));
#42924=CARTESIAN_POINT('Ctrl Pts',(370.48749400721,-12.4258371046063,3.91939525923777));
#42925=CARTESIAN_POINT('Ctrl Pts',(370.372293007109,-12.4316901259344,3.90576779155804));
#42926=CARTESIAN_POINT('Ctrl Pts',(370.257053585249,-12.4375450993582,3.89213577885466));
#42927=CARTESIAN_POINT('Ctrl Pts',(370.142464928797,-12.443400072782,3.87340482300757));
#42928=CARTESIAN_POINT('Ctrl Pts',(370.029005416085,-12.4492550462058,3.84967022984951));
#42929=CARTESIAN_POINT('Ctrl Pts',(369.915417311589,-12.45511665549,3.8259087365787));
#42930=CARTESIAN_POINT('Ctrl Pts',(369.802961309736,-12.4609782647741,3.79713237170392));
#42931=CARTESIAN_POINT('Ctrl Pts',(369.692103038645,-12.4668398740583,3.76348698913067));
#42932=CARTESIAN_POINT('Ctrl Pts',(369.581170015007,-12.4727054358686,3.72981891922885));
#42933=CARTESIAN_POINT('Ctrl Pts',(369.471837256076,-12.4785709976789,3.69127543104224));
#42934=CARTESIAN_POINT('Ctrl Pts',(369.364551107941,-12.4844365594893,3.6480508102905));
#42935=CARTESIAN_POINT('Ctrl Pts',(369.257108081144,-12.4903106981896,3.60476298454168));
#42936=CARTESIAN_POINT('Ctrl Pts',(369.151718012278,-12.4961848368899,3.55678053593318));
#42937=CARTESIAN_POINT('Ctrl Pts',(369.048803392988,-12.5020589755902,3.50434403452155));
#42938=CARTESIAN_POINT('Ctrl Pts',(369.022777965861,-12.5035444493716,3.49108369934611));
#42939=CARTESIAN_POINT('Ctrl Pts',(368.9969107006,-12.505029923153,3.47753874390215));
#42940=CARTESIAN_POINT('Ctrl Pts',(368.971208127801,-12.5065153969343,3.46371349147624));
#42941=CARTESIAN_POINT('Ctrl Pts',(368.869577973802,-12.5123890863249,3.40904727015684));
#42942=CARTESIAN_POINT('Ctrl Pts',(368.770186568244,-12.5182627757155,3.34981325754346));
#42943=CARTESIAN_POINT('Ctrl Pts',(368.67347249404,-12.524136465106,3.28621915484853));
#42944=CARTESIAN_POINT('Ctrl Pts',(368.576883286792,-12.5300025710118,3.22270715811459));
#42945=CARTESIAN_POINT('Ctrl Pts',(368.482964878732,-12.5358686769175,3.1548464910175));
#42946=CARTESIAN_POINT('Ctrl Pts',(368.392132013744,-12.5417347828233,3.08289106610039));
#42947=CARTESIAN_POINT('Ctrl Pts',(368.301392160452,-12.5475948819113,3.01100932262175));
#42948=CARTESIAN_POINT('Ctrl Pts',(368.21373188753,-12.5534549809994,2.93504141652399));
#42949=CARTESIAN_POINT('Ctrl Pts',(368.12953708023,-12.5593150800874,2.85528456901245));
#42950=CARTESIAN_POINT('Ctrl Pts',(368.042304716361,-12.5653865981815,2.77265027639719));
#42951=CARTESIAN_POINT('Ctrl Pts',(367.958792968798,-12.5714581162756,2.68594873601823));
#42952=CARTESIAN_POINT('Ctrl Pts',(367.879393897138,-12.5775296343697,2.59555647477586));
#42953=CARTESIAN_POINT('Ctrl Pts',(367.802847697578,-12.5833829979665,2.50841207971957));
#42954=CARTESIAN_POINT('Ctrl Pts',(367.730124012735,-12.5892363615633,2.4178379575032));
#42955=CARTESIAN_POINT('Ctrl Pts',(367.661536093058,-12.59508972516,2.32420844640926));
#42956=CARTESIAN_POINT('Ctrl Pts',(367.592958471627,-12.6009422098939,2.23059299347138));
#42957=CARTESIAN_POINT('Ctrl Pts',(367.528515624721,-12.6067946946278,2.13392339703362));
#42958=CARTESIAN_POINT('Ctrl Pts',(367.468479193618,-12.6126471793617,2.03460539601712));
#42959=CARTESIAN_POINT('Ctrl Pts',(367.408437257981,-12.6185002006899,1.93527828887332));
#42960=CARTESIAN_POINT('Ctrl Pts',(367.352802755018,-12.6243532220181,1.83330264802757));
#42961=CARTESIAN_POINT('Ctrl Pts',(367.301802465215,-12.6302062433463,1.72911076379639));
#42962=CARTESIAN_POINT('Ctrl Pts',(367.250785165829,-12.6360612167701,1.62488412955972));
#42963=CARTESIAN_POINT('Ctrl Pts',(367.204405334497,-12.6419161901939,1.51844015302647));
#42964=CARTESIAN_POINT('Ctrl Pts',(367.162842218422,-12.6477711636177,1.41023248546389));
#42965=CARTESIAN_POINT('Ctrl Pts',(367.121231995895,-12.6536327729019,1.30190217840888));
#42966=CARTESIAN_POINT('Ctrl Pts',(367.084449532938,-12.6594943821861,1.19180457649475));
#42967=CARTESIAN_POINT('Ctrl Pts',(367.052624688804,-12.6653559914702,1.08041001947464));
#42968=CARTESIAN_POINT('Ctrl Pts',(367.020778384944,-12.6712215532806,0.968940348286627));
#42969=CARTESIAN_POINT('Ctrl Pts',(366.993896452045,-12.6770871150909,0.856172381466249));
#42970=CARTESIAN_POINT('Ctrl Pts',(366.972057598752,-12.6829526769013,0.74258651127268));
#42971=CARTESIAN_POINT('Ctrl Pts',(366.950186811699,-12.6888268156016,0.628834550678171));
#42972=CARTESIAN_POINT('Ctrl Pts',(366.933373881095,-12.6947009543019,0.514262707040079));
#42973=CARTESIAN_POINT('Ctrl Pts',(366.921645690772,-12.7005750930023,0.399356418718606));
#42974=CARTESIAN_POINT('Ctrl Pts',(366.918679822903,-12.7020605667835,0.370298494262007));
#42975=CARTESIAN_POINT('Ctrl Pts',(366.916038864731,-12.7035460405648,0.341219179107332));
#42976=CARTESIAN_POINT('Ctrl Pts',(366.913722723663,-12.705031514346,0.312126304660802));
#42977=CARTESIAN_POINT('Ctrl Pts',(366.905508391466,-12.7102998355524,0.208946693323902));
#42978=CARTESIAN_POINT('Ctrl Pts',(366.901366522409,-12.7155681567587,0.105438589692428));
#42979=CARTESIAN_POINT('Ctrl Pts',(366.901318279586,-12.720836477965,0.00183132919630113));
#42980=CARTESIAN_POINT('',(366.901318610208,-13.9708364779208,0.0024401713694973));
#42981=CARTESIAN_POINT('Ctrl Pts',(366.901318279586,-12.7208364780083,0.00183132834482709));
#42982=CARTESIAN_POINT('Ctrl Pts',(366.901265096517,-12.7266442978278,-0.112385758538794));
#42983=CARTESIAN_POINT('Ctrl Pts',(366.906191542405,-12.7324521176473,-0.226804680662638));
#42984=CARTESIAN_POINT('Ctrl Pts',(366.916124073898,-12.7382599374667,-0.340949420952398));
#42985=CARTESIAN_POINT('Ctrl Pts',(366.926044537002,-12.7440607005732,-0.454955471218333));
#42986=CARTESIAN_POINT('Ctrl Pts',(366.940958958238,-12.7498614636797,-0.568687584188307));
#42987=CARTESIAN_POINT('Ctrl Pts',(366.960841789125,-12.7556622267863,-0.681668673808639));
#42988=CARTESIAN_POINT('Ctrl Pts',(366.980706057939,-12.7614575744574,-0.794544287343653));
#42989=CARTESIAN_POINT('Ctrl Pts',(367.005529440934,-12.7672529221286,-0.906669857240528));
#42990=CARTESIAN_POINT('Ctrl Pts',(367.03523455997,-12.7730482697998,-1.01757315752793));
#42991=CARTESIAN_POINT('Ctrl Pts',(367.064921968539,-12.778840162231,-1.12841033624065));
#42992=CARTESIAN_POINT('Ctrl Pts',(367.09948521823,-12.7846320546623,-1.23802628648387));
#42993=CARTESIAN_POINT('Ctrl Pts',(367.138795941476,-12.7904239470935,-1.34595943467496));
#42994=CARTESIAN_POINT('Ctrl Pts',(367.178095158455,-12.7962141442351,-1.45386099078354));
#42995=CARTESIAN_POINT('Ctrl Pts',(367.22213894297,-12.8020043413767,-1.56008032651987));
#42996=CARTESIAN_POINT('Ctrl Pts',(367.270749445553,-12.8077945385184,-1.66417222782126));
#42997=CARTESIAN_POINT('Ctrl Pts',(367.319358096353,-12.8135845150864,-1.76826016381273));
#42998=CARTESIAN_POINT('Ctrl Pts',(367.372532939982,-12.8193744916544,-1.87022044337752));
#42999=CARTESIAN_POINT('Ctrl Pts',(367.43004883268,-12.8251644682224,-1.96962977124236));
#43000=CARTESIAN_POINT('Ctrl Pts',(367.487577179154,-12.83095569848,-2.06906062396677));
#43001=CARTESIAN_POINT('Ctrl Pts',(367.5494482303,-12.8367469287375,-2.16593906156535));
#43002=CARTESIAN_POINT('Ctrl Pts',(367.61539237484,-12.842538158995,-2.25986897067346));
#43003=CARTESIAN_POINT('Ctrl Pts',(367.681406160354,-12.8483355051392,-2.35389807540132));
#43004=CARTESIAN_POINT('Ctrl Pts',(367.751501382006,-12.8541328512834,-2.44497208956146));
#43005=CARTESIAN_POINT('Ctrl Pts',(367.825366830433,-12.8599301974275,-2.53272634574798));
#43006=CARTESIAN_POINT('Ctrl Pts',(367.899276057181,-12.8657309795229,-2.62053261182553));
#43007=CARTESIAN_POINT('Ctrl Pts',(367.976959672241,-12.8715317616182,-2.70501489314302));
#43008=CARTESIAN_POINT('Ctrl Pts',(368.058069457938,-12.8773325437136,-2.78584526628359));
#43009=CARTESIAN_POINT('Ctrl Pts',(368.139302682601,-12.8831421538749,-2.86679865315757));
#43010=CARTESIAN_POINT('Ctrl Pts',(368.223972174227,-12.8889517640361,-2.94408875383431));
#43011=CARTESIAN_POINT('Ctrl Pts',(368.311696438841,-12.8947613741974,-3.01742774556374));
#43012=CARTESIAN_POINT('Ctrl Pts',(368.355920173985,-12.8976901267175,-3.05439954760996));
#43013=CARTESIAN_POINT('Ctrl Pts',(368.400919777681,-12.9006188792376,-3.09036789966459));
#43014=CARTESIAN_POINT('Ctrl Pts',(368.44664376155,-12.9035476317577,-3.12530021469093));
#43015=CARTESIAN_POINT('Ctrl Pts',(368.53834440102,-12.9094213211482,-3.1953578814793));
#43016=CARTESIAN_POINT('Ctrl Pts',(368.633283764046,-12.9152950105388,-3.26149287295319));
#43017=CARTESIAN_POINT('Ctrl Pts',(368.731091819641,-12.9211686999294,-3.32339122759557));
#43018=CARTESIAN_POINT('Ctrl Pts',(368.828773595847,-12.9270348058351,-3.38520966564688));
#43019=CARTESIAN_POINT('Ctrl Pts',(368.929316353155,-12.9329009117408,-3.4428021257796));
#43020=CARTESIAN_POINT('Ctrl Pts',(369.032317785736,-12.9387670176466,-3.49589541559407));
#43021=CARTESIAN_POINT('Ctrl Pts',(369.135213746161,-12.9446271167346,-3.54893433855632));
#43022=CARTESIAN_POINT('Ctrl Pts',(369.240563008995,-12.9504872158226,-3.59748306692291));
#43023=CARTESIAN_POINT('Ctrl Pts',(369.347935707373,-12.9563473149107,-3.64131255407921));
#43024=CARTESIAN_POINT('Ctrl Pts',(369.459182167752,-12.9624188330048,-3.68672330914106));
#43025=CARTESIAN_POINT('Ctrl Pts',(369.572600440471,-12.9684903510989,-3.7270676333852));
#43026=CARTESIAN_POINT('Ctrl Pts',(369.687685859732,-12.974561869193,-3.7621435474341));
#43027=CARTESIAN_POINT('Ctrl Pts',(369.798636167905,-12.9804152327898,-3.79595915585919));
#43028=CARTESIAN_POINT('Ctrl Pts',(369.911135451532,-12.9862685963865,-3.8248783041136));
#43029=CARTESIAN_POINT('Ctrl Pts',(370.024713526672,-12.9921219599832,-3.84876991185864));
#43030=CARTESIAN_POINT('Ctrl Pts',(370.138274548446,-12.9979744447171,-3.87265793235914));
#43031=CARTESIAN_POINT('Ctrl Pts',(370.252913635475,-13.003826929451,-3.8915198282893));
#43032=CARTESIAN_POINT('Ctrl Pts',(370.368149148131,-13.0096794141849,-3.90527537292721));
#43033=CARTESIAN_POINT('Ctrl Pts',(370.483395226336,-13.0155324355131,-3.91903217876389));
#43034=CARTESIAN_POINT('Ctrl Pts',(370.599237428621,-13.0213854568412,-3.92768165363084));
#43035=CARTESIAN_POINT('Ctrl Pts',(370.715188418144,-13.0272384781694,-3.93119538788108));
#43036=CARTESIAN_POINT('Ctrl Pts',(370.83117807956,-13.0330934515932,-3.93471029402954));
#43037=CARTESIAN_POINT('Ctrl Pts',(370.947276187628,-13.038948425017,-3.9330860410911));
#43038=CARTESIAN_POINT('Ctrl Pts',(371.062995538878,-13.0448033984408,-3.92634633165287));
#43039=CARTESIAN_POINT('Ctrl Pts',(371.178846043149,-13.0506650077249,-3.91959898361965));
#43040=CARTESIAN_POINT('Ctrl Pts',(371.294316521124,-13.0565266170091,-3.90772463123588));
#43041=CARTESIAN_POINT('Ctrl Pts',(371.408924924247,-13.0623882262932,-3.89079885292595));
#43042=CARTESIAN_POINT('Ctrl Pts',(371.523610608658,-13.0682537881036,-3.87386166143937));
#43043=CARTESIAN_POINT('Ctrl Pts',(371.637432656077,-13.0741193499139,-3.85186633969296));
#43044=CARTESIAN_POINT('Ctrl Pts',(371.749920945379,-13.0799849117243,-3.82493921227999));
#43045=CARTESIAN_POINT('Ctrl Pts',(371.862573720149,-13.0858590504246,-3.7979727108025));
#43046=CARTESIAN_POINT('Ctrl Pts',(371.973888448911,-13.0917331891249,-3.76606012471782));
#43047=CARTESIAN_POINT('Ctrl Pts',(372.083411777131,-13.0976073278252,-3.72937707523109));
#43048=CARTESIAN_POINT('Ctrl Pts',(372.111108438858,-13.0990928016066,-3.72010053087057));
#43049=CARTESIAN_POINT('Ctrl Pts',(372.138690650169,-13.100578275388,-3.71051915052909));
#43050=CARTESIAN_POINT('Ctrl Pts',(372.166151314215,-13.1020637491693,-3.70063624694249));
#43051=CARTESIAN_POINT('Ctrl Pts',(372.274733110197,-13.1079374385599,-3.6615584074864));
#43052=CARTESIAN_POINT('Ctrl Pts',(372.381774394173,-13.1138111279505,-3.61763252361551));
#43053=CARTESIAN_POINT('Ctrl Pts',(372.4868107445,-13.119684817341,-3.56899933374663));
#43054=CARTESIAN_POINT('Ctrl Pts',(372.59171148303,-13.1255509232468,-3.52042893389471));
#43055=CARTESIAN_POINT('Ctrl Pts',(372.69461206422,-13.1314170291526,-3.46716348634923));
#43056=CARTESIAN_POINT('Ctrl Pts',(372.795064828534,-13.1372831350583,-3.40939295165738));
#43057=CARTESIAN_POINT('Ctrl Pts',(372.895414730498,-13.1431432341464,-3.35168157325728));
#43058=CARTESIAN_POINT('Ctrl Pts',(372.993321445276,-13.1490033332344,-3.28947448839614));
#43059=CARTESIAN_POINT('Ctrl Pts',(373.088359468285,-13.1548634323224,-3.22300874922352));
#43060=CARTESIAN_POINT('Ctrl Pts',(373.186826246349,-13.1609349504166,-3.15414507781414));
#43061=CARTESIAN_POINT('Ctrl Pts',(373.282213022964,-13.1670064685107,-3.08070985512041));
#43062=CARTESIAN_POINT('Ctrl Pts',(373.374076489147,-13.1730779866048,-3.00301766082958));
#43063=CARTESIAN_POINT('Ctrl Pts',(373.462639227575,-13.1789313502015,-2.92811700916959));
#43064=CARTESIAN_POINT('Ctrl Pts',(373.547927146423,-13.1847847137983,-2.84926032365174));
#43065=CARTESIAN_POINT('Ctrl Pts',(373.629575206669,-13.190638077395,-2.7667716436326));
#43066=CARTESIAN_POINT('Ctrl Pts',(373.711211007734,-13.196490562129,-2.68429534901106));
#43067=CARTESIAN_POINT('Ctrl Pts',(373.789207746309,-13.2023430468629,-2.59818843776364));
#43068=CARTESIAN_POINT('Ctrl Pts',(373.863236905828,-13.2081955315968,-2.50881214377893));
#43069=CARTESIAN_POINT('Ctrl Pts',(373.937272852827,-13.214048552925,-2.41942765518805));
#43070=CARTESIAN_POINT('Ctrl Pts',(374.007340234067,-13.2199015742532,-2.3267735061606));
#43071=CARTESIAN_POINT('Ctrl Pts',(374.073150986761,-13.2257545955814,-2.23124380852941));
#43072=CARTESIAN_POINT('Ctrl Pts',(374.138983688613,-13.2316095690052,-2.13568224989932));
#43073=CARTESIAN_POINT('Ctrl Pts',(374.200556704717,-13.237464542429,-2.03724357567743));
#43074=CARTESIAN_POINT('Ctrl Pts',(374.257625834908,-13.2433195158529,-1.93635003616015));
#43075=CARTESIAN_POINT('Ctrl Pts',(374.314759645629,-13.249181125137,-1.83534214677508));
#43076=CARTESIAN_POINT('Ctrl Pts',(374.367379178491,-13.2550427344212,-1.73187419864738));
#43077=CARTESIAN_POINT('Ctrl Pts',(374.415286619531,-13.2609043437053,-1.62639223274409));
#43078=CARTESIAN_POINT('Ctrl Pts',(374.463226364911,-13.2667699055157,-1.52083913957675));
#43079=CARTESIAN_POINT('Ctrl Pts',(374.506447537913,-13.272635467326,-1.41326970682986));
#43080=CARTESIAN_POINT('Ctrl Pts',(374.544801432953,-13.2785010291364,-1.30414746273616));
#43081=CARTESIAN_POINT('Ctrl Pts',(374.583211410794,-13.2843751678367,-1.19486565515765));
#43082=CARTESIAN_POINT('Ctrl Pts',(374.61673978746,-13.290249306537,-1.0840268986315));
#43083=CARTESIAN_POINT('Ctrl Pts',(374.645288371022,-13.2961234452374,-0.972107356456605));
#43084=CARTESIAN_POINT('Ctrl Pts',(374.652507841745,-13.2976089190186,-0.943804731341924));
#43085=CARTESIAN_POINT('Ctrl Pts',(374.659409111743,-13.2990943927998,-0.915433025324876));
#43086=CARTESIAN_POINT('Ctrl Pts',(374.665991117463,-13.300579866581,-0.886999997809702));
#43087=CARTESIAN_POINT('Ctrl Pts',(374.692016926641,-13.3064535559716,-0.774573394143596));
#43088=CARTESIAN_POINT('Ctrl Pts',(374.713133759842,-13.3123272453622,-0.660813123817876));
#43089=CARTESIAN_POINT('Ctrl Pts',(374.729208113275,-13.3182009347527,-0.546185739618226));
#43090=CARTESIAN_POINT('Ctrl Pts',(374.745261713206,-13.3240670406585,-0.431706350140542));
#43091=CARTESIAN_POINT('Ctrl Pts',(374.7562857234,-13.3299331465642,-0.316362478562879));
#43092=CARTESIAN_POINT('Ctrl Pts',(374.762197088704,-13.33579925247,-0.200633276123563));
#43093=CARTESIAN_POINT('Ctrl Pts',(374.768102400844,-13.341659351558,-0.0850225789127362));
#43094=CARTESIAN_POINT('Ctrl Pts',(374.768905460556,-13.3475194506461,0.0309722541648994));
#43095=CARTESIAN_POINT('Ctrl Pts',(374.76457479454,-13.3533795497341,0.146865160044948));
#43096=CARTESIAN_POINT('Ctrl Pts',(374.760087887974,-13.3594510678282,0.26693921757465));
#43097=CARTESIAN_POINT('Ctrl Pts',(374.750089772911,-13.3655225859223,0.386903407149259));
#43098=CARTESIAN_POINT('Ctrl Pts',(374.734604471114,-13.3715941040164,0.506214676110398));
#43099=CARTESIAN_POINT('Ctrl Pts',(374.719675568586,-13.3774474676132,0.621238995826725));
#43100=CARTESIAN_POINT('Ctrl Pts',(374.699647068922,-13.38330083121,0.735656062532786));
#43101=CARTESIAN_POINT('Ctrl Pts',(374.674593373812,-13.3891541948067,0.848983466255619));
#43102=CARTESIAN_POINT('Ctrl Pts',(374.649543440429,-13.3950066795406,0.962293854250114));
#43103=CARTESIAN_POINT('Ctrl Pts',(374.619469901018,-13.4008591642745,1.07451450128166));
#43104=CARTESIAN_POINT('Ctrl Pts',(374.584498211296,-13.4067116490084,1.18517352397492));
#43105=CARTESIAN_POINT('Ctrl Pts',(374.549523315139,-13.4125646703366,1.29584269261457));
#43106=CARTESIAN_POINT('Ctrl Pts',(374.509649500417,-13.4184176916647,1.40494955832535));
#43107=CARTESIAN_POINT('Ctrl Pts',(374.465051780819,-13.4242707129929,1.51203840791429));
#43108=CARTESIAN_POINT('Ctrl Pts',(374.420439187021,-13.4301256864167,1.6191629737025));
#43109=CARTESIAN_POINT('Ctrl Pts',(374.371099714255,-13.4359806598405,1.72426780385694));
#43110=CARTESIAN_POINT('Ctrl Pts',(374.317255799529,-13.4418356332643,1.8269187891613));
#43111=CARTESIAN_POINT('Ctrl Pts',(374.263350859641,-13.4476972425485,1.92968611617289));
#43112=CARTESIAN_POINT('Ctrl Pts',(374.204931480124,-13.4535588518326,2.02999368131795));
#43113=CARTESIAN_POINT('Ctrl Pts',(374.142265235874,-13.4594204611168,2.1274334569198));
#43114=CARTESIAN_POINT('Ctrl Pts',(374.079556735314,-13.4652860229271,2.22493893687804));
#43115=CARTESIAN_POINT('Ctrl Pts',(374.012595905819,-13.4711515847375,2.31957244030342));
#43116=CARTESIAN_POINT('Ctrl Pts',(373.941691639087,-13.4770171465478,2.41095772566206));
#43117=CARTESIAN_POINT('Ctrl Pts',(373.870683692927,-13.4828912852482,2.50247663872151));
#43118=CARTESIAN_POINT('Ctrl Pts',(373.795721067923,-13.4887654239485,2.59073754083909));
#43119=CARTESIAN_POINT('Ctrl Pts',(373.717150657053,-13.4946395626489,2.67539978791368));
#43120=CARTESIAN_POINT('Ctrl Pts',(373.697281482816,-13.4961250364301,2.6968094880769));
#43121=CARTESIAN_POINT('Ctrl Pts',(373.677181759714,-13.4976105102114,2.71798925108762));
#43122=CARTESIAN_POINT('Ctrl Pts',(373.656857431475,-13.4990959839926,2.73893397678799));
#43123=CARTESIAN_POINT('Ctrl Pts',(373.576493312867,-13.5049696733832,2.82175119960748));
#43124=CARTESIAN_POINT('Ctrl Pts',(373.492347301133,-13.5108433627738,2.90116636477356));
#43125=CARTESIAN_POINT('Ctrl Pts',(373.404739070565,-13.5167170521643,2.97681436529804));
#43126=CARTESIAN_POINT('Ctrl Pts',(373.317243950452,-13.5225831580701,3.05236469714692));
#43127=CARTESIAN_POINT('Ctrl Pts',(373.226295810814,-13.5284492639758,3.12415726923927));
#43128=CARTESIAN_POINT('Ctrl Pts',(373.132252261207,-13.5343153698816,3.19186253723524));
#43129=CARTESIAN_POINT('Ctrl Pts',(373.038305010998,-13.5401754689696,3.25949847589931));
#43130=CARTESIAN_POINT('Ctrl Pts',(372.941268988835,-13.5460355680577,3.32305519551618));
#43131=CARTESIAN_POINT('Ctrl Pts',(372.841535575353,-13.5518956671457,3.38224274941507));
#43132=CARTESIAN_POINT('Ctrl Pts',(372.738204007841,-13.5579671852398,3.44356565523023));
#43133=CARTESIAN_POINT('Ctrl Pts',(372.63197708469,-13.5640387033339,3.50019788883422));
#43134=CARTESIAN_POINT('Ctrl Pts',(372.523324159736,-13.570110221428,3.55186524189211));
#43135=CARTESIAN_POINT('Ctrl Pts',(372.41857522121,-13.5759635850248,3.60167614566312));
#43136=CARTESIAN_POINT('Ctrl Pts',(372.311572022044,-13.5818169486215,3.64687262031137));
#43137=CARTESIAN_POINT('Ctrl Pts',(372.202760268987,-13.5876703122183,3.68725566712433));
#43138=CARTESIAN_POINT('Ctrl Pts',(372.093964853649,-13.5935227969522,3.72763265055867));
#43139=CARTESIAN_POINT('Ctrl Pts',(371.983361811586,-13.5993752816861,3.76319749948606));
#43140=CARTESIAN_POINT('Ctrl Pts',(371.871415680838,-13.60522776642,3.79379982286338));
#43141=CARTESIAN_POINT('Ctrl Pts',(371.759459286133,-13.6110807877482,3.82440495206294));
#43142=CARTESIAN_POINT('Ctrl Pts',(371.646159956491,-13.6169338090764,3.85004654227227));
#43143=CARTESIAN_POINT('Ctrl Pts',(371.53199550787,-13.6227868304046,3.87062461241184));
#43144=CARTESIAN_POINT('Ctrl Pts',(371.4177929832,-13.6286418038284,3.89120954573506));
#43145=CARTESIAN_POINT('Ctrl Pts',(371.302725172188,-13.6344967772522,3.90672752767294));
#43146=CARTESIAN_POINT('Ctrl Pts',(371.187277445431,-13.6403517506759,3.91713013905194));
#43147=CARTESIAN_POINT('Ctrl Pts',(371.071698873503,-13.6462133599601,3.92754454045484));
#43148=CARTESIAN_POINT('Ctrl Pts',(370.955739938115,-13.6520749692443,3.93283196250979));
#43149=CARTESIAN_POINT('Ctrl Pts',(370.839888563019,-13.6579365785284,3.93299605481526));
#43150=CARTESIAN_POINT('Ctrl Pts',(370.723959068491,-13.6638021403388,3.93316025776937));
#43151=CARTESIAN_POINT('Ctrl Pts',(370.60813769042,-13.6696677021491,3.92819426955626));
#43152=CARTESIAN_POINT('Ctrl Pts',(370.492908040648,-13.6755332639594,3.91815369018076));
#43153=CARTESIAN_POINT('Ctrl Pts',(370.377509896867,-13.6814074026597,3.90809842901557));
#43154=CARTESIAN_POINT('Ctrl Pts',(370.262705616231,-13.6872815413601,3.89295382146564));
#43155=CARTESIAN_POINT('Ctrl Pts',(370.148969498636,-13.6931556800604,3.87282669801567));
#43156=CARTESIAN_POINT('Ctrl Pts',(370.120207491251,-13.6946411538417,3.86773687707284));
#43157=CARTESIAN_POINT('Ctrl Pts',(370.091513719128,-13.696126627623,3.86232867299299));
#43158=CARTESIAN_POINT('Ctrl Pts',(370.062895690121,-13.6976121014043,3.85660431549224));
#43159=CARTESIAN_POINT('Ctrl Pts',(369.949737574861,-13.7034857907949,3.83396972015764));
#43160=CARTESIAN_POINT('Ctrl Pts',(369.83738803511,-13.7093594801855,3.80631288254161));
#43161=CARTESIAN_POINT('Ctrl Pts',(369.72632717161,-13.715233169576,3.77370449948814));
#43162=CARTESIAN_POINT('Ctrl Pts',(369.615409698119,-13.7210992754818,3.7411382169206));
#43163=CARTESIAN_POINT('Ctrl Pts',(369.505777984912,-13.7269653813875,3.70363321764485));
#43164=CARTESIAN_POINT('Ctrl Pts',(369.397902814227,-13.7328314872933,3.66131135465738));
#43165=CARTESIAN_POINT('Ctrl Pts',(369.290138106343,-13.7386915863813,3.61903282871851));
#43166=CARTESIAN_POINT('Ctrl Pts',(369.184126745581,-13.7445516854694,3.57194740002689));
#43167=CARTESIAN_POINT('Ctrl Pts',(369.080324547569,-13.7504117845574,3.52022676595108));
#43168=CARTESIAN_POINT('Ctrl Pts',(368.972777403064,-13.7564833026515,3.46664016939145));
#43169=CARTESIAN_POINT('Ctrl Pts',(368.867602267396,-13.7625548207456,3.40807772474953));
#43170=CARTESIAN_POINT('Ctrl Pts',(368.765284001161,-13.7686263388397,3.34478518279095));
#43171=CARTESIAN_POINT('Ctrl Pts',(368.666642112003,-13.7744797024365,3.28376679244713));
#43172=CARTESIAN_POINT('Ctrl Pts',(368.570655707714,-13.7803330660332,3.21835260328292));
#43173=CARTESIAN_POINT('Ctrl Pts',(368.477733630341,-13.7861864296299,3.14880926708183));
#43174=CARTESIAN_POINT('Ctrl Pts',(368.384825504906,-13.7920389143638,3.0792763725786));
#43175=CARTESIAN_POINT('Ctrl Pts',(368.294981122219,-13.7978913990977,3.00561581126936));
#43176=CARTESIAN_POINT('Ctrl Pts',(368.208578687543,-13.8037438838316,2.92813640969977));
#43177=CARTESIAN_POINT('Ctrl Pts',(368.122168330924,-13.8095969051598,2.85064990430941));
#43178=CARTESIAN_POINT('Ctrl Pts',(368.039200857267,-13.815449926488,2.76934413845824));
#43179=CARTESIAN_POINT('Ctrl Pts',(367.960019310032,-13.8213029478161,2.68456642395093));
#43180=CARTESIAN_POINT('Ctrl Pts',(367.880811354222,-13.8271579212399,2.599760434439));
#43181=CARTESIAN_POINT('Ctrl Pts',(367.805392117466,-13.8330128946637,2.51148049548522));
#43182=CARTESIAN_POINT('Ctrl Pts',(367.734065410794,-13.8388678680875,2.42010821931692));
#43183=CARTESIAN_POINT('Ctrl Pts',(367.66265786446,-13.8447294773717,2.32863238440924));
#43184=CARTESIAN_POINT('Ctrl Pts',(367.595352360455,-13.8505910866558,2.23405754283356));
#43185=CARTESIAN_POINT('Ctrl Pts',(367.532410340101,-13.85645269594,2.13679567923062));
#43186=CARTESIAN_POINT('Ctrl Pts',(367.469425877479,-13.8623182577503,2.03946823123901));
#43187=CARTESIAN_POINT('Ctrl Pts',(367.410810965714,-13.8681838195607,1.93945050893014));
#43188=CARTESIAN_POINT('Ctrl Pts',(367.356781054262,-13.874049381371,1.83717903642075));
#43189=CARTESIAN_POINT('Ctrl Pts',(367.302672137828,-13.8799235200713,1.7347580179346));
#43190=CARTESIAN_POINT('Ctrl Pts',(367.253161777958,-13.8857976587717,1.63007704423034));
#43191=CARTESIAN_POINT('Ctrl Pts',(367.208417326641,-13.891671797472,1.52359258705272));
#43192=CARTESIAN_POINT('Ctrl Pts',(367.197102185361,-13.8931572712533,1.49666440620367));
#43193=CARTESIAN_POINT('Ctrl Pts',(367.186091574914,-13.8946427450346,1.46962096545369));
#43194=CARTESIAN_POINT('Ctrl Pts',(367.175387691731,-13.896128218816,1.44246978246126));
#43195=CARTESIAN_POINT('Ctrl Pts',(367.127536355304,-13.902768977543,1.32109136590888));
#43196=CARTESIAN_POINT('Ctrl Pts',(367.085685534993,-13.90940973627,1.19722064348745));
#43197=CARTESIAN_POINT('Ctrl Pts',(367.050069812319,-13.9160504949971,1.07142697600303));
#43198=CARTESIAN_POINT('Ctrl Pts',(367.014571606434,-13.9226693420351,0.946048374301991));
#43199=CARTESIAN_POINT('Ctrl Pts',(366.985267539514,-13.9292881890731,0.81875967944162));
#43200=CARTESIAN_POINT('Ctrl Pts',(366.962343410939,-13.9359070361111,0.690147026575956));
#43201=CARTESIAN_POINT('Ctrl Pts',(366.93956000388,-13.9424852528505,0.562323872313213));
#43202=CARTESIAN_POINT('Ctrl Pts',(366.923078544681,-13.9490634695899,0.433193162774451));
#43203=CARTESIAN_POINT('Ctrl Pts',(366.913033877604,-13.9556416863293,0.303349604497033));
#43204=CARTESIAN_POINT('Ctrl Pts',(366.905299936483,-13.9607066168598,0.203375914276909));
#43205=CARTESIAN_POINT('Ctrl Pts',(366.901380988686,-13.9657715473903,0.102980039154434));
#43206=CARTESIAN_POINT('Ctrl Pts',(366.901318610208,-13.9708364779208,0.00244017136950739));
#43207=CARTESIAN_POINT('',(366.901319086285,-15.2208364780051,-0.00311436343212247));
#43208=CARTESIAN_POINT('Ctrl Pts',(366.901318610208,-13.9708364779651,0.00244017049049901));
#43209=CARTESIAN_POINT('Ctrl Pts',(366.901245969927,-13.9767346357568,-0.114639422405236));
#43210=CARTESIAN_POINT('Ctrl Pts',(366.906405595384,-13.9826327935485,-0.231739061658494));
#43211=CARTESIAN_POINT('Ctrl Pts',(366.916776250793,-13.9885309513401,-0.348363019306832));
#43212=CARTESIAN_POINT('Ctrl Pts',(366.927148018102,-13.9944297415088,-0.46499948091072));
#43213=CARTESIAN_POINT('Ctrl Pts',(366.942731891741,-14.0003285316774,-0.581159756870668));
#43214=CARTESIAN_POINT('Ctrl Pts',(366.963454737144,-14.006227321846,-0.696353169425402));
#43215=CARTESIAN_POINT('Ctrl Pts',(366.984184520303,-14.0121280868579,-0.811585147335559));
#43216=CARTESIAN_POINT('Ctrl Pts',(367.010056627378,-14.0180288518699,-0.925849220139976));
#43217=CARTESIAN_POINT('Ctrl Pts',(367.040946903125,-14.0239296168818,-1.0386654104878));
#43218=CARTESIAN_POINT('Ctrl Pts',(367.071876808775,-14.029837952132,-1.15162633553298));
#43219=CARTESIAN_POINT('Ctrl Pts',(367.107837636474,-14.0357462873822,-1.26313527712464));
#43220=CARTESIAN_POINT('Ctrl Pts',(367.148655325033,-14.0416546226323,-1.37272747779266));
#43221=CARTESIAN_POINT('Ctrl Pts',(367.189499302339,-14.0475667631625,-1.48239026162705));
#43222=CARTESIAN_POINT('Ctrl Pts',(367.235206215648,-14.0534789036927,-1.5901334729216));
#43223=CARTESIAN_POINT('Ctrl Pts',(367.285554573887,-14.0593910442229,-1.69551413654578));
#43224=CARTESIAN_POINT('Ctrl Pts',(367.335995824196,-14.0653140925759,-1.80108922613311));
#43225=CARTESIAN_POINT('Ctrl Pts',(367.39109544319,-14.071237140929,-1.90429269979353));
#43226=CARTESIAN_POINT('Ctrl Pts',(367.450586467606,-14.0771601892821,-2.0047071880907));
#43227=CARTESIAN_POINT('Ctrl Pts',(367.509123319511,-14.0829882382639,-2.10351113521302));
#43228=CARTESIAN_POINT('Ctrl Pts',(367.571911478936,-14.0888162872458,-2.19961464379094));
#43229=CARTESIAN_POINT('Ctrl Pts',(367.638658335005,-14.0946443362276,-2.29265113866326));
#43230=CARTESIAN_POINT('Ctrl Pts',(367.705927896665,-14.1005180256182,-2.38641621760659));
#43231=CARTESIAN_POINT('Ctrl Pts',(367.777439788768,-14.1063917150087,-2.47737427957401));
#43232=CARTESIAN_POINT('Ctrl Pts',(367.852931686877,-14.1122654043993,-2.56511705914408));
#43233=CARTESIAN_POINT('Ctrl Pts',(367.928326117852,-14.118131510305,-2.65274655454247));
#43234=CARTESIAN_POINT('Ctrl Pts',(368.007690068925,-14.1239976162108,-2.73716871266057));
#43235=CARTESIAN_POINT('Ctrl Pts',(368.090718449835,-14.1298637221165,-2.81800484629188));
#43236=CARTESIAN_POINT('Ctrl Pts',(368.173661810741,-14.1357238212045,-2.89875820475225));
#43237=CARTESIAN_POINT('Ctrl Pts',(368.260261843529,-14.1415839202926,-2.97593255623396));
#43238=CARTESIAN_POINT('Ctrl Pts',(368.350174215594,-14.1474440193806,-3.04918339684968));
#43239=CARTESIAN_POINT('Ctrl Pts',(368.443330420921,-14.1535155374747,-3.12507696068299));
#43240=CARTESIAN_POINT('Ctrl Pts',(368.540042186724,-14.1595870555688,-3.19675822350987));
#43241=CARTESIAN_POINT('Ctrl Pts',(368.639885738655,-14.1656585736629,-3.26388674658754));
#43242=CARTESIAN_POINT('Ctrl Pts',(368.736141831973,-14.1715119372597,-3.32860328818311));
#43243=CARTESIAN_POINT('Ctrl Pts',(368.835308157173,-14.1773653008564,-3.38908837641716));
#43244=CARTESIAN_POINT('Ctrl Pts',(368.936973234927,-14.1832186644531,-3.44507944747595));
#43245=CARTESIAN_POINT('Ctrl Pts',(369.038623048013,-14.189071149187,-3.50106211166386));
#43246=CARTESIAN_POINT('Ctrl Pts',(369.142770505862,-14.1949236339209,-3.55255190110144));
#43247=CARTESIAN_POINT('Ctrl Pts',(369.248978334202,-14.2007761186548,-3.59933155036128));
#43248=CARTESIAN_POINT('Ctrl Pts',(369.355195900373,-14.206629139983,-3.64611548868689));
#43249=CARTESIAN_POINT('Ctrl Pts',(369.463473834451,-14.2124821613112,-3.68818826180188));
#43250=CARTESIAN_POINT('Ctrl Pts',(369.573354294008,-14.2183351826393,-3.72538050436855));
#43251=CARTESIAN_POINT('Ctrl Pts',(369.683271400821,-14.2241901560632,-3.76258515126637));
#43252=CARTESIAN_POINT('Ctrl Pts',(369.794791704764,-14.230045129487,-3.79490589851788));
#43253=CARTESIAN_POINT('Ctrl Pts',(369.907442286025,-14.2359001029108,-3.82222326440111));
#43254=CARTESIAN_POINT('Ctrl Pts',(370.020220542249,-14.2417617121949,-3.84957159100977));
#43255=CARTESIAN_POINT('Ctrl Pts',(370.134131230905,-14.2476233214791,-3.87190512047534));
#43256=CARTESIAN_POINT('Ctrl Pts',(370.248691226803,-14.2534849307632,-3.8891554937322));
#43257=CARTESIAN_POINT('Ctrl Pts',(370.363328471349,-14.2593504925736,-3.90641749904246));
#43258=CARTESIAN_POINT('Ctrl Pts',(370.478615485115,-14.2652160543839,-3.91858947974169));
#43259=CARTESIAN_POINT('Ctrl Pts',(370.594065744978,-14.2710816161943,-3.92565509494702));
#43260=CARTESIAN_POINT('Ctrl Pts',(370.709684821437,-14.2769557548946,-3.93273104181472));
#43261=CARTESIAN_POINT('Ctrl Pts',(370.825467208893,-14.2828298935949,-3.93468571446805));
#43262=CARTESIAN_POINT('Ctrl Pts',(370.940928037821,-14.2887040322952,-3.93155481566012));
#43263=CARTESIAN_POINT('Ctrl Pts',(370.970126196545,-14.2901895060766,-3.93076306246387));
#43264=CARTESIAN_POINT('Ctrl Pts',(370.999303827869,-14.2916749798579,-3.9296463438869));
#43265=CARTESIAN_POINT('Ctrl Pts',(371.028453177175,-14.2931604536392,-3.92820575784855));
#43266=CARTESIAN_POINT('Ctrl Pts',(371.143712177982,-14.2990341430298,-3.92250955840297));
#43267=CARTESIAN_POINT('Ctrl Pts',(371.258912228079,-14.3049078324204,-3.91172678479568));
#43268=CARTESIAN_POINT('Ctrl Pts',(371.373568050256,-14.3107815218109,-3.89585654574198));
#43269=CARTESIAN_POINT('Ctrl Pts',(371.488075840995,-14.3166476277167,-3.88000679665785));
#43270=CARTESIAN_POINT('Ctrl Pts',(371.602040395648,-14.3225137336225,-3.85908270064155));
#43271=CARTESIAN_POINT('Ctrl Pts',(371.714978108051,-14.3283798395282,-3.83313533749692));
#43272=CARTESIAN_POINT('Ctrl Pts',(371.827800173676,-14.3342399386162,-3.80721454412161));
#43273=CARTESIAN_POINT('Ctrl Pts',(371.939597088257,-14.3401000377043,-3.77628080694578));
#43274=CARTESIAN_POINT('Ctrl Pts',(372.049892696494,-14.3459601367923,-3.74043671252544));
#43275=CARTESIAN_POINT('Ctrl Pts',(372.164167518653,-14.3520316548864,-3.70329944495187));
#43276=CARTESIAN_POINT('Ctrl Pts',(372.276830214372,-14.3581031729805,-3.66089088357033));
#43277=CARTESIAN_POINT('Ctrl Pts',(372.3873649782,-14.3641746910746,-3.61338257420981));
#43278=CARTESIAN_POINT('Ctrl Pts',(372.493928139627,-14.3700280546714,-3.56758127637227));
#43279=CARTESIAN_POINT('Ctrl Pts',(372.598513241972,-14.3758814182681,-3.51704057673411));
#43280=CARTESIAN_POINT('Ctrl Pts',(372.700676583944,-14.3817347818649,-3.46196390626241));
#43281=CARTESIAN_POINT('Ctrl Pts',(372.802824586435,-14.3875872665988,-3.40689550536744));
#43282=CARTESIAN_POINT('Ctrl Pts',(372.902551187998,-14.3934397513327,-3.34729268384393));
#43283=CARTESIAN_POINT('Ctrl Pts',(372.999436768247,-14.3992922360666,-3.2834051050411));
#43284=CARTESIAN_POINT('Ctrl Pts',(373.096331231603,-14.4051452573948,-3.21951166860511));
#43285=CARTESIAN_POINT('Ctrl Pts',(373.190383810901,-14.410998278723,-3.15133292138041));
#43286=CARTESIAN_POINT('Ctrl Pts',(373.281203986385,-14.4168513000512,-3.07916177739099));
#43287=CARTESIAN_POINT('Ctrl Pts',(373.372054452151,-14.422706273475,-3.00696656293132));
#43288=CARTESIAN_POINT('Ctrl Pts',(373.459670047133,-14.4285612468988,-2.93077656089247));
#43289=CARTESIAN_POINT('Ctrl Pts',(373.543693995571,-14.4344162203226,-2.85092439732811));
#43290=CARTESIAN_POINT('Ctrl Pts',(373.627813174363,-14.4402778296068,-2.77098173159286));
#43291=CARTESIAN_POINT('Ctrl Pts',(373.708332282154,-14.446139438891,-2.68736890477264));
#43292=CARTESIAN_POINT('Ctrl Pts',(373.784931969527,-14.4520010481751,-2.60045483265399));
#43293=CARTESIAN_POINT('Ctrl Pts',(373.861583308632,-14.4578666099855,-2.5134821537382));
#43294=CARTESIAN_POINT('Ctrl Pts',(373.934309706187,-14.4637321717958,-2.42320411789462));
#43295=CARTESIAN_POINT('Ctrl Pts',(374.00283368201,-14.4695977336062,-2.3300206957733));
#43296=CARTESIAN_POINT('Ctrl Pts',(374.071457856692,-14.4754718723065,-2.23670101663432));
#43297=CARTESIAN_POINT('Ctrl Pts',(374.135867116908,-14.4813460110068,-2.14046781452352));
#43298=CARTESIAN_POINT('Ctrl Pts',(374.195828611582,-14.4872201497072,-2.04174788390892));
#43299=CARTESIAN_POINT('Ctrl Pts',(374.210991894706,-14.4887056234884,-2.01678322507182));
#43300=CARTESIAN_POINT('Ctrl Pts',(374.225870978771,-14.4901910972697,-1.99165964874743));
#43301=CARTESIAN_POINT('Ctrl Pts',(374.240462582516,-14.4916765710509,-1.96638426639299));
#43302=CARTESIAN_POINT('Ctrl Pts',(374.298159021989,-14.4975502604415,-1.8664432596576));
#43303=CARTESIAN_POINT('Ctrl Pts',(374.351549215539,-14.503423949832,-1.7637943094351));
#43304=CARTESIAN_POINT('Ctrl Pts',(374.40036934082,-14.5092976392226,-1.65884471479912));
#43305=CARTESIAN_POINT('Ctrl Pts',(374.449126434732,-14.5151637451284,-1.55403061994929));
#43306=CARTESIAN_POINT('Ctrl Pts',(374.493325021649,-14.5210298510341,-1.44692215891161));
#43307=CARTESIAN_POINT('Ctrl Pts',(374.53274585683,-14.5268959569399,-1.33795340058751));
#43308=CARTESIAN_POINT('Ctrl Pts',(374.572126325577,-14.5327560560279,-1.22909622488415));
#43309=CARTESIAN_POINT('Ctrl Pts',(374.606738634181,-14.5386161551159,-1.11838292713463));
#43310=CARTESIAN_POINT('Ctrl Pts',(374.636410858612,-14.5444762542039,-1.00626923752171));
#43311=CARTESIAN_POINT('Ctrl Pts',(374.667153589207,-14.550547772298,-0.890110741759438));
#43312=CARTESIAN_POINT('Ctrl Pts',(374.692592861174,-14.5566192903922,-0.772449309986367));
#43313=CARTESIAN_POINT('Ctrl Pts',(374.71259320278,-14.5626908084863,-0.653811374196177));
#43314=CARTESIAN_POINT('Ctrl Pts',(374.731874916127,-14.568544172083,-0.539436194252071));
#43315=CARTESIAN_POINT('Ctrl Pts',(374.746101748309,-14.5743975356797,-0.424153918084294));
#43316=CARTESIAN_POINT('Ctrl Pts',(374.755204109274,-14.5802508992765,-0.308447673230766));
#43317=CARTESIAN_POINT('Ctrl Pts',(374.764305103549,-14.5861033840104,-0.192758801280381));
#43318=CARTESIAN_POINT('Ctrl Pts',(374.768283124115,-14.5919558687443,-0.0766464989810674));
#43319=CARTESIAN_POINT('Ctrl Pts',(374.767120484841,-14.5978083534782,0.0394012784874696));
#43320=CARTESIAN_POINT('Ctrl Pts',(374.765957738968,-14.6036613748064,0.155459695978858));
#43321=CARTESIAN_POINT('Ctrl Pts',(374.759653400435,-14.6095143961346,0.271453163731976));
#43322=CARTESIAN_POINT('Ctrl Pts',(374.74824190272,-14.6153674174627,0.386894733452537));
#43323=CARTESIAN_POINT('Ctrl Pts',(374.736826599051,-14.6212223908865,0.50237480516592));
#43324=CARTESIAN_POINT('Ctrl Pts',(374.720300789811,-14.6270773643103,0.617302201915252));
#43325=CARTESIAN_POINT('Ctrl Pts',(374.698750571753,-14.6329323377342,0.731196802483956));
#43326=CARTESIAN_POINT('Ctrl Pts',(374.67717592929,-14.6387939470183,0.845220487953348));
#43327=CARTESIAN_POINT('Ctrl Pts',(374.650565588938,-14.6446555563025,0.958208634741834));
#43328=CARTESIAN_POINT('Ctrl Pts',(374.61905643117,-14.6505171655866,1.06969289827048));
#43329=CARTESIAN_POINT('Ctrl Pts',(374.587526026544,-14.6563827273969,1.18125233645673));
#43330=CARTESIAN_POINT('Ctrl Pts',(374.551090356411,-14.6622482892073,1.29130548088762));
#43331=CARTESIAN_POINT('Ctrl Pts',(374.509935094599,-14.6681138510176,1.39940233489322));
#43332=CARTESIAN_POINT('Ctrl Pts',(374.4687196537,-14.6739879897179,1.50765725301193));
#43333=CARTESIAN_POINT('Ctrl Pts',(374.422771011365,-14.6798621284183,1.61394979394341));
#43334=CARTESIAN_POINT('Ctrl Pts',(374.372321575551,-14.6857362671186,1.71785292176003));
#43335=CARTESIAN_POINT('Ctrl Pts',(374.359563736827,-14.6872217408999,1.74412832655396));
#43336=CARTESIAN_POINT('Ctrl Pts',(374.346518291478,-14.6887072146812,1.77025106732983));
#43337=CARTESIAN_POINT('Ctrl Pts',(374.333189436515,-14.6901926884625,1.79621453162981));
#43338=CARTESIAN_POINT('Ctrl Pts',(374.280486012888,-14.6960663778531,1.89887627276619));
#43339=CARTESIAN_POINT('Ctrl Pts',(374.223172626226,-14.7019400672436,1.99938744358015));
#43340=CARTESIAN_POINT('Ctrl Pts',(374.161448512536,-14.7078137566342,2.09730555138372));
#43341=CARTESIAN_POINT('Ctrl Pts',(374.099804090476,-14.71367986254,2.19509723771105));
#43342=CARTESIAN_POINT('Ctrl Pts',(374.033760484505,-14.7195459684457,2.29030217257058));
#43343=CARTESIAN_POINT('Ctrl Pts',(373.963563591468,-14.7254120743514,2.38250081000633));
#43344=CARTESIAN_POINT('Ctrl Pts',(373.893438579156,-14.7312721734395,2.47460503721192));
#43345=CARTESIAN_POINT('Ctrl Pts',(373.819168987959,-14.7371322725275,2.56370876344664));
#43346=CARTESIAN_POINT('Ctrl Pts',(373.741044569875,-14.7429923716155,2.64942046393343));
#43347=CARTESIAN_POINT('Ctrl Pts',(373.660101601016,-14.7490638897097,2.73822444703425));
#43348=CARTESIAN_POINT('Ctrl Pts',(373.575020647871,-14.7551354078038,2.8233866481389));
#43349=CARTESIAN_POINT('Ctrl Pts',(373.486170634858,-14.7612069258979,2.90450784549498));
#43350=CARTESIAN_POINT('Ctrl Pts',(373.400513073819,-14.7670602894946,2.98271429339955));
#43351=CARTESIAN_POINT('Ctrl Pts',(373.311352973549,-14.7729136530914,3.05716483048401));
#43352=CARTESIAN_POINT('Ctrl Pts',(373.21905858448,-14.7787670166881,3.12753907164879));
#43353=CARTESIAN_POINT('Ctrl Pts',(373.126778053102,-14.784619501422,3.19790274635807));
#43354=CARTESIAN_POINT('Ctrl Pts',(373.031364497107,-14.7904719861559,3.26419109167765));
#43355=CARTESIAN_POINT('Ctrl Pts',(372.933218361241,-14.7963244708898,3.32612472066898));
#43356=CARTESIAN_POINT('Ctrl Pts',(372.835063226692,-14.802177492218,3.38806402814259));
#43357=CARTESIAN_POINT('Ctrl Pts',(372.734175363635,-14.8080305135462,3.44564760508579));
#43358=CARTESIAN_POINT('Ctrl Pts',(372.630982625259,-14.8138835348744,3.49864040691914));
#43359=CARTESIAN_POINT('Ctrl Pts',(372.527755470112,-14.8197385082982,3.55165088287532));
#43360=CARTESIAN_POINT('Ctrl Pts',(372.422222278399,-14.825593481722,3.60006735054329));
#43361=CARTESIAN_POINT('Ctrl Pts',(372.314833173612,-14.8314484551459,3.64370187942084));
#43362=CARTESIAN_POINT('Ctrl Pts',(372.20732235707,-14.83731006443,3.68738586243212));
#43363=CARTESIAN_POINT('Ctrl Pts',(372.097951812086,-14.8431716737142,3.72627693362258));
#43364=CARTESIAN_POINT('Ctrl Pts',(371.987189296493,-14.8490332829983,3.76023622067742));
#43365=CARTESIAN_POINT('Ctrl Pts',(371.876352092922,-14.8548988448087,3.79421840672896));
#43366=CARTESIAN_POINT('Ctrl Pts',(371.764121448728,-14.860764406619,3.8232620835104));
#43367=CARTESIAN_POINT('Ctrl Pts',(371.650976155193,-14.8666299684294,3.84727932672243));
#43368=CARTESIAN_POINT('Ctrl Pts',(371.537665415487,-14.8725041071297,3.87133168903465));
#43369=CARTESIAN_POINT('Ctrl Pts',(371.423437763215,-14.87837824583,3.89034288170026));
#43370=CARTESIAN_POINT('Ctrl Pts',(371.308778030582,-14.8842523845304,3.90427669871148));
#43371=CARTESIAN_POINT('Ctrl Pts',(371.279782456033,-14.8857378583117,3.90780033356239));
#43372=CARTESIAN_POINT('Ctrl Pts',(371.25075925197,-14.887223332093,3.91099952969364));
#43373=CARTESIAN_POINT('Ctrl Pts',(371.221716250132,-14.8887088058742,3.9138742292099));
#43374=CARTESIAN_POINT('Ctrl Pts',(371.106877756236,-14.8945824952648,3.9252410350481));
#43375=CARTESIAN_POINT('Ctrl Pts',(370.991347298652,-14.9004561846554,3.93156820814741));
#43376=CARTESIAN_POINT('Ctrl Pts',(370.875604715191,-14.906329874046,3.93278328859206));
#43377=CARTESIAN_POINT('Ctrl Pts',(370.760011566279,-14.9121959799517,3.9339968002537));
#43378=CARTESIAN_POINT('Ctrl Pts',(370.644207245485,-14.9180620858574,3.93011134058085));
#43379=CARTESIAN_POINT('Ctrl Pts',(370.528677603588,-14.9239281917632,3.92110609876889));
#43380=CARTESIAN_POINT('Ctrl Pts',(370.413266262572,-14.9297882908512,3.91211007820978));
#43381=CARTESIAN_POINT('Ctrl Pts',(370.298129450435,-14.9356483899393,3.89800473537626));
#43382=CARTESIAN_POINT('Ctrl Pts',(370.183753245832,-14.9415084890274,3.87882130184023));
#43383=CARTESIAN_POINT('Ctrl Pts',(370.065250608702,-14.9475800071215,3.85894577378668));
#43384=CARTESIAN_POINT('Ctrl Pts',(369.947564948923,-14.9536515252156,3.83361882040805));
#43385=CARTESIAN_POINT('Ctrl Pts',(369.831231733103,-14.9597230433097,3.80293402988006));
#43386=CARTESIAN_POINT('Ctrl Pts',(369.719078462698,-14.9655764069064,3.77335176839843));
#43387=CARTESIAN_POINT('Ctrl Pts',(369.608182553798,-14.9714297705032,3.73879018073696));
#43388=CARTESIAN_POINT('Ctrl Pts',(369.499012860579,-14.9772831340999,3.69938502681424));
#43389=CARTESIAN_POINT('Ctrl Pts',(369.389859558822,-14.9831356188338,3.65998578944272));
#43390=CARTESIAN_POINT('Ctrl Pts',(369.282432345887,-14.9889881035677,3.61574457207696));
#43391=CARTESIAN_POINT('Ctrl Pts',(369.177183077718,-14.9948405883016,3.56684641326339));
#43392=CARTESIAN_POINT('Ctrl Pts',(369.071924159605,-15.0006936096298,3.51794377114532));
#43393=CARTESIAN_POINT('Ctrl Pts',(368.968843957921,-15.006546630958,3.46438351286968));
#43394=CARTESIAN_POINT('Ctrl Pts',(368.868371925755,-15.0123996522861,3.40639774692673));
#43395=CARTESIAN_POINT('Ctrl Pts',(368.767866384225,-15.0182546257099,3.34839264161094));
#43396=CARTESIAN_POINT('Ctrl Pts',(368.669971099555,-15.0241095991338,3.28595930008585));
#43397=CARTESIAN_POINT('Ctrl Pts',(368.575088007447,-15.0299645725576,3.21937408574269));
#43398=CARTESIAN_POINT('Ctrl Pts',(368.480097377542,-15.0358261818417,3.15271340561161));
#43399=CARTESIAN_POINT('Ctrl Pts',(368.388126092574,-15.0416877911259,3.08189169799442));
#43400=CARTESIAN_POINT('Ctrl Pts',(368.29954442401,-15.04754940041,3.00722673946475));
#43401=CARTESIAN_POINT('Ctrl Pts',(368.210903024176,-15.0534149622204,2.93251143380498));
#43402=CARTESIAN_POINT('Ctrl Pts',(368.125656095021,-15.0592805240307,2.85394799620949));
#43403=CARTESIAN_POINT('Ctrl Pts',(368.04413707733,-15.0651460858411,2.77189109415042));
#43404=CARTESIAN_POINT('Ctrl Pts',(367.962498858841,-15.0710202245414,2.68971420477493));
#43405=CARTESIAN_POINT('Ctrl Pts',(367.884599707743,-15.0768943632418,2.60403396056261));
#43406=CARTESIAN_POINT('Ctrl Pts',(367.810732880377,-15.0827685019421,2.51523814219873));
#43407=CARTESIAN_POINT('Ctrl Pts',(367.792053165621,-15.0842539757234,2.49278312933733));
#43408=CARTESIAN_POINT('Ctrl Pts',(367.773631101045,-15.0857394495046,2.47012901786266));
#43409=CARTESIAN_POINT('Ctrl Pts',(367.755470980959,-15.0872249232859,2.44728235746135));
#43410=CARTESIAN_POINT('Ctrl Pts',(367.683793739455,-15.093088026749,2.35710753552393));
#43411=CARTESIAN_POINT('Ctrl Pts',(367.615956575156,-15.098951130212,2.26362391034172));
#43412=CARTESIAN_POINT('Ctrl Pts',(367.552281197227,-15.1048142336751,2.1671927437798));
#43413=CARTESIAN_POINT('Ctrl Pts',(367.488685545306,-15.1106699961243,2.070882315755));
#43414=CARTESIAN_POINT('Ctrl Pts',(367.429241547768,-15.1165257585734,1.97163202414228));
#43415=CARTESIAN_POINT('Ctrl Pts',(367.374231072832,-15.1223815210226,1.86983648273214));
#43416=CARTESIAN_POINT('Ctrl Pts',(367.319276074643,-15.1282313780755,1.76814359968881));
#43417=CARTESIAN_POINT('Ctrl Pts',(367.26874590511,-15.1340812351284,1.66391093220002));
#43418=CARTESIAN_POINT('Ctrl Pts',(367.222879046891,-15.1399310921813,1.55756179592009));
#43419=CARTESIAN_POINT('Ctrl Pts',(367.177047273904,-15.1457764744652,1.45129400997268));
#43420=CARTESIAN_POINT('Ctrl Pts',(367.135871881179,-15.1516218567491,1.34291335396061));
#43421=CARTESIAN_POINT('Ctrl Pts',(367.099544979911,-15.157467239033,1.23286681550194));
#43422=CARTESIAN_POINT('Ctrl Pts',(367.063234004256,-15.1633100587175,1.122868521141));
#43423=CARTESIAN_POINT('Ctrl Pts',(367.031767424684,-15.169152878402,1.0112061886496));
#43424=CARTESIAN_POINT('Ctrl Pts',(367.005288628067,-15.1749956980865,0.898345252612361));
#43425=CARTESIAN_POINT('Ctrl Pts',(366.978816924361,-15.1808369526468,0.785514548789961));
#43426=CARTESIAN_POINT('Ctrl Pts',(366.957330437256,-15.1866782072072,0.671486283929554));
#43427=CARTESIAN_POINT('Ctrl Pts',(366.940922026421,-15.1925194617675,0.556738660264014));
#43428=CARTESIAN_POINT('Ctrl Pts',(366.92450971715,-15.1983621041381,0.441963773973242));
#43429=CARTESIAN_POINT('Ctrl Pts',(366.913177954739,-15.2042047465087,0.326469597483944));
#43430=CARTESIAN_POINT('Ctrl Pts',(366.906967993488,-15.2100473888794,0.210741735856712));
#43431=CARTESIAN_POINT('Ctrl Pts',(366.903145532068,-15.2136437519079,0.139506945751349));
#43432=CARTESIAN_POINT('Ctrl Pts',(366.901262628572,-15.2172401149365,0.0681837294482758));
#43433=CARTESIAN_POINT('Ctrl Pts',(366.901319086285,-15.2208364779651,-0.00311436263953608));
#43434=CARTESIAN_POINT('',(366.901317920817,-16.47083647792,-0.000729168186946121));
#43435=CARTESIAN_POINT('Ctrl Pts',(366.901319086285,-15.2208364780051,-0.00311436343211994));
#43436=CARTESIAN_POINT('Ctrl Pts',(366.901426740083,-15.2276940359743,-0.139065822086587));
#43437=CARTESIAN_POINT('Ctrl Pts',(366.908587402639,-15.2345515939436,-0.274721646700906));
#43438=CARTESIAN_POINT('Ctrl Pts',(366.92268598836,-15.2414091519128,-0.409420509722039));
#43439=CARTESIAN_POINT('Ctrl Pts',(366.936878419049,-15.2483123561134,-0.545015974052312));
#43440=CARTESIAN_POINT('Ctrl Pts',(366.958101331657,-15.2552155603139,-0.679641608731294));
#43441=CARTESIAN_POINT('Ctrl Pts',(366.98618838034,-15.2621187645144,-0.812642947378062));
#43442=CARTESIAN_POINT('Ctrl Pts',(367.014475827037,-15.2690712223202,-0.946593235997586));
#43443=CARTESIAN_POINT('Ctrl Pts',(367.04972563269,-15.2760236801261,-1.07889588617637));
#43444=CARTESIAN_POINT('Ctrl Pts',(367.091719796211,-15.2829761379319,-1.20890395964389));
#43445=CARTESIAN_POINT('Ctrl Pts',(367.097286641879,-15.2838977721871,-1.22613813744253));
#43446=CARTESIAN_POINT('Ctrl Pts',(367.102971936878,-15.2848194064424,-1.24333202509166));
#43447=CARTESIAN_POINT('Ctrl Pts',(367.108775111529,-15.2857410406976,-1.26048414500428));
#43448=CARTESIAN_POINT('Ctrl Pts',(367.145759463176,-15.2916147300882,-1.36979673205895));
#43449=CARTESIAN_POINT('Ctrl Pts',(367.187620563434,-15.2974884194787,-1.4776622410702));
#43450=CARTESIAN_POINT('Ctrl Pts',(367.234226623194,-15.3033621088693,-1.58361363200196));
#43451=CARTESIAN_POINT('Ctrl Pts',(367.280772510153,-15.3092282147751,-1.68942822973434));
#43452=CARTESIAN_POINT('Ctrl Pts',(367.332051008801,-15.3150943206809,-1.79333324928479));
#43453=CARTESIAN_POINT('Ctrl Pts',(367.387880794919,-15.3209604265866,-1.89487746388623));
#43454=CARTESIAN_POINT('Ctrl Pts',(367.443653412048,-15.3268205256747,-1.99631769850556));
#43455=CARTESIAN_POINT('Ctrl Pts',(367.50396784874,-15.3326806247627,-2.09540157677105));
#43456=CARTESIAN_POINT('Ctrl Pts',(367.568595272185,-15.3385407238508,-2.19169911796628));
#43457=CARTESIAN_POINT('Ctrl Pts',(367.63555430563,-15.3446122419449,-2.29147085475769));
#43458=CARTESIAN_POINT('Ctrl Pts',(367.70714322511,-15.350683760039,-2.38825099576136));
#43459=CARTESIAN_POINT('Ctrl Pts',(367.783056026683,-15.3567552781331,-2.48159026954379));
#43460=CARTESIAN_POINT('Ctrl Pts',(367.856241220628,-15.3626086417299,-2.57157578862457));
#43461=CARTESIAN_POINT('Ctrl Pts',(367.933444640014,-15.3684620053266,-2.65836310329369));
#43462=CARTESIAN_POINT('Ctrl Pts',(368.014349319108,-15.3743153689234,-2.74158101587276));
#43463=CARTESIAN_POINT('Ctrl Pts',(368.095241850636,-15.3801678536573,-2.82478643356228));
#43464=CARTESIAN_POINT('Ctrl Pts',(368.179834248955,-15.3860203383912,-2.9044232186531));
#43465=CARTESIAN_POINT('Ctrl Pts',(368.267771658926,-15.3918728231251,-2.98015597453164));
#43466=CARTESIAN_POINT('Ctrl Pts',(368.355717131578,-15.3977258444533,-3.05589567408727));
#43467=CARTESIAN_POINT('Ctrl Pts',(368.447007912489,-15.4035788657815,-3.12773036324572));
#43468=CARTESIAN_POINT('Ctrl Pts',(368.541255497375,-15.4094318871097,-3.19536445999363));
#43469=CARTESIAN_POINT('Ctrl Pts',(368.635534515651,-15.4152868605335,-3.26302111401864));
#43470=CARTESIAN_POINT('Ctrl Pts',(368.732771963341,-15.4211418339573,-3.32647414910308));
#43471=CARTESIAN_POINT('Ctrl Pts',(368.832550360121,-15.4269968073811,-3.38547129711021));
#43472=CARTESIAN_POINT('Ctrl Pts',(368.932441842899,-15.4328584166653,-3.44453531080686));
#43473=CARTESIAN_POINT('Ctrl Pts',(369.034879666925,-15.4387200259495,-3.49913314718487));
#43474=CARTESIAN_POINT('Ctrl Pts',(369.139421674341,-15.4445816352336,-3.54905845863487));
#43475=CARTESIAN_POINT('Ctrl Pts',(369.2440341752,-15.450447197044,-3.59901743508896));
#43476=CARTESIAN_POINT('Ctrl Pts',(369.35075330534,-15.4563127588543,-3.64429745186666));
#43477=CARTESIAN_POINT('Ctrl Pts',(369.459118479303,-15.4621783206647,-3.68474092467395));
#43478=CARTESIAN_POINT('Ctrl Pts',(369.567642109729,-15.468052459365,-3.72524353575792));
#43479=CARTESIAN_POINT('Ctrl Pts',(369.677816196019,-15.4739265980653,-3.76089536180227));
#43480=CARTESIAN_POINT('Ctrl Pts',(369.78916654942,-15.4798007367657,-3.7915890800767));
#43481=CARTESIAN_POINT('Ctrl Pts',(369.817325235985,-15.4812862105468,-3.79935102034902));
#43482=CARTESIAN_POINT('Ctrl Pts',(369.84555910456,-15.482771684328,-3.8067961459464));
#43483=CARTESIAN_POINT('Ctrl Pts',(369.873860417607,-15.4842571581092,-3.81392324442529));
#43484=CARTESIAN_POINT('Ctrl Pts',(369.985766211092,-15.4901308474997,-3.84210439662835));
#43485=CARTESIAN_POINT('Ctrl Pts',(370.099099745348,-15.4960045368903,-3.86540310393339));
#43486=CARTESIAN_POINT('Ctrl Pts',(370.213397118836,-15.5018782262808,-3.88367692291822));
#43487=CARTESIAN_POINT('Ctrl Pts',(370.327546923678,-15.5077443321866,-3.90192714868599));
#43488=CARTESIAN_POINT('Ctrl Pts',(370.442657688797,-15.5136104380923,-3.91516532321915));
#43489=CARTESIAN_POINT('Ctrl Pts',(370.558251947216,-15.519476543998,-3.92329920035934));
#43490=CARTESIAN_POINT('Ctrl Pts',(370.673727838588,-15.5253366430861,-3.93142474851296));
#43491=CARTESIAN_POINT('Ctrl Pts',(370.789685828807,-15.5311967421741,-3.93445636685652));
#43492=CARTESIAN_POINT('Ctrl Pts',(370.905640549261,-15.5370568412621,-3.93235324875957));
#43493=CARTESIAN_POINT('Ctrl Pts',(371.025778651495,-15.5431283593562,-3.93017425495966));
#43494=CARTESIAN_POINT('Ctrl Pts',(371.145912797567,-15.5491998774503,-3.9224829590621));
#43495=CARTESIAN_POINT('Ctrl Pts',(371.265499573519,-15.5552713955444,-3.90929294426539));
#43496=CARTESIAN_POINT('Ctrl Pts',(371.380789501039,-15.5611247591412,-3.89657685724157));
#43497=CARTESIAN_POINT('Ctrl Pts',(371.495570270525,-15.5669781227379,-3.87875044681748));
#43498=CARTESIAN_POINT('Ctrl Pts',(371.609358131515,-15.5728314863346,-3.85587883199502));
#43499=CARTESIAN_POINT('Ctrl Pts',(371.72312890764,-15.5786839710685,-3.83301065126854));
#43500=CARTESIAN_POINT('Ctrl Pts',(371.835906666765,-15.5845364558024,-3.80509885377174));
#43501=CARTESIAN_POINT('Ctrl Pts',(371.947217202139,-15.5903889405363,-3.77225980536663));
#43502=CARTESIAN_POINT('Ctrl Pts',(372.058537943194,-15.5962419618645,-3.73941774606172));
#43503=CARTESIAN_POINT('Ctrl Pts',(372.168390796794,-15.6020949831926,-3.7016476546982));
#43504=CARTESIAN_POINT('Ctrl Pts',(372.276316771186,-15.6079480045208,-3.65911575665432));
#43505=CARTESIAN_POINT('Ctrl Pts',(372.384278740974,-15.6138029779446,-3.61656967340109));
#43506=CARTESIAN_POINT('Ctrl Pts',(372.490312169504,-15.6196579513684,-3.56925877688727));
#43507=CARTESIAN_POINT('Ctrl Pts',(372.593978753825,-15.6255129247922,-3.51739712214837));
#43508=CARTESIAN_POINT('Ctrl Pts',(372.697762830903,-15.6313745340763,-3.46547668888518));
#43509=CARTESIAN_POINT('Ctrl Pts',(372.799174339944,-15.6372361433605,-3.40899538788675));
#43510=CARTESIAN_POINT('Ctrl Pts',(372.897800187449,-15.6430977526446,-3.34821290487047));
#43511=CARTESIAN_POINT('Ctrl Pts',(372.996492539088,-15.6489633144549,-3.28738943577955));
#43512=CARTESIAN_POINT('Ctrl Pts',(373.092395147963,-15.6548288762653,-3.22225924103046));
#43513=CARTESIAN_POINT('Ctrl Pts',(373.185125906998,-15.6606944380756,-3.15312392625312));
#43514=CARTESIAN_POINT('Ctrl Pts',(373.277992261147,-15.6665685767759,-3.08388751868903));
#43515=CARTESIAN_POINT('Ctrl Pts',(373.367677190384,-15.6724427154762,-3.01063456340494));
#43516=CARTESIAN_POINT('Ctrl Pts',(373.453833448343,-15.6783168541765,-2.93370534425832));
#43517=CARTESIAN_POINT('Ctrl Pts',(373.475620959471,-15.679802327958,-2.91425120061299));
#43518=CARTESIAN_POINT('Ctrl Pts',(373.497183005625,-15.6812878017394,-2.89456213268642));
#43519=CARTESIAN_POINT('Ctrl Pts',(373.518514373385,-15.6827732755208,-2.87464398511441));
#43520=CARTESIAN_POINT('Ctrl Pts',(373.602860411711,-15.6886469649114,-2.79588593934087));
#43521=CARTESIAN_POINT('Ctrl Pts',(373.683877685125,-15.694520654302,-2.71328133197832));
#43522=CARTESIAN_POINT('Ctrl Pts',(373.761195011868,-15.7003943436926,-2.62714276319492));
#43523=CARTESIAN_POINT('Ctrl Pts',(373.838412514679,-15.7062604495983,-2.5411154073962));
#43524=CARTESIAN_POINT('Ctrl Pts',(373.911939297212,-15.7121265555041,-2.45156346849149));
#43525=CARTESIAN_POINT('Ctrl Pts',(373.981439004909,-15.7179926614098,-2.35883815820824));
#43526=CARTESIAN_POINT('Ctrl Pts',(374.05086754579,-15.7238527604979,-2.26620779746146));
#43527=CARTESIAN_POINT('Ctrl Pts',(374.116276967849,-15.7297128595859,-2.1704108574716));
#43528=CARTESIAN_POINT('Ctrl Pts',(374.177369858013,-15.735572958674,-2.0718330756301));
#43529=CARTESIAN_POINT('Ctrl Pts',(374.240666840279,-15.7416444767681,-1.96969883231179));
#43530=CARTESIAN_POINT('Ctrl Pts',(374.299329647164,-15.7477159948622,-1.86457964199185));
#43531=CARTESIAN_POINT('Ctrl Pts',(374.35307510286,-15.7537875129563,-1.75693950326599));
#43532=CARTESIAN_POINT('Ctrl Pts',(374.40488944138,-15.759640876553,-1.65316696074828));
#43533=CARTESIAN_POINT('Ctrl Pts',(374.452133515632,-15.7654942401498,-1.54705191280296));
#43534=CARTESIAN_POINT('Ctrl Pts',(374.494599799898,-15.7713476037466,-1.43903616036896));
#43535=CARTESIAN_POINT('Ctrl Pts',(374.537059707995,-15.7772000884805,-1.3310366261367));
#43536=CARTESIAN_POINT('Ctrl Pts',(374.574743101381,-15.7830525732144,-1.22113733926093));
#43537=CARTESIAN_POINT('Ctrl Pts',(374.607490691213,-15.7889050579483,-1.10979986243639));
#43538=CARTESIAN_POINT('Ctrl Pts',(374.640241283559,-15.7947580792765,-0.998452177460075));
#43539=CARTESIAN_POINT('Ctrl Pts',(374.668055056145,-15.8006111006046,-0.88566643678181));
#43540=CARTESIAN_POINT('Ctrl Pts',(374.690822865664,-15.8064641219328,-0.77191844713202));
#43541=CARTESIAN_POINT('Ctrl Pts',(374.713598268688,-15.8123190953567,-0.658132520330992));
#43542=CARTESIAN_POINT('Ctrl Pts',(374.73132428118,-15.8181740687805,-0.543384111297028));
#43543=CARTESIAN_POINT('Ctrl Pts',(374.743943167067,-15.8240290422043,-0.428157570708126));
#43544=CARTESIAN_POINT('Ctrl Pts',(374.756576354842,-15.8298906514885,-0.312800435635769));
#43545=CARTESIAN_POINT('Ctrl Pts',(374.764090817968,-15.8357522607726,-0.196964498326556));
#43546=CARTESIAN_POINT('Ctrl Pts',(374.766480830481,-15.8416138700568,-0.0811376625844174));
#43547=CARTESIAN_POINT('Ctrl Pts',(374.768872454596,-15.8474794318671,0.0347672760436905));
#43548=CARTESIAN_POINT('Ctrl Pts',(374.76613275726,-15.8533449936775,0.150662688876631));
#43549=CARTESIAN_POINT('Ctrl Pts',(374.75830803617,-15.8592105554878,0.266063985059273));
#43550=CARTESIAN_POINT('Ctrl Pts',(374.750471873418,-15.8650846941882,0.381634026240967));
#43551=CARTESIAN_POINT('Ctrl Pts',(374.737535893395,-15.8709588328885,0.496708099823931));
#43552=CARTESIAN_POINT('Ctrl Pts',(374.719597793738,-15.8768329715888,0.610809940846733));
#43553=CARTESIAN_POINT('Ctrl Pts',(374.715061541177,-15.8783184453701,0.639664433713723));
#43554=CARTESIAN_POINT('Ctrl Pts',(374.710205653192,-15.8798039191513,0.668456821280135));
#43555=CARTESIAN_POINT('Ctrl Pts',(374.705032214831,-15.8812893929325,0.697179554237102));
#43556=CARTESIAN_POINT('Ctrl Pts',(374.684576000529,-15.8871630823231,0.810751677804809));
#43557=CARTESIAN_POINT('Ctrl Pts',(374.659082935221,-15.8930367717137,0.923611871718623));
#43558=CARTESIAN_POINT('Ctrl Pts',(374.628614478119,-15.8989104611042,1.03527876550775));
#43559=CARTESIAN_POINT('Ctrl Pts',(374.598185358657,-15.90477656701,1.14680148684628));
#43560=CARTESIAN_POINT('Ctrl Pts',(374.562793729788,-15.9106426729157,1.25713357699837));
#43561=CARTESIAN_POINT('Ctrl Pts',(374.522552376477,-15.9165087788215,1.36580199936999));
#43562=CARTESIAN_POINT('Ctrl Pts',(374.4823522298,-15.9223688779095,1.4743591466615));
#43563=CARTESIAN_POINT('Ctrl Pts',(374.437312379196,-15.9282289769976,1.58125562959299));
#43564=CARTESIAN_POINT('Ctrl Pts',(374.387595732367,-15.9340890760856,1.68603241771671));
#43565=CARTESIAN_POINT('Ctrl Pts',(374.336085422343,-15.9401605941797,1.79458931332171));
#43566=CARTESIAN_POINT('Ctrl Pts',(374.27955460738,-15.9462321122738,1.90087024314795));
#43567=CARTESIAN_POINT('Ctrl Pts',(374.218239676841,-15.9523036303679,2.00438571429028));
#43568=CARTESIAN_POINT('Ctrl Pts',(374.159127840757,-15.9581569939647,2.10418179182708));
#43569=CARTESIAN_POINT('Ctrl Pts',(374.095569995253,-15.9640103575614,2.20140733490737));
#43570=CARTESIAN_POINT('Ctrl Pts',(374.027824887459,-15.9698637211582,2.29564845355112));
#43571=CARTESIAN_POINT('Ctrl Pts',(373.960089951365,-15.9757162058921,2.38987542220805));
#43572=CARTESIAN_POINT('Ctrl Pts',(373.888169244162,-15.981568690626,2.48111852204783));
#43573=CARTESIAN_POINT('Ctrl Pts',(373.812364268609,-15.9874211753599,2.56899368387903));
#43574=CARTESIAN_POINT('Ctrl Pts',(373.736552342758,-15.9932741966881,2.65687690268273));
#43575=CARTESIAN_POINT('Ctrl Pts',(373.656855710469,-15.9991272180163,2.74139125677456));
#43576=CARTESIAN_POINT('Ctrl Pts',(373.573615028248,-16.0049802393445,2.82218709282486));
#43577=CARTESIAN_POINT('Ctrl Pts',(373.490346583652,-16.0108352127683,2.90300987584687));
#43578=CARTESIAN_POINT('Ctrl Pts',(373.40353203505,-16.0166901861921,2.98011138715356));
#43579=CARTESIAN_POINT('Ctrl Pts',(373.313547086845,-16.0225451596159,3.05318053956203));
#43580=CARTESIAN_POINT('Ctrl Pts',(373.223460152259,-16.0284067689001,3.12633250646928));
#43581=CARTESIAN_POINT('Ctrl Pts',(373.130195967081,-16.0342683781843,3.19544273213424));
#43582=CARTESIAN_POINT('Ctrl Pts',(373.034161416605,-16.0401299874684,3.2602419076892));
#43583=CARTESIAN_POINT('Ctrl Pts',(372.938062109325,-16.0459955492788,3.32508477780416));
#43584=CARTESIAN_POINT('Ctrl Pts',(372.839189068483,-16.0518611110891,3.3856105942126));
#43585=CARTESIAN_POINT('Ctrl Pts',(372.737974597999,-16.0577266728995,3.44159555992142));
#43586=CARTESIAN_POINT('Ctrl Pts',(372.636612127135,-16.0636008115998,3.49766238938128));
#43587=CARTESIAN_POINT('Ctrl Pts',(372.532901762289,-16.0694749503001,3.54917493361627));
#43588=CARTESIAN_POINT('Ctrl Pts',(372.427296675464,-16.0753490890005,3.59595710095316));
#43589=CARTESIAN_POINT('Ctrl Pts',(372.400590873023,-16.0768345627817,3.60778754734757));
#43590=CARTESIAN_POINT('Ctrl Pts',(372.37376398075,-16.0783200365629,3.61931573371256));
#43591=CARTESIAN_POINT('Ctrl Pts',(372.346823472713,-16.0798055103441,3.63053931957964));
#43592=CARTESIAN_POINT('Ctrl Pts',(372.240298417723,-16.0856791997347,3.67491833054902));
#43593=CARTESIAN_POINT('Ctrl Pts',(372.131641077973,-16.0915528891252,3.71467889225633));
#43594=CARTESIAN_POINT('Ctrl Pts',(372.021289270468,-16.0974265785158,3.74961169384864));
#43595=CARTESIAN_POINT('Ctrl Pts',(371.911079937514,-16.1032926844216,3.78449939391228));
#43596=CARTESIAN_POINT('Ctrl Pts',(371.799180877741,-16.1091587903273,3.8145716058894));
#43597=CARTESIAN_POINT('Ctrl Pts',(371.686050729313,-16.1150248962331,3.83966666623411));
#43598=CARTESIAN_POINT('Ctrl Pts',(371.573036424716,-16.1208849953211,3.86473602955671));
#43599=CARTESIAN_POINT('Ctrl Pts',(371.458793939884,-16.1267450944091,3.88483828974794));
#43600=CARTESIAN_POINT('Ctrl Pts',(371.343797315517,-16.1326051934971,3.8998614946561));
#43601=CARTESIAN_POINT('Ctrl Pts',(371.224651875293,-16.1386767115913,3.91542670252396));
#43602=CARTESIAN_POINT('Ctrl Pts',(371.104697283495,-16.1447482296854,3.92553931799939));
#43603=CARTESIAN_POINT('Ctrl Pts',(370.984473013775,-16.1508197477795,3.9301326221592));
#43604=CARTESIAN_POINT('Ctrl Pts',(370.868568498146,-16.1566731113762,3.93456088522967));
#43605=CARTESIAN_POINT('Ctrl Pts',(370.752413798801,-16.162526474973,3.93385962051803));
#43606=CARTESIAN_POINT('Ctrl Pts',(370.636496980016,-16.1683798385697,3.92802188157386));
#43607=CARTESIAN_POINT('Ctrl Pts',(370.520597565751,-16.1742323233036,3.92218501914655));
#43608=CARTESIAN_POINT('Ctrl Pts',(370.404936373539,-16.1800848080375,3.911213236745));
#43609=CARTESIAN_POINT('Ctrl Pts',(370.289999587249,-16.1859372927714,3.89515168194081));
#43610=CARTESIAN_POINT('Ctrl Pts',(370.175052262799,-16.1917903140996,3.8790886545077));
#43611=CARTESIAN_POINT('Ctrl Pts',(370.060829885495,-16.1976433354278,3.85793498416944));
#43612=CARTESIAN_POINT('Ctrl Pts',(369.947810944906,-16.2034963567559,3.83178737686533));
#43613=CARTESIAN_POINT('Ctrl Pts',(369.834754310318,-16.2093513301797,3.80563104882924));
#43614=CARTESIAN_POINT('Ctrl Pts',(369.722902312845,-16.2152063036035,3.77447756498039));
#43615=CARTESIAN_POINT('Ctrl Pts',(369.612720034418,-16.2210612770274,3.73847398935558));
#43616=CARTESIAN_POINT('Ctrl Pts',(369.502412878531,-16.2269228863115,3.70242960830225));
#43617=CARTESIAN_POINT('Ctrl Pts',(369.393779611761,-16.2327844955957,3.66152429227512));
#43618=CARTESIAN_POINT('Ctrl Pts',(369.287267112851,-16.2386461048798,3.61595395528093));
#43619=CARTESIAN_POINT('Ctrl Pts',(369.180682791781,-16.2445116666902,3.57035288987379));
#43620=CARTESIAN_POINT('Ctrl Pts',(369.076222457472,-16.2503772285005,3.52008071851414));
#43621=CARTESIAN_POINT('Ctrl Pts',(368.97430852436,-16.2562427903108,3.46537938710012));
#43622=CARTESIAN_POINT('Ctrl Pts',(368.872245568082,-16.2621169290112,3.4105980689233));
#43623=CARTESIAN_POINT('Ctrl Pts',(368.772736797759,-16.2679910677115,3.35137487567273));
#43624=CARTESIAN_POINT('Ctrl Pts',(368.676175853458,-16.2738652064118,3.28799515036809));
#43625=CARTESIAN_POINT('Ctrl Pts',(368.651757167012,-16.2753506801931,3.27196745251969));
#43626=CARTESIAN_POINT('Ctrl Pts',(368.627526828092,-16.2768361539745,3.25567414389832));
#43627=CARTESIAN_POINT('Ctrl Pts',(368.603490855174,-16.2783216277558,3.23912023623242));
#43628=CARTESIAN_POINT('Ctrl Pts',(368.508920869072,-16.2841662522001,3.17398857614697));
#43629=CARTESIAN_POINT('Ctrl Pts',(368.417040452205,-16.2900108766443,3.10459792704851));
#43630=CARTESIAN_POINT('Ctrl Pts',(368.328260515829,-16.2958555010885,3.03119871036011));
#43631=CARTESIAN_POINT('Ctrl Pts',(368.239595465043,-16.3016925623022,2.95789447585637));
#43632=CARTESIAN_POINT('Ctrl Pts',(368.154023236462,-16.3075296235159,2.88059225098274));
#43633=CARTESIAN_POINT('Ctrl Pts',(368.071926197233,-16.3133666847296,2.7995859227593));
#43634=CARTESIAN_POINT('Ctrl Pts',(367.989912890329,-16.319197792614,2.71866221442457));
#43635=CARTESIAN_POINT('Ctrl Pts',(367.911368019625,-16.3250289004984,2.63404220735748));
#43636=CARTESIAN_POINT('Ctrl Pts',(367.836640672554,-16.3308600083827,2.54605980300708));
#43637=CARTESIAN_POINT('Ctrl Pts',(367.761897370278,-16.3366923612801,2.458058613335));
#43638=CARTESIAN_POINT('Ctrl Pts',(367.690973526947,-16.3425247141775,2.36669387758273));
#43639=CARTESIAN_POINT('Ctrl Pts',(367.624181520526,-16.3483570670749,2.27233662239791));
#43640=CARTESIAN_POINT('Ctrl Pts',(367.557477847291,-16.3541817066194,2.17810415575409));
#43641=CARTESIAN_POINT('Ctrl Pts',(367.494895343439,-16.3600063461638,2.08088741183962));
#43642=CARTESIAN_POINT('Ctrl Pts',(367.436704138707,-16.3658309857083,1.98108809670978));
#43643=CARTESIAN_POINT('Ctrl Pts',(367.378520858579,-16.3716548320407,1.88130237246761));
#43644=CARTESIAN_POINT('Ctrl Pts',(367.324727898941,-16.3774786783731,1.77893513706548));
#43645=CARTESIAN_POINT('Ctrl Pts',(367.275550703742,-16.3833025247055,1.67441493536281));
#43646=CARTESIAN_POINT('Ctrl Pts',(367.226368005011,-16.3891270227978,1.56988303656711));
#43647=CARTESIAN_POINT('Ctrl Pts',(367.181802274987,-16.3949515208901,1.46319807070222));
#43648=CARTESIAN_POINT('Ctrl Pts',(367.142031525462,-16.4007760189823,1.35481019845036));
#43649=CARTESIAN_POINT('Ctrl Pts',(367.102166045212,-16.4066143905605,1.24616415500668));
#43650=CARTESIAN_POINT('Ctrl Pts',(367.06711855498,-16.4124527621386,1.13580748026041));
#43651=CARTESIAN_POINT('Ctrl Pts',(367.037018242879,-16.4182911337167,1.02420928978219));
#43652=CARTESIAN_POINT('Ctrl Pts',(367.006944774031,-16.4241242986751,0.912710621805926));
#43653=CARTESIAN_POINT('Ctrl Pts',(366.981809722171,-16.4299574636334,0.799973067514173));
#43654=CARTESIAN_POINT('Ctrl Pts',(366.961690530963,-16.4357906285918,0.686474051132961));
#43655=CARTESIAN_POINT('Ctrl Pts',(366.941537999637,-16.4416334598636,0.572786952110634));
#43656=CARTESIAN_POINT('Ctrl Pts',(366.926417992745,-16.4474762911354,0.458336284254925));
#43657=CARTESIAN_POINT('Ctrl Pts',(366.916356076746,-16.4533191224073,0.3436051775739));
#43658=CARTESIAN_POINT('Ctrl Pts',(366.906300554488,-16.4591582409115,0.228946975605304));
#43659=CARTESIAN_POINT('Ctrl Pts',(366.901296648633,-16.4649973594158,0.114009106601531));
#43660=CARTESIAN_POINT('Ctrl Pts',(366.901317920817,-16.47083647792,-0.0007291681869142));
#43661=CARTESIAN_POINT('',(366.901319463554,-17.7208364779321,0.00355905278372125));
#43662=CARTESIAN_POINT('Ctrl Pts',(366.901317920817,-16.4708364779651,-0.000729169072720509));
#43663=CARTESIAN_POINT('Ctrl Pts',(366.901325208459,-16.4728369003659,-0.0400373309035736));
#43664=CARTESIAN_POINT('Ctrl Pts',(366.901921774908,-16.4748373227667,-0.0793393664645878));
#43665=CARTESIAN_POINT('Ctrl Pts',(366.90310716762,-16.4768377451675,-0.118623544857057));
#43666=CARTESIAN_POINT('Ctrl Pts',(366.90658774682,-16.4827114345581,-0.233970714409067));
#43667=CARTESIAN_POINT('Ctrl Pts',(366.915155093854,-16.4885851239486,-0.34935667678678));
#43668=CARTESIAN_POINT('Ctrl Pts',(366.928819423885,-16.4944588133392,-0.464296261488943));
#43669=CARTESIAN_POINT('Ctrl Pts',(366.942466111982,-16.5003249192449,-0.579087448389017));
#43670=CARTESIAN_POINT('Ctrl Pts',(366.961196647927,-16.5061910251507,-0.693432997207112));
#43671=CARTESIAN_POINT('Ctrl Pts',(366.984969253279,-16.5120571310564,-0.806848409615581));
#43672=CARTESIAN_POINT('Ctrl Pts',(367.008717515785,-16.5179172301445,-0.920147686086775));
#43673=CARTESIAN_POINT('Ctrl Pts',(367.037497493783,-16.5237773292325,-1.03251831869163));
#43674=CARTESIAN_POINT('Ctrl Pts',(367.071215768427,-16.5296374283205,-1.14348226894757));
#43675=CARTESIAN_POINT('Ctrl Pts',(367.106150521497,-16.5357089464146,-1.25844954537938));
#43676=CARTESIAN_POINT('Ctrl Pts',(367.146386570428,-16.5417804645087,-1.37190627480334));
#43677=CARTESIAN_POINT('Ctrl Pts',(367.191762311665,-16.5478519826029,-1.48333345093234));
#43678=CARTESIAN_POINT('Ctrl Pts',(367.235507666256,-16.5537053461996,-1.59075695957264));
#43679=CARTESIAN_POINT('Ctrl Pts',(367.284029553862,-16.5595587097964,-1.69629383642354));
#43680=CARTESIAN_POINT('Ctrl Pts',(367.33713310628,-16.5654120733931,-1.79949655341228));
#43681=CARTESIAN_POINT('Ctrl Pts',(367.390228685378,-16.571264558127,-1.90268377486036));
#43682=CARTESIAN_POINT('Ctrl Pts',(367.447904372462,-16.5771170428609,-2.00353716603906));
#43683=CARTESIAN_POINT('Ctrl Pts',(367.509918612793,-16.5829695275948,-2.10163238703194));
#43684=CARTESIAN_POINT('Ctrl Pts',(367.571938538997,-16.588822548923,-2.19973660203955));
#43685=CARTESIAN_POINT('Ctrl Pts',(367.638297588432,-16.5946755702512,-2.29508179491208));
#43686=CARTESIAN_POINT('Ctrl Pts',(367.708710404532,-16.6005285915793,-2.38727188997903));
#43687=CARTESIAN_POINT('Ctrl Pts',(367.779146704667,-16.6063835650032,-2.47949273222297));
#43688=CARTESIAN_POINT('Ctrl Pts',(367.853639209241,-16.612238538427,-2.56855605608288));
#43689=CARTESIAN_POINT('Ctrl Pts',(367.931862208638,-16.6180935118508,-2.65409876063665));
#43690=CARTESIAN_POINT('Ctrl Pts',(368.010173863758,-16.623955121135,-2.73973841685849));
#43691=CARTESIAN_POINT('Ctrl Pts',(368.092224173651,-16.6298167304191,-2.82184918457442));
#43692=CARTESIAN_POINT('Ctrl Pts',(368.177650426563,-16.6356783397033,-2.90010468502771));
#43693=CARTESIAN_POINT('Ctrl Pts',(368.263134283025,-16.6415439015136,-2.9784129537397));
#43694=CARTESIAN_POINT('Ctrl Pts',(368.351998299459,-16.6474094633239,-3.05286051407843));
#43695=CARTESIAN_POINT('Ctrl Pts',(368.443847910513,-16.6532750251343,-3.12316225210861));
#43696=CARTESIAN_POINT('Ctrl Pts',(368.535831828226,-16.6591491638346,-3.19356678852246));
#43697=CARTESIAN_POINT('Ctrl Pts',(368.630809715783,-16.665023302535,-3.25981316853858));
#43698=CARTESIAN_POINT('Ctrl Pts',(368.72835933147,-16.6708974412353,-3.32166038370168));
#43699=CARTESIAN_POINT('Ctrl Pts',(368.753028036768,-16.6723829150166,-3.33730053475299));
#43700=CARTESIAN_POINT('Ctrl Pts',(368.777861090773,-16.6738683887979,-3.35265959262553));
#43701=CARTESIAN_POINT('Ctrl Pts',(368.802851446387,-16.6753538625791,-3.36773414002573));
#43702=CARTESIAN_POINT('Ctrl Pts',(368.901665433203,-16.6812275519697,-3.42734017969365));
#43703=CARTESIAN_POINT('Ctrl Pts',(369.003269603158,-16.6871012413603,-3.48269279839281));
#43704=CARTESIAN_POINT('Ctrl Pts',(369.107261801409,-16.6929749307509,-3.53352039669936));
#43705=CARTESIAN_POINT('Ctrl Pts',(369.211119735963,-16.6988410366566,-3.58428237180148));
#43706=CARTESIAN_POINT('Ctrl Pts',(369.31735919961,-16.7047071425624,-3.63053076502087));
#43707=CARTESIAN_POINT('Ctrl Pts',(369.425550416114,-16.7105732484682,-3.67203803195696));
#43708=CARTESIAN_POINT('Ctrl Pts',(369.53363084619,-16.7164333475562,-3.7135027959805));
#43709=CARTESIAN_POINT('Ctrl Pts',(369.643658670363,-16.7222934466443,-3.75023594332008));
#43710=CARTESIAN_POINT('Ctrl Pts',(369.7551815459,-16.7281535457323,-3.78205682535497));
#43711=CARTESIAN_POINT('Ctrl Pts',(369.870727912361,-16.7342250638264,-3.81502573221851));
#43712=CARTESIAN_POINT('Ctrl Pts',(369.987878837225,-16.7402965819205,-3.84272103667008));
#43713=CARTESIAN_POINT('Ctrl Pts',(370.106110588611,-16.7463681000146,-3.86499717720014));
#43714=CARTESIAN_POINT('Ctrl Pts',(370.220094178682,-16.7522214636114,-3.88647291819838));
#43715=CARTESIAN_POINT('Ctrl Pts',(370.335081821234,-16.7580748272082,-3.90291213998415));
#43716=CARTESIAN_POINT('Ctrl Pts',(370.450591815006,-16.7639281908049,-3.91423598261445));
#43717=CARTESIAN_POINT('Ctrl Pts',(370.566084465342,-16.7697806755389,-3.92555812500789));
#43718=CARTESIAN_POINT('Ctrl Pts',(370.682098899889,-16.7756331602728,-3.9317663751336));
#43719=CARTESIAN_POINT('Ctrl Pts',(370.798147593364,-16.7814856450067,-3.93283367462974));
#43720=CARTESIAN_POINT('Ctrl Pts',(370.914206926947,-16.7873386663349,-3.93390107198293));
#43721=CARTESIAN_POINT('Ctrl Pts',(371.030300112551,-16.7931916876631,-3.92982657789486));
#43722=CARTESIAN_POINT('Ctrl Pts',(371.145939630176,-16.7990447089913,-3.92063526333801));
#43723=CARTESIAN_POINT('Ctrl Pts',(371.261617715813,-16.8048996824151,-3.91144088330025));
#43724=CARTESIAN_POINT('Ctrl Pts',(371.376841420979,-16.8107546558389,-3.89712632209527));
#43725=CARTESIAN_POINT('Ctrl Pts',(371.49112905884,-16.8166096292628,-3.87776843560543));
#43726=CARTESIAN_POINT('Ctrl Pts',(371.605546227058,-16.822471238547,-3.85838860943768));
#43727=CARTESIAN_POINT('Ctrl Pts',(371.719024802884,-16.8283328478311,-3.8339541183041));
#43728=CARTESIAN_POINT('Ctrl Pts',(371.831093898196,-16.8341944571153,-3.80459281870881));
#43729=CARTESIAN_POINT('Ctrl Pts',(371.943238562521,-16.8400600189256,-3.77521172057359));
#43730=CARTESIAN_POINT('Ctrl Pts',(372.053971460174,-16.845925580736,-3.74089732076055));
#43731=CARTESIAN_POINT('Ctrl Pts',(372.162839110048,-16.8517911425463,-3.70182661265579));
#43732=CARTESIAN_POINT('Ctrl Pts',(372.271865951127,-16.8576652812467,-3.66269877359306));
#43733=CARTESIAN_POINT('Ctrl Pts',(372.379021720284,-16.863539419947,-3.61880090204385));
#43734=CARTESIAN_POINT('Ctrl Pts',(372.483874994972,-16.8694135586474,-3.57035715805946));
#43735=CARTESIAN_POINT('Ctrl Pts',(372.510390676396,-16.8708990324285,-3.55810652605699));
#43736=CARTESIAN_POINT('Ctrl Pts',(372.536759248013,-16.8723845062097,-3.54556540726016));
#43737=CARTESIAN_POINT('Ctrl Pts',(372.562974017947,-16.8738699799908,-3.53273787085405));
#43738=CARTESIAN_POINT('Ctrl Pts',(372.666629442893,-16.8797436693814,-3.48201670333702));
#43739=CARTESIAN_POINT('Ctrl Pts',(372.76822326964,-16.8856173587719,-3.42664510307133));
#43740=CARTESIAN_POINT('Ctrl Pts',(372.867309259094,-16.8914910481625,-3.36681376729656));
#43741=CARTESIAN_POINT('Ctrl Pts',(372.966267319227,-16.8973571540683,-3.30705967939723));
#43742=CARTESIAN_POINT('Ctrl Pts',(373.062723630657,-16.903223259974,-3.24285751824523));
#43743=CARTESIAN_POINT('Ctrl Pts',(373.156254000254,-16.9090893658797,-3.17444507420077));
#43744=CARTESIAN_POINT('Ctrl Pts',(373.249688595943,-16.9149494649678,-3.10610268362744));
#43745=CARTESIAN_POINT('Ctrl Pts',(373.340202877864,-16.9208095640558,-3.03355882810684));
#43746=CARTESIAN_POINT('Ctrl Pts',(373.427399826266,-16.9266696631438,-2.95709568345065));
#43747=CARTESIAN_POINT('Ctrl Pts',(373.517742641639,-16.9327411812379,-2.87787392297556));
#43748=CARTESIAN_POINT('Ctrl Pts',(373.604523853892,-16.9388126993321,-2.79444496945871));
#43749=CARTESIAN_POINT('Ctrl Pts',(373.687337226515,-16.9448842174262,-2.70717000862969));
#43750=CARTESIAN_POINT('Ctrl Pts',(373.767175048477,-16.9507375810229,-2.62303090689171));
#43751=CARTESIAN_POINT('Ctrl Pts',(373.843324950221,-16.9565909446197,-2.53531774700826));
#43752=CARTESIAN_POINT('Ctrl Pts',(373.915459530284,-16.9624443082164,-2.44439255560179));
#43753=CARTESIAN_POINT('Ctrl Pts',(373.987583279583,-16.9682967929503,-2.35348101630686));
#43754=CARTESIAN_POINT('Ctrl Pts',(374.055692649264,-16.9741492776842,-2.25935872800813));
#43755=CARTESIAN_POINT('Ctrl Pts',(374.119500609878,-16.9800017624181,-2.16242069343142));
#43756=CARTESIAN_POINT('Ctrl Pts',(374.183314420827,-16.9858547837463,-2.06547377093849));
#43757=CARTESIAN_POINT('Ctrl Pts',(374.24282581155,-16.9917078050744,-1.96571093407093));
#43758=CARTESIAN_POINT('Ctrl Pts',(374.297791560155,-16.9975608264026,-1.86355544092449));
#43759=CARTESIAN_POINT('Ctrl Pts',(374.352775640898,-17.0034157998264,-1.76136587694822));
#43760=CARTESIAN_POINT('Ctrl Pts',(374.403210869252,-17.0092707732502,-1.65678243353831));
#43761=CARTESIAN_POINT('Ctrl Pts',(374.448900700805,-17.015125746674,-1.55025154022651));
#43762=CARTESIAN_POINT('Ctrl Pts',(374.494642315913,-17.0209873559582,-1.44359990783055));
#43763=CARTESIAN_POINT('Ctrl Pts',(374.535627636522,-17.0268489652423,-1.33499680003465));
#43764=CARTESIAN_POINT('Ctrl Pts',(374.571708828526,-17.0327105745265,-1.22490722004938));
#43765=CARTESIAN_POINT('Ctrl Pts',(374.607814350344,-17.0385761363368,-1.11474340585184));
#43766=CARTESIAN_POINT('Ctrl Pts',(374.639009047908,-17.0444416981472,-1.00309152050713));
#43767=CARTESIAN_POINT('Ctrl Pts',(374.66519581373,-17.0503072599575,-0.890428577546521));
#43768=CARTESIAN_POINT('Ctrl Pts',(374.691420871026,-17.0561813986578,-0.777600893730893));
#43769=CARTESIAN_POINT('Ctrl Pts',(374.712623306707,-17.0620555373582,-0.663759606355524));
#43770=CARTESIAN_POINT('Ctrl Pts',(374.728757605958,-17.0679296760585,-0.549388762467288));
#43771=CARTESIAN_POINT('Ctrl Pts',(374.732837706844,-17.0694151498398,-0.520466243165366));
#43772=CARTESIAN_POINT('Ctrl Pts',(374.736593959772,-17.0709006236211,-0.49150986573407));
#43773=CARTESIAN_POINT('Ctrl Pts',(374.74002615638,-17.0723860974024,-0.462527459354832));
#43774=CARTESIAN_POINT('Ctrl Pts',(374.753597353027,-17.078259786793,-0.347928565046032));
#43775=CARTESIAN_POINT('Ctrl Pts',(374.762143142551,-17.0841334761836,-0.232541004059265));
#43776=CARTESIAN_POINT('Ctrl Pts',(374.765581858882,-17.0900071655741,-0.116843133392955));
#43777=CARTESIAN_POINT('Ctrl Pts',(374.769016135506,-17.0958732714799,-0.001294639547041));
#43778=CARTESIAN_POINT('Ctrl Pts',(374.767356439506,-17.1017393773857,0.114562958048043));
#43779=CARTESIAN_POINT('Ctrl Pts',(374.760572628855,-17.1076054832914,0.230244298159953));
#43780=CARTESIAN_POINT('Ctrl Pts',(374.75379576474,-17.1134655823795,0.345807182053286));
#43781=CARTESIAN_POINT('Ctrl Pts',(374.741905246791,-17.1193256814675,0.461193757478856));
#43782=CARTESIAN_POINT('Ctrl Pts',(374.724922961374,-17.1251857805555,0.575917435433359));
#43783=CARTESIAN_POINT('Ctrl Pts',(374.707327993842,-17.1312572986497,0.694780081961744));
#43784=CARTESIAN_POINT('Ctrl Pts',(374.684266910057,-17.1373288167438,0.812930644803329));
#43785=CARTESIAN_POINT('Ctrl Pts',(374.655822992546,-17.1434003348379,0.929831958010082));
#43786=CARTESIAN_POINT('Ctrl Pts',(374.628401087722,-17.1492536984346,1.04253291360825));
#43787=CARTESIAN_POINT('Ctrl Pts',(374.595976617167,-17.1551070620314,1.15407241182109));
#43788=CARTESIAN_POINT('Ctrl Pts',(374.558676307244,-17.1609604256281,1.26397907655505));
#43789=CARTESIAN_POINT('Ctrl Pts',(374.521381597838,-17.166812910362,1.37386923917312));
#43790=CARTESIAN_POINT('Ctrl Pts',(374.479212637476,-17.172665395096,1.48212666466833));
#43791=CARTESIAN_POINT('Ctrl Pts',(374.432345748655,-17.1785178798299,1.58829602520976));
#43792=CARTESIAN_POINT('Ctrl Pts',(374.385474562771,-17.184370901158,1.69447512005612));
#43793=CARTESIAN_POINT('Ctrl Pts',(374.333904759016,-17.1902239224862,1.7985653913906));
#43794=CARTESIAN_POINT('Ctrl Pts',(374.277860151588,-17.1960769438144,1.90013300570704));
#43795=CARTESIAN_POINT('Ctrl Pts',(374.221796852201,-17.2019319172382,2.00173449478428));
#43796=CARTESIAN_POINT('Ctrl Pts',(374.161255980997,-17.2077868906621,2.10081129231268));
#43797=CARTESIAN_POINT('Ctrl Pts',(374.096506127618,-17.2136418640859,2.19695622678428));
#43798=CARTESIAN_POINT('Ctrl Pts',(374.031682888597,-17.2195034733701,2.29321012918976));
#43799=CARTESIAN_POINT('Ctrl Pts',(373.962641376999,-17.2253650826542,2.38652519337903));
#43800=CARTESIAN_POINT('Ctrl Pts',(373.889692196396,-17.2312266919384,2.47652511053001));
#43801=CARTESIAN_POINT('Ctrl Pts',(373.816693825625,-17.2370922537487,2.56658571528611));
#43802=CARTESIAN_POINT('Ctrl Pts',(373.739782812457,-17.2429578155591,2.65332641340825));
#43803=CARTESIAN_POINT('Ctrl Pts',(373.659307352212,-17.2488233773694,2.73640701113821));
#43804=CARTESIAN_POINT('Ctrl Pts',(373.578714217107,-17.2546975160698,2.8196090930789));
#43805=CARTESIAN_POINT('Ctrl Pts',(373.494546532028,-17.2605716547701,2.89914011079338));
#43806=CARTESIAN_POINT('Ctrl Pts',(373.407186371495,-17.2664457934704,2.97469941131716));
#43807=CARTESIAN_POINT('Ctrl Pts',(373.385094413062,-17.2679312672517,2.99380712490413));
#43808=CARTESIAN_POINT('Ctrl Pts',(373.362798442319,-17.2694167410329,3.01266106132462));
#43809=CARTESIAN_POINT('Ctrl Pts',(373.340304925234,-17.2709022148141,3.03125680121626));
#43810=CARTESIAN_POINT('Ctrl Pts',(373.251363649844,-17.2767759042047,3.10478593481075));
#43811=CARTESIAN_POINT('Ctrl Pts',(373.159035330657,-17.2826495935952,3.17451972307088));
#43812=CARTESIAN_POINT('Ctrl Pts',(373.063677662859,-17.2885232829858,3.2401302194792));
#43813=CARTESIAN_POINT('Ctrl Pts',(372.96844311077,-17.2943893888915,3.30565600657279));
#43814=CARTESIAN_POINT('Ctrl Pts',(372.870187325365,-17.3002554947973,3.36706885657835));
#43815=CARTESIAN_POINT('Ctrl Pts',(372.76930181922,-17.306121600703,3.42408032197541));
#43816=CARTESIAN_POINT('Ctrl Pts',(372.668519618547,-17.3119816997911,3.48103340835827));
#43817=CARTESIAN_POINT('Ctrl Pts',(372.565113410884,-17.3178417988791,3.53359387279936));
#43818=CARTESIAN_POINT('Ctrl Pts',(372.459503945596,-17.3237018979671,3.5815163220571));
#43819=CARTESIAN_POINT('Ctrl Pts',(372.350084331733,-17.3297734160612,3.6311677039555));
#43820=CARTESIAN_POINT('Ctrl Pts',(372.238299853772,-17.3358449341553,3.67583983813364));
#43821=CARTESIAN_POINT('Ctrl Pts',(372.124647044722,-17.3419164522494,3.71531150478226));
#43822=CARTESIAN_POINT('Ctrl Pts',(372.015077871931,-17.3477698158462,3.75336492290316));
#43823=CARTESIAN_POINT('Ctrl Pts',(371.903772742432,-17.3536231794429,3.78658500868818));
#43824=CARTESIAN_POINT('Ctrl Pts',(371.791196456824,-17.3594765430397,3.81482271383259));
#43825=CARTESIAN_POINT('Ctrl Pts',(371.678637074166,-17.3653290277736,3.84305617918061));
#43826=CARTESIAN_POINT('Ctrl Pts',(371.564807315523,-17.3711815125075,3.86630865087828));
#43827=CARTESIAN_POINT('Ctrl Pts',(371.450185382546,-17.3770339972413,3.88448145655589));
#43828=CARTESIAN_POINT('Ctrl Pts',(371.335552940278,-17.3828870185695,3.90265592843578));
#43829=CARTESIAN_POINT('Ctrl Pts',(371.220128587361,-17.3887400398977,3.91574974375585));
#43830=CARTESIAN_POINT('Ctrl Pts',(371.104398209302,-17.3945930612258,3.92371579007204));
#43831=CARTESIAN_POINT('Ctrl Pts',(370.988629232927,-17.4004480346497,3.93168449321852));
#43832=CARTESIAN_POINT('Ctrl Pts',(370.872554440404,-17.4063030080735,3.93452199832939));
#43833=CARTESIAN_POINT('Ctrl Pts',(370.756661586145,-17.4121579814973,3.93223327184228));
#43834=CARTESIAN_POINT('Ctrl Pts',(370.640637382223,-17.4180195907814,3.92994195137766));
#43835=CARTESIAN_POINT('Ctrl Pts',(370.52479594143,-17.4238812000656,3.92251281121648));
#43836=CARTESIAN_POINT('Ctrl Pts',(370.409621860176,-17.4297428093497,3.91000285338626));
#43837=CARTESIAN_POINT('Ctrl Pts',(370.294370116192,-17.43560837116,3.8974844599996));
#43838=CARTESIAN_POINT('Ctrl Pts',(370.179787035149,-17.4414739329704,3.87987848954197));
#43839=CARTESIAN_POINT('Ctrl Pts',(370.066347244525,-17.4473394947807,3.85729311100074));
#43840=CARTESIAN_POINT('Ctrl Pts',(369.952741577103,-17.453213633481,3.83467470709667));
#43841=CARTESIAN_POINT('Ctrl Pts',(369.840282936222,-17.4590877721813,3.80706246196776));
#43842=CARTESIAN_POINT('Ctrl Pts',(369.729431089154,-17.4649619108817,3.77461444899779));
#43843=CARTESIAN_POINT('Ctrl Pts',(369.701398466699,-17.466447384663,3.76640887623504));
#43844=CARTESIAN_POINT('Ctrl Pts',(369.673468498175,-17.4679328584444,3.75789429531162));
#43845=CARTESIAN_POINT('Ctrl Pts',(369.645648402469,-17.4694183322257,3.74907374385222));
#43846=CARTESIAN_POINT('Ctrl Pts',(369.535645383201,-17.4752920216163,3.71419653485915));
#43847=CARTESIAN_POINT('Ctrl Pts',(369.426995473744,-17.4811657110069,3.67441567358145));
#43848=CARTESIAN_POINT('Ctrl Pts',(369.320168160092,-17.4870394003974,3.62985395116513));
#43849=CARTESIAN_POINT('Ctrl Pts',(369.213478770539,-17.4929055063032,3.58534976211886));
#43850=CARTESIAN_POINT('Ctrl Pts',(369.10860767498,-17.4987716122089,3.53607714469621));
#43851=CARTESIAN_POINT('Ctrl Pts',(369.006009500822,-17.5046377181147,3.48220871984097));
#43852=CARTESIAN_POINT('Ctrl Pts',(368.903516385887,-17.5104978172028,3.42839545556647));
#43853=CARTESIAN_POINT('Ctrl Pts',(368.803291926492,-17.5163579162908,3.36999593549393));
#43854=CARTESIAN_POINT('Ctrl Pts',(368.705770420738,-17.5222180153788,3.30723068860623));
#43855=CARTESIAN_POINT('Ctrl Pts',(368.604730561539,-17.528289533473,3.24220101480139));
#43856=CARTESIAN_POINT('Ctrl Pts',(368.506592787952,-17.5343610515671,3.17248482958971));
#43857=CARTESIAN_POINT('Ctrl Pts',(368.411812167986,-17.5404325696612,3.09837944819399));
#43858=CARTESIAN_POINT('Ctrl Pts',(368.320437091443,-17.5462859332579,3.02693673237529));
#43859=CARTESIAN_POINT('Ctrl Pts',(368.232182423347,-17.5521392968547,2.95141508308358));
#43860=CARTESIAN_POINT('Ctrl Pts',(368.147425382985,-17.5579926604514,2.87212427540527));
#43861=CARTESIAN_POINT('Ctrl Pts',(368.062681068607,-17.5638451451853,2.792845372975));
#43862=CARTESIAN_POINT('Ctrl Pts',(367.981433639376,-17.5696976299192,2.70979871960333));
#43863=CARTESIAN_POINT('Ctrl Pts',(367.904025248123,-17.5755501146531,2.62333266066097));
#43864=CARTESIAN_POINT('Ctrl Pts',(367.82660975956,-17.5814031359813,2.53685867394199));
#43865=CARTESIAN_POINT('Ctrl Pts',(367.753034284279,-17.5872561573095,2.44696496624837));
#43866=CARTESIAN_POINT('Ctrl Pts',(367.683601814389,-17.5931091786377,2.35403429087829));
#43867=CARTESIAN_POINT('Ctrl Pts',(367.614146187431,-17.5989641520615,2.26107262133322));
#43868=CARTESIAN_POINT('Ctrl Pts',(367.548836560604,-17.6048191254853,2.16507230082104));
#43869=CARTESIAN_POINT('Ctrl Pts',(367.48793317688,-17.6106740989091,2.06644588555582));
#43870=CARTESIAN_POINT('Ctrl Pts',(367.426960766993,-17.6165357081933,1.96770768991693));
#43871=CARTESIAN_POINT('Ctrl Pts',(367.370404784946,-17.6223973174774,1.86633781064752));
#43872=CARTESIAN_POINT('Ctrl Pts',(367.318480035809,-17.6282589267616,1.76277435925219));
#43873=CARTESIAN_POINT('Ctrl Pts',(367.266520273433,-17.634124488572,1.65914107426099));
#43874=CARTESIAN_POINT('Ctrl Pts',(367.219198130532,-17.6399900503823,1.55331164806737));
#43875=CARTESIAN_POINT('Ctrl Pts',(367.176680011928,-17.6458556121927,1.44574355330331));
#43876=CARTESIAN_POINT('Ctrl Pts',(367.134099721406,-17.651729750893,1.338018167602));
#43877=CARTESIAN_POINT('Ctrl Pts',(367.09633760885,-17.6576038895933,1.228549428478));
#43878=CARTESIAN_POINT('Ctrl Pts',(367.063510088167,-17.6634780282936,1.11780937506533));
#43879=CARTESIAN_POINT('Ctrl Pts',(367.055208544099,-17.6649635020749,1.08980502340273));
#43880=CARTESIAN_POINT('Ctrl Pts',(367.047222311687,-17.6664489758562,1.06171941638091));
#43881=CARTESIAN_POINT('Ctrl Pts',(367.039552751816,-17.6679344496374,1.0335602668127));
#43882=CARTESIAN_POINT('Ctrl Pts',(367.000890946421,-17.6754226366022,0.891611631032549));
#43883=CARTESIAN_POINT('Ctrl Pts',(366.970176145368,-17.682910823567,0.747412562252043));
#43884=CARTESIAN_POINT('Ctrl Pts',(366.947623622355,-17.6903990105317,0.60174492580523));
#43885=CARTESIAN_POINT('Ctrl Pts',(366.925476457884,-17.6977526049923,0.458695516182048));
#43886=CARTESIAN_POINT('Ctrl Pts',(366.911200774692,-17.7051061994529,0.314229690773424));
#43887=CARTESIAN_POINT('Ctrl Pts',(366.904955180256,-17.7124597939135,0.169109385555225));
#43888=CARTESIAN_POINT('Ctrl Pts',(366.902583670133,-17.7152520219197,0.114005859970163));
#43889=CARTESIAN_POINT('Ctrl Pts',(366.901369459675,-17.7180442499259,0.0588082087437617));
#43890=CARTESIAN_POINT('Ctrl Pts',(366.901319463554,-17.7208364779321,0.00355905278374745));
#43891=CARTESIAN_POINT('',(366.901318079705,-18.970836477995,-0.00133472881288598));
#43892=CARTESIAN_POINT('Ctrl Pts',(366.901319463554,-17.7208364779651,0.00355905213086757));
#43893=CARTESIAN_POINT('Ctrl Pts',(366.901210826618,-17.7269037316769,-0.116492263818606));
#43894=CARTESIAN_POINT('Ctrl Pts',(366.906603967799,-17.7329709853888,-0.236671020316424));
#43895=CARTESIAN_POINT('Ctrl Pts',(366.91750180444,-17.7390382391006,-0.356428169460981));
#43896=CARTESIAN_POINT('Ctrl Pts',(366.927912467658,-17.7448342642326,-0.470831733108454));
#43897=CARTESIAN_POINT('Ctrl Pts',(366.943346248658,-17.7506302893647,-0.584850100472219));
#43898=CARTESIAN_POINT('Ctrl Pts',(366.963752437188,-17.7564263144968,-0.698005988649075));
#43899=CARTESIAN_POINT('Ctrl Pts',(366.984153960437,-17.7622210145362,-0.811136007022495));
#43900=CARTESIAN_POINT('Ctrl Pts',(367.009525557066,-17.7680157145757,-0.923403522833011));
#43901=CARTESIAN_POINT('Ctrl Pts',(367.039765022357,-17.7738104146152,-1.03433931268109));
#43902=CARTESIAN_POINT('Ctrl Pts',(367.070005243591,-17.7796052595138,-1.14527787576476));
#43903=CARTESIAN_POINT('Ctrl Pts',(367.105113463762,-17.7854001044125,-1.25488423951657));
#43904=CARTESIAN_POINT('Ctrl Pts',(367.144937235379,-17.7911949493111,-1.36270306988447));
#43905=CARTESIAN_POINT('Ctrl Pts',(367.18477210334,-17.7969914088631,-1.4705519424782));
#43906=CARTESIAN_POINT('Ctrl Pts',(367.229324987372,-17.8027878684152,-1.57661189611944));
#43907=CARTESIAN_POINT('Ctrl Pts',(367.278395124978,-17.8085843279672,-1.6804471282203));
#43908=CARTESIAN_POINT('Ctrl Pts',(367.327519250044,-17.8143871648424,-1.78439660088862));
#43909=CARTESIAN_POINT('Ctrl Pts',(367.38117036646,-17.8201900017176,-1.88611608537424));
#43910=CARTESIAN_POINT('Ctrl Pts',(367.439101540829,-17.8259928385927,-1.98519399355422));
#43911=CARTESIAN_POINT('Ctrl Pts',(367.497070148194,-17.8317994250479,-2.08433592223832));
#43912=CARTESIAN_POINT('Ctrl Pts',(367.559324089116,-17.8376060115031,-2.18083252392297));
#43913=CARTESIAN_POINT('Ctrl Pts',(367.625573909863,-17.8434125979582,-2.27430237786089));
#43914=CARTESIAN_POINT('Ctrl Pts',(367.691922206198,-17.8492278154861,-2.36791116800698));
#43915=CARTESIAN_POINT('Ctrl Pts',(367.762277976017,-17.855043033014,-2.45848390128039));
#43916=CARTESIAN_POINT('Ctrl Pts',(367.836312460296,-17.8608582505418,-2.54567332232082));
#43917=CARTESIAN_POINT('Ctrl Pts',(367.860044691954,-17.8627223560442,-2.5736224538425));
#43918=CARTESIAN_POINT('Ctrl Pts',(367.884154662209,-17.8645864615467,-2.6012242220321));
#43919=CARTESIAN_POINT('Ctrl Pts',(367.908630796946,-17.8664505670491,-2.62846804217356));
#43920=CARTESIAN_POINT('Ctrl Pts',(367.985753691945,-17.8723242564397,-2.71431175494456));
#43921=CARTESIAN_POINT('Ctrl Pts',(368.066786396822,-17.8781979458302,-2.79690122454739));
#43922=CARTESIAN_POINT('Ctrl Pts',(368.151423500947,-17.8840716352208,-2.87585933149078));
#43923=CARTESIAN_POINT('Ctrl Pts',(368.23595133062,-17.8899377411266,-2.95471549610037));
#43924=CARTESIAN_POINT('Ctrl Pts',(368.324074005681,-17.8958038470324,-3.02994934254857));
#43925=CARTESIAN_POINT('Ctrl Pts',(368.415446841904,-17.9016699529381,-3.10121783023935));
#43926=CARTESIAN_POINT('Ctrl Pts',(368.506726113506,-17.9075300520262,-3.17241333990654));
#43927=CARTESIAN_POINT('Ctrl Pts',(368.601248602522,-17.9133901511142,-3.23965131485939));
#43928=CARTESIAN_POINT('Ctrl Pts',(368.698634357218,-17.9192502502022,-3.30262698542935));
#43929=CARTESIAN_POINT('Ctrl Pts',(368.79953356777,-17.9253217682963,-3.36787467452288));
#43930=CARTESIAN_POINT('Ctrl Pts',(368.903506214627,-17.9313932863905,-3.42854639603025));
#43931=CARTESIAN_POINT('Ctrl Pts',(369.010093825745,-17.9374648044846,-3.48435011122124));
#43932=CARTESIAN_POINT('Ctrl Pts',(369.112851658812,-17.9433181680813,-3.53814875432834));
#43933=CARTESIAN_POINT('Ctrl Pts',(369.218039377229,-17.9491715316781,-3.58742298539051));
#43934=CARTESIAN_POINT('Ctrl Pts',(369.32521924898,-17.9550248952748,-3.63195682830467));
#43935=CARTESIAN_POINT('Ctrl Pts',(369.432383028034,-17.9608773800087,-3.67648398461213));
#43936=CARTESIAN_POINT('Ctrl Pts',(369.54153798425,-17.9667298647427,-3.71627200952271));
#43937=CARTESIAN_POINT('Ctrl Pts',(369.652225700691,-17.9725823494766,-3.75115277520406));
#43938=CARTESIAN_POINT('Ctrl Pts',(369.76292356571,-17.9784353708047,-3.78603673898321));
#43939=CARTESIAN_POINT('Ctrl Pts',(369.875154076256,-17.9842883921329,-3.81601242493424));
#43940=CARTESIAN_POINT('Ctrl Pts',(369.988443610498,-17.9901414134611,-3.84096156782295));
#43941=CARTESIAN_POINT('Ctrl Pts',(370.101770928988,-17.9959963868849,-3.8659190317327));
#43942=CARTESIAN_POINT('Ctrl Pts',(370.216157570246,-18.0018513603087,-3.88584653022815));
#43943=CARTESIAN_POINT('Ctrl Pts',(370.33112038234,-18.0077063337326,-3.90067703165696));
#43944=CARTESIAN_POINT('Ctrl Pts',(370.446213490015,-18.0135679430167,-3.91552434155424));
#43945=CARTESIAN_POINT('Ctrl Pts',(370.561883661927,-18.0194295523009,-3.9252630713686));
#43946=CARTESIAN_POINT('Ctrl Pts',(370.677643194357,-18.0252911615851,-3.92987812168124));
#43947=CARTESIAN_POINT('Ctrl Pts',(370.79348078429,-18.0311567233954,-3.93449628395621));
#43948=CARTESIAN_POINT('Ctrl Pts',(370.909407442608,-18.0370222852058,-3.93398388900959));
#43949=CARTESIAN_POINT('Ctrl Pts',(371.024937778355,-18.0428878470161,-3.9283779151379));
#43950=CARTESIAN_POINT('Ctrl Pts',(371.140637047788,-18.0487619857165,-3.92276374395747));
#43951=CARTESIAN_POINT('Ctrl Pts',(371.255938428284,-18.0546361244168,-3.91204116750197));
#43952=CARTESIAN_POINT('Ctrl Pts',(371.370363865654,-18.0605102631172,-3.89629871449274));
#43953=CARTESIAN_POINT('Ctrl Pts',(371.399300190754,-18.0619957368983,-3.89231770512442));
#43954=CARTESIAN_POINT('Ctrl Pts',(371.428180563444,-18.0634812106795,-3.88801592605576));
#43955=CARTESIAN_POINT('Ctrl Pts',(371.456997395747,-18.0649666844607,-3.88339531690034));
#43956=CARTESIAN_POINT('Ctrl Pts',(371.570941596116,-18.0708403738513,-3.86512503618736));
#43957=CARTESIAN_POINT('Ctrl Pts',(371.684270775537,-18.0767140632418,-3.84180515537925));
#43958=CARTESIAN_POINT('Ctrl Pts',(371.796502471532,-18.0825877526324,-3.81348787336368));
#43959=CARTESIAN_POINT('Ctrl Pts',(371.908589265863,-18.0884538585381,-3.7852071516195));
#43960=CARTESIAN_POINT('Ctrl Pts',(372.019580997695,-18.0943199644439,-3.75194195995824));
#43961=CARTESIAN_POINT('Ctrl Pts',(372.129002550724,-18.1001860703496,-3.71379597367167));
#43962=CARTESIAN_POINT('Ctrl Pts',(372.238312057476,-18.1060461694377,-3.67568904838903));
#43963=CARTESIAN_POINT('Ctrl Pts',(372.346054195759,-18.1119062685257,-3.63271140485454));
#43964=CARTESIAN_POINT('Ctrl Pts',(372.451766889779,-18.1177663676138,-3.58501710095596));
#43965=CARTESIAN_POINT('Ctrl Pts',(372.56129345663,-18.1238378857079,-3.53560209538083));
#43966=CARTESIAN_POINT('Ctrl Pts',(372.668640941062,-18.129909403802,-3.4811237816107));
#43967=CARTESIAN_POINT('Ctrl Pts',(372.773315398583,-18.1359809218961,-3.42180910032845));
#43968=CARTESIAN_POINT('Ctrl Pts',(372.874228819192,-18.1418342854928,-3.36462564294782));
#43969=CARTESIAN_POINT('Ctrl Pts',(372.972657604813,-18.1476876490896,-3.30294760703959));
#43970=CARTESIAN_POINT('Ctrl Pts',(373.068182970345,-18.1535410126863,-3.23702573955043));
#43971=CARTESIAN_POINT('Ctrl Pts',(373.163693993064,-18.1593934974202,-3.17111377000791));
#43972=CARTESIAN_POINT('Ctrl Pts',(373.25630212256,-18.1652459821541,-3.10095947046653));
#43973=CARTESIAN_POINT('Ctrl Pts',(373.345617567513,-18.171098466888,-3.02685690857922));
#43974=CARTESIAN_POINT('Ctrl Pts',(373.434941201493,-18.1769514882162,-2.95274755248196));
#43975=CARTESIAN_POINT('Ctrl Pts',(373.520971232815,-18.1828045095444,-2.87468947822724));
#43976=CARTESIAN_POINT('Ctrl Pts',(373.603351527376,-18.1886575308725,-2.79301656124916));
#43977=CARTESIAN_POINT('Ctrl Pts',(373.685759297356,-18.1945125042964,-2.71131640477564));
#43978=CARTESIAN_POINT('Ctrl Pts',(373.764514616876,-18.2003674777202,-2.62599929897565));
#43979=CARTESIAN_POINT('Ctrl Pts',(373.839299237453,-18.206222451144,-2.53743490171398));
#43980=CARTESIAN_POINT('Ctrl Pts',(373.914168616792,-18.2120840604282,-2.44877012808402));
#43981=CARTESIAN_POINT('Ctrl Pts',(373.98505804821,-18.2179456697123,-2.35685103299713));
#43982=CARTESIAN_POINT('Ctrl Pts',(374.051690454723,-18.2238072789965,-2.26207925217577));
#43983=CARTESIAN_POINT('Ctrl Pts',(374.118367791957,-18.2296728408068,-2.16724356604643));
#43984=CARTESIAN_POINT('Ctrl Pts',(374.180782166516,-18.2355384026172,-2.06955171118823));
#43985=CARTESIAN_POINT('Ctrl Pts',(374.238701516499,-18.2414039644275,-1.96943161171589));
#43986=CARTESIAN_POINT('Ctrl Pts',(374.296705558777,-18.2472781031279,-1.86916511210221));
#43987=CARTESIAN_POINT('Ctrl Pts',(374.350201268639,-18.2531522418282,-1.76646364659903));
#43988=CARTESIAN_POINT('Ctrl Pts',(374.39900387974,-18.2590263805285,-1.66177692015447));
#43989=CARTESIAN_POINT('Ctrl Pts',(374.41134526338,-18.2605118543098,-1.63530335605997));
#43990=CARTESIAN_POINT('Ctrl Pts',(374.423386769389,-18.2619973280911,-1.60870291690914));
#43991=CARTESIAN_POINT('Ctrl Pts',(374.435125914126,-18.2634828018724,-1.58198303042164));
#43992=CARTESIAN_POINT('Ctrl Pts',(374.481543488617,-18.269356491263,-1.47633033176422));
#43993=CARTESIAN_POINT('Ctrl Pts',(374.523384435817,-18.2752301806536,-1.36845700379822));
#43994=CARTESIAN_POINT('Ctrl Pts',(374.560431071363,-18.2811038700441,-1.25879676104185));
#43995=CARTESIAN_POINT('Ctrl Pts',(374.597429876223,-18.2869699759499,-1.1492780999608));
#43996=CARTESIAN_POINT('Ctrl Pts',(374.6296465481,-18.2928360818556,-1.03797749994231));
#43997=CARTESIAN_POINT('Ctrl Pts',(374.65691064109,-18.2987021877614,-0.925350408305881));
#43998=CARTESIAN_POINT('Ctrl Pts',(374.684146815997,-18.3045622868495,-0.812838645376354));
#43999=CARTESIAN_POINT('Ctrl Pts',(374.70644040278,-18.3104223859375,-0.699003491781595));
#44000=CARTESIAN_POINT('Ctrl Pts',(374.723670361809,-18.3162824850256,-0.584316749682578));
#44001=CARTESIAN_POINT('Ctrl Pts',(374.741521938453,-18.3223540031197,-0.465492371571384));
#44002=CARTESIAN_POINT('Ctrl Pts',(374.753937476183,-18.3284255212138,-0.345754225987014));
#44003=CARTESIAN_POINT('Ctrl Pts',(374.760839903029,-18.3344970393079,-0.225640405064929));
#44004=CARTESIAN_POINT('Ctrl Pts',(374.767494320161,-18.3403504029046,-0.109842369720977));
#44005=CARTESIAN_POINT('Ctrl Pts',(374.76902496343,-18.3462037665014,0.0063043611136395));
#44006=CARTESIAN_POINT('Ctrl Pts',(374.765415510074,-18.3520571300981,0.122311946726538));
#44007=CARTESIAN_POINT('Ctrl Pts',(374.761806598665,-18.357909614832,0.238302114190843));
#44008=CARTESIAN_POINT('Ctrl Pts',(374.753059138041,-18.3637620995659,0.354152765140715));
#44009=CARTESIAN_POINT('Ctrl Pts',(374.739208925978,-18.3696145842998,0.46937693800074));
#44010=CARTESIAN_POINT('Ctrl Pts',(374.725357444036,-18.375467605628,0.584611675370635));
#44011=CARTESIAN_POINT('Ctrl Pts',(374.706402329915,-18.3813206269562,0.699219410251301));
#44012=CARTESIAN_POINT('Ctrl Pts',(374.682431078075,-18.3871736482844,0.812719883311904));
#44013=CARTESIAN_POINT('Ctrl Pts',(374.658451831359,-18.3930286217083,0.926258210972364));
#44014=CARTESIAN_POINT('Ctrl Pts',(374.629453205608,-18.3988835951321,1.03868813847992));
#44015=CARTESIAN_POINT('Ctrl Pts',(374.595573301698,-18.404738568556,1.1495418440936));
#44016=CARTESIAN_POINT('Ctrl Pts',(374.561654999269,-18.4106001778401,1.26052118814344));
#44017=CARTESIAN_POINT('Ctrl Pts',(374.522844497361,-18.4164617871243,1.36992034933774));
#44018=CARTESIAN_POINT('Ctrl Pts',(374.479329087555,-18.4223233964084,1.4772887671675));
#44019=CARTESIAN_POINT('Ctrl Pts',(374.435784334989,-18.4281889582188,1.58472958430979));
#44020=CARTESIAN_POINT('Ctrl Pts',(374.387528528816,-18.4340545200291,1.69013655669644));
#44021=CARTESIAN_POINT('Ctrl Pts',(374.334795454063,-18.4399200818394,1.79308269915879));
#44022=CARTESIAN_POINT('Ctrl Pts',(374.281985270622,-18.4457942205398,1.8961793741305));
#44023=CARTESIAN_POINT('Ctrl Pts',(374.224684956354,-18.4516683592401,1.99680768016255));
#44024=CARTESIAN_POINT('Ctrl Pts',(374.163172238265,-18.4575424979404,2.0945685673172));
#44025=CARTESIAN_POINT('Ctrl Pts',(374.147616676064,-18.4590279717216,2.119290699719));
#44026=CARTESIAN_POINT('Ctrl Pts',(374.131791933241,-18.4605134455028,2.14382962276991));
#44027=CARTESIAN_POINT('Ctrl Pts',(374.115702904964,-18.461998919284,2.1681792228086));
#44028=CARTESIAN_POINT('Ctrl Pts',(374.052085521813,-18.4678726086746,2.26445960770738));
#44029=CARTESIAN_POINT('Ctrl Pts',(373.984121093246,-18.4737462980651,2.35809804104824));
#44030=CARTESIAN_POINT('Ctrl Pts',(373.912056064212,-18.4796199874557,2.44867648018807));
#44031=CARTESIAN_POINT('Ctrl Pts',(373.8400840779,-18.4854860933614,2.53913797405344));
#44032=CARTESIAN_POINT('Ctrl Pts',(373.764022274544,-18.4913521992672,2.62654701009376));
#44033=CARTESIAN_POINT('Ctrl Pts',(373.684160969754,-18.4972183051729,2.71051345895347));
#44034=CARTESIAN_POINT('Ctrl Pts',(373.604381441921,-18.503078404261,2.79439392723967));
#44035=CARTESIAN_POINT('Ctrl Pts',(373.520810434497,-18.5089385033491,2.87483852260677));
#44036=CARTESIAN_POINT('Ctrl Pts',(373.433778789806,-18.5147986024371,2.95148976606502));
#44037=CARTESIAN_POINT('Ctrl Pts',(373.343607241924,-18.5208701205312,3.03090641151743));
#44038=CARTESIAN_POINT('Ctrl Pts',(373.249720919668,-18.5269416386254,3.10625047285099));
#44039=CARTESIAN_POINT('Ctrl Pts',(373.152530204631,-18.5330131567195,3.17716548101968));
#44040=CARTESIAN_POINT('Ctrl Pts',(373.058831629659,-18.5388665203162,3.24553245627108));
#44041=CARTESIAN_POINT('Ctrl Pts',(372.962062396585,-18.544719883913,3.30978291527873));
#44042=CARTESIAN_POINT('Ctrl Pts',(372.862623593065,-18.5505732475097,3.36963867880925));
#44043=CARTESIAN_POINT('Ctrl Pts',(372.763199719947,-18.5564257322436,3.42948545519824));
#44044=CARTESIAN_POINT('Ctrl Pts',(372.661107427249,-18.5622782169775,3.48493863512953));
#44045=CARTESIAN_POINT('Ctrl Pts',(372.556775318918,-18.5681307017114,3.535764313253));
#44046=CARTESIAN_POINT('Ctrl Pts',(372.452433644734,-18.5739837230396,3.58659465140874));
#44047=CARTESIAN_POINT('Ctrl Pts',(372.345852118116,-18.5798367443678,3.63279646338135));
#44048=CARTESIAN_POINT('Ctrl Pts',(372.237481736329,-18.585689765696,3.67418291830293));
#44049=CARTESIAN_POINT('Ctrl Pts',(372.129075210927,-18.5915447391198,3.71558317640636));
#44050=CARTESIAN_POINT('Ctrl Pts',(372.018879029757,-18.5973997125436,3.75216473665363));
#44051=CARTESIAN_POINT('Ctrl Pts',(371.907361172898,-18.6032546859674,3.78379003567901));
#44052=CARTESIAN_POINT('Ctrl Pts',(371.795716924871,-18.6091162952515,3.81545117791885));
#44053=CARTESIAN_POINT('Ctrl Pts',(371.68274840903,-18.6149779045357,3.84214473439152));
#44054=CARTESIAN_POINT('Ctrl Pts',(371.568935767455,-18.6208395138198,3.86378383454503));
#44055=CARTESIAN_POINT('Ctrl Pts',(371.455046381179,-18.6267050756302,3.88543752610263));
#44056=CARTESIAN_POINT('Ctrl Pts',(371.340312143645,-18.6325706374405,3.9020299157595));
#44057=CARTESIAN_POINT('Ctrl Pts',(371.225218590926,-18.6384361992508,3.91352598218839));
#44058=CARTESIAN_POINT('Ctrl Pts',(371.109956743205,-18.6443103379512,3.92503885868602));
#44059=CARTESIAN_POINT('Ctrl Pts',(370.994334942647,-18.6501844766515,3.93144051673639));
#44060=CARTESIAN_POINT('Ctrl Pts',(370.878839072497,-18.6560586153518,3.93274800375443));
#44061=CARTESIAN_POINT('Ctrl Pts',(370.84963205242,-18.6575440891331,3.93307864587641));
#44062=CARTESIAN_POINT('Ctrl Pts',(370.820433059223,-18.6590295629144,3.93308377387879));
#44063=CARTESIAN_POINT('Ctrl Pts',(370.791249883981,-18.6605150366957,3.93276418693331));
#44064=CARTESIAN_POINT('Ctrl Pts',(370.675857132547,-18.6663887260863,3.93150051303031));
#44065=CARTESIAN_POINT('Ctrl Pts',(370.560327859073,-18.6722624154769,3.92515175568437));
#44066=CARTESIAN_POINT('Ctrl Pts',(370.445146948226,-18.6781361048674,3.91369837962803));
#44067=CARTESIAN_POINT('Ctrl Pts',(370.330114746755,-18.6840022107732,3.90225979095617));
#44068=CARTESIAN_POINT('Ctrl Pts',(370.21543042083,-18.689868316679,3.88572973050901));
#44069=CARTESIAN_POINT('Ctrl Pts',(370.101579182062,-18.6957344225847,3.86414065993771));
#44070=CARTESIAN_POINT('Ctrl Pts',(369.987844525513,-18.7015945216727,3.84257369629974));
#44071=CARTESIAN_POINT('Ctrl Pts',(369.874941662792,-18.7074546207608,3.81595810322047));
#44072=CARTESIAN_POINT('Ctrl Pts',(369.763350339071,-18.7133147198488,3.78437809734019));
#44073=CARTESIAN_POINT('Ctrl Pts',(369.64773305497,-18.7193862379429,3.75165875689323));
#44074=CARTESIAN_POINT('Ctrl Pts',(369.533524180742,-18.725457756037,3.71361007580265));
#44075=CARTESIAN_POINT('Ctrl Pts',(369.42124573189,-18.7315292741311,3.67038365568348));
#44076=CARTESIAN_POINT('Ctrl Pts',(369.313001537436,-18.7373826377279,3.62871039538488));
#44077=CARTESIAN_POINT('Ctrl Pts',(369.206551850923,-18.7432360013246,3.58222523437972));
#44078=CARTESIAN_POINT('Ctrl Pts',(369.102347861977,-18.7490893649214,3.53111440616399));
#44079=CARTESIAN_POINT('Ctrl Pts',(368.998159518908,-18.7549418496553,3.48001125206714));
#44080=CARTESIAN_POINT('Ctrl Pts',(368.896216573787,-18.7607943343892,3.42428399363021));
#44081=CARTESIAN_POINT('Ctrl Pts',(368.796947929391,-18.7666468191231,3.36416598779867));
#44082=CARTESIAN_POINT('Ctrl Pts',(368.697670183393,-18.7724998404512,3.30404246995336));
#44083=CARTESIAN_POINT('Ctrl Pts',(368.601067578961,-18.7783528617794,3.23952761846563));
#44084=CARTESIAN_POINT('Ctrl Pts',(368.507541601444,-18.7842058831075,3.17089912708547));
#44085=CARTESIAN_POINT('Ctrl Pts',(368.413984431207,-18.7900608565313,3.10224774677808));
#44086=CARTESIAN_POINT('Ctrl Pts',(368.323506261179,-18.7959158299551,3.02948024274656));
#44087=CARTESIAN_POINT('Ctrl Pts',(368.236476383387,-18.8017708033789,2.95291528791404));
#44088=CARTESIAN_POINT('Ctrl Pts',(368.149347868407,-18.8076324126631,2.87626355653949));
#44089=CARTESIAN_POINT('Ctrl Pts',(368.065675756552,-18.8134940219472,2.79580605703821));
#44090=CARTESIAN_POINT('Ctrl Pts',(367.985793335415,-18.8193556312314,2.71189916321431));
#44091=CARTESIAN_POINT('Ctrl Pts',(367.905857048975,-18.8252211930417,2.62793569035545));
#44092=CARTESIAN_POINT('Ctrl Pts',(367.829715812337,-18.8310867548521,2.54051850245526));
#44093=CARTESIAN_POINT('Ctrl Pts',(367.75766226792,-18.8369523166624,2.45003661389321));
#44094=CARTESIAN_POINT('Ctrl Pts',(367.685503363549,-18.8428264553628,2.35942241861817));
#44095=CARTESIAN_POINT('Ctrl Pts',(367.617444322292,-18.8487005940631,2.26573491201658));
#44096=CARTESIAN_POINT('Ctrl Pts',(367.553734221,-18.8545747327634,2.16939162715773));
#44097=CARTESIAN_POINT('Ctrl Pts',(367.537622976458,-18.8560602065447,2.14502798323234));
#44098=CARTESIAN_POINT('Ctrl Pts',(367.521789615433,-18.857545680326,2.12049462005745));
#44099=CARTESIAN_POINT('Ctrl Pts',(367.506237689991,-18.8590311541073,2.0957985177716));
#44100=CARTESIAN_POINT('Ctrl Pts',(367.443144816677,-18.8650575981924,1.99560847644104));
#44101=CARTESIAN_POINT('Ctrl Pts',(367.384486334511,-18.8710840422775,1.89241860176349));
#44102=CARTESIAN_POINT('Ctrl Pts',(367.330551037451,-18.8771104863626,1.7866468875205));
#44103=CARTESIAN_POINT('Ctrl Pts',(367.276696694135,-18.8831278851054,1.68103393047141));
#44104=CARTESIAN_POINT('Ctrl Pts',(367.227551599139,-18.8891452838483,1.57284718607505));
#44105=CARTESIAN_POINT('Ctrl Pts',(367.183360883035,-18.8951626825911,1.4625328036765));
#44106=CARTESIAN_POINT('Ctrl Pts',(367.137049631408,-18.9014688322056,1.34692487577215));
#44107=CARTESIAN_POINT('Ctrl Pts',(367.096180300861,-18.9077749818201,1.22898037755567));
#44108=CARTESIAN_POINT('Ctrl Pts',(367.060981137706,-18.9140811314346,1.10924254846433));
#44109=CARTESIAN_POINT('Ctrl Pts',(367.02748605307,-18.9200819847541,0.995301523735869));
#44110=CARTESIAN_POINT('Ctrl Pts',(366.99912516879,-18.9260828380735,0.879737151549372));
#44111=CARTESIAN_POINT('Ctrl Pts',(366.976045925749,-18.932083691393,0.763037832388592));
#44112=CARTESIAN_POINT('Ctrl Pts',(366.952985535877,-18.938079642684,0.646433843567439));
#44113=CARTESIAN_POINT('Ctrl Pts',(366.935198273749,-18.944075593975,0.528697128891053));
#44114=CARTESIAN_POINT('Ctrl Pts',(366.922781205807,-18.9500715452659,0.41032920431667));
#44115=CARTESIAN_POINT('Ctrl Pts',(366.91037342804,-18.9560630105191,0.292049839999562));
#44116=CARTESIAN_POINT('Ctrl Pts',(366.903327879835,-18.9620544757722,0.17314058812312));
#44117=CARTESIAN_POINT('Ctrl Pts',(366.901690099519,-18.9680459410253,0.0541105422818254));
#44118=CARTESIAN_POINT('Ctrl Pts',(366.901435833031,-18.9689761200053,0.0356310482111091));
#44119=CARTESIAN_POINT('Ctrl Pts',(366.901311807065,-18.9699062989852,0.0171486531679969));
#44120=CARTESIAN_POINT('Ctrl Pts',(366.901318079705,-18.9708364779651,-0.00133472821883135));
#44121=CARTESIAN_POINT('',(366.901318910622,-20.2208364779229,-0.00288400549572383));
#44122=CARTESIAN_POINT('Ctrl Pts',(366.901318079705,-18.970836477995,-0.00133472881285637));
#44123=CARTESIAN_POINT('Ctrl Pts',(366.901360682557,-18.9771541147819,-0.126871096239978));
#44124=CARTESIAN_POINT('Ctrl Pts',(366.907417918414,-18.9834717515689,-0.252229964907151));
#44125=CARTESIAN_POINT('Ctrl Pts',(366.919413884164,-18.9897893883558,-0.376849987441945));
#44126=CARTESIAN_POINT('Ctrl Pts',(366.931459197123,-18.9961330136919,-0.501982653182976));
#44127=CARTESIAN_POINT('Ctrl Pts',(366.949492110904,-19.002476639028,-0.626370088264227));
#44128=CARTESIAN_POINT('Ctrl Pts',(366.973385122635,-19.008820264364,-0.749458104145278));
#44129=CARTESIAN_POINT('Ctrl Pts',(366.997328647286,-19.0151773009453,-0.872806344026037));
#44130=CARTESIAN_POINT('Ctrl Pts',(367.027156945381,-19.0215343375265,-0.994849386593892));
#44131=CARTESIAN_POINT('Ctrl Pts',(367.06269260094,-19.0278913741077,-1.11504796144853));
#44132=CARTESIAN_POINT('Ctrl Pts',(367.098341619796,-19.0342686904509,-1.23562998517139));
#44133=CARTESIAN_POINT('Ctrl Pts',(367.139734326602,-19.040646006794,-1.3543554840663));
#44134=CARTESIAN_POINT('Ctrl Pts',(367.186644262668,-19.0470233231372,-1.47070268129113));
#44135=CARTESIAN_POINT('Ctrl Pts',(367.212448102359,-19.0505313059311,-1.53470201016626));
#44136=CARTESIAN_POINT('Ctrl Pts',(367.239920520888,-19.0540392887251,-1.5979821369739));
#44137=CARTESIAN_POINT('Ctrl Pts',(367.269018002693,-19.057547271519,-1.66045956765047));
#44138=CARTESIAN_POINT('Ctrl Pts',(367.317738187542,-19.0634209609096,-1.76507040620682));
#44139=CARTESIAN_POINT('Ctrl Pts',(367.371147557887,-19.0692946503001,-1.86770937983961));
#44140=CARTESIAN_POINT('Ctrl Pts',(367.42906402566,-19.0751683396907,-1.96792666780601));
#44141=CARTESIAN_POINT('Ctrl Pts',(367.486905717833,-19.0810344455964,-2.06801456583865));
#44142=CARTESIAN_POINT('Ctrl Pts',(367.549242730345,-19.0869005515022,-2.16568664159388));
#44143=CARTESIAN_POINT('Ctrl Pts',(367.615845467115,-19.0927666574079,-2.26051421138093));
#44144=CARTESIAN_POINT('Ctrl Pts',(367.682380003531,-19.0986267564959,-2.35524467894446));
#44145=CARTESIAN_POINT('Ctrl Pts',(367.753171339751,-19.104486855584,-2.44713609813943));
#44146=CARTESIAN_POINT('Ctrl Pts',(367.82794498033,-19.110346954672,-2.53578610082354));
#44147=CARTESIAN_POINT('Ctrl Pts',(367.905416283276,-19.1164184727661,-2.62763439336167));
#44148=CARTESIAN_POINT('Ctrl Pts',(367.987162434697,-19.1224899908602,-2.71600257662339));
#44149=CARTESIAN_POINT('Ctrl Pts',(368.072830120906,-19.1285615089543,-2.80047754932223));
#44150=CARTESIAN_POINT('Ctrl Pts',(368.155419698686,-19.1344148725511,-2.88191726874117));
#44151=CARTESIAN_POINT('Ctrl Pts',(368.241653533961,-19.1402682361478,-2.95973842014678));
#44152=CARTESIAN_POINT('Ctrl Pts',(368.331175957581,-19.1461215997446,-3.03360670659181));
#44153=CARTESIAN_POINT('Ctrl Pts',(368.420684939711,-19.1519740844785,-3.1074639019622));
#44154=CARTESIAN_POINT('Ctrl Pts',(368.513481209804,-19.1578265692124,-3.17736914961774));
#44155=CARTESIAN_POINT('Ctrl Pts',(368.609175352991,-19.1636790539462,-3.24302788357669));
#44156=CARTESIAN_POINT('Ctrl Pts',(368.704878270046,-19.1695320752744,-3.30869263755996));
#44157=CARTESIAN_POINT('Ctrl Pts',(368.80347924769,-19.1753850966026,-3.37010987010404));
#44158=CARTESIAN_POINT('Ctrl Pts',(368.90455977919,-19.1812381179307,-3.42702827179763));
#44159=CARTESIAN_POINT('Ctrl Pts',(369.005674022999,-19.1870930913546,-3.48396565687741));
#44160=CARTESIAN_POINT('Ctrl Pts',(369.109269105275,-19.1929480647784,-3.53640102493135));
#44161=CARTESIAN_POINT('Ctrl Pts',(369.214902455271,-19.1988030382022,-3.58412929020052));
#44162=CARTESIAN_POINT('Ctrl Pts',(369.320655527102,-19.2046646474863,-3.63191164932791));
#44163=CARTESIAN_POINT('Ctrl Pts',(369.428451100795,-19.2105262567705,-3.67497608733073));
#44164=CARTESIAN_POINT('Ctrl Pts',(369.537827099443,-19.2163878660546,-3.71316586289387));
#44165=CARTESIAN_POINT('Ctrl Pts',(369.64727685113,-19.222253427865,-3.75138139010318));
#44166=CARTESIAN_POINT('Ctrl Pts',(369.758308755084,-19.2281189896753,-3.7847155911826));
#44167=CARTESIAN_POINT('Ctrl Pts',(369.870447751639,-19.2339845514857,-3.81306221130359));
#44168=CARTESIAN_POINT('Ctrl Pts',(369.982750722912,-19.239858690186,-3.84145028113563));
#44169=CARTESIAN_POINT('Ctrl Pts',(370.096163614508,-19.2457328288863,-3.86483613176681));
#44170=CARTESIAN_POINT('Ctrl Pts',(370.210203343254,-19.2516069675866,-3.88316495637836));
#44171=CARTESIAN_POINT('Ctrl Pts',(370.239042128942,-19.253092441368,-3.88780001690246));
#44172=CARTESIAN_POINT('Ctrl Pts',(370.267920988874,-19.2545779151493,-3.89211193979668));
#44173=CARTESIAN_POINT('Ctrl Pts',(370.296832099317,-19.2560633889306,-3.89610036630829));
#44174=CARTESIAN_POINT('Ctrl Pts',(370.411149083444,-19.2619370783212,-3.91187094319813));
#44175=CARTESIAN_POINT('Ctrl Pts',(370.526351146057,-19.2678107677117,-3.92263219398958));
#44176=CARTESIAN_POINT('Ctrl Pts',(370.641961587585,-19.2736844571023,-3.92829327661127));
#44177=CARTESIAN_POINT('Ctrl Pts',(370.757422765171,-19.279550563008,-3.93394705024346));
#44178=CARTESIAN_POINT('Ctrl Pts',(370.873290864252,-19.2854166689138,-3.93451373068495));
#44179=CARTESIAN_POINT('Ctrl Pts',(370.989081192337,-19.2912827748195,-3.92995385581899));
#44180=CARTESIAN_POINT('Ctrl Pts',(371.104752952602,-19.2971428739076,-3.9253986502068));
#44181=CARTESIAN_POINT('Ctrl Pts',(371.220346689904,-19.3030029729956,-3.9157273471927));
#44182=CARTESIAN_POINT('Ctrl Pts',(371.335375484545,-19.3088630720836,-3.90095247985606));
#44183=CARTESIAN_POINT('Ctrl Pts',(371.454554255674,-19.3149345901777,-3.88564456901275));
#44184=CARTESIAN_POINT('Ctrl Pts',(371.573126099686,-19.3210061082718,-3.8648578691115));
#44185=CARTESIAN_POINT('Ctrl Pts',(371.690552349617,-19.3270776263659,-3.83866532628028));
#44186=CARTESIAN_POINT('Ctrl Pts',(371.803759380543,-19.3329309899627,-3.81341390244562));
#44187=CARTESIAN_POINT('Ctrl Pts',(371.915901287021,-19.3387843535594,-3.78313852030409));
#44188=CARTESIAN_POINT('Ctrl Pts',(372.026504345074,-19.3446377171562,-3.74795682587877));
#44189=CARTESIAN_POINT('Ctrl Pts',(372.137090796449,-19.35049020189,-3.71278041386648));
#44190=CARTESIAN_POINT('Ctrl Pts',(372.246138465218,-19.3563426866239,-3.67269927954016));
#44191=CARTESIAN_POINT('Ctrl Pts',(372.35318871977,-19.3621951713578,-3.62788096424845));
#44192=CARTESIAN_POINT('Ctrl Pts',(372.460248789394,-19.368048192686,-3.58305853971897));
#44193=CARTESIAN_POINT('Ctrl Pts',(372.56531069963,-19.3739012140142,-3.53349823036469));
#44194=CARTESIAN_POINT('Ctrl Pts',(372.667936396727,-19.3797542353423,-3.47941547345534));
#44195=CARTESIAN_POINT('Ctrl Pts',(372.770596321477,-19.3856092087661,-3.42531467890212));
#44196=CARTESIAN_POINT('Ctrl Pts',(372.870818052119,-19.3914641821899,-3.36668863006954));
#44197=CARTESIAN_POINT('Ctrl Pts',(372.96818933167,-19.3973191556137,-3.30379804368741));
#44198=CARTESIAN_POINT('Ctrl Pts',(373.065670969061,-19.4031807648979,-3.24083617890363));
#44199=CARTESIAN_POINT('Ctrl Pts',(373.160295359994,-19.409042374182,-3.17360035386299));
#44200=CARTESIAN_POINT('Ctrl Pts',(373.251680297225,-19.4149039834662,-3.10239388445946));
#44201=CARTESIAN_POINT('Ctrl Pts',(373.343126855991,-19.4207695452765,-3.03113940001062));
#44202=CARTESIAN_POINT('Ctrl Pts',(373.431329297897,-19.4266351070868,-2.95590920727541));
#44203=CARTESIAN_POINT('Ctrl Pts',(373.515940801815,-19.4325006688972,-2.87704490086488));
#44204=CARTESIAN_POINT('Ctrl Pts',(373.600676028503,-19.4383748075975,-2.79806527549567));
#44205=CARTESIAN_POINT('Ctrl Pts',(373.681809549507,-19.4442489462978,-2.71544122476306));
#44206=CARTESIAN_POINT('Ctrl Pts',(373.759033426244,-19.4501230849981,-2.62954897595268));
#44207=CARTESIAN_POINT('Ctrl Pts',(373.778562083983,-19.4516085587795,-2.60782822842825));
#44208=CARTESIAN_POINT('Ctrl Pts',(373.797840931265,-19.4530940325609,-2.58589863021964));
#44209=CARTESIAN_POINT('Ctrl Pts',(373.816865425307,-19.4545795063423,-2.56376656118758));
#44210=CARTESIAN_POINT('Ctrl Pts',(373.892089889188,-19.4604531957329,-2.47625448208237));
#44211=CARTESIAN_POINT('Ctrl Pts',(373.963584786505,-19.4663268851236,-2.38528306125726));
#44212=CARTESIAN_POINT('Ctrl Pts',(374.03101535858,-19.4722005745142,-2.29120362675335));
#44213=CARTESIAN_POINT('Ctrl Pts',(374.098358871452,-19.47806668042,-2.19724565763779));
#44214=CARTESIAN_POINT('Ctrl Pts',(374.161648256009,-19.4839327863259,-2.10018798759542));
#44215=CARTESIAN_POINT('Ctrl Pts',(374.220587595515,-19.4897988922317,-2.00041651473943));
#44216=CARTESIAN_POINT('Ctrl Pts',(374.279466581889,-19.4956589913198,-1.90074720660059));
#44217=CARTESIAN_POINT('Ctrl Pts',(374.334004174478,-19.5015190904079,-1.79836997670861));
#44218=CARTESIAN_POINT('Ctrl Pts',(374.383946941129,-19.507379189496,-1.69370078180889));
#44219=CARTESIAN_POINT('Ctrl Pts',(374.435691528861,-19.5134507075901,-1.58525536114756));
#44220=CARTESIAN_POINT('Ctrl Pts',(374.482503226193,-19.5195222256841,-1.47434984244847));
#44221=CARTESIAN_POINT('Ctrl Pts',(374.524151313843,-19.5255937437782,-1.3614764165776));
#44222=CARTESIAN_POINT('Ctrl Pts',(374.56430295242,-19.531447107375,-1.25265862310272));
#44223=CARTESIAN_POINT('Ctrl Pts',(374.599655505314,-19.5373004709719,-1.142012326479));
#44224=CARTESIAN_POINT('Ctrl Pts',(374.630051021127,-19.5431538345687,-1.02999937770978));
#44225=CARTESIAN_POINT('Ctrl Pts',(374.660441973156,-19.5490063193026,-0.918003247307915));
#44226=CARTESIAN_POINT('Ctrl Pts',(374.685877259849,-19.5548588040366,-0.804641271390275));
#44227=CARTESIAN_POINT('Ctrl Pts',(374.706249038959,-19.5607112887706,-0.690389667455808));
#44228=CARTESIAN_POINT('Ctrl Pts',(374.726622685888,-19.5665643100988,-0.576127588183244));
#44229=CARTESIAN_POINT('Ctrl Pts',(374.741931829811,-19.5724173314271,-0.460976125498675));
#44230=CARTESIAN_POINT('Ctrl Pts',(374.752120031252,-19.5782703527553,-0.34542016999933));
#44231=CARTESIAN_POINT('Ctrl Pts',(374.762311630654,-19.5841253261792,-0.22982567435726));
#44232=CARTESIAN_POINT('Ctrl Pts',(374.767378855159,-19.5899802996031,-0.113826828971878));
#44233=CARTESIAN_POINT('Ctrl Pts',(374.76731729865,-19.595835273027,0.00208860636006148));
#44234=CARTESIAN_POINT('Ctrl Pts',(374.767255672375,-19.6016968823112,0.118135416949179));
#44235=CARTESIAN_POINT('Ctrl Pts',(374.762053663277,-19.6075584915954,0.234098215423539));
#44236=CARTESIAN_POINT('Ctrl Pts',(374.751758951901,-19.6134201008796,0.349491399606124));
#44237=CARTESIAN_POINT('Ctrl Pts',(374.741457298725,-19.61928566269,0.464962394260245));
#44238=CARTESIAN_POINT('Ctrl Pts',(374.726056160073,-19.6251512245004,0.579862601334531));
#44239=CARTESIAN_POINT('Ctrl Pts',(374.705654565544,-19.6310167863108,0.693715402625332));
#44240=CARTESIAN_POINT('Ctrl Pts',(374.685223138881,-19.6368909250112,0.807734684635805));
#44241=CARTESIAN_POINT('Ctrl Pts',(374.659776754079,-19.6427650637116,0.920703102748728));
#44242=CARTESIAN_POINT('Ctrl Pts',(374.629464621444,-19.648639202412,1.03215793736561));
#44243=CARTESIAN_POINT('Ctrl Pts',(374.621799177954,-19.6501246761927,1.0603430455137));
#44244=CARTESIAN_POINT('Ctrl Pts',(374.61382281097,-19.6516101499733,1.08843145591653));
#44245=CARTESIAN_POINT('Ctrl Pts',(374.605538418854,-19.6530956237539,1.11641589265502));
#44246=CARTESIAN_POINT('Ctrl Pts',(374.572781229388,-19.6589693131444,1.22706873036416));
#44247=CARTESIAN_POINT('Ctrl Pts',(374.535095294422,-19.6648430025348,1.33646292607124));
#44248=CARTESIAN_POINT('Ctrl Pts',(374.492594361804,-19.6707166919253,1.44412672115984));
#44249=CARTESIAN_POINT('Ctrl Pts',(374.450148301883,-19.676582797831,1.55165151217438));
#44250=CARTESIAN_POINT('Ctrl Pts',(374.402899757431,-19.6824489037366,1.65744996470563));
#44251=CARTESIAN_POINT('Ctrl Pts',(374.351012582384,-19.6883150096423,1.76106421856201));
#44252=CARTESIAN_POINT('Ctrl Pts',(374.299178539143,-19.6941751087302,1.86457237274251));
#44253=CARTESIAN_POINT('Ctrl Pts',(374.242715497142,-19.7000352078182,1.96590040979602));
#44254=CARTESIAN_POINT('Ctrl Pts',(374.181835600117,-19.7058953069061,2.06460987458625));
#44255=CARTESIAN_POINT('Ctrl Pts',(374.118759295294,-19.7119668250002,2.16688055167612));
#44256=CARTESIAN_POINT('Ctrl Pts',(374.050941583983,-19.7180383430944,2.26633972479668));
#44257=CARTESIAN_POINT('Ctrl Pts',(373.978670982913,-19.7241098611885,2.3625266973765));
#44258=CARTESIAN_POINT('Ctrl Pts',(373.908997122298,-19.7299632247852,2.45525759515865));
#44259=CARTESIAN_POINT('Ctrl Pts',(373.835185126145,-19.7358165883818,2.54494703252978));
#44260=CARTESIAN_POINT('Ctrl Pts',(373.757537464523,-19.7416699519785,2.63121190786983));
#44261=CARTESIAN_POINT('Ctrl Pts',(373.679901461436,-19.7475224367123,2.71746383082914));
#44262=CARTESIAN_POINT('Ctrl Pts',(373.598431214332,-19.7533749214461,2.80029190716383));
#44263=CARTESIAN_POINT('Ctrl Pts',(373.513468430205,-19.7592274061799,2.8793473541516));
#44264=CARTESIAN_POINT('Ctrl Pts',(373.428497856132,-19.765080427508,2.95841004946246));
#44265=CARTESIAN_POINT('Ctrl Pts',(373.34003441095,-19.7709334488361,3.03369914636178));
#44266=CARTESIAN_POINT('Ctrl Pts',(373.248454955657,-19.7767864701641,3.1049043545102));
#44267=CARTESIAN_POINT('Ctrl Pts',(373.156844956847,-19.7826414435879,3.17613331097065));
#44268=CARTESIAN_POINT('Ctrl Pts',(373.062117207405,-19.7884964170116,3.24327541683511));
#44269=CARTESIAN_POINT('Ctrl Pts',(372.964679187118,-19.7943513904353,3.3060625503836));
#44270=CARTESIAN_POINT('Ctrl Pts',(372.867130733351,-19.8002129997194,3.36892084508327));
#44271=CARTESIAN_POINT('Ctrl Pts',(372.766866225204,-19.8060746090034,3.42741409199333));
#44272=CARTESIAN_POINT('Ctrl Pts',(372.664319566075,-19.8119362182875,3.48131910789031));
#44273=CARTESIAN_POINT('Ctrl Pts',(372.561703758981,-19.8178017800978,3.53526047233538));
#44274=CARTESIAN_POINT('Ctrl Pts',(372.456803109591,-19.823667341908,3.58460726974267));
#44275=CARTESIAN_POINT('Ctrl Pts',(372.35007180881,-19.8295329037182,3.62918433620061));
#44276=CARTESIAN_POINT('Ctrl Pts',(372.243184440691,-19.8354070424185,3.67382658526298));
#44277=CARTESIAN_POINT('Ctrl Pts',(372.134461465246,-19.8412811811187,3.71368504233485));
#44278=CARTESIAN_POINT('Ctrl Pts',(372.024372597712,-19.847155319819,3.74863424531133));
#44279=CARTESIAN_POINT('Ctrl Pts',(371.996532920309,-19.8486407936012,3.75747232819979));
#44280=CARTESIAN_POINT('Ctrl Pts',(371.968605944197,-19.8501262673834,3.76599671886881));
#44281=CARTESIAN_POINT('Ctrl Pts',(371.940599354617,-19.8516117411656,3.77420590848924));
#44282=CARTESIAN_POINT('Ctrl Pts',(371.829858922811,-19.8574854305561,3.80666574087095));
#44283=CARTESIAN_POINT('Ctrl Pts',(371.717504217943,-19.8633591199467,3.83430158793234));
#44284=CARTESIAN_POINT('Ctrl Pts',(371.603993326271,-19.8692328093372,3.85695328804873));
#44285=CARTESIAN_POINT('Ctrl Pts',(371.490628987824,-19.8750989152429,3.87957574269224));
#44286=CARTESIAN_POINT('Ctrl Pts',(371.37611183261,-19.8809650211486,3.897226767387));
#44287=CARTESIAN_POINT('Ctrl Pts',(371.260915430919,-19.8868311270543,3.90979583951701));
#44288=CARTESIAN_POINT('Ctrl Pts',(371.145836988876,-19.8926912261422,3.92235204107728));
#44289=CARTESIAN_POINT('Ctrl Pts',(371.030081092109,-19.8985513252302,3.92983659642516));
#44290=CARTESIAN_POINT('Ctrl Pts',(370.914131183045,-19.9044114243182,3.93219008090693));
#44291=CARTESIAN_POINT('Ctrl Pts',(370.793998065785,-19.9104829424123,3.93462847373969));
#44292=CARTESIAN_POINT('Ctrl Pts',(370.673657115819,-19.9165544605065,3.93155848245061));
#44293=CARTESIAN_POINT('Ctrl Pts',(370.553651867755,-19.9226259786006,3.92297280191958));
#44294=CARTESIAN_POINT('Ctrl Pts',(370.437958504162,-19.9284793421973,3.91469561175165));
#44295=CARTESIAN_POINT('Ctrl Pts',(370.322577580986,-19.934332705794,3.90129230920255));
#44296=CARTESIAN_POINT('Ctrl Pts',(370.207994993426,-19.9401860693907,3.88280937921176));
#44297=CARTESIAN_POINT('Ctrl Pts',(370.093429610056,-19.9460385541245,3.86432922437072));
#44298=CARTESIAN_POINT('Ctrl Pts',(369.979662731724,-19.9518910388584,3.84077102437501));
#44299=CARTESIAN_POINT('Ctrl Pts',(369.867172685898,-19.9577435235922,3.81223283986149));
#44300=CARTESIAN_POINT('Ctrl Pts',(369.754672326246,-19.9635965449203,3.78369203877961));
#44301=CARTESIAN_POINT('Ctrl Pts',(369.643449432302,-19.9694495662484,3.75017044710643));
#44302=CARTESIAN_POINT('Ctrl Pts',(369.533969043405,-19.9753025875765,3.71181653275089));
#44303=CARTESIAN_POINT('Ctrl Pts',(369.424452140684,-19.9811575610003,3.67344982662421));
#44304=CARTESIAN_POINT('Ctrl Pts',(369.316679288319,-19.9870125344241,3.63024772959784));
#44305=CARTESIAN_POINT('Ctrl Pts',(369.211096689763,-19.9928675078478,3.58240729879948));
#44306=CARTESIAN_POINT('Ctrl Pts',(369.105394426893,-19.9987291171319,3.53451264701771));
#44307=CARTESIAN_POINT('Ctrl Pts',(369.001887749023,-20.004590726416,3.4819693395051));
#44308=CARTESIAN_POINT('Ctrl Pts',(368.900999421924,-20.0104523357001,3.42502099894235));
#44309=CARTESIAN_POINT('Ctrl Pts',(368.800043065086,-20.0163178975104,3.36803425769536));
#44310=CARTESIAN_POINT('Ctrl Pts',(368.701708924245,-20.0221834593206,3.30663678704779));
#44311=CARTESIAN_POINT('Ctrl Pts',(368.606390412219,-20.0280490211309,3.24111528915836));
#44312=CARTESIAN_POINT('Ctrl Pts',(368.51093252115,-20.0339231598312,3.17549798276875));
#44313=CARTESIAN_POINT('Ctrl Pts',(368.418499387841,-20.0397972985315,3.10574486200305));
#44314=CARTESIAN_POINT('Ctrl Pts',(368.32945107618,-20.0456714372317,3.0321826180591));
#44315=CARTESIAN_POINT('Ctrl Pts',(368.306932211876,-20.0471569110136,3.01357992747079));
#44316=CARTESIAN_POINT('Ctrl Pts',(368.284629620145,-20.0486423847955,2.9947338235567));
#44317=CARTESIAN_POINT('Ctrl Pts',(368.262548735111,-20.0501278585773,2.97564994633464));
#44318=CARTESIAN_POINT('Ctrl Pts',(368.176502957271,-20.0559165190782,2.90128304223486));
#44319=CARTESIAN_POINT('Ctrl Pts',(368.093522159799,-20.0617051795791,2.82303935525769));
#44320=CARTESIAN_POINT('Ctrl Pts',(368.013983734837,-20.0674938400799,2.74120492861447));
#44321=CARTESIAN_POINT('Ctrl Pts',(367.934548696519,-20.0732749762907,2.65947687303393));
#44322=CARTESIAN_POINT('Ctrl Pts',(367.858547431796,-20.0790561125014,2.574167656681));
#44323=CARTESIAN_POINT('Ctrl Pts',(367.78632452466,-20.0848372487121,2.48560368301691));
#44324=CARTESIAN_POINT('Ctrl Pts',(367.714182760477,-20.0906118897749,2.39713921161277));
#44325=CARTESIAN_POINT('Ctrl Pts',(367.645811177665,-20.0963865308376,2.30542758485855));
#44326=CARTESIAN_POINT('Ctrl Pts',(367.581517011793,-20.1021611719003,2.21083144676017));
#44327=CARTESIAN_POINT('Ctrl Pts',(367.517262887755,-20.1079322165679,2.11629422229607));
#44328=CARTESIAN_POINT('Ctrl Pts',(367.457081374441,-20.1137032612354,2.01887640667268));
#44329=CARTESIAN_POINT('Ctrl Pts',(367.401238614753,-20.119474305903,1.91897262679348));
#44330=CARTESIAN_POINT('Ctrl Pts',(367.3454162108,-20.1252432469165,1.81910526371693));
#44331=CARTESIAN_POINT('Ctrl Pts',(367.293929624938,-20.13101218793,1.71675410887057));
#44332=CARTESIAN_POINT('Ctrl Pts',(367.247000467295,-20.1367811289435,1.61234083636549));
#44333=CARTESIAN_POINT('Ctrl Pts',(367.200076297233,-20.1425494568401,1.50793866079034));
#44334=CARTESIAN_POINT('Ctrl Pts',(367.157708765978,-20.1483177847368,1.40147519241846));
#44335=CARTESIAN_POINT('Ctrl Pts',(367.120072119742,-20.1540861126335,1.29339384230438));
#44336=CARTESIAN_POINT('Ctrl Pts',(367.082410796346,-20.1598582226405,1.185241626664));
#44337=CARTESIAN_POINT('Ctrl Pts',(367.049486696699,-20.1656303326475,1.07546981267461));
#44338=CARTESIAN_POINT('Ctrl Pts',(367.021424697576,-20.1714024426545,0.964538637699085));
#44339=CARTESIAN_POINT('Ctrl Pts',(366.993353773675,-20.1771763884111,0.853572182409189));
#44340=CARTESIAN_POINT('Ctrl Pts',(366.970148118481,-20.1829503341676,0.741446048957956));
#44341=CARTESIAN_POINT('Ctrl Pts',(366.95188144196,-20.1887242799242,0.62863066461313));
#44342=CARTESIAN_POINT('Ctrl Pts',(366.933590720042,-20.1945058262322,0.515666775386035));
#44343=CARTESIAN_POINT('Ctrl Pts',(366.92025201549,-20.2002873725403,0.402012246335616));
#44344=CARTESIAN_POINT('Ctrl Pts',(366.911887134562,-20.2060689188483,0.288142772418037));
#44345=CARTESIAN_POINT('Ctrl Pts',(366.904765114104,-20.2109914385398,0.191192112895476));
#44346=CARTESIAN_POINT('Ctrl Pts',(366.901247804181,-20.2159139582314,0.0940858361474233));
#44347=CARTESIAN_POINT('Ctrl Pts',(366.901318910622,-20.2208364779229,-0.00288400549575217));
#44348=CARTESIAN_POINT('',(366.901319072764,-21.4708364780021,0.00309724080919957));
#44349=CARTESIAN_POINT('Ctrl Pts',(366.901318910622,-20.2208364779651,-0.00288400632674463));
#44350=CARTESIAN_POINT('Ctrl Pts',(366.901452804976,-20.230105643973,-0.185479428239274));
#44351=CARTESIAN_POINT('Ctrl Pts',(366.914303573141,-20.239374809981,-0.367615513842659));
#44352=CARTESIAN_POINT('Ctrl Pts',(366.939675353735,-20.248643975989,-0.547949633793549));
#44353=CARTESIAN_POINT('Ctrl Pts',(366.95575295536,-20.2545176653786,-0.662223842069158));
#44354=CARTESIAN_POINT('Ctrl Pts',(366.976891041824,-20.2603913547682,-0.775980165170206));
#44355=CARTESIAN_POINT('Ctrl Pts',(367.003046693838,-20.2662650441578,-0.88873522674322));
#44356=CARTESIAN_POINT('Ctrl Pts',(367.029168576447,-20.2721311500625,-1.00134471093884));
#44357=CARTESIAN_POINT('Ctrl Pts',(367.060295049186,-20.2779972559673,-1.11295510562502));
#44358=CARTESIAN_POINT('Ctrl Pts',(367.096331584714,-20.2838633618721,-1.22308939020565));
#44359=CARTESIAN_POINT('Ctrl Pts',(367.132331219289,-20.2897234609591,-1.33311089868209));
#44360=CARTESIAN_POINT('Ctrl Pts',(367.173230788142,-20.2955835600462,-1.44165891326165));
#44361=CARTESIAN_POINT('Ctrl Pts',(367.218885140078,-20.3014436591332,-1.54826848340756));
#44362=CARTESIAN_POINT('Ctrl Pts',(367.266186596888,-20.3075151772277,-1.65872428365451));
#44363=CARTESIAN_POINT('Ctrl Pts',(367.318592295747,-20.3135866953222,-1.76709868937213));
#44364=CARTESIAN_POINT('Ctrl Pts',(367.375884828439,-20.3196582134167,-1.87289348684829));
#44365=CARTESIAN_POINT('Ctrl Pts',(367.431118794632,-20.3255115770124,-1.97488699267859));
#44366=CARTESIAN_POINT('Ctrl Pts',(367.490894249033,-20.3313649406082,-2.07448268033402));
#44367=CARTESIAN_POINT('Ctrl Pts',(367.554968537456,-20.3372183042039,-2.17125702420816));
#44368=CARTESIAN_POINT('Ctrl Pts',(367.619033205341,-20.3430707889368,-2.26801683774035));
#44369=CARTESIAN_POINT('Ctrl Pts',(367.68739519582,-20.3489232736698,-2.36195580540828));
#44370=CARTESIAN_POINT('Ctrl Pts',(367.759767984918,-20.3547757584027,-2.45267855767936));
#44371=CARTESIAN_POINT('Ctrl Pts',(367.832147409629,-20.3606287797299,-2.54340962800885));
#44372=CARTESIAN_POINT('Ctrl Pts',(367.908538106326,-20.3664818010571,-2.63092357375398));
#44373=CARTESIAN_POINT('Ctrl Pts',(367.988613103915,-20.3723348223843,-2.71485791152273));
#44374=CARTESIAN_POINT('Ctrl Pts',(368.068714808062,-20.3781897958071,-2.79882024301425));
#44375=CARTESIAN_POINT('Ctrl Pts',(368.152502971456,-20.3840447692299,-2.87920029380748));
#44376=CARTESIAN_POINT('Ctrl Pts',(368.23961411925,-20.3898997426528,-2.95567277162098));
#44377=CARTESIAN_POINT('Ctrl Pts',(368.326823996341,-20.395761351936,-3.03223192116581));
#44378=CARTESIAN_POINT('Ctrl Pts',(368.417364064238,-20.4016229612192,-3.10487438553329));
#44379=CARTESIAN_POINT('Ctrl Pts',(368.510838085076,-20.4074845705024,-3.17331542192186));
#44380=CARTESIAN_POINT('Ctrl Pts',(368.604375136133,-20.4133501323118,-3.24180260860396));
#44381=CARTESIAN_POINT('Ctrl Pts',(368.700849736569,-20.4192156941212,-3.30608249755406));
#44382=CARTESIAN_POINT('Ctrl Pts',(368.799838500068,-20.4250812559306,-3.36591484764299));
#44383=CARTESIAN_POINT('Ctrl Pts',(368.898972009419,-20.43095539463,-3.42583468730284));
#44384=CARTESIAN_POINT('Ctrl Pts',(369.000626657562,-20.4368295333294,-3.48129381185933));
#44385=CARTESIAN_POINT('Ctrl Pts',(369.104356372638,-20.4427036720288,-3.53209884851597));
#44386=CARTESIAN_POINT('Ctrl Pts',(369.130587924348,-20.4441891458194,-3.54494661297028));
#44387=CARTESIAN_POINT('Ctrl Pts',(369.156952089498,-20.4456746196099,-3.55749699290705));
#44388=CARTESIAN_POINT('Ctrl Pts',(369.183441489458,-20.4471600934005,-3.56974736242766));
#44389=CARTESIAN_POINT('Ctrl Pts',(369.288182824173,-20.4530337827909,-3.61818636279223));
#44390=CARTESIAN_POINT('Ctrl Pts',(369.395232312874,-20.4589074721814,-3.66209224755502));
#44391=CARTESIAN_POINT('Ctrl Pts',(369.504160503663,-20.4647811615719,-3.701239039215));
#44392=CARTESIAN_POINT('Ctrl Pts',(369.612948057924,-20.4706472674776,-3.74033528868918));
#44393=CARTESIAN_POINT('Ctrl Pts',(369.723609105338,-20.4765133733832,-3.77468452587851));
#44394=CARTESIAN_POINT('Ctrl Pts',(369.835691557586,-20.4823794792889,-3.80410758544755));
#44395=CARTESIAN_POINT('Ctrl Pts',(369.947659238829,-20.4882395783768,-3.83350051617837));
#44396=CARTESIAN_POINT('Ctrl Pts',(370.061045032564,-20.4940996774647,-3.85797719862751));
#44397=CARTESIAN_POINT('Ctrl Pts',(370.175379549363,-20.4999597765527,-3.87740755037494));
#44398=CARTESIAN_POINT('Ctrl Pts',(370.293838994691,-20.5060312946468,-3.89753890488617));
#44399=CARTESIAN_POINT('Ctrl Pts',(370.413316486025,-20.512102812741,-3.91225278098042));
#44400=CARTESIAN_POINT('Ctrl Pts',(370.533275511409,-20.5181743308351,-3.92146178209539));
#44401=CARTESIAN_POINT('Ctrl Pts',(370.64892431314,-20.5240276944317,-3.93033989644041));
#44402=CARTESIAN_POINT('Ctrl Pts',(370.765020193394,-20.5298810580284,-3.93410188256667));
#44403=CARTESIAN_POINT('Ctrl Pts',(370.881075715139,-20.535734421625,-3.9327220474309));
#44404=CARTESIAN_POINT('Ctrl Pts',(370.997113811538,-20.5415869063588,-3.93134241947274));
#44405=CARTESIAN_POINT('Ctrl Pts',(371.113111148472,-20.5474393910926,-3.92482251024291));
#44406=CARTESIAN_POINT('Ctrl Pts',(371.228580166447,-20.5532918758263,-3.91318875450339));
#44407=CARTESIAN_POINT('Ctrl Pts',(371.344059771381,-20.5591448971544,-3.90155393210469));
#44408=CARTESIAN_POINT('Ctrl Pts',(371.459010549976,-20.5649979184824,-3.88480437254234));
#44409=CARTESIAN_POINT('Ctrl Pts',(371.572950650453,-20.5708509398104,-3.86301832649777));
#44410=CARTESIAN_POINT('Ctrl Pts',(371.686928752154,-20.5767059132341,-3.84122501438613));
#44411=CARTESIAN_POINT('Ctrl Pts',(371.799895099893,-20.5825608866578,-3.81439195320187));
#44412=CARTESIAN_POINT('Ctrl Pts',(371.911379304842,-20.5884158600815,-3.7826482296718));
#44413=CARTESIAN_POINT('Ctrl Pts',(372.022989862817,-20.5942774693655,-3.75086852870852));
#44414=CARTESIAN_POINT('Ctrl Pts',(372.133114527611,-20.6001390786495,-3.71416716999102));
#44415=CARTESIAN_POINT('Ctrl Pts',(372.241299223299,-20.6060006879335,-3.67272275352536));
#44416=CARTESIAN_POINT('Ctrl Pts',(372.349556868721,-20.6118662497437,-3.63125039078536));
#44417=CARTESIAN_POINT('Ctrl Pts',(372.455871562301,-20.6177318115538,-3.58502876613249));
#44418=CARTESIAN_POINT('Ctrl Pts',(372.559811905784,-20.623597373364,-3.53428341741013));
#44419=CARTESIAN_POINT('Ctrl Pts',(372.663904235542,-20.6294715120642,-3.48346386654189));
#44420=CARTESIAN_POINT('Ctrl Pts',(372.765614924711,-20.6353456507643,-3.42810758687781));
#44421=CARTESIAN_POINT('Ctrl Pts',(372.864539660816,-20.6412197894645,-3.36848458686931));
#44422=CARTESIAN_POINT('Ctrl Pts',(372.889556111642,-20.6427052632471,-3.35340690350608));
#44423=CARTESIAN_POINT('Ctrl Pts',(372.914394558932,-20.6441907370297,-3.33805656905684));
#44424=CARTESIAN_POINT('Ctrl Pts',(372.9390487961,-20.6456762108123,-3.32243836031613));
#44425=CARTESIAN_POINT('Ctrl Pts',(373.036533742045,-20.6515499002076,-3.26068263757789));
#44426=CARTESIAN_POINT('Ctrl Pts',(373.1314607476,-20.6574235896028,-3.19452990984376));
#44427=CARTESIAN_POINT('Ctrl Pts',(373.223407112138,-20.6632972789981,-3.12421854436298));
#44428=CARTESIAN_POINT('Ctrl Pts',(373.315234765282,-20.6691633849086,-3.05399795746024));
#44429=CARTESIAN_POINT('Ctrl Pts',(373.404089105203,-20.675029490819,-2.97962965904482));
#44430=CARTESIAN_POINT('Ctrl Pts',(373.489574496485,-20.6808955967295,-2.90139641524899));
#44431=CARTESIAN_POINT('Ctrl Pts',(373.574972351815,-20.6867556958223,-2.82324328129798));
#44432=CARTESIAN_POINT('Ctrl Pts',(373.657007817398,-20.692615794915,-2.74123335133565));
#44433=CARTESIAN_POINT('Ctrl Pts',(373.735317123481,-20.6984758940078,-2.65569053806536));
#44434=CARTESIAN_POINT('Ctrl Pts',(373.816451650586,-20.7045474121001,-2.56706153534387));
#44435=CARTESIAN_POINT('Ctrl Pts',(373.893585720489,-20.7106189301924,-2.47464019400463));
#44436=CARTESIAN_POINT('Ctrl Pts',(373.96635504494,-20.7166904482848,-2.37882997074371));
#44437=CARTESIAN_POINT('Ctrl Pts',(374.036509709485,-20.7225438118862,-2.28646228527293));
#44438=CARTESIAN_POINT('Ctrl Pts',(374.102607616852,-20.7283971754877,-2.19094541444005));
#44439=CARTESIAN_POINT('Ctrl Pts',(374.164362932726,-20.7342505390892,-2.092675026966));
#44440=CARTESIAN_POINT('Ctrl Pts',(374.226108976246,-20.7401030238278,-1.99441939446011));
#44441=CARTESIAN_POINT('Ctrl Pts',(374.283513504976,-20.7459555085664,-1.89341141708286));
#44442=CARTESIAN_POINT('Ctrl Pts',(374.336334421615,-20.751807993305,-1.79007512543936));
#44443=CARTESIAN_POINT('Ctrl Pts',(374.389160181222,-20.7576610146378,-1.68672935924563));
#44444=CARTESIAN_POINT('Ctrl Pts',(374.437401305259,-20.7635140359707,-1.58105522230921));
#44445=CARTESIAN_POINT('Ctrl Pts',(374.480862331955,-20.7693670573035,-1.47350003890016));
#44446=CARTESIAN_POINT('Ctrl Pts',(374.524337853742,-20.775222030732,-1.36590898376075));
#44447=CARTESIAN_POINT('Ctrl Pts',(374.563029953382,-20.7810770041605,-1.25643601750802));
#44448=CARTESIAN_POINT('Ctrl Pts',(374.596792101207,-20.786931977589,-1.14554639070893));
#44449=CARTESIAN_POINT('Ctrl Pts',(374.630592514089,-20.7927935868778,-1.03453108476222));
#44450=CARTESIAN_POINT('Ctrl Pts',(374.659451702506,-20.7986551961665,-0.922096309035752));
#44451=CARTESIAN_POINT('Ctrl Pts',(374.683273586565,-20.8045168054553,-0.808720447855802));
#44452=CARTESIAN_POINT('Ctrl Pts',(374.707111533896,-20.8103823672702,-0.695268136500583));
#44453=CARTESIAN_POINT('Ctrl Pts',(374.725905346492,-20.8162479290851,-0.580873882771531));
#44454=CARTESIAN_POINT('Ctrl Pts',(374.739610680474,-20.8221134909,-0.46602246021866));
#44455=CARTESIAN_POINT('Ctrl Pts',(374.753336055016,-20.8279876296049,-0.351003096718436));
#44456=CARTESIAN_POINT('Ctrl Pts',(374.761958070728,-20.8338617683097,-0.235525640664858));
#44457=CARTESIAN_POINT('Ctrl Pts',(374.765484436191,-20.8397359070146,-0.120076213154389));
#44458=CARTESIAN_POINT('Ctrl Pts',(374.76637619642,-20.841221380751,-0.0908809385667788));
#44459=CARTESIAN_POINT('Ctrl Pts',(374.766942348414,-20.8427068544874,-0.0616874349996441));
#44460=CARTESIAN_POINT('Ctrl Pts',(374.767183541498,-20.8441923282239,-0.0325035074423659));
#44461=CARTESIAN_POINT('Ctrl Pts',(374.76813723945,-20.8500660176043,0.0828922219920092));
#44462=CARTESIAN_POINT('Ctrl Pts',(374.76400941581,-20.8559397069847,0.198522152277014));
#44463=CARTESIAN_POINT('Ctrl Pts',(374.754771222418,-20.8618133963651,0.313901863608043));
#44464=CARTESIAN_POINT('Ctrl Pts',(374.745544956401,-20.8676795022607,0.429132608892232));
#44465=CARTESIAN_POINT('Ctrl Pts',(374.731221474499,-20.8735456081563,0.544113369609628));
#44466=CARTESIAN_POINT('Ctrl Pts',(374.711823909588,-20.8794117140519,0.65835840000756));
#44467=CARTESIAN_POINT('Ctrl Pts',(374.692446207536,-20.8852718131298,0.77248644495004));
#44468=CARTESIAN_POINT('Ctrl Pts',(374.668004826092,-20.8911319122077,0.885879853210644));
#44469=CARTESIAN_POINT('Ctrl Pts',(374.638574748598,-20.8969920112856,0.998057350056903));
#44470=CARTESIAN_POINT('Ctrl Pts',(374.608082900976,-20.9030635293835,1.11428195534522));
#44471=CARTESIAN_POINT('Ctrl Pts',(374.572235635544,-20.9091350474815,1.22920080788944));
#44472=CARTESIAN_POINT('Ctrl Pts',(374.531174496003,-20.9152065655794,1.34228907569993));
#44473=CARTESIAN_POINT('Ctrl Pts',(374.491588716113,-20.9210599291661,1.45131399141539));
#44474=CARTESIAN_POINT('Ctrl Pts',(374.447157444423,-20.9269132927529,1.55863718558821));
#44475=CARTESIAN_POINT('Ctrl Pts',(374.39805821096,-20.9327666563396,1.66380397362335));
#44476=CARTESIAN_POINT('Ctrl Pts',(374.348966349581,-20.9386191410636,1.76895497122027));
#44477=CARTESIAN_POINT('Ctrl Pts',(374.295208094768,-20.9444716257875,1.87194983221472));
#44478=CARTESIAN_POINT('Ctrl Pts',(374.237008519516,-20.9503241105115,1.9723552493226));
#44479=CARTESIAN_POINT('Ctrl Pts',(374.178803608143,-20.9561771318298,2.07276987226034));
#44480=CARTESIAN_POINT('Ctrl Pts',(374.116156774036,-20.9620301531481,2.17059422189032));
#44481=CARTESIAN_POINT('Ctrl Pts',(374.049337945602,-20.9678831744664,2.2654215514133));
#44482=CARTESIAN_POINT('Ctrl Pts',(373.982496831797,-20.9737381478804,2.36028050768339));
#44483=CARTESIAN_POINT('Ctrl Pts',(373.911481194693,-20.9795931212944,2.45214011871587));
#44484=CARTESIAN_POINT('Ctrl Pts',(373.836602552863,-20.9854480947085,2.54062503772484));
#44485=CARTESIAN_POINT('Ctrl Pts',(373.761639045708,-20.991309703983,2.62921024302679));
#44486=CARTESIAN_POINT('Ctrl Pts',(373.682804062196,-20.9971713132576,2.7144128067209));
#44487=CARTESIAN_POINT('Ctrl Pts',(373.600447506606,-21.0030329225321,2.79589265542889));
#44488=CARTESIAN_POINT('Ctrl Pts',(373.518035417384,-21.0088984843329,2.87742744659855));
#44489=CARTESIAN_POINT('Ctrl Pts',(373.432097333195,-21.0147640461337,2.9552342477066));
#44490=CARTESIAN_POINT('Ctrl Pts',(373.343016573817,-21.0206296079345,3.02901299589426));
#44491=CARTESIAN_POINT('Ctrl Pts',(373.253805556517,-21.0265037466255,3.10289962670991));
#44492=CARTESIAN_POINT('Ctrl Pts',(373.161443021103,-21.0323778853165,3.1727462014037));
#44493=CARTESIAN_POINT('Ctrl Pts',(373.066341637842,-21.0382520240075,3.23829566668944));
#44494=CARTESIAN_POINT('Ctrl Pts',(373.042292048985,-21.0397374978835,3.25487205744056));
#44495=CARTESIAN_POINT('Ctrl Pts',(373.018067432976,-21.0412229717596,3.27117387689709));
#44496=CARTESIAN_POINT('Ctrl Pts',(372.993674700417,-21.0427084456356,3.28719743953415));
#44497=CARTESIAN_POINT('Ctrl Pts',(372.897223771986,-21.0485821350287,3.35055596197067));
#44498=CARTESIAN_POINT('Ctrl Pts',(372.797821301549,-21.0544558244219,3.40977140443017));
#44499=CARTESIAN_POINT('Ctrl Pts',(372.695858712007,-21.0603295138151,3.46455691699246));
#44500=CARTESIAN_POINT('Ctrl Pts',(372.59402776575,-21.0661956197233,3.51927169631031));
#44501=CARTESIAN_POINT('Ctrl Pts',(372.489643634267,-21.0720617256316,3.56956772609213));
#44502=CARTESIAN_POINT('Ctrl Pts',(372.38312703408,-21.0779278315399,3.61520111768275));
#44503=CARTESIAN_POINT('Ctrl Pts',(372.276719505538,-21.0837879306303,3.660787781261));
#44504=CARTESIAN_POINT('Ctrl Pts',(372.168184229198,-21.0896480297208,3.70172114175997));
#44505=CARTESIAN_POINT('Ctrl Pts',(372.057966273182,-21.0955081288112,3.73780330466084));
#44506=CARTESIAN_POINT('Ctrl Pts',(371.943771904825,-21.1015796469044,3.77518722966137));
#44507=CARTESIAN_POINT('Ctrl Pts',(371.827771547821,-21.1076511649975,3.80736309407919));
#44508=CARTESIAN_POINT('Ctrl Pts',(371.710482954793,-21.1137226830907,3.83416532178671));
#44509=CARTESIAN_POINT('Ctrl Pts',(371.597408634589,-21.1195760466896,3.86000452404651));
#44510=CARTESIAN_POINT('Ctrl Pts',(371.483137497155,-21.1254294102886,3.88084950207157));
#44511=CARTESIAN_POINT('Ctrl Pts',(371.368147858245,-21.1312827738875,3.89660294689349));
#44512=CARTESIAN_POINT('Ctrl Pts',(371.253175484644,-21.1371352586235,3.91235402638843));
#44513=CARTESIAN_POINT('Ctrl Pts',(371.137485233285,-21.1429877433595,3.92301503668544));
#44514=CARTESIAN_POINT('Ctrl Pts',(371.021563229891,-21.1488402280955,3.92854020838743));
#44515=CARTESIAN_POINT('Ctrl Pts',(370.905630598008,-21.1546932494256,3.93406588667338));
#44516=CARTESIAN_POINT('Ctrl Pts',(370.789466584549,-21.1605462707558,3.93445477061387));
#44517=CARTESIAN_POINT('Ctrl Pts',(370.673559312802,-21.166399292086,3.92971318185962));
#44518=CARTESIAN_POINT('Ctrl Pts',(370.557613383742,-21.1722542655117,3.92497001169402));
#44519=CARTESIAN_POINT('Ctrl Pts',(370.441924779238,-21.1781092389374,3.91509298324243));
#44520=CARTESIAN_POINT('Ctrl Pts',(370.326977783324,-21.1839642123631,3.90014038894418));
#44521=CARTESIAN_POINT('Ctrl Pts',(370.211900509757,-21.189825821649,3.88517084780129));
#44522=CARTESIAN_POINT('Ctrl Pts',(370.097566932325,-21.1956874309349,3.86511431248825));
#44523=CARTESIAN_POINT('Ctrl Pts',(369.984452503796,-21.2015490402208,3.8400804533032));
#44524=CARTESIAN_POINT('Ctrl Pts',(369.871261801379,-21.2074146020328,3.81502971360342));
#44525=CARTESIAN_POINT('Ctrl Pts',(369.759292282861,-21.2132801638448,3.78499507377435));
#44526=CARTESIAN_POINT('Ctrl Pts',(369.649003894717,-21.2191457256568,3.75013597350411));
#44527=CARTESIAN_POINT('Ctrl Pts',(369.538554237903,-21.2250198643587,3.71522590068036));
#44528=CARTESIAN_POINT('Ctrl Pts',(369.429791004014,-21.2308940030605,3.67547742958702));
#44529=CARTESIAN_POINT('Ctrl Pts',(369.323153909422,-21.2367681417624,3.63109797925539));
#44530=CARTESIAN_POINT('Ctrl Pts',(369.296187129427,-21.238253615524,3.61987514091798));
#44531=CARTESIAN_POINT('Ctrl Pts',(369.269356189941,-21.2397390892856,3.60835637822619));
#44532=CARTESIAN_POINT('Ctrl Pts',(369.242667934241,-21.2412245630472,3.59654550025453));
#44533=CARTESIAN_POINT('Ctrl Pts',(369.137140304322,-21.2470982524757,3.54984428554753));
#44534=CARTESIAN_POINT('Ctrl Pts',(369.033494078067,-21.2529719419041,3.49841686381802));
#44535=CARTESIAN_POINT('Ctrl Pts',(368.932182491796,-21.2588456313325,3.44243664673818));
#44536=CARTESIAN_POINT('Ctrl Pts',(368.831001708298,-21.2647117372763,3.38652870537574));
#44537=CARTESIAN_POINT('Ctrl Pts',(368.73214992876,-21.2705778432201,3.3260798562357));
#44538=CARTESIAN_POINT('Ctrl Pts',(368.636060169164,-21.2764439491639,3.26131141635881));
#44539=CARTESIAN_POINT('Ctrl Pts',(368.540068804256,-21.28230404829,3.19660929853768));
#44540=CARTESIAN_POINT('Ctrl Pts',(368.446834174171,-21.2881641474162,3.12759661764776));
#44541=CARTESIAN_POINT('Ctrl Pts',(368.35676384689,-21.2940242465424,3.05454008742687));
#44542=CARTESIAN_POINT('Ctrl Pts',(368.26344398851,-21.3000957646222,2.97884784493437));
#44543=CARTESIAN_POINT('Ctrl Pts',(368.173521460681,-21.3061672827021,2.89881467686665));
#44544=CARTESIAN_POINT('Ctrl Pts',(368.087416076936,-21.3122388007819,2.81478589442049));
#44545=CARTESIAN_POINT('Ctrl Pts',(368.004404527708,-21.3180921644168,2.73377633256362));
#44546=CARTESIAN_POINT('Ctrl Pts',(367.924940858342,-21.3239455280518,2.64905365930629));
#44547=CARTESIAN_POINT('Ctrl Pts',(367.849366137848,-21.3297988916867,2.56096705501532));
#44548=CARTESIAN_POINT('Ctrl Pts',(367.773802764645,-21.3356513764586,2.4728936766323));
#44549=CARTESIAN_POINT('Ctrl Pts',(367.702127448222,-21.3415038612306,2.38145768498256));
#44550=CARTESIAN_POINT('Ctrl Pts',(367.634642182345,-21.3473563460026,2.28704276330556));
#44551=CARTESIAN_POINT('Ctrl Pts',(367.567150728977,-21.3532093673688,2.19261918504946));
#44552=CARTESIAN_POINT('Ctrl Pts',(367.503850330107,-21.359062388735,2.0952164699443));
#44553=CARTESIAN_POINT('Ctrl Pts',(367.445000289882,-21.3649154101012,1.9952482188496));
#44554=CARTESIAN_POINT('Ctrl Pts',(367.386130622034,-21.3707703835628,1.89524662641543));
#44555=CARTESIAN_POINT('Ctrl Pts',(367.331714473735,-21.3766253570245,1.79267815239974));
#44556=CARTESIAN_POINT('Ctrl Pts',(367.281965396373,-21.3824803304862,1.68798134536636));
#44557=CARTESIAN_POINT('Ctrl Pts',(367.232159934826,-21.3883419398078,1.58316587795775));
#44558=CARTESIAN_POINT('Ctrl Pts',(367.187032279204,-21.3942035491294,1.47621763630986));
#44559=CARTESIAN_POINT('Ctrl Pts',(367.146748020166,-21.400065158451,1.36759560043083));
#44560=CARTESIAN_POINT('Ctrl Pts',(367.106436597157,-21.4059307202986,1.25890031991917));
#44561=CARTESIAN_POINT('Ctrl Pts',(367.070975200002,-21.4117962821462,1.14852939014845));
#44562=CARTESIAN_POINT('Ctrl Pts',(367.040479191642,-21.4176618439938,1.03695574152691));
#44563=CARTESIAN_POINT('Ctrl Pts',(367.009938590641,-21.4235359827309,0.925218944877583));
#44564=CARTESIAN_POINT('Ctrl Pts',(366.984377959642,-21.4294101214679,0.812276320919939));
#44565=CARTESIAN_POINT('Ctrl Pts',(366.963861377235,-21.4352842602049,0.698609810606347));
#44566=CARTESIAN_POINT('Ctrl Pts',(366.958673069781,-21.4367697336229,0.669865412977412));
#44567=CARTESIAN_POINT('Ctrl Pts',(366.953807070168,-21.4382552070409,0.641074739808697));
#44568=CARTESIAN_POINT('Ctrl Pts',(366.949263887404,-21.4397406804589,0.612245606489808));
#44569=CARTESIAN_POINT('Ctrl Pts',(366.919679988603,-21.4494136558938,0.424518586249826));
#44570=CARTESIAN_POINT('Ctrl Pts',(366.903697510534,-21.4590866313286,0.234593952454445));
#44571=CARTESIAN_POINT('Ctrl Pts',(366.901564247857,-21.4687596067635,0.0440236239979143));
#44572=CARTESIAN_POINT('Ctrl Pts',(366.901411571228,-21.469451897164,0.0303845932875485));
#44573=CARTESIAN_POINT('Ctrl Pts',(366.901329818244,-21.4701441875646,0.0167422730070523));
#44574=CARTESIAN_POINT('Ctrl Pts',(366.901319072765,-21.4708364779651,0.00309724153850734));
#44575=CARTESIAN_POINT('',(366.901317979184,-22.7208364779192,0.000995388470130986));
#44576=CARTESIAN_POINT('Ctrl Pts',(366.901319072764,-21.4708364780021,0.00309724080919957));
#44577=CARTESIAN_POINT('Ctrl Pts',(366.901229367429,-21.4766158530609,-0.110814138701328));
#44578=CARTESIAN_POINT('Ctrl Pts',(366.906092658234,-21.4823952281197,-0.224907569796787));
#44579=CARTESIAN_POINT('Ctrl Pts',(366.91592978844,-21.4881746031785,-0.338709276167276));
#44580=CARTESIAN_POINT('Ctrl Pts',(366.925756862887,-21.4939480704164,-0.452394651602257));
#44581=CARTESIAN_POINT('Ctrl Pts',(366.94054763356,-21.4997215376542,-0.565788472930522));
#44582=CARTESIAN_POINT('Ctrl Pts',(366.960270897962,-21.5054950048921,-0.678416677585149));
#44583=CARTESIAN_POINT('Ctrl Pts',(366.979980182921,-21.5112643800155,-0.790965053693971));
#44584=CARTESIAN_POINT('Ctrl Pts',(367.004614938388,-21.517033755139,-0.902748473242205));
#44585=CARTESIAN_POINT('Ctrl Pts',(367.034092188521,-21.5228031302625,-1.01329852330451));
#44586=CARTESIAN_POINT('Ctrl Pts',(367.063558679286,-21.5285703995306,-1.12380822195673));
#44587=CARTESIAN_POINT('Ctrl Pts',(367.097864043444,-21.5343376687986,-1.23308503391867));
#44588=CARTESIAN_POINT('Ctrl Pts',(367.136874475267,-21.5401049380667,-1.34067202059475));
#44589=CARTESIAN_POINT('Ctrl Pts',(367.175880754778,-21.5458715934604,-1.44824755559515));
#44590=CARTESIAN_POINT('Ctrl Pts',(367.219590960946,-21.551638248854,-1.55413322193989));
#44591=CARTESIAN_POINT('Ctrl Pts',(367.267822107052,-21.5574049042477,-1.65788934870166));
#44592=CARTESIAN_POINT('Ctrl Pts',(367.316060590951,-21.563172436969,-1.76166126071782));
#44593=CARTESIAN_POINT('Ctrl Pts',(367.368821200754,-21.5689399696904,-1.86330260306287));
#44594=CARTESIAN_POINT('Ctrl Pts',(367.425874093819,-21.5747075024117,-1.96239652949444));
#44595=CARTESIAN_POINT('Ctrl Pts',(367.482984649202,-21.5804808642732,-2.0615906083499));
#44596=CARTESIAN_POINT('Ctrl Pts',(367.544395935419,-21.5862542261347,-2.15823176110984));
#44597=CARTESIAN_POINT('Ctrl Pts',(367.60983371631,-21.5920275879961,-2.25193051642203));
#44598=CARTESIAN_POINT('Ctrl Pts',(367.675306973377,-21.5978040798048,-2.34568006920018));
#44599=CARTESIAN_POINT('Ctrl Pts',(367.744810810353,-21.6035805716134,-2.43648371170479));
#44600=CARTESIAN_POINT('Ctrl Pts',(367.818030698075,-21.609357063422,-2.52398510250822));
#44601=CARTESIAN_POINT('Ctrl Pts',(367.891364596513,-21.6151425498083,-2.61162274176244));
#44602=CARTESIAN_POINT('Ctrl Pts',(367.968425810692,-21.6209280361947,-2.69594754916856));
#44603=CARTESIAN_POINT('Ctrl Pts',(368.048862868866,-21.626713522581,-2.7766399712806));
#44604=CARTESIAN_POINT('Ctrl Pts',(368.102359212646,-21.6305612810109,-2.83030615017597));
#44605=CARTESIAN_POINT('Ctrl Pts',(368.157348031264,-21.6344090394407,-2.88236645748791));
#44606=CARTESIAN_POINT('Ctrl Pts',(368.213718362491,-21.6382567978706,-2.93273717014811));
#44607=CARTESIAN_POINT('Ctrl Pts',(368.299768935969,-21.6441304873147,-3.00962919147517));
#44608=CARTESIAN_POINT('Ctrl Pts',(368.389349871925,-21.6500041767589,-3.08285880193323));
#44609=CARTESIAN_POINT('Ctrl Pts',(368.482116339173,-21.6558778662031,-3.15208455427479));
#44610=CARTESIAN_POINT('Ctrl Pts',(368.574763036186,-21.6617439721618,-3.22122092965851));
#44611=CARTESIAN_POINT('Ctrl Pts',(368.67058675735,-21.6676100781204,-3.28636348225071));
#44612=CARTESIAN_POINT('Ctrl Pts',(368.769207361484,-21.673476184079,-3.34720893535269));
#44613=CARTESIAN_POINT('Ctrl Pts',(368.867726979363,-21.6793362832191,-3.407992083478));
#44614=CARTESIAN_POINT('Ctrl Pts',(368.969037434012,-21.6851963823593,-3.4644866687855));
#44615=CARTESIAN_POINT('Ctrl Pts',(369.072727714875,-21.6910564814994,-3.51643131377137));
#44616=CARTESIAN_POINT('Ctrl Pts',(369.180158903211,-21.6971279995736,-3.57025000238972));
#44617=CARTESIAN_POINT('Ctrl Pts',(369.290144515212,-21.7031995176479,-3.61918397922799));
#44618=CARTESIAN_POINT('Ctrl Pts',(369.402196883889,-21.7092710357222,-3.6629931107211));
#44619=CARTESIAN_POINT('Ctrl Pts',(369.51022312268,-21.7151243993687,-3.70522814560526));
#44620=CARTESIAN_POINT('Ctrl Pts',(369.620169735998,-21.7209777630153,-3.74270011324703));
#44621=CARTESIAN_POINT('Ctrl Pts',(369.731577992946,-21.7268311266618,-3.77524221746824));
#44622=CARTESIAN_POINT('Ctrl Pts',(369.842969522302,-21.7326836114445,-3.8077794355969));
#44623=CARTESIAN_POINT('Ctrl Pts',(369.955821862452,-21.7385360962273,-3.8353881462999));
#44624=CARTESIAN_POINT('Ctrl Pts',(370.069660955866,-21.74438858101,-3.85795137726262));
#44625=CARTESIAN_POINT('Ctrl Pts',(370.183510486777,-21.750241602386,-3.88051667696689));
#44626=CARTESIAN_POINT('Ctrl Pts',(370.298346545519,-21.7560946237621,-3.8980354969932));
#44627=CARTESIAN_POINT('Ctrl Pts',(370.413685415421,-21.7619476451381,-3.91044209166534));
#44628=CARTESIAN_POINT('Ctrl Pts',(370.529062753043,-21.7678026186088,-3.92285282417418));
#44629=CARTESIAN_POINT('Ctrl Pts',(370.644942824728,-21.7736575920794,-3.93014789680097));
#44630=CARTESIAN_POINT('Ctrl Pts',(370.760838045376,-21.7795125655501,-3.9323135324944));
#44631=CARTESIAN_POINT('Ctrl Pts',(370.876864618334,-21.7853741748793,-3.93448162265705));
#44632=CARTESIAN_POINT('Ctrl Pts',(370.992905961218,-21.7912357842085,-3.93150866465491));
#44633=CARTESIAN_POINT('Ctrl Pts',(371.108475645362,-21.7970973935378,-3.92343299993893));
#44634=CARTESIAN_POINT('Ctrl Pts',(371.224123258974,-21.8029629553922,-3.91535188974429));
#44635=CARTESIAN_POINT('Ctrl Pts',(371.339298171105,-21.8088285172467,-3.90216126834873));
#44636=CARTESIAN_POINT('Ctrl Pts',(371.45352194879,-21.8146940791011,-3.88395098939656));
#44637=CARTESIAN_POINT('Ctrl Pts',(371.567912749618,-21.8205682178438,-3.86571408255577));
#44638=CARTESIAN_POINT('Ctrl Pts',(371.681349237169,-21.8264423565866,-3.84244295213261));
#44639=CARTESIAN_POINT('Ctrl Pts',(371.793365910351,-21.8323164953293,-3.81427789025932));
#44640=CARTESIAN_POINT('Ctrl Pts',(371.821693089267,-21.8338019686469,-3.8071554081841));
#44641=CARTESIAN_POINT('Ctrl Pts',(371.849929562381,-21.8352874419645,-3.79972020227114));
#44642=CARTESIAN_POINT('Ctrl Pts',(371.878067999437,-21.8367729152822,-3.7919750305456));
#44643=CARTESIAN_POINT('Ctrl Pts',(371.989329807703,-21.8426466049661,-3.76134995318875));
#44644=CARTESIAN_POINT('Ctrl Pts',(372.099427906212,-21.8485202946499,-3.72577285636308));
#44645=CARTESIAN_POINT('Ctrl Pts',(372.207888437869,-21.8543939843338,-3.68534840266124));
#44646=CARTESIAN_POINT('Ctrl Pts',(372.316208936825,-21.8602600905344,-3.64497614071385));
#44647=CARTESIAN_POINT('Ctrl Pts',(372.422895689887,-21.8661261967349,-3.59976911074903));
#44648=CARTESIAN_POINT('Ctrl Pts',(372.527487773092,-21.8719923029355,-3.54988233924066));
#44649=CARTESIAN_POINT('Ctrl Pts',(372.631972755362,-21.8778524023195,-3.50004665113853));
#44650=CARTESIAN_POINT('Ctrl Pts',(372.734366963505,-21.8837125017035,-3.44554092997041));
#44651=CARTESIAN_POINT('Ctrl Pts',(372.834227947198,-21.8895726010875,-3.38656885593958));
#44652=CARTESIAN_POINT('Ctrl Pts',(372.937691680256,-21.8956441190711,-3.32546920821231));
#44653=CARTESIAN_POINT('Ctrl Pts',(373.038435529005,-21.9017156370547,-3.25957500974351));
#44654=CARTESIAN_POINT('Ctrl Pts',(373.135993338471,-21.9077871550383,-3.18916587223289));
#44655=CARTESIAN_POINT('Ctrl Pts',(373.230045824359,-21.9136405189319,-3.12128658662391));
#44656=CARTESIAN_POINT('Ctrl Pts',(373.321136920447,-21.9194938828256,-3.04921149089762));
#44657=CARTESIAN_POINT('Ctrl Pts',(373.408877784197,-21.9253472467192,-2.97323563846321));
#44658=CARTESIAN_POINT('Ctrl Pts',(373.49660547395,-21.9311997317499,-2.89727119354882));
#44659=CARTESIAN_POINT('Ctrl Pts',(373.580983619329,-21.9370522167806,-2.81740742686313));
#44660=CARTESIAN_POINT('Ctrl Pts',(373.661656936468,-21.9429047018112,-2.73397928089499));
#44661=CARTESIAN_POINT('Ctrl Pts',(373.742337650259,-21.9487577234357,-2.6505434856929));
#44662=CARTESIAN_POINT('Ctrl Pts',(373.819312573345,-21.9546107450602,-2.56354295856598));
#44663=CARTESIAN_POINT('Ctrl Pts',(373.892264231691,-21.9604637666847,-2.47334852910365));
#44664=CARTESIAN_POINT('Ctrl Pts',(373.965240220813,-21.966318740404,-2.3831240180712));
#44665=CARTESIAN_POINT('Ctrl Pts',(374.034190017342,-21.9721737141233,-2.28970380759661));
#44666=CARTESIAN_POINT('Ctrl Pts',(374.098837719774,-21.9780286878426,-2.19349015062801));
#44667=CARTESIAN_POINT('Ctrl Pts',(374.16355869204,-21.9838902974196,-2.09716744788689));
#44668=CARTESIAN_POINT('Ctrl Pts',(374.223967607723,-21.9897519069966,-1.99804532259946));
#44669=CARTESIAN_POINT('Ctrl Pts',(374.279832987824,-21.9956135165736,-1.8965533098875));
#44670=CARTESIAN_POINT('Ctrl Pts',(374.335736038347,-22.0014790786755,-1.79499286038996));
#44671=CARTESIAN_POINT('Ctrl Pts',(374.387089270144,-22.0073446407775,-1.69105971091343));
#44672=CARTESIAN_POINT('Ctrl Pts',(374.43370882486,-22.0132102028795,-1.58520460297973));
#44673=CARTESIAN_POINT('Ctrl Pts',(374.480396548763,-22.0190843418675,-1.47919470899576));
#44674=CARTESIAN_POINT('Ctrl Pts',(374.522336632368,-22.0249584808554,-1.37125763137149));
#44675=CARTESIAN_POINT('Ctrl Pts',(374.559394611669,-22.0308326198434,-1.26186058805801));
#44676=CARTESIAN_POINT('Ctrl Pts',(374.568765951338,-22.0323180907935,-1.23419591580405));
#44677=CARTESIAN_POINT('Ctrl Pts',(374.577825335228,-22.0338035617437,-1.20643793408156));
#44678=CARTESIAN_POINT('Ctrl Pts',(374.586571107134,-22.0352890326939,-1.17859429767826));
#44679=CARTESIAN_POINT('Ctrl Pts',(374.621152692097,-22.0411627211946,-1.06849800333977));
#44680=CARTESIAN_POINT('Ctrl Pts',(374.650942200166,-22.0470364096953,-0.956695046797344));
#44681=CARTESIAN_POINT('Ctrl Pts',(374.675770697657,-22.052910098196,-0.843640352283101));
#44682=CARTESIAN_POINT('Ctrl Pts',(374.700567139219,-22.0587762032118,-0.730731622025469));
#44683=CARTESIAN_POINT('Ctrl Pts',(374.720415220098,-22.0646423082276,-0.616574767554941));
#44684=CARTESIAN_POINT('Ctrl Pts',(374.735195338943,-22.0705084132434,-0.501641148042162));
#44685=CARTESIAN_POINT('Ctrl Pts',(374.749960323135,-22.0763685114423,-0.386825219091741));
#44686=CARTESIAN_POINT('Ctrl Pts',(374.759667615314,-22.0822286096413,-0.271234514545874));
#44687=CARTESIAN_POINT('Ctrl Pts',(374.764248512977,-22.0880887078402,-0.155351245687263));
#44688=CARTESIAN_POINT('Ctrl Pts',(374.768994679957,-22.0941602262679,-0.0352871480472851));
#44689=CARTESIAN_POINT('Ctrl Pts',(374.768237472187,-22.1002317446957,0.0850905815487117));
#44690=CARTESIAN_POINT('Ctrl Pts',(374.761959142466,-22.1063032631234,0.205238648986715));
#44691=CARTESIAN_POINT('Ctrl Pts',(374.755906399394,-22.1121566258388,0.321069676536308));
#44692=CARTESIAN_POINT('Ctrl Pts',(374.744722488423,-22.1180099885542,0.436686813924215));
#44693=CARTESIAN_POINT('Ctrl Pts',(374.728444549976,-22.1238633512696,0.551603362611651));
#44694=CARTESIAN_POINT('Ctrl Pts',(374.712169055594,-22.1297158351265,0.666502657048842));
#44695=CARTESIAN_POINT('Ctrl Pts',(374.690801112468,-22.1355683189834,0.780701162992073));
#44696=CARTESIAN_POINT('Ctrl Pts',(374.664429572601,-22.1414208028403,0.893718757266345));
#44697=CARTESIAN_POINT('Ctrl Pts',(374.638055614794,-22.1472738232967,1.00674671383995));
#44698=CARTESIAN_POINT('Ctrl Pts',(374.606677242145,-22.1531268437532,1.11859314114516));
#44699=CARTESIAN_POINT('Ctrl Pts',(374.570433959941,-22.1589798642096,1.22879023316963));
#44700=CARTESIAN_POINT('Ctrl Pts',(374.534178589861,-22.164834836768,1.33902407817497));
#44701=CARTESIAN_POINT('Ctrl Pts',(374.493055212875,-22.1706898093263,1.44760710182469));
#44702=CARTESIAN_POINT('Ctrl Pts',(374.447252276424,-22.1765447818846,1.55408939693147));
#44703=CARTESIAN_POINT('Ctrl Pts',(374.401397428115,-22.1824063903167,1.66069237630617));
#44704=CARTESIAN_POINT('Ctrl Pts',(374.350852597835,-22.1882679987489,1.76518949524678));
#44705=CARTESIAN_POINT('Ctrl Pts',(374.295853240312,-22.1941296071811,1.86715338522054));
#44706=CARTESIAN_POINT('Ctrl Pts',(374.240816796248,-22.1999951681463,1.96918603032332));
#44707=CARTESIAN_POINT('Ctrl Pts',(374.181320055366,-22.2058607291115,2.06868169139114));
#44708=CARTESIAN_POINT('Ctrl Pts',(374.117642107897,-22.2117262900767,2.16524151970987));
#44709=CARTESIAN_POINT('Ctrl Pts',(374.053871047459,-22.2176004279483,2.26194254247199));
#44710=CARTESIAN_POINT('Ctrl Pts',(373.985906820052,-22.22347456582,2.35569883168704));
#44711=CARTESIAN_POINT('Ctrl Pts',(373.914069138321,-22.2293487036916,2.44614411307786));
#44712=CARTESIAN_POINT('Ctrl Pts',(373.895902456609,-22.2308341858296,2.46901638010719));
#44713=CARTESIAN_POINT('Ctrl Pts',(373.877488248296,-22.2323196679675,2.49167708902266));
#44714=CARTESIAN_POINT('Ctrl Pts',(373.858832048042,-22.2338051501055,2.51412069824459));
#44715=CARTESIAN_POINT('Ctrl Pts',(373.785064254748,-22.2396788402356,2.60286414564367));
#44716=CARTESIAN_POINT('Ctrl Pts',(373.707264507631,-22.2455525303657,2.688505969082));
#44717=CARTESIAN_POINT('Ctrl Pts',(373.625723502741,-22.2514262204958,2.77065759339582));
#44718=CARTESIAN_POINT('Ctrl Pts',(373.544287775022,-22.257292327135,2.85270315217211));
#44719=CARTESIAN_POINT('Ctrl Pts',(373.459120683839,-22.2631584337742,2.93126718258746));
#44720=CARTESIAN_POINT('Ctrl Pts',(373.37055347917,-22.2690245404133,3.00599365429825));
#44721=CARTESIAN_POINT('Ctrl Pts',(373.282076966284,-22.2748846402278,3.08064360697555));
#44722=CARTESIAN_POINT('Ctrl Pts',(373.190207579146,-22.2807447400424,3.15146355244152));
#44723=CARTESIAN_POINT('Ctrl Pts',(373.095313279593,-22.2866048398569,3.218134348025));
#44724=CARTESIAN_POINT('Ctrl Pts',(372.996995426842,-22.2926763576761,3.28721046212124));
#44725=CARTESIAN_POINT('Ctrl Pts',(372.895430596163,-22.2987478754953,3.35183207104542));
#44726=CARTESIAN_POINT('Ctrl Pts',(372.791065700638,-22.3048193933144,3.41168973701297));
#44727=CARTESIAN_POINT('Ctrl Pts',(372.690450702543,-22.3106727576161,3.46939667876823));
#44728=CARTESIAN_POINT('Ctrl Pts',(372.587233782069,-22.3165261219178,3.52267590579358));
#44729=CARTESIAN_POINT('Ctrl Pts',(372.481844050169,-22.3223794862195,3.57129478346174));
#44730=CARTESIAN_POINT('Ctrl Pts',(372.376470142345,-22.3282319716492,3.61990636109416));
#44731=CARTESIAN_POINT('Ctrl Pts',(372.268924446838,-22.334084457079,3.66385880770208));
#44732=CARTESIAN_POINT('Ctrl Pts',(372.159658582617,-22.3399369425087,3.70296650687138));
#44733=CARTESIAN_POINT('Ctrl Pts',(372.050382700368,-22.3457899645229,3.74207779162542));
#44734=CARTESIAN_POINT('Ctrl Pts',(371.939386724887,-22.351642986537,3.77634330670344));
#44735=CARTESIAN_POINT('Ctrl Pts',(371.827139384565,-22.3574960085512,3.80562667729063));
#44736=CARTESIAN_POINT('Ctrl Pts',(371.714854607794,-22.3633509826504,3.83491981439346));
#44737=CARTESIAN_POINT('Ctrl Pts',(371.601318035845,-22.3692059567497,3.85922739868854));
#44738=CARTESIAN_POINT('Ctrl Pts',(371.487009888607,-22.3750609308489,3.87846388496112));
#44739=CARTESIAN_POINT('Ctrl Pts',(371.372572188149,-22.3809225407896,3.89772217325554));
#44740=CARTESIAN_POINT('Ctrl Pts',(371.257361574639,-22.3867841507303,3.91189782341989));
#44741=CARTESIAN_POINT('Ctrl Pts',(371.141864811662,-22.3926457606711,3.92095700924605));
#44742=CARTESIAN_POINT('Ctrl Pts',(371.026290168578,-22.3985113231277,3.93002230373129));
#44743=CARTESIAN_POINT('Ctrl Pts',(370.910429403701,-22.4043768855844,3.93396425002952));
#44744=CARTESIAN_POINT('Ctrl Pts',(370.794768970429,-22.4102424480411,3.93280115005445));
#44745=CARTESIAN_POINT('Ctrl Pts',(370.678939413645,-22.4161165873679,3.93163634934608));
#44746=CARTESIAN_POINT('Ctrl Pts',(370.563311184037,-22.4219907266948,3.9253516268132));
#44747=CARTESIAN_POINT('Ctrl Pts',(370.448365384261,-22.4278648660216,3.91401707861642));
#44748=CARTESIAN_POINT('Ctrl Pts',(370.419297600566,-22.4293503331868,3.91115076948723));
#44749=CARTESIAN_POINT('Ctrl Pts',(370.390273403415,-22.430835800352,3.90796178063459));
#44750=CARTESIAN_POINT('Ctrl Pts',(370.361300449601,-22.4323212675171,3.90445175868131));
#44751=CARTESIAN_POINT('Ctrl Pts',(370.24673837912,-22.4381949590698,3.89057276708868));
#44752=CARTESIAN_POINT('Ctrl Pts',(370.132596868298,-22.4440686506226,3.87162427043359));
#44753=CARTESIAN_POINT('Ctrl Pts',(370.019360029201,-22.4499423421753,3.84763989285173));
#44754=CARTESIAN_POINT('Ctrl Pts',(369.90626938917,-22.4558084502576,3.82368648128416));
#44755=CARTESIAN_POINT('Ctrl Pts',(369.794081498555,-22.4616745583399,3.79471020352575));
#44756=CARTESIAN_POINT('Ctrl Pts',(369.683275106397,-22.4675406664223,3.76079640435063));
#44757=CARTESIAN_POINT('Ctrl Pts',(369.572582178309,-22.4734007676986,3.72691733239324));
#44758=CARTESIAN_POINT('Ctrl Pts',(369.463268327563,-22.4792608689749,3.68811091591094));
#44759=CARTESIAN_POINT('Ctrl Pts',(369.355801208018,-22.4851209702513,3.64451334609282));
#44760=CARTESIAN_POINT('Ctrl Pts',(369.244456976512,-22.4911924875295,3.59934289835524));
#44761=CARTESIAN_POINT('Ctrl Pts',(369.135095683615,-22.4972640048077,3.5490291612149));
#44762=CARTESIAN_POINT('Ctrl Pts',(369.028219627798,-22.503335522086,3.49377993012068));
#44763=CARTESIAN_POINT('Ctrl Pts',(368.925183661447,-22.5091888878862,3.4405158208454));
#44764=CARTESIAN_POINT('Ctrl Pts',(368.824457813454,-22.5150422536864,3.38266498754485));
#44765=CARTESIAN_POINT('Ctrl Pts',(368.726470193779,-22.5208956194866,3.32046190229214));
#44766=CARTESIAN_POINT('Ctrl Pts',(368.62849728658,-22.5267481064257,3.25826815660054));
#44767=CARTESIAN_POINT('Ctrl Pts',(368.533262138914,-22.5326005933649,3.19172367967013));
#44768=CARTESIAN_POINT('Ctrl Pts',(368.441165552764,-22.5384530803041,3.12110734624765));
#44769=CARTESIAN_POINT('Ctrl Pts',(368.349060522606,-22.5443061038369,3.05048453826534));
#44770=CARTESIAN_POINT('Ctrl Pts',(368.260094953887,-22.5501591273698,2.97578938304197));
#44771=CARTESIAN_POINT('Ctrl Pts',(368.17463754566,-22.5560121509026,2.89734182684032));
#44772=CARTESIAN_POINT('Ctrl Pts',(368.089151635793,-22.561867126528,2.81886810691423));
#44773=CARTESIAN_POINT('Ctrl Pts',(368.007176517172,-22.5677221021535,2.73663977670339));
#44774=CARTESIAN_POINT('Ctrl Pts',(367.929044405982,-22.5735770777789,2.65101399406912));
#44775=CARTESIAN_POINT('Ctrl Pts',(367.850823742321,-22.5794386892492,2.56529116587223));
#44776=CARTESIAN_POINT('Ctrl Pts',(367.776455058126,-22.5853003007194,2.47616350511215));
#44777=CARTESIAN_POINT('Ctrl Pts',(367.706230657093,-22.5911619121896,2.38402170573178));
#44778=CARTESIAN_POINT('Ctrl Pts',(367.635958903325,-22.5970274761796,2.29181777458389));
#44779=CARTESIAN_POINT('Ctrl Pts',(367.56983723228,-22.6028930401696,2.19659599626579));
#44780=CARTESIAN_POINT('Ctrl Pts',(367.508113975826,-22.6087586041595,2.09877506321652));
#44781=CARTESIAN_POINT('Ctrl Pts',(367.446300465141,-22.6146327450132,2.00081109246209));
#44782=CARTESIAN_POINT('Ctrl Pts',(367.388898408793,-22.620506885867,1.90024073939001));
#44783=CARTESIAN_POINT('Ctrl Pts',(367.336109714849,-22.6263810267207,1.79750627832298));
#44784=CARTESIAN_POINT('Ctrl Pts',(367.322760509952,-22.6278664794567,1.77152678786151));
#44785=CARTESIAN_POINT('Ctrl Pts',(367.309706078323,-22.6293519321928,1.74540899848703));
#44786=CARTESIAN_POINT('Ctrl Pts',(367.296949187031,-22.6308373849288,1.7191602366962));
#44787=CARTESIAN_POINT('Ctrl Pts',(367.242672211498,-22.6371575674847,1.6074791563363));
#44788=CARTESIAN_POINT('Ctrl Pts',(367.19362551988,-22.6434777500406,1.4930970559787));
#44789=CARTESIAN_POINT('Ctrl Pts',(367.150065578657,-22.6497979325966,1.37650796486861));
#44790=CARTESIAN_POINT('Ctrl Pts',(367.106647535126,-22.6560975269861,1.26029866589119));
#44791=CARTESIAN_POINT('Ctrl Pts',(367.068680713728,-22.6623971213756,1.14189700515019));
#44792=CARTESIAN_POINT('Ctrl Pts',(367.036373913979,-22.6686967157651,1.0218174173262));
#44793=CARTESIAN_POINT('Ctrl Pts',(367.004131677013,-22.6749837208745,0.901977799802725));
#44794=CARTESIAN_POINT('Ctrl Pts',(366.977527006976,-22.681270725984,0.780467237829525));
#44795=CARTESIAN_POINT('Ctrl Pts',(366.956720096784,-22.6875577310934,0.657818089785108));
#44796=CARTESIAN_POINT('Ctrl Pts',(366.935976328002,-22.6938256574271,0.535541137333476));
#44797=CARTESIAN_POINT('Ctrl Pts',(366.920995294742,-22.7000935837608,0.412132796286274));
#44798=CARTESIAN_POINT('Ctrl Pts',(366.911886720925,-22.7063615100944,0.288137141606198));
#44799=CARTESIAN_POINT('Ctrl Pts',(366.904875028599,-22.7111864993694,0.1926864818321));
#44800=CARTESIAN_POINT('Ctrl Pts',(366.901342248334,-22.7160114886443,0.0968881668734049));
#44801=CARTESIAN_POINT('Ctrl Pts',(366.901317979184,-22.7208364779192,0.000995388470100028));
#44802=CARTESIAN_POINT('',(366.901319515466,-23.9708364779953,-0.00361596385032392));
#44803=CARTESIAN_POINT('Ctrl Pts',(366.901317979183,-22.7208364779651,0.00099538755728252));
#44804=CARTESIAN_POINT('Ctrl Pts',(366.901287676336,-22.7268610418477,-0.118737970686335));
#44805=CARTESIAN_POINT('Ctrl Pts',(366.906729329308,-22.7328856057302,-0.238412572221518));
#44806=CARTESIAN_POINT('Ctrl Pts',(366.91760070142,-22.7389101696128,-0.357513290336023));
#44807=CARTESIAN_POINT('Ctrl Pts',(366.928480551288,-22.7449394315943,-0.476706886035791));
#44808=CARTESIAN_POINT('Ctrl Pts',(366.944798523797,-22.7509686935757,-0.595325330626995));
#44809=CARTESIAN_POINT('Ctrl Pts',(366.966460780102,-22.7569979555571,-0.712860899403337));
#44810=CARTESIAN_POINT('Ctrl Pts',(366.988162752378,-22.763038271696,-0.830611960007766));
#44811=CARTESIAN_POINT('Ctrl Pts',(367.015228520396,-22.7690785878349,-0.947275804961401));
#44812=CARTESIAN_POINT('Ctrl Pts',(367.047513327082,-22.7751189039738,-1.06235609886111));
#44813=CARTESIAN_POINT('Ctrl Pts',(367.079828053996,-22.781164818029,-1.17754304443784));
#44814=CARTESIAN_POINT('Ctrl Pts',(367.117371345748,-22.7872107320841,-1.29114315418572));
#44815=CARTESIAN_POINT('Ctrl Pts',(367.159949518888,-22.7932566461392,-1.40267827516699));
#44816=CARTESIAN_POINT('Ctrl Pts',(367.202620316752,-22.7993157124995,-1.51445603008713));
#44817=CARTESIAN_POINT('Ctrl Pts',(367.250347743227,-22.8053747788597,-1.6241594678244));
#44818=CARTESIAN_POINT('Ctrl Pts',(367.302890635125,-22.81143384522,-1.73133208924998));
#44819=CARTESIAN_POINT('Ctrl Pts',(367.354689077928,-22.8174070642601,-1.83698624532299));
#44820=CARTESIAN_POINT('Ctrl Pts',(367.41116717659,-22.8233802833003,-1.94018057508564));
#44821=CARTESIAN_POINT('Ctrl Pts',(367.472052951154,-22.8293535023405,-2.04050575306956));
#44822=CARTESIAN_POINT('Ctrl Pts',(367.531924296908,-22.8352272005068,-2.13915939526883));
#44823=CARTESIAN_POINT('Ctrl Pts',(367.596240994351,-22.8411008986732,-2.23534004410958));
#44824=CARTESIAN_POINT('Ctrl Pts',(367.664772841031,-22.8469745968396,-2.32862049627674));
#44825=CARTESIAN_POINT('Ctrl Pts',(367.733216206224,-22.8528407114727,-2.42178051402745));
#44826=CARTESIAN_POINT('Ctrl Pts',(367.805863655565,-22.8587068261058,-2.51204745167245));
#44827=CARTESIAN_POINT('Ctrl Pts',(367.88244007591,-22.8645729407389,-2.59902031307939));
#44828=CARTESIAN_POINT('Ctrl Pts',(367.958938082337,-22.8704330484964,-2.685904114658));
#44829=CARTESIAN_POINT('Ctrl Pts',(368.0393567858,-22.8762931562539,-2.76950024117513));
#44830=CARTESIAN_POINT('Ctrl Pts',(368.12337932194,-22.8821532640113,-2.84943876572168));
#44831=CARTESIAN_POINT('Ctrl Pts',(368.210433023802,-22.8882247788339,-2.93226112270937));
#44832=CARTESIAN_POINT('Ctrl Pts',(368.301355221014,-22.8942962936564,-3.01115663087208));
#44833=CARTESIAN_POINT('Ctrl Pts',(368.39574953221,-22.9003678084789,-3.08575331868064));
#44834=CARTESIAN_POINT('Ctrl Pts',(368.486752361127,-22.9062211805483,-3.15766983072856));
#44835=CARTESIAN_POINT('Ctrl Pts',(368.580981747322,-22.9120745526176,-3.22559083205616));
#44836=CARTESIAN_POINT('Ctrl Pts',(368.678047586308,-22.917927924687,-3.28922293802281));
#44837=CARTESIAN_POINT('Ctrl Pts',(368.775098849769,-22.9237804178067,-3.35284548891371));
#44838=CARTESIAN_POINT('Ctrl Pts',(368.874985373697,-22.9296329109265,-3.41218019856358));
#44839=CARTESIAN_POINT('Ctrl Pts',(368.977287856577,-22.9354854040462,-3.46697686631361));
#44840=CARTESIAN_POINT('Ctrl Pts',(369.079599717541,-22.9413384336649,-3.52177855728224));
#44841=CARTESIAN_POINT('Ctrl Pts',(369.184327613512,-22.9471914632835,-3.57204118429289));
#44842=CARTESIAN_POINT('Ctrl Pts',(369.291028057516,-22.9530444929022,-3.61756072602311));
#44843=CARTESIAN_POINT('Ctrl Pts',(369.397764086232,-22.9588994745124,-3.6630954485688));
#44844=CARTESIAN_POINT('Ctrl Pts',(369.506473591278,-22.9647544561226,-3.70388377841954));
#44845=CARTESIAN_POINT('Ctrl Pts',(369.616694222458,-22.9706094377329,-3.73977027286435));
#44846=CARTESIAN_POINT('Ctrl Pts',(369.727039770731,-22.976471055009,-3.77569743879262));
#44847=CARTESIAN_POINT('Ctrl Pts',(369.838899470347,-22.9823326722852,-3.80671155303308));
#44848=CARTESIAN_POINT('Ctrl Pts',(369.951796870379,-22.9881942895613,-3.8327073609706));
#44849=CARTESIAN_POINT('Ctrl Pts',(370.064770395858,-22.9940598592601,-3.85872069758919));
#44850=CARTESIAN_POINT('Ctrl Pts',(370.178782609719,-22.9999254289589,-3.87970891541977));
#44851=CARTESIAN_POINT('Ctrl Pts',(370.293349678834,-23.0057909986577,-3.8956183635332));
#44852=CARTESIAN_POINT('Ctrl Pts',(370.408084268749,-23.011665145035,-3.91155107455712));
#44853=CARTESIAN_POINT('Ctrl Pts',(370.523374923347,-23.0175392914124,-3.92239015648457));
#44854=CARTESIAN_POINT('Ctrl Pts',(370.638735461975,-23.0234134377898,-3.92813397534163));
#44855=CARTESIAN_POINT('Ctrl Pts',(370.667906653746,-23.0248988317772,-3.92958641344023));
#44856=CARTESIAN_POINT('Ctrl Pts',(370.697082330539,-23.0263842257647,-3.93071330423601));
#44857=CARTESIAN_POINT('Ctrl Pts',(370.726254677598,-23.0278696197521,-3.93151514687068));
#44858=CARTESIAN_POINT('Ctrl Pts',(370.84161110108,-23.0337433239663,-3.93468587901459));
#44859=CARTESIAN_POINT('Ctrl Pts',(370.957299310999,-23.0396170281805,-3.93278049909092));
#44860=CARTESIAN_POINT('Ctrl Pts',(371.072835528839,-23.0454907323946,-3.92576085853677));
#44861=CARTESIAN_POINT('Ctrl Pts',(371.188222581599,-23.051356853259,-3.91875028081384));
#44862=CARTESIAN_POINT('Ctrl Pts',(371.303457623906,-23.0572229741233,-3.90663859820559));
#44863=CARTESIAN_POINT('Ctrl Pts',(371.418054553035,-23.0630890949877,-3.88943960813041));
#44864=CARTESIAN_POINT('Ctrl Pts',(371.532534138928,-23.06894920915,-3.87225822921777));
#44865=CARTESIAN_POINT('Ctrl Pts',(371.646376505183,-23.0748093233124,-3.8499999653729));
#44866=CARTESIAN_POINT('Ctrl Pts',(371.759099023238,-23.0806694374747,-3.822730540803));
#44867=CARTESIAN_POINT('Ctrl Pts',(371.875887904304,-23.0867409499617,-3.79447739637549));
#44868=CARTESIAN_POINT('Ctrl Pts',(371.991474166008,-23.0928124624488,-3.76084474692569));
#44869=CARTESIAN_POINT('Ctrl Pts',(372.105330357215,-23.0988839749358,-3.72196402651858));
#44870=CARTESIAN_POINT('Ctrl Pts',(372.215095992104,-23.1047373537975,-3.68448018909865));
#44871=CARTESIAN_POINT('Ctrl Pts',(372.32325330665,-23.1105907326592,-3.64211903554325));
#44872=CARTESIAN_POINT('Ctrl Pts',(372.429344287467,-23.1164441115208,-3.59504932846093));
#44873=CARTESIAN_POINT('Ctrl Pts',(372.535419339916,-23.1222966115635,-3.54798668836569));
#44874=CARTESIAN_POINT('Ctrl Pts',(372.639428297962,-23.1281491116062,-3.49621706790352));
#44875=CARTESIAN_POINT('Ctrl Pts',(372.740933608191,-23.1340016116488,-3.4399571745752));
#44876=CARTESIAN_POINT('Ctrl Pts',(372.84244822554,-23.1398546483129,-3.38369212272267));
#44877=CARTESIAN_POINT('Ctrl Pts',(372.941458377355,-23.145707684977,-3.32293617983975));
#44878=CARTESIAN_POINT('Ctrl Pts',(373.037552204011,-23.151560721641,-3.25795141085801));
#44879=CARTESIAN_POINT('Ctrl Pts',(373.133678079901,-23.1574157104112,-3.19294496814228));
#44880=CARTESIAN_POINT('Ctrl Pts',(373.226885354509,-23.1632706991813,-3.12370712612603));
#44881=CARTESIAN_POINT('Ctrl Pts',(373.316792763345,-23.1691256879514,-3.05054213552566));
#44882=CARTESIAN_POINT('Ctrl Pts',(373.406802069448,-23.1749873125189,-2.97729422281013));
#44883=CARTESIAN_POINT('Ctrl Pts',(373.493503724484,-23.1808489370864,-2.90011053877019));
#44884=CARTESIAN_POINT('Ctrl Pts',(373.576550993332,-23.1867105616539,-2.81933439047121));
#44885=CARTESIAN_POINT('Ctrl Pts',(373.659654261159,-23.1925761387294,-2.73850377461465));
#44886=CARTESIAN_POINT('Ctrl Pts',(373.739097953685,-23.1984417158049,-2.65407617108448));
#44887=CARTESIAN_POINT('Ctrl Pts',(373.814574696856,-23.2043072928804,-2.56642906505969));
#44888=CARTESIAN_POINT('Ctrl Pts',(373.890161803387,-23.2101814467011,-2.47865379996664));
#44889=CARTESIAN_POINT('Ctrl Pts',(373.961770129644,-23.2160556005217,-2.38764996060215));
#44890=CARTESIAN_POINT('Ctrl Pts',(374.029134739244,-23.2219297543424,-2.29382520362811));
#44891=CARTESIAN_POINT('Ctrl Pts',(374.046168429106,-23.2234150819495,-2.27010085012677));
#44892=CARTESIAN_POINT('Ctrl Pts',(374.062931014547,-23.2249004095566,-2.24619626191627));
#44893=CARTESIAN_POINT('Ctrl Pts',(374.079418679064,-23.2263857371637,-2.2221182754591));
#44894=CARTESIAN_POINT('Ctrl Pts',(374.144617931055,-23.2322593555188,-2.12690365578005));
#44895=CARTESIAN_POINT('Ctrl Pts',(374.205731692429,-23.2381329738739,-2.02865848239646));
#44896=CARTESIAN_POINT('Ctrl Pts',(374.262465646344,-23.244006592229,-1.92776858272025));
#44897=CARTESIAN_POINT('Ctrl Pts',(374.31912634959,-23.2498726270041,-1.82700894459285));
#44898=CARTESIAN_POINT('Ctrl Pts',(374.371418290418,-23.2557386617792,-1.72361172766874));
#44899=CARTESIAN_POINT('Ctrl Pts',(374.419089542026,-23.2616046965543,-1.61799287364358));
#44900=CARTESIAN_POINT('Ctrl Pts',(374.466711978198,-23.2674647245005,-1.51248217349212));
#44901=CARTESIAN_POINT('Ctrl Pts',(374.509722967717,-23.2733247524468,-1.40475473565745));
#44902=CARTESIAN_POINT('Ctrl Pts',(374.547916101235,-23.279184780393,-1.29525173320391));
#44903=CARTESIAN_POINT('Ctrl Pts',(374.587487810059,-23.2852563251506,-1.18179623664475));
#44904=CARTESIAN_POINT('Ctrl Pts',(374.621887072299,-23.2913278699082,-1.06643497056012));
#44905=CARTESIAN_POINT('Ctrl Pts',(374.650938386052,-23.2973994146658,-0.949682425023584));
#44906=CARTESIAN_POINT('Ctrl Pts',(374.678945401484,-23.3032527075383,-0.837126746045857));
#44907=CARTESIAN_POINT('Ctrl Pts',(374.701982222204,-23.3091060004108,-0.723278524510714));
#44908=CARTESIAN_POINT('Ctrl Pts',(374.719942367608,-23.3149592932833,-0.608614108627111));
#44909=CARTESIAN_POINT('Ctrl Pts',(374.737899817165,-23.3208117075672,-0.49396690405588));
#44910=CARTESIAN_POINT('Ctrl Pts',(374.750782042665,-23.3266641218511,-0.378504156805758));
#44911=CARTESIAN_POINT('Ctrl Pts',(374.758533943495,-23.3325165361349,-0.26271101396801));
#44912=CARTESIAN_POINT('Ctrl Pts',(374.76628655554,-23.3383694873619,-0.146907247424043));
#44913=CARTESIAN_POINT('Ctrl Pts',(374.768907879622,-23.3442224385889,-0.0307734372891979));
#44914=CARTESIAN_POINT('Ctrl Pts',(374.766394858187,-23.3500753898159,0.0852022713527328));
#44915=CARTESIAN_POINT('Ctrl Pts',(374.763880998418,-23.3559302935623,0.20121666899282));
#44916=CARTESIAN_POINT('Ctrl Pts',(374.756229396263,-23.3617851973086,0.317072447428953));
#44917=CARTESIAN_POINT('Ctrl Pts',(374.743489029117,-23.367640101055,0.432284301783718));
#44918=CARTESIAN_POINT('Ctrl Pts',(374.730734220103,-23.3735016416387,0.547626754755979));
#44919=CARTESIAN_POINT('Ctrl Pts',(374.712879178201,-23.3793631822224,0.662323415885602));
#44920=CARTESIAN_POINT('Ctrl Pts',(374.690024418826,-23.3852247228061,0.775896823020315));
#44921=CARTESIAN_POINT('Ctrl Pts',(374.667154246245,-23.3910902164017,0.889546823848221));
#44922=CARTESIAN_POINT('Ctrl Pts',(374.6392777413,-23.3969557099974,1.00207166225154));
#44923=CARTESIAN_POINT('Ctrl Pts',(374.606545477403,-23.4028212035931,1.11300842376944));
#44924=CARTESIAN_POINT('Ctrl Pts',(374.573765343465,-23.4086952753128,1.22410742726817));
#44925=CARTESIAN_POINT('Ctrl Pts',(374.536115411754,-23.4145693470325,1.33361332951313));
#44926=CARTESIAN_POINT('Ctrl Pts',(374.493794614669,-23.4204434187523,1.44108252103892));
#44927=CARTESIAN_POINT('Ctrl Pts',(374.483087416051,-23.4219295640267,1.46827232033845));
#44928=CARTESIAN_POINT('Ctrl Pts',(374.472081468001,-23.4234157093011,1.49533187305735));
#44929=CARTESIAN_POINT('Ctrl Pts',(374.46078045256,-23.4249018545755,1.52225425458903));
#44930=CARTESIAN_POINT('Ctrl Pts',(374.416114739073,-23.4307756399335,1.62866127493066));
#44931=CARTESIAN_POINT('Ctrl Pts',(374.36668741188,-23.4366494252915,1.73327796734298));
#44932=CARTESIAN_POINT('Ctrl Pts',(374.31266315186,-23.4425232106496,1.83564783753799));
#44933=CARTESIAN_POINT('Ctrl Pts',(374.258708644464,-23.4483894121566,1.93788553439055));
#44934=CARTESIAN_POINT('Ctrl Pts',(374.200169198598,-23.4542556136636,2.0378818160345));
#44935=CARTESIAN_POINT('Ctrl Pts',(374.137257779935,-23.4601218151706,2.13519948495123));
#44936=CARTESIAN_POINT('Ctrl Pts',(374.074410785778,-23.4659820093878,2.23241749560526));
#44937=CARTESIAN_POINT('Ctrl Pts',(374.007200947151,-23.4718422036049,2.32696200477624));
#44938=CARTESIAN_POINT('Ctrl Pts',(373.935887106773,-23.477702397822,2.41842038641772));
#44939=CARTESIAN_POINT('Ctrl Pts',(373.862002061246,-23.4837738800789,2.51317628030224));
#44940=CARTESIAN_POINT('Ctrl Pts',(373.783711702946,-23.4898453623357,2.60461890883726));
#44941=CARTESIAN_POINT('Ctrl Pts',(373.701353200303,-23.4959168445926,2.6923219195701));
#44942=CARTESIAN_POINT('Ctrl Pts',(373.621952169263,-23.5017703015603,2.77687553885777));
#44943=CARTESIAN_POINT('Ctrl Pts',(373.538770447679,-23.507623758528,2.85795317135498));
#44944=CARTESIAN_POINT('Ctrl Pts',(373.452150606204,-23.5134772154956,2.93520709276592));
#44945=CARTESIAN_POINT('Ctrl Pts',(373.365543782114,-23.5193297927954,3.01244940431997));
#44946=CARTESIAN_POINT('Ctrl Pts',(373.27550017374,-23.5251823700951,3.08586887246897));
#44947=CARTESIAN_POINT('Ctrl Pts',(373.182397599193,-23.5310349473949,3.15515617784124));
#44948=CARTESIAN_POINT('Ctrl Pts',(373.089286502858,-23.5368880603879,3.22444982516199));
#44949=CARTESIAN_POINT('Ctrl Pts',(372.993116215198,-23.5427411733809,3.28961031117638));
#44950=CARTESIAN_POINT('Ctrl Pts',(372.894295286998,-23.5485942863739,3.35037042315363));
#44951=CARTESIAN_POINT('Ctrl Pts',(372.79544141747,-23.5544493504649,3.41115078912777));
#44952=CARTESIAN_POINT('Ctrl Pts',(372.693935502195,-23.5603044145559,3.46752764805658));
#44953=CARTESIAN_POINT('Ctrl Pts',(372.59021191469,-23.5661594786469,3.51927905186658));
#44954=CARTESIAN_POINT('Ctrl Pts',(372.486370805763,-23.5720211766722,3.57108909131369));
#44955=CARTESIAN_POINT('Ctrl Pts',(372.380307379329,-23.5778828746975,3.61826303085876));
#44956=CARTESIAN_POINT('Ctrl Pts',(372.272477358661,-23.5837445727229,3.66062648148104));
#44957=CARTESIAN_POINT('Ctrl Pts',(372.164574647179,-23.58961022226,3.70301849032574));
#44958=CARTESIAN_POINT('Ctrl Pts',(372.054903359969,-23.5954758717971,3.74059341940055));
#44959=CARTESIAN_POINT('Ctrl Pts',(371.94393413421,-23.6013415213343,3.77322682978001));
#44960=CARTESIAN_POINT('Ctrl Pts',(371.832802687362,-23.6072157456095,3.80590794552373));
#44961=CARTESIAN_POINT('Ctrl Pts',(371.720369914805,-23.6130899698848,3.83363302716284));
#44962=CARTESIAN_POINT('Ctrl Pts',(371.60711644896,-23.61896419416,3.85632873733921));
#44963=CARTESIAN_POINT('Ctrl Pts',(371.578493902312,-23.6204487867691,3.86206462381642));
#44964=CARTESIAN_POINT('Ctrl Pts',(371.549818958025,-23.6219333793781,3.86747953104869));
#44965=CARTESIAN_POINT('Ctrl Pts',(371.521099406255,-23.6234179719871,3.87257280091881));
#44966=CARTESIAN_POINT('Ctrl Pts',(371.407470725055,-23.6292917509944,3.8927242831904));
#44967=CARTESIAN_POINT('Ctrl Pts',(371.29276517905,-23.6351655300016,3.90790395531421));
#44968=CARTESIAN_POINT('Ctrl Pts',(371.177455643018,-23.6410393090088,3.91800273828579));
#44969=CARTESIAN_POINT('Ctrl Pts',(371.062294955964,-23.6469055057638,3.92808848509783));
#44970=CARTESIAN_POINT('Ctrl Pts',(370.946532237188,-23.6527717025188,3.93310635023573));
#44971=CARTESIAN_POINT('Ctrl Pts',(370.830650320756,-23.6586378992737,3.93299829000797));
#44972=CARTESIAN_POINT('Ctrl Pts',(370.714887042171,-23.6644980903206,3.93289034041034));
#44973=CARTESIAN_POINT('Ctrl Pts',(370.599005219337,-23.6703582813675,3.92766690421058));
#44974=CARTESIAN_POINT('Ctrl Pts',(370.48349190796,-23.6762184724144,3.91732180911012));
#44975=CARTESIAN_POINT('Ctrl Pts',(370.363813689121,-23.6822899564555,3.90660371488717));
#44976=CARTESIAN_POINT('Ctrl Pts',(370.244531506929,-23.6883614404965,3.8903876239092));
#44977=CARTESIAN_POINT('Ctrl Pts',(370.126186412439,-23.6944329245375,3.86872574145181));
#44978=CARTESIAN_POINT('Ctrl Pts',(370.012091077365,-23.7002863822498,3.84784173482723));
#44979=CARTESIAN_POINT('Ctrl Pts',(369.898867127292,-23.7061398399621,3.82189640608091));
#44980=CARTESIAN_POINT('Ctrl Pts',(369.786992468093,-23.7119932976744,3.79098912391743));
#44981=CARTESIAN_POINT('Ctrl Pts',(369.675134594174,-23.7178458771545,3.76008647897377));
#44982=CARTESIAN_POINT('Ctrl Pts',(369.564626006703,-23.7236984566347,3.72422347089168));
#44983=CARTESIAN_POINT('Ctrl Pts',(369.455931446481,-23.7295510361148,3.68354990650394));
#44984=CARTESIAN_POINT('Ctrl Pts',(369.34722691083,-23.7354041527146,3.64287260930569));
#44985=CARTESIAN_POINT('Ctrl Pts',(369.240337120329,-23.7412572693143,3.59738402295964));
#44986=CARTESIAN_POINT('Ctrl Pts',(369.135708092673,-23.7471103859141,3.54728260522892));
#44987=CARTESIAN_POINT('Ctrl Pts',(369.031044162269,-23.7529654550299,3.49716447438157));
#44988=CARTESIAN_POINT('Ctrl Pts',(368.928642866734,-23.7588205241456,3.44243063069062));
#44989=CARTESIAN_POINT('Ctrl Pts',(368.828926185299,-23.7646755932614,3.38332576885757));
#44990=CARTESIAN_POINT('Ctrl Pts',(368.729096487465,-23.7705372983664,3.32415391904925));
#44991=CARTESIAN_POINT('Ctrl Pts',(368.631957832316,-23.7763990034714,3.26060137397325));
#44992=CARTESIAN_POINT('Ctrl Pts',(368.537903807971,-23.7822607085764,3.19295655040372));
#44993=CARTESIAN_POINT('Ctrl Pts',(368.443786360278,-23.7881263663986,3.12526611197358));
#44994=CARTESIAN_POINT('Ctrl Pts',(368.352758008835,-23.7939920242208,3.05347815537743));
#44995=CARTESIAN_POINT('Ctrl Pts',(368.265178452428,-23.7998576820431,2.97792070735228));
#44996=CARTESIAN_POINT('Ctrl Pts',(368.177470842316,-23.8057319162871,2.90225278364609));
#44997=CARTESIAN_POINT('Ctrl Pts',(368.093222390468,-23.8116061505311,2.82280465122889));
#44998=CARTESIAN_POINT('Ctrl Pts',(368.012755272469,-23.8174803847751,2.73994043783507));
#44999=CARTESIAN_POINT('Ctrl Pts',(367.992419187765,-23.818964952983,2.71899854623452));
#45000=CARTESIAN_POINT('Ctrl Pts',(367.972324411649,-23.8204495211909,2.69783862802931));
#45001=CARTESIAN_POINT('Ctrl Pts',(367.952475719901,-23.8219340893987,2.67646687231542));
#45002=CARTESIAN_POINT('Ctrl Pts',(367.874845640598,-23.8277403737206,2.59287994820201));
#45003=CARTESIAN_POINT('Ctrl Pts',(367.800710733703,-23.8335466580424,2.50575695135316));
#45004=CARTESIAN_POINT('Ctrl Pts',(367.730415982015,-23.8393529423643,2.41542587837121));
#45005=CARTESIAN_POINT('Ctrl Pts',(367.660234682271,-23.8451498556559,2.32524059487712));
#45006=CARTESIAN_POINT('Ctrl Pts',(367.593881462807,-23.8509467689475,2.23185786899363));
#45007=CARTESIAN_POINT('Ctrl Pts',(367.531663925594,-23.8567436822391,2.13564183193501));
#45008=CARTESIAN_POINT('Ctrl Pts',(367.469503925471,-23.8625352347026,2.03951477285719));
#45009=CARTESIAN_POINT('Ctrl Pts',(367.411472236767,-23.8683267871661,1.94055996201908));
#45010=CARTESIAN_POINT('Ctrl Pts',(367.357835537159,-23.8741183396295,1.83917364761615));
#45011=CARTESIAN_POINT('Ctrl Pts',(367.304234736478,-23.8799060158194,1.73785519085511));
#45012=CARTESIAN_POINT('Ctrl Pts',(367.255023275686,-23.8856936920093,1.6341088381618));
#45013=CARTESIAN_POINT('Ctrl Pts',(367.210423457027,-23.8914813681991,1.52835807493371));
#45014=CARTESIAN_POINT('Ctrl Pts',(367.165842098073,-23.8972666488906,1.42265108156752));
#45015=CARTESIAN_POINT('Ctrl Pts',(367.125868749843,-23.903051929582,1.31494171714988));
#45016=CARTESIAN_POINT('Ctrl Pts',(367.090678486224,-23.9088372102735,1.20567544963205));
#45017=CARTESIAN_POINT('Ctrl Pts',(367.055483948564,-23.9146231936173,1.09639591115743));
#45018=CARTESIAN_POINT('Ctrl Pts',(367.025073795471,-23.9204091769612,0.985559492047928));
#45019=CARTESIAN_POINT('Ctrl Pts',(366.99957375711,-23.9261951603051,0.873628477854232));
#45020=CARTESIAN_POINT('Ctrl Pts',(366.974072376168,-23.931981448282,0.761691570472836));
#45021=CARTESIAN_POINT('Ctrl Pts',(366.953481710402,-23.937767736259,0.6486603683265));
#45022=CARTESIAN_POINT('Ctrl Pts',(366.937876438124,-23.9435540242359,0.535007755729943));
#45023=CARTESIAN_POINT('Ctrl Pts',(366.922259595966,-23.9493446022151,0.42127088013648));
#45024=CARTESIAN_POINT('Ctrl Pts',(366.911635576298,-23.9551351801943,0.306912095255886));
#45025=CARTESIAN_POINT('Ctrl Pts',(366.906027187634,-23.9609257581735,0.192409580431338));
#45026=CARTESIAN_POINT('Ctrl Pts',(366.902827554902,-23.9642293314374,0.127084936159333));
#45027=CARTESIAN_POINT('Ctrl Pts',(366.901259452096,-23.9675329047012,0.0617135537141975));
#45028=CARTESIAN_POINT('Ctrl Pts',(366.901319515466,-23.9708364779651,-0.00361596325308196));
#45029=CARTESIAN_POINT('',(369.0856199232,-24.9999241866122,3.52286027959241));
#45030=CARTESIAN_POINT('Ctrl Pts',(366.901319515466,-23.9708364779953,-0.0036159638503537));
#45031=CARTESIAN_POINT('Ctrl Pts',(366.901456107264,-23.9783492256021,-0.152183630750229));
#45032=CARTESIAN_POINT('Ctrl Pts',(366.910014340773,-23.9858619732089,-0.300376388370299));
#45033=CARTESIAN_POINT('Ctrl Pts',(366.926846153848,-23.9933747208157,-0.44738564860611));
#45034=CARTESIAN_POINT('Ctrl Pts',(366.944059171198,-24.0010576159569,-0.5977243516073));
#45035=CARTESIAN_POINT('Ctrl Pts',(366.969924781452,-24.0087405110982,-0.746825627686831));
#45036=CARTESIAN_POINT('Ctrl Pts',(367.004236650054,-24.0164234062394,-0.893849527115906));
#45037=CARTESIAN_POINT('Ctrl Pts',(367.010231224128,-24.0177656730964,-0.919535847671266));
#45038=CARTESIAN_POINT('Ctrl Pts',(367.016483487021,-24.0191079399534,-0.945158813959882));
#45039=CARTESIAN_POINT('Ctrl Pts',(367.022992190536,-24.0204502068104,-0.970714011920837));
#45040=CARTESIAN_POINT('Ctrl Pts',(367.051478761199,-24.0263248913126,-1.08256116409416));
#45041=CARTESIAN_POINT('Ctrl Pts',(367.084940277723,-24.0321995758149,-1.19333931436811));
#45042=CARTESIAN_POINT('Ctrl Pts',(367.123281110201,-24.0380742603171,-1.30257256685918));
#45043=CARTESIAN_POINT('Ctrl Pts',(367.161572432422,-24.0439413587258,-1.41166476434215));
#45044=CARTESIAN_POINT('Ctrl Pts',(367.204730404835,-24.0498084571345,-1.51921564525133));
#45045=CARTESIAN_POINT('Ctrl Pts',(367.252608796212,-24.0556755555432,-1.62476128428616));
#45046=CARTESIAN_POINT('Ctrl Pts',(367.300438138591,-24.0615366434055,-1.73019879713768));
#45047=CARTESIAN_POINT('Ctrl Pts',(367.352978111397,-24.0673977312678,-1.83363478038146));
#45048=CARTESIAN_POINT('Ctrl Pts',(367.410033485655,-24.0732588191302,-1.93462284955583));
#45049=CARTESIAN_POINT('Ctrl Pts',(367.469133693319,-24.0793299651757,-2.03923027589216));
#45050=CARTESIAN_POINT('Ctrl Pts',(367.533078883881,-24.0854011112212,-2.14121060684055));
#45051=CARTESIAN_POINT('Ctrl Pts',(367.601598550317,-24.0914722572667,-2.2400926116147));
#45052=CARTESIAN_POINT('Ctrl Pts',(367.667671284332,-24.0973265942577,-2.33544340271097));
#45053=CARTESIAN_POINT('Ctrl Pts',(367.737997104383,-24.1031809312487,-2.42791300605906));
#45054=CARTESIAN_POINT('Ctrl Pts',(367.812288408596,-24.1090352682398,-2.51710687810465));
#45055=CARTESIAN_POINT('Ctrl Pts',(367.886568467241,-24.1148887190525,-2.60628724876231));
#45056=CARTESIAN_POINT('Ctrl Pts',(367.964812552246,-24.1207421698653,-2.69219255682018));
#45057=CARTESIAN_POINT('Ctrl Pts',(368.046692534289,-24.126595620678,-2.7744610433796));
#45058=CARTESIAN_POINT('Ctrl Pts',(368.128579905949,-24.132449599761,-2.85673695461818));
#45059=CARTESIAN_POINT('Ctrl Pts',(368.214103535594,-24.138303578844,-2.93537509915258));
#45060=CARTESIAN_POINT('Ctrl Pts',(368.302898684382,-24.144157557927,-3.01005082874341));
#45061=CARTESIAN_POINT('Ctrl Pts',(368.391723301553,-24.150013479766,-3.08475134091618));
#45062=CARTESIAN_POINT('Ctrl Pts',(368.483821280868,-24.1558694016049,-3.15548655763097));
#45063=CARTESIAN_POINT('Ctrl Pts',(368.578795662652,-24.1617253234438,-3.22197278818994));
#45064=CARTESIAN_POINT('Ctrl Pts',(368.673877367559,-24.1675878626022,-3.2885341496399));
#45065=CARTESIAN_POINT('Ctrl Pts',(368.77184162403,-24.1734504017605,-3.35083670452901));
#45066=CARTESIAN_POINT('Ctrl Pts',(368.872263336832,-24.1793129409189,-3.40864064910112));
#45067=CARTESIAN_POINT('Ctrl Pts',(368.972752588234,-24.1851794229266,-3.46648346970289));
#45068=CARTESIAN_POINT('Ctrl Pts',(369.075702221223,-24.1910459049343,-3.51982146586649));
#45069=CARTESIAN_POINT('Ctrl Pts',(369.180665013877,-24.196912386942,-3.56846203383452));
#45070=CARTESIAN_POINT('Ctrl Pts',(369.285780885032,-24.2027874246699,-3.61717353956118));
#45071=CARTESIAN_POINT('Ctrl Pts',(369.392915394834,-24.2086624623977,-3.661173788335));
#45072=CARTESIAN_POINT('Ctrl Pts',(369.501603889699,-24.2145375001255,-3.70031924182562));
#45073=CARTESIAN_POINT('Ctrl Pts',(369.528915046232,-24.2160137748243,-3.71015567952021));
#45074=CARTESIAN_POINT('Ctrl Pts',(369.556324263869,-24.2174900495232,-3.71968582967798));
#45075=CARTESIAN_POINT('Ctrl Pts',(369.583824063438,-24.218966324222,-3.72890792078692));
#45076=CARTESIAN_POINT('Ctrl Pts',(369.693245676619,-24.2248404164544,-3.76560259136011));
#45077=CARTESIAN_POINT('Ctrl Pts',(369.804465679604,-24.2307145086869,-3.79753784266033));
#45078=CARTESIAN_POINT('Ctrl Pts',(369.91703237222,-24.2365886009193,-3.82453609557273));
#45079=CARTESIAN_POINT('Ctrl Pts',(370.029453951596,-24.2424551206759,-3.85149954419402));
#45080=CARTESIAN_POINT('Ctrl Pts',(370.143218370111,-24.2483216404325,-3.87353855580781));
#45081=CARTESIAN_POINT('Ctrl Pts',(370.257856559393,-24.2541881601892,-3.89052456318099));
#45082=CARTESIAN_POINT('Ctrl Pts',(370.372377571614,-24.2600486835013,-3.90749320836076));
#45083=CARTESIAN_POINT('Ctrl Pts',(370.487770171911,-24.2659092068134,-3.91941906260197));
#45084=CARTESIAN_POINT('Ctrl Pts',(370.603553474848,-24.2717697301256,-3.92622424240805));
#45085=CARTESIAN_POINT('Ctrl Pts',(370.723502227145,-24.2778410931051,-3.93327424708221));
#45086=CARTESIAN_POINT('Ctrl Pts',(370.843869884325,-24.2839124560846,-3.93482808927835));
#45087=CARTESIAN_POINT('Ctrl Pts',(370.964113675291,-24.2899838190641,-3.9308576728971));
#45088=CARTESIAN_POINT('Ctrl Pts',(371.080048827408,-24.2958376297676,-3.9270295265668));
#45089=CARTESIAN_POINT('Ctrl Pts',(371.195868389765,-24.3016914404711,-3.91806623889434));
#45090=CARTESIAN_POINT('Ctrl Pts',(371.311084975544,-24.3075452511746,-3.90399565971514));
#45091=CARTESIAN_POINT('Ctrl Pts',(371.426284413518,-24.3133981906493,-3.88992717467496));
#45092=CARTESIAN_POINT('Ctrl Pts',(371.540880643439,-24.319251130124,-3.87075295960273));
#45093=CARTESIAN_POINT('Ctrl Pts',(371.654391866833,-24.3251040695987,-3.84655269198321));
#45094=CARTESIAN_POINT('Ctrl Pts',(371.767913634676,-24.3309575527731,-3.82235017631749));
#45095=CARTESIAN_POINT('Ctrl Pts',(371.880349791616,-24.3368110359475,-3.79312076609747));
#45096=CARTESIAN_POINT('Ctrl Pts',(371.991229887442,-24.342664519122,-3.75899501796459));
#45097=CARTESIAN_POINT('Ctrl Pts',(372.102147085676,-24.3485199609737,-3.72485785076274));
#45098=CARTESIAN_POINT('Ctrl Pts',(372.21150679285,-24.3543754028254,-3.68582120918149));
#45099=CARTESIAN_POINT('Ctrl Pts',(372.318855519323,-24.3602308446771,-3.64206492500245));
#45100=CARTESIAN_POINT('Ctrl Pts',(372.426326035282,-24.3660929296561,-3.59825899835889));
#45101=CARTESIAN_POINT('Ctrl Pts',(372.53178063407,-24.3719550146351,-3.54972289777598));
#45102=CARTESIAN_POINT('Ctrl Pts',(372.634787461301,-24.377817099614,-3.49668388482455));
#45103=CARTESIAN_POINT('Ctrl Pts',(372.737863825642,-24.3836831419273,-3.44360906667695));
#45104=CARTESIAN_POINT('Ctrl Pts',(372.838488770445,-24.3895491842405,-3.38602548789292));
#45105=CARTESIAN_POINT('Ctrl Pts',(372.936258120726,-24.3954152265537,-3.32420458333332));
#45106=CARTESIAN_POINT('Ctrl Pts',(373.034170476087,-24.4012898489982,-3.26229325469496));
#45107=CARTESIAN_POINT('Ctrl Pts',(373.129218563327,-24.4071644714426,-3.19613246601103));
#45108=CARTESIAN_POINT('Ctrl Pts',(373.221029997727,-24.413039093887,-3.12603489092557));
#45109=CARTESIAN_POINT('Ctrl Pts',(373.244177591977,-24.4145202098026,-3.10836181745));
#45110=CARTESIAN_POINT('Ctrl Pts',(373.267119627545,-24.4160013257182,-3.09043868874957));
#45111=CARTESIAN_POINT('Ctrl Pts',(373.289850507784,-24.4174824416337,-3.07227088362816));
#45112=CARTESIAN_POINT('Ctrl Pts',(373.379915437798,-24.4233509605769,-3.00028589758434));
#45113=CARTESIAN_POINT('Ctrl Pts',(373.466963916202,-24.4292194795201,-2.92421591213455));
#45114=CARTESIAN_POINT('Ctrl Pts',(373.550602150184,-24.4350879984633,-2.84434326657155));
#45115=CARTESIAN_POINT('Ctrl Pts',(373.634132114576,-24.4409489206161,-2.76457401604811));
#45116=CARTESIAN_POINT('Ctrl Pts',(373.714260316684,-24.4468098427689,-2.68101217755409));
#45117=CARTESIAN_POINT('Ctrl Pts',(373.790624674593,-24.4526707649217,-2.59398129868439));
#45118=CARTESIAN_POINT('Ctrl Pts',(373.866910673734,-24.4585256730824,-2.50703972368229));
#45119=CARTESIAN_POINT('Ctrl Pts',(373.939440239106,-24.4643805812431,-2.41663649771471));
#45120=CARTESIAN_POINT('Ctrl Pts',(374.007887427826,-24.4702354894038,-2.32313261678282));
#45121=CARTESIAN_POINT('Ctrl Pts',(374.078889625628,-24.4763089506389,-2.22613840601473));
#45122=CARTESIAN_POINT('Ctrl Pts',(374.145498396162,-24.4823824118739,-2.12580785300024));
#45123=CARTESIAN_POINT('Ctrl Pts',(374.207394854622,-24.488455873109,-2.0225826417324));
#45124=CARTESIAN_POINT('Ctrl Pts',(374.266995477316,-24.4943040602351,-1.92318621385329));
#45125=CARTESIAN_POINT('Ctrl Pts',(374.32222691206,-24.5001522473612,-1.82110642942066));
#45126=CARTESIAN_POINT('Ctrl Pts',(374.372848546649,-24.5060004344873,-1.71676717457149));
#45127=CARTESIAN_POINT('Ctrl Pts',(374.423462695258,-24.5118477567775,-1.61244334952002));
#45128=CARTESIAN_POINT('Ctrl Pts',(374.469468218461,-24.5176950790676,-1.50586109073311));
#45129=CARTESIAN_POINT('Ctrl Pts',(374.510671076805,-24.5235424013577,-1.39746770104633));
#45130=CARTESIAN_POINT('Ctrl Pts',(374.55187785325,-24.5293902796868,-1.28906400391402));
#45131=CARTESIAN_POINT('Ctrl Pts',(374.588280909871,-24.535238158016,-1.17884922048234));
#45132=CARTESIAN_POINT('Ctrl Pts',(374.619735111485,-24.5410860363451,-1.06728870548844));
#45133=CARTESIAN_POINT('Ctrl Pts',(374.651199946746,-24.5469358916529,-0.955690475491368));
#45134=CARTESIAN_POINT('Ctrl Pts',(374.677712488063,-24.5527857469606,-0.842746007520911));
#45135=CARTESIAN_POINT('Ctrl Pts',(374.699178202527,-24.5586356022684,-0.728933111050087));
#45136=CARTESIAN_POINT('Ctrl Pts',(374.72066849635,-24.5644921559646,-0.614989892895866));
#45137=CARTESIAN_POINT('Ctrl Pts',(374.737100352414,-24.5703487096608,-0.500176668518449));
#45138=CARTESIAN_POINT('Ctrl Pts',(374.748430823958,-24.576205263357,-0.384978768675763));
#45139=CARTESIAN_POINT('Ctrl Pts',(374.759769000728,-24.5820657997706,-0.269702529128345));
#45140=CARTESIAN_POINT('Ctrl Pts',(374.765998863326,-24.5879263361843,-0.154041505544829));
#45141=CARTESIAN_POINT('Ctrl Pts',(374.767129590379,-24.5937868725979,-0.0384816851803687));
#45142=CARTESIAN_POINT('Ctrl Pts',(374.768261988245,-24.599656068801,0.0772488915170869));
#45143=CARTESIAN_POINT('Ctrl Pts',(374.764280227651,-24.605525265004,0.192877554481354));
#45144=CARTESIAN_POINT('Ctrl Pts',(374.755245371977,-24.6113944612071,0.307922705695058));
#45145=CARTESIAN_POINT('Ctrl Pts',(374.752882904271,-24.6129291604865,0.338005140249838));
#45146=CARTESIAN_POINT('Ctrl Pts',(374.750175209379,-24.6144638597659,0.368047730990852));
#45147=CARTESIAN_POINT('Ctrl Pts',(374.747123952468,-24.6159985590453,0.398041994923376));
#45148=CARTESIAN_POINT('Ctrl Pts',(374.735426283552,-24.6218821685148,0.513031646428155));
#45149=CARTESIAN_POINT('Ctrl Pts',(374.718636173904,-24.6277657779843,0.627693739462631));
#45150=CARTESIAN_POINT('Ctrl Pts',(374.696778725557,-24.6336493874539,0.741542318211561));
#45151=CARTESIAN_POINT('Ctrl Pts',(374.674949511691,-24.6395253967378,0.855243832419721));
#45152=CARTESIAN_POINT('Ctrl Pts',(374.648066054391,-24.6454014060217,0.968133521689445));
#45153=CARTESIAN_POINT('Ctrl Pts',(374.616205263135,-24.6512774153057,1.07972988231311));
#45154=CARTESIAN_POINT('Ctrl Pts',(374.584377195175,-24.6571473895104,1.19121162554159));
#45155=CARTESIAN_POINT('Ctrl Pts',(374.547582074684,-24.6630173637151,1.30140228899552));
#45156=CARTESIAN_POINT('Ctrl Pts',(374.505947848885,-24.6688873379198,1.40983054831438));
#45157=CARTESIAN_POINT('Ctrl Pts',(374.462910454372,-24.6749551436922,1.52191308817569));
#45158=CARTESIAN_POINT('Ctrl Pts',(374.414702094429,-24.6810229494646,1.6321118898979));
#45159=CARTESIAN_POINT('Ctrl Pts',(374.361520288645,-24.687090755237,1.73992298092849));
#45160=CARTESIAN_POINT('Ctrl Pts',(374.310132589878,-24.6929538614367,1.84409702669276));
#45161=CARTESIAN_POINT('Ctrl Pts',(374.254101795052,-24.6988169676364,1.94604146672834));
#45162=CARTESIAN_POINT('Ctrl Pts',(374.193654735131,-24.7046800738362,2.04532264297282));
#45163=CARTESIAN_POINT('Ctrl Pts',(374.13321741465,-24.7105422353519,2.14458782269084));
#45164=CARTESIAN_POINT('Ctrl Pts',(374.068365458107,-24.7164043968677,2.24119024048417));
#45165=CARTESIAN_POINT('Ctrl Pts',(373.999370619686,-24.7222665583835,2.33472267850232));
#45166=CARTESIAN_POINT('Ctrl Pts',(373.930370362768,-24.728129180283,2.42826246207226));
#45167=CARTESIAN_POINT('Ctrl Pts',(373.857226821597,-24.7339918021825,2.51873145534644));
#45168=CARTESIAN_POINT('Ctrl Pts',(373.78025344888,-24.739854424082,2.60575372325304));
#45169=CARTESIAN_POINT('Ctrl Pts',(373.703255583957,-24.7457189114129,2.69280368083081));
#45170=CARTESIAN_POINT('Ctrl Pts',(373.622425736794,-24.7515833987438,2.77640442399754));
#45171=CARTESIAN_POINT('Ctrl Pts',(373.538115300845,-24.7574478860747,2.85621574154327));
#45172=CARTESIAN_POINT('Ctrl Pts',(373.45371199277,-24.7633188334292,2.93611497521268));
#45173=CARTESIAN_POINT('Ctrl Pts',(373.365820742306,-24.7691897807837,3.01221616835958));
#45174=CARTESIAN_POINT('Ctrl Pts',(373.274827279402,-24.7750607281382,3.08421833545199));
#45175=CARTESIAN_POINT('Ctrl Pts',(373.183773975019,-24.7809355364972,3.15626785447475));
#45176=CARTESIAN_POINT('Ctrl Pts',(373.089614728311,-24.7868103448562,3.22421273865896));
#45177=CARTESIAN_POINT('Ctrl Pts',(372.992764187068,-24.7926851532151,3.28779537439818));
#45178=CARTESIAN_POINT('Ctrl Pts',(372.895775611393,-24.7985683345355,3.35146863010644));
#45179=CARTESIAN_POINT('Ctrl Pts',(372.796088438266,-24.8044515158558,3.41076701919639));
#45180=CARTESIAN_POINT('Ctrl Pts',(372.694141866626,-24.8103346971761,3.46547884702414));
#45181=CARTESIAN_POINT('Ctrl Pts',(372.669997641815,-24.8117280236031,3.47843636633704));
#45182=CARTESIAN_POINT('Ctrl Pts',(372.645726774633,-24.81312135003,3.49113684132792));
#45183=CARTESIAN_POINT('Ctrl Pts',(372.62133524988,-24.814514676457,3.50357786042328));
#45184=CARTESIAN_POINT('Ctrl Pts',(372.519529775596,-24.8203301496251,3.55550425134935));
#45185=CARTESIAN_POINT('Ctrl Pts',(372.415275008324,-24.8261456227933,3.60308336030811));
#45186=CARTESIAN_POINT('Ctrl Pts',(372.308982646098,-24.8319610959615,3.64607360713652));
#45187=CARTESIAN_POINT('Ctrl Pts',(372.202826302923,-24.8377691272484,3.6890088406751));
#45188=CARTESIAN_POINT('Ctrl Pts',(372.094637935516,-24.8435771585353,3.72736672841206));
#45189=CARTESIAN_POINT('Ctrl Pts',(371.984854025107,-24.8493851898223,3.760951411171));
#45190=CARTESIAN_POINT('Ctrl Pts',(371.875179831196,-24.8551874166443,3.79450252986967));
#45191=CARTESIAN_POINT('Ctrl Pts',(371.763913665966,-24.8609896434664,3.82328980564147));
#45192=CARTESIAN_POINT('Ctrl Pts',(371.651511457012,-24.8667918702884,3.8471656597979));
#45193=CARTESIAN_POINT('Ctrl Pts',(371.539187024154,-24.8725900822912,3.87102499318718));
#45194=CARTESIAN_POINT('Ctrl Pts',(371.425728522169,-24.878388294294,3.88997957516185));
#45195=CARTESIAN_POINT('Ctrl Pts',(371.311605765081,-24.8841865062969,3.90393202415144));
#45196=CARTESIAN_POINT('Ctrl Pts',(371.197523572533,-24.8899826573452,3.91787951379123));
#45197=CARTESIAN_POINT('Ctrl Pts',(371.082778012525,-24.8957788083936,3.92682835261829));
#45198=CARTESIAN_POINT('Ctrl Pts',(370.96784708384,-24.901574959442,3.93073262186212));
#45199=CARTESIAN_POINT('Ctrl Pts',(370.85292786991,-24.9073705196966,3.93463649314905));
#45200=CARTESIAN_POINT('Ctrl Pts',(370.737823746668,-24.9131660799511,3.93349680303252));
#45201=CARTESIAN_POINT('Ctrl Pts',(370.623014968402,-24.9189616402056,3.92731970825724));
#45202=CARTESIAN_POINT('Ctrl Pts',(370.508188785343,-24.924758079056,3.92114167704619));
#45203=CARTESIAN_POINT('Ctrl Pts',(370.393658457635,-24.9305545179064,3.90992474698988));
#45204=CARTESIAN_POINT('Ctrl Pts',(370.279900534571,-24.9363509567568,3.89372706244001));
#45205=CARTESIAN_POINT('Ctrl Pts',(370.166029974372,-24.9421531349372,3.87751333979161));
#45206=CARTESIAN_POINT('Ctrl Pts',(370.052933764254,-24.9479553131176,3.85630907571423));
#45207=CARTESIAN_POINT('Ctrl Pts',(369.941079656376,-24.9537574912981,3.83022382161817));
#45208=CARTESIAN_POINT('Ctrl Pts',(369.82916584053,-24.9595627666939,3.80412464315652));
#45209=CARTESIAN_POINT('Ctrl Pts',(369.718495852986,-24.9653680420897,3.7731394012963));
#45210=CARTESIAN_POINT('Ctrl Pts',(369.609521853363,-24.9711733174855,3.73742742521155));
#45211=CARTESIAN_POINT('Ctrl Pts',(369.500382321148,-24.9769874111524,3.70166120227943));
#45212=CARTESIAN_POINT('Ctrl Pts',(369.392944315382,-24.9828015048194,3.66115405719538));
#45213=CARTESIAN_POINT('Ctrl Pts',(369.287639788638,-24.9886155984863,3.61611337827333));
#45214=CARTESIAN_POINT('Ctrl Pts',(369.219366291571,-24.9923851278616,3.58691155043805));
#45215=CARTESIAN_POINT('Ctrl Pts',(369.151989131291,-24.9961546572369,3.5558050141533));
#45216=CARTESIAN_POINT('Ctrl Pts',(369.0856199232,-24.9999241866122,3.52286027959241));
#45217=CARTESIAN_POINT('',(372.583012328556,-25.,3.52286199445081));
#45218=CARTESIAN_POINT('Origin',(370.834317853224,-25.,0.));
#45219=CARTESIAN_POINT('',(366.902348364549,-24.1541640165523,-0.00373514424167985));
#45220=CARTESIAN_POINT('Ctrl Pts',(372.583012328555,-25.,3.52286199445091));
#45221=CARTESIAN_POINT('Ctrl Pts',(373.754775930706,-24.9338279608628,2.94121657640655));
#45222=CARTESIAN_POINT('Ctrl Pts',(375.451192048449,-24.8014838825885,0.524644555208875));
#45223=CARTESIAN_POINT('Ctrl Pts',(373.777719574704,-24.6029677651766,-3.60213327029863));
#45224=CARTESIAN_POINT('Ctrl Pts',(369.40332532051,-24.4044516477652,-4.42278112563621));
#45225=CARTESIAN_POINT('Ctrl Pts',(367.096283649816,-24.2548503982235,-1.99166067173424));
#45226=CARTESIAN_POINT('Ctrl Pts',(366.899312227999,-24.1714211878193,-0.345061147376345));
#45227=CARTESIAN_POINT('Ctrl Pts',(366.902348364549,-24.1541640165523,-0.00373514424167984));
#45228=CARTESIAN_POINT('',(366.901318041952,-22.9041635220074,0.00121841432566519));
#45229=CARTESIAN_POINT('Ctrl Pts',(366.901319618492,-24.154163522035,-0.00372633806003078));
#45230=CARTESIAN_POINT('Ctrl Pts',(366.901211040247,-24.1483709030749,0.110873582393982));
#45231=CARTESIAN_POINT('Ctrl Pts',(366.906115515684,-24.1425782841149,0.225595340395165));
#45232=CARTESIAN_POINT('Ctrl Pts',(366.916038151957,-24.1367856651548,0.33996056042058));
#45233=CARTESIAN_POINT('Ctrl Pts',(366.925955279232,-24.1309962622284,0.454262285436717));
#45234=CARTESIAN_POINT('Ctrl Pts',(366.940884993294,-24.125206859302,0.568207445362342));
#45235=CARTESIAN_POINT('Ctrl Pts',(366.960780336364,-24.1194174563756,0.681319385807697));
#45236=CARTESIAN_POINT('Ctrl Pts',(366.980670394066,-24.1136295914535,0.794401277099489));
#45237=CARTESIAN_POINT('Ctrl Pts',(367.005523386089,-24.1078417265315,0.906649972262003));
#45238=CARTESIAN_POINT('Ctrl Pts',(367.035240796864,-24.1020538616094,1.01759644252616));
#45239=CARTESIAN_POINT('Ctrl Pts',(367.064957886073,-24.0962660593168,1.12854171225819));
#45240=CARTESIAN_POINT('Ctrl Pts',(367.099539179392,-24.0904782570242,1.23818437640287));
#45241=CARTESIAN_POINT('Ctrl Pts',(367.138835807161,-24.0846904547317,1.34606888650933));
#45242=CARTESIAN_POINT('Ctrl Pts',(367.178142024708,-24.078901240009,1.45397972428082));
#45243=CARTESIAN_POINT('Ctrl Pts',(367.222165718138,-24.0731120252864,1.5601311580188));
#45244=CARTESIAN_POINT('Ctrl Pts',(367.270709548455,-24.0673228105638,1.66408679166055));
#45245=CARTESIAN_POINT('Ctrl Pts',(367.319305922783,-24.0615273295749,1.76815494724423));
#45246=CARTESIAN_POINT('Ctrl Pts',(367.372432019966,-24.055731848586,1.87002217515476));
#45247=CARTESIAN_POINT('Ctrl Pts',(367.429844131953,-24.0499363675972,1.96927592814549));
#45248=CARTESIAN_POINT('Ctrl Pts',(367.487291682565,-24.0441373092467,2.06859094724314));
#45249=CARTESIAN_POINT('Ctrl Pts',(367.549030285807,-24.0383382508963,2.16528892502502));
#45250=CARTESIAN_POINT('Ctrl Pts',(367.614773482489,-24.0325391925459,2.25898717235545));
#45251=CARTESIAN_POINT('Ctrl Pts',(367.680616649138,-24.0267313160712,2.35282789846979));
#45252=CARTESIAN_POINT('Ctrl Pts',(367.75047630523,-24.0209234395966,2.44365945622849));
#45253=CARTESIAN_POINT('Ctrl Pts',(367.824026372663,-24.015115563122,2.53113298782669));
#45254=CARTESIAN_POINT('Ctrl Pts',(367.856513999148,-24.0125501797286,2.56977071476638));
#45255=CARTESIAN_POINT('Ctrl Pts',(367.889721171392,-24.0099847963352,2.60775376482483));
#45256=CARTESIAN_POINT('Ctrl Pts',(367.923617651581,-24.0074194129418,2.64505450532738));
#45257=CARTESIAN_POINT('Ctrl Pts',(368.001233225964,-24.001545242394,2.73046509613132));
#45258=CARTESIAN_POINT('Ctrl Pts',(368.082740585547,-23.9956710718462,2.81259869280454));
#45259=CARTESIAN_POINT('Ctrl Pts',(368.167832125766,-23.9897969012984,2.89107987874132));
#45260=CARTESIAN_POINT('Ctrl Pts',(368.252813755781,-23.9839303182415,2.96945969287133));
#45261=CARTESIAN_POINT('Ctrl Pts',(368.341370058817,-23.9780637351846,3.04419620078266));
#45262=CARTESIAN_POINT('Ctrl Pts',(368.433154352334,-23.9721971521277,3.11494828881526));
#45263=CARTESIAN_POINT('Ctrl Pts',(368.524844595914,-23.9663365804671,3.18562787828477));
#45264=CARTESIAN_POINT('Ctrl Pts',(368.619755925512,-23.9604760088065,3.25233091819105));
#45265=CARTESIAN_POINT('Ctrl Pts',(368.71750660987,-23.9546154371459,3.31475476619477));
#45266=CARTESIAN_POINT('Ctrl Pts',(368.818772766051,-23.9485440979119,3.3794236038904));
#45267=CARTESIAN_POINT('Ctrl Pts',(368.923086016428,-23.9424727586779,3.43949935932853));
#45268=CARTESIAN_POINT('Ctrl Pts',(369.029986329454,-23.9364014194439,3.49469265491671));
#45269=CARTESIAN_POINT('Ctrl Pts',(369.133056728276,-23.9305475978926,3.54790854201389));
#45270=CARTESIAN_POINT('Ctrl Pts',(369.238531598795,-23.9246937763412,3.59658560823897));
#45271=CARTESIAN_POINT('Ctrl Pts',(369.345971937449,-23.9188399547899,3.64051032617621));
#45272=CARTESIAN_POINT('Ctrl Pts',(369.453396031117,-23.9129870183367,3.68442840269325));
#45273=CARTESIAN_POINT('Ctrl Pts',(369.562784619767,-23.9071340818835,3.72359540341856));
#45274=CARTESIAN_POINT('Ctrl Pts',(369.673678284574,-23.9012811454303,3.75784576475462));
#45275=CARTESIAN_POINT('Ctrl Pts',(369.784581987966,-23.8954276791435,3.79209922658462));
#45276=CARTESIAN_POINT('Ctrl Pts',(369.896990643664,-23.8895742128567,3.82143504235808));
#45277=CARTESIAN_POINT('Ctrl Pts',(370.010429907833,-23.8837207465699,3.84573759549974));
#45278=CARTESIAN_POINT('Ctrl Pts',(370.123906862006,-23.8778653354788,3.87004822312337));
#45279=CARTESIAN_POINT('Ctrl Pts',(370.238414701848,-23.8720099243878,3.88932217634726));
#45280=CARTESIAN_POINT('Ctrl Pts',(370.353469839863,-23.8661545132968,3.90349512463473));
#45281=CARTESIAN_POINT('Ctrl Pts',(370.468655110893,-23.8602924794481,3.917684103223));
#45282=CARTESIAN_POINT('Ctrl Pts',(370.584388505427,-23.8544304455994,3.92676051077787));
#45283=CARTESIAN_POINT('Ctrl Pts',(370.700182174666,-23.8485684117508,3.93071197364267));
#45284=CARTESIAN_POINT('Ctrl Pts',(370.816053777859,-23.8427024325097,3.93466609600625));
#45285=CARTESIAN_POINT('Ctrl Pts',(370.931985324504,-23.8368364532685,3.93348840949058));
#45286=CARTESIAN_POINT('Ctrl Pts',(371.047491567142,-23.8309704740274,3.92721860452079));
#45287=CARTESIAN_POINT('Ctrl Pts',(371.163166426168,-23.8250959316108,3.92093964686941));
#45288=CARTESIAN_POINT('Ctrl Pts',(371.278414332609,-23.8192213891941,3.90955377580453));
#45289=CARTESIAN_POINT('Ctrl Pts',(371.392757661741,-23.8133468467775,3.89315219073992));
#45290=CARTESIAN_POINT('Ctrl Pts',(371.421587733758,-23.8118656630284,3.88901676034632));
#45291=CARTESIAN_POINT('Ctrl Pts',(371.450360364779,-23.8103844792792,3.8845627185368));
#45292=CARTESIAN_POINT('Ctrl Pts',(371.479068043468,-23.80890329553,3.87979202950115));
#45293=CARTESIAN_POINT('Ctrl Pts',(371.592926779711,-23.8030287101393,3.86087079833835));
#45294=CARTESIAN_POINT('Ctrl Pts',(371.706140862762,-23.7971541247486,3.83690186711168));
#45295=CARTESIAN_POINT('Ctrl Pts',(371.818228011975,-23.7912795393579,3.80794036186305));
#45296=CARTESIAN_POINT('Ctrl Pts',(371.930170779619,-23.7854125211314,3.77901616247521));
#45297=CARTESIAN_POINT('Ctrl Pts',(372.040989104025,-23.7795455029048,3.74511228076714));
#45298=CARTESIAN_POINT('Ctrl Pts',(372.150208364254,-23.7736784846783,3.70633527395741));
#45299=CARTESIAN_POINT('Ctrl Pts',(372.259316084241,-23.767817458148,3.66759786819163));
#45300=CARTESIAN_POINT('Ctrl Pts',(372.366827601449,-23.7619564316177,3.62399737380741));
#45301=CARTESIAN_POINT('Ctrl Pts',(372.472281640284,-23.7560954050875,3.57569065108807));
#45302=CARTESIAN_POINT('Ctrl Pts',(372.581516778433,-23.7500242289637,3.52565187032618));
#45303=CARTESIAN_POINT('Ctrl Pts',(372.688543688626,-23.74395305284,3.4705631527276));
#45304=CARTESIAN_POINT('Ctrl Pts',(372.792869968271,-23.7378818767163,3.4106542792613));
#45305=CARTESIAN_POINT('Ctrl Pts',(372.893469871702,-23.7320275537803,3.35288525974034));
#45306=CARTESIAN_POINT('Ctrl Pts',(372.991558381076,-23.7261732308443,3.29063475531567));
#45307=CARTESIAN_POINT('Ctrl Pts',(373.086718083544,-23.7203189079082,3.22415604499136));
#45308=CARTESIAN_POINT('Ctrl Pts',(373.18186366578,-23.7144654536634,3.15768719908175));
#45309=CARTESIAN_POINT('Ctrl Pts',(373.274080966771,-23.7086119994185,3.08699163124631));
#45310=CARTESIAN_POINT('Ctrl Pts',(373.362981823317,-23.7027585451737,3.01236576901852));
#45311=CARTESIAN_POINT('Ctrl Pts',(373.451890968636,-23.6969045451753,2.93773294896269));
#45312=CARTESIAN_POINT('Ctrl Pts',(373.537482738475,-23.6910505451769,2.85916937158491));
#45313=CARTESIAN_POINT('Ctrl Pts',(373.619402860261,-23.6851965451785,2.77701107372275));
#45314=CARTESIAN_POINT('Ctrl Pts',(373.701350413512,-23.6793405849316,2.69482526464086));
#45315=CARTESIAN_POINT('Ctrl Pts',(373.779623582479,-23.6734846246847,2.60904263381188));
#45316=CARTESIAN_POINT('Ctrl Pts',(373.853906188467,-23.6676286644378,2.52003477866117));
#45317=CARTESIAN_POINT('Ctrl Pts',(373.928273060669,-23.6617660611877,2.43092595296979));
#45318=CARTESIAN_POINT('Ctrl Pts',(373.998640069694,-23.6559034579375,2.33858491766555));
#45319=CARTESIAN_POINT('Ctrl Pts',(374.064732393004,-23.6500408546873,2.24341500868123));
#45320=CARTESIAN_POINT('Ctrl Pts',(374.130869335962,-23.6441742935299,2.14818084945474));
#45321=CARTESIAN_POINT('Ctrl Pts',(374.192725626933,-23.6383077323724,2.05011436212437));
#45322=CARTESIAN_POINT('Ctrl Pts',(374.250071609165,-23.6324411712149,1.94964491094506));
#45323=CARTESIAN_POINT('Ctrl Pts',(374.307501433047,-23.6265660329584,1.84902857023195));
#45324=CARTESIAN_POINT('Ctrl Pts',(374.360407599833,-23.6206908947019,1.74600262014703));
#45325=CARTESIAN_POINT('Ctrl Pts',(374.408607872484,-23.6148157564454,1.641017933546));
#45326=CARTESIAN_POINT('Ctrl Pts',(374.420718718419,-23.6133395636698,1.61463938224214));
#45327=CARTESIAN_POINT('Ctrl Pts',(374.432532715833,-23.6118633708941,1.58813725214939));
#45328=CARTESIAN_POINT('Ctrl Pts',(374.444047468922,-23.6103871781184,1.56151884444309));
#45329=CARTESIAN_POINT('Ctrl Pts',(374.489859508578,-23.6045140689465,1.4556161351097));
#45330=CARTESIAN_POINT('Ctrl Pts',(374.531083565184,-23.5986409597746,1.34751893434641));
#45331=CARTESIAN_POINT('Ctrl Pts',(374.567504376343,-23.5927678506027,1.23766206357107));
#45332=CARTESIAN_POINT('Ctrl Pts',(374.603878113192,-23.5869023324907,1.12794718404289));
#45333=CARTESIAN_POINT('Ctrl Pts',(374.635460821849,-23.5810368143788,1.01647754615335));
#45334=CARTESIAN_POINT('Ctrl Pts',(374.662084596016,-23.5751712962669,0.903709445991489));
#45335=CARTESIAN_POINT('Ctrl Pts',(374.688681074097,-23.5693117917908,0.791056961582879));
#45336=CARTESIAN_POINT('Ctrl Pts',(374.71032863606,-23.5634522873148,0.677109062643));
#45337=CARTESIAN_POINT('Ctrl Pts',(374.726908870607,-23.5575927828387,0.562338129054325));
#45338=CARTESIAN_POINT('Ctrl Pts',(374.744089648872,-23.5515210444166,0.443410139483239));
#45339=CARTESIAN_POINT('Ctrl Pts',(374.7558289184,-23.5454493059944,0.323598792791398));
#45340=CARTESIAN_POINT('Ctrl Pts',(374.762052576321,-23.5393775675722,0.203442731438583));
#45341=CARTESIAN_POINT('Ctrl Pts',(374.768051772455,-23.5335248118243,0.0876202058567169));
#45342=CARTESIAN_POINT('Ctrl Pts',(374.768926310938,-23.5276720560764,-0.0285221508597304));
#45343=CARTESIAN_POINT('Ctrl Pts',(374.764662591531,-23.5218193003285,-0.144496498450968));
#45344=CARTESIAN_POINT('Ctrl Pts',(374.760399515183,-23.5159674273001,-0.260453354655197));
#45345=CARTESIAN_POINT('Ctrl Pts',(374.750999737023,-23.5101155542717,-0.376241839268233));
#45346=CARTESIAN_POINT('Ctrl Pts',(374.7365017716,-23.5042636812433,-0.491375281397875));
#45347=CARTESIAN_POINT('Ctrl Pts',(374.722002484717,-23.4984112748287,-0.606519217703132));
#45348=CARTESIAN_POINT('Ctrl Pts',(374.702404138451,-23.4925588684142,-0.721007582811191));
#45349=CARTESIAN_POINT('Ctrl Pts',(374.677796905732,-23.4867064619996,-0.834360697140713));
#45350=CARTESIAN_POINT('Ctrl Pts',(374.653181475933,-23.4808521060508,-0.947751571284607));
#45351=CARTESIAN_POINT('Ctrl Pts',(374.623553929497,-23.4749977501019,-1.06000603906158));
#45352=CARTESIAN_POINT('Ctrl Pts',(374.589054975105,-23.4691433941531,-1.17065714261912));
#45353=CARTESIAN_POINT('Ctrl Pts',(374.554516920495,-23.4632824030292,-1.28143365526499));
#45354=CARTESIAN_POINT('Ctrl Pts',(374.515096561176,-23.4574214119053,-1.39060278192006));
#45355=CARTESIAN_POINT('Ctrl Pts',(374.47098369848,-23.4515604207814,-1.49771510306407));
#45356=CARTESIAN_POINT('Ctrl Pts',(374.426841095714,-23.4456954782865,-1.60489963733956));
#45357=CARTESIAN_POINT('Ctrl Pts',(374.377999863869,-23.4398305357916,-1.71002423113383));
#45358=CARTESIAN_POINT('Ctrl Pts',(374.324696163445,-23.4339655932967,-1.81266330341204));
#45359=CARTESIAN_POINT('Ctrl Pts',(374.271314483747,-23.4280920708354,-1.91545252887505));
#45360=CARTESIAN_POINT('Ctrl Pts',(374.213457512432,-23.422218548374,-2.01574861945833));
#45361=CARTESIAN_POINT('Ctrl Pts',(374.151405192807,-23.4163450259127,-2.1131541783731));
#45362=CARTESIAN_POINT('Ctrl Pts',(374.135649745613,-23.4148537041774,-2.13788601997338));
#45363=CARTESIAN_POINT('Ctrl Pts',(374.119624035791,-23.4133623824421,-2.16243167915984));
#45364=CARTESIAN_POINT('Ctrl Pts',(374.103333052733,-23.4118710607068,-2.18678499752064));
#45365=CARTESIAN_POINT('Ctrl Pts',(374.039168680047,-23.4059972762164,-2.28270403382942));
#45366=CARTESIAN_POINT('Ctrl Pts',(373.970672218861,-23.400123491726,-2.37595634356408));
#45367=CARTESIAN_POINT('Ctrl Pts',(373.898092499842,-23.3942497072356,-2.46612528366739));
#45368=CARTESIAN_POINT('Ctrl Pts',(373.82560648435,-23.3883835060527,-2.55617781180404));
#45369=CARTESIAN_POINT('Ctrl Pts',(373.74904795132,-23.3825173048699,-2.64315456786081));
#45370=CARTESIAN_POINT('Ctrl Pts',(373.668709442221,-23.376651103687,-2.7266670717601));
#45371=CARTESIAN_POINT('Ctrl Pts',(373.588453196589,-23.370790909263,-2.81009406214707));
#45372=CARTESIAN_POINT('Ctrl Pts',(373.504424958444,-23.3649307148389,-2.89006356021101));
#45373=CARTESIAN_POINT('Ctrl Pts',(373.416957609282,-23.3590705204149,-2.96621996662902));
#45374=CARTESIAN_POINT('Ctrl Pts',(373.326336645055,-23.3529990380349,-3.04512217468414));
#45375=CARTESIAN_POINT('Ctrl Pts',(373.232024180959,-23.3469275556549,-3.11993079081061));
#45376=CARTESIAN_POINT('Ctrl Pts',(373.134432603918,-23.3408560732749,-3.19029170039991));
#45377=CARTESIAN_POINT('Ctrl Pts',(373.040345492086,-23.3350026148209,-3.25812598456511));
#45378=CARTESIAN_POINT('Ctrl Pts',(372.943211083313,-23.3291491563668,-3.32182623581534));
#45379=CARTESIAN_POINT('Ctrl Pts',(372.843432051197,-23.3232956979128,-3.3811165521914));
#45380=CARTESIAN_POINT('Ctrl Pts',(372.743668006188,-23.3174431186656,-3.44039796298622));
#45381=CARTESIAN_POINT('Ctrl Pts',(372.641260482743,-23.3115905394184,-3.49527054499489));
#45382=CARTESIAN_POINT('Ctrl Pts',(372.53663941868,-23.3057379601712,-3.5455028258041));
#45383=CARTESIAN_POINT('Ctrl Pts',(372.432008770451,-23.2998848447787,-3.595739708311));
#45384=CARTESIAN_POINT('Ctrl Pts',(372.325164550945,-23.2940317293862,-3.64133526575361));
#45385=CARTESIAN_POINT('Ctrl Pts',(372.21655882358,-23.2881786139937,-3.68210522661568));
#45386=CARTESIAN_POINT('Ctrl Pts',(372.107916884977,-23.28232354706,-3.72288878096662));
#45387=CARTESIAN_POINT('Ctrl Pts',(371.99751265722,-23.2764684801262,-3.75884339430151));
#45388=CARTESIAN_POINT('Ctrl Pts',(371.885814906657,-23.2706134131925,-3.78983415819493));
#45389=CARTESIAN_POINT('Ctrl Pts',(371.77399058791,-23.2647517117009,-3.82086003868378));
#45390=CARTESIAN_POINT('Ctrl Pts',(371.66087021916,-23.2588900102093,-3.84691073266935));
#45391=CARTESIAN_POINT('Ctrl Pts',(371.546934440917,-23.2530283087177,-3.86790209272996));
#45392=CARTESIAN_POINT('Ctrl Pts',(371.432921848747,-23.247162655348,-3.88890760487548));
#45393=CARTESIAN_POINT('Ctrl Pts',(371.318093160626,-23.2412970019783,-3.90484693450206));
#45394=CARTESIAN_POINT('Ctrl Pts',(371.202934117157,-23.2354313486085,-3.91568781313882));
#45395=CARTESIAN_POINT('Ctrl Pts',(371.087606718133,-23.2295571200084,-3.92654454048432));
#45396=CARTESIAN_POINT('Ctrl Pts',(370.97194841093,-23.2236828914082,-3.93228792085756));
#45397=CARTESIAN_POINT('Ctrl Pts',(370.856444988247,-23.2178086628081,-3.93293775565997));
#45398=CARTESIAN_POINT('Ctrl Pts',(370.827254213739,-23.2163240896371,-3.93310198612816));
#45399=CARTESIAN_POINT('Ctrl Pts',(370.798073303989,-23.2148395164661,-3.93294114682943));
#45400=CARTESIAN_POINT('Ctrl Pts',(370.768910031146,-23.2133549432951,-3.93245607945098));
#45401=CARTESIAN_POINT('Ctrl Pts',(370.653524345242,-23.2074811686151,-3.93053689046032));
#45402=CARTESIAN_POINT('Ctrl Pts',(370.538031092616,-23.2016073939351,-3.9235317517467));
#45403=CARTESIAN_POINT('Ctrl Pts',(370.422915275364,-23.1957336192552,-3.91142389916133));
#45404=CARTESIAN_POINT('Ctrl Pts',(370.307948048513,-23.1898674263876,-3.89933167527679));
#45405=CARTESIAN_POINT('Ctrl Pts',(370.193357695288,-23.18400123352,-3.8821498788094));
#45406=CARTESIAN_POINT('Ctrl Pts',(370.079629247252,-23.1781350406525,-3.85991374359787));
#45407=CARTESIAN_POINT('Ctrl Pts',(369.966017223771,-23.1722748530449,-3.8377003716631));
#45408=CARTESIAN_POINT('Ctrl Pts',(369.85326575348,-23.1664146654373,-3.81044303162838));
#45409=CARTESIAN_POINT('Ctrl Pts',(369.741854105687,-23.1605544778296,-3.77822868025699));
#45410=CARTESIAN_POINT('Ctrl Pts',(369.626425343137,-23.1544829923319,-3.74485279192934));
#45411=CARTESIAN_POINT('Ctrl Pts',(369.512435294055,-23.1484115068341,-3.70615572923897));
#45412=CARTESIAN_POINT('Ctrl Pts',(369.400405081633,-23.1423400213364,-3.66229206419552));
#45413=CARTESIAN_POINT('Ctrl Pts',(369.292397929558,-23.1364865658862,-3.62000356506178));
#45414=CARTESIAN_POINT('Ctrl Pts',(369.186212695366,-23.1306331104361,-3.57291331529551));
#45415=CARTESIAN_POINT('Ctrl Pts',(369.082299511122,-23.1247796549859,-3.52121012280412));
#45416=CARTESIAN_POINT('Ctrl Pts',(368.978401909709,-23.1189270773205,-3.46951468372823));
#45417=CARTESIAN_POINT('Ctrl Pts',(368.876776050546,-23.113074499655,-3.41320786138786));
#45418=CARTESIAN_POINT('Ctrl Pts',(368.777849510401,-23.1072219219896,-3.35252545925701));
#45419=CARTESIAN_POINT('Ctrl Pts',(368.678913883569,-23.101368806748,-3.29183748327281));
#45420=CARTESIAN_POINT('Ctrl Pts',(368.582678420814,-23.0955156915065,-3.2267733445655));
#45421=CARTESIAN_POINT('Ctrl Pts',(368.489543029175,-23.0896625762649,-3.15761302640246));
#45422=CARTESIAN_POINT('Ctrl Pts',(368.396376561482,-23.0838075080416,-3.08842963183652));
#45423=CARTESIAN_POINT('Ctrl Pts',(368.306312553243,-23.0779524398182,-3.01514758625118));
#45424=CARTESIAN_POINT('Ctrl Pts',(368.219718485244,-23.0720973715948,-2.93808766801781));
#45425=CARTESIAN_POINT('Ctrl Pts',(368.133026263153,-23.0662356666708,-2.86094040261986));
#45426=CARTESIAN_POINT('Ctrl Pts',(368.049812140463,-23.0603739617468,-2.78000699234342));
#45427=CARTESIAN_POINT('Ctrl Pts',(367.970407379493,-23.0545122568227,-2.69564571085522));
#45428=CARTESIAN_POINT('Ctrl Pts',(367.890949067956,-23.0486465987652,-2.6112275361234));
#45429=CARTESIAN_POINT('Ctrl Pts',(367.815305502559,-23.0427809407077,-2.52337719924941));
#45430=CARTESIAN_POINT('Ctrl Pts',(367.743767115392,-23.0369152826502,-2.4324853826663));
#45431=CARTESIAN_POINT('Ctrl Pts',(367.672124121428,-23.0310410475515,-2.34146065979118));
#45432=CARTESIAN_POINT('Ctrl Pts',(367.604598525725,-23.0251668124527,-2.24738591565487));
#45433=CARTESIAN_POINT('Ctrl Pts',(367.541437033318,-23.0192925773539,-2.15068010310603));
#45434=CARTESIAN_POINT('Ctrl Pts',(367.525474354209,-23.0178079935305,-2.12623983428272));
#45435=CARTESIAN_POINT('Ctrl Pts',(367.50979018446,-23.016323409707,-2.1016316320158));
#45436=CARTESIAN_POINT('Ctrl Pts',(367.494388030071,-23.0148388258835,-2.07686248375052));
#45437=CARTESIAN_POINT('Ctrl Pts',(367.431746748682,-23.0088009541236,-1.97612520070657));
#45438=CARTESIAN_POINT('Ctrl Pts',(367.373574834104,-23.0027630823638,-1.87240387406079));
#45439=CARTESIAN_POINT('Ctrl Pts',(367.320159377181,-22.9967252106039,-1.76611981622393));
#45440=CARTESIAN_POINT('Ctrl Pts',(367.266825227544,-22.9906965294975,-1.65999754054877));
#45441=CARTESIAN_POINT('Ctrl Pts',(367.218233294385,-22.9846678483911,-1.5513206366528));
#45442=CARTESIAN_POINT('Ctrl Pts',(367.174626820583,-22.9786391672847,-1.44053828328386));
#45443=CARTESIAN_POINT('Ctrl Pts',(367.129735571898,-22.9724328635139,-1.32649195618223));
#45444=CARTESIAN_POINT('Ctrl Pts',(367.0901283489,-22.9662265597431,-1.21021451682593));
#45445=CARTESIAN_POINT('Ctrl Pts',(367.056019779913,-22.9600202559723,-1.09222372672062));
#45446=CARTESIAN_POINT('Ctrl Pts',(367.022980401753,-22.9540084992981,-0.977931557645554));
#45447=CARTESIAN_POINT('Ctrl Pts',(366.995100256272,-22.9479967426239,-0.862032241019598));
#45448=CARTESIAN_POINT('Ctrl Pts',(366.972525565224,-22.9419849859498,-0.745016324883455));
#45449=CARTESIAN_POINT('Ctrl Pts',(366.948855061212,-22.9356814086307,-0.622320261999813));
#45450=CARTESIAN_POINT('Ctrl Pts',(366.931018180592,-22.9293778313115,-0.498396867271249));
#45451=CARTESIAN_POINT('Ctrl Pts',(366.919124201177,-22.9230742539924,-0.373828392409864));
#45452=CARTESIAN_POINT('Ctrl Pts',(366.907230221762,-22.9167706766733,-0.249259917548461));
#45453=CARTESIAN_POINT('Ctrl Pts',(366.901279235717,-22.9104670993541,-0.12404684158491));
#45454=CARTESIAN_POINT('Ctrl Pts',(366.901318041952,-22.904163522035,0.00121841377663275));
#45455=CARTESIAN_POINT('',(366.901318968034,-21.6541635220757,0.00296126550371377));
#45456=CARTESIAN_POINT('Ctrl Pts',(366.901318041952,-22.9041635220074,0.00121841432564433));
#45457=CARTESIAN_POINT('Ctrl Pts',(366.901356814938,-22.8978653482165,0.126376290286846));
#45458=CARTESIAN_POINT('Ctrl Pts',(366.907374045914,-22.8915671744257,0.251362841332967));
#45459=CARTESIAN_POINT('Ctrl Pts',(366.919295671331,-22.8852690006348,0.375619908000912));
#45460=CARTESIAN_POINT('Ctrl Pts',(366.931264251033,-22.8789460209772,0.500366371174498));
#45461=CARTESIAN_POINT('Ctrl Pts',(366.94918373839,-22.8726230413195,0.624377293027341));
#45462=CARTESIAN_POINT('Ctrl Pts',(366.972928461376,-22.8663000616618,0.74710170962471));
#45463=CARTESIAN_POINT('Ctrl Pts',(366.996721025578,-22.8599643423721,0.870073393174389));
#45464=CARTESIAN_POINT('Ctrl Pts',(367.026362194002,-22.8536286230824,0.99175309786698));
#45465=CARTESIAN_POINT('Ctrl Pts',(367.06167635572,-22.8472929037927,1.11160475498688));
#45466=CARTESIAN_POINT('Ctrl Pts',(367.097101549305,-22.8409372642584,1.23183323977499));
#45467=CARTESIAN_POINT('Ctrl Pts',(367.138235322381,-22.8345816247241,1.3502218874582));
#45468=CARTESIAN_POINT('Ctrl Pts',(367.184852995517,-22.8282259851898,1.46625211077756));
#45469=CARTESIAN_POINT('Ctrl Pts',(367.213955918482,-22.8242582262838,1.53868855866898));
#45470=CARTESIAN_POINT('Ctrl Pts',(367.245195188944,-22.8202904673778,1.61020630411966));
#45471=CARTESIAN_POINT('Ctrl Pts',(367.278507222014,-22.8163227084717,1.68068431151555));
#45472=CARTESIAN_POINT('Ctrl Pts',(367.32782096343,-22.8104490040274,1.78501700789984));
#45473=CARTESIAN_POINT('Ctrl Pts',(367.381812636293,-22.8045752995831,1.88735121774635));
#45474=CARTESIAN_POINT('Ctrl Pts',(367.440297597901,-22.7987015951388,1.98723816047698));
#45475=CARTESIAN_POINT('Ctrl Pts',(367.498707051017,-22.7928354740894,2.08699614163915));
#45476=CARTESIAN_POINT('Ctrl Pts',(367.561598049398,-22.78696935304,2.18431278583786));
#45477=CARTESIAN_POINT('Ctrl Pts',(367.628738563243,-22.7811032319907,2.2787607192605));
#45478=CARTESIAN_POINT('Ctrl Pts',(367.695810327044,-22.7752431176882,2.37311194059153));
#45479=CARTESIAN_POINT('Ctrl Pts',(367.767122713087,-22.7693830033858,2.46459995931142));
#45480=CARTESIAN_POINT('Ctrl Pts',(367.8423989425,-22.7635228890834,2.55282397192895));
#45481=CARTESIAN_POINT('Ctrl Pts',(367.920390691134,-22.7574513766658,2.64423058287519));
#45482=CARTESIAN_POINT('Ctrl Pts',(368.002637437747,-22.7513798642481,2.73213286028289));
#45483=CARTESIAN_POINT('Ctrl Pts',(368.088783529227,-22.7453083518305,2.81611971971314));
#45484=CARTESIAN_POINT('Ctrl Pts',(368.171834617418,-22.7394549729415,2.89708915140137));
#45485=CARTESIAN_POINT('Ctrl Pts',(368.258509364299,-22.7336015940525,2.97441935203995));
#45486=CARTESIAN_POINT('Ctrl Pts',(368.348450205572,-22.7277482151635,3.04777804939232));
#45487=CARTESIAN_POINT('Ctrl Pts',(368.438377542599,-22.7218957151351,3.12112573223926));
#45488=CARTESIAN_POINT('Ctrl Pts',(368.531569678868,-22.7160432151068,3.19050283641997));
#45489=CARTESIAN_POINT('Ctrl Pts',(368.627635530635,-22.7101907150784,3.25561701174666));
#45490=CARTESIAN_POINT('Ctrl Pts',(368.72371019009,-22.7043376784703,3.32073715699181));
#45491=CARTESIAN_POINT('Ctrl Pts',(368.822658746798,-22.6984846418622,3.38159336461209));
#45492=CARTESIAN_POINT('Ctrl Pts',(368.924061271353,-22.6926316052541,3.43793670555734));
#45493=CARTESIAN_POINT('Ctrl Pts',(369.025497614978,-22.6867766165817,3.49429883774479));
#45494=CARTESIAN_POINT('Ctrl Pts',(369.129389192919,-22.6809216279092,3.54614490987749));
#45495=CARTESIAN_POINT('Ctrl Pts',(369.235292274704,-22.6750666392367,3.59327235249964));
#45496=CARTESIAN_POINT('Ctrl Pts',(369.341315381472,-22.669205014828,3.64045320688651));
#45497=CARTESIAN_POINT('Ctrl Pts',(369.449354164626,-22.6633433904193,3.68290458971904));
#45498=CARTESIAN_POINT('Ctrl Pts',(369.558945662437,-22.6574817660107,3.7204723859972));
#45499=CARTESIAN_POINT('Ctrl Pts',(369.6686110574,-22.6516161891298,3.75806551410465));
#45500=CARTESIAN_POINT('Ctrl Pts',(369.779830856427,-22.645750612249,3.79076838233586));
#45501=CARTESIAN_POINT('Ctrl Pts',(369.892129401949,-22.6398850353681,3.81847743508899));
#45502=CARTESIAN_POINT('Ctrl Pts',(370.004592151318,-22.634010881793,3.84622700424463));
#45503=CARTESIAN_POINT('Ctrl Pts',(370.118136391639,-22.6281367282179,3.86896810414709));
#45504=CARTESIAN_POINT('Ctrl Pts',(370.232278734123,-22.6222625746428,3.88664867193735));
#45505=CARTESIAN_POINT('Ctrl Pts',(370.261140560636,-22.620777246782,3.89111934836741));
#45506=CARTESIAN_POINT('Ctrl Pts',(370.290040617557,-22.6192919189211,3.8952667281833));
#45507=CARTESIAN_POINT('Ctrl Pts',(370.318971081571,-22.6178065910602,3.89909049714761));
#45508=CARTESIAN_POINT('Ctrl Pts',(370.433375978564,-22.6119328940175,3.91421150918101));
#45509=CARTESIAN_POINT('Ctrl Pts',(370.548637482259,-22.6060591969748,3.92431823208454));
#45510=CARTESIAN_POINT('Ctrl Pts',(370.664278383264,-22.6001854999321,3.92932253431245));
#45511=CARTESIAN_POINT('Ctrl Pts',(370.779769984465,-22.5943193862082,3.93432037566593));
#45512=CARTESIAN_POINT('Ctrl Pts',(370.895639599885,-22.5884532724842,3.93422887912631));
#45513=CARTESIAN_POINT('Ctrl Pts',(371.011402319388,-22.5825871587603,3.9290113377087));
#45514=CARTESIAN_POINT('Ctrl Pts',(371.127046502571,-22.5767270516983,3.92379913884144));
#45515=CARTESIAN_POINT('Ctrl Pts',(371.242583597283,-22.5708669446364,3.91347135400912));
#45516=CARTESIAN_POINT('Ctrl Pts',(371.357526761736,-22.5650068375745,3.89804328324526));
#45517=CARTESIAN_POINT('Ctrl Pts',(371.476616593808,-22.5589353224109,3.88205863235104));
#45518=CARTESIAN_POINT('Ctrl Pts',(371.595068382299,-22.5528638072473,3.86059873458005));
#45519=CARTESIAN_POINT('Ctrl Pts',(371.712343885212,-22.5467922920837,3.83373959563648));
#45520=CARTESIAN_POINT('Ctrl Pts',(371.825405800721,-22.5409389201742,3.807845477748));
#45521=CARTESIAN_POINT('Ctrl Pts',(371.93737406427,-22.5350855482646,3.77693352043325));
#45522=CARTESIAN_POINT('Ctrl Pts',(372.047775626912,-22.529232176355,3.7411240598883));
#45523=CARTESIAN_POINT('Ctrl Pts',(372.158160615257,-22.5233796831969,3.70531997532418));
#45524=CARTESIAN_POINT('Ctrl Pts',(372.266978977489,-22.5175271900388,3.6646199769158));
#45525=CARTESIAN_POINT('Ctrl Pts',(372.373773040315,-22.5116746968806,3.61919420961895));
#45526=CARTESIAN_POINT('Ctrl Pts',(372.480576896583,-22.5058216670255,3.57376427659764));
#45527=CARTESIAN_POINT('Ctrl Pts',(372.585355704218,-22.4999686371703,3.52360787490648));
#45528=CARTESIAN_POINT('Ctrl Pts',(372.687672639604,-22.4941156073152,3.4689429277235));
#45529=CARTESIAN_POINT('Ctrl Pts',(372.79002370126,-22.4882606252702,3.41425974787208));
#45530=CARTESIAN_POINT('Ctrl Pts',(372.889910893705,-22.4824056432253,3.35506522695551));
#45531=CARTESIAN_POINT('Ctrl Pts',(372.986923446946,-22.4765506611803,3.2916224203086));
#45532=CARTESIAN_POINT('Ctrl Pts',(373.084045952894,-22.4706890431784,3.22810770844783));
#45533=CARTESIAN_POINT('Ctrl Pts',(373.178286970748,-22.4648274251764,3.1603353267557));
#45534=CARTESIAN_POINT('Ctrl Pts',(373.26926602179,-22.4589658071745,3.08861075831808));
#45535=CARTESIAN_POINT('Ctrl Pts',(373.360306421624,-22.4531002365793,3.01683782472846));
#45536=CARTESIAN_POINT('Ctrl Pts',(373.448080162715,-22.4472346659841,2.94110766694654));
#45537=CARTESIAN_POINT('Ctrl Pts',(373.532242369358,-22.4413690953889,2.86176384512115));
#45538=CARTESIAN_POINT('Ctrl Pts',(373.616527642049,-22.4354949478727,2.78230400292307));
#45539=CARTESIAN_POINT('Ctrl Pts',(373.697190554142,-22.4296208003566,2.69922024628117));
#45540=CARTESIAN_POINT('Ctrl Pts',(373.773925308593,-22.4237466528405,2.61289054656712));
#45541=CARTESIAN_POINT('Ctrl Pts',(373.793329191747,-22.4222612597764,2.59106039388171));
#45542=CARTESIAN_POINT('Ctrl Pts',(373.812482109396,-22.4207758667124,2.56902283568234));
#45543=CARTESIAN_POINT('Ctrl Pts',(373.831379555812,-22.4192904736484,2.54678427647057));
#45544=CARTESIAN_POINT('Ctrl Pts',(373.906105627588,-22.413416791762,2.4588464601537));
#45545=CARTESIAN_POINT('Ctrl Pts',(373.977082558144,-22.4075431098756,2.36747054783791));
#45546=CARTESIAN_POINT('Ctrl Pts',(374.043977589642,-22.4016694279892,2.27300976161881));
#45547=CARTESIAN_POINT('Ctrl Pts',(374.110786252033,-22.3958033296954,2.17867093503745));
#45548=CARTESIAN_POINT('Ctrl Pts',(374.173523259468,-22.3899372314015,2.08125548936411));
#45549=CARTESIAN_POINT('Ctrl Pts',(374.231894891679,-22.3840711331077,1.9811509957004));
#45550=CARTESIAN_POINT('Ctrl Pts',(374.29020675103,-22.3782110417294,1.88114900956628));
#45551=CARTESIAN_POINT('Ctrl Pts',(374.344161919814,-22.3723509503512,1.77846380735943));
#45552=CARTESIAN_POINT('Ctrl Pts',(374.393509332309,-22.3664908589729,1.67351277712822));
#45553=CARTESIAN_POINT('Ctrl Pts',(374.444637178159,-22.3604193380256,1.56477515899839));
#45554=CARTESIAN_POINT('Ctrl Pts',(374.490818237052,-22.3543478170783,1.45360549414194));
#45555=CARTESIAN_POINT('Ctrl Pts',(374.531824587499,-22.3482762961309,1.34049727713028));
#45556=CARTESIAN_POINT('Ctrl Pts',(374.571357475034,-22.3424229404393,1.23145332726116));
#45557=CARTESIAN_POINT('Ctrl Pts',(374.606080981888,-22.3365695847477,1.12060816350951));
#45558=CARTESIAN_POINT('Ctrl Pts',(374.635839782227,-22.3307162290561,1.00842452534259));
#45559=CARTESIAN_POINT('Ctrl Pts',(374.665594114077,-22.3248637522862,0.896257732320513));
#45560=CARTESIAN_POINT('Ctrl Pts',(374.690385115814,-22.3190112755162,0.782753263736838));
#45561=CARTESIAN_POINT('Ctrl Pts',(374.710107651526,-22.3131587987462,0.668387940778114));
#45562=CARTESIAN_POINT('Ctrl Pts',(374.729831995362,-22.3073057854323,0.554012133024494));
#45563=CARTESIAN_POINT('Ctrl Pts',(374.744486879243,-22.3014527721184,0.438775721166163));
#45564=CARTESIAN_POINT('Ctrl Pts',(374.754018618452,-22.2955997588045,0.323163907441151));
#45565=CARTESIAN_POINT('Ctrl Pts',(374.763553536615,-22.2897447934369,0.207513535719724));
#45566=CARTESIAN_POINT('Ctrl Pts',(374.767961878637,-22.2838898280694,0.0914879247014605));
#45567=CARTESIAN_POINT('Ctrl Pts',(374.767242008615,-22.2780348627018,-0.0244251497270083));
#45568=CARTESIAN_POINT('Ctrl Pts',(374.766521322715,-22.2721732614956,-0.140469596488608));
#45569=CARTESIAN_POINT('Ctrl Pts',(374.760660826619,-22.2663116602893,-0.256400838717909));
#45570=CARTESIAN_POINT('Ctrl Pts',(374.749710957994,-22.2604500590831,-0.37173355393506));
#45571=CARTESIAN_POINT('Ctrl Pts',(374.738753705824,-22.2545845053732,-0.48714403851341));
#45572=CARTESIAN_POINT('Ctrl Pts',(374.722700304747,-22.2487189516633,-0.60195478429041));
#45573=CARTESIAN_POINT('Ctrl Pts',(374.701652489631,-22.2428533979533,-0.715689744265365));
#45574=CARTESIAN_POINT('Ctrl Pts',(374.680573897299,-22.2369792673241,-0.829591013445971));
#45575=CARTESIAN_POINT('Ctrl Pts',(374.654486408507,-22.2311051366948,-0.942412956393667));
#45576=CARTESIAN_POINT('Ctrl Pts',(374.623541859078,-22.2252310060656,-1.05369370950997));
#45577=CARTESIAN_POINT('Ctrl Pts',(374.615716075734,-22.2237454561226,-1.08183627678901));
#45578=CARTESIAN_POINT('Ctrl Pts',(374.607579891213,-22.2222599061797,-1.10988037189724));
#45579=CARTESIAN_POINT('Ctrl Pts',(374.59913624562,-22.2207743562368,-1.13781873436821));
#45580=CARTESIAN_POINT('Ctrl Pts',(374.565751053908,-22.2149006647021,-1.24828376714679));
#45581=CARTESIAN_POINT('Ctrl Pts',(374.527444341865,-22.2090269731674,-1.35746218034026));
#45582=CARTESIAN_POINT('Ctrl Pts',(374.484332535484,-22.2031532816327,-1.46488286879456));
#45583=CARTESIAN_POINT('Ctrl Pts',(374.441276390344,-22.1972871735652,-1.57216486742287));
#45584=CARTESIAN_POINT('Ctrl Pts',(374.393427640688,-22.1914210654976,-1.67769327445173));
#45585=CARTESIAN_POINT('Ctrl Pts',(374.340952738837,-22.18555495743,-1.78101116756819));
#45586=CARTESIAN_POINT('Ctrl Pts',(374.288531570463,-22.1796948561652,-1.88422326478095));
#45587=CARTESIAN_POINT('Ctrl Pts',(374.23149385837,-22.1738347549003,-1.9852289842659));
#45588=CARTESIAN_POINT('Ctrl Pts',(374.170054233665,-22.1679746536355,-2.08359108277054));
#45589=CARTESIAN_POINT('Ctrl Pts',(374.10639803961,-22.1619031363517,-2.18550180993181));
#45590=CARTESIAN_POINT('Ctrl Pts',(374.038016487171,-22.155831619068,-2.28457414669948));
#45591=CARTESIAN_POINT('Ctrl Pts',(373.965200705124,-22.1497601017842,-2.3803490432448));
#45592=CARTESIAN_POINT('Ctrl Pts',(373.895001216564,-22.1439067359873,-2.47268271824497));
#45593=CARTESIAN_POINT('Ctrl Pts',(373.820680932575,-22.1380533701905,-2.5619514741141));
#45594=CARTESIAN_POINT('Ctrl Pts',(373.742544494684,-22.1322000043936,-2.64777393330716));
#45595=CARTESIAN_POINT('Ctrl Pts',(373.664419788648,-22.1263475174548,-2.73358350662222));
#45596=CARTESIAN_POINT('Ctrl Pts',(373.582480346069,-22.1204950305159,-2.8159475067253));
#45597=CARTESIAN_POINT('Ctrl Pts',(373.497069849824,-22.1146425435771,-2.89451909729439));
#45598=CARTESIAN_POINT('Ctrl Pts',(373.411651522551,-22.1087895200416,-2.97309789185331));
#45599=CARTESIAN_POINT('Ctrl Pts',(373.322761813033,-22.102936496506,-3.04788330592844));
#45600=CARTESIAN_POINT('Ctrl Pts',(373.230779338935,-22.0970834729705,-3.11856719464307));
#45601=CARTESIAN_POINT('Ctrl Pts',(373.138766186917,-22.0912284973393,-3.18927465779119));
#45602=CARTESIAN_POINT('Ctrl Pts',(373.04365854665,-22.0853735217081,-3.2558776238942));
#45603=CARTESIAN_POINT('Ctrl Pts',(372.945865414572,-22.0795185460768,-3.31811028993385));
#45604=CARTESIAN_POINT('Ctrl Pts',(372.847961446768,-22.0736569345964,-3.38041348856185));
#45605=CARTESIAN_POINT('Ctrl Pts',(372.747366260951,-22.067795323116,-3.43833627897722));
#45606=CARTESIAN_POINT('Ctrl Pts',(372.644515021486,-22.0619337116356,-3.49165794602192));
#45607=CARTESIAN_POINT('Ctrl Pts',(372.541594428768,-22.0560681476329,-3.54501556820991));
#45608=CARTESIAN_POINT('Ctrl Pts',(372.436415127124,-22.0502025836301,-3.59376571582147));
#45609=CARTESIAN_POINT('Ctrl Pts',(372.329432295354,-22.0443370196274,-3.63773580746802));
#45610=CARTESIAN_POINT('Ctrl Pts',(372.222293028913,-22.0384628787572,-3.68177019397988));
#45611=CARTESIAN_POINT('Ctrl Pts',(372.113345356373,-22.032588737887,-3.72101043559348));
#45612=CARTESIAN_POINT('Ctrl Pts',(372.003059698307,-22.0267145970168,-3.75533374010241));
#45613=CARTESIAN_POINT('Ctrl Pts',(371.975170661334,-22.0252291442863,-3.76401341727225));
#45614=CARTESIAN_POINT('Ctrl Pts',(371.947196111318,-22.0237436915557,-3.77237892031219));
#45615=CARTESIAN_POINT('Ctrl Pts',(371.919143741613,-22.0222582388252,-3.78042878413019));
#45616=CARTESIAN_POINT('Ctrl Pts',(371.808220707546,-22.01638454881,-3.81225908324351));
#45617=CARTESIAN_POINT('Ctrl Pts',(371.695710827206,-22.0105108587948,-3.83925630424263));
#45618=CARTESIAN_POINT('Ctrl Pts',(371.582073089335,-22.0046371687797,-3.86126289015244));
#45619=CARTESIAN_POINT('Ctrl Pts',(371.468582068139,-21.9987710622335,-3.88324106355463));
#45620=CARTESIAN_POINT('Ctrl Pts',(371.353966487155,-21.9929049556873,-3.90024133777612));
#45621=CARTESIAN_POINT('Ctrl Pts',(371.238700536937,-21.9870388491412,-3.91215588200584));
#45622=CARTESIAN_POINT('Ctrl Pts',(371.123552617278,-21.9811787493978,-3.92405822592576));
#45623=CARTESIAN_POINT('Ctrl Pts',(371.007756061563,-21.9753186496544,-3.93088515619298));
#45624=CARTESIAN_POINT('Ctrl Pts',(370.89179464207,-21.969458549911,-3.93257999521229));
#45625=CARTESIAN_POINT('Ctrl Pts',(370.771649617299,-21.9633870320569,-3.93433597989108));
#45626=CARTESIAN_POINT('Ctrl Pts',(370.651328051823,-21.9573155142029,-3.9305824892373));
#45627=CARTESIAN_POINT('Ctrl Pts',(370.531373512831,-21.9512439963488,-3.92131530568809));
#45628=CARTESIAN_POINT('Ctrl Pts',(370.415729018113,-21.9453906320634,-3.91238109804568));
#45629=CARTESIAN_POINT('Ctrl Pts',(370.300426076018,-21.9395372677781,-3.89832263430539));
#45630=CARTESIAN_POINT('Ctrl Pts',(370.185950309952,-21.9336839034927,-3.87918915868136));
#45631=CARTESIAN_POINT('Ctrl Pts',(370.071491731816,-21.927831418059,-3.86005855584751));
#45632=CARTESIAN_POINT('Ctrl Pts',(369.957860490144,-21.9219789326253,-3.83585452433464));
#45633=CARTESIAN_POINT('Ctrl Pts',(369.845534347769,-21.9161264471917,-3.80667784023542));
#45634=CARTESIAN_POINT('Ctrl Pts',(369.733197906395,-21.9102734251533,-3.77749848097424));
#45635=CARTESIAN_POINT('Ctrl Pts',(369.622167202093,-21.9044204031149,-3.74334566664515));
#45636=CARTESIAN_POINT('Ctrl Pts',(369.512906423454,-21.8985673810765,-3.70437050431956));
#45637=CARTESIAN_POINT('Ctrl Pts',(369.403609204057,-21.8927124069327,-3.66538234296141));
#45638=CARTESIAN_POINT('Ctrl Pts',(369.29608347304,-21.886857432789,-3.62156877420024));
#45639=CARTESIAN_POINT('Ctrl Pts',(369.190774307414,-21.8810024586452,-3.57312938654996));
#45640=CARTESIAN_POINT('Ctrl Pts',(369.085345787194,-21.8751408486302,-3.52463509899225));
#45641=CARTESIAN_POINT('Ctrl Pts',(368.982139222108,-21.8692792386152,-3.47150470101704));
#45642=CARTESIAN_POINT('Ctrl Pts',(368.881575987362,-21.8634176286002,-3.41398421280908));
#45643=CARTESIAN_POINT('Ctrl Pts',(368.780944941972,-21.8575520660518,-3.35642493804724));
#45644=CARTESIAN_POINT('Ctrl Pts',(368.682961124448,-21.8516865035034,-3.29446989873784));
#45645=CARTESIAN_POINT('Ctrl Pts',(368.588016312816,-21.8458209409549,-3.2284080271181));
#45646=CARTESIAN_POINT('Ctrl Pts',(368.492932668519,-21.8399468015116,-3.16224955679558));
#45647=CARTESIAN_POINT('Ctrl Pts',(368.40089722587,-21.8340726620682,-3.09197251906454));
#45648=CARTESIAN_POINT('Ctrl Pts',(368.312268187356,-21.8281985226248,-3.01790564512828));
#45649=CARTESIAN_POINT('Ctrl Pts',(368.289855454484,-21.8267130555544,-2.9991754288466));
#45650=CARTESIAN_POINT('Ctrl Pts',(368.267660371344,-21.8252275884839,-2.980203033827));
#45651=CARTESIAN_POINT('Ctrl Pts',(368.24568833986,-21.8237421214135,-2.96099413078456));
#45652=CARTESIAN_POINT('Ctrl Pts',(368.160079295419,-21.8179543354027,-2.88615099052049));
#45653=CARTESIAN_POINT('Ctrl Pts',(368.077556050416,-21.812166549392,-2.80744951203021));
#45654=CARTESIAN_POINT('Ctrl Pts',(367.998494309132,-21.8063787633812,-2.72517776058249));
#45655=CARTESIAN_POINT('Ctrl Pts',(367.919535386016,-21.800598504267,-2.64301300185433));
#45656=CARTESIAN_POINT('Ctrl Pts',(367.844029312231,-21.7948182451529,-2.55728750250962));
#45657=CARTESIAN_POINT('Ctrl Pts',(367.772318758495,-21.7890379860387,-2.46832950472104));
#45658=CARTESIAN_POINT('Ctrl Pts',(367.700688942408,-21.7832642348164,-2.37947166317517));
#45659=CARTESIAN_POINT('Ctrl Pts',(367.632846412028,-21.7774904835942,-2.28738889234054));
#45660=CARTESIAN_POINT('Ctrl Pts',(367.569096284465,-21.7717167323719,-2.19244546269971));
#45661=CARTESIAN_POINT('Ctrl Pts',(367.505385908326,-21.7659465813751,-2.09756123508105));
#45662=CARTESIAN_POINT('Ctrl Pts',(367.445763102122,-21.7601764303783,-1.9998202451201));
#45663=CARTESIAN_POINT('Ctrl Pts',(367.390491709746,-21.7544062793814,-1.89961851262268));
#45664=CARTESIAN_POINT('Ctrl Pts',(367.335240498746,-21.7486382352536,-1.79945336702284));
#45665=CARTESIAN_POINT('Ctrl Pts',(367.284337749468,-21.7428701911257,-1.69682963741078));
#45666=CARTESIAN_POINT('Ctrl Pts',(367.238002619847,-21.7371021469979,-1.59217013606627));
#45667=CARTESIAN_POINT('Ctrl Pts',(367.191672436426,-21.7313347185994,-1.48752180695413));
#45668=CARTESIAN_POINT('Ctrl Pts',(367.149909074613,-21.7255672902009,-1.38083852842445));
#45669=CARTESIAN_POINT('Ctrl Pts',(367.112884205147,-21.7197998618025,-1.27256457712676));
#45670=CARTESIAN_POINT('Ctrl Pts',(367.075835587684,-21.7140287341372,-1.16422117819842));
#45671=CARTESIAN_POINT('Ctrl Pts',(367.043531673585,-21.7082576064719,-1.05428547188577));
#45672=CARTESIAN_POINT('Ctrl Pts',(367.016094664113,-21.7024864788066,-0.943218255833407));
#45673=CARTESIAN_POINT('Ctrl Pts',(366.988648916011,-21.6967135130491,-0.832115665104043));
#45674=CARTESIAN_POINT('Ctrl Pts',(366.966073245815,-21.6909405472917,-0.719881264654684));
#45675=CARTESIAN_POINT('Ctrl Pts',(366.948438634091,-21.6851675815342,-0.606985744735938));
#45676=CARTESIAN_POINT('Ctrl Pts',(366.930781460406,-21.6793872297663,-0.493945784760898));
#45677=CARTESIAN_POINT('Ctrl Pts',(366.918078021018,-21.6736068779983,-0.380243439605345));
#45678=CARTESIAN_POINT('Ctrl Pts',(366.910347366434,-21.6678265262303,-0.26635431064342));
#45679=CARTESIAN_POINT('Ctrl Pts',(366.904256389624,-21.6632721915121,-0.176621153410323));
#45680=CARTESIAN_POINT('Ctrl Pts',(366.901251405202,-21.6587178567939,-0.086772175312987));
#45681=CARTESIAN_POINT('Ctrl Pts',(366.901318968034,-21.6541635220757,0.00296126550371329));
#45682=CARTESIAN_POINT('',(366.901319018817,-20.4041635219962,-0.00302796160370392));
#45683=CARTESIAN_POINT('Ctrl Pts',(366.901318968035,-21.654163522035,0.00296126630494888));
#45684=CARTESIAN_POINT('Ctrl Pts',(366.901462062567,-21.6445176826906,0.193011933961706));
#45685=CARTESIAN_POINT('Ctrl Pts',(366.915382244365,-21.6348718433462,0.382553237646774));
#45686=CARTESIAN_POINT('Ctrl Pts',(366.942850574199,-21.6252260040018,0.570062642413103));
#45687=CARTESIAN_POINT('Ctrl Pts',(366.959577003038,-21.6193523143247,0.684243691444853));
#45688=CARTESIAN_POINT('Ctrl Pts',(366.981360893976,-21.6134786246476,0.797878119509283));
#45689=CARTESIAN_POINT('Ctrl Pts',(367.008156582755,-21.6076049349706,0.910482801795613));
#45690=CARTESIAN_POINT('Ctrl Pts',(367.034917675798,-21.6017388287755,1.02294210091921));
#45691=CARTESIAN_POINT('Ctrl Pts',(367.066677603814,-21.5958727225804,1.13437389994923));
#45692=CARTESIAN_POINT('Ctrl Pts',(367.103339131433,-21.5900066163853,1.24430172287202));
#45693=CARTESIAN_POINT('Ctrl Pts',(367.139963118132,-21.5841465170056,1.35411698115575));
#45694=CARTESIAN_POINT('Ctrl Pts',(367.181478590949,-21.5782864176258,1.4624309370287));
#45695=CARTESIAN_POINT('Ctrl Pts',(367.227737760038,-21.572426318246,1.56877947189326));
#45696=CARTESIAN_POINT('Ctrl Pts',(367.275665851171,-21.5663548002604,1.67896481182259));
#45697=CARTESIAN_POINT('Ctrl Pts',(367.328686279273,-21.5602832822747,1.78703979826397));
#45698=CARTESIAN_POINT('Ctrl Pts',(367.386578809746,-21.554211764289,1.89250746050753));
#45699=CARTESIAN_POINT('Ctrl Pts',(367.442391219151,-21.5483584003963,1.99418559231555));
#45700=CARTESIAN_POINT('Ctrl Pts',(367.502731424096,-21.5425050365037,2.09344014831502));
#45701=CARTESIAN_POINT('Ctrl Pts',(367.567354368616,-21.536651672611,2.18984898799886));
#45702=CARTESIAN_POINT('Ctrl Pts',(367.631967610231,-21.5307991875801,2.28624335223775));
#45703=CARTESIAN_POINT('Ctrl Pts',(367.700862082847,-21.5249467025493,2.37979250665416));
#45704=CARTESIAN_POINT('Ctrl Pts',(367.773749021348,-21.5190942175184,2.47010271554592));
#45705=CARTESIAN_POINT('Ctrl Pts',(367.84664264261,-21.5132411958926,2.56042120468205));
#45706=CARTESIAN_POINT('Ctrl Pts',(367.923529197954,-21.5073881742667,2.64749983643114));
#45707=CARTESIAN_POINT('Ctrl Pts',(368.004079662593,-21.5015351526409,2.7309779904447));
#45708=CARTESIAN_POINT('Ctrl Pts',(368.084656992372,-21.4956801789189,2.81448398603912));
#45709=CARTESIAN_POINT('Ctrl Pts',(368.168900374585,-21.489825205197,2.89438681895903));
#45710=CARTESIAN_POINT('Ctrl Pts',(368.25644449253,-21.4839702314751,2.97036326671102));
#45711=CARTESIAN_POINT('Ctrl Pts',(368.34408783047,-21.4781086218938,3.04642582399143));
#45712=CARTESIAN_POINT('Ctrl Pts',(368.435039058674,-21.4722470123125,3.11855284312117));
#45713=CARTESIAN_POINT('Ctrl Pts',(368.528900328275,-21.4663854027312,3.18646183652911));
#45714=CARTESIAN_POINT('Ctrl Pts',(368.622824889213,-21.4605198406238,3.25441662146577));
#45715=CARTESIAN_POINT('Ctrl Pts',(368.719663054588,-21.4546542785165,3.31814749059416));
#45716=CARTESIAN_POINT('Ctrl Pts',(368.818990080293,-21.4487887164091,3.37741661150248));
#45717=CARTESIAN_POINT('Ctrl Pts',(368.91846234642,-21.4429145774144,3.4367723983722));
#45718=CARTESIAN_POINT('Ctrl Pts',(369.020430373649,-21.4370404384196,3.49165322137277));
#45719=CARTESIAN_POINT('Ctrl Pts',(369.12444699891,-21.4311662994248,3.54186824452422));
#45720=CARTESIAN_POINT('Ctrl Pts',(369.15075105381,-21.4296808284799,3.55456677922894));
#45721=CARTESIAN_POINT('Ctrl Pts',(369.177186030337,-21.4281953575351,3.56696718210002));
#45722=CARTESIAN_POINT('Ctrl Pts',(369.20374453511,-21.4267098865903,3.57906686920699));
#45723=CARTESIAN_POINT('Ctrl Pts',(369.308759318052,-21.4208361971574,3.62691015052295));
#45724=CARTESIAN_POINT('Ctrl Pts',(369.416056469331,-21.4149625077246,3.67020727878341));
#45725=CARTESIAN_POINT('Ctrl Pts',(369.525205260397,-21.4090888182918,3.70873471945656));
#45726=CARTESIAN_POINT('Ctrl Pts',(369.634213130147,-21.4032227123424,3.74721241759396));
#45727=CARTESIAN_POINT('Ctrl Pts',(369.745067499455,-21.397356606393,3.78093253835209));
#45728=CARTESIAN_POINT('Ctrl Pts',(369.85731526961,-21.3914905004436,3.80971848718675));
#45729=CARTESIAN_POINT('Ctrl Pts',(369.969448099506,-21.3856304013105,3.83847495958339));
#45730=CARTESIAN_POINT('Ctrl Pts',(370.082971094361,-21.3797703021775,3.86230720793355));
#45731=CARTESIAN_POINT('Ctrl Pts',(370.197414133432,-21.3739102030444,3.88108781808859));
#45732=CARTESIAN_POINT('Ctrl Pts',(370.315986015037,-21.3678386849667,3.90054598961064));
#45733=CARTESIAN_POINT('Ctrl Pts',(370.435545154513,-21.3617671668889,3.91458098755703));
#45734=CARTESIAN_POINT('Ctrl Pts',(370.555554552153,-21.3556956488112,3.92310846421255));
#45735=CARTESIAN_POINT('Ctrl Pts',(370.67125191749,-21.3498422851663,3.93132954190662));
#45736=CARTESIAN_POINT('Ctrl Pts',(370.78736729414,-21.3439889215214,3.93443203439455));
#45737=CARTESIAN_POINT('Ctrl Pts',(370.903413106987,-21.3381355578765,3.932393017732));
#45738=CARTESIAN_POINT('Ctrl Pts',(371.019441495968,-21.3322830730934,3.93035430722056));
#45739=CARTESIAN_POINT('Ctrl Pts',(371.135399928944,-21.3264305883103,3.92317562979976));
#45740=CARTESIAN_POINT('Ctrl Pts',(371.250801004433,-21.3205781035271,3.91088618918516));
#45741=CARTESIAN_POINT('Ctrl Pts',(371.366212660671,-21.3147250821487,3.89859562179172));
#45742=CARTESIAN_POINT('Ctrl Pts',(371.48106644699,-21.3088720607703,3.88119340344505));
#45743=CARTESIAN_POINT('Ctrl Pts',(371.59488096385,-21.3030190393919,3.85876052052402));
#45744=CARTESIAN_POINT('Ctrl Pts',(371.708733440068,-21.2971640659168,3.83632015579964));
#45745=CARTESIAN_POINT('Ctrl Pts',(371.821545552466,-21.2913090924418,3.80884587007231));
#45746=CARTESIAN_POINT('Ctrl Pts',(371.932847653023,-21.2854541189668,3.77646941983565));
#45747=CARTESIAN_POINT('Ctrl Pts',(372.044275900236,-21.2795925096302,3.74405627504493));
#45748=CARTESIAN_POINT('Ctrl Pts',(372.154190322822,-21.2737309002936,3.70672999181425));
#45749=CARTESIAN_POINT('Ctrl Pts',(372.262137866638,-21.267869290957,3.66467174645908));
#45750=CARTESIAN_POINT('Ctrl Pts',(372.370158200288,-21.2620037290935,3.62258514091495));
#45751=CARTESIAN_POINT('Ctrl Pts',(372.47620863724,-21.25613816723,3.57576038612259));
#45752=CARTESIAN_POINT('Ctrl Pts',(372.579859067264,-21.2502726053664,3.52442546666655));
#45753=CARTESIAN_POINT('Ctrl Pts',(372.68366105965,-21.2443984666122,3.47301548296206));
#45754=CARTESIAN_POINT('Ctrl Pts',(372.785055680867,-21.238524327858,3.41708237148672));
#45755=CARTESIAN_POINT('Ctrl Pts',(372.883640158626,-21.2326501891038,3.35689843286626));
#45756=CARTESIAN_POINT('Ctrl Pts',(372.908570555483,-21.2311647157954,3.3416789022838));
#45757=CARTESIAN_POINT('Ctrl Pts',(372.933321403113,-21.229679242487,3.32618773626215));
#45758=CARTESIAN_POINT('Ctrl Pts',(372.957886522166,-21.2281937691786,3.310429746768));
#45759=CARTESIAN_POINT('Ctrl Pts',(373.055019116987,-21.2223200798767,3.24812130016971));
#45760=CARTESIAN_POINT('Ctrl Pts',(373.14956883754,-21.2164463905749,3.18143044890682));
#45761=CARTESIAN_POINT('Ctrl Pts',(373.241114343966,-21.2105727012731,3.11059795733082));
#45762=CARTESIAN_POINT('Ctrl Pts',(373.332541656519,-21.2047065954575,3.03985691717411));
#45763=CARTESIAN_POINT('Ctrl Pts',(373.420972144683,-21.1988404896419,2.96498512114153));
#45764=CARTESIAN_POINT('Ctrl Pts',(373.506011785558,-21.1929743838263,2.88626757802014));
#45765=CARTESIAN_POINT('Ctrl Pts',(373.590964346904,-21.1871142848296,2.8076306406784));
#45766=CARTESIAN_POINT('Ctrl Pts',(373.672532666037,-21.181254185833,2.72515606823215));
#45767=CARTESIAN_POINT('Ctrl Pts',(373.750354818921,-21.1753940868364,2.6391698343777));
#45768=CARTESIAN_POINT('Ctrl Pts',(373.830984619247,-21.1693225687085,2.55008141148618));
#45769=CARTESIAN_POINT('Ctrl Pts',(373.907592486155,-21.1632510505806,2.4572234339288));
#45770=CARTESIAN_POINT('Ctrl Pts',(373.97981642891,-21.1571795324527,2.3610014210833));
#45771=CARTESIAN_POINT('Ctrl Pts',(374.049445306176,-21.15132616895,2.26823674406441));
#45772=CARTESIAN_POINT('Ctrl Pts',(374.114999604277,-21.1454728054472,2.17234597520425));
#45773=CARTESIAN_POINT('Ctrl Pts',(374.176195740932,-21.1396194419445,2.07372640038332));
#45774=CARTESIAN_POINT('Ctrl Pts',(374.237382689185,-21.1337669573054,1.97512163297348));
#45775=CARTESIAN_POINT('Ctrl Pts',(374.294212559335,-21.1279144726664,1.87378922523877));
#45776=CARTESIAN_POINT('Ctrl Pts',(374.346445666511,-21.1220619880273,1.77015457605792));
#45777=CARTESIAN_POINT('Ctrl Pts',(374.398683562755,-21.1162089667947,1.66651042498352));
#45778=CARTESIAN_POINT('Ctrl Pts',(374.446323672241,-21.110355945562,1.56056398180142));
#45779=CARTESIAN_POINT('Ctrl Pts',(374.489173077186,-21.1045029243294,1.45276367378729));
#45780=CARTESIAN_POINT('Ctrl Pts',(374.532036773231,-21.0986479510017,1.34492741229908));
#45781=CARTESIAN_POINT('Ctrl Pts',(374.570106435071,-21.092792977674,1.23523644023758));
#45782=CARTESIAN_POINT('Ctrl Pts',(374.603238178056,-21.0869380043463,1.12415683294903));
#45783=CARTESIAN_POINT('Ctrl Pts',(374.636407471615,-21.0810763951587,1.01295133119911));
#45784=CARTESIAN_POINT('Ctrl Pts',(374.664627557895,-21.0752147859711,0.90035444906362));
#45785=CARTESIAN_POINT('Ctrl Pts',(374.68780507581,-21.0693531767835,0.786845108878447));
#45786=CARTESIAN_POINT('Ctrl Pts',(374.710998222494,-21.0634876150701,0.67325922851727));
#45787=CARTESIAN_POINT('Ctrl Pts',(374.729141965679,-21.0576220533567,0.55876007199698));
#45788=CARTESIAN_POINT('Ctrl Pts',(374.742194715749,-21.0517564916432,0.44383265691022));
#45789=CARTESIAN_POINT('Ctrl Pts',(374.755266552142,-21.0458823530396,0.328737189747755));
#45790=CARTESIAN_POINT('Ctrl Pts',(374.763232510194,-21.040008214436,0.213212624824722));
#45791=CARTESIAN_POINT('Ctrl Pts',(374.766103059565,-21.0341340758323,0.0977450315970521));
#45792=CARTESIAN_POINT('Ctrl Pts',(374.766828975093,-21.0326486011438,0.0685451439789517));
#45793=CARTESIAN_POINT('Ctrl Pts',(374.76722929728,-21.0311631264554,0.0393488768321781));
#45794=CARTESIAN_POINT('Ctrl Pts',(374.767304719775,-21.0296776517669,0.0101640313471547));
#45795=CARTESIAN_POINT('Ctrl Pts',(374.767602946543,-21.0238039623397,-0.105235254610351));
#45796=CARTESIAN_POINT('Ctrl Pts',(374.762818403329,-21.0179302729126,-0.220839874219748));
#45797=CARTESIAN_POINT('Ctrl Pts',(374.752924993982,-21.0120565834854,-0.336165251624106));
#45798=CARTESIAN_POINT('Ctrl Pts',(374.743044357955,-21.0061904775427,-0.451341733140617));
#45799=CARTESIAN_POINT('Ctrl Pts',(374.728068008118,-21.0003243715999,-0.566239281550414));
#45800=CARTESIAN_POINT('Ctrl Pts',(374.708021836049,-20.9944582656572,-0.680372290326572));
#45801=CARTESIAN_POINT('Ctrl Pts',(374.687996191004,-20.9885981665318,-0.79438842836331));
#45802=CARTESIAN_POINT('Ctrl Pts',(374.662911120963,-20.9827380674064,-0.907641179479606));
#45803=CARTESIAN_POINT('Ctrl Pts',(374.632844341741,-20.9768779682811,-1.01964970261153));
#45804=CARTESIAN_POINT('Ctrl Pts',(374.601692821987,-20.9708064502008,-1.13569923672116));
#45805=CARTESIAN_POINT('Ctrl Pts',(374.565193387622,-20.9647349321206,-1.25041261998707));
#45806=CARTESIAN_POINT('Ctrl Pts',(374.523490561151,-20.9586634140403,-1.36326583287554));
#45807=CARTESIAN_POINT('Ctrl Pts',(374.48328615021,-20.9528100504056,-1.47206414058933));
#45808=CARTESIAN_POINT('Ctrl Pts',(374.438245991465,-20.9469566867709,-1.57913323143716));
#45809=CARTESIAN_POINT('Ctrl Pts',(374.388550194724,-20.9411033231361,-1.6840194365367));
#45810=CARTESIAN_POINT('Ctrl Pts',(374.338861859639,-20.9352508383641,-1.78888989332864));
#45811=CARTESIAN_POINT('Ctrl Pts',(374.28451945334,-20.929398353592,-1.89157774281137));
#45812=CARTESIAN_POINT('Ctrl Pts',(374.225750506413,-20.92354586882,-1.99165096311623));
#45813=CARTESIAN_POINT('Ctrl Pts',(374.166976171161,-20.9176928474535,-2.09173335879387));
#45814=CARTESIAN_POINT('Ctrl Pts',(374.103774697706,-20.9118398260871,-2.18920029246472));
#45815=CARTESIAN_POINT('Ctrl Pts',(374.036418320457,-20.9059868047206,-2.28364655709858));
#45816=CARTESIAN_POINT('Ctrl Pts',(373.969039478554,-20.9001318312584,-2.37812432138689));
#45817=CARTESIAN_POINT('Ctrl Pts',(373.897503217131,-20.8942768577962,-2.46957907718035));
#45818=CARTESIAN_POINT('Ctrl Pts',(373.822123181737,-20.8884218843341,-2.55763725319067));
#45819=CARTESIAN_POINT('Ctrl Pts',(373.746657712757,-20.8825602750116,-2.64579523183126));
#45820=CARTESIAN_POINT('Ctrl Pts',(373.667340043466,-20.8766986656891,-2.73054863311337));
#45821=CARTESIAN_POINT('Ctrl Pts',(373.584522004144,-20.8708370563667,-2.81155937662081));
#45822=CARTESIAN_POINT('Ctrl Pts',(373.501648120009,-20.864971494518,-2.89262474626734));
#45823=CARTESIAN_POINT('Ctrl Pts',(373.415269472988,-20.8591059326693,-2.96994215802653));
#45824=CARTESIAN_POINT('Ctrl Pts',(373.325771081059,-20.8532403708207,-3.04321373115855));
#45825=CARTESIAN_POINT('Ctrl Pts',(373.236141820534,-20.8473662320823,-3.11659244529731));
#45826=CARTESIAN_POINT('Ctrl Pts',(373.143384040499,-20.8414920933439,-3.18591326757319));
#45827=CARTESIAN_POINT('Ctrl Pts',(373.047911864646,-20.8356179546056,-3.25092149283786));
#45828=CARTESIAN_POINT('Ctrl Pts',(373.023768516049,-20.8341324811888,-3.26736100759955));
#45829=CARTESIAN_POINT('Ctrl Pts',(372.999451702815,-20.832647007772,-3.28352496149948));
#45830=CARTESIAN_POINT('Ctrl Pts',(372.974968356363,-20.8311615343553,-3.29940970832831));
#45831=CARTESIAN_POINT('Ctrl Pts',(372.878159103019,-20.8252878449632,-3.3622193607201));
#45832=CARTESIAN_POINT('Ctrl Pts',(372.778421888268,-20.8194141555711,-3.42086923500197));
#45833=CARTESIAN_POINT('Ctrl Pts',(372.676149758024,-20.8135404661791,-3.47507470919122));
#45834=CARTESIAN_POINT('Ctrl Pts',(372.574009670706,-20.8076743602717,-3.52921019902198));
#45835=CARTESIAN_POINT('Ctrl Pts',(372.469341538159,-20.8018082543643,-3.57891250832556));
#45836=CARTESIAN_POINT('Ctrl Pts',(372.36256745542,-20.795942148457,-3.62394014208116));
#45837=CARTESIAN_POINT('Ctrl Pts',(372.25590270798,-20.7900820493672,-3.66892166811432));
#45838=CARTESIAN_POINT('Ctrl Pts',(372.147136678156,-20.7842219502774,-3.70923788037558));
#45839=CARTESIAN_POINT('Ctrl Pts',(372.036715550944,-20.7783618511876,-3.74469341555734));
#45840=CARTESIAN_POINT('Ctrl Pts',(371.922310681417,-20.7722903330941,-3.78142810554691));
#45841=CARTESIAN_POINT('Ctrl Pts',(371.806129434527,-20.7662188150006,-3.81294456082372));
#45842=CARTESIAN_POINT('Ctrl Pts',(371.688690495029,-20.7601472969071,-3.83908014880324));
#45843=CARTESIAN_POINT('Ctrl Pts',(371.575471230432,-20.7542939333084,-3.86427666423074));
#45844=CARTESIAN_POINT('Ctrl Pts',(371.461083535459,-20.7484405697096,-3.88447223798209));
#45845=CARTESIAN_POINT('Ctrl Pts',(371.346006270866,-20.7425872061109,-3.89957227952645));
#45846=CARTESIAN_POINT('Ctrl Pts',(371.230946284735,-20.7367347213749,-3.91467005385065));
#45847=CARTESIAN_POINT('Ctrl Pts',(371.115197344378,-20.7308822366389,-3.92467376349189));
#45848=CARTESIAN_POINT('Ctrl Pts',(370.999245827649,-20.7250297519029,-3.92954040102045));
#45849=CARTESIAN_POINT('Ctrl Pts',(370.883283679722,-20.7191767305725,-3.9344074847544));
#45850=CARTESIAN_POINT('Ctrl Pts',(370.767119331304,-20.7133237092421,-3.93413654274455));
#45851=CARTESIAN_POINT('Ctrl Pts',(370.651240861902,-20.7074706879118,-3.92873666911497));
#45852=CARTESIAN_POINT('Ctrl Pts',(370.535323744791,-20.7016157144856,-3.92333499452317));
#45853=CARTESIAN_POINT('Ctrl Pts',(370.41969310876,-20.6957607410595,-3.91280100608526));
#45854=CARTESIAN_POINT('Ctrl Pts',(370.304832898927,-20.6899057676334,-3.89719574606833));
#45855=CARTESIAN_POINT('Ctrl Pts',(370.189842509796,-20.6840441583469,-3.88157279949325));
#45856=CARTESIAN_POINT('Ctrl Pts',(370.075624699288,-20.6781825490603,-3.86086716505694));
#45857=CARTESIAN_POINT('Ctrl Pts',(369.962654289566,-20.6723209397737,-3.83519121189423));
#45858=CARTESIAN_POINT('Ctrl Pts',(369.849607703065,-20.6664553779609,-3.80949794524739));
#45859=CARTESIAN_POINT('Ctrl Pts',(369.737810589667,-20.660589816148,-3.77882779528158));
#45860=CARTESIAN_POINT('Ctrl Pts',(369.627721982798,-20.6547242543352,-3.74334281164189));
#45861=CARTESIAN_POINT('Ctrl Pts',(369.517472399383,-20.6488501156323,-3.70780594025235));
#45862=CARTESIAN_POINT('Ctrl Pts',(369.408936694131,-20.6429759769294,-3.66744032764705));
#45863=CARTESIAN_POINT('Ctrl Pts',(369.302553398164,-20.6371018382264,-3.62245588713179));
#45864=CARTESIAN_POINT('Ctrl Pts',(369.275650799715,-20.6356163644655,-3.6110800566627));
#45865=CARTESIAN_POINT('Ctrl Pts',(369.248885720453,-20.6341308907045,-3.59940907819713));
#45866=CARTESIAN_POINT('Ctrl Pts',(369.222264981911,-20.6326454169436,-3.58744679961843));
#45867=CARTESIAN_POINT('Ctrl Pts',(369.117004321368,-20.6267717275623,-3.54014693441));
#45868=CARTESIAN_POINT('Ctrl Pts',(369.013651879269,-20.6208980381811,-3.48813162499381));
#45869=CARTESIAN_POINT('Ctrl Pts',(368.912659899626,-20.6150243487998,-3.43157685465056));
#45870=CARTESIAN_POINT('Ctrl Pts',(368.81179831012,-20.6091582429035,-3.37509510183053));
#45871=CARTESIAN_POINT('Ctrl Pts',(368.713291479616,-20.6032921370072,-3.31408574345183));
#45872=CARTESIAN_POINT('Ctrl Pts',(368.61757116001,-20.5974260311109,-3.24877255253829));
#45873=CARTESIAN_POINT('Ctrl Pts',(368.521948856795,-20.5915659320324,-3.18352624150192));
#45874=CARTESIAN_POINT('Ctrl Pts',(368.429107728167,-20.585705832954,-3.1139850954336));
#45875=CARTESIAN_POINT('Ctrl Pts',(368.339453820575,-20.5798457338755,-3.0404181387758));
#45876=CARTESIAN_POINT('Ctrl Pts',(368.246565404325,-20.5737742157779,-2.96419705398559));
#45877=CARTESIAN_POINT('Ctrl Pts',(368.157098920584,-20.5677026976802,-2.88365441067547));
#45878=CARTESIAN_POINT('Ctrl Pts',(368.071472214734,-20.5616311795826,-2.79913789904588));
#45879=CARTESIAN_POINT('Ctrl Pts',(367.988922145043,-20.5557778159957,-2.71765813340816));
#45880=CARTESIAN_POINT('Ctrl Pts',(367.909940988646,-20.5499244524088,-2.63248546851741));
#45881=CARTESIAN_POINT('Ctrl Pts',(367.83486782568,-20.544071088822,-2.54397101639699));
#45882=CARTESIAN_POINT('Ctrl Pts',(367.759805934698,-20.538218604098,-2.45546985442505));
#45883=CARTESIAN_POINT('Ctrl Pts',(367.688651137584,-20.5323661193741,-2.36362821790201));
#45884=CARTESIAN_POINT('Ctrl Pts',(367.621703243882,-20.5265136346502,-2.26883149921726));
#45885=CARTESIAN_POINT('Ctrl Pts',(367.554749211957,-20.520660613332,-2.1740260889475));
#45886=CARTESIAN_POINT('Ctrl Pts',(367.492003088555,-20.5148075920139,-2.07626539540011));
#45887=CARTESIAN_POINT('Ctrl Pts',(367.433721824355,-20.5089545706958,-1.97596448562208));
#45888=CARTESIAN_POINT('Ctrl Pts',(367.375421122228,-20.5030995972821,-1.87563012355448));
#45889=CARTESIAN_POINT('Ctrl Pts',(367.321588447799,-20.4972446238683,-1.77275421764004));
#45890=CARTESIAN_POINT('Ctrl Pts',(367.272434858023,-20.4913896504546,-1.66777652234879));
#45891=CARTESIAN_POINT('Ctrl Pts',(367.223225558967,-20.4855280411807,-1.5626798483248));
#45892=CARTESIAN_POINT('Ctrl Pts',(367.178706104605,-20.4796664319067,-1.4554770047493));
#45893=CARTESIAN_POINT('Ctrl Pts',(367.139039475882,-20.4738048226327,-1.34662790478673));
#45894=CARTESIAN_POINT('Ctrl Pts',(367.099346099661,-20.4679392608326,-1.23770540707748));
#45895=CARTESIAN_POINT('Ctrl Pts',(367.06451218878,-20.4620736990324,-1.12713483563783));
#45896=CARTESIAN_POINT('Ctrl Pts',(367.034650418039,-20.4562081372323,-1.01538976851012));
#45897=CARTESIAN_POINT('Ctrl Pts',(367.004744982065,-20.4503339985422,-0.903481302686307));
#45898=CARTESIAN_POINT('Ctrl Pts',(366.979826284859,-20.4444598598521,-0.790395315589137));
#45899=CARTESIAN_POINT('Ctrl Pts',(366.959955666518,-20.4385857211619,-0.676614104360887));
#45900=CARTESIAN_POINT('Ctrl Pts',(366.954930711198,-20.4371002472853,-0.647840691635513));
#45901=CARTESIAN_POINT('Ctrl Pts',(366.950228321566,-20.4356147734086,-0.61902283481969));
#45902=CARTESIAN_POINT('Ctrl Pts',(366.945848962233,-20.4341292995319,-0.590168352075471));
#45903=CARTESIAN_POINT('Ctrl Pts',(366.916401365424,-20.4241407070329,-0.396145640250567));
#45904=CARTESIAN_POINT('Ctrl Pts',(366.901470561325,-20.414152114534,-0.199865450662548));
#45905=CARTESIAN_POINT('Ctrl Pts',(366.901319018817,-20.404163522035,-0.00302796236916899));
#45906=CARTESIAN_POINT('',(366.901318010803,-19.1541635220604,-0.00111333548553648));
#45907=CARTESIAN_POINT('Ctrl Pts',(366.901319018817,-20.4041635219962,-0.0030279616036751));
#45908=CARTESIAN_POINT('Ctrl Pts',(366.901231322656,-20.3983832201483,0.11087998863384));
#45909=CARTESIAN_POINT('Ctrl Pts',(366.90609632481,-20.3926029183004,0.224972287379443));
#45910=CARTESIAN_POINT('Ctrl Pts',(366.915935485385,-20.3868226164526,0.338775175314392));
#45911=CARTESIAN_POINT('Ctrl Pts',(366.925764417016,-20.3810483238963,0.452459752000542));
#45912=CARTESIAN_POINT('Ctrl Pts',(366.940557191422,-20.3752740313399,0.565855093955342));
#45913=CARTESIAN_POINT('Ctrl Pts',(366.960283225851,-20.3694997387836,0.678487071293573));
#45914=CARTESIAN_POINT('Ctrl Pts',(366.979994813569,-20.3637296751327,0.791036560608706));
#45915=CARTESIAN_POINT('Ctrl Pts',(367.004632405412,-20.3579596114818,0.902823378231744));
#45916=CARTESIAN_POINT('Ctrl Pts',(367.034113639211,-20.3521895478308,1.01337896751405));
#45917=CARTESIAN_POINT('Ctrl Pts',(367.063583643743,-20.3464216819709,1.1238924466753));
#45918=CARTESIAN_POINT('Ctrl Pts',(367.097893515297,-20.340653816111,1.23317521771722));
#45919=CARTESIAN_POINT('Ctrl Pts',(367.136910043896,-20.3348859502511,1.34077011136149));
#45920=CARTESIAN_POINT('Ctrl Pts',(367.175921796339,-20.3291187904567,1.44835183392218));
#45921=CARTESIAN_POINT('Ctrl Pts',(367.219638915172,-20.3233516306623,1.55424568894855));
#45922=CARTESIAN_POINT('Ctrl Pts',(367.267878980043,-20.3175844708678,1.65801168990651));
#45923=CARTESIAN_POINT('Ctrl Pts',(367.316125609432,-20.3118165262773,1.76179181136108));
#45924=CARTESIAN_POINT('Ctrl Pts',(367.368896227151,-20.3060485816867,1.86344311711508));
#45925=CARTESIAN_POINT('Ctrl Pts',(367.425961516331,-20.3002806370961,1.96254836392981));
#45926=CARTESIAN_POINT('Ctrl Pts',(367.483083981629,-20.2945069133588,2.06175290846663));
#45927=CARTESIAN_POINT('Ctrl Pts',(367.54450949664,-20.2887331896216,2.15840593060013));
#45928=CARTESIAN_POINT('Ctrl Pts',(367.609964294208,-20.2829594658843,2.25211747616834));
#45929=CARTESIAN_POINT('Ctrl Pts',(367.675453624201,-20.277182696065,2.34587846176203));
#45930=CARTESIAN_POINT('Ctrl Pts',(367.744976208484,-20.2714059262458,2.43669454396946));
#45931=CARTESIAN_POINT('Ctrl Pts',(367.818217922316,-20.2656291564266,2.52420882788628));
#45932=CARTESIAN_POINT('Ctrl Pts',(367.89157503594,-20.2598432847172,2.61186099948479));
#45933=CARTESIAN_POINT('Ctrl Pts',(367.968662692478,-20.2540574130078,2.69620067064413));
#45934=CARTESIAN_POINT('Ctrl Pts',(368.049129715814,-20.2482715412984,2.77690763966548));
#45935=CARTESIAN_POINT('Ctrl Pts',(368.107811768382,-20.2440520882391,2.83576467702415));
#45936=CARTESIAN_POINT('Ctrl Pts',(368.168290314052,-20.2398326351797,2.89269051561767));
#45937=CARTESIAN_POINT('Ctrl Pts',(368.230418786639,-20.2356131821203,2.94757504587047));
#45938=CARTESIAN_POINT('Ctrl Pts',(368.316904723356,-20.2297394927299,3.02397705307496));
#45939=CARTESIAN_POINT('Ctrl Pts',(368.406900162807,-20.2238658033395,3.09669665584127));
#45940=CARTESIAN_POINT('Ctrl Pts',(368.500058339928,-20.2179921139491,3.16539437109935));
#45941=CARTESIAN_POINT('Ctrl Pts',(368.59309624109,-20.2121260080435,3.23400339115313));
#45942=CARTESIAN_POINT('Ctrl Pts',(368.689288429921,-20.2062599021379,3.29860060718184));
#45943=CARTESIAN_POINT('Ctrl Pts',(368.788253048743,-20.2003937962324,3.35888490661179));
#45944=CARTESIAN_POINT('Ctrl Pts',(368.887116329057,-20.1945336971445,3.41910747568724));
#45945=CARTESIAN_POINT('Ctrl Pts',(368.988746041749,-20.1886735980566,3.47502569904019));
#45946=CARTESIAN_POINT('Ctrl Pts',(369.092729698256,-20.1828134989688,3.52638053795624));
#45947=CARTESIAN_POINT('Ctrl Pts',(369.20046484787,-20.1767419808746,3.57958814230331));
#45948=CARTESIAN_POINT('Ctrl Pts',(369.310726634467,-20.1706704627804,3.627896604315));
#45949=CARTESIAN_POINT('Ctrl Pts',(369.423026034938,-20.1645989446862,3.67106856427918));
#45950=CARTESIAN_POINT('Ctrl Pts',(369.531290428198,-20.1587455810896,3.71268932121818));
#45951=CARTESIAN_POINT('Ctrl Pts',(369.641448110423,-20.152892217493,3.74953617995368));
#45952=CARTESIAN_POINT('Ctrl Pts',(369.753039410706,-20.1470388538964,3.78144495262681));
#45953=CARTESIAN_POINT('Ctrl Pts',(369.864613955932,-20.1411863691627,3.81334893430517));
#45954=CARTESIAN_POINT('Ctrl Pts',(369.977621294096,-20.1353338844289,3.84031619062319));
#45955=CARTESIAN_POINT('Ctrl Pts',(370.09158671091,-20.1294813996951,3.86223244383833));
#45956=CARTESIAN_POINT('Ctrl Pts',(370.205562576823,-20.1236283783671,3.8841507064796));
#45957=CARTESIAN_POINT('Ctrl Pts',(370.320496290277,-20.1177753570391,3.90101696737526));
#45958=CARTESIAN_POINT('Ctrl Pts',(370.43590376897,-20.111922335711,3.91276822945954));
#45959=CARTESIAN_POINT('Ctrl Pts',(370.551349738286,-20.1060673622873,3.92452341081674));
#45960=CARTESIAN_POINT('Ctrl Pts',(370.667269376239,-20.1002123888636,3.93116015932616));
#45961=CARTESIAN_POINT('Ctrl Pts',(370.783175027343,-20.0943574154399,3.93266746768156));
#45962=CARTESIAN_POINT('Ctrl Pts',(370.899212042615,-20.0884958061559,3.93417648437738));
#45963=CARTESIAN_POINT('Ctrl Pts',(371.015234626056,-20.0826341968718,3.93054445202503));
#45964=CARTESIAN_POINT('Ctrl Pts',(371.130756574637,-20.0767725875878,3.92181247441115));
#45965=CARTESIAN_POINT('Ctrl Pts',(371.246356420516,-20.0709070257775,3.91307460876061));
#45966=CARTESIAN_POINT('Ctrl Pts',(371.361454550161,-20.0650414639673,3.89922999939243));
#45967=CARTESIAN_POINT('Ctrl Pts',(371.475573048707,-20.059175902157,3.88037121603933));
#45968=CARTESIAN_POINT('Ctrl Pts',(371.589858416487,-20.0533017634568,3.8614848565195));
#45969=CARTESIAN_POINT('Ctrl Pts',(371.703160891651,-20.0474276247565,3.8375697752771));
#45970=CARTESIAN_POINT('Ctrl Pts',(371.815015777495,-20.0415534860563,3.80876890626494));
#45971=CARTESIAN_POINT('Ctrl Pts',(371.843302052105,-20.0400680122737,3.80148563666306));
#45972=CARTESIAN_POINT('Ctrl Pts',(371.871495846026,-20.0385825384911,3.79389016328918));
#45973=CARTESIAN_POINT('Ctrl Pts',(371.899589844776,-20.0370970647086,3.78598528576312));
#45974=CARTESIAN_POINT('Ctrl Pts',(372.010675899816,-20.0312233753189,3.75472872923835));
#45975=CARTESIAN_POINT('Ctrl Pts',(372.120570136323,-20.0253496859293,3.71852684355849));
#45976=CARTESIAN_POINT('Ctrl Pts',(372.228799299368,-20.0194759965397,3.67748698112704));
#45977=CARTESIAN_POINT('Ctrl Pts',(372.336888728397,-20.0136098906349,3.63650010501367));
#45978=CARTESIAN_POINT('Ctrl Pts',(372.443316976368,-20.0077437847302,3.59068781910305));
#45979=CARTESIAN_POINT('Ctrl Pts',(372.547624007345,-20.0018776788254,3.54020776540738));
#45980=CARTESIAN_POINT('Ctrl Pts',(372.651824229251,-19.9960175797383,3.48977940264374));
#45981=CARTESIAN_POINT('Ctrl Pts',(372.753907184975,-19.9901574806513,3.43469295828946));
#45982=CARTESIAN_POINT('Ctrl Pts',(372.853431588279,-19.9842973815643,3.37515462237087));
#45983=CARTESIAN_POINT('Ctrl Pts',(372.956546605026,-19.9782258634698,3.31346827910693));
#45984=CARTESIAN_POINT('Ctrl Pts',(373.056914547964,-19.9721543453753,3.24700291130202));
#45985=CARTESIAN_POINT('Ctrl Pts',(373.154070857786,-19.9660828272808,3.17604077395526));
#45986=CARTESIAN_POINT('Ctrl Pts',(373.247736263728,-19.9602294636851,3.10762836293089));
#45987=CARTESIAN_POINT('Ctrl Pts',(373.338416495504,-19.9543761000894,3.03503703071331));
#45988=CARTESIAN_POINT('Ctrl Pts',(373.425724392798,-19.9485227364937,2.95856403457036));
#45989=CARTESIAN_POINT('Ctrl Pts',(373.513019181105,-19.9426702517608,2.8821025205905));
#45990=CARTESIAN_POINT('Ctrl Pts',(373.596942331033,-19.9368177670279,2.80176077369107));
#45991=CARTESIAN_POINT('Ctrl Pts',(373.677140466967,-19.930965282295,2.7178757489612));
#45992=CARTESIAN_POINT('Ctrl Pts',(373.757345955993,-19.9251122609679,2.63398303310116));
#45993=CARTESIAN_POINT('Ctrl Pts',(373.833825466572,-19.9192592396408,2.54654669224039));
#45994=CARTESIAN_POINT('Ctrl Pts',(373.906263636155,-19.9134062183136,2.45593935322757));
#45995=CARTESIAN_POINT('Ctrl Pts',(373.978725965266,-19.9075512448909,2.36530179491757));
#45996=CARTESIAN_POINT('Ctrl Pts',(374.047144015364,-19.9016962714681,2.27149145800744));
#45997=CARTESIAN_POINT('Ctrl Pts',(374.111244174247,-19.8958412980453,2.17491215606266));
#45998=CARTESIAN_POINT('Ctrl Pts',(374.175416982426,-19.8899796887622,2.07822339388427));
#45999=CARTESIAN_POINT('Ctrl Pts',(374.235261903116,-19.8841180794791,1.9787597473006));
#46000=CARTESIAN_POINT('Ctrl Pts',(374.290549900864,-19.878256470196,1.87695205928742));
#46001=CARTESIAN_POINT('Ctrl Pts',(374.345875179716,-19.8723909083867,1.7750757216023));
#46002=CARTESIAN_POINT('Ctrl Pts',(374.396637236606,-19.8665253465774,1.67085256566643));
#46003=CARTESIAN_POINT('Ctrl Pts',(374.442654776415,-19.8606597847681,1.56473437002358));
#46004=CARTESIAN_POINT('Ctrl Pts',(374.488739605154,-19.8547856460689,1.4584610035519));
#46005=CARTESIAN_POINT('Ctrl Pts',(374.530065924134,-19.8489115073696,1.35028745158401));
#46006=CARTESIAN_POINT('Ctrl Pts',(374.566501925374,-19.8430373686703,1.24068168826238));
#46007=CARTESIAN_POINT('Ctrl Pts',(374.575715995328,-19.8415518948792,1.2129641798573));
#46008=CARTESIAN_POINT('Ctrl Pts',(374.584617583338,-19.8400664210881,1.18515513506618));
#46009=CARTESIAN_POINT('Ctrl Pts',(374.593205076696,-19.838580947297,1.15726221800511));
#46010=CARTESIAN_POINT('Ctrl Pts',(374.627160753958,-19.8327072579059,1.04697125763385));
#46011=CARTESIAN_POINT('Ctrl Pts',(374.656314736158,-19.8268335685148,0.93500088175898));
#46012=CARTESIAN_POINT('Ctrl Pts',(374.680500676367,-19.8209598791237,0.821806966968872));
#46013=CARTESIAN_POINT('Ctrl Pts',(374.704655390255,-19.8150937732174,0.708759196156783));
#46014=CARTESIAN_POINT('Ctrl Pts',(374.723854732371,-19.8092276673111,0.594491428277202));
#46015=CARTESIAN_POINT('Ctrl Pts',(374.737981780678,-19.8033615614048,0.479475694372454));
#46016=CARTESIAN_POINT('Ctrl Pts',(374.752094363068,-19.7975014623162,0.364577735113922));
#46017=CARTESIAN_POINT('Ctrl Pts',(374.761144932806,-19.7916413632276,0.248933740910155));
#46018=CARTESIAN_POINT('Ctrl Pts',(374.765067527524,-19.785781264139,0.133026305624597));
#46019=CARTESIAN_POINT('Ctrl Pts',(374.76913164051,-19.7797097460451,0.0129371945163077));
#46020=CARTESIAN_POINT('Ctrl Pts',(374.767690686835,-19.7736382279512,-0.107434283569311));
#46021=CARTESIAN_POINT('Ctrl Pts',(374.760730005568,-19.7675667098573,-0.227544742681113));
#46022=CARTESIAN_POINT('Ctrl Pts',(374.754019427142,-19.76171334626,-0.343339537021934));
#46023=CARTESIAN_POINT('Ctrl Pts',(374.742178977134,-19.7558599826627,-0.458891299009031));
#46024=CARTESIAN_POINT('Ctrl Pts',(374.72524855987,-19.7500066190654,-0.573713548799026));
#46025=CARTESIAN_POINT('Ctrl Pts',(374.708320684652,-19.7441541343309,-0.688518558414818));
#46026=CARTESIAN_POINT('Ctrl Pts',(374.686304422026,-19.7383016495965,-0.80259386501185));
#46027=CARTESIAN_POINT('Ctrl Pts',(374.659291349718,-19.732449164862,-0.915459857730073));
#46028=CARTESIAN_POINT('Ctrl Pts',(374.632275800675,-19.7265961435332,-1.02833619874454));
#46029=CARTESIAN_POINT('Ctrl Pts',(374.600262627379,-19.7207431222045,-1.1400026036461));
#46030=CARTESIAN_POINT('Ctrl Pts',(374.563393990059,-19.7148901008758,-1.24999206625128));
#46031=CARTESIAN_POINT('Ctrl Pts',(374.526513056336,-19.7090351274514,-1.360018212466));
#46032=CARTESIAN_POINT('Ctrl Pts',(374.484773569738,-19.703180154027,-1.46836591274371));
#46033=CARTESIAN_POINT('Ctrl Pts',(374.438366530196,-19.6973251806026,-1.57458633742882));
#46034=CARTESIAN_POINT('Ctrl Pts',(374.391906894235,-19.6914635713179,-1.68092714932196));
#46035=CARTESIAN_POINT('Ctrl Pts',(374.340769312161,-19.6856019620332,-1.7851354946226));
#46036=CARTESIAN_POINT('Ctrl Pts',(374.285191662409,-19.6797403527485,-1.88678534896728));
#46037=CARTESIAN_POINT('Ctrl Pts',(374.229576536241,-19.6738747909376,-1.98850374655527));
#46038=CARTESIAN_POINT('Ctrl Pts',(374.169515594253,-19.6680092291267,-2.08765986541362));
#46039=CARTESIAN_POINT('Ctrl Pts',(374.105290187692,-19.6621436673158,-2.1838564483839));
#46040=CARTESIAN_POINT('Ctrl Pts',(374.040970867834,-19.6562695286149,-2.28019369435216));
#46041=CARTESIAN_POINT('Ctrl Pts',(373.972475173792,-19.650395389914,-2.37356243585731));
#46042=CARTESIAN_POINT('Ctrl Pts',(373.900124893551,-19.6445212512131,-2.46359822038484));
#46043=CARTESIAN_POINT('Ctrl Pts',(373.881828688872,-19.6430357774372,-2.48636680036273));
#46044=CARTESIAN_POINT('Ctrl Pts',(373.863286166021,-19.6415503036612,-2.50892242206025));
#46045=CARTESIAN_POINT('Ctrl Pts',(373.844502890951,-19.6400648298853,-2.53125957551702));
#46046=CARTESIAN_POINT('Ctrl Pts',(373.77023222708,-19.6341911404948,-2.61958257616356));
#46047=CARTESIAN_POINT('Ctrl Pts',(373.691947292622,-19.6283174511043,-2.70478110188831));
#46048=CARTESIAN_POINT('Ctrl Pts',(373.609940985998,-19.6224437617138,-2.78646823502634));
#46049=CARTESIAN_POINT('Ctrl Pts',(373.52804055722,-19.6165776558081,-2.86804990240119));
#46050=CARTESIAN_POINT('Ctrl Pts',(373.442428601165,-19.6107115499024,-2.94612890400492));
#46051=CARTESIAN_POINT('Ctrl Pts',(373.353438384673,-19.6048454439967,-3.02035109681497));
#46052=CARTESIAN_POINT('Ctrl Pts',(373.26453929303,-19.5989853449088,-3.09449728704487));
#46053=CARTESIAN_POINT('Ctrl Pts',(373.172269137165,-19.5931252458208,-3.16479426096192));
#46054=CARTESIAN_POINT('Ctrl Pts',(373.076997685662,-19.5872651467329,-3.23092497114606));
#46055=CARTESIAN_POINT('Ctrl Pts',(372.978289057536,-19.5811936286387,-3.29944152648665));
#46056=CARTESIAN_POINT('Ctrl Pts',(372.876358805226,-19.5751221105446,-3.36348520493569));
#46057=CARTESIAN_POINT('Ctrl Pts',(372.771655592382,-19.5690505924505,-3.42274911210763));
#46058=CARTESIAN_POINT('Ctrl Pts',(372.670714449654,-19.5631972288538,-3.47988361973153));
#46059=CARTESIAN_POINT('Ctrl Pts',(372.567196576746,-19.5573438652571,-3.53257570586077));
#46060=CARTESIAN_POINT('Ctrl Pts',(372.461532399002,-19.5514905016604,-3.58059517706343));
#46061=CARTESIAN_POINT('Ctrl Pts',(372.355884086378,-19.5456380169266,-3.62860743830404));
#46062=CARTESIAN_POINT('Ctrl Pts',(372.248090485718,-19.5397855321927,-3.6719483087314));
#46063=CARTESIAN_POINT('Ctrl Pts',(372.138604262947,-19.5339330474589,-3.71043474021725));
#46064=CARTESIAN_POINT('Ctrl Pts',(372.02910800176,-19.5280800261308,-3.74892470039212));
#46065=CARTESIAN_POINT('Ctrl Pts',(371.917919199743,-19.5222270048027,-3.78255919981715));
#46066=CARTESIAN_POINT('Ctrl Pts',(371.80550735227,-19.5163739834746,-3.81120452835368));
#46067=CARTESIAN_POINT('Ctrl Pts',(371.693058013274,-19.5105190100508,-3.83985941066048));
#46068=CARTESIAN_POINT('Ctrl Pts',(371.579385217847,-19.504664036627,-3.8635217113549));
#46069=CARTESIAN_POINT('Ctrl Pts',(371.464969663949,-19.4988090632033,-3.88210861435243));
#46070=CARTESIAN_POINT('Ctrl Pts',(371.350424434717,-19.4929474539192,-3.90071658321714));
#46071=CARTESIAN_POINT('Ctrl Pts',(371.235135174816,-19.4870858446351,-3.91423760683349));
#46072=CARTESIAN_POINT('Ctrl Pts',(371.119588832025,-19.481224235351,-3.92264062445873));
#46073=CARTESIAN_POINT('Ctrl Pts',(371.003964575486,-19.4753586735407,-3.93104930830047));
#46074=CARTESIAN_POINT('Ctrl Pts',(370.888083302831,-19.4694931117304,-3.9343331025536));
#46075=CARTESIAN_POINT('Ctrl Pts',(370.772431355553,-19.4636275499201,-3.93251307199429));
#46076=CARTESIAN_POINT('Ctrl Pts',(370.656610296762,-19.4577534112198,-3.93069038010392));
#46077=CARTESIAN_POINT('Ctrl Pts',(370.5410196434,-19.4518792725196,-3.92374899371222));
#46078=CARTESIAN_POINT('Ctrl Pts',(370.4261400921,-19.4460051338193,-3.91176174061301));
#46079=CARTESIAN_POINT('Ctrl Pts',(370.397088928987,-19.4445196600374,-3.90873035999636));
#46080=CARTESIAN_POINT('Ctrl Pts',(370.368083184964,-19.4430341862556,-3.90537654957453));
#46081=CARTESIAN_POINT('Ctrl Pts',(370.339130507451,-19.4415487124737,-3.90170199945955));
#46082=CARTESIAN_POINT('Ctrl Pts',(370.224649163647,-19.4356750230832,-3.88717251648345));
#46083=CARTESIAN_POINT('Ctrl Pts',(370.110617166372,-19.4298013336927,-3.86757600285977));
#46084=CARTESIAN_POINT('Ctrl Pts',(369.997518428598,-19.4239276443022,-3.84294883168448));
#46085=CARTESIAN_POINT('Ctrl Pts',(369.884565711919,-19.4180615383965,-3.8183534565009));
#46086=CARTESIAN_POINT('Ctrl Pts',(369.772544258537,-19.4121954324909,-3.78874042739295));
#46087=CARTESIAN_POINT('Ctrl Pts',(369.661932324736,-19.4063293265852,-3.75419780680127));
#46088=CARTESIAN_POINT('Ctrl Pts',(369.551433656145,-19.4004692274973,-3.71969055741278));
#46089=CARTESIAN_POINT('Ctrl Pts',(369.442342028251,-19.3946091284093,-3.68026387953251));
#46090=CARTESIAN_POINT('Ctrl Pts',(369.335124313554,-19.3887490293213,-3.63605661818013));
#46091=CARTESIAN_POINT('Ctrl Pts',(369.224038428312,-19.3826775112271,-3.59025445969042));
#46092=CARTESIAN_POINT('Ctrl Pts',(369.11496466351,-19.376605993133,-3.53932035601397));
#46093=CARTESIAN_POINT('Ctrl Pts',(369.008404129742,-19.3705344750389,-3.48346495237152));
#46094=CARTESIAN_POINT('Ctrl Pts',(368.905672401115,-19.3646811114422,-3.42961647802152));
#46095=CARTESIAN_POINT('Ctrl Pts',(368.805276804193,-19.3588277478455,-3.37119447813662));
#46096=CARTESIAN_POINT('Ctrl Pts',(368.707644109995,-19.3529743842489,-3.30843585246246));
#46097=CARTESIAN_POINT('Ctrl Pts',(368.610026075017,-19.3471218995151,-3.2456866497847));
#46098=CARTESIAN_POINT('Ctrl Pts',(368.515170465349,-19.3412694147812,-3.17860233934627));
#46099=CARTESIAN_POINT('Ctrl Pts',(368.423476492272,-19.3354169300474,-3.10746406774455));
#46100=CARTESIAN_POINT('Ctrl Pts',(368.331774112089,-19.3295639087193,-3.03631927371842));
#46101=CARTESIAN_POINT('Ctrl Pts',(368.243234271194,-19.3237108873912,-2.96112003289903));
#46102=CARTESIAN_POINT('Ctrl Pts',(368.158223845174,-19.3178578660631,-2.88218838039403));
#46103=CARTESIAN_POINT('Ctrl Pts',(368.073185066535,-19.3120028926394,-2.80323040265899));
#46104=CARTESIAN_POINT('Ctrl Pts',(367.991678346035,-19.3061479192157,-2.72053781890731));
#46105=CARTESIAN_POINT('Ctrl Pts',(367.914033865616,-19.300292945792,-2.63446966802033));
#46106=CARTESIAN_POINT('Ctrl Pts',(367.836301385151,-19.2944313365079,-2.54830396993912));
#46107=CARTESIAN_POINT('Ctrl Pts',(367.762440158595,-19.2885697272239,-2.45875537564755));
#46108=CARTESIAN_POINT('Ctrl Pts',(367.692740265555,-19.2827081179398,-2.36621623286088));
#46109=CARTESIAN_POINT('Ctrl Pts',(367.622993373365,-19.2768425561296,-2.27361469025088));
#46110=CARTESIAN_POINT('Ctrl Pts',(367.557413635232,-19.2709769943193,-2.17801892359211));
#46111=CARTESIAN_POINT('Ctrl Pts',(367.496247000607,-19.2651114325091,-2.07984902887398));
#46112=CARTESIAN_POINT('Ctrl Pts',(367.43499092536,-19.2592372938089,-1.98153558569172));
#46113=CARTESIAN_POINT('Ctrl Pts',(367.378161034244,-19.2533631551086,-1.88064086102556));
#46114=CARTESIAN_POINT('Ctrl Pts',(367.325956719709,-19.2474890164084,-1.77760826866929));
#46115=CARTESIAN_POINT('Ctrl Pts',(367.312755100797,-19.2460035426262,-1.75155300806664));
#46116=CARTESIAN_POINT('Ctrl Pts',(367.299849044302,-19.2445180688441,-1.72536112121797));
#46117=CARTESIAN_POINT('Ctrl Pts',(367.287241275747,-19.243032595062,-1.69903995053532));
#46118=CARTESIAN_POINT('Ctrl Pts',(367.233428325467,-19.23669224019,-1.58669494331932));
#46119=CARTESIAN_POINT('Ctrl Pts',(367.184895602673,-19.2303518853181,-1.47166404912409));
#46120=CARTESIAN_POINT('Ctrl Pts',(367.141897960567,-19.2240115304461,-1.35444613636435));
#46121=CARTESIAN_POINT('Ctrl Pts',(367.099044455801,-19.2176924298067,-1.23762116324669));
#46122=CARTESIAN_POINT('Ctrl Pts',(367.061689140577,-19.2113733291672,-1.11862407952074));
#46123=CARTESIAN_POINT('Ctrl Pts',(367.030039023062,-19.2050542285278,-0.99797373832264));
#46124=CARTESIAN_POINT('Ctrl Pts',(366.998454638872,-19.198748251868,-0.877573972753616));
#46125=CARTESIAN_POINT('Ctrl Pts',(366.972551921596,-19.1924422752082,-0.755528088159374));
#46126=CARTESIAN_POINT('Ctrl Pts',(366.952489164617,-19.1861362985484,-0.632372542341981));
#46127=CARTESIAN_POINT('Ctrl Pts',(366.932489836403,-19.1798502583463,-0.50960635497981));
#46128=CARTESIAN_POINT('Ctrl Pts',(366.918293709533,-19.1735642181442,-0.385737804481959));
#46129=CARTESIAN_POINT('Ctrl Pts',(366.910008536092,-19.167278177942,-0.261314721109544));
#46130=CARTESIAN_POINT('Ctrl Pts',(366.904246710676,-19.1629066259815,-0.174786166317576));
#46131=CARTESIAN_POINT('Ctrl Pts',(366.901342603383,-19.158535074021,-0.0879897673060905));
#46132=CARTESIAN_POINT('Ctrl Pts',(366.901318010803,-19.1541635220605,-0.00111333548552649));
#46133=CARTESIAN_POINT('',(366.901319490285,-17.9041635219925,0.00358847020308838));
#46134=CARTESIAN_POINT('Ctrl Pts',(366.901318010803,-19.154163522035,-0.0011133349797373));
#46135=CARTESIAN_POINT('Ctrl Pts',(366.90128418225,-19.1481501902697,0.118390404615894));
#46136=CARTESIAN_POINT('Ctrl Pts',(366.906701360906,-19.1421368585045,0.237841410527132));
#46137=CARTESIAN_POINT('Ctrl Pts',(366.917528943227,-19.1361235267392,0.356726273948674));
#46138=CARTESIAN_POINT('Ctrl Pts',(366.928364304895,-19.1301058745454,0.47569655317238));
#46139=CARTESIAN_POINT('Ctrl Pts',(366.944617781229,-19.1240882223516,0.594099501001153));
#46140=CARTESIAN_POINT('Ctrl Pts',(366.966197139492,-19.1180705701578,0.711428945152156));
#46141=CARTESIAN_POINT('Ctrl Pts',(366.988177612702,-19.1119410624489,0.830939297238127));
#46142=CARTESIAN_POINT('Ctrl Pts',(367.015683841127,-19.1058115547399,0.949335435228387));
#46143=CARTESIAN_POINT('Ctrl Pts',(367.048564873449,-19.0996820470309,1.06609726391429));
#46144=CARTESIAN_POINT('Ctrl Pts',(367.080932279724,-19.0936482867664,1.18103518646783));
#46145=CARTESIAN_POINT('Ctrl Pts',(367.118507592269,-19.0876145265018,1.29438915399849));
#46146=CARTESIAN_POINT('Ctrl Pts',(367.161097846325,-19.0815807662372,1.40568267433245));
#46147=CARTESIAN_POINT('Ctrl Pts',(367.204701873171,-19.0754033848061,1.51962530641805));
#46148=CARTESIAN_POINT('Ctrl Pts',(367.253562401351,-19.0692260033749,1.6314077777596));
#46149=CARTESIAN_POINT('Ctrl Pts',(367.30742253689,-19.0630486219438,1.74054543968912));
#46150=CARTESIAN_POINT('Ctrl Pts',(367.361282672429,-19.0568712405126,1.84968310161863));
#46151=CARTESIAN_POINT('Ctrl Pts',(367.420142152239,-19.0506938590815,1.95617561959075));
#46152=CARTESIAN_POINT('Ctrl Pts',(367.483697301148,-19.0445164776503,2.05957056592082));
#46153=CARTESIAN_POINT('Ctrl Pts',(367.544127955791,-19.0386427882598,2.15788241634883));
#46154=CARTESIAN_POINT('Ctrl Pts',(367.608989833161,-19.0327690988692,2.25369607202037));
#46155=CARTESIAN_POINT('Ctrl Pts',(367.678050308889,-19.0268954094786,2.34658564484133));
#46156=CARTESIAN_POINT('Ctrl Pts',(367.747021621055,-19.0210293035729,2.43935528849727));
#46157=CARTESIAN_POINT('Ctrl Pts',(367.820180507169,-19.0151631976671,2.52920802854385));
#46158=CARTESIAN_POINT('Ctrl Pts',(367.897249581732,-19.0092970917614,2.61574443870113));
#46159=CARTESIAN_POINT('Ctrl Pts',(367.974239738545,-19.0034369926734,2.70219223667677));
#46160=CARTESIAN_POINT('Ctrl Pts',(368.055131846414,-18.9975768935853,2.7853301527562));
#46161=CARTESIAN_POINT('Ctrl Pts',(368.139606945752,-18.9917167944973,2.86479006650617));
#46162=CARTESIAN_POINT('Ctrl Pts',(368.227129713956,-18.9856452764032,2.94711671266731));
#46163=CARTESIAN_POINT('Ctrl Pts',(368.318498617669,-18.9795737583091,3.02549459551379));
#46164=CARTESIAN_POINT('Ctrl Pts',(368.413315167613,-18.973502240215,3.09955399957246));
#46165=CARTESIAN_POINT('Ctrl Pts',(368.504724883143,-18.9676488766182,3.17095239005631));
#46166=CARTESIAN_POINT('Ctrl Pts',(368.59933840182,-18.9617955130215,3.23833701764886));
#46167=CARTESIAN_POINT('Ctrl Pts',(368.696763959796,-18.9559421494248,3.30141671902981));
#46168=CARTESIAN_POINT('Ctrl Pts',(368.794174889652,-18.9500896646909,3.3644869492059));
#46169=CARTESIAN_POINT('Ctrl Pts',(368.894396672571,-18.944237179957,3.42325331391641));
#46170=CARTESIAN_POINT('Ctrl Pts',(368.997008593458,-18.9383846952231,3.47746799898695));
#46171=CARTESIAN_POINT('Ctrl Pts',(369.09962992248,-18.9325316738949,3.5316876548161));
#46172=CARTESIAN_POINT('Ctrl Pts',(369.204641459794,-18.9266786525668,3.58135460838431));
#46173=CARTESIAN_POINT('Ctrl Pts',(369.311598567582,-18.9208256312386,3.62626736150748));
#46174=CARTESIAN_POINT('Ctrl Pts',(369.418591347632,-18.9149706578148,3.67119509390114));
#46175=CARTESIAN_POINT('Ctrl Pts',(369.527530607717,-18.909115684391,3.71136531305094));
#46176=CARTESIAN_POINT('Ctrl Pts',(369.637953123096,-18.9032607109672,3.74662520576918));
#46177=CARTESIAN_POINT('Ctrl Pts',(369.748500788212,-18.8973991016831,3.78192506104692));
#46178=CARTESIAN_POINT('Ctrl Pts',(369.860534670168,-18.891537492399,3.81230335629716));
#46179=CARTESIAN_POINT('Ctrl Pts',(369.973577728849,-18.8856758831148,3.83765754572904));
#46180=CARTESIAN_POINT('Ctrl Pts',(370.086697013295,-18.8798103213045,3.86302883167708));
#46181=CARTESIAN_POINT('Ctrl Pts',(370.200826423755,-18.8739447594941,3.88336919365258));
#46182=CARTESIAN_POINT('Ctrl Pts',(370.315481831255,-18.8680791976838,3.89862773066463));
#46183=CARTESIAN_POINT('Ctrl Pts',(370.430304893082,-18.8622050589835,3.91390857940021));
#46184=CARTESIAN_POINT('Ctrl Pts',(370.54565507699,-18.8563309202831,3.92409273681971));
#46185=CARTESIAN_POINT('Ctrl Pts',(370.66104620208,-18.8504567815828,3.92918133138568));
#46186=CARTESIAN_POINT('Ctrl Pts',(370.690226733843,-18.8489713078014,3.93046815387957));
#46187=CARTESIAN_POINT('Ctrl Pts',(370.719409901697,-18.8474858340201,3.93142937397189));
#46188=CARTESIAN_POINT('Ctrl Pts',(370.748587892579,-18.8460003602387,3.93206553529412));
#46189=CARTESIAN_POINT('Ctrl Pts',(370.863960144606,-18.8401266708481,3.9345809711476));
#46190=CARTESIAN_POINT('Ctrl Pts',(370.979635351959,-18.8342529814576,3.93201852063389));
#46191=CARTESIAN_POINT('Ctrl Pts',(371.095129529651,-18.828379292067,3.92434278184756));
#46192=CARTESIAN_POINT('Ctrl Pts',(371.21047459351,-18.8225131861612,3.91667695316111));
#46193=CARTESIAN_POINT('Ctrl Pts',(371.325638684041,-18.8166470802555,3.90391099203634));
#46194=CARTESIAN_POINT('Ctrl Pts',(371.440135786891,-18.8107809743497,3.88606145489848));
#46195=CARTESIAN_POINT('Ctrl Pts',(371.554515646166,-18.8049208752617,3.86823019545921));
#46196=CARTESIAN_POINT('Ctrl Pts',(371.668229470489,-18.7990607761736,3.84532577747209));
#46197=CARTESIAN_POINT('Ctrl Pts',(371.780795014347,-18.7932006770856,3.81741666359245));
#46198=CARTESIAN_POINT('Ctrl Pts',(371.897421666223,-18.7871291589915,3.78850065255498));
#46199=CARTESIAN_POINT('Ctrl Pts',(372.012815167939,-18.7810576408974,3.75421204151851));
#46200=CARTESIAN_POINT('Ctrl Pts',(372.126448819855,-18.7749861228033,3.71468525787507));
#46201=CARTESIAN_POINT('Ctrl Pts',(372.235999523843,-18.7691327592065,3.67657870315703));
#46202=CARTESIAN_POINT('Ctrl Pts',(372.343914243535,-18.7632793956098,3.63360406847437));
#46203=CARTESIAN_POINT('Ctrl Pts',(372.449735933199,-18.757426032013,3.58593271365921));
#46204=CARTESIAN_POINT('Ctrl Pts',(372.555541734092,-18.7515735472791,3.53826851653749));
#46205=CARTESIAN_POINT('Ctrl Pts',(372.65925475324,-18.7457210625452,3.48590917112646));
#46206=CARTESIAN_POINT('Ctrl Pts',(372.760438676795,-18.7398685778113,3.4290738652014));
#46207=CARTESIAN_POINT('Ctrl Pts',(372.861631877556,-18.7340155564832,3.37223334824185));
#46208=CARTESIAN_POINT('Ctrl Pts',(372.96029516153,-18.728162535155,3.31091625730226));
#46209=CARTESIAN_POINT('Ctrl Pts',(373.056018165821,-18.7223095138268,3.24538699094666));
#46210=CARTESIAN_POINT('Ctrl Pts',(373.151773095583,-18.716454540403,3.17983586931544));
#46211=CARTESIAN_POINT('Ctrl Pts',(373.244585454973,-18.7105995669792,3.11007001205712));
#46212=CARTESIAN_POINT('Ctrl Pts',(373.334075715332,-18.7047445935554,3.0363958290761));
#46213=CARTESIAN_POINT('Ctrl Pts',(373.423667401406,-18.6988829842713,2.96263814587162));
#46214=CARTESIAN_POINT('Ctrl Pts',(373.509929154253,-18.6930213749871,2.88496355849492));
#46215=CARTESIAN_POINT('Ctrl Pts',(373.592516195857,-18.687159765703,2.80371733644781));
#46216=CARTESIAN_POINT('Ctrl Pts',(373.675158926509,-18.6812942038926,2.72241632947651));
#46217=CARTESIAN_POINT('Ctrl Pts',(373.754121731188,-18.6754286420823,2.63753919395465));
#46218=CARTESIAN_POINT('Ctrl Pts',(373.82909938647,-18.669563080272,2.54946515334626));
#46219=CARTESIAN_POINT('Ctrl Pts',(373.904186677474,-18.6636889415716,2.46126232688874));
#46220=CARTESIAN_POINT('Ctrl Pts',(373.975276936664,-18.6578148028713,2.36985359077235));
#46221=CARTESIAN_POINT('Ctrl Pts',(374.042107549006,-18.651940664171,2.27564809837372));
#46222=CARTESIAN_POINT('Ctrl Pts',(374.05900791985,-18.6504551903896,2.25182506726159));
#46223=CARTESIAN_POINT('Ctrl Pts',(374.075636113491,-18.6489697166083,2.22782330886233));
#46224=CARTESIAN_POINT('Ctrl Pts',(374.091988351211,-18.647484242827,2.20364968326233));
#46225=CARTESIAN_POINT('Ctrl Pts',(374.156646486828,-18.6416105534364,2.10806511623511));
#46226=CARTESIAN_POINT('Ctrl Pts',(374.217201869648,-18.6357368640458,2.00947320297338));
#46227=CARTESIAN_POINT('Ctrl Pts',(374.273362378306,-18.6298631746553,1.90826144815202));
#46228=CARTESIAN_POINT('Ctrl Pts',(374.329450378471,-18.6239970687495,1.80718036721465));
#46229=CARTESIAN_POINT('Ctrl Pts',(374.381154589964,-18.6181309628438,1.70348652928221));
#46230=CARTESIAN_POINT('Ctrl Pts',(374.428225452276,-18.612264856938,1.59759731142581));
#46231=CARTESIAN_POINT('Ctrl Pts',(374.475248114625,-18.60640475785,1.49181652277923));
#46232=CARTESIAN_POINT('Ctrl Pts',(374.517646698153,-18.6005446587619,1.38384520102957));
#46233=CARTESIAN_POINT('Ctrl Pts',(374.555217302689,-18.5946845596739,1.27412569512333));
#46234=CARTESIAN_POINT('Ctrl Pts',(374.594143368923,-18.5886130415798,1.16044775975463));
#46235=CARTESIAN_POINT('Ctrl Pts',(374.627886294788,-18.5825415234857,1.044893512584));
#46236=CARTESIAN_POINT('Ctrl Pts',(374.656273511792,-18.5764700053915,0.927978417820083));
#46237=CARTESIAN_POINT('Ctrl Pts',(374.683640753402,-18.5706166417948,0.815264175847031));
#46238=CARTESIAN_POINT('Ctrl Pts',(374.706030426571,-18.564763278198,0.701285631866943));
#46239=CARTESIAN_POINT('Ctrl Pts',(374.72333875747,-18.5589099146013,0.586519740789697));
#46240=CARTESIAN_POINT('Ctrl Pts',(374.740644489582,-18.5530574298674,0.471771081424861));
#46241=CARTESIAN_POINT('Ctrl Pts',(374.752870334855,-18.5472049451335,0.356235718439138));
#46242=CARTESIAN_POINT('Ctrl Pts',(374.759963948607,-18.5413524603996,0.240399113562284));
#46243=CARTESIAN_POINT('Ctrl Pts',(374.767058212749,-18.5354994390714,0.124551888024065));
#46244=CARTESIAN_POINT('Ctrl Pts',(374.769019284694,-18.5296464177432,0.00840377808418154));
#46245=CARTESIAN_POINT('Ctrl Pts',(374.765846879003,-18.523793396415,-0.107557052120743));
#46246=CARTESIAN_POINT('Ctrl Pts',(374.762673415252,-18.5179384229912,-0.223556557501702));
#46247=CARTESIAN_POINT('Ctrl Pts',(374.754363080696,-18.5120834495674,-0.339368246178464));
#46248=CARTESIAN_POINT('Ctrl Pts',(374.740967607883,-18.5062284761436,-0.454507089516433));
#46249=CARTESIAN_POINT('Ctrl Pts',(374.727556953023,-18.5003668668594,-0.569776427944547));
#46250=CARTESIAN_POINT('Ctrl Pts',(374.709049704376,-18.4945052575753,-0.684370988356086));
#46251=CARTESIAN_POINT('Ctrl Pts',(374.685549087174,-18.4886436482911,-0.797813877198597));
#46252=CARTESIAN_POINT('Ctrl Pts',(374.662032623332,-18.4827780864808,-0.911333261414341));
#46253=CARTESIAN_POINT('Ctrl Pts',(374.633516187737,-18.4769125246704,-1.02369902825722));
#46254=CARTESIAN_POINT('Ctrl Pts',(374.60015298032,-18.4710469628601,-1.13444911544304));
#46255=CARTESIAN_POINT('Ctrl Pts',(374.566740987711,-18.4651728241597,-1.24536114641937));
#46256=CARTESIAN_POINT('Ctrl Pts',(374.528468215096,-18.4592986854594,-1.35465239431463));
#46257=CARTESIAN_POINT('Ctrl Pts',(374.485536111161,-18.4534245467591,-1.4618803757175));
#46258=CARTESIAN_POINT('Ctrl Pts',(374.474679282948,-18.4519390729778,-1.4889965817034));
#46259=CARTESIAN_POINT('Ctrl Pts',(374.463524718943,-18.4504535991966,-1.51598096481221));
#46260=CARTESIAN_POINT('Ctrl Pts',(374.452076135251,-18.4489681254154,-1.54282663083928));
#46261=CARTESIAN_POINT('Ctrl Pts',(374.406807463788,-18.4430944360248,-1.64897667247484));
#46262=CARTESIAN_POINT('Ctrl Pts',(374.356787554373,-18.4372207466342,-1.75330944973641));
#46263=CARTESIAN_POINT('Ctrl Pts',(374.302183668454,-18.4313470572437,-1.85536942077899));
#46264=CARTESIAN_POINT('Ctrl Pts',(374.247650281281,-18.4254809513379,-1.95729762281074));
#46265=CARTESIAN_POINT('Ctrl Pts',(374.188544880369,-18.4196148454322,-2.05695849323815));
#46266=CARTESIAN_POINT('Ctrl Pts',(374.125082901821,-18.4137487395264,-2.15391606032656));
#46267=CARTESIAN_POINT('Ctrl Pts',(374.06168590753,-18.4078886404384,-2.25077434410155));
#46268=CARTESIAN_POINT('Ctrl Pts',(373.993941433975,-18.4020285413504,-2.34493448698738));
#46269=CARTESIAN_POINT('Ctrl Pts',(373.922110654224,-18.3961684422623,-2.43598534849728));
#46270=CARTESIAN_POINT('Ctrl Pts',(373.847688383811,-18.3900969241682,-2.53032111737022));
#46271=CARTESIAN_POINT('Ctrl Pts',(373.768879604177,-18.3840254060741,-2.62131861919105));
#46272=CARTESIAN_POINT('Ctrl Pts',(373.686023912919,-18.37795388798,-2.70855340525163));
#46273=CARTESIAN_POINT('Ctrl Pts',(373.606145292864,-18.3721005243832,-2.79265377573266));
#46274=CARTESIAN_POINT('Ctrl Pts',(373.522505882718,-18.3662471607865,-2.87325684653467));
#46275=CARTESIAN_POINT('Ctrl Pts',(373.435450214655,-18.3603937971898,-2.95001685390382));
#46276=CARTESIAN_POINT('Ctrl Pts',(373.348407617707,-18.3545413124558,-3.02676533601632));
#46277=CARTESIAN_POINT('Ctrl Pts',(373.257950092563,-18.3486888277219,-3.09967162886994));
#46278=CARTESIAN_POINT('Ctrl Pts',(373.164457199974,-18.342836342988,-3.16842857339812));
#46279=CARTESIAN_POINT('Ctrl Pts',(373.070955735342,-18.3369833216598,-3.23719182201521));
#46280=CARTESIAN_POINT('Ctrl Pts',(372.974418682875,-18.3311303003316,-3.30180472124391));
#46281=CARTESIAN_POINT('Ctrl Pts',(372.875256095986,-18.3252772790034,-3.36200239280549));
#46282=CARTESIAN_POINT('Ctrl Pts',(372.776060436461,-18.3194223055796,-3.42222014145301));
#46283=CARTESIAN_POINT('Ctrl Pts',(372.674237854264,-18.3135673321557,-3.47801952003003));
#46284=CARTESIAN_POINT('Ctrl Pts',(372.570223967472,-18.3077123587319,-3.5291810611691));
#46285=CARTESIAN_POINT('Ctrl Pts',(372.466092194301,-18.3018507494477,-3.58040058734349));
#46286=CARTESIAN_POINT('Ctrl Pts',(372.359764530426,-18.2959891401635,-3.62697160218444));
#46287=CARTESIAN_POINT('Ctrl Pts',(372.251697672621,-18.2901275308794,-3.66872231813269));
#46288=CARTESIAN_POINT('Ctrl Pts',(372.143557944541,-18.284261969069,-3.71050118689534));
#46289=CARTESIAN_POINT('Ctrl Pts',(372.03367707795,-18.2783964072587,-3.74745315320763));
#46290=CARTESIAN_POINT('Ctrl Pts',(371.922526398551,-18.2725308454483,-3.7794564638157));
#46291=CARTESIAN_POINT('Ctrl Pts',(371.811213189597,-18.266656706748,-3.81150657111314));
#46292=CARTESIAN_POINT('Ctrl Pts',(371.698626862312,-18.2607825680476,-3.83859348490467));
#46293=CARTESIAN_POINT('Ctrl Pts',(371.585248446229,-18.2549084293473,-3.86064660963543));
#46294=CARTESIAN_POINT('Ctrl Pts',(371.556576895719,-18.2534229555661,-3.86622348485963));
#46295=CARTESIAN_POINT('Ctrl Pts',(371.527854711603,-18.2519374817849,-3.87147870792586));
#46296=CARTESIAN_POINT('Ctrl Pts',(371.49908970167,-18.2504520080037,-3.87641166409268));
#46297=CARTESIAN_POINT('Ctrl Pts',(371.385350411352,-18.2445783186131,-3.89591699139472));
#46298=CARTESIAN_POINT('Ctrl Pts',(371.270562491265,-18.2387046292226,-3.91044465985997));
#46299=CARTESIAN_POINT('Ctrl Pts',(371.155199410817,-18.232830939832,-3.91988826702961));
#46300=CARTESIAN_POINT('Ctrl Pts',(371.039985274945,-18.2269648339262,-3.92931968161521));
#46301=CARTESIAN_POINT('Ctrl Pts',(370.924197863479,-18.2210987280205,-3.9336800551511));
#46302=CARTESIAN_POINT('Ctrl Pts',(370.80832031685,-18.2152326221147,-3.93291407586061));
#46303=CARTESIAN_POINT('Ctrl Pts',(370.692561427353,-18.2093725230267,-3.93214888092315));
#46304=CARTESIAN_POINT('Ctrl Pts',(370.57671299696,-18.2035124239387,-3.92626777720655));
#46305=CARTESIAN_POINT('Ctrl Pts',(370.461262094652,-18.1976523248507,-3.91526734732078));
#46306=CARTESIAN_POINT('Ctrl Pts',(370.341645987175,-18.1915808067566,-3.90387004702072));
#46307=CARTESIAN_POINT('Ctrl Pts',(370.222457083328,-18.1855092886625,-3.88697702228025));
#46308=CARTESIAN_POINT('Ctrl Pts',(370.104236149779,-18.1794377705683,-3.86464354194478));
#46309=CARTESIAN_POINT('Ctrl Pts',(369.990262988853,-18.1735844069716,-3.84311252140624));
#46310=CARTESIAN_POINT('Ctrl Pts',(369.877189876214,-18.1677310433748,-3.81652536002296));
#46311=CARTESIAN_POINT('Ctrl Pts',(369.765494134026,-18.1618776797781,-3.7849841290658));
#46312=CARTESIAN_POINT('Ctrl Pts',(369.653815162578,-18.1560251950442,-3.7534476339183));
#46313=CARTESIAN_POINT('Ctrl Pts',(369.543513547859,-18.1501727103103,-3.71695866046925));
#46314=CARTESIAN_POINT('Ctrl Pts',(369.435053161538,-18.1443202255764,-3.67566964274565));
#46315=CARTESIAN_POINT('Ctrl Pts',(369.326582830856,-18.1384672042482,-3.63437683937355));
#46316=CARTESIAN_POINT('Ctrl Pts',(369.219954450297,-18.1326141829201,-3.58828326384494));
#46317=CARTESIAN_POINT('Ctrl Pts',(369.115612893013,-18.1267611615919,-3.53758989422811));
#46318=CARTESIAN_POINT('Ctrl Pts',(369.011236535803,-18.1209061881681,-3.48687961739333));
#46319=CARTESIAN_POINT('Ctrl Pts',(368.909148889872,-18.1150512147442,-3.43156667638602));
#46320=CARTESIAN_POINT('Ctrl Pts',(368.809770528071,-18.1091962413204,-3.37189814914625));
#46321=CARTESIAN_POINT('Ctrl Pts',(368.710279533662,-18.1033346320362,-3.31216199529506));
#46322=CARTESIAN_POINT('Ctrl Pts',(368.613504306569,-18.0974730227521,-3.24806061504867));
#46323=CARTESIAN_POINT('Ctrl Pts',(368.51983678089,-18.0916114134679,-3.17988464662003));
#46324=CARTESIAN_POINT('Ctrl Pts',(368.426106094512,-18.0857458516576,-3.11166270663559));
#46325=CARTESIAN_POINT('Ctrl Pts',(368.335487604394,-18.0798802898473,-3.03936096456994));
#46326=CARTESIAN_POINT('Ctrl Pts',(368.248339130896,-18.074014728037,-2.96330947551348));
#46327=CARTESIAN_POINT('Ctrl Pts',(368.161063224955,-18.0681405893366,-2.88714678052682));
#46328=CARTESIAN_POINT('Ctrl Pts',(368.077267759909,-18.0622664506363,-2.80722367981215));
#46329=CARTESIAN_POINT('Ctrl Pts',(367.99727282844,-18.056392311936,-2.72390611573736));
#46330=CARTESIAN_POINT('Ctrl Pts',(367.977043416199,-18.0549068381547,-2.70283646395222));
#46331=CARTESIAN_POINT('Ctrl Pts',(367.95705684183,-18.0534213643734,-2.68154989365601));
#46332=CARTESIAN_POINT('Ctrl Pts',(367.937317854584,-18.0519358905921,-2.66005263253901));
#46333=CARTESIAN_POINT('Ctrl Pts',(367.860117706328,-18.0461261297005,-2.57597578884998));
#46334=CARTESIAN_POINT('Ctrl Pts',(367.78643768348,-18.040316368809,-2.48837936147946));
#46335=CARTESIAN_POINT('Ctrl Pts',(367.716621101547,-18.0345066079174,-2.39759378639936));
#46336=CARTESIAN_POINT('Ctrl Pts',(367.646917585048,-18.0287062557239,-2.3069552352809));
#46337=CARTESIAN_POINT('Ctrl Pts',(367.581065314757,-18.0229059035304,-2.21313814581991));
#46338=CARTESIAN_POINT('Ctrl Pts',(367.519370000745,-18.0171055513369,-2.11650885548427));
#46339=CARTESIAN_POINT('Ctrl Pts',(367.457731987188,-18.0113105863081,-2.01996931106288));
#46340=CARTESIAN_POINT('Ctrl Pts',(367.400243484369,-18.0055156212794,-1.92062310980084));
#46341=CARTESIAN_POINT('Ctrl Pts',(367.347169085525,-17.9997206562507,-1.81886845921795));
#46342=CARTESIAN_POINT('Ctrl Pts',(367.294130453419,-17.993929596438,-1.71718238090259));
#46343=CARTESIAN_POINT('Ctrl Pts',(367.245500207612,-17.9881385366253,-1.61309145307366));
#46344=CARTESIAN_POINT('Ctrl Pts',(367.201498406724,-17.9823474768126,-1.50702085889003));
#46345=CARTESIAN_POINT('Ctrl Pts',(367.157515047021,-17.9765588440371,-1.40099471896696));
#46346=CARTESIAN_POINT('Ctrl Pts',(367.118156436423,-17.9707702112616,-1.29299095283894));
#46347=CARTESIAN_POINT('Ctrl Pts',(367.083595280145,-17.9649815784862,-1.18345645454238));
#46348=CARTESIAN_POINT('Ctrl Pts',(367.04903064302,-17.9591923627051,-1.07391092441323));
#46349=CARTESIAN_POINT('Ctrl Pts',(367.019264562183,-17.953403146924,-0.962834754694295));
#46350=CARTESIAN_POINT('Ctrl Pts',(366.994420301154,-17.9476139311429,-0.850691359780153));
#46351=CARTESIAN_POINT('Ctrl Pts',(366.96957484929,-17.9418244378733,-0.738542589612216));
#46352=CARTESIAN_POINT('Ctrl Pts',(366.949651770194,-17.9360349446037,-0.625326907398582));
#46353=CARTESIAN_POINT('Ctrl Pts',(366.934723222317,-17.9302454513341,-0.511518049147073));
#46354=CARTESIAN_POINT('Ctrl Pts',(366.919784200993,-17.9244518963195,-0.397629345815158));
#46355=CARTESIAN_POINT('Ctrl Pts',(366.909846752754,-17.918658341305,-0.283147056364034));
#46356=CARTESIAN_POINT('Ctrl Pts',(366.90493114092,-17.9128647862904,-0.168549889250918));
#46357=CARTESIAN_POINT('Ctrl Pts',(366.902470243282,-17.909964364872,-0.1111792287226));
#46358=CARTESIAN_POINT('Ctrl Pts',(366.901267147452,-17.9070639434535,-0.0537797989658822));
#46359=CARTESIAN_POINT('Ctrl Pts',(366.901319490284,-17.904163522035,0.00358846936293337));
#46360=CARTESIAN_POINT('',(366.901317976443,-16.6541635220067,-0.000984499013828783));
#46361=CARTESIAN_POINT('Ctrl Pts',(366.901319490285,-17.9041635219925,0.0035884702030614));
#46362=CARTESIAN_POINT('Ctrl Pts',(366.901453987089,-17.8967107857687,0.150998280634382));
#46363=CARTESIAN_POINT('Ctrl Pts',(366.909879461701,-17.8892580495449,0.298039224628797));
#46364=CARTESIAN_POINT('Ctrl Pts',(366.926450625096,-17.881805313321,0.443917478055424));
#46365=CARTESIAN_POINT('Ctrl Pts',(366.943372590596,-17.87419480691,0.592883891139391));
#46366=CARTESIAN_POINT('Ctrl Pts',(366.968788773385,-17.866584300499,0.740638106576088));
#46367=CARTESIAN_POINT('Ctrl Pts',(367.00249633415,-17.858973794088,0.886359321021127));
#46368=CARTESIAN_POINT('Ctrl Pts',(367.010696073086,-17.8571224537854,0.921807626648902));
#46369=CARTESIAN_POINT('Ctrl Pts',(367.019386242384,-17.8552711134829,0.9571357292265));
#46370=CARTESIAN_POINT('Ctrl Pts',(367.028563499469,-17.8534197731803,0.992332000328052));
#46371=CARTESIAN_POINT('Ctrl Pts',(367.057679895574,-17.8475460837898,1.10399810724094));
#46372=CARTESIAN_POINT('Ctrl Pts',(367.091763607331,-17.8416723943992,1.21456763442583));
#46373=CARTESIAN_POINT('Ctrl Pts',(367.130716395201,-17.8357987050086,1.3235653516671));
#46374=CARTESIAN_POINT('Ctrl Pts',(367.169618891363,-17.8299325991029,1.43242234261545));
#46375=CARTESIAN_POINT('Ctrl Pts',(367.213377824216,-17.8240664931971,1.5397111738462));
#46376=CARTESIAN_POINT('Ctrl Pts',(367.261844419909,-17.8182003872913,1.64496886543682));
#46377=CARTESIAN_POINT('Ctrl Pts',(367.310261386425,-17.8123402882033,1.7501187744923));
#46378=CARTESIAN_POINT('Ctrl Pts',(367.363376255463,-17.8064801891153,1.85324130788109));
#46379=CARTESIAN_POINT('Ctrl Pts',(367.420991353868,-17.8006200900272,1.9538912991242));
#46380=CARTESIAN_POINT('Ctrl Pts',(367.480685073582,-17.7945485719331,2.05817251243197));
#46381=CARTESIAN_POINT('Ctrl Pts',(367.545209717467,-17.788477053839,2.15979898249089));
#46382=CARTESIAN_POINT('Ctrl Pts',(367.6142920086,-17.7824055357449,2.25830081254818));
#46383=CARTESIAN_POINT('Ctrl Pts',(367.680892117804,-17.7765521721482,2.35326339313078));
#46384=CARTESIAN_POINT('Ctrl Pts',(367.751727733438,-17.7706988085514,2.44532164376651));
#46385=CARTESIAN_POINT('Ctrl Pts',(367.826509091948,-17.7648454449547,2.53408276415557));
#46386=CARTESIAN_POINT('Ctrl Pts',(367.901279222288,-17.7589929602208,2.62283055736104));
#46387=CARTESIAN_POINT('Ctrl Pts',(367.979993651387,-17.7531404754869,2.70828188879846));
#46388=CARTESIAN_POINT('Ctrl Pts',(368.062322276064,-17.747287990753,2.790076973885));
#46389=CARTESIAN_POINT('Ctrl Pts',(368.14465844917,-17.7414349694248,2.87187955848261));
#46390=CARTESIAN_POINT('Ctrl Pts',(368.23060918349,-17.7355819480967,2.95002493912365));
#46391=CARTESIAN_POINT('Ctrl Pts',(368.319807980291,-17.7297289267685,3.02419065188109));
#46392=CARTESIAN_POINT('Ctrl Pts',(368.409036526614,-17.7238739533447,3.09838110033589));
#46393=CARTESIAN_POINT('Ctrl Pts',(368.501514971988,-17.7180189799209,3.16858897764201));
#46394=CARTESIAN_POINT('Ctrl Pts',(368.596844834535,-17.7121640064971,3.23453296329477));
#46395=CARTESIAN_POINT('Ctrl Pts',(368.692282741237,-17.706302397213,3.30055168798519));
#46396=CARTESIAN_POINT('Ctrl Pts',(368.790578175458,-17.7004407879289,3.36229664032803));
#46397=CARTESIAN_POINT('Ctrl Pts',(368.891304774407,-17.6945791786447,3.41953054900028));
#46398=CARTESIAN_POINT('Ctrl Pts',(368.992099294042,-17.6887136168344,3.47680305091751));
#46399=CARTESIAN_POINT('Ctrl Pts',(369.095327875743,-17.682848055024,3.52955826466164));
#46400=CARTESIAN_POINT('Ctrl Pts',(369.200542307743,-17.6769824932137,3.57760624817583));
#46401=CARTESIAN_POINT('Ctrl Pts',(369.305910589047,-17.6711083545134,3.6257244896264));
#46402=CARTESIAN_POINT('Ctrl Pts',(369.413270134343,-17.6652342158131,3.66912160962348));
#46403=CARTESIAN_POINT('Ctrl Pts',(369.522155588414,-17.6593600771127,3.70765683293493));
#46404=CARTESIAN_POINT('Ctrl Pts',(369.549690942181,-17.6578746033314,3.71740176181834));
#46405=CARTESIAN_POINT('Ctrl Pts',(369.577323819415,-17.6563891295501,3.72683602521239));
#46406=CARTESIAN_POINT('Ctrl Pts',(369.6050465884,-17.6549036557688,3.73595786345068));
#46407=CARTESIAN_POINT('Ctrl Pts',(369.714664769561,-17.6490299663783,3.77202638593624));
#46408=CARTESIAN_POINT('Ctrl Pts',(369.82605431523,-17.6431562769877,3.80332636779954));
#46409=CARTESIAN_POINT('Ctrl Pts',(369.938762629141,-17.6372825875971,3.82968273367613));
#46410=CARTESIAN_POINT('Ctrl Pts',(370.051325426029,-17.6314164816914,3.8560050710083));
#46411=CARTESIAN_POINT('Ctrl Pts',(370.165203206521,-17.6255503757856,3.87739639218186));
#46412=CARTESIAN_POINT('Ctrl Pts',(370.279926273235,-17.6196842698798,3.89373072721228));
#46413=CARTESIAN_POINT('Ctrl Pts',(370.394531864989,-17.6138241707918,3.91004833609172));
#46414=CARTESIAN_POINT('Ctrl Pts',(370.509980614702,-17.6079640717038,3.92131920098443));
#46415=CARTESIAN_POINT('Ctrl Pts',(370.625791284987,-17.6021039726157,3.92746809921346));
#46416=CARTESIAN_POINT('Ctrl Pts',(370.74578014005,-17.5960324545216,3.9338388356627));
#46417=CARTESIAN_POINT('Ctrl Pts',(370.866157083469,-17.5899609364275,3.93471094705701));
#46418=CARTESIAN_POINT('Ctrl Pts',(370.986379111295,-17.5838894183334,3.93005933464035));
#46419=CARTESIAN_POINT('Ctrl Pts',(371.102281465584,-17.5780360547366,3.92557485837528));
#46420=CARTESIAN_POINT('Ctrl Pts',(371.218039396946,-17.5721826911399,3.91595678793277));
#46421=CARTESIAN_POINT('Ctrl Pts',(371.33316574863,-17.5663293275431,3.9012356731232));
#46422=CARTESIAN_POINT('Ctrl Pts',(371.44827481448,-17.5604768428092,3.88651676863947));
#46423=CARTESIAN_POINT('Ctrl Pts',(371.562752079509,-17.5546243580753,3.86669639567965));
#46424=CARTESIAN_POINT('Ctrl Pts',(371.676116261836,-17.5487718733413,3.84185689989346));
#46425=CARTESIAN_POINT('Ctrl Pts',(371.789490838136,-17.5429188520131,3.81701512665902));
#46426=CARTESIAN_POINT('Ctrl Pts',(371.901751725264,-17.537065830685,3.78715340422332));
#46427=CARTESIAN_POINT('Ctrl Pts',(372.012429271805,-17.5312128093568,3.75240489358614));
#46428=CARTESIAN_POINT('Ctrl Pts',(372.123143731444,-17.5253578359329,3.7176447936496));
#46429=CARTESIAN_POINT('Ctrl Pts',(372.232273406481,-17.5195028625091,3.67799478833975));
#46430=CARTESIAN_POINT('Ctrl Pts',(372.339365880272,-17.5136478890852,3.63363721858418));
#46431=CARTESIAN_POINT('Ctrl Pts',(372.446579729625,-17.5077862798011,3.58922937522082));
#46432=CARTESIAN_POINT('Ctrl Pts',(372.551751387384,-17.5019246705169,3.54010347642277));
#46433=CARTESIAN_POINT('Ctrl Pts',(372.65445033727,-17.4960630612327,3.48648917114653));
#46434=CARTESIAN_POINT('Ctrl Pts',(372.757218537811,-17.4901974994224,3.43283871335054));
#46435=CARTESIAN_POINT('Ctrl Pts',(372.857510353849,-17.484331937612,3.37469402921715));
#46436=CARTESIAN_POINT('Ctrl Pts',(372.954923195721,-17.4784663758017,3.3123287852164));
#46437=CARTESIAN_POINT('Ctrl Pts',(373.05247847906,-17.4725922371013,3.24987234793281));
#46438=CARTESIAN_POINT('Ctrl Pts',(373.147146050141,-17.466718098401,3.18318327104919));
#46439=CARTESIAN_POINT('Ctrl Pts',(373.238555340947,-17.4608439597007,3.11257628061211));
#46440=CARTESIAN_POINT('Ctrl Pts',(373.261671258322,-17.4593584859195,3.09472092539933));
#46441=CARTESIAN_POINT('Ctrl Pts',(373.284578989448,-17.4578730121383,3.07661520573558));
#46442=CARTESIAN_POINT('Ctrl Pts',(373.307272918438,-17.4563875383571,3.05826458067883));
#46443=CARTESIAN_POINT('Ctrl Pts',(373.397006639506,-17.4505138489665,2.98570465194085));
#46444=CARTESIAN_POINT('Ctrl Pts',(373.483693592017,-17.4446401595759,2.90907116048099));
#46445=CARTESIAN_POINT('Ctrl Pts',(373.566941302027,-17.4387664701854,2.82864951647443));
#46446=CARTESIAN_POINT('Ctrl Pts',(373.650081531423,-17.4329003642796,2.7483317043656));
#46447=CARTESIAN_POINT('Ctrl Pts',(373.729791054364,-17.4270342583739,2.66423575045738));
#46448=CARTESIAN_POINT('Ctrl Pts',(373.805709389867,-17.4211681524681,2.57668805561883));
#46449=CARTESIAN_POINT('Ctrl Pts',(373.881549985961,-17.4153080533801,2.48923000850444));
#46450=CARTESIAN_POINT('Ctrl Pts',(373.953606847428,-17.4094479542921,2.39832756122708));
#46451=CARTESIAN_POINT('Ctrl Pts',(374.021555880699,-17.403587855204,2.30434432240852));
#46452=CARTESIAN_POINT('Ctrl Pts',(374.091956360075,-17.3975163371099,2.20697038274338));
#46453=CARTESIAN_POINT('Ctrl Pts',(374.157946688056,-17.3914448190158,2.10628947244759));
#46454=CARTESIAN_POINT('Ctrl Pts',(374.219211406358,-17.3853733009217,2.00274427572518));
#46455=CARTESIAN_POINT('Ctrl Pts',(374.27827483437,-17.379519937325,1.90291954067239));
#46456=CARTESIAN_POINT('Ctrl Pts',(374.332946169868,-17.3736665737282,1.80043319510798));
#46457=CARTESIAN_POINT('Ctrl Pts',(374.38298699179,-17.3678132101315,1.69571116201729));
#46458=CARTESIAN_POINT('Ctrl Pts',(374.43302030025,-17.3619607253976,1.59100485258745));
#46459=CARTESIAN_POINT('Ctrl Pts',(374.478424299484,-17.3561082406637,1.48406389576369));
#46460=CARTESIAN_POINT('Ctrl Pts',(374.519007277702,-17.3502557559298,1.37533735684865));
#46461=CARTESIAN_POINT('Ctrl Pts',(374.559593976833,-17.3444027346017,1.26660084916981));
#46462=CARTESIAN_POINT('Ctrl Pts',(374.595358631766,-17.3385497132735,1.156078821034));
#46463=CARTESIAN_POINT('Ctrl Pts',(374.626158536234,-17.3326966919453,1.0442381120572));
#46464=CARTESIAN_POINT('Ctrl Pts',(374.656968713064,-17.3268417185215,0.932360102044108));
#46465=CARTESIAN_POINT('Ctrl Pts',(374.682810737231,-17.3209867450977,0.819162934758138));
#46466=CARTESIAN_POINT('Ctrl Pts',(374.703592571882,-17.3151317716739,0.705125628206122));
#46467=CARTESIAN_POINT('Ctrl Pts',(374.724397960073,-17.3092701623897,0.590959075014662));
#46468=CARTESIAN_POINT('Ctrl Pts',(374.740131637772,-17.3034085531056,0.475950888721588));
#46469=CARTESIAN_POINT('Ctrl Pts',(374.750753193829,-17.2975469438215,0.360587330416915));
#46470=CARTESIAN_POINT('Ctrl Pts',(374.76138191208,-17.2916813820111,0.245145981617632));
#46471=CARTESIAN_POINT('Ctrl Pts',(374.766891625081,-17.2858158202008,0.129349195307191));
#46472=CARTESIAN_POINT('Ctrl Pts',(374.767294049227,-17.2799502583904,0.013683627934948));
#46473=CARTESIAN_POINT('Ctrl Pts',(374.767697061816,-17.2740761196901,-0.102151070865607));
#46474=CARTESIAN_POINT('Ctrl Pts',(374.762977897856,-17.2682019809898,-0.217853756580347));
#46475=CARTESIAN_POINT('Ctrl Pts',(374.753200135664,-17.2623278422895,-0.332942422010732));
#46476=CARTESIAN_POINT('Ctrl Pts',(374.750727499229,-17.2608423685082,-0.362046466662447));
#46477=CARTESIAN_POINT('Ctrl Pts',(374.747931619835,-17.2593568947268,-0.391111295725008));
#46478=CARTESIAN_POINT('Ctrl Pts',(374.744814040346,-17.2578714209455,-0.420129230717538));
#46479=CARTESIAN_POINT('Ctrl Pts',(374.732486866484,-17.2519977315549,-0.534868608177085));
#46480=CARTESIAN_POINT('Ctrl Pts',(374.715084963688,-17.2461240421644,-0.649256079204849));
#46481=CARTESIAN_POINT('Ctrl Pts',(374.692635400511,-17.2402503527738,-0.762807121295351));
#46482=CARTESIAN_POINT('Ctrl Pts',(374.670214821828,-17.234384246868,-0.876211558322815));
#46483=CARTESIAN_POINT('Ctrl Pts',(374.642759622345,-17.2285181409623,-0.98878131239848));
#46484=CARTESIAN_POINT('Ctrl Pts',(374.610348659104,-17.2226520350565,-1.10003652350676));
#46485=CARTESIAN_POINT('Ctrl Pts',(374.577970884275,-17.2167919359685,-1.21117781069622));
#46486=CARTESIAN_POINT('Ctrl Pts',(374.540647554432,-17.2109318368804,-1.3210068380751));
#46487=CARTESIAN_POINT('Ctrl Pts',(374.498508518548,-17.2050717377924,-1.42905415158215));
#46488=CARTESIAN_POINT('Ctrl Pts',(374.454849202383,-17.1990002196983,-1.54099956566508));
#46489=CARTESIAN_POINT('Ctrl Pts',(374.406020227831,-17.1929287016042,-1.65103183515607));
#46490=CARTESIAN_POINT('Ctrl Pts',(374.352222572966,-17.1868571835101,-1.75864589466433));
#46491=CARTESIAN_POINT('Ctrl Pts',(374.300357910833,-17.1810038199133,-1.8623932950115));
#46492=CARTESIAN_POINT('Ctrl Pts',(374.243875681377,-17.1751504563166,-1.96389286992713));
#46493=CARTESIAN_POINT('Ctrl Pts',(374.183004540698,-17.1692970927198,-2.06271337541898));
#46494=CARTESIAN_POINT('Ctrl Pts',(374.122142539616,-17.1634446079859,-2.16151904334446));
#46495=CARTESIAN_POINT('Ctrl Pts',(374.056893154232,-17.157592123252,-2.25764609000586));
#46496=CARTESIAN_POINT('Ctrl Pts',(373.987529808859,-17.1517396385181,-2.35068997590965));
#46497=CARTESIAN_POINT('Ctrl Pts',(373.918160103798,-17.1458866171899,-2.44374239268857));
#46498=CARTESIAN_POINT('Ctrl Pts',(373.844675935864,-17.1400335958617,-2.5337107555099));
#46499=CARTESIAN_POINT('Ctrl Pts',(373.767392231623,-17.1341805745335,-2.62022206898151));
#46500=CARTESIAN_POINT('Ctrl Pts',(373.690082751775,-17.1283256011097,-2.70676223564684));
#46501=CARTESIAN_POINT('Ctrl Pts',(373.608971490908,-17.1224706276859,-2.78984275234716));
#46502=CARTESIAN_POINT('Ctrl Pts',(373.524411077558,-17.1166156542621,-2.86912659957516));
#46503=CARTESIAN_POINT('Ctrl Pts',(373.439754825842,-17.1107540449779,-2.94850030486038));
#46504=CARTESIAN_POINT('Ctrl Pts',(373.35164192073,-17.1048924356937,-3.02406846932926));
#46505=CARTESIAN_POINT('Ctrl Pts',(373.260459063966,-17.0990308264096,-3.09553352841481));
#46506=CARTESIAN_POINT('Ctrl Pts',(373.169214721931,-17.0931652645992,-3.16704677691452));
#46507=CARTESIAN_POINT('Ctrl Pts',(373.074896641534,-17.0872997027889,-3.23445117118757));
#46508=CARTESIAN_POINT('Ctrl Pts',(372.977920115577,-17.0814341409785,-3.29749273552443));
#46509=CARTESIAN_POINT('Ctrl Pts',(372.880801786154,-17.0755600022782,-3.3606264820903));
#46510=CARTESIAN_POINT('Ctrl Pts',(372.781017607738,-17.0696858635779,-3.41938445795735));
#46511=CARTESIAN_POINT('Ctrl Pts',(372.679007081172,-17.0638117248775,-3.47355878779874));
#46512=CARTESIAN_POINT('Ctrl Pts',(372.653210284338,-17.0623262510963,-3.48725859141288));
#46513=CARTESIAN_POINT('Ctrl Pts',(372.627271207589,-17.060840777315,-3.50066551228831));
#46514=CARTESIAN_POINT('Ctrl Pts',(372.601197139614,-17.0593553035338,-3.51377668432798));
#46515=CARTESIAN_POINT('Ctrl Pts',(372.498098062157,-17.0534816141432,-3.56561937120597));
#46516=CARTESIAN_POINT('Ctrl Pts',(372.392543635615,-17.0476079247526,-3.61300695171475));
#46517=CARTESIAN_POINT('Ctrl Pts',(372.284955682171,-17.041734235362,-3.65569950751248));
#46518=CARTESIAN_POINT('Ctrl Pts',(372.177506634883,-17.0358681294563,-3.69833694320987));
#46519=CARTESIAN_POINT('Ctrl Pts',(372.068029662409,-17.0300020235505,-3.73629125797415));
#46520=CARTESIAN_POINT('Ctrl Pts',(371.956970744038,-17.0241359176448,-3.7693685793176));
#46521=CARTESIAN_POINT('Ctrl Pts',(371.846025548585,-17.0182758185567,-3.80241202990538));
#46522=CARTESIAN_POINT('Ctrl Pts',(371.733502022937,-17.0124157194687,-3.83058830328173));
#46523=CARTESIAN_POINT('Ctrl Pts',(371.61986504539,-17.0065556203807,-3.85375201704524));
#46524=CARTESIAN_POINT('Ctrl Pts',(371.50212830494,-17.0004841022865,-3.87775142475645));
#46525=CARTESIAN_POINT('Ctrl Pts',(371.383196673924,-16.9944125841924,-3.89636959407857));
#46526=CARTESIAN_POINT('Ctrl Pts',(371.263603514877,-16.9883410660983,-3.90950160771155));
#46527=CARTESIAN_POINT('Ctrl Pts',(371.148307433611,-16.9824877025016,-3.92216177759986));
#46528=CARTESIAN_POINT('Ctrl Pts',(371.03239699053,-16.9766343389048,-3.92972320188549));
#46529=CARTESIAN_POINT('Ctrl Pts',(370.916358519993,-16.9707809753081,-3.93214424061429));
#46530=CARTESIAN_POINT('Ctrl Pts',(370.800337472241,-16.9649284905742,-3.93456491583227));
#46531=CARTESIAN_POINT('Ctrl Pts',(370.684188848199,-16.9590760058403,-3.93184673152903));
#46532=CARTESIAN_POINT('Ctrl Pts',(370.568400811497,-16.9532235211064,-3.92400014359316));
#46533=CARTESIAN_POINT('Ctrl Pts',(370.452602158587,-16.9473704997782,-3.91615283623052));
#46534=CARTESIAN_POINT('Ctrl Pts',(370.337164570962,-16.94151747845,-3.90317621844518));
#46535=CARTESIAN_POINT('Ctrl Pts',(370.222572204265,-16.9356644571218,-3.88513272115385));
#46536=CARTESIAN_POINT('Ctrl Pts',(370.107941618801,-16.929809483698,-3.86708320600773));
#46537=CARTESIAN_POINT('Ctrl Pts',(369.994157222702,-16.9239545102742,-3.84396351528716));
#46538=CARTESIAN_POINT('Ctrl Pts',(369.881693379389,-16.9180995368504,-3.81588726403835));
#46539=CARTESIAN_POINT('Ctrl Pts',(369.769102072754,-16.9122379275662,-3.78777919196498));
#46540=CARTESIAN_POINT('Ctrl Pts',(369.657834707248,-16.9063763182821,-3.75470344704786));
#46541=CARTESIAN_POINT('Ctrl Pts',(369.548350963405,-16.9005147089979,-3.7168236652132));
#46542=CARTESIAN_POINT('Ctrl Pts',(369.438793393869,-16.8946491471876,-3.67891834076345));
#46543=CARTESIAN_POINT('Ctrl Pts',(369.331022223981,-16.8887835853773,-3.63620268089129));
#46544=CARTESIAN_POINT('Ctrl Pts',(369.225476005703,-16.8829180235669,-3.58888797675068));
#46545=CARTESIAN_POINT('Ctrl Pts',(369.119775452967,-16.8770438848666,-3.54150408690794));
#46546=CARTESIAN_POINT('Ctrl Pts',(369.016306712592,-16.8711697461663,-3.48950791632338));
#46547=CARTESIAN_POINT('Ctrl Pts',(368.915482721435,-16.8652956074659,-3.43315608981197));
#46548=CARTESIAN_POINT('Ctrl Pts',(368.889985980036,-16.8638101336847,-3.41890563283775));
#46549=CARTESIAN_POINT('Ctrl Pts',(368.864658219004,-16.8623246599034,-3.40437684241616));
#46550=CARTESIAN_POINT('Ctrl Pts',(368.839505798013,-16.8608391861221,-3.38957428955112));
#46551=CARTESIAN_POINT('Ctrl Pts',(368.740050990944,-16.8549654967315,-3.3310437393572));
#46552=CARTESIAN_POINT('Ctrl Pts',(368.643008776625,-16.849091807341,-3.26803478452446));
#46553=CARTESIAN_POINT('Ctrl Pts',(368.548809434139,-16.8432181179504,-3.20077182352843));
#46554=CARTESIAN_POINT('Ctrl Pts',(368.454731711855,-16.8373520120447,-3.13359570533412));
#46555=CARTESIAN_POINT('Ctrl Pts',(368.363489895308,-16.8314859061389,-3.06217674129353));
#46556=CARTESIAN_POINT('Ctrl Pts',(368.275488666688,-16.8256198002332,-2.98678459118322));
#46557=CARTESIAN_POINT('Ctrl Pts',(368.187577550204,-16.8197597011451,-2.91146964167412));
#46558=CARTESIAN_POINT('Ctrl Pts',(368.102900733115,-16.8138996020571,-2.83218986585944));
#46559=CARTESIAN_POINT('Ctrl Pts',(368.021832396338,-16.8080395029691,-2.74925709143536));
#46560=CARTESIAN_POINT('Ctrl Pts',(367.937839298918,-16.801967984875,-2.66333229171));
#46561=CARTESIAN_POINT('Ctrl Pts',(367.857720336802,-16.7958964667808,-2.57348619555311));
#46562=CARTESIAN_POINT('Ctrl Pts',(367.781852813725,-16.7898249486867,-2.48011011502305));
#46563=CARTESIAN_POINT('Ctrl Pts',(367.708711271385,-16.78397158509,-2.39008911169083));
#46564=CARTESIAN_POINT('Ctrl Pts',(367.639521193603,-16.7781182214932,-2.29678777681932));
#46565=CARTESIAN_POINT('Ctrl Pts',(367.574581217239,-16.7722648578965,-2.20059220757036));
#46566=CARTESIAN_POINT('Ctrl Pts',(367.509650991395,-16.7664123731626,-2.1044110817624));
#46567=CARTESIAN_POINT('Ctrl Pts',(367.448969829211,-16.7605598884287,-2.00533692797415));
#46568=CARTESIAN_POINT('Ctrl Pts',(367.39279358267,-16.7547074036948,-1.90378562217243));
#46569=CARTESIAN_POINT('Ctrl Pts',(367.336612185522,-16.7488543823666,-1.80222500547942));
#46570=CARTESIAN_POINT('Ctrl Pts',(367.284936725098,-16.7430013610385,-1.69818714681387));
#46571=CARTESIAN_POINT('Ctrl Pts',(367.237977205588,-16.7371483397103,-1.59211273035536));
#46572=CARTESIAN_POINT('Ctrl Pts',(367.191002024171,-16.7312933662865,-1.48600293603049));
#46573=CARTESIAN_POINT('Ctrl Pts',(367.148746078379,-16.7254383928627,-1.37785561086782));
#46574=CARTESIAN_POINT('Ctrl Pts',(367.111371053518,-16.7195834194389,-1.26813095796898));
#46575=CARTESIAN_POINT('Ctrl Pts',(367.073953668867,-16.7137218101547,-1.15828194626963));
#46576=CARTESIAN_POINT('Ctrl Pts',(367.041428379768,-16.7078602008705,-1.04685242999428));
#46577=CARTESIAN_POINT('Ctrl Pts',(367.013906878856,-16.7019985915864,-0.934317390893775));
#46578=CARTESIAN_POINT('Ctrl Pts',(366.986366819993,-16.696133029776,-0.821706468590008));
#46579=CARTESIAN_POINT('Ctrl Pts',(366.963837347974,-16.6902674679657,-0.707988943345657));
#46580=CARTESIAN_POINT('Ctrl Pts',(366.946378656372,-16.6844019061554,-0.593647876758552));
#46581=CARTESIAN_POINT('Ctrl Pts',(366.92889443588,-16.6785277674551,-0.479139615488192));
#46582=CARTESIAN_POINT('Ctrl Pts',(366.916495837798,-16.6726536287547,-0.364006402401481));
#46583=CARTESIAN_POINT('Ctrl Pts',(366.909191075276,-16.6667794900544,-0.248734350331171));
#46584=CARTESIAN_POINT('Ctrl Pts',(366.907343820085,-16.6652940162731,-0.219583930192212));
#46585=CARTESIAN_POINT('Ctrl Pts',(366.905822056539,-16.6638085424918,-0.19042461837385));
#46586=CARTESIAN_POINT('Ctrl Pts',(366.904625391226,-16.6623230687105,-0.161264236942553));
#46587=CARTESIAN_POINT('Ctrl Pts',(366.902434340218,-16.6596032198186,-0.107872630763614));
#46588=CARTESIAN_POINT('Ctrl Pts',(366.901331356318,-16.6568833709268,-0.0544360677886615));
#46589=CARTESIAN_POINT('Ctrl Pts',(366.901317976443,-16.654163522035,-0.000984499569211797));
#46590=CARTESIAN_POINT('',(366.90131898798,-15.4041635220771,-0.00298763949216439));
#46591=CARTESIAN_POINT('Ctrl Pts',(366.901317976443,-16.6541635220067,-0.000984499013828783));
#46592=CARTESIAN_POINT('Ctrl Pts',(366.901289272163,-16.6483285386861,0.113686948345892));
#46593=CARTESIAN_POINT('Ctrl Pts',(366.906279900742,-16.6424935553654,0.228559854945339));
#46594=CARTESIAN_POINT('Ctrl Pts',(366.916316614802,-16.6366585720448,0.343154915056637));
#46595=CARTESIAN_POINT('Ctrl Pts',(366.926340568907,-16.6308310069019,0.457604287256876));
#46596=CARTESIAN_POINT('Ctrl Pts',(366.941397817925,-16.625003441759,0.571776101619367));
#46597=CARTESIAN_POINT('Ctrl Pts',(366.9614631222,-16.6191758766162,0.68518992431947));
#46598=CARTESIAN_POINT('Ctrl Pts',(366.981508457437,-16.6133541110802,0.79849087730859));
#46599=CARTESIAN_POINT('Ctrl Pts',(367.006551864193,-16.6075323455443,0.911034928450505));
#46600=CARTESIAN_POINT('Ctrl Pts',(367.036516271438,-16.6017105800084,1.02234639207432));
#46601=CARTESIAN_POINT('Ctrl Pts',(367.066460120965,-16.5958928086184,1.13358148810336));
#46602=CARTESIAN_POINT('Ctrl Pts',(367.101318148562,-16.5900750372285,1.24358527486813));
#46603=CARTESIAN_POINT('Ctrl Pts',(367.140962274659,-16.5842572658385,1.35189258829449));
#46604=CARTESIAN_POINT('Ctrl Pts',(367.180592203786,-16.5784415778525,1.46016111575435));
#46605=CARTESIAN_POINT('Ctrl Pts',(367.22500468116,-16.5726258898665,1.56673398421441));
#46606=CARTESIAN_POINT('Ctrl Pts',(367.274022078907,-16.5668102018805,1.67116217028183));
#46607=CARTESIAN_POINT('Ctrl Pts',(367.323034171011,-16.5609951433846,1.77557905304157));
#46608=CARTESIAN_POINT('Ctrl Pts',(367.376650014403,-16.5551800848887,1.87785133560505));
#46609=CARTESIAN_POINT('Ctrl Pts',(367.434644568087,-16.5493650263928,1.97755165655074));
#46610=CARTESIAN_POINT('Ctrl Pts',(367.492647335919,-16.5435491442721,2.07726609870441));
#46611=CARTESIAN_POINT('Ctrl Pts',(367.555029835655,-16.5377332621515,2.17440749309849));
#46612=CARTESIAN_POINT('Ctrl Pts',(367.621522377866,-16.5319173800309,2.26857537532211));
#46613=CARTESIAN_POINT('Ctrl Pts',(367.688083066218,-16.5260955373933,2.36283976728419));
#46614=CARTESIAN_POINT('Ctrl Pts',(367.758761967659,-16.5202736947556,2.45412421762823));
#46615=CARTESIAN_POINT('Ctrl Pts',(367.833247496876,-16.514451852118,2.54205934554102));
#46616=CARTESIAN_POINT('Ctrl Pts',(367.907771530795,-16.5086269999252,2.63003993081756));
#46617=CARTESIAN_POINT('Ctrl Pts',(367.986105826632,-16.5028021477324,2.71466743813535));
#46618=CARTESIAN_POINT('Ctrl Pts',(368.06790144736,-16.4969772955396,2.79560892640024));
#46619=CARTESIAN_POINT('Ctrl Pts',(368.149831300989,-16.4911428843166,2.87668324586925));
#46620=CARTESIAN_POINT('Ctrl Pts',(368.235233516678,-16.4853084730937,2.95405918018264));
#46621=CARTESIAN_POINT('Ctrl Pts',(368.323725223505,-16.4794740618707,3.02744341773692));
#46622=CARTESIAN_POINT('Ctrl Pts',(368.40293397897,-16.4742516916801,3.09312950670421));
#46623=CARTESIAN_POINT('Ctrl Pts',(368.484617425624,-16.4690293214894,3.15561790045603));
#46624=CARTESIAN_POINT('Ctrl Pts',(368.568482590461,-16.4638069512988,3.21472853628711));
#46625=CARTESIAN_POINT('Ctrl Pts',(368.662807180821,-16.4579332619082,3.28121128298605));
#46626=CARTESIAN_POINT('Ctrl Pts',(368.760217391912,-16.4520595725177,3.34364981695612));
#46627=CARTESIAN_POINT('Ctrl Pts',(368.860331403367,-16.4461858831271,3.40174462530376));
#46628=CARTESIAN_POINT('Ctrl Pts',(368.960316158229,-16.4403197772213,3.45976442779601));
#46629=CARTESIAN_POINT('Ctrl Pts',(369.062997417204,-16.4344536713156,3.51345145198798));
#46630=CARTESIAN_POINT('Ctrl Pts',(369.167962675288,-16.4285875654098,3.56254816402064));
#46631=CARTESIAN_POINT('Ctrl Pts',(369.272820450285,-16.4227274663218,3.61159460164553));
#46632=CARTESIAN_POINT('Ctrl Pts',(369.379957200345,-16.4168673672338,3.65605990263528));
#46633=CARTESIAN_POINT('Ctrl Pts',(369.488934575887,-16.4110072681458,3.69573170523251));
#46634=CARTESIAN_POINT('Ctrl Pts',(369.601843606521,-16.4049357500516,3.73683477596164));
#46635=CARTESIAN_POINT('Ctrl Pts',(369.716728190647,-16.3988642319575,3.77279171431088));
#46636=CARTESIAN_POINT('Ctrl Pts',(369.833076274915,-16.3927927138634,3.80342007959482));
#46637=CARTESIAN_POINT('Ctrl Pts',(369.945243879532,-16.3869393502667,3.83294794323654));
#46638=CARTESIAN_POINT('Ctrl Pts',(370.058771190997,-16.3810859866699,3.85752344941448));
#46639=CARTESIAN_POINT('Ctrl Pts',(370.173183336342,-16.3752326230732,3.87703367932067));
#46640=CARTESIAN_POINT('Ctrl Pts',(370.287578303087,-16.3693801383393,3.8965409798315));
#46641=CARTESIAN_POINT('Ctrl Pts',(370.40285743239,-16.3635276536054,3.91098444686748));
#46642=CARTESIAN_POINT('Ctrl Pts',(370.518536357881,-16.3576751688715,3.92030241782428));
#46643=CARTESIAN_POINT('Ctrl Pts',(370.634225889576,-16.3518221475433,3.92962124311391));
#46644=CARTESIAN_POINT('Ctrl Pts',(370.750314878494,-16.3459691262151,3.9338136049559));
#46645=CARTESIAN_POINT('Ctrl Pts',(370.866315256099,-16.3401161048869,3.93286983845248));
#46646=CARTESIAN_POINT('Ctrl Pts',(370.98235432207,-16.3342611314631,3.93192575718471));
#46647=CARTESIAN_POINT('Ctrl Pts',(371.098304305053,-16.3284061580393,3.92584214471083));
#46648=CARTESIAN_POINT('Ctrl Pts',(371.213679271971,-16.3225511846155,3.91466140476619));
#46649=CARTESIAN_POINT('Ctrl Pts',(371.329185001595,-16.3166895753313,3.90346799288891));
#46650=CARTESIAN_POINT('Ctrl Pts',(371.444114002938,-16.3108279660472,3.8871659629905));
#46651=CARTESIAN_POINT('Ctrl Pts',(371.557987487129,-16.304966356763,3.86584935828651));
#46652=CARTESIAN_POINT('Ctrl Pts',(371.671937757046,-16.2991007949527,3.84451837963943));
#46653=CARTESIAN_POINT('Ctrl Pts',(371.78483069124,-16.2932352331423,3.8181661868216));
#46654=CARTESIAN_POINT('Ctrl Pts',(371.896201369164,-16.287369671332,3.78693707349024));
#46655=CARTESIAN_POINT('Ctrl Pts',(372.007734898335,-16.2814955326316,3.75566229553574));
#46656=CARTESIAN_POINT('Ctrl Pts',(372.117741337905,-16.2756213939313,3.71949649341316));
#46657=CARTESIAN_POINT('Ctrl Pts',(372.225774415544,-16.269747255231,3.67863257681136));
#46658=CARTESIAN_POINT('Ctrl Pts',(372.253094217225,-16.2682617814497,3.66829875941133));
#46659=CARTESIAN_POINT('Ctrl Pts',(372.280287941014,-16.2667763076684,3.65766472835757));
#46660=CARTESIAN_POINT('Ctrl Pts',(372.307348622577,-16.2652908338872,3.64673406660523));
#46661=CARTESIAN_POINT('Ctrl Pts',(372.414348853888,-16.2594171444966,3.60351330244472));
#46662=CARTESIAN_POINT('Ctrl Pts',(372.519623445852,-16.2535434551061,3.55550726078602));
#46663=CARTESIAN_POINT('Ctrl Pts',(372.622713726984,-16.2476697657155,3.50287441949009));
#46664=CARTESIAN_POINT('Ctrl Pts',(372.725670908878,-16.2418036598097,3.45030953213686));
#46665=CARTESIAN_POINT('Ctrl Pts',(372.826449023692,-16.235937553904,3.39312991089134));
#46666=CARTESIAN_POINT('Ctrl Pts',(372.924608040818,-16.2300714479982,3.33154257539175));
#46667=CARTESIAN_POINT('Ctrl Pts',(373.022666544361,-16.2242113489102,3.27001830453916));
#46668=CARTESIAN_POINT('Ctrl Pts',(373.118110936897,-16.2183512498221,3.20409551531621));
#46669=CARTESIAN_POINT('Ctrl Pts',(373.210525135698,-16.2124911507341,3.13402743298718));
#46670=CARTESIAN_POINT('Ctrl Pts',(373.306273427962,-16.20641963264,3.06143145409861));
#46671=CARTESIAN_POINT('Ctrl Pts',(373.398768351141,-16.2003481145459,2.98438563480101));
#46672=CARTESIAN_POINT('Ctrl Pts',(373.487579009906,-16.1942765964518,2.90322135471013));
#46673=CARTESIAN_POINT('Ctrl Pts',(373.573198630725,-16.188423232855,2.82497337206782));
#46674=CARTESIAN_POINT('Ctrl Pts',(373.65539385672,-16.1825698692583,2.7428980970087));
#46675=CARTESIAN_POINT('Ctrl Pts',(373.733812368177,-16.1767165056615,2.65733335465462));
#46676=CARTESIAN_POINT('Ctrl Pts',(373.812219105358,-16.1708640209276,2.57178145955866));
#46677=CARTESIAN_POINT('Ctrl Pts',(373.886849976465,-16.1650115361937,2.4827414434387));
#46678=CARTESIAN_POINT('Ctrl Pts',(373.957390586312,-16.1591590514598,2.39058689527163));
#46679=CARTESIAN_POINT('Ctrl Pts',(374.027937663785,-16.1533060301316,2.29842389776959));
#46680=CARTESIAN_POINT('Ctrl Pts',(374.094393483355,-16.1474530088034,2.20314612863588));
#46681=CARTESIAN_POINT('Ctrl Pts',(374.156485336937,-16.1415999874752,2.10515847625797));
#46682=CARTESIAN_POINT('Ctrl Pts',(374.218597899351,-16.1357450140514,2.0071381431058));
#46683=CARTESIAN_POINT('Ctrl Pts',(374.276343380626,-16.1298900406276,1.90640647833789));
#46684=CARTESIAN_POINT('Ctrl Pts',(374.329493984012,-16.1240350672038,1.80339480280124));
#46685=CARTESIAN_POINT('Ctrl Pts',(374.38270482678,-16.1181734579196,1.70026637676184));
#46686=CARTESIAN_POINT('Ctrl Pts',(374.431310207849,-16.1123118486355,1.59485314960579));
#46687=CARTESIAN_POINT('Ctrl Pts',(374.475129596472,-16.1064502393513,1.48760843309944));
#46688=CARTESIAN_POINT('Ctrl Pts',(374.51897853283,-16.100584677541,1.38029140069316));
#46689=CARTESIAN_POINT('Ctrl Pts',(374.558034911766,-16.0947191157306,1.27114080783373));
#46690=CARTESIAN_POINT('Ctrl Pts',(374.592167946523,-16.0888535539203,1.16062555386829));
#46691=CARTESIAN_POINT('Ctrl Pts',(374.626350892148,-16.08297941522,1.04994869949578));
#46692=CARTESIAN_POINT('Ctrl Pts',(374.655596021987,-16.0771052765196,0.937903599777784));
#46693=CARTESIAN_POINT('Ctrl Pts',(374.679823511091,-16.0712311378193,0.824969839033651));
#46694=CARTESIAN_POINT('Ctrl Pts',(374.685950247568,-16.069745664038,0.796410734599247));
#46695=CARTESIAN_POINT('Ctrl Pts',(374.691756364132,-16.0682601902568,0.767794825730232));
#46696=CARTESIAN_POINT('Ctrl Pts',(374.697241096136,-16.0667747164755,0.739129906964046));
#46697=CARTESIAN_POINT('Ctrl Pts',(374.718928191924,-16.0609010270849,0.625786385616273));
#46698=CARTESIAN_POINT('Ctrl Pts',(374.735658695976,-16.0550273376944,0.51129878810818));
#46699=CARTESIAN_POINT('Ctrl Pts',(374.747317128308,-16.0491536483038,0.396138452044766));
#46700=CARTESIAN_POINT('Ctrl Pts',(374.758960508509,-16.043287542398,0.281126798793892));
#46701=CARTESIAN_POINT('Ctrl Pts',(374.765544798619,-16.0374214364923,0.165444541575756));
#46702=CARTESIAN_POINT('Ctrl Pts',(374.767005414085,-16.0315553305865,0.0495736688790276));
#46703=CARTESIAN_POINT('Ctrl Pts',(374.7684645339,-16.0256952314985,-0.0661785535205626));
#46704=CARTESIAN_POINT('Ctrl Pts',(374.764810409773,-16.0198351324104,-0.182118596570821));
#46705=CARTESIAN_POINT('Ctrl Pts',(374.756030266475,-16.0139750333223,-0.297759546865992));
#46706=CARTESIAN_POINT('Ctrl Pts',(374.746933355639,-16.0079035152282,-0.417572558827964));
#46707=CARTESIAN_POINT('Ctrl Pts',(374.732333526664,-16.0018319971341,-0.537064040026449));
#46708=CARTESIAN_POINT('Ctrl Pts',(374.712275647986,-15.99576047904,-0.655692261693141));
#46709=CARTESIAN_POINT('Ctrl Pts',(374.692938464919,-15.9899071154433,-0.770058076550187));
#46710=CARTESIAN_POINT('Ctrl Pts',(374.668528780996,-15.9840537518465,-0.883621157184588));
#46711=CARTESIAN_POINT('Ctrl Pts',(374.639139477452,-15.9782003882498,-0.995902308365154));
#46712=CARTESIAN_POINT('Ctrl Pts',(374.609754586613,-15.9723479035159,-1.1081666009087));
#46713=CARTESIAN_POINT('Ctrl Pts',(374.575391667394,-15.966495418782,-1.21914894714273));
#46714=CARTESIAN_POINT('Ctrl Pts',(374.536194212923,-15.9606429340481,-1.32838263218773));
#46715=CARTESIAN_POINT('Ctrl Pts',(374.496993164573,-15.9547899127199,-1.43762633249508));
#46716=CARTESIAN_POINT('Ctrl Pts',(374.452956839356,-15.9489368913917,-1.54512066400708));
#46717=CARTESIAN_POINT('Ctrl Pts',(374.404277630517,-15.9430838700635,-1.65041697413445));
#46718=CARTESIAN_POINT('Ctrl Pts',(374.355582186221,-15.9372288966397,-1.75574840261525));
#46719=CARTESIAN_POINT('Ctrl Pts',(374.302240952471,-15.9313739232158,-1.85887997720267));
#46720=CARTESIAN_POINT('Ctrl Pts',(374.244492880775,-15.925518949792,-1.95938645536516));
#46721=CARTESIAN_POINT('Ctrl Pts',(374.186679359057,-15.9196573405078,-2.06000684471049));
#46722=CARTESIAN_POINT('Ctrl Pts',(374.124449236442,-15.9137957312236,-2.1579958408669));
#46723=CARTESIAN_POINT('Ctrl Pts',(374.05808556693,-15.9079341219395,-2.25295599780995));
#46724=CARTESIAN_POINT('Ctrl Pts',(373.991677147908,-15.9020685601292,-2.34798018708392));
#46725=CARTESIAN_POINT('Ctrl Pts',(373.921129882688,-15.8962029983188,-2.43997114330849));
#46726=CARTESIAN_POINT('Ctrl Pts',(373.846766890326,-15.8903374365085,-2.52856477054929));
#46727=CARTESIAN_POINT('Ctrl Pts',(373.77229516103,-15.8844632978082,-2.61728794340256));
#46728=CARTESIAN_POINT('Ctrl Pts',(373.693996847533,-15.8785891591078,-2.70260356971809));
#46729=CARTESIAN_POINT('Ctrl Pts',(373.612231674436,-15.8727150204075,-2.78418458474306));
#46730=CARTESIAN_POINT('Ctrl Pts',(373.591554596987,-15.8712295466263,-2.80481509162167));
#46731=CARTESIAN_POINT('Ctrl Pts',(373.570655975222,-15.8697440728451,-2.82520697329511));
#46732=CARTESIAN_POINT('Ctrl Pts',(373.549541944429,-15.8682585990639,-2.84535536173276));
#46733=CARTESIAN_POINT('Ctrl Pts',(373.466055274903,-15.8623849096733,-2.92502379943988));
#46734=CARTESIAN_POINT('Ctrl Pts',(373.37892021368,-15.8565112202828,-3.00114738878447));
#46735=CARTESIAN_POINT('Ctrl Pts',(373.28847022665,-15.8506375308922,-3.07337357443036));
#46736=CARTESIAN_POINT('Ctrl Pts',(373.198137019051,-15.8447714249864,-3.14550650928519));
#46737=CARTESIAN_POINT('Ctrl Pts',(373.10449771682,-15.8389053190807,-3.2137517918253));
#46738=CARTESIAN_POINT('Ctrl Pts',(373.007922326767,-15.8330392131749,-3.27779386060109));
#46739=CARTESIAN_POINT('Ctrl Pts',(372.911445828683,-15.8271791140869,-3.34177035111417));
#46740=CARTESIAN_POINT('Ctrl Pts',(372.81203956526,-15.8213190149989,-3.40155196197912));
#46741=CARTESIAN_POINT('Ctrl Pts',(372.71010576808,-15.8154589159109,-3.4568639976836));
#46742=CARTESIAN_POINT('Ctrl Pts',(372.604494432045,-15.8093873978168,-3.51417156544958));
#46743=CARTESIAN_POINT('Ctrl Pts',(372.496170096574,-15.8033158797227,-3.56668068303658));
#46744=CARTESIAN_POINT('Ctrl Pts',(372.385612304205,-15.7972443616286,-3.614135377425));
#46745=CARTESIAN_POINT('Ctrl Pts',(372.279026941672,-15.7913909980318,-3.65988498671914));
#46746=CARTESIAN_POINT('Ctrl Pts',(372.170366272047,-15.7855376344351,-3.70093696388265));
#46747=CARTESIAN_POINT('Ctrl Pts',(372.060083318644,-15.7796842708383,-3.73710958145248));
#46748=CARTESIAN_POINT('Ctrl Pts',(371.949816923855,-15.7738317861044,-3.77327676782547));
#46749=CARTESIAN_POINT('Ctrl Pts',(371.837929122079,-15.7679793013705,-3.80456592260049));
#46750=CARTESIAN_POINT('Ctrl Pts',(371.724889886481,-15.7621268166366,-3.83084461360422));
#46751=CARTESIAN_POINT('Ctrl Pts',(371.611840286703,-15.7562737953084,-3.85712571401107));
#46752=CARTESIAN_POINT('Ctrl Pts',(371.497639445674,-15.7504207739803,-3.87839534386183));
#46753=CARTESIAN_POINT('Ctrl Pts',(371.382768667892,-15.7445677526521,-3.89457195387243));
#46754=CARTESIAN_POINT('Ctrl Pts',(371.267859578487,-15.7387127792283,-3.91075395909494));
#46755=CARTESIAN_POINT('Ctrl Pts',(371.152280516923,-15.7328578058044,-3.92183950926487));
#46756=CARTESIAN_POINT('Ctrl Pts',(371.036518355719,-15.7270028323806,-3.92779886918752));
#46757=CARTESIAN_POINT('Ctrl Pts',(370.920624992975,-15.7211412230964,-3.93376498327917));
#46758=CARTESIAN_POINT('Ctrl Pts',(370.804548529225,-15.7152796138123,-3.93459328970434));
#46759=CARTESIAN_POINT('Ctrl Pts',(370.688776387746,-15.7094180045281,-3.93030618168947));
#46760=CARTESIAN_POINT('Ctrl Pts',(370.572926180261,-15.7035524427178,-3.92601618284617));
#46761=CARTESIAN_POINT('Ctrl Pts',(370.457381114422,-15.6976868809075,-3.91660393457932));
#46762=CARTESIAN_POINT('Ctrl Pts',(370.342622308813,-15.6918213190971,-3.90214357649819));
#46763=CARTESIAN_POINT('Ctrl Pts',(370.227695697683,-15.6859471803968,-3.88766207382693));
#46764=CARTESIAN_POINT('Ctrl Pts',(370.113558046959,-15.6800730416965,-3.86811779903562));
#46765=CARTESIAN_POINT('Ctrl Pts',(370.000679201845,-15.6741989029962,-3.84363572661713));
#46766=CARTESIAN_POINT('Ctrl Pts',(369.972133984676,-15.6727134292148,-3.83744461017511));
#46767=CARTESIAN_POINT('Ctrl Pts',(369.943669184858,-15.6712279554335,-3.83093796731186));
#46768=CARTESIAN_POINT('Ctrl Pts',(369.915292219035,-15.6697424816522,-3.82411831455342));
#46769=CARTESIAN_POINT('Ctrl Pts',(369.803087288063,-15.6638687922616,-3.79715282882214));
#46770=CARTESIAN_POINT('Ctrl Pts',(369.691883293148,-15.6579951028711,-3.76519987490573));
#46771=CARTESIAN_POINT('Ctrl Pts',(369.582157264336,-15.6521214134805,-3.72834854320739));
#46772=CARTESIAN_POINT('Ctrl Pts',(369.472572902136,-15.6462553075748,-3.69154479004025));
#46773=CARTESIAN_POINT('Ctrl Pts',(369.364463099339,-15.640389201669,-3.64985536631524));
#46774=CARTESIAN_POINT('Ctrl Pts',(369.258293608919,-15.6345230957633,-3.60342012279473));
#46775=CARTESIAN_POINT('Ctrl Pts',(369.152232834704,-15.6286629966752,-3.55703242837201));
#46776=CARTESIAN_POINT('Ctrl Pts',(369.048108797119,-15.6228028975872,-3.505908744989));
#46777=CARTESIAN_POINT('Ctrl Pts',(368.946370378527,-15.6169427984991,-3.45023815595173));
#46778=CARTESIAN_POINT('Ctrl Pts',(368.840961469895,-15.610871280405,-3.39255909906695));
#46779=CARTESIAN_POINT('Ctrl Pts',(368.738113993804,-15.6047997623109,-3.32999900198542));
#46780=CARTESIAN_POINT('Ctrl Pts',(368.638303010963,-15.5987282442168,-3.26282206265844));
#46781=CARTESIAN_POINT('Ctrl Pts',(368.542078316503,-15.5928748806201,-3.19805884444795));
#46782=CARTESIAN_POINT('Ctrl Pts',(368.448676035473,-15.5870215170233,-3.12900509834564));
#46783=CARTESIAN_POINT('Ctrl Pts',(368.358494463133,-15.5811681534266,-3.05594298721042));
#46784=CARTESIAN_POINT('Ctrl Pts',(368.268326431253,-15.5753156686927,-2.98289184610529));
#46785=CARTESIAN_POINT('Ctrl Pts',(368.181378467454,-15.5694631839588,-2.90583379666114));
#46786=CARTESIAN_POINT('Ctrl Pts',(368.098016632455,-15.5636106992249,-2.82509196827603));
#46787=CARTESIAN_POINT('Ctrl Pts',(368.014647154295,-15.5577576778967,-2.74434273694954));
#46788=CARTESIAN_POINT('Ctrl Pts',(367.934864755337,-15.5519046565686,-2.6599093427132));
#46789=CARTESIAN_POINT('Ctrl Pts',(367.858998881832,-15.5460516352404,-2.57215202087127));
#46790=CARTESIAN_POINT('Ctrl Pts',(367.783107705592,-15.5401966618165,-2.48436543026701));
#46791=CARTESIAN_POINT('Ctrl Pts',(367.711135922245,-15.5343416883927,-2.39325302004321));
#46792=CARTESIAN_POINT('Ctrl Pts',(367.643372456735,-15.5284867149688,-2.29920779326774));
#46793=CARTESIAN_POINT('Ctrl Pts',(367.57553219004,-15.5226251056847,-2.20505597830778));
#46794=CARTESIAN_POINT('Ctrl Pts',(367.511910002647,-15.5167634964005,-2.10796504773326));
#46795=CARTESIAN_POINT('Ctrl Pts',(367.452751314148,-15.5109018871163,-2.00835672673068));
#46796=CARTESIAN_POINT('Ctrl Pts',(367.393552734511,-15.505036325306,-1.90868123910544));
#46797=CARTESIAN_POINT('Ctrl Pts',(367.338823841448,-15.4991707634956,-1.80648534426908));
#46798=CARTESIAN_POINT('Ctrl Pts',(367.288763153824,-15.4933052016852,-1.7022135217306));
#46799=CARTESIAN_POINT('Ctrl Pts',(367.238629265197,-15.4874310629849,-1.59778922821404));
#46800=CARTESIAN_POINT('Ctrl Pts',(367.19317736665,-15.4815569242846,-1.49128332739846));
#46801=CARTESIAN_POINT('Ctrl Pts',(367.152557148692,-15.4756827855843,-1.38315838375919));
#46802=CARTESIAN_POINT('Ctrl Pts',(367.142284958701,-15.4741973118031,-1.3558153506665));
#46803=CARTESIAN_POINT('Ctrl Pts',(367.132321503048,-15.4727118380218,-1.32836884303118));
#46804=CARTESIAN_POINT('Ctrl Pts',(367.12266868771,-15.4712263642406,-1.30082645734926));
#46805=CARTESIAN_POINT('Ctrl Pts',(367.078037802287,-15.464358107902,-1.17348111646888));
#46806=CARTESIAN_POINT('Ctrl Pts',(367.039929871042,-15.4574898515634,-1.04373804609832));
#46807=CARTESIAN_POINT('Ctrl Pts',(367.008570512254,-15.4506215952247,-0.912220523260835));
#46808=CARTESIAN_POINT('Ctrl Pts',(366.977357634567,-15.4437854208482,-0.781317325219555));
#46809=CARTESIAN_POINT('Ctrl Pts',(366.952830523815,-15.4369492464716,-0.648656316079149));
#46810=CARTESIAN_POINT('Ctrl Pts',(366.935164839185,-15.430113072095,-0.514873550602358));
#46811=CARTESIAN_POINT('Ctrl Pts',(366.917647225344,-15.4233341973793,-0.382212129705779));
#46812=CARTESIAN_POINT('Ctrl Pts',(366.906876582261,-15.4165553226636,-0.248447798149102));
#46813=CARTESIAN_POINT('Ctrl Pts',(366.902976767002,-15.4097764479478,-0.11422024244691));
#46814=CARTESIAN_POINT('Ctrl Pts',(366.901900414615,-15.4079054726576,-0.07717332086797));
#46815=CARTESIAN_POINT('Ctrl Pts',(366.901347173121,-15.4060344973673,-0.0400912217293683));
#46816=CARTESIAN_POINT('Ctrl Pts',(366.90131898798,-15.4041635220771,-0.00298763949216487));
#46817=CARTESIAN_POINT('',(366.901318718745,-14.1541635219903,0.00260925113160348));
#46818=CARTESIAN_POINT('Ctrl Pts',(366.901318987979,-15.404163522035,-0.00298763865733689));
#46819=CARTESIAN_POINT('Ctrl Pts',(366.901230807502,-15.3983099575575,0.113095247154288));
#46820=CARTESIAN_POINT('Ctrl Pts',(366.906286231407,-15.39245639308,0.229234623628663));
#46821=CARTESIAN_POINT('Ctrl Pts',(366.916473529392,-15.3866028286025,0.344941812805038));
#46822=CARTESIAN_POINT('Ctrl Pts',(366.926659429648,-15.3807500672531,0.460633126580709));
#46823=CARTESIAN_POINT('Ctrl Pts',(366.94197576806,-15.3748973059036,0.575891960223361));
#46824=CARTESIAN_POINT('Ctrl Pts',(366.962358825895,-15.3690445445541,0.690233504465105));
#46825=CARTESIAN_POINT('Ctrl Pts',(366.982743993784,-15.3631911773267,0.804586885343415));
#46826=CARTESIAN_POINT('Ctrl Pts',(367.008196851816,-15.3573378100994,0.918022381936605));
#46827=CARTESIAN_POINT('Ctrl Pts',(367.038602447749,-15.351484442872,1.03006483322241));
#46828=CARTESIAN_POINT('Ctrl Pts',(367.069018510601,-15.3456290606631,1.14214585435476));
#46829=CARTESIAN_POINT('Ctrl Pts',(367.104390594125,-15.3397736784542,1.25283247866511));
#46830=CARTESIAN_POINT('Ctrl Pts',(367.144553925521,-15.3339182962453,1.36166484783184));
#46831=CARTESIAN_POINT('Ctrl Pts',(367.184765537014,-15.3280558753168,1.47062804373068));
#46832=CARTESIAN_POINT('Ctrl Pts',(367.229779751747,-15.3221934543884,1.57773214729682));
#46833=CARTESIAN_POINT('Ctrl Pts',(367.279383620603,-15.31633103346,1.68253725121945));
#46834=CARTESIAN_POINT('Ctrl Pts',(367.329021195188,-15.3104646290284,1.78741356999753));
#46835=CARTESIAN_POINT('Ctrl Pts',(367.383254441836,-15.3045982245969,1.88998741450882));
#46836=CARTESIAN_POINT('Ctrl Pts',(367.441825313054,-15.2987318201653,1.98984506052449));
#46837=CARTESIAN_POINT('Ctrl Pts',(367.500489987237,-15.2928560205154,2.08986263148266));
#46838=CARTESIAN_POINT('Ctrl Pts',(367.563505932161,-15.2869802208654,2.18715497353206));
#46839=CARTESIAN_POINT('Ctrl Pts',(367.63057266669,-15.2811044212155,2.28133859384338));
#46840=CARTESIAN_POINT('Ctrl Pts',(367.662509872331,-15.2783063630866,2.32618887127282));
#46841=CARTESIAN_POINT('Ctrl Pts',(367.695365085426,-15.2755083049578,2.37033469463753));
#46842=CARTESIAN_POINT('Ctrl Pts',(367.72910285911,-15.2727102468289,2.41373752515242));
#46843=CARTESIAN_POINT('Ctrl Pts',(367.799925263156,-15.2668365574383,2.50484883641647));
#46844=CARTESIAN_POINT('Ctrl Pts',(367.874879018075,-15.2609628680478,2.59299221037365));
#46845=CARTESIAN_POINT('Ctrl Pts',(367.953686307312,-15.2550891786572,2.6777697617046));
#46846=CARTESIAN_POINT('Ctrl Pts',(368.032391848936,-15.2492230727515,2.76243785725226));
#46847=CARTESIAN_POINT('Ctrl Pts',(368.114940751969,-15.2433569668457,2.84374847229937));
#46848=CARTESIAN_POINT('Ctrl Pts',(368.201013602022,-15.23749086094,2.9213349209912));
#46849=CARTESIAN_POINT('Ctrl Pts',(368.286998314574,-15.231630761852,2.99884192214788));
#46850=CARTESIAN_POINT('Ctrl Pts',(368.376499491537,-15.225770662764,3.07263206734134));
#46851=CARTESIAN_POINT('Ctrl Pts',(368.469159818497,-15.2199105636759,3.14237433651128));
#46852=CARTESIAN_POINT('Ctrl Pts',(368.565163118662,-15.2138390455818,3.2146327476456));
#46853=CARTESIAN_POINT('Ctrl Pts',(368.664557514951,-15.2077675274877,3.28254536113834));
#46854=CARTESIAN_POINT('Ctrl Pts',(368.766906466049,-15.2016960093936,3.34578827127157));
#46855=CARTESIAN_POINT('Ctrl Pts',(368.865577937538,-15.1958426457969,3.40675881310102));
#46856=CARTESIAN_POINT('Ctrl Pts',(368.966994917187,-15.1899892822001,3.46338921298559));
#46857=CARTESIAN_POINT('Ctrl Pts',(369.070736141624,-15.1841359186034,3.51543291025592));
#46858=CARTESIAN_POINT('Ctrl Pts',(369.174461789665,-15.1782834338695,3.56746879334026));
#46859=CARTESIAN_POINT('Ctrl Pts',(369.280510619413,-15.1724309491356,3.61491915795378));
#46860=CARTESIAN_POINT('Ctrl Pts',(369.388437331984,-15.1665784644017,3.65758369942494));
#46861=CARTESIAN_POINT('Ctrl Pts',(369.496373939986,-15.1607254430735,3.70025215266173));
#46862=CARTESIAN_POINT('Ctrl Pts',(369.606188388848,-15.1548724217454,3.73813375857935));
#46863=CARTESIAN_POINT('Ctrl Pts',(369.71741666707,-15.1490194004172,3.77107686747001));
#46864=CARTESIAN_POINT('Ctrl Pts',(369.828682042071,-15.1431644269934,3.80403096352368));
#46865=CARTESIAN_POINT('Ctrl Pts',(369.941361788145,-15.1373094535696,3.83204317013469));
#46866=CARTESIAN_POINT('Ctrl Pts',(370.054978744096,-15.1314544801458,3.85501226366195));
#46867=CARTESIAN_POINT('Ctrl Pts',(370.168724470273,-15.1255928708616,3.87800738970641));
#46868=CARTESIAN_POINT('Ctrl Pts',(370.283409121249,-15.1197312615775,3.89594791252033));
#46869=CARTESIAN_POINT('Ctrl Pts',(370.398547302153,-15.1138696522934,3.9087840854694));
#46870=CARTESIAN_POINT('Ctrl Pts',(370.513763121577,-15.108004090483,3.92162891394418));
#46871=CARTESIAN_POINT('Ctrl Pts',(370.629432668677,-15.1021385286727,3.92936251147359));
#46872=CARTESIAN_POINT('Ctrl Pts',(370.745069151725,-15.0962729668624,3.93198724174949));
#46873=CARTESIAN_POINT('Ctrl Pts',(370.860874723673,-15.0903988281621,3.93461581002482));
#46874=CARTESIAN_POINT('Ctrl Pts',(370.976646723617,-15.0845246894618,3.93212061084049));
#46875=CARTESIAN_POINT('Ctrl Pts',(371.091902011755,-15.0786505507614,3.92455594956598));
#46876=CARTESIAN_POINT('Ctrl Pts',(371.121048192571,-15.07716507698,3.9226429702235));
#46877=CARTESIAN_POINT('Ctrl Pts',(371.150161375778,-15.0756796031986,3.92040605411145));
#46878=CARTESIAN_POINT('Ctrl Pts',(371.179233854668,-15.0741941294172,3.91784659627555));
#46879=CARTESIAN_POINT('Ctrl Pts',(371.294188903319,-15.0683204400266,3.90772628279413));
#46880=CARTESIAN_POINT('Ctrl Pts',(371.408889615562,-15.062446750636,3.89252541571288));
#46881=CARTESIAN_POINT('Ctrl Pts',(371.522851038245,-15.0565730612454,3.872261749046));
#46882=CARTESIAN_POINT('Ctrl Pts',(371.636665326025,-15.0507069553397,3.85202424467645));
#46883=CARTESIAN_POINT('Ctrl Pts',(371.749741819369,-15.0448408494339,3.82673701144267));
#46884=CARTESIAN_POINT('Ctrl Pts',(371.861599231695,-15.0389747435281,3.79646967187226));
#46885=CARTESIAN_POINT('Ctrl Pts',(371.973342103457,-15.0331146444401,3.76623332567197));
#46886=CARTESIAN_POINT('Ctrl Pts',(372.083867980788,-15.027254545352,3.73102712386354));
#46887=CARTESIAN_POINT('Ctrl Pts',(372.192705001393,-15.0213944462639,3.69097187143041));
#46888=CARTESIAN_POINT('Ctrl Pts',(372.305468613403,-15.0153229281698,3.64947151687038));
#46889=CARTESIAN_POINT('Ctrl Pts',(372.416418763014,-15.0092514100757,3.60276569939196));
#46890=CARTESIAN_POINT('Ctrl Pts',(372.52504661651,-15.0031798919816,3.55104565571842));
#46891=CARTESIAN_POINT('Ctrl Pts',(372.629771384418,-14.9973265283849,3.50118395454752));
#46892=CARTESIAN_POINT('Ctrl Pts',(372.732337463077,-14.9914731647881,3.4466623490975));
#46893=CARTESIAN_POINT('Ctrl Pts',(372.832309294742,-14.9856198011914,3.38770116740256));
#46894=CARTESIAN_POINT('Ctrl Pts',(372.932266115973,-14.9797673164574,3.32874883853065));
#46895=CARTESIAN_POINT('Ctrl Pts',(373.029629108948,-14.9739148317235,3.26535846866416));
#46896=CARTESIAN_POINT('Ctrl Pts',(373.123988555321,-14.9680623469896,3.19779565888131));
#46897=CARTESIAN_POINT('Ctrl Pts',(373.218356653188,-14.9622093256614,3.13022665449567));
#46898=CARTESIAN_POINT('Ctrl Pts',(373.30972032108,-14.9563563043332,3.05848469024007));
#46899=CARTESIAN_POINT('Ctrl Pts',(373.39770058151,-14.950503283005,2.98287746786997));
#46900=CARTESIAN_POINT('Ctrl Pts',(373.485710185055,-14.9446483095812,2.90724502903149));
#46901=CARTESIAN_POINT('Ctrl Pts',(373.570333824133,-14.9387933361573,2.82774503781185));
#46902=CARTESIAN_POINT('Ctrl Pts',(373.6512277661,-14.9329383627335,2.74472358221049));
#46903=CARTESIAN_POINT('Ctrl Pts',(373.73221339096,-14.9270767534493,2.66160803245279));
#46904=CARTESIAN_POINT('Ctrl Pts',(373.809460593124,-14.9212151441652,2.57496334833301));
#46905=CARTESIAN_POINT('Ctrl Pts',(373.882664432929,-14.915353534881,2.48517044284681));
#46906=CARTESIAN_POINT('Ctrl Pts',(373.955917634621,-14.9094879730707,2.39531698934497));
#46907=CARTESIAN_POINT('Ctrl Pts',(374.025121798929,-14.9036224112603,2.30231141800824));
#46908=CARTESIAN_POINT('Ctrl Pts',(374.090015017657,-14.8977568494499,2.20656406512561));
#46909=CARTESIAN_POINT('Ctrl Pts',(374.155003126186,-14.8918827107496,2.11067670612951));
#46910=CARTESIAN_POINT('Ctrl Pts',(374.215667493009,-14.8860085720492,2.01203991487935));
#46911=CARTESIAN_POINT('Ctrl Pts',(374.271791836672,-14.8801344333489,1.91108911699985));
#46912=CARTESIAN_POINT('Ctrl Pts',(374.285984766946,-14.8786489595678,1.88556030825338));
#46913=CARTESIAN_POINT('Ctrl Pts',(374.299887602293,-14.8771634857867,1.85988361845331));
#46914=CARTESIAN_POINT('Ctrl Pts',(374.313497337101,-14.8756780120056,1.83406627987418));
#46915=CARTESIAN_POINT('Ctrl Pts',(374.367311383478,-14.869804322615,1.73198233222461));
#46916=CARTESIAN_POINT('Ctrl Pts',(374.416718322612,-14.8639306332244,1.62735788902665));
#46917=CARTESIAN_POINT('Ctrl Pts',(374.461470175623,-14.8580569438339,1.52061008483956));
#46918=CARTESIAN_POINT('Ctrl Pts',(374.506164249788,-14.8521908379281,1.41400010209652));
#46919=CARTESIAN_POINT('Ctrl Pts',(374.54621503178,-14.8463247320224,1.30527258776348));
#46920=CARTESIAN_POINT('Ctrl Pts',(374.581420115924,-14.8404586261167,1.19486971376396));
#46921=CARTESIAN_POINT('Ctrl Pts',(374.61658915051,-14.8345985270286,1.08457989090077));
#46922=CARTESIAN_POINT('Ctrl Pts',(374.646922232174,-14.8287384279406,0.972618512013859));
#46923=CARTESIAN_POINT('Ctrl Pts',(374.672265073252,-14.8228783288526,0.859447576224516));
#46924=CARTESIAN_POINT('Ctrl Pts',(374.69852222622,-14.8168068107585,0.742193691255936));
#46925=CARTESIAN_POINT('Ctrl Pts',(374.719422092635,-14.8107352926643,0.623641742014381));
#46926=CARTESIAN_POINT('Ctrl Pts',(374.734849526619,-14.8046637745702,0.50432297671088));
#46927=CARTESIAN_POINT('Ctrl Pts',(374.749722640572,-14.7988104109735,0.389291430001907));
#46928=CARTESIAN_POINT('Ctrl Pts',(374.759509754418,-14.7929570473767,0.273547668377663));
#46929=CARTESIAN_POINT('Ctrl Pts',(374.764159891538,-14.78710368378,0.157577136353263));
#46930=CARTESIAN_POINT('Ctrl Pts',(374.768809330455,-14.7812511990461,0.0416240169141522));
#46931=CARTESIAN_POINT('Ctrl Pts',(374.768323309732,-14.7753987143122,-0.0745553925209104));
#46932=CARTESIAN_POINT('Ctrl Pts',(374.762702903824,-14.7695462295783,-0.190472817539133));
#46933=CARTESIAN_POINT('Ctrl Pts',(374.757081982601,-14.7636932082501,-0.30640087062888));
#46934=CARTESIAN_POINT('Ctrl Pts',(374.746325760388,-14.7578401869219,-0.422066478868533));
#46935=CARTESIAN_POINT('Ctrl Pts',(374.730487354086,-14.7519871655937,-0.536984376453905));
#46936=CARTESIAN_POINT('Ctrl Pts',(374.714643665369,-14.7461321921699,-0.651940601378014));
#46937=CARTESIAN_POINT('Ctrl Pts',(374.693714478494,-14.740277218746,-0.766148210719741));
#46938=CARTESIAN_POINT('Ctrl Pts',(374.66780427319,-14.7344222453222,-0.879130745645707));
#46939=CARTESIAN_POINT('Ctrl Pts',(374.641864701995,-14.728560636038,-0.992241331762467));
#46940=CARTESIAN_POINT('Ctrl Pts',(374.610932937003,-14.7226990267539,-1.10412366925524));
#46941=CARTESIAN_POINT('Ctrl Pts',(374.575163751701,-14.7168374174697,-1.21431501837412));
#46942=CARTESIAN_POINT('Ctrl Pts',(374.539370446974,-14.7109718556594,-1.32458067032894));
#46943=CARTESIAN_POINT('Ctrl Pts',(374.498733371219,-14.705106293849,-1.43315267745457));
#46944=CARTESIAN_POINT('Ctrl Pts',(374.453455350315,-14.6992407320387,-1.53958850903295));
#46945=CARTESIAN_POINT('Ctrl Pts',(374.40811112184,-14.6933665933384,-1.64617997590203));
#46946=CARTESIAN_POINT('Ctrl Pts',(374.358112582364,-14.687492454638,-1.75062866206103));
#46947=CARTESIAN_POINT('Ctrl Pts',(374.303708375224,-14.6816183159377,-1.85251677613444));
#46948=CARTESIAN_POINT('Ctrl Pts',(374.289950439393,-14.6801328421564,-1.8782826168477));
#46949=CARTESIAN_POINT('Ctrl Pts',(374.275910974734,-14.6786473683752,-1.90388485624279));
#46950=CARTESIAN_POINT('Ctrl Pts',(374.261594429211,-14.6771618945939,-1.92931704799581));
#46951=CARTESIAN_POINT('Ctrl Pts',(374.204985593295,-14.6712882052033,-2.02987809239845));
#46952=CARTESIAN_POINT('Ctrl Pts',(374.143852824281,-14.6654145158128,-2.12811303680021));
#46953=CARTESIAN_POINT('Ctrl Pts',(374.078412211903,-14.6595408264222,-2.2235873699914));
#46954=CARTESIAN_POINT('Ctrl Pts',(374.013056089504,-14.6536747205165,-2.31893843684897));
#46955=CARTESIAN_POINT('Ctrl Pts',(373.943403415844,-14.6478086146107,-2.41153564287199));
#46956=CARTESIAN_POINT('Ctrl Pts',(373.869716025419,-14.641942508705,-2.50096919937757));
#46957=CARTESIAN_POINT('Ctrl Pts',(373.796104089942,-14.636082409617,-2.59031117706091));
#46958=CARTESIAN_POINT('Ctrl Pts',(373.718465916748,-14.6302223105289,-2.67649563197344));
#46959=CARTESIAN_POINT('Ctrl Pts',(373.637106086513,-14.6243622114409,-2.75914246086314));
#46960=CARTESIAN_POINT('Ctrl Pts',(373.552810979214,-14.6182906933468,-2.84477099879153));
#46961=CARTESIAN_POINT('Ctrl Pts',(373.464520862328,-14.6122191752527,-2.92660145977807));
#46962=CARTESIAN_POINT('Ctrl Pts',(373.372619726218,-14.6061476571586,-3.00424909113023));
#46963=CARTESIAN_POINT('Ctrl Pts',(373.284020671374,-14.6002942935618,-3.07910678103333));
#46964=CARTESIAN_POINT('Ctrl Pts',(373.192065967718,-14.5944409299651,-3.15007676361626));
#46965=CARTESIAN_POINT('Ctrl Pts',(373.097135903173,-14.5885875663683,-3.21685303873576));
#46966=CARTESIAN_POINT('Ctrl Pts',(373.002220092059,-14.5827350816344,-3.2836192876222));
#46967=CARTESIAN_POINT('Ctrl Pts',(372.90433014617,-14.5768825969006,-3.3461928434322));
#46968=CARTESIAN_POINT('Ctrl Pts',(372.803876948802,-14.5710301121667,-3.40430991083767));
#46969=CARTESIAN_POINT('Ctrl Pts',(372.703414541224,-14.5651770908385,-3.46243230679772));
#46970=CARTESIAN_POINT('Ctrl Pts',(372.600388772605,-14.5593240695104,-3.5160971951892));
#46971=CARTESIAN_POINT('Ctrl Pts',(372.495236210784,-14.5534710481822,-3.56508614335194));
#46972=CARTESIAN_POINT('Ctrl Pts',(372.390048578553,-14.5476160747584,-3.61409143027529));
#46973=CARTESIAN_POINT('Ctrl Pts',(372.28273311695,-14.5417611013346,-3.65841750156287));
#46974=CARTESIAN_POINT('Ctrl Pts',(372.173746837527,-14.5359061279108,-3.69789385948378));
#46975=CARTESIAN_POINT('Ctrl Pts',(372.064637036156,-14.5300445186266,-3.73741495878573));
#46976=CARTESIAN_POINT('Ctrl Pts',(371.953853026003,-14.5241829093425,-3.77207523320374));
#46977=CARTESIAN_POINT('Ctrl Pts',(371.841867555091,-14.5183213000583,-3.80175388449437));
#46978=CARTESIAN_POINT('Ctrl Pts',(371.729806571553,-14.512455738248,-3.83145254831762));
#46979=CARTESIAN_POINT('Ctrl Pts',(371.616542916712,-14.5065901764376,-3.85616281236564));
#46980=CARTESIAN_POINT('Ctrl Pts',(371.502558406441,-14.5007246146273,-3.87581521270505));
#46981=CARTESIAN_POINT('Ctrl Pts',(371.38840722286,-14.494850475927,-3.89549634967374));
#46982=CARTESIAN_POINT('Ctrl Pts',(371.273533488464,-14.4889763372266,-3.91010481078251));
#46983=CARTESIAN_POINT('Ctrl Pts',(371.158423068542,-14.4831021985263,-3.91962304429951));
#46984=CARTESIAN_POINT('Ctrl Pts',(371.129313522534,-14.481616724745,-3.92203005016975));
#46985=CARTESIAN_POINT('Ctrl Pts',(371.100188832541,-14.4801312509636,-3.92411179532515));
#46986=CARTESIAN_POINT('Ctrl Pts',(371.071056826746,-14.4786457771823,-3.92586852281323));
#46987=CARTESIAN_POINT('Ctrl Pts',(370.955866403654,-14.4727720877917,-3.93281477237915));
#46988=CARTESIAN_POINT('Ctrl Pts',(370.840178153486,-14.4668983984012,-3.9346985245286));
#46989=CARTESIAN_POINT('Ctrl Pts',(370.724474343722,-14.4610247090106,-3.93146580850201));
#46990=CARTESIAN_POINT('Ctrl Pts',(370.608919918447,-14.4551586031048,-3.9282372662155));
#46991=CARTESIAN_POINT('Ctrl Pts',(370.493350382738,-14.449292497199,-3.91990540403812));
#46992=CARTESIAN_POINT('Ctrl Pts',(370.378252028211,-14.4434263912933,-3.9064680932084));
#46993=CARTESIAN_POINT('Ctrl Pts',(370.263271532933,-14.4375662922052,-3.8930445420138));
#46994=CARTESIAN_POINT('Ctrl Pts',(370.148761667057,-14.4317061931172,-3.87452598854489));
#46995=CARTESIAN_POINT('Ctrl Pts',(370.03520695041,-14.4258460940291,-3.8509623167468));
#46996=CARTESIAN_POINT('Ctrl Pts',(369.917555438646,-14.419774575935,-3.82654852142761));
#46997=CARTESIAN_POINT('Ctrl Pts',(369.800929748047,-14.4137030578409,-3.79671871456802));
#46998=CARTESIAN_POINT('Ctrl Pts',(369.685861354147,-14.4076315397468,-3.76158698819103));
#46999=CARTESIAN_POINT('Ctrl Pts',(369.574927459601,-14.4017781761501,-3.7277175728193));
#47000=CARTESIAN_POINT('Ctrl Pts',(369.465441306886,-14.3959248125533,-3.68892081630371));
#47001=CARTESIAN_POINT('Ctrl Pts',(369.357866188026,-14.3900714489565,-3.64535039198334));
#47002=CARTESIAN_POINT('Ctrl Pts',(369.250307221208,-14.3842189642226,-3.60178650961562));
#47003=CARTESIAN_POINT('Ctrl Pts',(369.144659100535,-14.3783664794887,-3.55345053966498));
#47004=CARTESIAN_POINT('Ctrl Pts',(369.041366239032,-14.3725139947548,-3.50054474463156));
#47005=CARTESIAN_POINT('Ctrl Pts',(368.938063906961,-14.3666609734267,-3.44763409884697));
#47006=CARTESIAN_POINT('Ctrl Pts',(368.837117631079,-14.3608079520985,-3.39015298341577));
#47007=CARTESIAN_POINT('Ctrl Pts',(368.738947629641,-14.3549549307703,-3.32834983529698));
#47008=CARTESIAN_POINT('Ctrl Pts',(368.640744886612,-14.3490999573465,-3.26652607463511));
#47009=CARTESIAN_POINT('Ctrl Pts',(368.545320608661,-14.3432449839227,-3.20037763495527));
#47010=CARTESIAN_POINT('Ctrl Pts',(368.453065816677,-14.3373900104989,-3.13019611820774));
#47011=CARTESIAN_POINT('Ctrl Pts',(368.360706465736,-14.3315284012147,-3.0599350597251));
#47012=CARTESIAN_POINT('Ctrl Pts',(368.271524099584,-14.3256667919306,-2.98563205106458));
#47013=CARTESIAN_POINT('Ctrl Pts',(368.185876507134,-14.3198051826464,-2.90761886022269));
#47014=CARTESIAN_POINT('Ctrl Pts',(368.100171161884,-14.3139396208361,-2.82955306451364));
#47015=CARTESIAN_POINT('Ctrl Pts',(368.018005628558,-14.3080740590258,-2.74777239570807));
#47016=CARTESIAN_POINT('Ctrl Pts',(367.939699475211,-14.3022084972155,-2.66264407040617));
#47017=CARTESIAN_POINT('Ctrl Pts',(367.861278819062,-14.2963343585151,-2.57739126661301));
#47018=CARTESIAN_POINT('Ctrl Pts',(367.786729070575,-14.2904602198148,-2.48878135187005));
#47019=CARTESIAN_POINT('Ctrl Pts',(367.716328370803,-14.2845860811144,-2.39721308763126));
#47020=CARTESIAN_POINT('Ctrl Pts',(367.69852518313,-14.2831006073331,-2.37405696846849));
#47021=CARTESIAN_POINT('Ctrl Pts',(367.680987104891,-14.2816151335519,-2.35071179676978));
#47022=CARTESIAN_POINT('Ctrl Pts',(367.663718175582,-14.2801296597706,-2.32718428237578));
#47023=CARTESIAN_POINT('Ctrl Pts',(367.595028837585,-14.2742210009985,-2.23360063515029));
#47024=CARTESIAN_POINT('Ctrl Pts',(367.530372135559,-14.2683123422264,-2.13681774927372));
#47025=CARTESIAN_POINT('Ctrl Pts',(367.470058265088,-14.2624036834543,-2.03721536015079));
#47026=CARTESIAN_POINT('Ctrl Pts',(367.409823572467,-14.2565027813539,-1.93774372541228));
#47027=CARTESIAN_POINT('Ctrl Pts',(367.353920582798,-14.2506018792536,-1.8354602919391));
#47028=CARTESIAN_POINT('Ctrl Pts',(367.302618260149,-14.2447009771533,-1.73077641082656));
#47029=CARTESIAN_POINT('Ctrl Pts',(367.251371377342,-14.2388064518613,-1.6262056563232));
#47030=CARTESIAN_POINT('Ctrl Pts',(367.204715450415,-14.2329119265693,-1.51923997634675));
#47031=CARTESIAN_POINT('Ctrl Pts',(367.162874922437,-14.2270174012773,-1.41031762591654));
#47032=CARTESIAN_POINT('Ctrl Pts',(367.119780629826,-14.2209462446738,-1.29813138286403));
#47033=CARTESIAN_POINT('Ctrl Pts',(367.081795113687,-14.2148750880703,-1.18386972379287));
#47034=CARTESIAN_POINT('Ctrl Pts',(367.049111648607,-14.2088039314667,-1.06803697901003));
#47035=CARTESIAN_POINT('Ctrl Pts',(367.017426479175,-14.2029182144791,-0.955742271722701));
#47036=CARTESIAN_POINT('Ctrl Pts',(366.990724299619,-14.1970324974915,-0.841971478729403));
#47037=CARTESIAN_POINT('Ctrl Pts',(366.969131337325,-14.1911467805039,-0.727201620814089));
#47038=CARTESIAN_POINT('Ctrl Pts',(366.946517890023,-14.1849829040924,-0.607007730852205));
#47039=CARTESIAN_POINT('Ctrl Pts',(366.929508554436,-14.178819027681,-0.485718479073686));
#47040=CARTESIAN_POINT('Ctrl Pts',(366.91818846086,-14.1726551512695,-0.363895015436532));
#47041=CARTESIAN_POINT('Ctrl Pts',(366.906868367283,-14.166491274858,-0.242071551799377));
#47042=CARTESIAN_POINT('Ctrl Pts',(366.901237566177,-14.1603273984465,-0.119714386616033));
#47043=CARTESIAN_POINT('Ctrl Pts',(366.901318718745,-14.154163522035,0.00260925024367697));
#47044=CARTESIAN_POINT('',(366.901318180018,-12.904163522076,0.00160329739904622));
#47045=CARTESIAN_POINT('Ctrl Pts',(366.901318718745,-14.1541635219903,0.0026092511316027));
#47046=CARTESIAN_POINT('Ctrl Pts',(366.901406072305,-14.1475286566482,0.134279778658182));
#47047=CARTESIAN_POINT('Ctrl Pts',(366.908109628326,-14.1408937913061,0.265695130277769));
#47048=CARTESIAN_POINT('Ctrl Pts',(366.921328559004,-14.134258925964,0.396237029214112));
#47049=CARTESIAN_POINT('Ctrl Pts',(366.934605952153,-14.1275947170512,0.527356266988295));
#47050=CARTESIAN_POINT('Ctrl Pts',(366.954456361042,-14.1209305081384,0.657594127909351));
#47051=CARTESIAN_POINT('Ctrl Pts',(366.980727954181,-14.1142662992256,0.786342094762591));
#47052=CARTESIAN_POINT('Ctrl Pts',(367.007149875336,-14.1075639572122,0.915826767086364));
#47053=CARTESIAN_POINT('Ctrl Pts',(367.040066574364,-14.1008616151989,1.04380426788823));
#47054=CARTESIAN_POINT('Ctrl Pts',(367.079275111599,-14.0941592731855,1.16967645465167));
#47055=CARTESIAN_POINT('Ctrl Pts',(367.103739184668,-14.08997736291,1.24821410465263));
#47056=CARTESIAN_POINT('Ctrl Pts',(367.13065178265,-14.0857954526344,1.32593255786291));
#47057=CARTESIAN_POINT('Ctrl Pts',(367.159954398002,-14.0816135423589,1.40269105612235));
#47058=CARTESIAN_POINT('Ctrl Pts',(367.201111297496,-14.0757398529684,1.51050197198495));
#47059=CARTESIAN_POINT('Ctrl Pts',(367.247085747281,-14.0698661635778,1.61667951064501));
#47060=CARTESIAN_POINT('Ctrl Pts',(367.297728111595,-14.0639924741873,1.72076204031903));
#47061=CARTESIAN_POINT('Ctrl Pts',(367.348305091858,-14.0581263682815,1.82471018966914));
#47062=CARTESIAN_POINT('Ctrl Pts',(367.40353782238,-14.0522602623758,1.92656834098912));
#47063=CARTESIAN_POINT('Ctrl Pts',(367.463227776419,-14.04639415647,2.02589256725735));
#47064=CARTESIAN_POINT('Ctrl Pts',(367.522856608706,-14.040534057382,2.12511508678322));
#47065=CARTESIAN_POINT('Ctrl Pts',(367.586933374509,-14.034673958294,2.2218084903306));
#47066=CARTESIAN_POINT('Ctrl Pts',(367.655212889862,-14.028813859206,2.31555190655016));
#47067=CARTESIAN_POINT('Ctrl Pts',(367.725955774359,-14.0227423411119,2.41267737136428));
#47068=CARTESIAN_POINT('Ctrl Pts',(367.801210187543,-14.0166708230177,2.50663556622445));
#47069=CARTESIAN_POINT('Ctrl Pts',(367.880653090131,-14.0105993049236,2.5969893082686));
#47070=CARTESIAN_POINT('Ctrl Pts',(367.957241545739,-14.0047459413269,2.68409656815192));
#47071=CARTESIAN_POINT('Ctrl Pts',(368.03772238303,-13.9988925777302,2.76785360237167));
#47072=CARTESIAN_POINT('Ctrl Pts',(368.121764608661,-13.9930392141334,2.84790166533418));
#47073=CARTESIAN_POINT('Ctrl Pts',(368.205794215636,-13.9871867293995,2.9279377093494));
#47074=CARTESIAN_POINT('Ctrl Pts',(368.293383848627,-13.9813342446656,3.00426560454728));
#47075=CARTESIAN_POINT('Ctrl Pts',(368.384166028363,-13.9754817599318,3.076563835699));
#47076=CARTESIAN_POINT('Ctrl Pts',(368.474956531607,-13.9696287386036,3.14886869562787));
#47077=CARTESIAN_POINT('Ctrl Pts',(368.568939840286,-13.9637757172754,3.21714289965433));
#47078=CARTESIAN_POINT('Ctrl Pts',(368.665716380528,-13.9579226959473,3.28110601057329));
#47079=CARTESIAN_POINT('Ctrl Pts',(368.762525197615,-13.9520677225235,3.34509045442497));
#47080=CARTESIAN_POINT('Ctrl Pts',(368.862128754223,-13.9462127490997,3.40476071842333));
#47081=CARTESIAN_POINT('Ctrl Pts',(368.96410018598,-13.9403577756758,3.45988076053612));
#47082=CARTESIAN_POINT('Ctrl Pts',(369.066187189257,-13.9344961663917,3.51506327413669));
#47083=CARTESIAN_POINT('Ctrl Pts',(369.170647060502,-13.9286345571076,3.5656850760382));
#47084=CARTESIAN_POINT('Ctrl Pts',(369.277030040322,-13.9227729478234,3.61155695895632));
#47085=CARTESIAN_POINT('Ctrl Pts',(369.383484754966,-13.9169073860131,3.65745977362198));
#47086=CARTESIAN_POINT('Ctrl Pts',(369.491864775044,-13.9110418242028,3.6986061453343));
#47087=CARTESIAN_POINT('Ctrl Pts',(369.601703800684,-13.9051762623925,3.73485630211955));
#47088=CARTESIAN_POINT('Ctrl Pts',(369.711703437921,-13.8993021236922,3.77115946552494));
#47089=CARTESIAN_POINT('Ctrl Pts',(369.823165942353,-13.8934279849918,3.80255201393562));
#47090=CARTESIAN_POINT('Ctrl Pts',(369.935613351939,-13.8875538462915,3.82894492247805));
#47091=CARTESIAN_POINT('Ctrl Pts',(369.964049466109,-13.8860683725101,3.8356192581816));
#47092=CARTESIAN_POINT('Ctrl Pts',(369.992548534568,-13.8845828987287,3.84197412459043));
#47093=CARTESIAN_POINT('Ctrl Pts',(370.021102778911,-13.8830974249473,3.84800860743701));
#47094=CARTESIAN_POINT('Ctrl Pts',(370.134008684185,-13.8772237355567,3.87186946470496));
#47095=CARTESIAN_POINT('Ctrl Pts',(370.24815368961,-13.8713500461661,3.89079662734276));
#47096=CARTESIAN_POINT('Ctrl Pts',(370.363068763407,-13.8654763567755,3.90466558047512));
#47097=CARTESIAN_POINT('Ctrl Pts',(370.477835471049,-13.8596102508697,3.91851662748604));
#47098=CARTESIAN_POINT('Ctrl Pts',(370.59336986344,-13.853744144964,3.92732240321013));
#47099=CARTESIAN_POINT('Ctrl Pts',(370.709191281988,-13.8478780390582,3.93100907416539));
#47100=CARTESIAN_POINT('Ctrl Pts',(370.824894100878,-13.8420179399701,3.93469197001656));
#47101=CARTESIAN_POINT('Ctrl Pts',(370.94088295083,-13.8361578408821,3.9332661746027));
#47102=CARTESIAN_POINT('Ctrl Pts',(371.056671253783,-13.830297741794,3.92670955957525));
#47103=CARTESIAN_POINT('Ctrl Pts',(371.176636934551,-13.8242262236999,3.91991639683568));
#47104=CARTESIAN_POINT('Ctrl Pts',(371.296386876134,-13.8181547056058,3.90761515397048));
#47105=CARTESIAN_POINT('Ctrl Pts',(371.415378587673,-13.8120831875117,3.8898402824386));
#47106=CARTESIAN_POINT('Ctrl Pts',(371.53009483192,-13.8062298239149,3.8727040762461));
#47107=CARTESIAN_POINT('Ctrl Pts',(371.644105952384,-13.8003764603181,3.85048088198511));
#47108=CARTESIAN_POINT('Ctrl Pts',(371.756931057686,-13.7945230967214,3.82325435655956));
#47109=CARTESIAN_POINT('Ctrl Pts',(371.869739222679,-13.7886706119874,3.79603191910517));
#47110=CARTESIAN_POINT('Ctrl Pts',(371.981361325085,-13.7828181272535,3.76380774111084));
#47111=CARTESIAN_POINT('Ctrl Pts',(372.091327979127,-13.7769656425196,3.72671632182777));
#47112=CARTESIAN_POINT('Ctrl Pts',(372.201304715634,-13.7711126211914,3.68962150175957));
#47113=CARTESIAN_POINT('Ctrl Pts',(372.309625310551,-13.7652595998632,3.64765868532898));
#47114=CARTESIAN_POINT('Ctrl Pts',(372.415837497496,-13.759406578535,3.60101160992063));
#47115=CARTESIAN_POINT('Ctrl Pts',(372.522085108256,-13.7535516051111,3.55434897681175));
#47116=CARTESIAN_POINT('Ctrl Pts',(372.626222534707,-13.7476966316873,3.50299914422174));
#47117=CARTESIAN_POINT('Ctrl Pts',(372.727820021639,-13.7418416582634,3.44719284900153));
#47118=CARTESIAN_POINT('Ctrl Pts',(372.829532656273,-13.7359800489793,3.39132330451377));
#47119=CARTESIAN_POINT('Ctrl Pts',(372.928699243372,-13.7301184396951,3.33098741526292));
#47120=CARTESIAN_POINT('Ctrl Pts',(373.024916971724,-13.7242568304109,3.26646054652843));
#47121=CARTESIAN_POINT('Ctrl Pts',(373.121199580397,-13.7183912686005,3.20189016685248));
#47122=CARTESIAN_POINT('Ctrl Pts',(373.214529039118,-13.7125257067902,3.1331234249489));
#47123=CARTESIAN_POINT('Ctrl Pts',(373.304535110808,-13.7066601449798,3.06047638454152));
#47124=CARTESIAN_POINT('Ctrl Pts',(373.394672793449,-13.7007860062795,2.98772311634321));
#47125=CARTESIAN_POINT('Ctrl Pts',(373.481477081996,-13.6949118675791,2.91107849826694));
#47126=CARTESIAN_POINT('Ctrl Pts',(373.56461406038,-13.6890377288788,2.83089590433689));
#47127=CARTESIAN_POINT('Ctrl Pts',(373.585638044988,-13.6875522550977,2.81061903532578));
#47128=CARTESIAN_POINT('Ctrl Pts',(373.606427705161,-13.6860667813166,2.7901160779877));
#47129=CARTESIAN_POINT('Ctrl Pts',(373.626978055884,-13.6845813075356,2.76939307294575));
#47130=CARTESIAN_POINT('Ctrl Pts',(373.708235886585,-13.678707618145,2.6874525524144));
#47131=CARTESIAN_POINT('Ctrl Pts',(373.78601962295,-13.6728339287545,2.60179620351885));
#47132=CARTESIAN_POINT('Ctrl Pts',(373.859970367563,-13.6669602393639,2.51275065664625));
#47133=CARTESIAN_POINT('Ctrl Pts',(373.933825634817,-13.6610941334582,2.42382007594017));
#47134=CARTESIAN_POINT('Ctrl Pts',(374.003857490222,-13.6552280275524,2.33150931416387));
#47135=CARTESIAN_POINT('Ctrl Pts',(374.069743321329,-13.6493619216467,2.23618224667331));
#47136=CARTESIAN_POINT('Ctrl Pts',(374.135561686184,-13.6435018225587,2.14095279288542));
#47137=CARTESIAN_POINT('Ctrl Pts',(374.197242237839,-13.6376417234706,2.04271351482894));
#47138=CARTESIAN_POINT('Ctrl Pts',(374.254502603075,-13.6317816243826,1.94186129187677));
#47139=CARTESIAN_POINT('Ctrl Pts',(374.313828791656,-13.6257101062885,1.83737055080101));
#47140=CARTESIAN_POINT('Ctrl Pts',(374.368409543021,-13.6196385881944,1.73007511443216));
#47141=CARTESIAN_POINT('Ctrl Pts',(374.417979717547,-13.6135670701003,1.62044951855945));
#47142=CARTESIAN_POINT('Ctrl Pts',(374.465768796086,-13.6077137065035,1.51476285795727));
#47143=CARTESIAN_POINT('Ctrl Pts',(374.508900984322,-13.6018603429068,1.40691101379008));
#47144=CARTESIAN_POINT('Ctrl Pts',(374.54718588402,-13.5960069793101,1.29734343405811));
#47145=CARTESIAN_POINT('Ctrl Pts',(374.585465035369,-13.5901544945762,1.18779230552955));
#47146=CARTESIAN_POINT('Ctrl Pts',(374.618898209084,-13.5843020098423,1.07652634358177));
#47147=CARTESIAN_POINT('Ctrl Pts',(374.647343967446,-13.5784495251084,0.964012890090213));
#47148=CARTESIAN_POINT('Ctrl Pts',(374.675792333903,-13.5725965037802,0.851489120625622));
#47149=CARTESIAN_POINT('Ctrl Pts',(374.699252274708,-13.5667434824521,0.737718032808258));
#47150=CARTESIAN_POINT('Ctrl Pts',(374.717633007921,-13.5608904611239,0.623179275410707));
#47151=CARTESIAN_POINT('Ctrl Pts',(374.736019871464,-13.5550354877001,0.508602317125604));
#47152=CARTESIAN_POINT('Ctrl Pts',(374.749324093517,-13.5491805142763,0.393257587856447));
#47153=CARTESIAN_POINT('Ctrl Pts',(374.757506589681,-13.5433255408525,0.277631298918333));
#47154=CARTESIAN_POINT('Ctrl Pts',(374.765698359653,-13.5374639315683,0.161873962433356));
#47155=CARTESIAN_POINT('Ctrl Pts',(374.768756788488,-13.5316023222842,0.045834841696479));
#47156=CARTESIAN_POINT('Ctrl Pts',(374.766694900003,-13.525740713,-0.0699982997340179));
#47157=CARTESIAN_POINT('Ctrl Pts',(374.764631621171,-13.5198751511897,-0.185909548302475));
#47158=CARTESIAN_POINT('Ctrl Pts',(374.757441175553,-13.5140095893794,-0.301614129668007));
#47159=CARTESIAN_POINT('Ctrl Pts',(374.745188444935,-13.508144027569,-0.416629589555363));
#47160=CARTESIAN_POINT('Ctrl Pts',(374.732917797818,-13.5022698888687,-0.531813230254458));
#47161=CARTESIAN_POINT('Ctrl Pts',(374.715570154221,-13.4963957501684,-0.646305331517802));
#47162=CARTESIAN_POINT('Ctrl Pts',(374.693261438031,-13.4905216114681,-0.759633733632965));
#47163=CARTESIAN_POINT('Ctrl Pts',(374.687619927899,-13.4890361376867,-0.788292636429524));
#47164=CARTESIAN_POINT('Ctrl Pts',(374.681661404466,-13.4875506639053,-0.81687719919626));
#47165=CARTESIAN_POINT('Ctrl Pts',(374.675388241292,-13.486065190124,-0.84537995830715));
#47166=CARTESIAN_POINT('Ctrl Pts',(374.650583621752,-13.4801915007334,-0.958082286609185));
#47167=CARTESIAN_POINT('Ctrl Pts',(374.620773222898,-13.4743178113429,-1.06987969207614));
#47168=CARTESIAN_POINT('Ctrl Pts',(374.586036953103,-13.4684441219523,-1.18029352095379));
#47169=CARTESIAN_POINT('Ctrl Pts',(374.551345531095,-13.4625780160465,-1.29056479520543));
#47170=CARTESIAN_POINT('Ctrl Pts',(374.511741008482,-13.4567119101408,-1.39945565478447));
#47171=CARTESIAN_POINT('Ctrl Pts',(374.467354261302,-13.450845804235,-1.50649774562634));
#47172=CARTESIAN_POINT('Ctrl Pts',(374.423012965586,-13.444985705147,-1.61343022673085));
#47173=CARTESIAN_POINT('Ctrl Pts',(374.373899343028,-13.439125606059,-1.71851732529531));
#47174=CARTESIAN_POINT('Ctrl Pts',(374.320193817271,-13.4332655069709,-1.82130660880562));
#47175=CARTESIAN_POINT('Ctrl Pts',(374.264550718667,-13.4271939888768,-1.92780429516515));
#47176=CARTESIAN_POINT('Ctrl Pts',(374.20397826595,-13.4211224707827,-2.03183480538675));
#47177=CARTESIAN_POINT('Ctrl Pts',(374.138731480556,-13.4150509526886,-2.13291809020006));
#47178=CARTESIAN_POINT('Ctrl Pts',(374.075829064305,-13.4091975890918,-2.23036937180622));
#47179=CARTESIAN_POINT('Ctrl Pts',(374.008582682789,-13.4033442254951,-2.32508119855126));
#47180=CARTESIAN_POINT('Ctrl Pts',(373.937266793996,-13.3974908618983,-2.41664992726786));
#47181=CARTESIAN_POINT('Ctrl Pts',(373.865961613043,-13.3916383771644,-2.50820490724797));
#47182=CARTESIAN_POINT('Ctrl Pts',(373.790588393545,-13.3857858924305,-2.59661740170089));
#47183=CARTESIAN_POINT('Ctrl Pts',(373.711463171816,-13.3799334076966,-2.68151520892666));
#47184=CARTESIAN_POINT('Ctrl Pts',(373.632330695366,-13.3740803863685,-2.76642080014151));
#47185=CARTESIAN_POINT('Ctrl Pts',(373.549445814526,-13.3682273650403,-2.84781076127858));
#47186=CARTESIAN_POINT('Ctrl Pts',(373.46316236817,-13.3623743437121,-2.92534878539939));
#47187=CARTESIAN_POINT('Ctrl Pts',(373.376850144618,-13.3565193702883,-3.00291266994868));
#47188=CARTESIAN_POINT('Ctrl Pts',(373.287137408791,-13.3506643968645,-3.07662178692235));
#47189=CARTESIAN_POINT('Ctrl Pts',(373.194411539847,-13.3448094234406,-3.14617971361475));
#47190=CARTESIAN_POINT('Ctrl Pts',(373.101580578041,-13.3389478141565,-3.21581647528265));
#47191=CARTESIAN_POINT('Ctrl Pts',(373.005729997663,-13.3330862048723,-3.28129240803352));
#47192=CARTESIAN_POINT('Ctrl Pts',(372.907276730594,-13.3272245955882,-3.34235403461864));
#47193=CARTESIAN_POINT('Ctrl Pts',(372.808757075764,-13.3213590337779,-3.40345683550697));
#47194=CARTESIAN_POINT('Ctrl Pts',(372.707631599127,-13.3154934719675,-3.46013920165507));
#47195=CARTESIAN_POINT('Ctrl Pts',(372.60434088383,-13.3096279101572,-3.51219411068426));
#47196=CARTESIAN_POINT('Ctrl Pts',(372.500899132173,-13.3037537714568,-3.56432513675778));
#47197=CARTESIAN_POINT('Ctrl Pts',(372.39528619845,-13.2978796327565,-3.61181503274264));
#47198=CARTESIAN_POINT('Ctrl Pts',(372.287961685617,-13.2920054940562,-3.65450524812137));
#47199=CARTESIAN_POINT('Ctrl Pts',(372.260821068406,-13.2905200202749,-3.66530090666781));
#47200=CARTESIAN_POINT('Ctrl Pts',(372.233571063781,-13.2890345464936,-3.67578987601278));
#47201=CARTESIAN_POINT('Ctrl Pts',(372.206219230214,-13.2875490727123,-3.68597010457407));
#47202=CARTESIAN_POINT('Ctrl Pts',(372.098067759174,-13.2816753833217,-3.72622359221338));
#47203=CARTESIAN_POINT('Ctrl Pts',(371.987963021316,-13.2758016939311,-3.76178011693721));
#47204=CARTESIAN_POINT('Ctrl Pts',(371.876350552237,-13.2699280045406,-3.79244734362742));
#47205=CARTESIAN_POINT('Ctrl Pts',(371.764882185342,-13.2640618986348,-3.8230749760469));
#47206=CARTESIAN_POINT('Ctrl Pts',(371.651910353161,-13.258195792729,-3.84882575554985));
#47207=CARTESIAN_POINT('Ctrl Pts',(371.537899566436,-13.2523296868233,-3.86955575910637));
#47208=CARTESIAN_POINT('Ctrl Pts',(371.424005525305,-13.2464695877352,-3.89026453540335));
#47209=CARTESIAN_POINT('Ctrl Pts',(371.309075049832,-13.2406094886472,-3.9059626885789));
#47210=CARTESIAN_POINT('Ctrl Pts',(371.193586131983,-13.2347493895592,-3.91655656206796));
#47211=CARTESIAN_POINT('Ctrl Pts',(371.073930637451,-13.2286778714651,-3.92753263834399));
#47212=CARTESIAN_POINT('Ctrl Pts',(370.95367608064,-13.2226063533709,-3.93302906002753));
#47213=CARTESIAN_POINT('Ctrl Pts',(370.833364100265,-13.2165348352768,-3.9329998843574));
#47214=CARTESIAN_POINT('Ctrl Pts',(370.717375025496,-13.2106814716801,-3.93297175699241));
#47215=CARTESIAN_POINT('Ctrl Pts',(370.601333031259,-13.2048281080833,-3.92780827699202));
#47216=CARTESIAN_POINT('Ctrl Pts',(370.485726088358,-13.1989747444866,-3.91752125475633));
#47217=CARTESIAN_POINT('Ctrl Pts',(370.370136503451,-13.1931222597527,-3.90723577708242));
#47218=CARTESIAN_POINT('Ctrl Pts',(370.254982251406,-13.1872697750188,-3.89182832340427));
#47219=CARTESIAN_POINT('Ctrl Pts',(370.140747422524,-13.1814172902849,-3.87136268743423));
#47220=CARTESIAN_POINT('Ctrl Pts',(370.026502119841,-13.1755642689567,-3.85089517504015));
#47221=CARTESIAN_POINT('Ctrl Pts',(369.913176814591,-13.1697112476285,-3.82536863128858));
#47222=CARTESIAN_POINT('Ctrl Pts',(369.801245927554,-13.1638582263003,-3.79489807457216));
#47223=CARTESIAN_POINT('Ctrl Pts',(369.689277709403,-13.1580032528765,-3.76441735533666));
#47224=CARTESIAN_POINT('Ctrl Pts',(369.578705232649,-13.1521482794527,-3.72898945278615));
#47225=CARTESIAN_POINT('Ctrl Pts',(369.469987585543,-13.1462933060288,-3.68877919109973));
#47226=CARTESIAN_POINT('Ctrl Pts',(369.361146720949,-13.1404316967447,-3.64852335624647));
#47227=CARTESIAN_POINT('Ctrl Pts',(369.254165269596,-13.1345700874605,-3.60347448728209));
#47228=CARTESIAN_POINT('Ctrl Pts',(369.149482253146,-13.1287084781764,-3.55384552291017));
#47229=CARTESIAN_POINT('Ctrl Pts',(369.044728648168,-13.122842916366,-3.50418309336308));
#47230=CARTESIAN_POINT('Ctrl Pts',(368.942276928405,-13.1169773545557,-3.44993461158795));
#47231=CARTESIAN_POINT('Ctrl Pts',(368.842539900701,-13.1111117927453,-3.3913580742591));
#47232=CARTESIAN_POINT('Ctrl Pts',(368.742657032999,-13.105237654045,-3.33269588366581));
#47233=CARTESIAN_POINT('Ctrl Pts',(368.645497124884,-13.0993635153446,-3.26969323098247));
#47234=CARTESIAN_POINT('Ctrl Pts',(368.551442562731,-13.0934893766443,-3.20265037243453));
#47235=CARTESIAN_POINT('Ctrl Pts',(368.527657699416,-13.0920039028631,-3.18569632799156));
#47236=CARTESIAN_POINT('Ctrl Pts',(368.504071249485,-13.0905184290819,-3.16848410531235));
#47237=CARTESIAN_POINT('Ctrl Pts',(368.48068903442,-13.0890329553007,-3.15101894365849));
#47238=CARTESIAN_POINT('Ctrl Pts',(368.389135817684,-13.0832165729492,-3.08263398843743));
#47239=CARTESIAN_POINT('Ctrl Pts',(368.300398414984,-13.0774001905977,-3.01013059775965));
#47240=CARTESIAN_POINT('Ctrl Pts',(368.214875700783,-13.0715838082462,-2.93377091982545));
#47241=CARTESIAN_POINT('Ctrl Pts',(368.129463801022,-13.0657749623623,-2.8575101835014));
#47242=CARTESIAN_POINT('Ctrl Pts',(368.047258621431,-13.0599661164783,-2.77740337089595));
#47243=CARTESIAN_POINT('Ctrl Pts',(367.968629026321,-13.0541572705944,-2.69375510159393));
#47244=CARTESIAN_POINT('Ctrl Pts',(367.890079276586,-13.0483543233734,-2.61019177394068));
#47245=CARTESIAN_POINT('Ctrl Pts',(367.815098179366,-13.0425513761524,-2.52309444557834));
#47246=CARTESIAN_POINT('Ctrl Pts',(367.744019929908,-13.0367484289314,-2.43280655728099));
#47247=CARTESIAN_POINT('Ctrl Pts',(367.672992694972,-13.0309496466213,-2.34258347071239));
#47248=CARTESIAN_POINT('Ctrl Pts',(367.605862997561,-13.0251508643112,-2.24917470849674));
#47249=CARTESIAN_POINT('Ctrl Pts',(367.542926173974,-13.0193520820012,-2.15295838644515));
#47250=CARTESIAN_POINT('Ctrl Pts',(367.480012683451,-13.0135554495193,-2.05677773542829));
#47251=CARTESIAN_POINT('Ctrl Pts',(367.421289208297,-13.0077588170375,-1.95779194582016));
#47252=CARTESIAN_POINT('Ctrl Pts',(367.367008575753,-13.0019621845556,-1.85640926909014));
#47253=CARTESIAN_POINT('Ctrl Pts',(367.312734307432,-12.9961662317095,-1.75503847913993));
#47254=CARTESIAN_POINT('Ctrl Pts',(367.262902045014,-12.9903702788635,-1.65127173294188));
#47255=CARTESIAN_POINT('Ctrl Pts',(367.217718930285,-12.9845743260174,-1.54554237424707));
#47256=CARTESIAN_POINT('Ctrl Pts',(367.172529659278,-12.9787775834628,-1.43979860974569));
#47257=CARTESIAN_POINT('Ctrl Pts',(367.131990959828,-12.9729808409082,-1.33209208974943));
#47258=CARTESIAN_POINT('Ctrl Pts',(367.096261725996,-12.9671840983536,-1.22287586847367));
#47259=CARTESIAN_POINT('Ctrl Pts',(367.060498227861,-12.9613817967279,-1.11355490893568));
#47260=CARTESIAN_POINT('Ctrl Pts',(367.029553535441,-12.9555794951022,-1.00272175917924));
#47261=CARTESIAN_POINT('Ctrl Pts',(367.003536554116,-12.9497771934764,-0.890844340166382));
#47262=CARTESIAN_POINT('Ctrl Pts',(366.977506020343,-12.9439718693866,-0.778908643335273));
#47263=CARTESIAN_POINT('Ctrl Pts',(366.956408385523,-12.9381665452968,-0.66592800876549));
#47264=CARTESIAN_POINT('Ctrl Pts',(366.940301024373,-12.9323612212071,-0.552378436057968));
#47265=CARTESIAN_POINT('Ctrl Pts',(366.924169836189,-12.9265473095126,-0.43866089360047));
#47266=CARTESIAN_POINT('Ctrl Pts',(366.913043701887,-12.9207333978182,-0.324373152081675));
#47267=CARTESIAN_POINT('Ctrl Pts',(366.906927960272,-12.9149194861238,-0.209994354062086));
#47268=CARTESIAN_POINT('Ctrl Pts',(366.903156506536,-12.9113341647745,-0.139459270628284));
#47269=CARTESIAN_POINT('Ctrl Pts',(366.901289443427,-12.9077488434253,-0.0688895532719928));
#47270=CARTESIAN_POINT('Ctrl Pts',(366.901318180018,-12.904163522076,0.00160329739904574));
#47271=CARTESIAN_POINT('',(366.901319491282,-11.654163521998,-0.00358956336470628));
#47272=CARTESIAN_POINT('Ctrl Pts',(366.901318180018,-12.904163522035,0.00160329820526979));
#47273=CARTESIAN_POINT('Ctrl Pts',(366.901354639733,-12.8996146273197,0.0910414613838704));
#47274=CARTESIAN_POINT('Ctrl Pts',(366.904441638581,-12.8950657326043,0.180414019458864));
#47275=CARTESIAN_POINT('Ctrl Pts',(366.910567340119,-12.890516837889,0.269575427124204));
#47276=CARTESIAN_POINT('Ctrl Pts',(366.91847705674,-12.8846431484984,0.384703704876417));
#47277=CARTESIAN_POINT('Ctrl Pts',(366.931471275856,-12.8787694591079,0.499675310147441));
#47278=CARTESIAN_POINT('Ctrl Pts',(366.949541564545,-12.8728957697173,0.614005038186002));
#47279=CARTESIAN_POINT('Ctrl Pts',(366.967588522794,-12.8670296638115,0.728187155804904));
#47280=CARTESIAN_POINT('Ctrl Pts',(366.990698453581,-12.8611635579058,0.841728639899142));
#47281=CARTESIAN_POINT('Ctrl Pts',(367.018810994597,-12.855297452,0.954146955020061));
#47282=CARTESIAN_POINT('Ctrl Pts',(367.04689474873,-12.849437352912,1.06645015521839));
#47283=CARTESIAN_POINT('Ctrl Pts',(367.079970824164,-12.843577253824,1.17763207568835));
#47284=CARTESIAN_POINT('Ctrl Pts',(367.117927504507,-12.8377171547359,1.28721862011198));
#47285=CARTESIAN_POINT('Ctrl Pts',(367.157253575284,-12.8316456366418,1.40075879705153));
#47286=CARTESIAN_POINT('Ctrl Pts',(367.201818991622,-12.8255741185477,1.51258586332659));
#47287=CARTESIAN_POINT('Ctrl Pts',(367.251442328755,-12.8195026004536,1.62218740476041));
#47288=CARTESIAN_POINT('Ctrl Pts',(367.299282659727,-12.8136492368569,1.72785087521913));
#47289=CARTESIAN_POINT('Ctrl Pts',(367.351823511469,-12.8077958732601,1.83144558961424));
#47290=CARTESIAN_POINT('Ctrl Pts',(367.408852965359,-12.8019425096634,1.93253183725558));
#47291=CARTESIAN_POINT('Ctrl Pts',(367.465873856469,-12.7960900249295,2.03360290713705));
#47292=CARTESIAN_POINT('Ctrl Pts',(367.527381806715,-12.7902375401956,2.13216589942832));
#47293=CARTESIAN_POINT('Ctrl Pts',(367.593119136315,-12.7843850554617,2.22780606819935));
#47294=CARTESIAN_POINT('Ctrl Pts',(367.658862493145,-12.7785320341335,2.32345500588973));
#47295=CARTESIAN_POINT('Ctrl Pts',(367.72883576616,-12.7726790128053,2.41618024684051));
#47296=CARTESIAN_POINT('Ctrl Pts',(367.802738592021,-12.7668259914772,2.50559697139118));
#47297=CARTESIAN_POINT('Ctrl Pts',(367.876666065902,-12.7609710180533,2.5950435181464));
#47298=CARTESIAN_POINT('Ctrl Pts',(367.954525435603,-12.7551160446295,2.68117903604957));
#47299=CARTESIAN_POINT('Ctrl Pts',(368.03597728144,-12.7492610712057,2.76365320623022));
#47300=CARTESIAN_POINT('Ctrl Pts',(368.117521442481,-12.7433994619215,2.84622085028926));
#47301=CARTESIAN_POINT('Ctrl Pts',(368.202665915875,-12.7375378526374,2.9251185700214));
#47302=CARTESIAN_POINT('Ctrl Pts',(368.291035718006,-12.7316762433532,3.00003416325228));
#47303=CARTESIAN_POINT('Ctrl Pts',(368.379465108544,-12.7258106815429,3.0750002726178));
#47304=CARTESIAN_POINT('Ctrl Pts',(368.471123832607,-12.7199451197325,3.145978656371));
#47305=CARTESIAN_POINT('Ctrl Pts',(368.565606661921,-12.7140795579222,3.21269957052569));
#47306=CARTESIAN_POINT('Ctrl Pts',(368.660227648304,-12.7082054192218,3.27951804702129));
#47307=CARTESIAN_POINT('Ctrl Pts',(368.757680635097,-12.7023312805215,3.34206640715481));
#47308=CARTESIAN_POINT('Ctrl Pts',(368.857534432652,-12.6964571418212,3.40012004319746));
#47309=CARTESIAN_POINT('Ctrl Pts',(368.882785827929,-12.6949716680399,3.4148008600198));
#47310=CARTESIAN_POINT('Ctrl Pts',(368.908190650798,-12.6934861942586,3.42919447683107));
#47311=CARTESIAN_POINT('Ctrl Pts',(368.933741728072,-12.6920007204774,3.44329774961458));
#47312=CARTESIAN_POINT('Ctrl Pts',(369.034772855911,-12.6861270310868,3.49906328702451));
#47313=CARTESIAN_POINT('Ctrl Pts',(369.138428687797,-12.6802533416962,3.55047134344653));
#47314=CARTESIAN_POINT('Ctrl Pts',(369.244296930802,-12.6743796523057,3.59726597102029));
#47315=CARTESIAN_POINT('Ctrl Pts',(369.350028487959,-12.6685135463999,3.64400018233366));
#47316=CARTESIAN_POINT('Ctrl Pts',(369.457966401305,-12.6626474404942,3.68613264456638));
#47317=CARTESIAN_POINT('Ctrl Pts',(369.567672469534,-12.6567813345884,3.72345249358408));
#47318=CARTESIAN_POINT('Ctrl Pts',(369.677266200147,-12.6509212355004,3.76073412755182));
#47319=CARTESIAN_POINT('Ctrl Pts',(369.788624095465,-12.6450611364124,3.79321281834872));
#47320=CARTESIAN_POINT('Ctrl Pts',(369.901287206112,-12.6392010373243,3.8207254300133));
#47321=CARTESIAN_POINT('Ctrl Pts',(370.018014944766,-12.6331295192302,3.84923063394046));
#47322=CARTESIAN_POINT('Ctrl Pts',(370.136143442146,-12.6270580011361,3.87240448109303));
#47323=CARTESIAN_POINT('Ctrl Pts',(370.255143760507,-12.620986483042,3.89012163952816));
#47324=CARTESIAN_POINT('Ctrl Pts',(370.369868302326,-12.6151331194453,3.9072022063015));
#47325=CARTESIAN_POINT('Ctrl Pts',(370.485402649207,-12.6092797558485,3.91921139624782));
#47326=CARTESIAN_POINT('Ctrl Pts',(370.601262425706,-12.6034263922518,3.92608891490046));
#47327=CARTESIAN_POINT('Ctrl Pts',(370.717104806249,-12.5975739075178,3.93296540091682));
#47328=CARTESIAN_POINT('Ctrl Pts',(370.833272106946,-12.5917214227839,3.93471172321431));
#47329=CARTESIAN_POINT('Ctrl Pts',(370.949276122877,-12.58586893805,3.93131957442261));
#47330=CARTESIAN_POINT('Ctrl Pts',(371.065290774818,-12.5800159167219,3.92792711461641));
#47331=CARTESIAN_POINT('Ctrl Pts',(371.181141699241,-12.5741628953937,3.91939525923755));
#47332=CARTESIAN_POINT('Ctrl Pts',(371.296342699342,-12.5683098740655,3.90576779155772));
#47333=CARTESIAN_POINT('Ctrl Pts',(371.411582121201,-12.5624549006417,3.89213577885425));
#47334=CARTESIAN_POINT('Ctrl Pts',(371.526170777654,-12.5565999272179,3.87340482300706));
#47335=CARTESIAN_POINT('Ctrl Pts',(371.639630290366,-12.5507449537941,3.84967022984889));
#47336=CARTESIAN_POINT('Ctrl Pts',(371.753218394861,-12.5448833445099,3.82590873657798));
#47337=CARTESIAN_POINT('Ctrl Pts',(371.865674396715,-12.5390217352258,3.79713237170308));
#47338=CARTESIAN_POINT('Ctrl Pts',(371.976532667806,-12.5331601259416,3.7634869891297));
#47339=CARTESIAN_POINT('Ctrl Pts',(372.087465691444,-12.5272945641313,3.72981891922774));
#47340=CARTESIAN_POINT('Ctrl Pts',(372.196798450375,-12.5214290023209,3.69127543104097));
#47341=CARTESIAN_POINT('Ctrl Pts',(372.30408459851,-12.5155634405106,3.64805081028907));
#47342=CARTESIAN_POINT('Ctrl Pts',(372.411527625307,-12.5096893018102,3.60476298454009));
#47343=CARTESIAN_POINT('Ctrl Pts',(372.516917694174,-12.5038151631099,3.55678053593144));
#47344=CARTESIAN_POINT('Ctrl Pts',(372.619832313464,-12.4979410244096,3.50434403451963));
#47345=CARTESIAN_POINT('Ctrl Pts',(372.645857740589,-12.4964555506283,3.49108369934473));
#47346=CARTESIAN_POINT('Ctrl Pts',(372.671725005849,-12.494970076847,3.47753874390132));
#47347=CARTESIAN_POINT('Ctrl Pts',(372.697427578647,-12.4934846030657,3.46371349147598));
#47348=CARTESIAN_POINT('Ctrl Pts',(372.799057732646,-12.4876109136751,3.40904727015657));
#47349=CARTESIAN_POINT('Ctrl Pts',(372.898449138204,-12.4817372242845,3.34981325754317));
#47350=CARTESIAN_POINT('Ctrl Pts',(372.995163212408,-12.475863534894,3.28621915484824));
#47351=CARTESIAN_POINT('Ctrl Pts',(373.091752419657,-12.4699974289882,3.22270715811428));
#47352=CARTESIAN_POINT('Ctrl Pts',(373.185670827716,-12.4641313230825,3.15484649101718));
#47353=CARTESIAN_POINT('Ctrl Pts',(373.276503692705,-12.4582652171767,3.08289106610005));
#47354=CARTESIAN_POINT('Ctrl Pts',(373.367243545997,-12.4524051180887,3.01100932262141));
#47355=CARTESIAN_POINT('Ctrl Pts',(373.454903818918,-12.4465450190006,2.93504141652364));
#47356=CARTESIAN_POINT('Ctrl Pts',(373.539098626219,-12.4406849199126,2.8552845690121));
#47357=CARTESIAN_POINT('Ctrl Pts',(373.626330990088,-12.4346134018185,2.77265027639684));
#47358=CARTESIAN_POINT('Ctrl Pts',(373.709842737651,-12.4285418837244,2.68594873601789));
#47359=CARTESIAN_POINT('Ctrl Pts',(373.78924180931,-12.4224703656303,2.59555647477553));
#47360=CARTESIAN_POINT('Ctrl Pts',(373.86578800887,-12.4166170020335,2.50841207971925));
#47361=CARTESIAN_POINT('Ctrl Pts',(373.938511693713,-12.4107636384368,2.41783795750291));
#47362=CARTESIAN_POINT('Ctrl Pts',(374.00709961339,-12.40491027484,2.32420844640899));
#47363=CARTESIAN_POINT('Ctrl Pts',(374.075677234821,-12.3990577901061,2.23059299347107));
#47364=CARTESIAN_POINT('Ctrl Pts',(374.140120081728,-12.3932053053722,2.13392339703328));
#47365=CARTESIAN_POINT('Ctrl Pts',(374.20015651283,-12.3873528206383,2.03460539601675));
#47366=CARTESIAN_POINT('Ctrl Pts',(374.260198448467,-12.3814997993102,1.93527828887301));
#47367=CARTESIAN_POINT('Ctrl Pts',(374.31583295143,-12.375646777982,1.83330264802732));
#47368=CARTESIAN_POINT('Ctrl Pts',(374.366833241234,-12.3697937566538,1.72911076379621));
#47369=CARTESIAN_POINT('Ctrl Pts',(374.417850540619,-12.36393878323,1.62488412955958));
#47370=CARTESIAN_POINT('Ctrl Pts',(374.464230371951,-12.3580838098062,1.51844015302638));
#47371=CARTESIAN_POINT('Ctrl Pts',(374.505793488026,-12.3522288363823,1.41023248546386));
#47372=CARTESIAN_POINT('Ctrl Pts',(374.547403710553,-12.3463672270982,1.30190217840889));
#47373=CARTESIAN_POINT('Ctrl Pts',(374.58418617351,-12.340505617814,1.19180457649481));
#47374=CARTESIAN_POINT('Ctrl Pts',(374.616011017644,-12.3346440085299,1.08041001947475));
#47375=CARTESIAN_POINT('Ctrl Pts',(374.647857321504,-12.3287784467195,0.968940348286817));
#47376=CARTESIAN_POINT('Ctrl Pts',(374.674739254403,-12.3229128849092,0.856172381466526));
#47377=CARTESIAN_POINT('Ctrl Pts',(374.696578107696,-12.3170473230988,0.742586511273045));
#47378=CARTESIAN_POINT('Ctrl Pts',(374.718448894749,-12.3111731843985,0.628834550678589));
#47379=CARTESIAN_POINT('Ctrl Pts',(374.735261825353,-12.3052990456982,0.51426270704055));
#47380=CARTESIAN_POINT('Ctrl Pts',(374.746990015676,-12.2994249069978,0.399356418719132));
#47381=CARTESIAN_POINT('Ctrl Pts',(374.749955883545,-12.2979394332166,0.370298494262374));
#47382=CARTESIAN_POINT('Ctrl Pts',(374.752596841717,-12.2964539594353,0.341219179107541));
#47383=CARTESIAN_POINT('Ctrl Pts',(374.754912982785,-12.2949684856541,0.312126304660852));
#47384=CARTESIAN_POINT('Ctrl Pts',(374.764071201122,-12.2890947962635,0.197090610234631));
#47385=CARTESIAN_POINT('Ctrl Pts',(374.768177421767,-12.2832211068729,0.0814599105867828));
#47386=CARTESIAN_POINT('Ctrl Pts',(374.76716841771,-12.2773474174824,-0.03428465281692));
#47387=CARTESIAN_POINT('Ctrl Pts',(374.766160716373,-12.2714813115766,-0.149879779115507));
#47388=CARTESIAN_POINT('Ctrl Pts',(374.760050927563,-12.2656152056709,-0.265588067461628));
#47389=CARTESIAN_POINT('Ctrl Pts',(374.748827579379,-12.2597490997651,-0.380923356911745));
#47390=CARTESIAN_POINT('Ctrl Pts',(374.73761572376,-12.2538890006771,-0.496140544494782));
#47391=CARTESIAN_POINT('Ctrl Pts',(374.721300763818,-12.248028901589,-0.610985084145689));
#47392=CARTESIAN_POINT('Ctrl Pts',(374.699923264801,-12.242168802501,-0.724971587018397));
#47393=CARTESIAN_POINT('Ctrl Pts',(374.67777451439,-12.2360972844069,-0.843070462869916));
#47394=CARTESIAN_POINT('Ctrl Pts',(374.650191042279,-12.2300257663128,-0.96024776933949));
#47395=CARTESIAN_POINT('Ctrl Pts',(374.617276707743,-12.2239542482187,-1.07596993685671));
#47396=CARTESIAN_POINT('Ctrl Pts',(374.58554501155,-12.2181008846219,-1.1875341144122));
#47397=CARTESIAN_POINT('Ctrl Pts',(374.548859067127,-12.2122475210252,-1.29774549056792));
#47398=CARTESIAN_POINT('Ctrl Pts',(374.507363617822,-12.2063941574284,-1.4061379061707));
#47399=CARTESIAN_POINT('Ctrl Pts',(374.465874398919,-12.2005416726945,-1.51451404701703));
#47400=CARTESIAN_POINT('Ctrl Pts',(374.41957725867,-12.1946891879606,-1.62107138462301));
#47401=CARTESIAN_POINT('Ctrl Pts',(374.368665883355,-12.1888367032267,-1.72536170176207));
#47402=CARTESIAN_POINT('Ctrl Pts',(374.31774984015,-12.1829836818985,-1.82966158092295));
#47403=CARTESIAN_POINT('Ctrl Pts',(374.26221890212,-12.1771306605703,-1.93169365513127));
#47404=CARTESIAN_POINT('Ctrl Pts',(374.202313386353,-12.1712776392422,-2.03103301027451));
#47405=CARTESIAN_POINT('Ctrl Pts',(374.142387890939,-12.1654226658183,-2.13040549701116));
#47406=CARTESIAN_POINT('Ctrl Pts',(374.078085129855,-12.1595676923945,-2.22708312530035));
#47407=CARTESIAN_POINT('Ctrl Pts',(374.009689138205,-12.1537127189707,-2.32066934364151));
#47408=CARTESIAN_POINT('Ctrl Pts',(373.941215628484,-12.1478511096865,-2.41436162994045));
#47409=CARTESIAN_POINT('Ctrl Pts',(373.868639872644,-12.1419895004024,-2.50495517933917));
#47410=CARTESIAN_POINT('Ctrl Pts',(373.792286702936,-12.1361278911182,-2.592085894436));
#47411=CARTESIAN_POINT('Ctrl Pts',(373.715882047724,-12.1302623293079,-2.67927536241393));
#47412=CARTESIAN_POINT('Ctrl Pts',(373.635695191791,-12.1243967674975,-2.76299704892786));
#47413=CARTESIAN_POINT('Ctrl Pts',(373.552087143815,-12.1185312056872,-2.84292438927202));
#47414=CARTESIAN_POINT('Ctrl Pts',(373.468356840368,-12.1126570669868,-2.92296860299122));
#47415=CARTESIAN_POINT('Ctrl Pts',(373.381195670678,-12.1067829282865,-2.99920712664242));
#47416=CARTESIAN_POINT('Ctrl Pts',(373.29099697843,-12.1009087895862,-3.07135420877801));
#47417=CARTESIAN_POINT('Ctrl Pts',(373.268187201665,-12.0994233158049,-3.08959902804002));
#47418=CARTESIAN_POINT('Ctrl Pts',(373.245183313492,-12.0979378420236,-3.10758241923529));
#47419=CARTESIAN_POINT('Ctrl Pts',(373.221991944898,-12.0964523682424,-3.12530021469079));
#47420=CARTESIAN_POINT('Ctrl Pts',(373.130291305428,-12.0905786788518,-3.19535788147928));
#47421=CARTESIAN_POINT('Ctrl Pts',(373.035351942402,-12.0847049894612,-3.26149287295327));
#47422=CARTESIAN_POINT('Ctrl Pts',(372.937543886807,-12.0788313000706,-3.32339122759574));
#47423=CARTESIAN_POINT('Ctrl Pts',(372.8398621106,-12.0729651941649,-3.38520966564726));
#47424=CARTESIAN_POINT('Ctrl Pts',(372.739319353292,-12.0670990882591,-3.44280212578014));
#47425=CARTESIAN_POINT('Ctrl Pts',(372.636317920711,-12.0612329823534,-3.49589541559476));
#47426=CARTESIAN_POINT('Ctrl Pts',(372.533421960285,-12.0553728832653,-3.54893433855698));
#47427=CARTESIAN_POINT('Ctrl Pts',(372.428072697452,-12.0495127841773,-3.59748306692355));
#47428=CARTESIAN_POINT('Ctrl Pts',(372.320699999074,-12.0436526850892,-3.64131255407982));
#47429=CARTESIAN_POINT('Ctrl Pts',(372.209453538694,-12.0375811669951,-3.68672330914158));
#47430=CARTESIAN_POINT('Ctrl Pts',(372.096035265976,-12.031509648901,-3.72706763338565));
#47431=CARTESIAN_POINT('Ctrl Pts',(371.980949846715,-12.0254381308069,-3.76214354743448));
#47432=CARTESIAN_POINT('Ctrl Pts',(371.869999538542,-12.0195847672102,-3.79595915585957));
#47433=CARTESIAN_POINT('Ctrl Pts',(371.757500254915,-12.0137314036134,-3.82487830411396));
#47434=CARTESIAN_POINT('Ctrl Pts',(371.643922179774,-12.0078780400167,-3.84876991185897));
#47435=CARTESIAN_POINT('Ctrl Pts',(371.530361158,-12.0020255552828,-3.87265793235948));
#47436=CARTESIAN_POINT('Ctrl Pts',(371.415722070971,-11.9961730705489,-3.89151982828963));
#47437=CARTESIAN_POINT('Ctrl Pts',(371.300486558315,-11.990320585815,-3.9052753729275));
#47438=CARTESIAN_POINT('Ctrl Pts',(371.185240480109,-11.9844675644868,-3.91903217876412));
#47439=CARTESIAN_POINT('Ctrl Pts',(371.069398277824,-11.9786145431586,-3.92768165363101));
#47440=CARTESIAN_POINT('Ctrl Pts',(370.953447288301,-11.9727615218304,-3.93119538788117));
#47441=CARTESIAN_POINT('Ctrl Pts',(370.837457626884,-11.9669065484066,-3.93471029402956));
#47442=CARTESIAN_POINT('Ctrl Pts',(370.721359518816,-11.9610515749828,-3.933086041091));
#47443=CARTESIAN_POINT('Ctrl Pts',(370.605640167566,-11.955196601559,-3.92634633165261));
#47444=CARTESIAN_POINT('Ctrl Pts',(370.489789663294,-11.9493349922748,-3.91959898361925));
#47445=CARTESIAN_POINT('Ctrl Pts',(370.374319185319,-11.9434733829907,-3.90772463123533));
#47446=CARTESIAN_POINT('Ctrl Pts',(370.259710782196,-11.9376117737065,-3.89079885292523));
#47447=CARTESIAN_POINT('Ctrl Pts',(370.145025097785,-11.9317462118962,-3.87386166143853));
#47448=CARTESIAN_POINT('Ctrl Pts',(370.031203050367,-11.9258806500858,-3.851866339692));
#47449=CARTESIAN_POINT('Ctrl Pts',(369.918714761065,-11.9200150882755,-3.82493921227891));
#47450=CARTESIAN_POINT('Ctrl Pts',(369.806061986295,-11.9141409495752,-3.79797271080122));
#47451=CARTESIAN_POINT('Ctrl Pts',(369.694747257532,-11.9082668108748,-3.76606012471631));
#47452=CARTESIAN_POINT('Ctrl Pts',(369.585223929312,-11.9023926721745,-3.72937707522931));
#47453=CARTESIAN_POINT('Ctrl Pts',(369.557527267587,-11.9009071983932,-3.72010053086942));
#47454=CARTESIAN_POINT('Ctrl Pts',(369.529945056278,-11.899421724612,-3.71051915052861));
#47455=CARTESIAN_POINT('Ctrl Pts',(369.502484392234,-11.8979362508307,-3.70063624694272));
#47456=CARTESIAN_POINT('Ctrl Pts',(369.393902596252,-11.8920625614401,-3.6615584074867));
#47457=CARTESIAN_POINT('Ctrl Pts',(369.286861312276,-11.8861888720496,-3.61763252361588));
#47458=CARTESIAN_POINT('Ctrl Pts',(369.181824961949,-11.880315182659,-3.5689993337471));
#47459=CARTESIAN_POINT('Ctrl Pts',(369.076924223419,-11.8744490767533,-3.52042893389528));
#47460=CARTESIAN_POINT('Ctrl Pts',(368.97402364223,-11.8685829708475,-3.46716348634993));
#47461=CARTESIAN_POINT('Ctrl Pts',(368.873570877915,-11.8627168649417,-3.40939295165821));
#47462=CARTESIAN_POINT('Ctrl Pts',(368.773220975951,-11.8568567658537,-3.35168157325814));
#47463=CARTESIAN_POINT('Ctrl Pts',(368.675314261174,-11.8509966667657,-3.28947448839703));
#47464=CARTESIAN_POINT('Ctrl Pts',(368.580276238164,-11.8451365676777,-3.22300874922444));
#47465=CARTESIAN_POINT('Ctrl Pts',(368.4818094601,-11.8390650495835,-3.15414507781506));
#47466=CARTESIAN_POINT('Ctrl Pts',(368.386422683485,-11.8329935314894,-3.08070985512133));
#47467=CARTESIAN_POINT('Ctrl Pts',(368.294559217302,-11.8269220133953,-3.00301766083049));
#47468=CARTESIAN_POINT('Ctrl Pts',(368.205996478874,-11.8210686497986,-2.92811700917058));
#47469=CARTESIAN_POINT('Ctrl Pts',(368.120708560026,-11.8152152862018,-2.8492603236528));
#47470=CARTESIAN_POINT('Ctrl Pts',(368.03906049978,-11.8093619226051,-2.76677164363374));
#47471=CARTESIAN_POINT('Ctrl Pts',(367.957424698715,-11.8035094378712,-2.6842953490124));
#47472=CARTESIAN_POINT('Ctrl Pts',(367.87942796014,-11.7976569531373,-2.5981884377652));
#47473=CARTESIAN_POINT('Ctrl Pts',(367.805398800622,-11.7918044684034,-2.50881214378072));
#47474=CARTESIAN_POINT('Ctrl Pts',(367.731362853623,-11.7859514470752,-2.41942765519019));
#47475=CARTESIAN_POINT('Ctrl Pts',(367.661295472383,-11.780098425747,-2.3267735061631));
#47476=CARTESIAN_POINT('Ctrl Pts',(367.595484719689,-11.7742454044189,-2.2312438085323));
#47477=CARTESIAN_POINT('Ctrl Pts',(367.529652017837,-11.7683904309951,-2.13568224990259));
#47478=CARTESIAN_POINT('Ctrl Pts',(367.468079001734,-11.7625354575713,-2.0372435756811));
#47479=CARTESIAN_POINT('Ctrl Pts',(367.411009871542,-11.7566804841475,-1.93635003616424));
#47480=CARTESIAN_POINT('Ctrl Pts',(367.353876060822,-11.7508188748633,-1.83534214677945));
#47481=CARTESIAN_POINT('Ctrl Pts',(367.301256527959,-11.7449572655792,-1.73187419865204));
#47482=CARTESIAN_POINT('Ctrl Pts',(367.253349086919,-11.739095656295,-1.62639223274904));
#47483=CARTESIAN_POINT('Ctrl Pts',(367.205409341539,-11.7332300944847,-1.52083913958189));
#47484=CARTESIAN_POINT('Ctrl Pts',(367.162188168537,-11.7273645326743,-1.41326970683518));
#47485=CARTESIAN_POINT('Ctrl Pts',(367.123834273497,-11.721498970864,-1.30414746274167));
#47486=CARTESIAN_POINT('Ctrl Pts',(367.085424295656,-11.7156248321637,-1.19486565516319));
#47487=CARTESIAN_POINT('Ctrl Pts',(367.05189591899,-11.7097506934633,-1.08402689863707));
#47488=CARTESIAN_POINT('Ctrl Pts',(367.023347335428,-11.703876554763,-0.972107356462185));
#47489=CARTESIAN_POINT('Ctrl Pts',(367.016127864704,-11.7023910809817,-0.943804731345743));
#47490=CARTESIAN_POINT('Ctrl Pts',(367.009226594706,-11.7009056072004,-0.915433025326923));
#47491=CARTESIAN_POINT('Ctrl Pts',(367.002644588985,-11.6994201334191,-0.886999997809972));
#47492=CARTESIAN_POINT('Ctrl Pts',(366.96759754733,-11.6915104682349,-0.735603365530406));
#47493=CARTESIAN_POINT('Ctrl Pts',(366.941511575413,-11.6836008030508,-0.582060497872048));
#47494=CARTESIAN_POINT('Ctrl Pts',(366.924595479983,-11.6756911378667,-0.427270364268486));
#47495=CARTESIAN_POINT('Ctrl Pts',(366.909248719815,-11.6685152659228,-0.286840377529521));
#47496=CARTESIAN_POINT('Ctrl Pts',(366.901448903756,-11.6613393939789,-0.145383673730004));
#47497=CARTESIAN_POINT('Ctrl Pts',(366.901319491283,-11.654163522035,-0.00358956409668104));
#47498=CARTESIAN_POINT('',(366.90131788919,-10.4041635220097,0.00053189028649518));
#47499=CARTESIAN_POINT('Ctrl Pts',(366.901319491282,-11.654163521998,-0.00358956336471676));
#47500=CARTESIAN_POINT('Ctrl Pts',(366.901215182272,-11.6483796262582,0.110699313728239));
#47501=CARTESIAN_POINT('Ctrl Pts',(366.906096752376,-11.6425957305185,0.225131833427297));
#47502=CARTESIAN_POINT('Ctrl Pts',(366.915974982574,-11.6368118347788,0.339231702561064));
#47503=CARTESIAN_POINT('Ctrl Pts',(366.925845835326,-11.6310322586764,0.453246357493513));
#47504=CARTESIAN_POINT('Ctrl Pts',(366.940705892319,-11.625252682574,0.566928433969708));
#47505=CARTESIAN_POINT('Ctrl Pts',(366.960513867979,-11.6194731064716,0.679802680118736));
#47506=CARTESIAN_POINT('Ctrl Pts',(366.980314074705,-11.6136957971903,0.792632655595791));
#47507=CARTESIAN_POINT('Ctrl Pts',(367.005058271152,-11.607918487909,0.904655012256961));
#47508=CARTESIAN_POINT('Ctrl Pts',(367.034653522482,-11.6021411786277,1.01540138550626));
#47509=CARTESIAN_POINT('Ctrl Pts',(367.064244769121,-11.5963646511048,1.12613277307442));
#47510=CARTESIAN_POINT('Ctrl Pts',(367.098685656149,-11.5905881235819,1.23558810989203));
#47511=CARTESIAN_POINT('Ctrl Pts',(367.137832716529,-11.5848115960591,1.34331181569878));
#47512=CARTESIAN_POINT('Ctrl Pts',(367.176984536858,-11.5790343661599,1.45104861978714));
#47513=CARTESIAN_POINT('Ctrl Pts',(367.220843521669,-11.5732571362606,1.55705297529893));
#47514=CARTESIAN_POINT('Ctrl Pts',(367.2692174786,-11.5674799063614,1.66088781043613));
#47515=CARTESIAN_POINT('Ctrl Pts',(367.317639838785,-11.5616968957335,1.76482654329352));
#47516=CARTESIAN_POINT('Ctrl Pts',(367.370586012797,-11.5559138851055,1.86659103486682));
#47517=CARTESIAN_POINT('Ctrl Pts',(367.427817094876,-11.5501308744776,1.96576742860724));
#47518=CARTESIAN_POINT('Ctrl Pts',(367.485077457007,-11.5443449051976,2.06499456208419));
#47519=CARTESIAN_POINT('Ctrl Pts',(367.546626862797,-11.5385589359176,2.16163060370046));
#47520=CARTESIAN_POINT('Ctrl Pts',(367.612183253346,-11.5327729666377,2.25529102784255));
#47521=CARTESIAN_POINT('Ctrl Pts',(367.677845415416,-11.5269776620242,2.34910256777101));
#47522=CARTESIAN_POINT('Ctrl Pts',(367.747527215841,-11.5211823574107,2.43992856443434));
#47523=CARTESIAN_POINT('Ctrl Pts',(367.820906340132,-11.5153870527972,2.52741766488383));
#47524=CARTESIAN_POINT('Ctrl Pts',(367.88203355878,-11.5105593738673,2.60029895672426));
#47525=CARTESIAN_POINT('Ctrl Pts',(367.945725724977,-11.5057316949374,2.67086518134212));
#47526=CARTESIAN_POINT('Ctrl Pts',(368.011778274973,-11.5009040160074,2.73893397678839));
#47527=CARTESIAN_POINT('Ctrl Pts',(368.092142393581,-11.4950303266169,2.82175119960785));
#47528=CARTESIAN_POINT('Ctrl Pts',(368.176288405315,-11.4891566372263,2.90116636477388));
#47529=CARTESIAN_POINT('Ctrl Pts',(368.263896635884,-11.4832829478357,2.97681436529831));
#47530=CARTESIAN_POINT('Ctrl Pts',(368.351391755996,-11.47741684193,3.05236469714728));
#47531=CARTESIAN_POINT('Ctrl Pts',(368.442339895635,-11.4715507360242,3.1241572692397));
#47532=CARTESIAN_POINT('Ctrl Pts',(368.536383445241,-11.4656846301184,3.19186253723573));
#47533=CARTESIAN_POINT('Ctrl Pts',(368.630330695451,-11.4598245310304,3.25949847589982));
#47534=CARTESIAN_POINT('Ctrl Pts',(368.727366717613,-11.4539644319424,3.32305519551668));
#47535=CARTESIAN_POINT('Ctrl Pts',(368.827100131096,-11.4481043328543,3.38224274941558));
#47536=CARTESIAN_POINT('Ctrl Pts',(368.930431698608,-11.4420328147602,3.44356565523069));
#47537=CARTESIAN_POINT('Ctrl Pts',(369.036658621759,-11.4359612966661,3.50019788883464));
#47538=CARTESIAN_POINT('Ctrl Pts',(369.145311546712,-11.429889778572,3.55186524189249));
#47539=CARTESIAN_POINT('Ctrl Pts',(369.250060485239,-11.4240364149752,3.60167614566354));
#47540=CARTESIAN_POINT('Ctrl Pts',(369.357063684405,-11.4181830513785,3.6468726203118));
#47541=CARTESIAN_POINT('Ctrl Pts',(369.465875437462,-11.4123296877817,3.68725566712477));
#47542=CARTESIAN_POINT('Ctrl Pts',(369.574670852801,-11.4064772030478,3.72763265055916));
#47543=CARTESIAN_POINT('Ctrl Pts',(369.685273894864,-11.4006247183139,3.76319749948658));
#47544=CARTESIAN_POINT('Ctrl Pts',(369.797220025612,-11.39477223358,3.79379982286389));
#47545=CARTESIAN_POINT('Ctrl Pts',(369.909176420316,-11.3889192122518,3.82440495206331));
#47546=CARTESIAN_POINT('Ctrl Pts',(370.022475749958,-11.3830661909237,3.85004654227254));
#47547=CARTESIAN_POINT('Ctrl Pts',(370.136640198579,-11.3772131695955,3.87062461241202));
#47548=CARTESIAN_POINT('Ctrl Pts',(370.25084272325,-11.3713581961716,3.89120954573541));
#47549=CARTESIAN_POINT('Ctrl Pts',(370.365910534263,-11.3655032227478,3.90672752767336));
#47550=CARTESIAN_POINT('Ctrl Pts',(370.481358261021,-11.3596482493239,3.91713013905234));
#47551=CARTESIAN_POINT('Ctrl Pts',(370.596936832949,-11.3537866400398,3.92754454045511));
#47552=CARTESIAN_POINT('Ctrl Pts',(370.712895768338,-11.3479250307556,3.93283196250993));
#47553=CARTESIAN_POINT('Ctrl Pts',(370.828747143433,-11.3420634214715,3.93299605481526));
#47554=CARTESIAN_POINT('Ctrl Pts',(370.944676637962,-11.3361978596611,3.93316025776924));
#47555=CARTESIAN_POINT('Ctrl Pts',(371.060498016033,-11.3303322978508,3.92819426955597));
#47556=CARTESIAN_POINT('Ctrl Pts',(371.175727665805,-11.3244667360404,3.91815369018025));
#47557=CARTESIAN_POINT('Ctrl Pts',(371.291125809587,-11.3185925973401,3.90809842901487));
#47558=CARTESIAN_POINT('Ctrl Pts',(371.405930090223,-11.3127184586397,3.89295382146471));
#47559=CARTESIAN_POINT('Ctrl Pts',(371.519666207819,-11.3068443199394,3.87282669801451));
#47560=CARTESIAN_POINT('Ctrl Pts',(371.548428215201,-11.3053588461582,3.86773687707201));
#47561=CARTESIAN_POINT('Ctrl Pts',(371.577121987322,-11.303873372377,3.86232867299253));
#47562=CARTESIAN_POINT('Ctrl Pts',(371.605740016327,-11.3023878985958,3.8566043154922));
#47563=CARTESIAN_POINT('Ctrl Pts',(371.718898131588,-11.2965142092052,3.83396972015762));
#47564=CARTESIAN_POINT('Ctrl Pts',(371.831247671338,-11.2906405198146,3.80631288254161));
#47565=CARTESIAN_POINT('Ctrl Pts',(371.942308534838,-11.2847668304241,3.77370449948818));
#47566=CARTESIAN_POINT('Ctrl Pts',(372.053226008329,-11.2789007245183,3.74113821692072));
#47567=CARTESIAN_POINT('Ctrl Pts',(372.162857721535,-11.2730346186126,3.70363321764507));
#47568=CARTESIAN_POINT('Ctrl Pts',(372.27073289222,-11.2671685127068,3.66131135465771));
#47569=CARTESIAN_POINT('Ctrl Pts',(372.378497600105,-11.2613084136188,3.61903282871878));
#47570=CARTESIAN_POINT('Ctrl Pts',(372.484508960866,-11.2554483145307,3.57194740002706));
#47571=CARTESIAN_POINT('Ctrl Pts',(372.588311158879,-11.2495882154427,3.52022676595114));
#47572=CARTESIAN_POINT('Ctrl Pts',(372.695858303384,-11.2435166973486,3.46664016939151));
#47573=CARTESIAN_POINT('Ctrl Pts',(372.801033439052,-11.2374451792545,3.40807772474959));
#47574=CARTESIAN_POINT('Ctrl Pts',(372.903351705287,-11.2313736611604,3.34478518279101));
#47575=CARTESIAN_POINT('Ctrl Pts',(373.001993594445,-11.2255202975636,3.28376679244709));
#47576=CARTESIAN_POINT('Ctrl Pts',(373.097979998734,-11.2196669339668,3.21835260328277));
#47577=CARTESIAN_POINT('Ctrl Pts',(373.190902076107,-11.2138135703701,3.14880926708155));
#47578=CARTESIAN_POINT('Ctrl Pts',(373.283810201543,-11.2079610856362,3.07927637257826));
#47579=CARTESIAN_POINT('Ctrl Pts',(373.37365458423,-11.2021086009023,3.00561581126896));
#47580=CARTESIAN_POINT('Ctrl Pts',(373.460057018905,-11.1962561161684,2.92813640969929));
#47581=CARTESIAN_POINT('Ctrl Pts',(373.546467375524,-11.1904030948402,2.8506499043089));
#47582=CARTESIAN_POINT('Ctrl Pts',(373.629434849181,-11.184550073512,2.7693441384577));
#47583=CARTESIAN_POINT('Ctrl Pts',(373.708616396416,-11.1786970521839,2.68456642395035));
#47584=CARTESIAN_POINT('Ctrl Pts',(373.787824352227,-11.17284207876,2.59976043443776));
#47585=CARTESIAN_POINT('Ctrl Pts',(373.863243588983,-11.1669871053362,2.51148049548327));
#47586=CARTESIAN_POINT('Ctrl Pts',(373.934570295656,-11.1611321319124,2.4201082193142));
#47587=CARTESIAN_POINT('Ctrl Pts',(374.00597784199,-11.1552705226282,2.3286323844066));
#47588=CARTESIAN_POINT('Ctrl Pts',(374.073283345994,-11.1494089133441,2.234057542831));
#47589=CARTESIAN_POINT('Ctrl Pts',(374.136225366349,-11.1435473040599,2.13679567922817));
#47590=CARTESIAN_POINT('Ctrl Pts',(374.19920982897,-11.1376817422495,2.03946823123608));
#47591=CARTESIAN_POINT('Ctrl Pts',(374.257824740736,-11.1318161804392,1.9394505089267));
#47592=CARTESIAN_POINT('Ctrl Pts',(374.311854652188,-11.1259506186288,1.83717903641679));
#47593=CARTESIAN_POINT('Ctrl Pts',(374.365963568622,-11.1200764799285,1.73475801793067));
#47594=CARTESIAN_POINT('Ctrl Pts',(374.415473928492,-11.1142023412282,1.63007704422646));
#47595=CARTESIAN_POINT('Ctrl Pts',(374.460218379809,-11.1083282025278,1.5235925870489));
#47596=CARTESIAN_POINT('Ctrl Pts',(374.471533521088,-11.1068427287466,1.49666440620109));
#47597=CARTESIAN_POINT('Ctrl Pts',(374.482544131535,-11.1053572549653,1.46962096545237));
#47598=CARTESIAN_POINT('Ctrl Pts',(374.493248014717,-11.1038717811841,1.4424697824612));
#47599=CARTESIAN_POINT('Ctrl Pts',(374.53557207717,-11.0979980917935,1.33511170082433));
#47600=CARTESIAN_POINT('Ctrl Pts',(374.573237573548,-11.092124402403,1.22571046622616));
#47601=CARTESIAN_POINT('Ctrl Pts',(374.606043643788,-11.0862507130124,1.11470783651795));
#47602=CARTESIAN_POINT('Ctrl Pts',(374.638807358309,-11.0803846071066,1.00384852163303));
#47603=CARTESIAN_POINT('Ctrl Pts',(374.666724007546,-11.0745185012009,0.891392315905275));
#47604=CARTESIAN_POINT('Ctrl Pts',(374.689640769999,-11.0686523952951,0.7778008790112));
#47605=CARTESIAN_POINT('Ctrl Pts',(374.712534065979,-11.0627922962071,0.664325758300855));
#47606=CARTESIAN_POINT('Ctrl Pts',(374.730437577704,-11.056932197119,0.549718121236184));
#47607=CARTESIAN_POINT('Ctrl Pts',(374.743248481834,-11.0510720980309,0.434454072040985));
#47608=CARTESIAN_POINT('Ctrl Pts',(374.756521574159,-11.0450005799368,0.315031558910803));
#47609=CARTESIAN_POINT('Ctrl Pts',(374.764327533741,-11.0389290618427,0.1949048088503));
#47610=CARTESIAN_POINT('Ctrl Pts',(374.76661001934,-11.0328575437486,0.0746144778491838));
#47611=CARTESIAN_POINT('Ctrl Pts',(374.768810493406,-11.0270041801519,-0.0413537254252988));
#47612=CARTESIAN_POINT('Ctrl Pts',(374.765877579626,-11.0211508165552,-0.157473508275035));
#47613=CARTESIAN_POINT('Ctrl Pts',(374.757813710422,-11.0152974529584,-0.273256763051596));
#47614=CARTESIAN_POINT('Ctrl Pts',(374.74975105198,-11.0094449682245,-0.389022633362168));
#47615=CARTESIAN_POINT('Ctrl Pts',(374.736558998648,-11.0035924834906,-0.504451664033412));
#47616=CARTESIAN_POINT('Ctrl Pts',(374.718292031124,-10.9977399987567,-0.619058628406891));
#47617=CARTESIAN_POINT('Ctrl Pts',(374.700023388765,-10.9918869774286,-0.733676100700433));
#47618=CARTESIAN_POINT('Ctrl Pts',(374.676678972271,-10.9860339561004,-0.847470948845424));
#47619=CARTESIAN_POINT('Ctrl Pts',(374.648364663355,-10.9801809347722,-0.959966629697134));
#47620=CARTESIAN_POINT('Ctrl Pts',(374.62004091107,-10.9743259613484,-1.07249983003061));
#47621=CARTESIAN_POINT('Ctrl Pts',(374.586744071174,-10.9684709879246,-1.18373260104513));
#47622=CARTESIAN_POINT('Ctrl Pts',(374.548630116569,-10.9626160145008,-1.29320277233124));
#47623=CARTESIAN_POINT('Ctrl Pts',(374.510472964692,-10.9567544052166,-1.40279701399576));
#47624=CARTESIAN_POINT('Ctrl Pts',(374.467487937032,-10.9508927959325,-1.51062427829115));
#47625=CARTESIAN_POINT('Ctrl Pts',(374.419879497689,-10.9450311866483,-1.61624153323157));
#47626=CARTESIAN_POINT('Ctrl Pts',(374.372238955626,-10.939165624838,-1.72193000666273));
#47627=CARTESIAN_POINT('Ctrl Pts',(374.319968979865,-10.9333000630276,-1.82540513551587));
#47628=CARTESIAN_POINT('Ctrl Pts',(374.263319587847,-10.9274345012173,-1.92624923204487));
#47629=CARTESIAN_POINT('Ctrl Pts',(374.206587360523,-10.921560362517,-2.02724078737673));
#47630=CARTESIAN_POINT('Ctrl Pts',(374.145463153846,-10.9156862238166,-2.12559328276021));
#47631=CARTESIAN_POINT('Ctrl Pts',(374.080239821498,-10.9098120851163,-2.22091863333134));
#47632=CARTESIAN_POINT('Ctrl Pts',(374.063745905526,-10.908326611335,-2.24502485829247));
#47633=CARTESIAN_POINT('Ctrl Pts',(374.046990046694,-10.9068411375538,-2.26893766709365));
#47634=CARTESIAN_POINT('Ctrl Pts',(374.029977371444,-10.9053556637725,-2.29265113866268));
#47635=CARTESIAN_POINT('Ctrl Pts',(373.962707809783,-10.8994819743819,-2.38641621760609));
#47636=CARTESIAN_POINT('Ctrl Pts',(373.89119591768,-10.8936082849913,-2.4773742795736));
#47637=CARTESIAN_POINT('Ctrl Pts',(373.815704019572,-10.8877345956008,-2.56511705914373));
#47638=CARTESIAN_POINT('Ctrl Pts',(373.740309588596,-10.881868489695,-2.65274655454223));
#47639=CARTESIAN_POINT('Ctrl Pts',(373.660945637523,-10.8760023837893,-2.73716871266042));
#47640=CARTESIAN_POINT('Ctrl Pts',(373.577917256613,-10.8701362778835,-2.81800484629181));
#47641=CARTESIAN_POINT('Ctrl Pts',(373.494973895707,-10.8642761787954,-2.89875820475259));
#47642=CARTESIAN_POINT('Ctrl Pts',(373.408373862918,-10.8584160797074,-2.97593255623467));
#47643=CARTESIAN_POINT('Ctrl Pts',(373.318461490852,-10.8525559806193,-3.04918339685073));
#47644=CARTESIAN_POINT('Ctrl Pts',(373.225305285526,-10.8464844625252,-3.12507696068391));
#47645=CARTESIAN_POINT('Ctrl Pts',(373.128593519723,-10.8404129444311,-3.19675822351067));
#47646=CARTESIAN_POINT('Ctrl Pts',(373.028749967792,-10.834341426337,-3.26388674658822));
#47647=CARTESIAN_POINT('Ctrl Pts',(372.932493874474,-10.8284880627402,-3.3286032881839));
#47648=CARTESIAN_POINT('Ctrl Pts',(372.833327549274,-10.8226346991435,-3.38908837641804));
#47649=CARTESIAN_POINT('Ctrl Pts',(372.731662471519,-10.8167813355467,-3.4450794474769));
#47650=CARTESIAN_POINT('Ctrl Pts',(372.630012658433,-10.8109288508128,-3.50106211166493));
#47651=CARTESIAN_POINT('Ctrl Pts',(372.525865200583,-10.8050763660789,-3.5525519011026));
#47652=CARTESIAN_POINT('Ctrl Pts',(372.419657372243,-10.799223881345,-3.5993315503625));
#47653=CARTESIAN_POINT('Ctrl Pts',(372.313439806072,-10.7933708600168,-3.64611548868808));
#47654=CARTESIAN_POINT('Ctrl Pts',(372.205161871994,-10.7875178386886,-3.68818826180301));
#47655=CARTESIAN_POINT('Ctrl Pts',(372.095281412437,-10.7816648173604,-3.72538050436962));
#47656=CARTESIAN_POINT('Ctrl Pts',(371.985364305624,-10.7758098439366,-3.76258515126731));
#47657=CARTESIAN_POINT('Ctrl Pts',(371.873844001681,-10.7699548705128,-3.79490589851871));
#47658=CARTESIAN_POINT('Ctrl Pts',(371.76119342042,-10.764099897089,-3.82222326440183));
#47659=CARTESIAN_POINT('Ctrl Pts',(371.648415164195,-10.7582382878048,-3.84957159101047));
#47660=CARTESIAN_POINT('Ctrl Pts',(371.53450447554,-10.7523766785207,-3.871905120476));
#47661=CARTESIAN_POINT('Ctrl Pts',(371.419944479641,-10.7465150692365,-3.88915549373279));
#47662=CARTESIAN_POINT('Ctrl Pts',(371.305307235095,-10.7406495074261,-3.906417499043));
#47663=CARTESIAN_POINT('Ctrl Pts',(371.190020221328,-10.7347839456158,-3.91858947974213));
#47664=CARTESIAN_POINT('Ctrl Pts',(371.074569961465,-10.7289183838054,-3.92565509494733));
#47665=CARTESIAN_POINT('Ctrl Pts',(370.958950885005,-10.7230442451051,-3.93273104181488));
#47666=CARTESIAN_POINT('Ctrl Pts',(370.84316849755,-10.7171701064047,-3.93468571446806));
#47667=CARTESIAN_POINT('Ctrl Pts',(370.727707668622,-10.7112959677044,-3.93155481565997));
#47668=CARTESIAN_POINT('Ctrl Pts',(370.698509509899,-10.7098104939232,-3.93076306246374));
#47669=CARTESIAN_POINT('Ctrl Pts',(370.669331878578,-10.708325020142,-3.92964634388684));
#47670=CARTESIAN_POINT('Ctrl Pts',(370.640182529275,-10.7068395463608,-3.92820575784862));
#47671=CARTESIAN_POINT('Ctrl Pts',(370.524923528467,-10.7009658569702,-3.92250955840308));
#47672=CARTESIAN_POINT('Ctrl Pts',(370.40972347837,-10.6950921675796,-3.91172678479583));
#47673=CARTESIAN_POINT('Ctrl Pts',(370.295067656193,-10.689218478189,-3.89585654574217));
#47674=CARTESIAN_POINT('Ctrl Pts',(370.180559865454,-10.6833523722833,-3.88000679665806));
#47675=CARTESIAN_POINT('Ctrl Pts',(370.066595310801,-10.6774862663775,-3.85908270064177));
#47676=CARTESIAN_POINT('Ctrl Pts',(369.953657598398,-10.6716201604718,-3.83313533749715));
#47677=CARTESIAN_POINT('Ctrl Pts',(369.840835532773,-10.6657600613837,-3.80721454412178));
#47678=CARTESIAN_POINT('Ctrl Pts',(369.729038618192,-10.6598999622957,-3.77628080694585));
#47679=CARTESIAN_POINT('Ctrl Pts',(369.618743009953,-10.6540398632076,-3.74043671252538));
#47680=CARTESIAN_POINT('Ctrl Pts',(369.504468187795,-10.6479683451135,-3.7032994449518));
#47681=CARTESIAN_POINT('Ctrl Pts',(369.391805492076,-10.6418968270194,-3.66089088357027));
#47682=CARTESIAN_POINT('Ctrl Pts',(369.281270728248,-10.6358253089253,-3.61338257420974));
#47683=CARTESIAN_POINT('Ctrl Pts',(369.174707566821,-10.6299719453285,-3.5675812763722));
#47684=CARTESIAN_POINT('Ctrl Pts',(369.070122464476,-10.6241185817318,-3.51704057673404));
#47685=CARTESIAN_POINT('Ctrl Pts',(368.967959122503,-10.618265218135,-3.46196390626234));
#47686=CARTESIAN_POINT('Ctrl Pts',(368.865811120013,-10.6124127334011,-3.40689550536733));
#47687=CARTESIAN_POINT('Ctrl Pts',(368.76608451845,-10.6065602486672,-3.34729268384378));
#47688=CARTESIAN_POINT('Ctrl Pts',(368.669198938201,-10.6007077639333,-3.2834051050409));
#47689=CARTESIAN_POINT('Ctrl Pts',(368.572304474845,-10.5948547426051,-3.21951166860491));
#47690=CARTESIAN_POINT('Ctrl Pts',(368.478251895547,-10.589001721277,-3.15133292138021));
#47691=CARTESIAN_POINT('Ctrl Pts',(368.387431720063,-10.5831486999488,-3.07916177739079));
#47692=CARTESIAN_POINT('Ctrl Pts',(368.296581254297,-10.577293726525,-3.00696656293146));
#47693=CARTESIAN_POINT('Ctrl Pts',(368.208965659316,-10.5714387531012,-2.930776560893));
#47694=CARTESIAN_POINT('Ctrl Pts',(368.124941710878,-10.5655837796774,-2.85092439732906));
#47695=CARTESIAN_POINT('Ctrl Pts',(368.040822532086,-10.5597221703933,-2.77098173159402));
#47696=CARTESIAN_POINT('Ctrl Pts',(367.960303424295,-10.5538605611091,-2.68736890477402));
#47697=CARTESIAN_POINT('Ctrl Pts',(367.883703736922,-10.547998951825,-2.60045483265561));
#47698=CARTESIAN_POINT('Ctrl Pts',(367.807052397818,-10.5421333900146,-2.51348215373961));
#47699=CARTESIAN_POINT('Ctrl Pts',(367.734326000261,-10.5362678282043,-2.42320411789578));
#47700=CARTESIAN_POINT('Ctrl Pts',(367.665802024439,-10.5304022663939,-2.33002069577421));
#47701=CARTESIAN_POINT('Ctrl Pts',(367.597177849757,-10.5245281276936,-2.23670101663513));
#47702=CARTESIAN_POINT('Ctrl Pts',(367.53276858954,-10.5186539889932,-2.14046781452422));
#47703=CARTESIAN_POINT('Ctrl Pts',(367.472807094867,-10.5127798502929,-2.0417478839095));
#47704=CARTESIAN_POINT('Ctrl Pts',(367.457643811743,-10.5112943765116,-2.01678322507226));
#47705=CARTESIAN_POINT('Ctrl Pts',(367.442764727678,-10.5098089027304,-1.99165964874772));
#47706=CARTESIAN_POINT('Ctrl Pts',(367.428173123932,-10.5083234289491,-1.96638426639313));
#47707=CARTESIAN_POINT('Ctrl Pts',(367.368141660461,-10.5022120263512,-1.86239856207889));
#47708=CARTESIAN_POINT('Ctrl Pts',(367.312793417312,-10.4961006237533,-1.75551901299763));
#47709=CARTESIAN_POINT('Ctrl Pts',(367.262405685373,-10.4899892211554,-1.64618725094086));
#47710=CARTESIAN_POINT('Ctrl Pts',(367.212102004518,-10.4838880129041,-1.53703786369272));
#47711=CARTESIAN_POINT('Ctrl Pts',(367.166742509801,-10.4777868046528,-1.42544473910998));
#47712=CARTESIAN_POINT('Ctrl Pts',(367.126559598673,-10.4716855964015,-1.3118756518083));
#47713=CARTESIAN_POINT('Ctrl Pts',(367.086459358382,-10.4655969405508,-1.19854021735285));
#47714=CARTESIAN_POINT('Ctrl Pts',(367.051514595037,-10.4595082847,-1.0832372664709));
#47715=CARTESIAN_POINT('Ctrl Pts',(367.02191005392,-10.4534196288493,-0.966455261149849));
#47716=CARTESIAN_POINT('Ctrl Pts',(366.992341577382,-10.4473383902664,-0.849815520959467));
#47717=CARTESIAN_POINT('Ctrl Pts',(366.968100460896,-10.4412571516836,-0.731700666398687));
#47718=CARTESIAN_POINT('Ctrl Pts',(366.949322268095,-10.4351759131007,-0.612615951090308));
#47719=CARTESIAN_POINT('Ctrl Pts',(366.93057115913,-10.4291034455039,-0.493702991971166));
#47720=CARTESIAN_POINT('Ctrl Pts',(366.917267326928,-10.423030977907,-0.373823320364159));
#47721=CARTESIAN_POINT('Ctrl Pts',(366.909495549282,-10.4169585103101,-0.253493357862614));
#47722=CARTESIAN_POINT('Ctrl Pts',(366.904037043204,-10.4126935142184,-0.168979638918359));
#47723=CARTESIAN_POINT('Ctrl Pts',(366.901306424284,-10.4084285181267,-0.084244080169046));
#47724=CARTESIAN_POINT('Ctrl Pts',(366.90131788919,-10.404163522035,0.000531889783890909));
#47725=CARTESIAN_POINT('',(366.901319257773,-9.15416352206362,0.0033238806608616));
#47726=CARTESIAN_POINT('Ctrl Pts',(366.90131788919,-10.4041635220097,0.000531890286507496));
#47727=CARTESIAN_POINT('Ctrl Pts',(366.901334546036,-10.397967106677,0.123698971514546));
#47728=CARTESIAN_POINT('Ctrl Pts',(366.90714118116,-10.3917706913442,0.24673041215044));
#47729=CARTESIAN_POINT('Ctrl Pts',(366.918674138795,-10.3855742760115,0.369084409932434));
#47730=CARTESIAN_POINT('Ctrl Pts',(366.930425787995,-10.3792603623053,0.493758522643907));
#47731=CARTESIAN_POINT('Ctrl Pts',(366.948123041569,-10.3729464485991,0.617728875741365));
#47732=CARTESIAN_POINT('Ctrl Pts',(366.971644572484,-10.366632534893,0.740435092533959));
#47733=CARTESIAN_POINT('Ctrl Pts',(366.994835326488,-10.3604074120428,0.861415725079769));
#47734=CARTESIAN_POINT('Ctrl Pts',(367.023687438356,-10.3541822891927,0.981167248159586));
#47735=CARTESIAN_POINT('Ctrl Pts',(367.058034653411,-10.3479571663425,1.09916977524578));
#47736=CARTESIAN_POINT('Ctrl Pts',(367.093116725923,-10.3415988572083,1.21969696224078));
#47737=CARTESIAN_POINT('Ctrl Pts',(367.133931549207,-10.3352405480742,1.33839911611543));
#47738=CARTESIAN_POINT('Ctrl Pts',(367.180251034586,-10.32888223894,1.45474557394974));
#47739=CARTESIAN_POINT('Ctrl Pts',(367.226570519964,-10.3225239298058,1.57109203178405));
#47740=CARTESIAN_POINT('Ctrl Pts',(367.278394451635,-10.3161656206716,1.68508249127342));
#47741=CARTESIAN_POINT('Ctrl Pts',(367.335446269933,-10.3098073115375,1.79621453163071));
#47742=CARTESIAN_POINT('Ctrl Pts',(367.388149693561,-10.3039336221469,1.89887627276736));
#47743=CARTESIAN_POINT('Ctrl Pts',(367.445463080222,-10.2980599327563,1.99938744358157));
#47744=CARTESIAN_POINT('Ctrl Pts',(367.507187193913,-10.2921862433658,2.09730555138536));
#47745=CARTESIAN_POINT('Ctrl Pts',(367.568831615974,-10.28632013746,2.19509723771302));
#47746=CARTESIAN_POINT('Ctrl Pts',(367.634875221945,-10.2804540315542,2.29030217257284));
#47747=CARTESIAN_POINT('Ctrl Pts',(367.705072114982,-10.2745879256485,2.38250081000885));
#47748=CARTESIAN_POINT('Ctrl Pts',(367.775197127294,-10.2687278265604,2.47460503721481));
#47749=CARTESIAN_POINT('Ctrl Pts',(367.849466718492,-10.2628677274724,2.56370876344987));
#47750=CARTESIAN_POINT('Ctrl Pts',(367.927591136577,-10.2570076283843,2.64942046393696));
#47751=CARTESIAN_POINT('Ctrl Pts',(368.008534105435,-10.2509361102902,2.73822444703758));
#47752=CARTESIAN_POINT('Ctrl Pts',(368.093615058581,-10.2448645921961,2.82338664814203));
#47753=CARTESIAN_POINT('Ctrl Pts',(368.182465071594,-10.238793074102,2.90450784549792));
#47754=CARTESIAN_POINT('Ctrl Pts',(368.268122632632,-10.2329397105052,2.98271429340253));
#47755=CARTESIAN_POINT('Ctrl Pts',(368.357282732902,-10.2270863469085,3.05716483048702));
#47756=CARTESIAN_POINT('Ctrl Pts',(368.449577121972,-10.2212329833117,3.1275390716518));
#47757=CARTESIAN_POINT('Ctrl Pts',(368.54185765335,-10.2153804985778,3.19790274636107));
#47758=CARTESIAN_POINT('Ctrl Pts',(368.637271209345,-10.2095280138439,3.2641910916806));
#47759=CARTESIAN_POINT('Ctrl Pts',(368.735417345211,-10.20367552911,3.32612472067188));
#47760=CARTESIAN_POINT('Ctrl Pts',(368.833572479761,-10.1978225077818,3.38806402814545));
#47761=CARTESIAN_POINT('Ctrl Pts',(368.934460342818,-10.1919694864536,3.44564760508858));
#47762=CARTESIAN_POINT('Ctrl Pts',(369.037653081194,-10.1861164651254,3.49864040692185));
#47763=CARTESIAN_POINT('Ctrl Pts',(369.140880236341,-10.1802614917016,3.55165088287785));
#47764=CARTESIAN_POINT('Ctrl Pts',(369.246413428055,-10.1744065182777,3.60006735054566));
#47765=CARTESIAN_POINT('Ctrl Pts',(369.353802532841,-10.1685515448539,3.64370187942303));
#47766=CARTESIAN_POINT('Ctrl Pts',(369.461313349384,-10.1626899355697,3.68738586243426));
#47767=CARTESIAN_POINT('Ctrl Pts',(369.570683894368,-10.1568283262856,3.72627693362464));
#47768=CARTESIAN_POINT('Ctrl Pts',(369.681446409961,-10.1509667170014,3.76023622067938));
#47769=CARTESIAN_POINT('Ctrl Pts',(369.792283613532,-10.145101155191,3.79421840673072));
#47770=CARTESIAN_POINT('Ctrl Pts',(369.904514257726,-10.1392355933807,3.82326208351196));
#47771=CARTESIAN_POINT('Ctrl Pts',(370.017659551262,-10.1333700315704,3.84727932672379));
#47772=CARTESIAN_POINT('Ctrl Pts',(370.130970290967,-10.12749589287,3.87133168903586));
#47773=CARTESIAN_POINT('Ctrl Pts',(370.24519794324,-10.1216217541697,3.89034288170131));
#47774=CARTESIAN_POINT('Ctrl Pts',(370.359857675873,-10.1157476154693,3.90427669871234));
#47775=CARTESIAN_POINT('Ctrl Pts',(370.38885325042,-10.1142621416881,3.90780033356294));
#47776=CARTESIAN_POINT('Ctrl Pts',(370.417876454481,-10.112776667907,3.91099952969392));
#47777=CARTESIAN_POINT('Ctrl Pts',(370.446919456317,-10.1112911941258,3.91387422920996));
#47778=CARTESIAN_POINT('Ctrl Pts',(370.561757950213,-10.1054175047352,3.92524103504811));
#47779=CARTESIAN_POINT('Ctrl Pts',(370.677288407797,-10.0995438153447,3.93156820814741));
#47780=CARTESIAN_POINT('Ctrl Pts',(370.793030991257,-10.0936701259541,3.93278328859206));
#47781=CARTESIAN_POINT('Ctrl Pts',(370.908624140169,-10.0878040200484,3.9339968002537));
#47782=CARTESIAN_POINT('Ctrl Pts',(371.024428460962,-10.0819379141426,3.93011134058086));
#47783=CARTESIAN_POINT('Ctrl Pts',(371.139958102859,-10.0760718082369,3.92110609876892));
#47784=CARTESIAN_POINT('Ctrl Pts',(371.255369443875,-10.0702117091488,3.91211007820986));
#47785=CARTESIAN_POINT('Ctrl Pts',(371.370506256012,-10.0643516100608,3.89800473537644));
#47786=CARTESIAN_POINT('Ctrl Pts',(371.484882460614,-10.0584915109728,3.87882130184055));
#47787=CARTESIAN_POINT('Ctrl Pts',(371.603385097744,-10.0524199928787,3.85894577378706));
#47788=CARTESIAN_POINT('Ctrl Pts',(371.721070757523,-10.0463484747846,3.83361882040846));
#47789=CARTESIAN_POINT('Ctrl Pts',(371.837403973344,-10.0402769566905,3.8029340298805));
#47790=CARTESIAN_POINT('Ctrl Pts',(371.949557243748,-10.0344235930937,3.77335176839896));
#47791=CARTESIAN_POINT('Ctrl Pts',(372.060453152648,-10.028570229497,3.7387901807376));
#47792=CARTESIAN_POINT('Ctrl Pts',(372.169622845867,-10.0227168659003,3.69938502681498));
#47793=CARTESIAN_POINT('Ctrl Pts',(372.278776147624,-10.0168643811664,3.65998578944362));
#47794=CARTESIAN_POINT('Ctrl Pts',(372.386203360558,-10.0110118964325,3.61574457207803));
#47795=CARTESIAN_POINT('Ctrl Pts',(372.491452628727,-10.0051594116986,3.56684641326465));
#47796=CARTESIAN_POINT('Ctrl Pts',(372.59671154684,-9.99930639037042,3.51794377114663));
#47797=CARTESIAN_POINT('Ctrl Pts',(372.699791748524,-9.99345336904225,3.46438351287105));
#47798=CARTESIAN_POINT('Ctrl Pts',(372.800263780691,-9.98760034771409,3.40639774692813));
#47799=CARTESIAN_POINT('Ctrl Pts',(372.90076932222,-9.98174537429027,3.34839264161242));
#47800=CARTESIAN_POINT('Ctrl Pts',(372.99866460689,-9.97589040086647,3.28595930008741));
#47801=CARTESIAN_POINT('Ctrl Pts',(373.093547698998,-9.97003542744265,3.21937408574433));
#47802=CARTESIAN_POINT('Ctrl Pts',(373.188538328904,-9.96417381815851,3.1527134056134));
#47803=CARTESIAN_POINT('Ctrl Pts',(373.280509613871,-9.95831220887437,3.08189169799638));
#47804=CARTESIAN_POINT('Ctrl Pts',(373.369091282435,-9.95245059959023,3.00722673946687));
#47805=CARTESIAN_POINT('Ctrl Pts',(373.457732682269,-9.94658503777989,2.93251143380745));
#47806=CARTESIAN_POINT('Ctrl Pts',(373.542979611424,-9.94071947596956,2.85394799621234));
#47807=CARTESIAN_POINT('Ctrl Pts',(373.624498629115,-9.93485391415923,2.77189109415366));
#47808=CARTESIAN_POINT('Ctrl Pts',(373.706136847603,-9.92897977545891,2.68971420477846));
#47809=CARTESIAN_POINT('Ctrl Pts',(373.784035998702,-9.92310563675859,2.60403396056645));
#47810=CARTESIAN_POINT('Ctrl Pts',(373.857902826068,-9.91723149805827,2.51523814220289));
#47811=CARTESIAN_POINT('Ctrl Pts',(373.876582540825,-9.91574602427691,2.49278312934004));
#47812=CARTESIAN_POINT('Ctrl Pts',(373.895004605402,-9.91426055049554,2.4701290178639));
#47813=CARTESIAN_POINT('Ctrl Pts',(373.91316472549,-9.91277507671417,2.44728235746109));
#47814=CARTESIAN_POINT('Ctrl Pts',(373.984971381404,-9.90690138732361,2.35694472343385));
#47815=CARTESIAN_POINT('Ctrl Pts',(374.052918314477,-9.90102769793304,2.26329359404956));
#47816=CARTESIAN_POINT('Ctrl Pts',(374.116684511433,-9.89515400854247,2.16669289957718));
#47817=CARTESIAN_POINT('Ctrl Pts',(374.180368380238,-9.88928790263671,2.07021692567662));
#47818=CARTESIAN_POINT('Ctrl Pts',(374.239882021702,-9.88342179673096,1.9707993015303));
#47819=CARTESIAN_POINT('Ctrl Pts',(374.294944564018,-9.8775556908252,1.86883700962394));
#47820=CARTESIAN_POINT('Ctrl Pts',(374.349950722991,-9.87169559173716,1.76697912580552));
#47821=CARTESIAN_POINT('Ctrl Pts',(374.400514653648,-9.86583549264912,1.66258211855848));
#47822=CARTESIAN_POINT('Ctrl Pts',(374.446399092259,-9.85997539356108,1.55607137452421));
#47823=CARTESIAN_POINT('Ctrl Pts',(374.493938936736,-9.85390387546697,1.4457179658352));
#47824=CARTESIAN_POINT('Ctrl Pts',(374.536455014542,-9.84783235737286,1.33309580010779));
#47825=CARTESIAN_POINT('Ctrl Pts',(374.573735687013,-9.84176083927875,1.21870556917476));
#47826=CARTESIAN_POINT('Ctrl Pts',(374.60967683513,-9.835907475682,1.10842547065745));
#47827=CARTESIAN_POINT('Ctrl Pts',(374.640752188752,-9.83005411208525,0.996502602799251));
#47828=CARTESIAN_POINT('Ctrl Pts',(374.666821657699,-9.82420074848849,0.883404544185893));
#47829=CARTESIAN_POINT('Ctrl Pts',(374.692887212402,-9.81834826375459,0.770323466865458));
#47830=CARTESIAN_POINT('Ctrl Pts',(374.713948284152,-9.81249577902068,0.656067952120754));
#47831=CARTESIAN_POINT('Ctrl Pts',(374.729915406888,-9.80664329428677,0.541118009202179));
#47832=CARTESIAN_POINT('Ctrl Pts',(374.745883993595,-9.80079027295859,0.426157526917199));
#47833=CARTESIAN_POINT('Ctrl Pts',(374.756757645998,-9.79493725163042,0.310502899127331));
#47834=CARTESIAN_POINT('Ctrl Pts',(374.762498596077,-9.78908423030223,0.194640826852297));
#47835=CARTESIAN_POINT('Ctrl Pts',(374.768241460874,-9.78322925687841,0.078740112338653));
#47836=CARTESIAN_POINT('Ctrl Pts',(374.768848198966,-9.77737428345458,-0.0373677718189149));
#47837=CARTESIAN_POINT('Ctrl Pts',(374.764333147511,-9.77151931003076,-0.153195256672398));
#47838=CARTESIAN_POINT('Ctrl Pts',(374.759812978826,-9.7656577007466,-0.269154017102489));
#47839=CARTESIAN_POINT('Ctrl Pts',(374.750159450483,-9.75979609146244,-0.384831330863294));
#47840=CARTESIAN_POINT('Ctrl Pts',(374.735438864949,-9.75393448217828,-0.499743786234178));
#47841=CARTESIAN_POINT('Ctrl Pts',(374.720708353216,-9.74806892036794,-0.614733727917623));
#47842=CARTESIAN_POINT('Ctrl Pts',(374.70090405118,-9.74220335855759,-0.72895737817487));
#47843=CARTESIAN_POINT('Ctrl Pts',(374.676143227281,-9.73633779674725,-0.841942275486847));
#47844=CARTESIAN_POINT('Ctrl Pts',(374.651346196984,-9.73046365804691,-0.955092384430067));
#47845=CARTESIAN_POINT('Ctrl Pts',(374.621578286132,-9.72458951934657,-1.06699972768164));
#47846=CARTESIAN_POINT('Ctrl Pts',(374.587006372825,-9.71871538064623,-1.17720766003844));
#47847=CARTESIAN_POINT('Ctrl Pts',(374.578263700341,-9.71722990686499,-1.20507744697278));
#47848=CARTESIAN_POINT('Ctrl Pts',(374.569214049117,-9.71574443308375,-1.23283866169124));
#47849=CARTESIAN_POINT('Ctrl Pts',(374.559860594919,-9.71425895930251,-1.26048414500367));
#47850=CARTESIAN_POINT('Ctrl Pts',(374.522876243273,-9.70838526991194,-1.36979673205813));
#47851=CARTESIAN_POINT('Ctrl Pts',(374.481015143014,-9.70251158052137,-1.47766224106919));
#47852=CARTESIAN_POINT('Ctrl Pts',(374.434409083254,-9.6966378911308,-1.58361363200077));
#47853=CARTESIAN_POINT('Ctrl Pts',(374.387863196296,-9.69077178522504,-1.68942822973297));
#47854=CARTESIAN_POINT('Ctrl Pts',(374.336584697648,-9.68490567931928,-1.79333324928324));
#47855=CARTESIAN_POINT('Ctrl Pts',(374.28075491153,-9.67903957341352,-1.89487746388453));
#47856=CARTESIAN_POINT('Ctrl Pts',(374.224982294401,-9.67317947432548,-1.99631769850368));
#47857=CARTESIAN_POINT('Ctrl Pts',(374.164667857709,-9.66731937523744,-2.095401576769));
#47858=CARTESIAN_POINT('Ctrl Pts',(374.100040434264,-9.6614592761494,-2.19169911796409));
#47859=CARTESIAN_POINT('Ctrl Pts',(374.03308140082,-9.6553877580553,-2.29147085475558));
#47860=CARTESIAN_POINT('Ctrl Pts',(373.961492481339,-9.64931623996119,-2.38825099575935));
#47861=CARTESIAN_POINT('Ctrl Pts',(373.885579679766,-9.64324472186708,-2.48159026954188));
#47862=CARTESIAN_POINT('Ctrl Pts',(373.812394485822,-9.63739135827033,-2.57157578862253));
#47863=CARTESIAN_POINT('Ctrl Pts',(373.735191066436,-9.63153799467359,-2.65836310329154));
#47864=CARTESIAN_POINT('Ctrl Pts',(373.654286387342,-9.62568463107683,-2.74158101587052));
#47865=CARTESIAN_POINT('Ctrl Pts',(373.573393855814,-9.61983214634293,-2.82478643355997));
#47866=CARTESIAN_POINT('Ctrl Pts',(373.488801457496,-9.61397966160902,-2.90442321865074));
#47867=CARTESIAN_POINT('Ctrl Pts',(373.400864047524,-9.60812717687512,-2.98015597452925));
#47868=CARTESIAN_POINT('Ctrl Pts',(373.312918574873,-9.60227415554695,-3.05589567408463));
#47869=CARTESIAN_POINT('Ctrl Pts',(373.221627793962,-9.59642113421877,-3.12773036324287));
#47870=CARTESIAN_POINT('Ctrl Pts',(373.127380209077,-9.5905681128906,-3.19536445999062));
#47871=CARTESIAN_POINT('Ctrl Pts',(373.033101190801,-9.58471313946678,-3.26302111401576));
#47872=CARTESIAN_POINT('Ctrl Pts',(372.935863743112,-9.57885816604297,-3.32647414910033));
#47873=CARTESIAN_POINT('Ctrl Pts',(372.836085346331,-9.57300319261915,-3.38547129710759));
#47874=CARTESIAN_POINT('Ctrl Pts',(372.736193863554,-9.56714158333499,-3.44453531080426));
#47875=CARTESIAN_POINT('Ctrl Pts',(372.633756039528,-9.56127997405084,-3.49913314718231));
#47876=CARTESIAN_POINT('Ctrl Pts',(372.529214032112,-9.55541836476668,-3.54905845863237));
#47877=CARTESIAN_POINT('Ctrl Pts',(372.424601531253,-9.54955280295634,-3.59901743508659));
#47878=CARTESIAN_POINT('Ctrl Pts',(372.317882401114,-9.543687241146,-3.64429745186442));
#47879=CARTESIAN_POINT('Ctrl Pts',(372.209517227151,-9.53782167933565,-3.68474092467185));
#47880=CARTESIAN_POINT('Ctrl Pts',(372.100993596725,-9.53194754063532,-3.72524353575592));
#47881=CARTESIAN_POINT('Ctrl Pts',(371.990819510435,-9.52607340193499,-3.76089536180038));
#47882=CARTESIAN_POINT('Ctrl Pts',(371.879469157034,-9.52019926323466,-3.79158908007496));
#47883=CARTESIAN_POINT('Ctrl Pts',(371.851310470467,-9.51871378945339,-3.79935102034784));
#47884=CARTESIAN_POINT('Ctrl Pts',(371.823076601891,-9.51722831567212,-3.80679614594573));
#47885=CARTESIAN_POINT('Ctrl Pts',(371.794775288842,-9.51574284189085,-3.8139232444251));
#47886=CARTESIAN_POINT('Ctrl Pts',(371.682869495356,-9.50986915250028,-3.84210439662827));
#47887=CARTESIAN_POINT('Ctrl Pts',(371.5695359611,-9.50399546310971,-3.86540310393339));
#47888=CARTESIAN_POINT('Ctrl Pts',(371.455238587611,-9.49812177371915,-3.88367692291827));
#47889=CARTESIAN_POINT('Ctrl Pts',(371.34108878277,-9.49225566781339,-3.90192714868608));
#47890=CARTESIAN_POINT('Ctrl Pts',(371.22597801765,-9.48638956190764,-3.91516532321926));
#47891=CARTESIAN_POINT('Ctrl Pts',(371.11038375923,-9.48052345600188,-3.92329920035943));
#47892=CARTESIAN_POINT('Ctrl Pts',(370.994907867858,-9.47466335691384,-3.93142474851303));
#47893=CARTESIAN_POINT('Ctrl Pts',(370.878949877639,-9.4688032578258,-3.93445636685655));
#47894=CARTESIAN_POINT('Ctrl Pts',(370.762995157184,-9.46294315873777,-3.93235324875953));
#47895=CARTESIAN_POINT('Ctrl Pts',(370.642857054951,-9.45687164064366,-3.93017425495955));
#47896=CARTESIAN_POINT('Ctrl Pts',(370.522722908879,-9.45080012254955,-3.92248295906194));
#47897=CARTESIAN_POINT('Ctrl Pts',(370.403136132927,-9.44472860445545,-3.9092929442652));
#47898=CARTESIAN_POINT('Ctrl Pts',(370.287846205406,-9.4388752408587,-3.8965768572413));
#47899=CARTESIAN_POINT('Ctrl Pts',(370.173065435921,-9.43302187726194,-3.87875044681709));
#47900=CARTESIAN_POINT('Ctrl Pts',(370.059277574931,-9.4271685136652,-3.85587883199449));
#47901=CARTESIAN_POINT('Ctrl Pts',(369.945506798805,-9.42131602893129,-3.83301065126789));
#47902=CARTESIAN_POINT('Ctrl Pts',(369.83272903968,-9.41546354419739,-3.80509885377092));
#47903=CARTESIAN_POINT('Ctrl Pts',(369.721418504306,-9.40961105946348,-3.77225980536563));
#47904=CARTESIAN_POINT('Ctrl Pts',(369.61009776325,-9.4037580381353,-3.73941774606053));
#47905=CARTESIAN_POINT('Ctrl Pts',(369.500244909649,-9.39790501680713,-3.70164765469679));
#47906=CARTESIAN_POINT('Ctrl Pts',(369.392318935258,-9.39205199547895,-3.65911575665266));
#47907=CARTESIAN_POINT('Ctrl Pts',(369.284356965469,-9.38619702205512,-3.61656967339911));
#47908=CARTESIAN_POINT('Ctrl Pts',(369.178323536939,-9.38034204863129,-3.56925877688493));
#47909=CARTESIAN_POINT('Ctrl Pts',(369.074656952618,-9.37448707520746,-3.51739712214563));
#47910=CARTESIAN_POINT('Ctrl Pts',(368.970872875539,-9.36862546592331,-3.46547668888213));
#47911=CARTESIAN_POINT('Ctrl Pts',(368.869461366498,-9.36276385663915,-3.40899538788337));
#47912=CARTESIAN_POINT('Ctrl Pts',(368.770835518993,-9.35690224735499,-3.34821290486675));
#47913=CARTESIAN_POINT('Ctrl Pts',(368.672143167354,-9.35103668554464,-3.28738943577538));
#47914=CARTESIAN_POINT('Ctrl Pts',(368.576240558479,-9.34517112373429,-3.22225924102581));
#47915=CARTESIAN_POINT('Ctrl Pts',(368.483509799443,-9.33930556192394,-3.15312392624795));
#47916=CARTESIAN_POINT('Ctrl Pts',(368.390643445294,-9.33343142322361,-3.08388751868344));
#47917=CARTESIAN_POINT('Ctrl Pts',(368.300958516057,-9.32755728452328,-3.0106345633989));
#47918=CARTESIAN_POINT('Ctrl Pts',(368.214802258098,-9.32168314582295,-2.9337053442518));
#47919=CARTESIAN_POINT('Ctrl Pts',(368.193014746972,-9.3201976720417,-2.91425120060883));
#47920=CARTESIAN_POINT('Ctrl Pts',(368.171452700821,-9.31871219826044,-2.89456213268467));
#47921=CARTESIAN_POINT('Ctrl Pts',(368.150121333064,-9.31722672447919,-2.87464398511513));
#47922=CARTESIAN_POINT('Ctrl Pts',(368.067026222552,-9.31144014719931,-2.79705399218618));
#47923=CARTESIAN_POINT('Ctrl Pts',(367.987139937561,-9.30565356991942,-2.71571004166305));
#47924=CARTESIAN_POINT('Ctrl Pts',(367.910828487414,-9.29986699263954,-2.63091218553541));
#47925=CARTESIAN_POINT('Ctrl Pts',(367.83076645626,-9.29379601469888,-2.54194665564336));
#47926=CARTESIAN_POINT('Ctrl Pts',(367.754640001564,-9.28772503675821,-2.44917930045951));
#47927=CARTESIAN_POINT('Ctrl Pts',(367.682832597279,-9.28165405881755,-2.35300439471732));
#47928=CARTESIAN_POINT('Ctrl Pts',(367.614559204841,-9.27588186493941,-2.26156275095226));
#47929=CARTESIAN_POINT('Ctrl Pts',(367.550190192005,-9.27010967106127,-2.1670413479476));
#47930=CARTESIAN_POINT('Ctrl Pts',(367.490016455998,-9.26433747718313,-2.06981573201827));
#47931=CARTESIAN_POINT('Ctrl Pts',(367.429879896641,-9.25856884949261,-1.97265018420083));
#47932=CARTESIAN_POINT('Ctrl Pts',(367.373933687928,-9.25280022180208,-1.87278410441214));
#47933=CARTESIAN_POINT('Ctrl Pts',(367.32242625392,-9.24703159411156,-1.77062316564955));
#47934=CARTESIAN_POINT('Ctrl Pts',(367.270937320453,-9.24126503840821,-1.6684989212562));
#47935=CARTESIAN_POINT('Ctrl Pts',(367.223884184249,-9.23549848270486,-1.56408183673553));
#47936=CARTESIAN_POINT('Ctrl Pts',(367.181469579154,-9.22973192700151,-1.45780262265575));
#47937=CARTESIAN_POINT('Ctrl Pts',(367.139059240161,-9.22396595130408,-1.35153409824537));
#47938=CARTESIAN_POINT('Ctrl Pts',(367.101286660911,-9.21819997560666,-1.24340421338312));
#47939=CARTESIAN_POINT('Ctrl Pts',(367.068306294295,-9.21243399990924,-1.13386328012323));
#47940=CARTESIAN_POINT('Ctrl Pts',(367.035307369128,-9.20666477961016,-1.024260706525));
#47941=CARTESIAN_POINT('Ctrl Pts',(367.007106164992,-9.20089555931108,-0.913245907654856));
#47942=CARTESIAN_POINT('Ctrl Pts',(366.983807043069,-9.19512633901201,-0.801283658189311));
#47943=CARTESIAN_POINT('Ctrl Pts',(366.9605002699,-9.18935522414678,-0.689284641209677));
#47944=CARTESIAN_POINT('Ctrl Pts',(366.942098854974,-9.18358410928155,-0.576337974633217));
#47945=CARTESIAN_POINT('Ctrl Pts',(366.928655620417,-9.17781299441632,-0.462916324213755));
#47946=CARTESIAN_POINT('Ctrl Pts',(366.915198115606,-9.17203575340115,-0.349374274520911));
#47947=CARTESIAN_POINT('Ctrl Pts',(366.906709328686,-9.16625851238598,-0.235356659343858));
#47948=CARTESIAN_POINT('Ctrl Pts',(366.903190035608,-9.16048127137082,-0.121338705950509));
#47949=CARTESIAN_POINT('Ctrl Pts',(366.901907185002,-9.15837535493508,-0.079776949847682));
#47950=CARTESIAN_POINT('Ctrl Pts',(366.901284152064,-9.15626943849936,-0.0382151271236437));
#47951=CARTESIAN_POINT('Ctrl Pts',(366.901319257773,-9.15416352206362,0.00332388066085588));
#47952=CARTESIAN_POINT('',(366.901318679092,-7.90416352198934,-0.00254877927961847));
#47953=CARTESIAN_POINT('Ctrl Pts',(366.901319257774,-9.15416352203497,0.00332388122593332));
#47954=CARTESIAN_POINT('Ctrl Pts',(366.901468264492,-9.14522492907225,0.179636804359732));
#47955=CARTESIAN_POINT('Ctrl Pts',(366.9134762834,-9.13628633610951,0.355464946286474));
#47956=CARTESIAN_POINT('Ctrl Pts',(366.937130866369,-9.12734774314678,0.529549421191803));
#47957=CARTESIAN_POINT('Ctrl Pts',(366.94474980792,-9.12446869778703,0.585620561445061));
#47958=CARTESIAN_POINT('Ctrl Pts',(366.953576681388,-9.12158965242729,0.641511085305567));
#47959=CARTESIAN_POINT('Ctrl Pts',(366.963603491617,-9.11871060706754,0.697179554237403));
#47960=CARTESIAN_POINT('Ctrl Pts',(366.984059705919,-9.11283691767697,0.810751677804974));
#47961=CARTESIAN_POINT('Ctrl Pts',(367.009552771227,-9.10696322828641,0.923611871718653));
#47962=CARTESIAN_POINT('Ctrl Pts',(367.040021228329,-9.10108953889585,1.03527876550764));
#47963=CARTESIAN_POINT('Ctrl Pts',(367.070450347791,-9.09522343299009,1.14680148684608));
#47964=CARTESIAN_POINT('Ctrl Pts',(367.10584197666,-9.08935732708435,1.25713357699809));
#47965=CARTESIAN_POINT('Ctrl Pts',(367.146083329971,-9.08349122117859,1.36580199936962));
#47966=CARTESIAN_POINT('Ctrl Pts',(367.186283476648,-9.07763112209055,1.47435914666115));
#47967=CARTESIAN_POINT('Ctrl Pts',(367.231323327252,-9.07177102300251,1.58125562959267));
#47968=CARTESIAN_POINT('Ctrl Pts',(367.281039974081,-9.06591092391447,1.68603241771641));
#47969=CARTESIAN_POINT('Ctrl Pts',(367.332550284105,-9.05983940582036,1.79458931332146));
#47970=CARTESIAN_POINT('Ctrl Pts',(367.389081099068,-9.05376788772626,1.90087024314777));
#47971=CARTESIAN_POINT('Ctrl Pts',(367.450396029607,-9.04769636963215,2.00438571429015));
#47972=CARTESIAN_POINT('Ctrl Pts',(367.509507865691,-9.0418430060354,2.10418179182689));
#47973=CARTESIAN_POINT('Ctrl Pts',(367.573065711195,-9.03598964243865,2.20140733490711));
#47974=CARTESIAN_POINT('Ctrl Pts',(367.640810818989,-9.0301362788419,2.2956484535508));
#47975=CARTESIAN_POINT('Ctrl Pts',(367.708545755083,-9.02428379410799,2.3898754222077));
#47976=CARTESIAN_POINT('Ctrl Pts',(367.780466462285,-9.01843130937409,2.48111852204744));
#47977=CARTESIAN_POINT('Ctrl Pts',(367.856271437838,-9.01257882464019,2.56899368387861));
#47978=CARTESIAN_POINT('Ctrl Pts',(367.93208336369,-9.00672580331202,2.65687690268219));
#47979=CARTESIAN_POINT('Ctrl Pts',(368.011779995979,-9.00087278198384,2.74139125677391));
#47980=CARTESIAN_POINT('Ctrl Pts',(368.095020678199,-8.99501976065567,2.82218709282411));
#47981=CARTESIAN_POINT('Ctrl Pts',(368.178289122796,-8.98916478723183,2.90300987584619));
#47982=CARTESIAN_POINT('Ctrl Pts',(368.265103671397,-8.983309813808,2.98011138715295));
#47983=CARTESIAN_POINT('Ctrl Pts',(368.355088619603,-8.97745484038416,3.05318053956148));
#47984=CARTESIAN_POINT('Ctrl Pts',(368.445175554188,-8.97159323110001,3.12633250646872));
#47985=CARTESIAN_POINT('Ctrl Pts',(368.538439739366,-8.96573162181585,3.19544273213369));
#47986=CARTESIAN_POINT('Ctrl Pts',(368.634474289843,-8.95987001253169,3.26024190768866));
#47987=CARTESIAN_POINT('Ctrl Pts',(368.730573597122,-8.95400445072135,3.3250847778036));
#47988=CARTESIAN_POINT('Ctrl Pts',(368.829446637963,-8.948138888911,3.38561059421203));
#47989=CARTESIAN_POINT('Ctrl Pts',(368.930661108447,-8.94227332710066,3.44159555992084));
#47990=CARTESIAN_POINT('Ctrl Pts',(369.032023579312,-8.93639918840032,3.49766238938069));
#47991=CARTESIAN_POINT('Ctrl Pts',(369.135733944158,-8.93052504969999,3.54917493361567));
#47992=CARTESIAN_POINT('Ctrl Pts',(369.241339030983,-8.92465091099966,3.59595710095255));
#47993=CARTESIAN_POINT('Ctrl Pts',(369.268044833424,-8.9231654372184,3.60778754734726));
#47994=CARTESIAN_POINT('Ctrl Pts',(369.294871725698,-8.92167996343715,3.61931573371251));
#47995=CARTESIAN_POINT('Ctrl Pts',(369.321812233735,-8.92019448965589,3.63053931957986));
#47996=CARTESIAN_POINT('Ctrl Pts',(369.428337288725,-8.91432080026535,3.67491833054907));
#47997=CARTESIAN_POINT('Ctrl Pts',(369.536994628475,-8.9084471108748,3.71467889225625));
#47998=CARTESIAN_POINT('Ctrl Pts',(369.64734643598,-8.90257342148426,3.74961169384846));
#47999=CARTESIAN_POINT('Ctrl Pts',(369.757555768934,-8.89670731557853,3.78449939391202));
#48000=CARTESIAN_POINT('Ctrl Pts',(369.869454828706,-8.8908412096728,3.81457160588909));
#48001=CARTESIAN_POINT('Ctrl Pts',(369.982584977134,-8.88497510376707,3.83966666623377));
#48002=CARTESIAN_POINT('Ctrl Pts',(370.09559928173,-8.87911500467905,3.86473602955636));
#48003=CARTESIAN_POINT('Ctrl Pts',(370.209841766562,-8.87325490559103,3.8848382897476));
#48004=CARTESIAN_POINT('Ctrl Pts',(370.324838390928,-8.86739480650302,3.89986149465579));
#48005=CARTESIAN_POINT('Ctrl Pts',(370.443983831153,-8.8613232884089,3.91542670252374));
#48006=CARTESIAN_POINT('Ctrl Pts',(370.563938422951,-8.85525177031479,3.92553931799925));
#48007=CARTESIAN_POINT('Ctrl Pts',(370.684162692671,-8.84918025222068,3.93013262215912));
#48008=CARTESIAN_POINT('Ctrl Pts',(370.800067208299,-8.84332688862395,3.93456088522963));
#48009=CARTESIAN_POINT('Ctrl Pts',(370.916221907645,-8.83747352502722,3.93385962051807));
#48010=CARTESIAN_POINT('Ctrl Pts',(371.032138726429,-8.8316201614305,3.92802188157401));
#48011=CARTESIAN_POINT('Ctrl Pts',(371.148038140694,-8.82576767669662,3.92218501914681));
#48012=CARTESIAN_POINT('Ctrl Pts',(371.263699332905,-8.81991519196274,3.9112132367454));
#48013=CARTESIAN_POINT('Ctrl Pts',(371.378636119195,-8.81406270722886,3.89515168194138));
#48014=CARTESIAN_POINT('Ctrl Pts',(371.493583443644,-8.80820968590071,3.87908865450844));
#48015=CARTESIAN_POINT('Ctrl Pts',(371.607805820948,-8.80235666457257,3.85793498417039));
#48016=CARTESIAN_POINT('Ctrl Pts',(371.720824761537,-8.79650364324442,3.83178737686651));
#48017=CARTESIAN_POINT('Ctrl Pts',(371.833881396125,-8.79064866982062,3.80563104883061));
#48018=CARTESIAN_POINT('Ctrl Pts',(371.945733393598,-8.78479369639682,3.77447756498198));
#48019=CARTESIAN_POINT('Ctrl Pts',(372.055915672024,-8.77893872297303,3.7384739893574));
#48020=CARTESIAN_POINT('Ctrl Pts',(372.166222827911,-8.7730771136889,3.70242960830435));
#48021=CARTESIAN_POINT('Ctrl Pts',(372.274856094681,-8.76721550440477,3.66152429227753));
#48022=CARTESIAN_POINT('Ctrl Pts',(372.38136859359,-8.76135389512064,3.61595395528367));
#48023=CARTESIAN_POINT('Ctrl Pts',(372.48795291466,-8.75548833331032,3.5703528898769));
#48024=CARTESIAN_POINT('Ctrl Pts',(372.592413248969,-8.7496227715,3.52008071851767));
#48025=CARTESIAN_POINT('Ctrl Pts',(372.694327182081,-8.74375720968968,3.4653793871041));
#48026=CARTESIAN_POINT('Ctrl Pts',(372.796390138358,-8.73788307098938,3.41059806892765));
#48027=CARTESIAN_POINT('Ctrl Pts',(372.895898908682,-8.73200893228908,3.35137487567747));
#48028=CARTESIAN_POINT('Ctrl Pts',(372.992459852983,-8.72613479358878,3.28799515037324));
#48029=CARTESIAN_POINT('Ctrl Pts',(373.016878539431,-8.72464931980726,3.27196745252298));
#48030=CARTESIAN_POINT('Ctrl Pts',(373.041108878354,-8.72316384602574,3.25567414389969));
#48031=CARTESIAN_POINT('Ctrl Pts',(373.065144851275,-8.72167837224423,3.2391202362318));
#48032=CARTESIAN_POINT('Ctrl Pts',(373.160185127915,-8.71580468285365,3.17366468053539));
#48033=CARTESIAN_POINT('Ctrl Pts',(373.252500417247,-8.70993099346308,3.10391364395067));
#48034=CARTESIAN_POINT('Ctrl Pts',(373.341677488955,-8.7040573040725,3.03012155814021));
#48035=CARTESIAN_POINT('Ctrl Pts',(373.430739424686,-8.69819119816673,2.95642474484502));
#48036=CARTESIAN_POINT('Ctrl Pts',(373.516670884969,-8.69232509226097,2.87869751895253));
#48037=CARTESIAN_POINT('Ctrl Pts',(373.599087390548,-8.68645898635521,2.79723763836516));
#48038=CARTESIAN_POINT('Ctrl Pts',(373.681419502674,-8.68059888726716,2.71586117165772));
#48039=CARTESIAN_POINT('Ctrl Pts',(373.760243527249,-8.67473878817911,2.6307599416109));
#48040=CARTESIAN_POINT('Ctrl Pts',(373.835208408026,-8.66887868909106,2.54227159802004));
#48041=CARTESIAN_POINT('Ctrl Pts',(373.91287785068,-8.66280717099696,2.4505907968669));
#48042=CARTESIAN_POINT('Ctrl Pts',(373.986404085922,-8.65673565290285,2.35527415710136));
#48043=CARTESIAN_POINT('Ctrl Pts',(374.055438595521,-8.65066413480875,2.25673883370292));
#48044=CARTESIAN_POINT('Ctrl Pts',(374.12199264002,-8.64481077121198,2.1617439632214));
#48045=CARTESIAN_POINT('Ctrl Pts',(374.184371929043,-8.63895740761523,2.06375809560105));
#48046=CARTESIAN_POINT('Ctrl Pts',(374.242306041148,-8.63310404401846,1.96318758934822));
#48047=CARTESIAN_POINT('Ctrl Pts',(374.30023145464,-8.62725155928455,1.86263218341846));
#48048=CARTESIAN_POINT('Ctrl Pts',(374.353712812143,-8.62139907455064,1.75949326839322));
#48049=CARTESIAN_POINT('Ctrl Pts',(374.402524486615,-8.61554658981672,1.65420386331987));
#48050=CARTESIAN_POINT('Ctrl Pts',(374.451340636463,-8.60969356848854,1.54890480462174));
#48051=CARTESIAN_POINT('Ctrl Pts',(374.495486078387,-8.60384054716035,1.4414552387634));
#48052=CARTESIAN_POINT('Ctrl Pts',(374.534782681401,-8.59798752583217,1.33230966949345));
#48053=CARTESIAN_POINT('Ctrl Pts',(374.574092390591,-8.59213255240833,1.22312769806832));
#48054=CARTESIAN_POINT('Ctrl Pts',(374.6085499053,-8.58627757898449,1.11224898697031));
#48055=CARTESIAN_POINT('Ctrl Pts',(374.638026679255,-8.58042260556066,1.00014407300846));
#48056=CARTESIAN_POINT('Ctrl Pts',(374.667536861347,-8.57456099627649,0.887912102526002));
#48057=CARTESIAN_POINT('Ctrl Pts',(374.692054930424,-8.56869938699233,0.774451555122436));
#48058=CARTESIAN_POINT('Ctrl Pts',(374.711503257349,-8.56283777770817,0.660244153358279));
#48059=CARTESIAN_POINT('Ctrl Pts',(374.730964698422,-8.55697221589781,0.545959740704368));
#48060=CARTESIAN_POINT('Ctrl Pts',(374.745349539085,-8.55110665408746,0.430927879829411));
#48061=CARTESIAN_POINT('Ctrl Pts',(374.754632093489,-8.54524109227711,0.315634690071573));
#48062=CARTESIAN_POINT('Ctrl Pts',(374.763928221264,-8.53936695357677,0.200172913392809));
#48063=CARTESIAN_POINT('Ctrl Pts',(374.76810715806,-8.53349281487642,0.0844494564905184));
#48064=CARTESIAN_POINT('Ctrl Pts',(374.76719528383,-8.52761867617608,-0.0310502146323147));
#48065=CARTESIAN_POINT('Ctrl Pts',(374.766964685724,-8.52613320239491,-0.0602581959107494));
#48066=CARTESIAN_POINT('Ctrl Pts',(374.766408787816,-8.52464772861374,-0.0894518974122133));
#48067=CARTESIAN_POINT('Ctrl Pts',(374.765528538828,-8.52316225483257,-0.11862354485694));
#48068=CARTESIAN_POINT('Ctrl Pts',(374.762047959628,-8.51728856544201,-0.233970714408904));
#48069=CARTESIAN_POINT('Ctrl Pts',(374.753480612594,-8.51141487605144,-0.349356676786575));
#48070=CARTESIAN_POINT('Ctrl Pts',(374.739816282563,-8.50554118666087,-0.464296261488693));
#48071=CARTESIAN_POINT('Ctrl Pts',(374.726169594465,-8.49967508075512,-0.579087448388813));
#48072=CARTESIAN_POINT('Ctrl Pts',(374.707439058521,-8.49380897484937,-0.693432997206952));
#48073=CARTESIAN_POINT('Ctrl Pts',(374.683666453169,-8.48794286894362,-0.806848409615465));
#48074=CARTESIAN_POINT('Ctrl Pts',(374.659918190663,-8.48208276985558,-0.920147686086541));
#48075=CARTESIAN_POINT('Ctrl Pts',(374.631138212665,-8.47622267076755,-1.03251831869128));
#48076=CARTESIAN_POINT('Ctrl Pts',(374.597419938021,-8.47036257167951,-1.14348226894711));
#48077=CARTESIAN_POINT('Ctrl Pts',(374.562485184951,-8.4642910535854,-1.2584495453789));
#48078=CARTESIAN_POINT('Ctrl Pts',(374.522249136021,-8.4582195354913,-1.37190627480284));
#48079=CARTESIAN_POINT('Ctrl Pts',(374.476873394784,-8.45214801739719,-1.48333345093183));
#48080=CARTESIAN_POINT('Ctrl Pts',(374.433128040193,-8.44629465380044,-1.59075695957209));
#48081=CARTESIAN_POINT('Ctrl Pts',(374.384606152586,-8.44044129020369,-1.69629383642295));
#48082=CARTESIAN_POINT('Ctrl Pts',(374.331502600168,-8.43458792660694,-1.79949655341166));
#48083=CARTESIAN_POINT('Ctrl Pts',(374.27840702107,-8.42873544187304,-1.90268377485972));
#48084=CARTESIAN_POINT('Ctrl Pts',(374.220731333986,-8.42288295713914,-2.00353716603838));
#48085=CARTESIAN_POINT('Ctrl Pts',(374.158717093655,-8.41703047240523,-2.10163238703123));
#48086=CARTESIAN_POINT('Ctrl Pts',(374.096697167452,-8.41117745107706,-2.19973660203876));
#48087=CARTESIAN_POINT('Ctrl Pts',(374.030338118017,-8.40532442974889,-2.29508179491122));
#48088=CARTESIAN_POINT('Ctrl Pts',(373.959925301916,-8.39947140842071,-2.38727188997809));
#48089=CARTESIAN_POINT('Ctrl Pts',(373.889489001781,-8.39361643499689,-2.47949273222214));
#48090=CARTESIAN_POINT('Ctrl Pts',(373.814996497208,-8.38776146157306,-2.56855605608216));
#48091=CARTESIAN_POINT('Ctrl Pts',(373.73677349781,-8.38190648814923,-2.65409876063602));
#48092=CARTESIAN_POINT('Ctrl Pts',(373.65846184269,-8.37604487886508,-2.73973841685784));
#48093=CARTESIAN_POINT('Ctrl Pts',(373.576411532798,-8.37018326958093,-2.82184918457374));
#48094=CARTESIAN_POINT('Ctrl Pts',(373.490985279885,-8.36432166029678,-2.90010468502701));
#48095=CARTESIAN_POINT('Ctrl Pts',(373.405501423424,-8.35845609848644,-2.97841295373893));
#48096=CARTESIAN_POINT('Ctrl Pts',(373.31663740699,-8.3525905366761,-3.05286051407759));
#48097=CARTESIAN_POINT('Ctrl Pts',(373.224787795936,-8.34672497486576,-3.12316225210772));
#48098=CARTESIAN_POINT('Ctrl Pts',(373.132803878223,-8.34085083616543,-3.19356678852152));
#48099=CARTESIAN_POINT('Ctrl Pts',(373.037825990666,-8.3349766974651,-3.25981316853759));
#48100=CARTESIAN_POINT('Ctrl Pts',(372.940276374979,-8.32910255876476,-3.32166038370065));
#48101=CARTESIAN_POINT('Ctrl Pts',(372.915607669681,-8.32761708498348,-3.33730053475203));
#48102=CARTESIAN_POINT('Ctrl Pts',(372.890774615676,-8.3261316112022,-3.35265959262464));
#48103=CARTESIAN_POINT('Ctrl Pts',(372.865784260062,-8.32464613742092,-3.36773414002491));
#48104=CARTESIAN_POINT('Ctrl Pts',(372.766970273246,-8.31877244803035,-3.42734017969275));
#48105=CARTESIAN_POINT('Ctrl Pts',(372.665366103292,-8.31289875863979,-3.48269279839185));
#48106=CARTESIAN_POINT('Ctrl Pts',(372.561373905041,-8.30702506924922,-3.53352039669837));
#48107=CARTESIAN_POINT('Ctrl Pts',(372.457515970487,-8.30115896334346,-3.58428237180044));
#48108=CARTESIAN_POINT('Ctrl Pts',(372.35127650684,-8.2952928574377,-3.6305307650198));
#48109=CARTESIAN_POINT('Ctrl Pts',(372.243085290337,-8.28942675153194,-3.67203803195589));
#48110=CARTESIAN_POINT('Ctrl Pts',(372.135004860261,-8.2835666524439,-3.71350279597942));
#48111=CARTESIAN_POINT('Ctrl Pts',(372.024977036089,-8.27770655335586,-3.750235943319));
#48112=CARTESIAN_POINT('Ctrl Pts',(371.913454160552,-8.27184645426782,-3.78205682535393));
#48113=CARTESIAN_POINT('Ctrl Pts',(371.797907794091,-8.26577493617372,-3.8150257322176));
#48114=CARTESIAN_POINT('Ctrl Pts',(371.680756869227,-8.25970341807961,-3.84272103666929));
#48115=CARTESIAN_POINT('Ctrl Pts',(371.56252511784,-8.2536318999855,-3.86499717719948));
#48116=CARTESIAN_POINT('Ctrl Pts',(371.448541527769,-8.24777853638875,-3.88647291819778));
#48117=CARTESIAN_POINT('Ctrl Pts',(371.333553885218,-8.241925172792,-3.90291213998364));
#48118=CARTESIAN_POINT('Ctrl Pts',(371.218043891446,-8.23607180919525,-3.91423598261404));
#48119=CARTESIAN_POINT('Ctrl Pts',(371.10255124111,-8.23021932446134,-3.92555812500758));
#48120=CARTESIAN_POINT('Ctrl Pts',(370.986536806563,-8.22436683972744,-3.93176637513341));
#48121=CARTESIAN_POINT('Ctrl Pts',(370.870488113088,-8.21851435499353,-3.9328336746297));
#48122=CARTESIAN_POINT('Ctrl Pts',(370.754428779506,-8.21266133366535,-3.93390107198302));
#48123=CARTESIAN_POINT('Ctrl Pts',(370.638335593902,-8.20680831233718,-3.92982657789512));
#48124=CARTESIAN_POINT('Ctrl Pts',(370.522696076278,-8.200955291009,-3.92063526333846));
#48125=CARTESIAN_POINT('Ctrl Pts',(370.407017990641,-8.19510031758518,-3.91144088330089));
#48126=CARTESIAN_POINT('Ctrl Pts',(370.291794285475,-8.18924534416136,-3.89712632209612));
#48127=CARTESIAN_POINT('Ctrl Pts',(370.177506647615,-8.18339037073754,-3.87776843560651));
#48128=CARTESIAN_POINT('Ctrl Pts',(370.063089479396,-8.17752876145338,-3.85838860943898));
#48129=CARTESIAN_POINT('Ctrl Pts',(369.949610903571,-8.17166715216923,-3.83395411830563));
#48130=CARTESIAN_POINT('Ctrl Pts',(369.837541808259,-8.16580554288508,-3.80459281871059));
#48131=CARTESIAN_POINT('Ctrl Pts',(369.725397143934,-8.15993998107473,-3.77521172057556));
#48132=CARTESIAN_POINT('Ctrl Pts',(369.61466424628,-8.15407441926437,-3.74089732076272));
#48133=CARTESIAN_POINT('Ctrl Pts',(369.505796596407,-8.14820885745402,-3.70182661265816));
#48134=CARTESIAN_POINT('Ctrl Pts',(369.396769755327,-8.14233471875369,-3.66269877359569));
#48135=CARTESIAN_POINT('Ctrl Pts',(369.289613986171,-8.13646058005336,-3.61880090204676));
#48136=CARTESIAN_POINT('Ctrl Pts',(369.184760711482,-8.13058644135303,-3.57035715806267));
#48137=CARTESIAN_POINT('Ctrl Pts',(369.158245030057,-8.12910096757177,-3.55810652605933));
#48138=CARTESIAN_POINT('Ctrl Pts',(369.131876458437,-8.12761549379052,-3.5455654072616));
#48139=CARTESIAN_POINT('Ctrl Pts',(369.105661688502,-8.12613002000926,-3.53273787085453));
#48140=CARTESIAN_POINT('Ctrl Pts',(369.002006263555,-8.1202563306187,-3.4820167033375));
#48141=CARTESIAN_POINT('Ctrl Pts',(368.900412436809,-8.11438264122813,-3.4266451030718));
#48142=CARTESIAN_POINT('Ctrl Pts',(368.801326447354,-8.10850895183756,-3.366813767297));
#48143=CARTESIAN_POINT('Ctrl Pts',(368.702368387222,-8.10264284593182,-3.30705967939769));
#48144=CARTESIAN_POINT('Ctrl Pts',(368.605912075792,-8.09677674002607,-3.24285751824571));
#48145=CARTESIAN_POINT('Ctrl Pts',(368.512381706195,-8.09091063412032,-3.17444507420126));
#48146=CARTESIAN_POINT('Ctrl Pts',(368.418947110506,-8.08505053503229,-3.10610268362794));
#48147=CARTESIAN_POINT('Ctrl Pts',(368.328432828584,-8.07919043594426,-3.03355882810736));
#48148=CARTESIAN_POINT('Ctrl Pts',(368.241235880182,-8.07333033685623,-2.95709568345119));
#48149=CARTESIAN_POINT('Ctrl Pts',(368.15089306481,-8.06725881876212,-2.87787392297609));
#48150=CARTESIAN_POINT('Ctrl Pts',(368.064111852556,-8.06118730066801,-2.79444496945922));
#48151=CARTESIAN_POINT('Ctrl Pts',(367.981298479933,-8.0551157825739,-2.70717000863017));
#48152=CARTESIAN_POINT('Ctrl Pts',(367.901460657971,-8.04926241897715,-2.62303090689219));
#48153=CARTESIAN_POINT('Ctrl Pts',(367.825310756227,-8.04340905538041,-2.53531774700873));
#48154=CARTESIAN_POINT('Ctrl Pts',(367.753176176164,-8.03755569178366,-2.44439255560225));
#48155=CARTESIAN_POINT('Ctrl Pts',(367.681052426865,-8.03170320704976,-2.35348101630726));
#48156=CARTESIAN_POINT('Ctrl Pts',(367.612943057185,-8.02585072231586,-2.25935872800847));
#48157=CARTESIAN_POINT('Ctrl Pts',(367.54913509657,-8.01999823758195,-2.16242069343169));
#48158=CARTESIAN_POINT('Ctrl Pts',(367.485321285622,-8.01414521625378,-2.06547377093875));
#48159=CARTESIAN_POINT('Ctrl Pts',(367.425809894898,-8.00829219492561,-1.96571093407117));
#48160=CARTESIAN_POINT('Ctrl Pts',(367.370844146293,-8.00243917359744,-1.86355544092471));
#48161=CARTESIAN_POINT('Ctrl Pts',(367.31586006555,-7.99658420017363,-1.76136587694856));
#48162=CARTESIAN_POINT('Ctrl Pts',(367.265424837196,-7.99072922674982,-1.65678243353877));
#48163=CARTESIAN_POINT('Ctrl Pts',(367.219735005643,-7.98487425332601,-1.5502515402271));
#48164=CARTESIAN_POINT('Ctrl Pts',(367.173993390536,-7.97901264404186,-1.44359990783109));
#48165=CARTESIAN_POINT('Ctrl Pts',(367.133008069927,-7.97315103475771,-1.33499680003515));
#48166=CARTESIAN_POINT('Ctrl Pts',(367.096926877922,-7.96728942547356,-1.22490722004983));
#48167=CARTESIAN_POINT('Ctrl Pts',(367.060821356105,-7.96142386366322,-1.11474340585235));
#48168=CARTESIAN_POINT('Ctrl Pts',(367.02962665854,-7.95555830185289,-1.00309152050772));
#48169=CARTESIAN_POINT('Ctrl Pts',(367.003439892718,-7.94969274004256,-0.89042857754718));
#48170=CARTESIAN_POINT('Ctrl Pts',(366.977214835422,-7.94381860134222,-0.777600893731445));
#48171=CARTESIAN_POINT('Ctrl Pts',(366.956012399741,-7.93794446264189,-0.663759606355969));
#48172=CARTESIAN_POINT('Ctrl Pts',(366.93987810049,-7.93207032394156,-0.549388762467624));
#48173=CARTESIAN_POINT('Ctrl Pts',(366.935797999604,-7.93058485016024,-0.520466243165588));
#48174=CARTESIAN_POINT('Ctrl Pts',(366.932041746676,-7.92909937637892,-0.491509865734178));
#48175=CARTESIAN_POINT('Ctrl Pts',(366.928609550068,-7.9276139025976,-0.462527459354826));
#48176=CARTESIAN_POINT('Ctrl Pts',(366.910548798985,-7.91979710907673,-0.310017540125761));
#48177=CARTESIAN_POINT('Ctrl Pts',(366.901418401507,-7.91198031555585,-0.156429518548803));
#48178=CARTESIAN_POINT('Ctrl Pts',(366.901318679092,-7.90416352203497,-0.00254878017787867));
#48179=CARTESIAN_POINT('',(366.901318248747,-6.65416352207208,-0.00176385594813664));
#48180=CARTESIAN_POINT('Ctrl Pts',(366.901318679092,-7.90416352198934,-0.00254877927963419));
#48181=CARTESIAN_POINT('Ctrl Pts',(366.901244822297,-7.89837421657266,0.11141899917109));
#48182=CARTESIAN_POINT('Ctrl Pts',(366.90612887188,-7.89258491115597,0.225581876613283));
#48183=CARTESIAN_POINT('Ctrl Pts',(366.915995242575,-7.88679560573928,0.339465637256839));
#48184=CARTESIAN_POINT('Ctrl Pts',(366.92585045942,-7.88101284508428,0.453220653255002));
#48185=CARTESIAN_POINT('Ctrl Pts',(366.940676765202,-7.87523008442928,0.566696759134401));
#48186=CARTESIAN_POINT('Ctrl Pts',(366.960446549786,-7.86944732377427,0.679418960879135));
#48187=CARTESIAN_POINT('Ctrl Pts',(366.980439020439,-7.86359942633309,0.793410861024053));
#48188=CARTESIAN_POINT('Ctrl Pts',(367.005487042511,-7.85775152889191,0.906631326792071));
#48189=CARTESIAN_POINT('Ctrl Pts',(367.035507950599,-7.85190363145073,1.01859330633901));
#48190=CARTESIAN_POINT('Ctrl Pts',(367.06515506273,-7.84612854727743,1.12916122627897));
#48191=CARTESIAN_POINT('Ctrl Pts',(367.099651809084,-7.84035346310412,1.23850140015343));
#48192=CARTESIAN_POINT('Ctrl Pts',(367.138867230103,-7.83457837893082,1.3461551515598));
#48193=CARTESIAN_POINT('Ctrl Pts',(367.178074621549,-7.82880447723762,1.4537868602711));
#48194=CARTESIAN_POINT('Ctrl Pts',(367.221998622053,-7.82303057554442,1.55973243314473));
#48195=CARTESIAN_POINT('Ctrl Pts',(367.270458937297,-7.81725667385122,1.66355000747509));
#48196=CARTESIAN_POINT('Ctrl Pts',(367.318921802855,-7.81148246829584,1.76737304539593));
#48197=CARTESIAN_POINT('Ctrl Pts',(367.371921276813,-7.80570826274047,1.86906747704612));
#48198=CARTESIAN_POINT('Ctrl Pts',(367.429229990094,-7.79993405718509,1.96821382079431));
#48199=CARTESIAN_POINT('Ctrl Pts',(367.487817207028,-7.7940310345185,2.06957202649772));
#48200=CARTESIAN_POINT('Ctrl Pts',(367.55090799828,-7.7881280118519,2.16826669130543));
#48201=CARTESIAN_POINT('Ctrl Pts',(367.618212020707,-7.78222498918531,2.26387991599553));
#48202=CARTESIAN_POINT('Ctrl Pts',(367.684140814576,-7.77644258346037,2.35753946789875));
#48203=CARTESIAN_POINT('Ctrl Pts',(367.754111989783,-7.77066017773543,2.44824200439943));
#48204=CARTESIAN_POINT('Ctrl Pts',(367.827811982307,-7.76487777201049,2.53562841286821));
#48205=CARTESIAN_POINT('Ctrl Pts',(367.903817970326,-7.75891444087307,2.62574905043641));
#48206=CARTESIAN_POINT('Ctrl Pts',(367.98378961237,-7.75295110973564,2.71234227090173));
#48207=CARTESIAN_POINT('Ctrl Pts',(368.067343253147,-7.74698777859822,2.79505645068774));
#48208=CARTESIAN_POINT('Ctrl Pts',(368.150896893925,-7.7410244474608,2.87777063047374));
#48209=CARTESIAN_POINT('Ctrl Pts',(368.238032121945,-7.73506111632337,2.95660549728913));
#48210=CARTESIAN_POINT('Ctrl Pts',(368.328330781215,-7.72909778518595,3.03125680121685));
#48211=CARTESIAN_POINT('Ctrl Pts',(368.417272056605,-7.72322409579538,3.10478593481145));
#48212=CARTESIAN_POINT('Ctrl Pts',(368.509600375792,-7.71735040640482,3.17451972307166));
#48213=CARTESIAN_POINT('Ctrl Pts',(368.60495804359,-7.71147671701425,3.24013021948005));
#48214=CARTESIAN_POINT('Ctrl Pts',(368.70019259568,-7.70561061110848,3.30565600657383));
#48215=CARTESIAN_POINT('Ctrl Pts',(368.798448381085,-7.69974450520272,3.36706885657954));
#48216=CARTESIAN_POINT('Ctrl Pts',(368.899333887231,-7.69387839929696,3.42408032197673));
#48217=CARTESIAN_POINT('Ctrl Pts',(369.000116087903,-7.68801830020892,3.48103340835951));
#48218=CARTESIAN_POINT('Ctrl Pts',(369.103522295566,-7.68215820112089,3.53359387280054));
#48219=CARTESIAN_POINT('Ctrl Pts',(369.209131760855,-7.67629810203285,3.5815163220582));
#48220=CARTESIAN_POINT('Ctrl Pts',(369.318551374717,-7.67022658393875,3.63116770395649));
#48221=CARTESIAN_POINT('Ctrl Pts',(369.430335852678,-7.66415506584464,3.67583983813451));
#48222=CARTESIAN_POINT('Ctrl Pts',(369.543988661728,-7.65808354775054,3.71531150478304));
#48223=CARTESIAN_POINT('Ctrl Pts',(369.653557834519,-7.65223018415378,3.75336492290394));
#48224=CARTESIAN_POINT('Ctrl Pts',(369.764862964019,-7.64637682055703,3.78658500868895));
#48225=CARTESIAN_POINT('Ctrl Pts',(369.877439249627,-7.64052345696027,3.81482271383333));
#48226=CARTESIAN_POINT('Ctrl Pts',(369.989998632285,-7.63467097222637,3.84305617918127));
#48227=CARTESIAN_POINT('Ctrl Pts',(370.103828390928,-7.62881848749247,3.86630865087886));
#48228=CARTESIAN_POINT('Ctrl Pts',(370.218450323905,-7.62296600275858,3.88448145655638));
#48229=CARTESIAN_POINT('Ctrl Pts',(370.333082766174,-7.6171129814304,3.90265592843621));
#48230=CARTESIAN_POINT('Ctrl Pts',(370.44850711909,-7.61125996010222,3.91574974375619));
#48231=CARTESIAN_POINT('Ctrl Pts',(370.564237497149,-7.60540693877404,3.92371579007229));
#48232=CARTESIAN_POINT('Ctrl Pts',(370.680006473524,-7.59955196535024,3.93168449321864));
#48233=CARTESIAN_POINT('Ctrl Pts',(370.796081266048,-7.59369699192644,3.93452199832942));
#48234=CARTESIAN_POINT('Ctrl Pts',(370.911974120306,-7.58784201850264,3.93223327184222));
#48235=CARTESIAN_POINT('Ctrl Pts',(371.027998324229,-7.58198040921848,3.92994195137751));
#48236=CARTESIAN_POINT('Ctrl Pts',(371.143839765021,-7.57611879993433,3.92251281121623));
#48237=CARTESIAN_POINT('Ctrl Pts',(371.259013846276,-7.57025719065017,3.91000285338588));
#48238=CARTESIAN_POINT('Ctrl Pts',(371.374265590259,-7.56439162883983,3.89748445999912));
#48239=CARTESIAN_POINT('Ctrl Pts',(371.488848671303,-7.5585260670295,3.87987848954137));
#48240=CARTESIAN_POINT('Ctrl Pts',(371.602288461927,-7.55266050521916,3.85729311100003));
#48241=CARTESIAN_POINT('Ctrl Pts',(371.715894129348,-7.54678636651883,3.83467470709581));
#48242=CARTESIAN_POINT('Ctrl Pts',(371.82835277023,-7.5409122278185,3.80706246196675));
#48243=CARTESIAN_POINT('Ctrl Pts',(371.939204617298,-7.53503808911817,3.77461444899661));
#48244=CARTESIAN_POINT('Ctrl Pts',(371.967237239752,-7.53355261533688,3.76640887623419));
#48245=CARTESIAN_POINT('Ctrl Pts',(371.995167208274,-7.53206714155559,3.75789429531113));
#48246=CARTESIAN_POINT('Ctrl Pts',(372.022987303979,-7.5305816677743,3.74907374385212));
#48247=CARTESIAN_POINT('Ctrl Pts',(372.132990323247,-7.52470797838373,3.71419653485905));
#48248=CARTESIAN_POINT('Ctrl Pts',(372.241640232704,-7.51883428899316,3.67441567358135));
#48249=CARTESIAN_POINT('Ctrl Pts',(372.348467546356,-7.51296059960259,3.62985395116504));
#48250=CARTESIAN_POINT('Ctrl Pts',(372.45515693591,-7.50709449369683,3.58534976211875));
#48251=CARTESIAN_POINT('Ctrl Pts',(372.560028031468,-7.50122838779108,3.53607714469605));
#48252=CARTESIAN_POINT('Ctrl Pts',(372.662626205627,-7.49536228188532,3.48220871984077));
#48253=CARTESIAN_POINT('Ctrl Pts',(372.765119320562,-7.48950218279727,3.42839545556629));
#48254=CARTESIAN_POINT('Ctrl Pts',(372.865343779956,-7.48364208370923,3.36999593549378));
#48255=CARTESIAN_POINT('Ctrl Pts',(372.96286528571,-7.47778198462119,3.30723068860612));
#48256=CARTESIAN_POINT('Ctrl Pts',(373.063905144909,-7.47171046652708,3.24220101480127));
#48257=CARTESIAN_POINT('Ctrl Pts',(373.162042918496,-7.46563894843298,3.17248482958958));
#48258=CARTESIAN_POINT('Ctrl Pts',(373.256823538462,-7.45956743033887,3.09837944819387));
#48259=CARTESIAN_POINT('Ctrl Pts',(373.348198615005,-7.45371406674212,3.02693673237523));
#48260=CARTESIAN_POINT('Ctrl Pts',(373.436453283101,-7.44786070314537,2.95141508308361));
#48261=CARTESIAN_POINT('Ctrl Pts',(373.521210323463,-7.44200733954862,2.87212427540538));
#48262=CARTESIAN_POINT('Ctrl Pts',(373.605954637841,-7.43615485481471,2.79284537297504));
#48263=CARTESIAN_POINT('Ctrl Pts',(373.687202067072,-7.43030237008081,2.70979871960328));
#48264=CARTESIAN_POINT('Ctrl Pts',(373.764610458325,-7.4244498853469,2.62333266066084));
#48265=CARTESIAN_POINT('Ctrl Pts',(373.842025946888,-7.41859686401873,2.53685867394186));
#48266=CARTESIAN_POINT('Ctrl Pts',(373.915601422169,-7.41274384269055,2.44696496624825));
#48267=CARTESIAN_POINT('Ctrl Pts',(373.985033892059,-7.40689082136238,2.35403429087817));
#48268=CARTESIAN_POINT('Ctrl Pts',(374.054489519017,-7.40103584793857,2.26107262133317));
#48269=CARTESIAN_POINT('Ctrl Pts',(374.119799145844,-7.39518087451475,2.16507230082107));
#48270=CARTESIAN_POINT('Ctrl Pts',(374.180702529568,-7.38932590109093,2.06644588555593));
#48271=CARTESIAN_POINT('Ctrl Pts',(374.241674939455,-7.38346429180678,1.96770768991714));
#48272=CARTESIAN_POINT('Ctrl Pts',(374.298230921501,-7.37760268252263,1.86633781064785));
#48273=CARTESIAN_POINT('Ctrl Pts',(374.350155670638,-7.37174107323848,1.76277435925264));
#48274=CARTESIAN_POINT('Ctrl Pts',(374.402115433015,-7.36587551142814,1.65914107426153));
#48275=CARTESIAN_POINT('Ctrl Pts',(374.449437575916,-7.36000994961779,1.553311648068));
#48276=CARTESIAN_POINT('Ctrl Pts',(374.49195569452,-7.35414438780745,1.44574355330403));
#48277=CARTESIAN_POINT('Ctrl Pts',(374.534535985041,-7.34827024910712,1.33801816760284));
#48278=CARTESIAN_POINT('Ctrl Pts',(374.572298097598,-7.34239611040679,1.22854942847895));
#48279=CARTESIAN_POINT('Ctrl Pts',(374.605125618281,-7.33652197170647,1.11780937506639));
#48280=CARTESIAN_POINT('Ctrl Pts',(374.613427162348,-7.33503649792519,1.08980502340337));
#48281=CARTESIAN_POINT('Ctrl Pts',(374.621413394761,-7.33355102414392,1.06171941638111));
#48282=CARTESIAN_POINT('Ctrl Pts',(374.629082954632,-7.33206555036264,1.03356026681246));
#48283=CARTESIAN_POINT('Ctrl Pts',(374.659409045212,-7.32619186097207,0.922216599792636));
#48284=CARTESIAN_POINT('Ctrl Pts',(374.684881024598,-7.3203181715815,0.809351645022848));
#48285=CARTESIAN_POINT('Ctrl Pts',(374.705347562333,-7.31444448219092,0.695426481516768));
#48286=CARTESIAN_POINT('Ctrl Pts',(374.725787675845,-7.30857837628516,0.581648406099501));
#48287=CARTESIAN_POINT('Ctrl Pts',(374.741235127104,-7.30271227037939,0.466813247019476));
#48288=CARTESIAN_POINT('Ctrl Pts',(374.751588513005,-7.29684616447362,0.35139661070802));
#48289=CARTESIAN_POINT('Ctrl Pts',(374.761931297171,-7.29098606538559,0.236098159562184));
#48290=CARTESIAN_POINT('Ctrl Pts',(374.767190354854,-7.28512596629757,0.120219824582055));
#48291=CARTESIAN_POINT('Ctrl Pts',(374.76731556116,-7.27926586720954,0.00424610072738966));
#48292=CARTESIAN_POINT('Ctrl Pts',(374.767445284623,-7.27319434911543,-0.115911690505665));
#48293=CARTESIAN_POINT('Ctrl Pts',(374.762063647564,-7.26712283102132,-0.236171438832659));
#48294=CARTESIAN_POINT('Ctrl Pts',(374.751173789599,-7.26105131292722,-0.355989569624242));
#48295=CARTESIAN_POINT('Ctrl Pts',(374.740675212935,-7.25519794933046,-0.471502539220447));
#48296=CARTESIAN_POINT('Ctrl Pts',(374.725057473366,-7.2493445857337,-0.586604633741704));
#48297=CARTESIAN_POINT('Ctrl Pts',(374.704376383168,-7.24349122213694,-0.700810940842099));
#48298=CARTESIAN_POINT('Ctrl Pts',(374.683698398167,-7.23763873740303,-0.815000100249708));
#48299=CARTESIAN_POINT('Ctrl Pts',(374.657958647785,-7.23178625266912,-0.928293333247853));
#48300=CARTESIAN_POINT('Ctrl Pts',(374.627264365069,-7.22593376793521,-1.04021428478964));
#48301=CARTESIAN_POINT('Ctrl Pts',(374.5965672681,-7.22008074660703,-1.15214549797992));
#48302=CARTESIAN_POINT('Ctrl Pts',(374.560914845037,-7.21422772527886,-1.26270378114107));
#48303=CARTESIAN_POINT('Ctrl Pts',(374.520464471577,-7.20837470395068,-1.37142703342242));
#48304=CARTESIAN_POINT('Ctrl Pts',(374.480000607137,-7.20251973052685,-1.48018654700817));
#48305=CARTESIAN_POINT('Ctrl Pts',(374.434735754339,-7.19666475710302,-1.5871094257381));
#48306=CARTESIAN_POINT('Ctrl Pts',(374.384875507219,-7.19080978367919,-1.69175333475488));
#48307=CARTESIAN_POINT('Ctrl Pts',(374.334958749914,-7.18494817439503,-1.79651584420155));
#48308=CARTESIAN_POINT('Ctrl Pts',(374.280436380666,-7.17908656511086,-1.89899385540377));
#48309=CARTESIAN_POINT('Ctrl Pts',(374.221560100138,-7.1732249558267,-1.998769361562));
#48310=CARTESIAN_POINT('Ctrl Pts',(374.162644118903,-7.16735939401636,-2.09861214707661));
#48311=CARTESIAN_POINT('Ctrl Pts',(374.099368605355,-7.16149383220602,-2.1957484535869));
#48312=CARTESIAN_POINT('Ctrl Pts',(374.032027767701,-7.15562827039568,-2.28979044955066));
#48313=CARTESIAN_POINT('Ctrl Pts',(373.964588461226,-7.14975413169534,-2.38396995797791));
#48314=CARTESIAN_POINT('Ctrl Pts',(373.893072221089,-7.143879992995,-2.47504580212331));
#48315=CARTESIAN_POINT('Ctrl Pts',(373.817812596392,-7.13800585429467,-2.56266426156235));
#48316=CARTESIAN_POINT('Ctrl Pts',(373.798780665929,-7.13652038051344,-2.58482153957156));
#48317=CARTESIAN_POINT('Ctrl Pts',(373.779509522504,-7.13503490673222,-2.60675790802626));
#48318=CARTESIAN_POINT('Ctrl Pts',(373.760004909503,-7.13354943295099,-2.62846804217276));
#48319=CARTESIAN_POINT('Ctrl Pts',(373.682882014504,-7.12767574356043,-2.71431175494352));
#48320=CARTESIAN_POINT('Ctrl Pts',(373.601849309627,-7.12180205416987,-2.79690122454613));
#48321=CARTESIAN_POINT('Ctrl Pts',(373.517212205502,-7.11592836477931,-2.87585933148935));
#48322=CARTESIAN_POINT('Ctrl Pts',(373.43268437583,-7.11006225887357,-2.95471549609863));
#48323=CARTESIAN_POINT('Ctrl Pts',(373.344561700769,-7.10419615296782,-3.02994934254657));
#48324=CARTESIAN_POINT('Ctrl Pts',(373.253188864547,-7.09833004706208,-3.10121783023713));
#48325=CARTESIAN_POINT('Ctrl Pts',(373.161909592945,-7.09246994797402,-3.17241333990454));
#48326=CARTESIAN_POINT('Ctrl Pts',(373.067387103929,-7.08660984888597,-3.2396513148576));
#48327=CARTESIAN_POINT('Ctrl Pts',(372.970001349233,-7.08074974979792,-3.30262698542776));
#48328=CARTESIAN_POINT('Ctrl Pts',(372.86910213868,-7.07467823170381,-3.36787467452141));
#48329=CARTESIAN_POINT('Ctrl Pts',(372.765129491823,-7.0686067136097,-3.4285463960289));
#48330=CARTESIAN_POINT('Ctrl Pts',(372.658541880706,-7.0625351955156,-3.48435011122001));
#48331=CARTESIAN_POINT('Ctrl Pts',(372.555784047638,-7.05668183191886,-3.53814875432692));
#48332=CARTESIAN_POINT('Ctrl Pts',(372.450596329222,-7.05082846832213,-3.58742298538895));
#48333=CARTESIAN_POINT('Ctrl Pts',(372.343416457472,-7.0449751047254,-3.63195682830301));
#48334=CARTESIAN_POINT('Ctrl Pts',(372.236252678418,-7.0391226199915,-3.67648398461054));
#48335=CARTESIAN_POINT('Ctrl Pts',(372.127097722202,-7.03327013525759,-3.71627200952119));
#48336=CARTESIAN_POINT('Ctrl Pts',(372.016410005761,-7.02741765052369,-3.75115277520263));
#48337=CARTESIAN_POINT('Ctrl Pts',(371.905712140743,-7.02156462919553,-3.7860367389819));
#48338=CARTESIAN_POINT('Ctrl Pts',(371.793481630196,-7.01571160786736,-3.81601242493306));
#48339=CARTESIAN_POINT('Ctrl Pts',(371.680192095955,-7.0098585865392,-3.8409615678219));
#48340=CARTESIAN_POINT('Ctrl Pts',(371.566864777465,-7.00400361311539,-3.86591903173173));
#48341=CARTESIAN_POINT('Ctrl Pts',(371.452478136207,-6.99814863969157,-3.88584653022729));
#48342=CARTESIAN_POINT('Ctrl Pts',(371.337515324113,-6.99229366626776,-3.90067703165623));
#48343=CARTESIAN_POINT('Ctrl Pts',(371.222422216439,-6.98643205698361,-3.91552434155363));
#48344=CARTESIAN_POINT('Ctrl Pts',(371.106752044528,-6.98057044769946,-3.92526307136814));
#48345=CARTESIAN_POINT('Ctrl Pts',(370.990992512098,-6.97470883841532,-3.92987812168097));
#48346=CARTESIAN_POINT('Ctrl Pts',(370.875154922165,-6.968843276605,-3.93449628395611));
#48347=CARTESIAN_POINT('Ctrl Pts',(370.759228263849,-6.96297771479469,-3.93398388900972));
#48348=CARTESIAN_POINT('Ctrl Pts',(370.643697928103,-6.95711215298438,-3.92837791513835));
#48349=CARTESIAN_POINT('Ctrl Pts',(370.52799865867,-6.95123801428405,-3.9227637439582));
#48350=CARTESIAN_POINT('Ctrl Pts',(370.412697278174,-6.94536387558372,-3.91204116750302));
#48351=CARTESIAN_POINT('Ctrl Pts',(370.298271840804,-6.9394897368834,-3.89629871449412));
#48352=CARTESIAN_POINT('Ctrl Pts',(370.269335515701,-6.93800426310204,-3.89231770512544));
#48353=CARTESIAN_POINT('Ctrl Pts',(370.240455143008,-6.93651878932069,-3.88801592605633));
#48354=CARTESIAN_POINT('Ctrl Pts',(370.211638310701,-6.93503331553933,-3.8833953169004));
#48355=CARTESIAN_POINT('Ctrl Pts',(370.097694110331,-6.92915962614875,-3.86512503618736));
#48356=CARTESIAN_POINT('Ctrl Pts',(369.984364930911,-6.92328593675816,-3.84180515537915));
#48357=CARTESIAN_POINT('Ctrl Pts',(369.872133234915,-6.91741224736758,-3.81348787336344));
#48358=CARTESIAN_POINT('Ctrl Pts',(369.760046440583,-6.91154614146182,-3.78520715161916));
#48359=CARTESIAN_POINT('Ctrl Pts',(369.649054708751,-6.90568003555606,-3.75194195995776));
#48360=CARTESIAN_POINT('Ctrl Pts',(369.539633155722,-6.8998139296503,-3.71379597367104));
#48361=CARTESIAN_POINT('Ctrl Pts',(369.430323648969,-6.89395383056222,-3.67568904838807));
#48362=CARTESIAN_POINT('Ctrl Pts',(369.322581510686,-6.88809373147414,-3.63271140485318));
#48363=CARTESIAN_POINT('Ctrl Pts',(369.216868816665,-6.88223363238606,-3.58501710095414));
#48364=CARTESIAN_POINT('Ctrl Pts',(369.107342249814,-6.87616211429196,-3.53560209537897));
#48365=CARTESIAN_POINT('Ctrl Pts',(368.999994765382,-6.87009059619786,-3.48112378160884));
#48366=CARTESIAN_POINT('Ctrl Pts',(368.895320307861,-6.86401907810376,-3.4218091003266));
#48367=CARTESIAN_POINT('Ctrl Pts',(368.794406887253,-6.858165714507,-3.36462564294582));
#48368=CARTESIAN_POINT('Ctrl Pts',(368.695978101632,-6.85231235091025,-3.30294760703743));
#48369=CARTESIAN_POINT('Ctrl Pts',(368.6004527361,-6.84645898731349,-3.23702573954811));
#48370=CARTESIAN_POINT('Ctrl Pts',(368.50494171338,-6.84060650257958,-3.17111377000538));
#48371=CARTESIAN_POINT('Ctrl Pts',(368.412333583885,-6.83475401784568,-3.10095947046379));
#48372=CARTESIAN_POINT('Ctrl Pts',(368.323018138932,-6.82890153311177,-3.02685690857625));
#48373=CARTESIAN_POINT('Ctrl Pts',(368.233694504952,-6.82304851178359,-2.95274755247875));
#48374=CARTESIAN_POINT('Ctrl Pts',(368.147664473629,-6.81719549045541,-2.87468947822377));
#48375=CARTESIAN_POINT('Ctrl Pts',(368.065284179068,-6.81134246912724,-2.79301656124543));
#48376=CARTESIAN_POINT('Ctrl Pts',(367.982876409087,-6.80548749570336,-2.71131640477127));
#48377=CARTESIAN_POINT('Ctrl Pts',(367.904121089567,-6.79963252227948,-2.62599929897062));
#48378=CARTESIAN_POINT('Ctrl Pts',(367.82933646899,-6.79377754885561,-2.53743490170824));
#48379=CARTESIAN_POINT('Ctrl Pts',(367.754467089651,-6.78791593957144,-2.44877012807792));
#48380=CARTESIAN_POINT('Ctrl Pts',(367.683577658234,-6.78205433028728,-2.35685103299066));
#48381=CARTESIAN_POINT('Ctrl Pts',(367.61694525172,-6.77619272100311,-2.26207925216892));
#48382=CARTESIAN_POINT('Ctrl Pts',(367.550267914486,-6.77032715919274,-2.16724356603906));
#48383=CARTESIAN_POINT('Ctrl Pts',(367.487853539927,-6.76446159738237,-2.06955171118032));
#48384=CARTESIAN_POINT('Ctrl Pts',(367.429934189944,-6.758596035572,-1.96943161170743));
#48385=CARTESIAN_POINT('Ctrl Pts',(367.371930147666,-6.75272189687167,-1.86916511209358));
#48386=CARTESIAN_POINT('Ctrl Pts',(367.318434437805,-6.74684775817134,-1.76646364659021));
#48387=CARTESIAN_POINT('Ctrl Pts',(367.269631826703,-6.74097361947101,-1.66177692014548));
#48388=CARTESIAN_POINT('Ctrl Pts',(367.257290443066,-6.7394881456899,-1.63530335605419));
#48389=CARTESIAN_POINT('Ctrl Pts',(367.245248937058,-6.73800267190878,-1.6087029169066));
#48390=CARTESIAN_POINT('Ctrl Pts',(367.233509792322,-6.73651719812767,-1.58198303042237));
#48391=CARTESIAN_POINT('Ctrl Pts',(367.182386656801,-6.73004806607979,-1.46561983628958));
#48392=CARTESIAN_POINT('Ctrl Pts',(367.136855419181,-6.7235789340319,-1.34665702101869));
#48393=CARTESIAN_POINT('Ctrl Pts',(367.097161857521,-6.71710980198402,-1.22562394876207));
#48394=CARTESIAN_POINT('Ctrl Pts',(367.05762730515,-6.71066658477084,-1.10507572548325));
#48395=CARTESIAN_POINT('Ctrl Pts',(367.023883885696,-6.70422336755765,-0.982474039744795));
#48396=CARTESIAN_POINT('Ctrl Pts',(366.996128507445,-6.69778015034447,-0.858365624862619));
#48397=CARTESIAN_POINT('Ctrl Pts',(366.968446864221,-6.69135405020284,-0.734586916794222));
#48398=CARTESIAN_POINT('Ctrl Pts',(366.946721618277,-6.68492795006121,-0.609309720773344));
#48399=CARTESIAN_POINT('Ctrl Pts',(366.93110035336,-6.67850184991958,-0.483096417658677));
#48400=CARTESIAN_POINT('Ctrl Pts',(366.915541521388,-6.67210143274021,-0.357387546692535));
#48401=CARTESIAN_POINT('Ctrl Pts',(366.906038079496,-6.66570101556084,-0.23075029565414));
#48402=CARTESIAN_POINT('Ctrl Pts',(366.902686689438,-6.65930059838148,-0.103756406788144));
#48403=CARTESIAN_POINT('Ctrl Pts',(366.901790063172,-6.65758823961168,-0.0697806372068197));
#48404=CARTESIAN_POINT('Ctrl Pts',(366.901333503911,-6.65587588084188,-0.0357794177768005));
#48405=CARTESIAN_POINT('Ctrl Pts',(366.901318248747,-6.65416352207208,-0.00176385594814673));
#48406=CARTESIAN_POINT('',(366.901319367511,-5.40416352200791,0.00345128679816103));
#48407=CARTESIAN_POINT('Ctrl Pts',(366.901318248747,-6.65416352203497,-0.00176385521094843));
#48408=CARTESIAN_POINT('Ctrl Pts',(366.901265199377,-6.64820884358741,0.116524284211845));
#48409=CARTESIAN_POINT('Ctrl Pts',(366.906552916805,-6.64225416513986,0.234793871859763));
#48410=CARTESIAN_POINT('Ctrl Pts',(366.917149970721,-6.6362994866923,0.352540466170501));
#48411=CARTESIAN_POINT('Ctrl Pts',(366.927751320045,-6.63034239457625,0.470334787868657));
#48412=CARTESIAN_POINT('Ctrl Pts',(366.943666256189,-6.6243853024602,0.587605302905504));
#48413=CARTESIAN_POINT('Ctrl Pts',(366.964811579099,-6.61842821034415,0.703853816146331));
#48414=CARTESIAN_POINT('Ctrl Pts',(366.98596984317,-6.61246747242437,0.820173474713461));
#48415=CARTESIAN_POINT('Ctrl Pts',(367.012364798096,-6.6065067345046,0.935469499932208));
#48416=CARTESIAN_POINT('Ctrl Pts',(367.043862465922,-6.60054599658482,1.04925542975754));
#48417=CARTESIAN_POINT('Ctrl Pts',(367.075408021142,-6.59457619627333,1.16321435371244));
#48418=CARTESIAN_POINT('Ctrl Pts',(367.112071678325,-6.58860639596184,1.27565821811409));
#48419=CARTESIAN_POINT('Ctrl Pts',(367.153669865202,-6.58263659565035,1.38611665752539));
#48420=CARTESIAN_POINT('Ctrl Pts',(367.195303399591,-6.57666172257948,1.49666895754418));
#48421=CARTESIAN_POINT('Ctrl Pts',(367.241879665614,-6.57068684950862,1.6052321101754));
#48422=CARTESIAN_POINT('Ctrl Pts',(367.293168055001,-6.56471197643775,1.71135826364399));
#48423=CARTESIAN_POINT('Ctrl Pts',(367.344548369054,-6.55872639454521,1.81767462802412));
#48424=CARTESIAN_POINT('Ctrl Pts',(367.400657490594,-6.55274081265266,1.92154492330828));
#48425=CARTESIAN_POINT('Ctrl Pts',(367.461219925966,-6.54675523076011,2.02254774310239));
#48426=CARTESIAN_POINT('Ctrl Pts',(367.490744910938,-6.54383718074542,2.07178794816112));
#48427=CARTESIAN_POINT('Ctrl Pts',(367.521327673345,-6.54091913073072,2.12034710914281));
#48428=CARTESIAN_POINT('Ctrl Pts',(367.552932801484,-6.53800108071602,2.16817922280896));
#48429=CARTESIAN_POINT('Ctrl Pts',(367.616550184635,-6.53212739132544,2.26445960770791));
#48430=CARTESIAN_POINT('Ctrl Pts',(367.684514613203,-6.52625370193487,2.35809804104892));
#48431=CARTESIAN_POINT('Ctrl Pts',(367.756579642237,-6.5203800125443,2.44867648018891));
#48432=CARTESIAN_POINT('Ctrl Pts',(367.828551628548,-6.51451390663854,2.53913797405444));
#48433=CARTESIAN_POINT('Ctrl Pts',(367.904613431905,-6.50864780073278,2.6265470100949));
#48434=CARTESIAN_POINT('Ctrl Pts',(367.984474736695,-6.50278169482702,2.71051345895475));
#48435=CARTESIAN_POINT('Ctrl Pts',(368.064254264528,-6.49692159573898,2.79439392724059));
#48436=CARTESIAN_POINT('Ctrl Pts',(368.147825271951,-6.49106149665095,2.87483852260736));
#48437=CARTESIAN_POINT('Ctrl Pts',(368.234856916643,-6.48520139756291,2.9514897660653));
#48438=CARTESIAN_POINT('Ctrl Pts',(368.325028464524,-6.4791298794688,3.0309064115177));
#48439=CARTESIAN_POINT('Ctrl Pts',(368.418914786781,-6.4730583613747,3.10625047285123));
#48440=CARTESIAN_POINT('Ctrl Pts',(368.516105501817,-6.46698684328059,3.1771654810199));
#48441=CARTESIAN_POINT('Ctrl Pts',(368.60980407679,-6.46113347968384,3.24553245627129));
#48442=CARTESIAN_POINT('Ctrl Pts',(368.706573309863,-6.45528011608708,3.30978291527893));
#48443=CARTESIAN_POINT('Ctrl Pts',(368.806012113383,-6.44942675249033,3.36963867880944));
#48444=CARTESIAN_POINT('Ctrl Pts',(368.905435986501,-6.44357426775642,3.42948545519847));
#48445=CARTESIAN_POINT('Ctrl Pts',(369.007528279199,-6.43772178302251,3.4849386351298));
#48446=CARTESIAN_POINT('Ctrl Pts',(369.11186038753,-6.4318692982886,3.53576431325329));
#48447=CARTESIAN_POINT('Ctrl Pts',(369.216202061715,-6.42601627696041,3.58659465140923));
#48448=CARTESIAN_POINT('Ctrl Pts',(369.322783588333,-6.42016325563221,3.63279646338199));
#48449=CARTESIAN_POINT('Ctrl Pts',(369.431153970121,-6.41431023430401,3.67418291830369));
#48450=CARTESIAN_POINT('Ctrl Pts',(369.539560495523,-6.40845526088018,3.71558317640724));
#48451=CARTESIAN_POINT('Ctrl Pts',(369.649756676694,-6.40260028745635,3.75216473665459));
#48452=CARTESIAN_POINT('Ctrl Pts',(369.761274533554,-6.39674531403253,3.78379003568001));
#48453=CARTESIAN_POINT('Ctrl Pts',(369.872918781581,-6.39088370474837,3.81545117791975));
#48454=CARTESIAN_POINT('Ctrl Pts',(369.985887297422,-6.38502209546421,3.84214473439232));
#48455=CARTESIAN_POINT('Ctrl Pts',(370.099699938997,-6.37916048618005,3.86378383454573));
#48456=CARTESIAN_POINT('Ctrl Pts',(370.213589325272,-6.37329492436972,3.88543752610323));
#48457=CARTESIAN_POINT('Ctrl Pts',(370.328323562807,-6.36742936255939,3.90202991575999));
#48458=CARTESIAN_POINT('Ctrl Pts',(370.443417115525,-6.36156380074906,3.91352598218878));
#48459=CARTESIAN_POINT('Ctrl Pts',(370.558678963247,-6.35568966204872,3.92503885868632));
#48460=CARTESIAN_POINT('Ctrl Pts',(370.674300763805,-6.34981552334837,3.93144051673659));
#48461=CARTESIAN_POINT('Ctrl Pts',(370.789796633956,-6.34394138464803,3.93274800375448));
#48462=CARTESIAN_POINT('Ctrl Pts',(370.819003654031,-6.34245591086681,3.93307864587641));
#48463=CARTESIAN_POINT('Ctrl Pts',(370.848202647226,-6.34097043708558,3.93308377387877));
#48464=CARTESIAN_POINT('Ctrl Pts',(370.877385822468,-6.33948496330436,3.93276418693331));
#48465=CARTESIAN_POINT('Ctrl Pts',(370.992778573902,-6.3336112739138,3.9315005130303));
#48466=CARTESIAN_POINT('Ctrl Pts',(371.108307847375,-6.32773758452324,3.92515175568437));
#48467=CARTESIAN_POINT('Ctrl Pts',(371.223488758222,-6.32186389513268,3.91369837962805));
#48468=CARTESIAN_POINT('Ctrl Pts',(371.338520959692,-6.31599778922692,3.90225979095622));
#48469=CARTESIAN_POINT('Ctrl Pts',(371.453205285617,-6.31013168332117,3.88572973050911));
#48470=CARTESIAN_POINT('Ctrl Pts',(371.567056524385,-6.30426557741542,3.8641406599379));
#48471=CARTESIAN_POINT('Ctrl Pts',(371.680791180934,-6.29840547832738,3.84257369629991));
#48472=CARTESIAN_POINT('Ctrl Pts',(371.793694043655,-6.29254537923935,3.81595810322062));
#48473=CARTESIAN_POINT('Ctrl Pts',(371.905285367377,-6.28668528015131,3.78437809734029));
#48474=CARTESIAN_POINT('Ctrl Pts',(372.020902651478,-6.2806137620572,3.75165875689333));
#48475=CARTESIAN_POINT('Ctrl Pts',(372.135111525706,-6.27454224396309,3.71361007580274));
#48476=CARTESIAN_POINT('Ctrl Pts',(372.247389974558,-6.26847072586898,3.67038365568356));
#48477=CARTESIAN_POINT('Ctrl Pts',(372.355634169012,-6.26261736227224,3.62871039538504));
#48478=CARTESIAN_POINT('Ctrl Pts',(372.462083855524,-6.2567639986755,3.58222523437998));
#48479=CARTESIAN_POINT('Ctrl Pts',(372.56628784447,-6.25091063507876,3.53111440616437));
#48480=CARTESIAN_POINT('Ctrl Pts',(372.670476187538,-6.24505815034487,3.48001125206761));
#48481=CARTESIAN_POINT('Ctrl Pts',(372.772419132659,-6.23920566561097,3.42428399363079));
#48482=CARTESIAN_POINT('Ctrl Pts',(372.871687777056,-6.23335318087708,3.36416598779938));
#48483=CARTESIAN_POINT('Ctrl Pts',(372.970965523054,-6.2275001595489,3.30404246995386));
#48484=CARTESIAN_POINT('Ctrl Pts',(373.067568127487,-6.22164713822072,3.23952761846589));
#48485=CARTESIAN_POINT('Ctrl Pts',(373.161094105004,-6.21579411689254,3.17089912708544));
#48486=CARTESIAN_POINT('Ctrl Pts',(373.254651275241,-6.20993914346874,3.1022477467781));
#48487=CARTESIAN_POINT('Ctrl Pts',(373.345129445268,-6.20408417004494,3.02948024274663));
#48488=CARTESIAN_POINT('Ctrl Pts',(373.432159323061,-6.19822919662114,2.95291528791417));
#48489=CARTESIAN_POINT('Ctrl Pts',(373.519287838041,-6.19236758733699,2.87626355653956));
#48490=CARTESIAN_POINT('Ctrl Pts',(373.602959949896,-6.18650597805284,2.79580605703823));
#48491=CARTESIAN_POINT('Ctrl Pts',(373.682842371033,-6.18064436876869,2.71189916321427));
#48492=CARTESIAN_POINT('Ctrl Pts',(373.762778657472,-6.17477880695837,2.62793569035573));
#48493=CARTESIAN_POINT('Ctrl Pts',(373.838919894111,-6.16891324514804,2.54051850245589));
#48494=CARTESIAN_POINT('Ctrl Pts',(373.910973438527,-6.16304768333771,2.45003661389421));
#48495=CARTESIAN_POINT('Ctrl Pts',(373.983132342898,-6.15717354463739,2.35942241861927));
#48496=CARTESIAN_POINT('Ctrl Pts',(374.051191384155,-6.15129940593707,2.2657349120178));
#48497=CARTESIAN_POINT('Ctrl Pts',(374.114901485447,-6.14542526723675,2.16939162715907));
#48498=CARTESIAN_POINT('Ctrl Pts',(374.13101272999,-6.1439397934554,2.14502798323304));
#48499=CARTESIAN_POINT('Ctrl Pts',(374.146846091015,-6.14245431967405,2.12049462005751));
#48500=CARTESIAN_POINT('Ctrl Pts',(374.162398016458,-6.1409688458927,2.09579851777101));
#48501=CARTESIAN_POINT('Ctrl Pts',(374.223891649414,-6.13509515650213,1.99814803358881));
#48502=CARTESIAN_POINT('Ctrl Pts',(374.281186256746,-6.12922146711156,1.89762615676717));
#48503=CARTESIAN_POINT('Ctrl Pts',(374.334002562226,-6.12334777772098,1.7946297494406));
#48504=CARTESIAN_POINT('Ctrl Pts',(374.386750676894,-6.11748167181523,1.69176632015215));
#48505=CARTESIAN_POINT('Ctrl Pts',(374.435031801233,-6.11161556590948,1.58643507813995));
#48506=CARTESIAN_POINT('Ctrl Pts',(374.478610175194,-6.10574946000373,1.47906134829925));
#48507=CARTESIAN_POINT('Ctrl Pts',(374.522143925455,-6.09988936091568,1.37179756778974));
#48508=CARTESIAN_POINT('Ctrl Pts',(374.560984349434,-6.09402926182763,1.26249584012391));
#48509=CARTESIAN_POINT('Ctrl Pts',(374.594942140613,-6.08816916273959,1.1516049535749));
#48510=CARTESIAN_POINT('Ctrl Pts',(374.630125051428,-6.08209764464548,1.03671337682208));
#48511=CARTESIAN_POINT('Ctrl Pts',(374.660066163093,-6.07602612655137,0.920116211687519));
#48512=CARTESIAN_POINT('Ctrl Pts',(374.684609878064,-6.06995460845727,0.802334296571989));
#48513=CARTESIAN_POINT('Ctrl Pts',(374.708271717741,-6.06410124486051,0.688784379795269));
#48514=CARTESIAN_POINT('Ctrl Pts',(374.726917259672,-6.05824788126375,0.574133824984173));
#48515=CARTESIAN_POINT('Ctrl Pts',(374.740458403138,-6.05239451766698,0.458862729270992));
#48516=CARTESIAN_POINT('Ctrl Pts',(374.753997513447,-6.04654203293307,0.34360894112484));
#48517=CARTESIAN_POINT('Ctrl Pts',(374.76243370101,-6.04068954819915,0.227735207551089));
#48518=CARTESIAN_POINT('Ctrl Pts',(374.765730545224,-6.03483706346523,0.111728443939046));
#48519=CARTESIAN_POINT('Ctrl Pts',(374.769027691713,-6.02898404213703,-0.00428895593571747));
#48520=CARTESIAN_POINT('Ctrl Pts',(374.767184546398,-6.02313102080884,-0.12043899709449));
#48521=CARTESIAN_POINT('Ctrl Pts',(374.760216808488,-6.01727799948065,-0.236233767823389));
#48522=CARTESIAN_POINT('Ctrl Pts',(374.753246746702,-6.01142302605686,-0.352067158343562));
#48523=CARTESIAN_POINT('Ctrl Pts',(374.741148718553,-6.00556805263307,-0.467544630646261));
#48524=CARTESIAN_POINT('Ctrl Pts',(374.72399031068,-5.99971307920928,-0.582183110120685));
#48525=CARTESIAN_POINT('Ctrl Pts',(374.706812455955,-5.99385146992511,-0.696951517587674));
#48526=CARTESIAN_POINT('Ctrl Pts',(374.6845628354,-5.98798986064094,-0.81087862548388));
#48527=CARTESIAN_POINT('Ctrl Pts',(374.657360234345,-5.98212825135678,-0.923491175999978));
#48528=CARTESIAN_POINT('Ctrl Pts',(374.630139290377,-5.97626268954643,-1.0361796619859));
#48529=CARTESIAN_POINT('Ctrl Pts',(374.597958829966,-5.97039712773607,-1.1475514296155));
#48530=CARTESIAN_POINT('Ctrl Pts',(374.560987100707,-5.96453156592572,-1.25714968077147));
#48531=CARTESIAN_POINT('Ctrl Pts',(374.523961309712,-5.95865742722538,-1.36690819145139));
#48532=CARTESIAN_POINT('Ctrl Pts',(374.482130416306,-5.95278328852503,-1.47488762628487));
#48533=CARTESIAN_POINT('Ctrl Pts',(374.435710249871,-5.94690914982468,-1.58065233539077));
#48534=CARTESIAN_POINT('Ctrl Pts',(374.423971347595,-5.94542367604347,-1.60739850370051));
#48535=CARTESIAN_POINT('Ctrl Pts',(374.411939185604,-5.94393820226226,-1.63400317072937));
#48536=CARTESIAN_POINT('Ctrl Pts',(374.399617703755,-5.94245272848105,-1.66045956765013));
#48537=CARTESIAN_POINT('Ctrl Pts',(374.350897518906,-5.9365790390905,-1.76507040620627));
#48538=CARTESIAN_POINT('Ctrl Pts',(374.297488148562,-5.93070534969995,-1.86770937983888));
#48539=CARTESIAN_POINT('Ctrl Pts',(374.239571680788,-5.92483166030939,-1.9679266678051));
#48540=CARTESIAN_POINT('Ctrl Pts',(374.181729988616,-5.91896555440365,-2.06801456583772));
#48541=CARTESIAN_POINT('Ctrl Pts',(374.119392976104,-5.9130994484979,-2.16568664159294));
#48542=CARTESIAN_POINT('Ctrl Pts',(374.052790239333,-5.90723334259215,-2.26051421137998));
#48543=CARTESIAN_POINT('Ctrl Pts',(373.986255702917,-5.90137324350412,-2.35524467894349));
#48544=CARTESIAN_POINT('Ctrl Pts',(373.915464366697,-5.89551314441609,-2.44713609813846));
#48545=CARTESIAN_POINT('Ctrl Pts',(373.840690726118,-5.88965304532807,-2.53578610082256));
#48546=CARTESIAN_POINT('Ctrl Pts',(373.763219423173,-5.88358152723396,-2.62763439336071));
#48547=CARTESIAN_POINT('Ctrl Pts',(373.681473271752,-5.87751000913985,-2.71600257662247));
#48548=CARTESIAN_POINT('Ctrl Pts',(373.595805585543,-5.87143849104573,-2.80047754932134));
#48549=CARTESIAN_POINT('Ctrl Pts',(373.513216007763,-5.86558512744899,-2.88191726874028));
#48550=CARTESIAN_POINT('Ctrl Pts',(373.426982172488,-5.85973176385225,-2.95973842014589));
#48551=CARTESIAN_POINT('Ctrl Pts',(373.337459748868,-5.8538784002555,-3.03360670659094));
#48552=CARTESIAN_POINT('Ctrl Pts',(373.247950766738,-5.84802591552162,-3.10746390196119));
#48553=CARTESIAN_POINT('Ctrl Pts',(373.155154496646,-5.84217343078773,-3.17736914961662));
#48554=CARTESIAN_POINT('Ctrl Pts',(373.059460353459,-5.83632094605385,-3.24302788357548));
#48555=CARTESIAN_POINT('Ctrl Pts',(372.963757436404,-5.83046792472569,-3.30869263755875));
#48556=CARTESIAN_POINT('Ctrl Pts',(372.86515645876,-5.82461490339752,-3.37010987010284));
#48557=CARTESIAN_POINT('Ctrl Pts',(372.76407592726,-5.81876188206936,-3.42702827179645));
#48558=CARTESIAN_POINT('Ctrl Pts',(372.662961683451,-5.81290690864556,-3.48396565687613));
#48559=CARTESIAN_POINT('Ctrl Pts',(372.559366601176,-5.80705193522176,-3.53640102493));
#48560=CARTESIAN_POINT('Ctrl Pts',(372.45373325118,-5.80119696179795,-3.58412929019914));
#48561=CARTESIAN_POINT('Ctrl Pts',(372.347980179349,-5.79533535251381,-3.63191164932661));
#48562=CARTESIAN_POINT('Ctrl Pts',(372.240184605656,-5.78947374322966,-3.6749760873295));
#48563=CARTESIAN_POINT('Ctrl Pts',(372.130808607008,-5.78361213394551,-3.71316586289273));
#48564=CARTESIAN_POINT('Ctrl Pts',(372.021358855321,-5.77774657213518,-3.75138139010204));
#48565=CARTESIAN_POINT('Ctrl Pts',(371.910326951368,-5.77188101032485,-3.78471559118148));
#48566=CARTESIAN_POINT('Ctrl Pts',(371.798187954813,-5.76601544851453,-3.81306221130252));
#48567=CARTESIAN_POINT('Ctrl Pts',(371.685884983541,-5.76014130981421,-3.84145028113463));
#48568=CARTESIAN_POINT('Ctrl Pts',(371.572472091944,-5.7542671711139,-3.86483613176591));
#48569=CARTESIAN_POINT('Ctrl Pts',(371.458432363199,-5.74839303241358,-3.88316495637757));
#48570=CARTESIAN_POINT('Ctrl Pts',(371.429593577509,-5.74690755863219,-3.88780001690193));
#48571=CARTESIAN_POINT('Ctrl Pts',(371.400714717576,-5.74542208485079,-3.89211193979637));
#48572=CARTESIAN_POINT('Ctrl Pts',(371.371803607131,-5.74393661106939,-3.89610036630818));
#48573=CARTESIAN_POINT('Ctrl Pts',(371.257486623005,-5.73806292167884,-3.91187094319804));
#48574=CARTESIAN_POINT('Ctrl Pts',(371.142284560392,-5.73218923228829,-3.9226321939895));
#48575=CARTESIAN_POINT('Ctrl Pts',(371.026674118864,-5.72631554289773,-3.92829327661122));
#48576=CARTESIAN_POINT('Ctrl Pts',(370.911212941278,-5.720449436992,-3.93394705024344));
#48577=CARTESIAN_POINT('Ctrl Pts',(370.795344842198,-5.71458333108627,-3.93451373068496));
#48578=CARTESIAN_POINT('Ctrl Pts',(370.679554514112,-5.70871722518053,-3.92995385581905));
#48579=CARTESIAN_POINT('Ctrl Pts',(370.563882753847,-5.70285712609249,-3.92539865020689));
#48580=CARTESIAN_POINT('Ctrl Pts',(370.448289016545,-5.69699702700445,-3.9157273471928));
#48581=CARTESIAN_POINT('Ctrl Pts',(370.333260221904,-5.6911369279164,-3.90095247985613));
#48582=CARTESIAN_POINT('Ctrl Pts',(370.214081450775,-5.68506540982229,-3.88564456901284));
#48583=CARTESIAN_POINT('Ctrl Pts',(370.095509606763,-5.67899389172818,-3.86485786911162));
#48584=CARTESIAN_POINT('Ctrl Pts',(369.978083356832,-5.67292237363407,-3.83866532628042));
#48585=CARTESIAN_POINT('Ctrl Pts',(369.864876325905,-5.66706901003732,-3.81341390244574));
#48586=CARTESIAN_POINT('Ctrl Pts',(369.752734419427,-5.66121564644057,-3.78313852030416));
#48587=CARTESIAN_POINT('Ctrl Pts',(369.642131361374,-5.65536228284383,-3.74795682587876));
#48588=CARTESIAN_POINT('Ctrl Pts',(369.531544909999,-5.64950979810993,-3.71278041386644));
#48589=CARTESIAN_POINT('Ctrl Pts',(369.42249724123,-5.64365731337604,-3.67269927954007));
#48590=CARTESIAN_POINT('Ctrl Pts',(369.315446986677,-5.63780482864214,-3.62788096424831));
#48591=CARTESIAN_POINT('Ctrl Pts',(369.208386917054,-5.631951807314,-3.58305853971895));
#48592=CARTESIAN_POINT('Ctrl Pts',(369.103325006818,-5.62609878598585,-3.53349823036481));
#48593=CARTESIAN_POINT('Ctrl Pts',(369.000699309721,-5.62024576465771,-3.47941547345564));
#48594=CARTESIAN_POINT('Ctrl Pts',(368.898039384972,-5.61439079123388,-3.4253146789023));
#48595=CARTESIAN_POINT('Ctrl Pts',(368.797817654329,-5.60853581781006,-3.36668863006956));
#48596=CARTESIAN_POINT('Ctrl Pts',(368.700446374777,-5.60268084438624,-3.30379804368727));
#48597=CARTESIAN_POINT('Ctrl Pts',(368.602964737387,-5.5968192351021,-3.24083617890346));
#48598=CARTESIAN_POINT('Ctrl Pts',(368.508340346454,-5.59095762581795,-3.1736003538628));
#48599=CARTESIAN_POINT('Ctrl Pts',(368.416955409222,-5.58509601653381,-3.10239388445924));
#48600=CARTESIAN_POINT('Ctrl Pts',(368.325508850456,-5.57923045472348,-3.03113940001043));
#48601=CARTESIAN_POINT('Ctrl Pts',(368.23730640855,-5.57336489291316,-2.95590920727524));
#48602=CARTESIAN_POINT('Ctrl Pts',(368.152694904633,-5.56749933110283,-2.87704490086473));
#48603=CARTESIAN_POINT('Ctrl Pts',(368.067959677945,-5.56162519240251,-2.79806527549552));
#48604=CARTESIAN_POINT('Ctrl Pts',(367.986826156941,-5.55575105370219,-2.71544122476289));
#48605=CARTESIAN_POINT('Ctrl Pts',(367.909602280204,-5.54987691500187,-2.62954897595249));
#48606=CARTESIAN_POINT('Ctrl Pts',(367.890073622465,-5.54839144122049,-2.60782822842837));
#48607=CARTESIAN_POINT('Ctrl Pts',(367.870794775183,-5.54690596743912,-2.58589863022008));
#48608=CARTESIAN_POINT('Ctrl Pts',(367.851770281142,-5.54542049365774,-2.56376656118834));
#48609=CARTESIAN_POINT('Ctrl Pts',(367.776391905551,-5.53953478650679,-2.47607542951134));
#48610=CARTESIAN_POINT('Ctrl Pts',(367.704746549278,-5.53364907935584,-2.38489680937957));
#48611=CARTESIAN_POINT('Ctrl Pts',(367.637177087695,-5.52776337220489,-2.29058506181116));
#48612=CARTESIAN_POINT('Ctrl Pts',(367.570345064632,-5.52194190039155,-2.19730261230155));
#48613=CARTESIAN_POINT('Ctrl Pts',(367.50750069668,-5.51612042857821,-2.10095540839542));
#48614=CARTESIAN_POINT('Ctrl Pts',(367.44893834687,-5.51029895676486,-2.00192272527074));
#48615=CARTESIAN_POINT('Ctrl Pts',(367.390431992956,-5.50448305130154,-1.90298473479348));
#48616=CARTESIAN_POINT('Ctrl Pts',(367.336199731708,-5.49866714583822,-1.80136672753239));
#48617=CARTESIAN_POINT('Ctrl Pts',(367.286493706853,-5.4928512403749,-1.69747837288983));
#48618=CARTESIAN_POINT('Ctrl Pts',(367.23682274017,-5.48703943692969,-1.59366329177548));
#48619=CARTESIAN_POINT('Ctrl Pts',(367.191671843342,-5.48122763348449,-1.48758142417816));
#48620=CARTESIAN_POINT('Ctrl Pts',(367.151247721531,-5.47541583003929,-1.37966786040398));
#48621=CARTESIAN_POINT('Ctrl Pts',(367.109947976893,-5.4694781377056,-1.26941679180456));
#48622=CARTESIAN_POINT('Ctrl Pts',(367.073582365988,-5.4635404453719,-1.15725414933701));
#48623=CARTESIAN_POINT('Ctrl Pts',(367.042319722158,-5.45760275303821,-1.04366621771041));
#48624=CARTESIAN_POINT('Ctrl Pts',(367.011734517152,-5.45179372619235,-0.932539654206915));
#48625=CARTESIAN_POINT('Ctrl Pts',(366.98603345829,-5.44598469934649,-0.820049372686403));
#48626=CARTESIAN_POINT('Ctrl Pts',(366.965324091192,-5.44017567250064,-0.706665599388753));
#48627=CARTESIAN_POINT('Ctrl Pts',(366.943926679205,-5.43417364742302,-0.589514780708706));
#48628=CARTESIAN_POINT('Ctrl Pts',(366.927858538497,-5.42817162234541,-0.471410527504311));
#48629=CARTESIAN_POINT('Ctrl Pts',(366.9171806346,-5.4221695972678,-0.352881014605549));
#48630=CARTESIAN_POINT('Ctrl Pts',(366.906502730703,-5.41616757219019,-0.234351501706782));
#48631=CARTESIAN_POINT('Ctrl Pts',(366.901215075524,-5.41016554711258,-0.115397222528112));
#48632=CARTESIAN_POINT('Ctrl Pts',(366.901319367511,-5.40416352203497,0.00345128626229814));
#48633=CARTESIAN_POINT('',(366.901317858377,-4.15416352198531,-0.000201332531193781));
#48634=CARTESIAN_POINT('Ctrl Pts',(366.901319367511,-5.40416352200791,0.00345128679815413));
#48635=CARTESIAN_POINT('Ctrl Pts',(366.901443455985,-5.39702220615151,0.144859349802664));
#48636=CARTESIAN_POINT('Ctrl Pts',(366.909197595463,-5.38988089029511,0.285932128098977));
#48637=CARTESIAN_POINT('Ctrl Pts',(366.924451232584,-5.3827395744387,0.425948364013215));
#48638=CARTESIAN_POINT('Ctrl Pts',(366.939931375364,-5.37549221512269,0.568043741412952));
#48639=CARTESIAN_POINT('Ctrl Pts',(366.963135339812,-5.36824485580668,0.709051009431602));
#48640=CARTESIAN_POINT('Ctrl Pts',(366.993877818114,-5.36099749649067,0.848238962043237));
#48641=CARTESIAN_POINT('Ctrl Pts',(367.013804958674,-5.35629978974247,0.938459986797252));
#48642=CARTESIAN_POINT('Ctrl Pts',(367.036898477992,-5.35160208299428,1.02791707226206));
#48643=CARTESIAN_POINT('Ctrl Pts',(367.063097287595,-5.34690437624608,1.11641589265549));
#48644=CARTESIAN_POINT('Ctrl Pts',(367.09585447706,-5.34103068685561,1.22706873036475));
#48645=CARTESIAN_POINT('Ctrl Pts',(367.133540412026,-5.33515699746515,1.33646292607195));
#48646=CARTESIAN_POINT('Ctrl Pts',(367.176041344644,-5.32928330807468,1.44412672116065));
#48647=CARTESIAN_POINT('Ctrl Pts',(367.218487404565,-5.32341720216902,1.55165151217537));
#48648=CARTESIAN_POINT('Ctrl Pts',(367.265735949017,-5.31755109626336,1.65744996470677));
#48649=CARTESIAN_POINT('Ctrl Pts',(367.317623124065,-5.3116849903577,1.76106421856329));
#48650=CARTESIAN_POINT('Ctrl Pts',(367.369457167306,-5.30582489126976,1.86457237274395));
#48651=CARTESIAN_POINT('Ctrl Pts',(367.425920209307,-5.29996479218181,1.9659004097976));
#48652=CARTESIAN_POINT('Ctrl Pts',(367.486800106332,-5.29410469309386,2.06460987458795));
#48653=CARTESIAN_POINT('Ctrl Pts',(367.549876411155,-5.28803317499972,2.16688055167779));
#48654=CARTESIAN_POINT('Ctrl Pts',(367.617694122466,-5.28196165690558,2.26633972479832));
#48655=CARTESIAN_POINT('Ctrl Pts',(367.689964723536,-5.27589013881143,2.36252669737809));
#48656=CARTESIAN_POINT('Ctrl Pts',(367.759638584152,-5.27003677521478,2.45525759516031));
#48657=CARTESIAN_POINT('Ctrl Pts',(367.833450580304,-5.26418341161812,2.54494703253149));
#48658=CARTESIAN_POINT('Ctrl Pts',(367.911098241926,-5.25833004802147,2.63121190787158));
#48659=CARTESIAN_POINT('Ctrl Pts',(367.988734245014,-5.25247756328766,2.71746383083095));
#48660=CARTESIAN_POINT('Ctrl Pts',(368.070204492117,-5.24662507855384,2.80029190716569));
#48661=CARTESIAN_POINT('Ctrl Pts',(368.155167276245,-5.24077259382003,2.8793473541535));
#48662=CARTESIAN_POINT('Ctrl Pts',(368.240137850318,-5.23491957249195,2.95841004946434));
#48663=CARTESIAN_POINT('Ctrl Pts',(368.3286012955,-5.22906655116387,3.03369914636362));
#48664=CARTESIAN_POINT('Ctrl Pts',(368.420180750793,-5.22321352983579,3.104904354512));
#48665=CARTESIAN_POINT('Ctrl Pts',(368.511790749603,-5.21735855641207,3.1761333109724));
#48666=CARTESIAN_POINT('Ctrl Pts',(368.606518499045,-5.21150358298834,3.24327541683681));
#48667=CARTESIAN_POINT('Ctrl Pts',(368.703956519332,-5.20564860956462,3.30606255038524));
#48668=CARTESIAN_POINT('Ctrl Pts',(368.8015049731,-5.19978700028055,3.36892084508492));
#48669=CARTESIAN_POINT('Ctrl Pts',(368.901769481247,-5.19392539099649,3.42741409199497));
#48670=CARTESIAN_POINT('Ctrl Pts',(369.004316140376,-5.18806378171242,3.48131910789192));
#48671=CARTESIAN_POINT('Ctrl Pts',(369.106931947471,-5.18219821990216,3.53526047233701));
#48672=CARTESIAN_POINT('Ctrl Pts',(369.211832596861,-5.17633265809191,3.58460726974429));
#48673=CARTESIAN_POINT('Ctrl Pts',(369.318563897641,-5.17046709628165,3.62918433620219));
#48674=CARTESIAN_POINT('Ctrl Pts',(369.425451265761,-5.1645929575814,3.67382658526451));
#48675=CARTESIAN_POINT('Ctrl Pts',(369.534174241206,-5.15871881888115,3.7136850423363));
#48676=CARTESIAN_POINT('Ctrl Pts',(369.64426310874,-5.15284468018091,3.7486342453127));
#48677=CARTESIAN_POINT('Ctrl Pts',(369.672102786142,-5.15135920639875,3.75747232820079));
#48678=CARTESIAN_POINT('Ctrl Pts',(369.700029762253,-5.14987373261658,3.76599671886946));
#48679=CARTESIAN_POINT('Ctrl Pts',(369.728036351832,-5.14838825883442,3.77420590848957));
#48680=CARTESIAN_POINT('Ctrl Pts',(369.838776783638,-5.14251456944392,3.80666574087116));
#48681=CARTESIAN_POINT('Ctrl Pts',(369.951131488505,-5.13664088005343,3.83430158793247));
#48682=CARTESIAN_POINT('Ctrl Pts',(370.064642380177,-5.13076719066293,3.8569532880488));
#48683=CARTESIAN_POINT('Ctrl Pts',(370.178006718624,-5.12490108475724,3.87957574269224));
#48684=CARTESIAN_POINT('Ctrl Pts',(370.292523873838,-5.11903497885156,3.89722676738695));
#48685=CARTESIAN_POINT('Ctrl Pts',(370.407720275528,-5.11316887294588,3.90979583951695));
#48686=CARTESIAN_POINT('Ctrl Pts',(370.522798717571,-5.10730877385791,3.92235204107722));
#48687=CARTESIAN_POINT('Ctrl Pts',(370.638554614338,-5.10144867476994,3.9298365964251));
#48688=CARTESIAN_POINT('Ctrl Pts',(370.754504523402,-5.09558857568197,3.93219008090691));
#48689=CARTESIAN_POINT('Ctrl Pts',(370.874637640662,-5.08951705758784,3.9346284737397));
#48690=CARTESIAN_POINT('Ctrl Pts',(370.994978590628,-5.08344553949371,3.93155848245066));
#48691=CARTESIAN_POINT('Ctrl Pts',(371.114983838692,-5.07737402139957,3.92297280191965));
#48692=CARTESIAN_POINT('Ctrl Pts',(371.230677202285,-5.0715206578029,3.91469561175176));
#48693=CARTESIAN_POINT('Ctrl Pts',(371.34605812546,-5.06566729420622,3.90129230920273));
#48694=CARTESIAN_POINT('Ctrl Pts',(371.46064071302,-5.05981393060954,3.88280937921204));
#48695=CARTESIAN_POINT('Ctrl Pts',(371.57520609639,-5.05396144587571,3.86432922437107));
#48696=CARTESIAN_POINT('Ctrl Pts',(371.688972974722,-5.04810896114188,3.84077102437545));
#48697=CARTESIAN_POINT('Ctrl Pts',(371.801463020548,-5.04225647640805,3.81223283986203));
#48698=CARTESIAN_POINT('Ctrl Pts',(371.9139633802,-5.03640345507995,3.78369203878026));
#48699=CARTESIAN_POINT('Ctrl Pts',(372.025186274143,-5.03055043375185,3.75017044710723));
#48700=CARTESIAN_POINT('Ctrl Pts',(372.13466666304,-5.02469741242375,3.71181653275185));
#48701=CARTESIAN_POINT('Ctrl Pts',(372.244183565761,-5.018842439,3.67344982662537));
#48702=CARTESIAN_POINT('Ctrl Pts',(372.351956418126,-5.01298746557626,3.63024772959922));
#48703=CARTESIAN_POINT('Ctrl Pts',(372.457539016682,-5.00713249215252,3.58240729880111));
#48704=CARTESIAN_POINT('Ctrl Pts',(372.563241279551,-5.00127088286844,3.53451264701955));
#48705=CARTESIAN_POINT('Ctrl Pts',(372.666747957422,-4.99540927358436,3.48196933950716));
#48706=CARTESIAN_POINT('Ctrl Pts',(372.76763628452,-4.98954766430028,3.42502099894465));
#48707=CARTESIAN_POINT('Ctrl Pts',(372.868592641358,-4.98368210249002,3.36803425769789));
#48708=CARTESIAN_POINT('Ctrl Pts',(372.966926782199,-4.97781654067976,3.30663678705056));
#48709=CARTESIAN_POINT('Ctrl Pts',(373.062245294225,-4.97195097886949,3.24111528916138));
#48710=CARTESIAN_POINT('Ctrl Pts',(373.157703185293,-4.96607684016924,3.17549798277209));
#48711=CARTESIAN_POINT('Ctrl Pts',(373.250136318602,-4.96020270146898,3.10574486200673));
#48712=CARTESIAN_POINT('Ctrl Pts',(373.339184630263,-4.95432856276873,3.03218261806313));
#48713=CARTESIAN_POINT('Ctrl Pts',(373.361703494569,-4.95284308898674,3.01357992747338));
#48714=CARTESIAN_POINT('Ctrl Pts',(373.384006086301,-4.95135761520476,2.9947338235578));
#48715=CARTESIAN_POINT('Ctrl Pts',(373.406086971337,-4.94987214142277,2.97564994633422));
#48716=CARTESIAN_POINT('Ctrl Pts',(373.493396664552,-4.94399845203163,2.90019067633606));
#48717=CARTESIAN_POINT('Ctrl Pts',(373.577527837825,-4.93812476264049,2.82075979169304));
#48718=CARTESIAN_POINT('Ctrl Pts',(373.658097573172,-4.93225107324935,2.73765540074166));
#48719=CARTESIAN_POINT('Ctrl Pts',(373.738563285421,-4.92638496734302,2.65465830536628));
#48720=CARTESIAN_POINT('Ctrl Pts',(373.815476419005,-4.92051886143669,2.56799742955658));
#48721=CARTESIAN_POINT('Ctrl Pts',(373.888487373944,-4.91465275553036,2.4780108027816));
#48722=CARTESIAN_POINT('Ctrl Pts',(373.961423566596,-4.90879265644175,2.38811632116605));
#48723=CARTESIAN_POINT('Ctrl Pts',(374.030465269786,-4.90293255735314,2.2949031813806));
#48724=CARTESIAN_POINT('Ctrl Pts',(374.095300469772,-4.89707245826453,2.19874540922173));
#48725=CARTESIAN_POINT('Ctrl Pts',(374.162474775852,-4.89100094017063,2.09911848402769));
#48726=CARTESIAN_POINT('Ctrl Pts',(374.225133011615,-4.88492942207674,1.99633076795799));
#48727=CARTESIAN_POINT('Ctrl Pts',(374.282974383232,-4.87885790398285,1.89083503723376));
#48728=CARTESIAN_POINT('Ctrl Pts',(374.338737468149,-4.87300454038553,1.78912985241094));
#48729=CARTESIAN_POINT('Ctrl Pts',(374.390023663683,-4.8671511767882,1.68490829944616));
#48730=CARTESIAN_POINT('Ctrl Pts',(374.436608623086,-4.86129781319088,1.57860387981518));
#48731=CARTESIAN_POINT('Ctrl Pts',(374.483186587914,-4.8554453284564,1.47231542143513));
#48732=CARTESIAN_POINT('Ctrl Pts',(374.525064554373,-4.84959284372192,1.36394509652811));
#48733=CARTESIAN_POINT('Ctrl Pts',(374.562065617717,-4.84374035898745,1.2539480070243));
#48734=CARTESIAN_POINT('Ctrl Pts',(374.599070073561,-4.8378873376587,1.14394083226427));
#48735=CARTESIAN_POINT('Ctrl Pts',(374.631196605674,-4.83203431632996,1.03230698801189));
#48736=CARTESIAN_POINT('Ctrl Pts',(374.658317870557,-4.82618129500121,0.919517736337605));
#48737=CARTESIAN_POINT('Ctrl Pts',(374.685448180905,-4.82032632157682,0.806690867269793));
#48738=CARTESIAN_POINT('Ctrl Pts',(374.70756980805,-4.81447134815243,0.692708226005589));
#48739=CARTESIAN_POINT('Ctrl Pts',(374.724606449506,-4.80861637472804,0.578051587351353));
#48740=CARTESIAN_POINT('Ctrl Pts',(374.741662399806,-4.80275476544333,0.463265000124452));
#48741=CARTESIAN_POINT('Ctrl Pts',(374.753621800706,-4.79689315615861,0.347803299717017));
#48742=CARTESIAN_POINT('Ctrl Pts',(374.760460184908,-4.7910315468739,0.232153809697238));
#48743=CARTESIAN_POINT('Ctrl Pts',(374.767303180283,-4.785165985063,0.116426336377062));
#48744=CARTESIAN_POINT('Ctrl Pts',(374.769018276898,-4.7793004232521,0.000511233377731596));
#48745=CARTESIAN_POINT('Ctrl Pts',(374.765633119996,-4.7734348614412,-0.115105487454939));
#48746=CARTESIAN_POINT('Ctrl Pts',(374.762243013165,-4.76756072274032,-0.230891268290099));
#48747=CARTESIAN_POINT('Ctrl Pts',(374.753737799107,-4.76168658403944,-0.346377385752583));
#48748=CARTESIAN_POINT('Ctrl Pts',(374.740196804942,-4.75581244533856,-0.461084172926413));
#48749=CARTESIAN_POINT('Ctrl Pts',(374.736772508589,-4.75432697156275,-0.490091646690872));
#48750=CARTESIAN_POINT('Ctrl Pts',(374.733026426693,-4.75284149778693,-0.519049341594463));
#48751=CARTESIAN_POINT('Ctrl Pts',(374.728960352713,-4.75135602401112,-0.547949633793531));
#48752=CARTESIAN_POINT('Ctrl Pts',(374.712882751089,-4.7454823346216,-0.662223842068144));
#48753=CARTESIAN_POINT('Ctrl Pts',(374.691744664624,-4.73960864523207,-0.775980165168239));
#48754=CARTESIAN_POINT('Ctrl Pts',(374.665589012611,-4.73373495584255,-0.888735226740352));
#48755=CARTESIAN_POINT('Ctrl Pts',(374.639467130002,-4.72786884993784,-1.00134471093508));
#48756=CARTESIAN_POINT('Ctrl Pts',(374.608340657263,-4.72200274403313,-1.11295510562042));
#48757=CARTESIAN_POINT('Ctrl Pts',(374.572304121735,-4.71613663812842,-1.22308939020026));
#48758=CARTESIAN_POINT('Ctrl Pts',(374.536304487161,-4.71027653904142,-1.33311089867579));
#48759=CARTESIAN_POINT('Ctrl Pts',(374.495404918309,-4.70441643995442,-1.44165891325449));
#48760=CARTESIAN_POINT('Ctrl Pts',(374.449750566373,-4.69855634086742,-1.54826848339961));
#48761=CARTESIAN_POINT('Ctrl Pts',(374.402449109563,-4.69248482277292,-1.6587242836469));
#48762=CARTESIAN_POINT('Ctrl Pts',(374.350043410704,-4.68641330467842,-1.76709868936488));
#48763=CARTESIAN_POINT('Ctrl Pts',(374.292750878012,-4.68034178658393,-1.87289348684141));
#48764=CARTESIAN_POINT('Ctrl Pts',(374.23751691182,-4.6744884229882,-1.97488699267111));
#48765=CARTESIAN_POINT('Ctrl Pts',(374.17774145742,-4.66863505939248,-2.074482680326));
#48766=CARTESIAN_POINT('Ctrl Pts',(374.113667168997,-4.66278169579675,-2.17125702419965));
#48767=CARTESIAN_POINT('Ctrl Pts',(374.049602501113,-4.65692921106386,-2.26801683773135));
#48768=CARTESIAN_POINT('Ctrl Pts',(373.981240510635,-4.65107672633098,-2.36195580539885));
#48769=CARTESIAN_POINT('Ctrl Pts',(373.908867721538,-4.64522424159809,-2.45267855766956));
#48770=CARTESIAN_POINT('Ctrl Pts',(373.836488296828,-4.63937122027092,-2.54340962799867));
#48771=CARTESIAN_POINT('Ctrl Pts',(373.760097600132,-4.63351819894376,-2.63092357374349));
#48772=CARTESIAN_POINT('Ctrl Pts',(373.680022602544,-4.62766517761659,-2.71485791151199));
#48773=CARTESIAN_POINT('Ctrl Pts',(373.599920898397,-4.62181020419378,-2.79882024300317));
#48774=CARTESIAN_POINT('Ctrl Pts',(373.516132735004,-4.61595523077096,-2.87920029379615));
#48775=CARTESIAN_POINT('Ctrl Pts',(373.429021587211,-4.61010025734814,-2.95567277160947));
#48776=CARTESIAN_POINT('Ctrl Pts',(373.341811710121,-4.60423864806497,-3.03223192115416));
#48777=CARTESIAN_POINT('Ctrl Pts',(373.251271642225,-4.59837703878179,-3.10487438552158));
#48778=CARTESIAN_POINT('Ctrl Pts',(373.157797621388,-4.59251542949862,-3.17331542191015));
#48779=CARTESIAN_POINT('Ctrl Pts',(373.064260570332,-4.58664986768925,-3.24180260859232));
#48780=CARTESIAN_POINT('Ctrl Pts',(372.967785969897,-4.58078430587988,-3.30608249754257));
#48781=CARTESIAN_POINT('Ctrl Pts',(372.868797206398,-4.57491874407051,-3.3659148476317));
#48782=CARTESIAN_POINT('Ctrl Pts',(372.769663697049,-4.56904460537112,-3.42583468729174));
#48783=CARTESIAN_POINT('Ctrl Pts',(372.668009048907,-4.56317046667174,-3.48129381184849));
#48784=CARTESIAN_POINT('Ctrl Pts',(372.564279333832,-4.55729632797235,-3.53209884850545));
#48785=CARTESIAN_POINT('Ctrl Pts',(372.538047782114,-4.55581085418139,-3.54494661296339));
#48786=CARTESIAN_POINT('Ctrl Pts',(372.511683616958,-4.55432538039042,-3.55749699290363));
#48787=CARTESIAN_POINT('Ctrl Pts',(372.48519421699,-4.55283990659946,-3.56974736242754));
#48788=CARTESIAN_POINT('Ctrl Pts',(372.380452882276,-4.54696621720899,-3.61818636279197));
#48789=CARTESIAN_POINT('Ctrl Pts',(372.273403393574,-4.54109252781852,-3.66209224755465));
#48790=CARTESIAN_POINT('Ctrl Pts',(372.164475202786,-4.53521883842805,-3.70123903921455));
#48791=CARTESIAN_POINT('Ctrl Pts',(372.055687648526,-4.5293527325224,-3.74033528868866));
#48792=CARTESIAN_POINT('Ctrl Pts',(371.945026601111,-4.52348662661676,-3.77468452587795));
#48793=CARTESIAN_POINT('Ctrl Pts',(371.832944148865,-4.51762052071111,-3.80410758544697));
#48794=CARTESIAN_POINT('Ctrl Pts',(371.720976467621,-4.51176042162319,-3.83350051617779));
#48795=CARTESIAN_POINT('Ctrl Pts',(371.607590673886,-4.50590032253527,-3.85797719862695));
#48796=CARTESIAN_POINT('Ctrl Pts',(371.493256157088,-4.50004022344735,-3.87740755037443));
#48797=CARTESIAN_POINT('Ctrl Pts',(371.37479671176,-4.4939687053532,-3.89753890488576));
#48798=CARTESIAN_POINT('Ctrl Pts',(371.255319220426,-4.48789718725905,-3.91225278098011));
#48799=CARTESIAN_POINT('Ctrl Pts',(371.135360195041,-4.48182566916491,-3.92146178209518));
#48800=CARTESIAN_POINT('Ctrl Pts',(371.019711393311,-4.4759723055683,-3.93033989644025));
#48801=CARTESIAN_POINT('Ctrl Pts',(370.903615513057,-4.47011894197169,-3.9341018825666));
#48802=CARTESIAN_POINT('Ctrl Pts',(370.787559991312,-4.46426557837508,-3.93272204743095));
#48803=CARTESIAN_POINT('Ctrl Pts',(370.671521894914,-4.45841309364133,-3.93134241947289));
#48804=CARTESIAN_POINT('Ctrl Pts',(370.55552455798,-4.45256060890758,-3.92482251024321));
#48805=CARTESIAN_POINT('Ctrl Pts',(370.440055540005,-4.44670812417383,-3.91318875450386));
#48806=CARTESIAN_POINT('Ctrl Pts',(370.324575935072,-4.44085510284582,-3.90155393210533));
#48807=CARTESIAN_POINT('Ctrl Pts',(370.209625156478,-4.4350020815178,-3.88480437254318));
#48808=CARTESIAN_POINT('Ctrl Pts',(370.095685056001,-4.42914906018979,-3.86301832649884));
#48809=CARTESIAN_POINT('Ctrl Pts',(369.9817069543,-4.42329408676615,-3.84122501438746));
#48810=CARTESIAN_POINT('Ctrl Pts',(369.868740606561,-4.4174391133425,-3.8143919532035));
#48811=CARTESIAN_POINT('Ctrl Pts',(369.757256401613,-4.41158413991886,-3.78264822967379));
#48812=CARTESIAN_POINT('Ctrl Pts',(369.645645843639,-4.40572253063489,-3.75086852871079));
#48813=CARTESIAN_POINT('Ctrl Pts',(369.535521178845,-4.39986092135091,-3.71416716999359));
#48814=CARTESIAN_POINT('Ctrl Pts',(369.427336483157,-4.39399931206694,-3.67272275352827));
#48815=CARTESIAN_POINT('Ctrl Pts',(369.319078837735,-4.38813375025678,-3.63125039078861));
#48816=CARTESIAN_POINT('Ctrl Pts',(369.212764144155,-4.38226818844663,-3.58502876613611));
#48817=CARTESIAN_POINT('Ctrl Pts',(369.108823800672,-4.37640262663648,-3.53428341741415));
#48818=CARTESIAN_POINT('Ctrl Pts',(369.004731470915,-4.37052848793635,-3.48346386654634));
#48819=CARTESIAN_POINT('Ctrl Pts',(368.903020781746,-4.36465434923621,-3.42810758688272));
#48820=CARTESIAN_POINT('Ctrl Pts',(368.804096045641,-4.35878021053608,-3.36848458687471));
#48821=CARTESIAN_POINT('Ctrl Pts',(368.779079594812,-4.35729473675332,-3.35340690350991));
#48822=CARTESIAN_POINT('Ctrl Pts',(368.754241147519,-4.35580926297056,-3.33805656905904));
#48823=CARTESIAN_POINT('Ctrl Pts',(368.729586910349,-4.3543237891878,-3.32243836031665));
#48824=CARTESIAN_POINT('Ctrl Pts',(368.632101964404,-4.34845009979252,-3.26068263757823));
#48825=CARTESIAN_POINT('Ctrl Pts',(368.537174958848,-4.34257641039724,-3.19452990984391));
#48826=CARTESIAN_POINT('Ctrl Pts',(368.44522859431,-4.33670272100197,-3.12421854436291));
#48827=CARTESIAN_POINT('Ctrl Pts',(368.353400941165,-4.33083661509148,-3.05399795745991));
#48828=CARTESIAN_POINT('Ctrl Pts',(368.264546601244,-4.324970509181,-2.97962965904421));
#48829=CARTESIAN_POINT('Ctrl Pts',(368.179061209962,-4.31910440327052,-2.90139641524809));
#48830=CARTESIAN_POINT('Ctrl Pts',(368.093663354632,-4.31324430417774,-2.82324328129676));
#48831=CARTESIAN_POINT('Ctrl Pts',(368.011627889049,-4.30738420508496,-2.74123335133408));
#48832=CARTESIAN_POINT('Ctrl Pts',(367.933318582965,-4.30152410599219,-2.65569053806343));
#48833=CARTESIAN_POINT('Ctrl Pts',(367.85218405586,-4.29545258789985,-2.56706153534194));
#48834=CARTESIAN_POINT('Ctrl Pts',(367.775049985958,-4.28938106980751,-2.47464019400271));
#48835=CARTESIAN_POINT('Ctrl Pts',(367.702280661507,-4.28330955171518,-2.37882997074181));
#48836=CARTESIAN_POINT('Ctrl Pts',(367.632125996962,-4.2774561881137,-2.28646228527073));
#48837=CARTESIAN_POINT('Ctrl Pts',(367.566028089594,-4.27160282451223,-2.19094541443752));
#48838=CARTESIAN_POINT('Ctrl Pts',(367.504272773721,-4.26574946091075,-2.09267502696315));
#48839=CARTESIAN_POINT('Ctrl Pts',(367.4425267302,-4.25989697617212,-1.99441939445682));
#48840=CARTESIAN_POINT('Ctrl Pts',(367.38512220147,-4.2540444914335,-1.89341141707912));
#48841=CARTESIAN_POINT('Ctrl Pts',(367.332301284831,-4.24819200669487,-1.79007512543516));
#48842=CARTESIAN_POINT('Ctrl Pts',(367.279475525224,-4.24233898536199,-1.68672935924111));
#48843=CARTESIAN_POINT('Ctrl Pts',(367.231234401187,-4.23648596402912,-1.58105522230436));
#48844=CARTESIAN_POINT('Ctrl Pts',(367.187773374491,-4.23063294269625,-1.47350003889497));
#48845=CARTESIAN_POINT('Ctrl Pts',(367.144297852704,-4.22477796926775,-1.36590898375529));
#48846=CARTESIAN_POINT('Ctrl Pts',(367.105605753064,-4.21892299583925,-1.25643601750229));
#48847=CARTESIAN_POINT('Ctrl Pts',(367.071843605239,-4.21306802241076,-1.14554639070291));
#48848=CARTESIAN_POINT('Ctrl Pts',(367.038043192357,-4.20720641312197,-1.03453108475579));
#48849=CARTESIAN_POINT('Ctrl Pts',(367.009184003941,-4.20134480383319,-0.922096309028896));
#48850=CARTESIAN_POINT('Ctrl Pts',(366.985362119881,-4.19548319454441,-0.808720447848522));
#48851=CARTESIAN_POINT('Ctrl Pts',(366.961524172551,-4.18961763272946,-0.695268136492842));
#48852=CARTESIAN_POINT('Ctrl Pts',(366.942730359955,-4.18375207091451,-0.580873882763329));
#48853=CARTESIAN_POINT('Ctrl Pts',(366.929025025973,-4.17788650909957,-0.466022460209995));
#48854=CARTESIAN_POINT('Ctrl Pts',(366.915299651431,-4.17201237039471,-0.351003096709402));
#48855=CARTESIAN_POINT('Ctrl Pts',(366.906677635719,-4.16613823168985,-0.235525640655453));
#48856=CARTESIAN_POINT('Ctrl Pts',(366.903151270257,-4.160264092985,-0.120076213144621));
#48857=CARTESIAN_POINT('Ctrl Pts',(366.902259510027,-4.15877861924871,-0.0908809385600446));
#48858=CARTESIAN_POINT('Ctrl Pts',(366.901693358034,-4.15729314551243,-0.061687434995945));
#48859=CARTESIAN_POINT('Ctrl Pts',(366.90145216495,-4.15580767177615,-0.0325035074416985));
#48860=CARTESIAN_POINT('Ctrl Pts',(366.901363179298,-4.15525962186242,-0.0217364042693529));
#48861=CARTESIAN_POINT('Ctrl Pts',(366.90131840958,-4.15471157194869,-0.0109689351661175));
#48862=CARTESIAN_POINT('Ctrl Pts',(366.901317858377,-4.15416352203497,-0.000201333506838279));
#48863=CARTESIAN_POINT('',(366.901319261778,-2.90416352206856,-0.00332861608659438));
#48864=CARTESIAN_POINT('Ctrl Pts',(366.901317858377,-4.15416352198531,-0.000201332531196401));
#48865=CARTESIAN_POINT('Ctrl Pts',(366.901311959597,-4.14829845024365,0.115030427635469));
#48866=CARTESIAN_POINT('Ctrl Pts',(366.906374564303,-4.14243337850199,0.230457043287648));
#48867=CARTESIAN_POINT('Ctrl Pts',(366.916531103072,-4.13656830676033,0.3455951103968));
#48868=CARTESIAN_POINT('Ctrl Pts',(366.926674528538,-4.13071080752541,0.460584520536864));
#48869=CARTESIAN_POINT('Ctrl Pts',(366.941898773558,-4.12485330829048,0.575285713870508));
#48870=CARTESIAN_POINT('Ctrl Pts',(366.962177279116,-4.11899580905555,0.689214316700083));
#48871=CARTESIAN_POINT('Ctrl Pts',(366.98243506294,-4.11314429534733,0.803026500787282));
#48872=CARTESIAN_POINT('Ctrl Pts',(367.007736762632,-4.10729278163911,0.916067258950138));
#48873=CARTESIAN_POINT('Ctrl Pts',(367.038004001566,-4.10144126793088,1.02785706190746));
#48874=CARTESIAN_POINT('Ctrl Pts',(367.069071559755,-4.09543502986562,1.14260278469151));
#48875=CARTESIAN_POINT('Ctrl Pts',(367.105370893532,-4.08942879180035,1.256030028129));
#48876=CARTESIAN_POINT('Ctrl Pts',(367.146761046028,-4.08342255373508,1.36763072270954));
#48877=CARTESIAN_POINT('Ctrl Pts',(367.187039217511,-4.07757767827118,1.47623317143383));
#48878=CARTESIAN_POINT('Ctrl Pts',(367.23213798919,-4.07173280280727,1.58310555597647));
#48879=CARTESIAN_POINT('Ctrl Pts',(367.281877114629,-4.06588792734336,1.68779554412487));
#48880=CARTESIAN_POINT('Ctrl Pts',(367.331609051504,-4.06004389661206,1.79247040191723));
#48881=CARTESIAN_POINT('Ctrl Pts',(367.385979830845,-4.05419986588076,1.89496311613479));
#48882=CARTESIAN_POINT('Ctrl Pts',(367.444761818848,-4.04835583514946,1.99484307398559));
#48883=CARTESIAN_POINT('Ctrl Pts',(367.503549640188,-4.04251122447522,2.09473294360429));
#48884=CARTESIAN_POINT('Ctrl Pts',(367.566749330053,-4.03666661380098,2.19200918422794));
#48885=CARTESIAN_POINT('Ctrl Pts',(367.634088602332,-4.03082200312674,2.28626808177333));
#48886=CARTESIAN_POINT('Ctrl Pts',(367.704687643426,-4.02469446572989,2.3850898770798));
#48887=CARTESIAN_POINT('Ctrl Pts',(367.779836810539,-4.01856692833304,2.48059445845192));
#48888=CARTESIAN_POINT('Ctrl Pts',(367.859173997445,-4.01243939093618,2.57235457070331));
#48889=CARTESIAN_POINT('Ctrl Pts',(367.934961989404,-4.00658597246905,2.66000974125744));
#48890=CARTESIAN_POINT('Ctrl Pts',(368.014571057159,-4.00073255400193,2.74424795993098));
#48891=CARTESIAN_POINT('Ctrl Pts',(368.097647806168,-3.9948791355348,2.82473468728379));
#48892=CARTESIAN_POINT('Ctrl Pts',(368.180782445084,-3.98902163826277,2.90527749975334));
#48893=CARTESIAN_POINT('Ctrl Pts',(368.267389266849,-3.98316414099074,2.98206334218022));
#48894=CARTESIAN_POINT('Ctrl Pts',(368.357082035874,-3.97730664371871,3.05479814476148));
#48895=CARTESIAN_POINT('Ctrl Pts',(368.446903188543,-3.97144076219393,3.12763705784251));
#48896=CARTESIAN_POINT('Ctrl Pts',(368.539818769934,-3.96557488066915,3.19641311649315));
#48897=CARTESIAN_POINT('Ctrl Pts',(368.63541389815,-3.95970899914438,3.26087571004458));
#48898=CARTESIAN_POINT('Ctrl Pts',(368.648546106992,-3.95890318421775,3.26973114291913));
#48899=CARTESIAN_POINT('Ctrl Pts',(368.661728846035,-3.95809736929113,3.27850524631598));
#48900=CARTESIAN_POINT('Ctrl Pts',(368.674961006031,-3.9572915543645,3.28719743953404));
#48901=CARTESIAN_POINT('Ctrl Pts',(368.771411934462,-3.95141786497133,3.35055596197065));
#48902=CARTESIAN_POINT('Ctrl Pts',(368.870814404899,-3.94554417557816,3.40977140443023));
#48903=CARTESIAN_POINT('Ctrl Pts',(368.972776994441,-3.93967048618499,3.46455691699257));
#48904=CARTESIAN_POINT('Ctrl Pts',(369.074607940699,-3.93380438027672,3.5192716963105));
#48905=CARTESIAN_POINT('Ctrl Pts',(369.178992072182,-3.92793827436845,3.56956772609239));
#48906=CARTESIAN_POINT('Ctrl Pts',(369.285508672368,-3.92207216846018,3.61520111768304));
#48907=CARTESIAN_POINT('Ctrl Pts',(369.391916200911,-3.91621206936971,3.66078778126142));
#48908=CARTESIAN_POINT('Ctrl Pts',(369.500451477251,-3.91035197027924,3.70172114176048));
#48909=CARTESIAN_POINT('Ctrl Pts',(369.610669433267,-3.90449187118878,3.7378033046614));
#48910=CARTESIAN_POINT('Ctrl Pts',(369.724863801624,-3.89842035309561,3.77518722966189));
#48911=CARTESIAN_POINT('Ctrl Pts',(369.840864158629,-3.89234883500245,3.80736309407966));
#48912=CARTESIAN_POINT('Ctrl Pts',(369.958152751656,-3.88627731690928,3.83416532178712));
#48913=CARTESIAN_POINT('Ctrl Pts',(370.071227071861,-3.88042395331036,3.86000452404688));
#48914=CARTESIAN_POINT('Ctrl Pts',(370.185498209295,-3.87457058971143,3.88084950207189));
#48915=CARTESIAN_POINT('Ctrl Pts',(370.300487848205,-3.8687172261125,3.89660294689376));
#48916=CARTESIAN_POINT('Ctrl Pts',(370.415460221806,-3.86286474137651,3.91235402638865));
#48917=CARTESIAN_POINT('Ctrl Pts',(370.531150473165,-3.85701225664053,3.9230150366856));
#48918=CARTESIAN_POINT('Ctrl Pts',(370.647072476559,-3.85115977190454,3.92854020838753));
#48919=CARTESIAN_POINT('Ctrl Pts',(370.763005108442,-3.84530675057437,3.93406588667342));
#48920=CARTESIAN_POINT('Ctrl Pts',(370.879169121901,-3.83945372924421,3.93445477061384));
#48921=CARTESIAN_POINT('Ctrl Pts',(370.995076393649,-3.83360070791404,3.92971318185953));
#48922=CARTESIAN_POINT('Ctrl Pts',(371.111022322708,-3.82774573448833,3.92497001169388));
#48923=CARTESIAN_POINT('Ctrl Pts',(371.226710927212,-3.82189076106261,3.91509298324222));
#48924=CARTESIAN_POINT('Ctrl Pts',(371.341657923126,-3.8160357876369,3.90014038894392));
#48925=CARTESIAN_POINT('Ctrl Pts',(371.456735196693,-3.810174178351,3.88517084780096));
#48926=CARTESIAN_POINT('Ctrl Pts',(371.571068774125,-3.8043125690651,3.86511431248785));
#48927=CARTESIAN_POINT('Ctrl Pts',(371.684183202654,-3.7984509597792,3.84008045330274));
#48928=CARTESIAN_POINT('Ctrl Pts',(371.797373905072,-3.79258539796719,3.81502971360289));
#48929=CARTESIAN_POINT('Ctrl Pts',(371.909343423589,-3.78671983615519,3.78499507377374));
#48930=CARTESIAN_POINT('Ctrl Pts',(372.019631811733,-3.78085427434318,3.75013597350344));
#48931=CARTESIAN_POINT('Ctrl Pts',(372.130081468547,-3.77498013564133,3.71522590067961));
#48932=CARTESIAN_POINT('Ctrl Pts',(372.238844702436,-3.76910599693947,3.6754774295862));
#48933=CARTESIAN_POINT('Ctrl Pts',(372.345481797028,-3.76323185823761,3.6310979792545));
#48934=CARTESIAN_POINT('Ctrl Pts',(372.372448577023,-3.76174638447602,3.61987514091721));
#48935=CARTESIAN_POINT('Ctrl Pts',(372.399279516508,-3.76026091071442,3.60835637822555));
#48936=CARTESIAN_POINT('Ctrl Pts',(372.425967772208,-3.75877543695283,3.59654550025402));
#48937=CARTESIAN_POINT('Ctrl Pts',(372.531495402127,-3.7529017475244,3.54984428554702));
#48938=CARTESIAN_POINT('Ctrl Pts',(372.635141628382,-3.74702805809597,3.49841686381751));
#48939=CARTESIAN_POINT('Ctrl Pts',(372.736453214653,-3.74115436866754,3.44243664673768));
#48940=CARTESIAN_POINT('Ctrl Pts',(372.837633998151,-3.73528826272376,3.38652870537523));
#48941=CARTESIAN_POINT('Ctrl Pts',(372.936485777689,-3.72942215677999,3.32607985623519));
#48942=CARTESIAN_POINT('Ctrl Pts',(373.032575537284,-3.72355605083621,3.2613114163583));
#48943=CARTESIAN_POINT('Ctrl Pts',(373.128566902192,-3.71769595171007,3.19660929853737));
#48944=CARTESIAN_POINT('Ctrl Pts',(373.221801532277,-3.71183585258392,3.12759661764766));
#48945=CARTESIAN_POINT('Ctrl Pts',(373.311871859558,-3.70597575345778,3.054540087427));
#48946=CARTESIAN_POINT('Ctrl Pts',(373.405191717938,-3.69990423537792,2.97884784493447));
#48947=CARTESIAN_POINT('Ctrl Pts',(373.495114245767,-3.69383271729806,2.89881467686671));
#48948=CARTESIAN_POINT('Ctrl Pts',(373.581219629511,-3.6877611992182,2.81478589442051));
#48949=CARTESIAN_POINT('Ctrl Pts',(373.66423117874,-3.68190783558331,2.73377633256367));
#48950=CARTESIAN_POINT('Ctrl Pts',(373.743694848106,-3.67605447194841,2.64905365930637));
#48951=CARTESIAN_POINT('Ctrl Pts',(373.8192695686,-3.67020110831352,2.56096705501544));
#48952=CARTESIAN_POINT('Ctrl Pts',(373.894832941803,-3.66434862354153,2.47289367663253));
#48953=CARTESIAN_POINT('Ctrl Pts',(373.966508258225,-3.65849613876954,2.38145768498292));
#48954=CARTESIAN_POINT('Ctrl Pts',(374.033993524102,-3.65264365399755,2.28704276330604));
#48955=CARTESIAN_POINT('Ctrl Pts',(374.101484977471,-3.64679063263138,2.19261918505006));
#48956=CARTESIAN_POINT('Ctrl Pts',(374.16478537634,-3.64093761126521,2.09521646994503));
#48957=CARTESIAN_POINT('Ctrl Pts',(374.223635416565,-3.63508458989904,1.99524821885047));
#48958=CARTESIAN_POINT('Ctrl Pts',(374.282505084414,-3.62922961643737,1.89524662641627));
#48959=CARTESIAN_POINT('Ctrl Pts',(374.336921232713,-3.6233746429757,1.79267815240053));
#48960=CARTESIAN_POINT('Ctrl Pts',(374.386670310075,-3.61751966951403,1.68798134536712));
#48961=CARTESIAN_POINT('Ctrl Pts',(374.436475771622,-3.61165806019242,1.58316587795847));
#48962=CARTESIAN_POINT('Ctrl Pts',(374.481603427243,-3.6057964508708,1.47621763631053));
#48963=CARTESIAN_POINT('Ctrl Pts',(374.521887686282,-3.59993484154919,1.36759560043147));
#48964=CARTESIAN_POINT('Ctrl Pts',(374.562199109291,-3.59406927970158,1.25890031991987));
#48965=CARTESIAN_POINT('Ctrl Pts',(374.597660506445,-3.58820371785396,1.14852939014922));
#48966=CARTESIAN_POINT('Ctrl Pts',(374.628156514806,-3.58233815600635,1.03695574152775));
#48967=CARTESIAN_POINT('Ctrl Pts',(374.658697115807,-3.57646401726932,0.925218944878658));
#48968=CARTESIAN_POINT('Ctrl Pts',(374.684257746806,-3.57058987853229,0.812276320921258));
#48969=CARTESIAN_POINT('Ctrl Pts',(374.704774329213,-3.56471573979525,0.698609810607917));
#48970=CARTESIAN_POINT('Ctrl Pts',(374.709962636666,-3.56323026637723,0.66986541297809));
#48971=CARTESIAN_POINT('Ctrl Pts',(374.71482863628,-3.56174479295921,0.641074739808487));
#48972=CARTESIAN_POINT('Ctrl Pts',(374.719371819044,-3.56025931954118,0.612245606488703));
#48973=CARTESIAN_POINT('Ctrl Pts',(374.737335953332,-3.55438563024687,0.49825274085406));
#48974=CARTESIAN_POINT('Ctrl Pts',(374.750308692182,-3.54851194095256,0.383278711694387));
#48975=CARTESIAN_POINT('Ctrl Pts',(374.758190051055,-3.54263825165825,0.267798385142579));
#48976=CARTESIAN_POINT('Ctrl Pts',(374.766061234354,-3.53677214584872,0.152467154543017));
#48977=CARTESIAN_POINT('Ctrl Pts',(374.76885408224,-3.53090604003919,0.0366313349230434));
#48978=CARTESIAN_POINT('Ctrl Pts',(374.766519827068,-3.52503993422966,-0.0792252289365442));
#48979=CARTESIAN_POINT('Ctrl Pts',(374.764187962143,-3.5191798352377,-0.194963157151585));
#48980=CARTESIAN_POINT('Ctrl Pts',(374.756739445294,-3.51331973624574,-0.310721376748395));
#48981=CARTESIAN_POINT('Ctrl Pts',(374.744177451681,-3.50745963725378,-0.426012817119104));
#48982=CARTESIAN_POINT('Ctrl Pts',(374.731162249707,-3.5013881191236,-0.545463712304576));
#48983=CARTESIAN_POINT('Ctrl Pts',(374.712657608584,-3.49531660099342,-0.664413061049791));
#48984=CARTESIAN_POINT('Ctrl Pts',(374.688726111108,-3.48924508286325,-0.782320894232927));
#48985=CARTESIAN_POINT('Ctrl Pts',(374.665654491975,-3.48339171936158,-0.895992202218437));
#48986=CARTESIAN_POINT('Ctrl Pts',(374.637539376976,-3.47753835585991,-1.00869511198927));
#48987=CARTESIAN_POINT('Ctrl Pts',(374.604489288355,-3.47168499235824,-1.11995372659874));
#48988=CARTESIAN_POINT('Ctrl Pts',(374.57144416209,-3.46583250771889,-1.23119563611135));
#48989=CARTESIAN_POINT('Ctrl Pts',(374.533465653143,-3.45998002307955,-1.34099328571946));
#48990=CARTESIAN_POINT('Ctrl Pts',(374.490712459852,-3.4541275384402,-1.44888490937688));
#48991=CARTESIAN_POINT('Ctrl Pts',(374.447955346663,-3.44827451720597,-1.55678642525895));
#48992=CARTESIAN_POINT('Ctrl Pts',(374.400422831082,-3.44242149597174,-1.66278118367952));
#48993=CARTESIAN_POINT('Ctrl Pts',(374.348321893907,-3.43656847473752,-1.7664270723876));
#48994=CARTESIAN_POINT('Ctrl Pts',(374.296203580056,-3.4307135014069,-1.87010752901486));
#48995=CARTESIAN_POINT('Ctrl Pts',(374.239514000343,-3.42485852807629,-1.97143718925419));
#48996=CARTESIAN_POINT('Ctrl Pts',(374.178505902321,-3.41900355474567,-2.06999886286803));
#48997=CARTESIAN_POINT('Ctrl Pts',(374.117428659439,-3.41314194555319,-2.16867224350662));
#48998=CARTESIAN_POINT('Ctrl Pts',(374.052023346714,-3.40728033636072,-2.26457102445186));
#48999=CARTESIAN_POINT('Ctrl Pts',(373.98258588037,-3.40141872716824,-2.35730724116484));
#49000=CARTESIAN_POINT('Ctrl Pts',(373.913101591823,-3.39555316544878,-2.45010599060338));
#49001=CARTESIAN_POINT('Ctrl Pts',(373.839579997071,-3.38968760372932,-2.53973761080811));
#49002=CARTESIAN_POINT('Ctrl Pts',(373.762355963892,-3.38382204200986,-2.62584878134184));
#49003=CARTESIAN_POINT('Ctrl Pts',(373.685019010211,-3.37794790339858,-2.71208586755588));
#49004=CARTESIAN_POINT('Ctrl Pts',(373.603969101428,-3.3720737647873,-2.79479193651726));
#49005=CARTESIAN_POINT('Ctrl Pts',(373.519576478687,-3.36619962617602,-2.87365187772935));
#49006=CARTESIAN_POINT('Ctrl Pts',(373.498234948849,-3.36471415149385,-2.89359428186034));
#49007=CARTESIAN_POINT('Ctrl Pts',(373.476679806803,-3.36322867681169,-2.91329093417751));
#49008=CARTESIAN_POINT('Ctrl Pts',(373.454917343959,-3.36174320212952,-2.93273717014677));
#49009=CARTESIAN_POINT('Ctrl Pts',(373.368866770481,-3.35586951268532,-3.00962919147399));
#49010=CARTESIAN_POINT('Ctrl Pts',(373.279285834524,-3.34999582324112,-3.0828588019322));
#49011=CARTESIAN_POINT('Ctrl Pts',(373.186519367276,-3.34412213379692,-3.15208455427388));
#49012=CARTESIAN_POINT('Ctrl Pts',(373.093872670263,-3.3382560278383,-3.22122092965763));
#49013=CARTESIAN_POINT('Ctrl Pts',(372.998048949099,-3.33238992187967,-3.28636348224985));
#49014=CARTESIAN_POINT('Ctrl Pts',(372.899428344965,-3.32652381592105,-3.34720893535185));
#49015=CARTESIAN_POINT('Ctrl Pts',(372.800908727086,-3.32066371678092,-3.40799208347748));
#49016=CARTESIAN_POINT('Ctrl Pts',(372.699598272437,-3.31480361764079,-3.46448666878525));
#49017=CARTESIAN_POINT('Ctrl Pts',(372.595907991573,-3.30894351850066,-3.51643131377136));
#49018=CARTESIAN_POINT('Ctrl Pts',(372.488476803237,-3.30287200042638,-3.57025000238973));
#49019=CARTESIAN_POINT('Ctrl Pts',(372.378491191236,-3.29680048235209,-3.61918397922802));
#49020=CARTESIAN_POINT('Ctrl Pts',(372.266438822559,-3.29072896427781,-3.66299311072114));
#49021=CARTESIAN_POINT('Ctrl Pts',(372.158412583767,-3.28487560063129,-3.70522814560539));
#49022=CARTESIAN_POINT('Ctrl Pts',(372.04846597045,-3.27902223698476,-3.74270011324722));
#49023=CARTESIAN_POINT('Ctrl Pts',(371.937057713501,-3.27316887333824,-3.77524221746847));
#49024=CARTESIAN_POINT('Ctrl Pts',(371.825666184145,-3.26731638855549,-3.80777943559712));
#49025=CARTESIAN_POINT('Ctrl Pts',(371.712813843995,-3.26146390377275,-3.83538814630011));
#49026=CARTESIAN_POINT('Ctrl Pts',(371.598974750581,-3.25561141899,-3.85795137726281));
#49027=CARTESIAN_POINT('Ctrl Pts',(371.48512521967,-3.24975839761397,-3.88051667696704));
#49028=CARTESIAN_POINT('Ctrl Pts',(371.370289160928,-3.24390537623794,-3.89803549699331));
#49029=CARTESIAN_POINT('Ctrl Pts',(371.254950291026,-3.23805235486191,-3.91044209166542));
#49030=CARTESIAN_POINT('Ctrl Pts',(371.139572953405,-3.23219738139126,-3.92285282417422));
#49031=CARTESIAN_POINT('Ctrl Pts',(371.023692881719,-3.22634240792062,-3.93014789680099));
#49032=CARTESIAN_POINT('Ctrl Pts',(370.907797661072,-3.22048743444998,-3.9323135324944));
#49033=CARTESIAN_POINT('Ctrl Pts',(370.791771088114,-3.21462582512074,-3.93448162265704));
#49034=CARTESIAN_POINT('Ctrl Pts',(370.675729745229,-3.20876421579151,-3.93150866465489));
#49035=CARTESIAN_POINT('Ctrl Pts',(370.560160061085,-3.20290260646227,-3.92343299993888));
#49036=CARTESIAN_POINT('Ctrl Pts',(370.444512447474,-3.19703704460784,-3.91535188974426));
#49037=CARTESIAN_POINT('Ctrl Pts',(370.329337535343,-3.19117148275342,-3.90216126834876));
#49038=CARTESIAN_POINT('Ctrl Pts',(370.215113757659,-3.18530592089899,-3.88395098939671));
#49039=CARTESIAN_POINT('Ctrl Pts',(370.100722956831,-3.17943178215628,-3.86571408255599));
#49040=CARTESIAN_POINT('Ctrl Pts',(369.987286469281,-3.17355764341358,-3.84244295213291));
#49041=CARTESIAN_POINT('Ctrl Pts',(369.875269796099,-3.16768350467087,-3.81427789025974));
#49042=CARTESIAN_POINT('Ctrl Pts',(369.846942617182,-3.16619803135321,-3.80715540818438));
#49043=CARTESIAN_POINT('Ctrl Pts',(369.818706144067,-3.16471255803554,-3.79972020227127));
#49044=CARTESIAN_POINT('Ctrl Pts',(369.790567707011,-3.16322708471787,-3.79197503054557));
#49045=CARTESIAN_POINT('Ctrl Pts',(369.679305898748,-3.15735339503414,-3.76134995318948));
#49046=CARTESIAN_POINT('Ctrl Pts',(369.569207800241,-3.15147970535042,-3.7257728563648));
#49047=CARTESIAN_POINT('Ctrl Pts',(369.460747268587,-3.14560601566669,-3.68534840266416));
#49048=CARTESIAN_POINT('Ctrl Pts',(369.352426769633,-3.13973990946625,-3.64497614071789));
#49049=CARTESIAN_POINT('Ctrl Pts',(369.245740016573,-3.13387380326582,-3.59976911075438));
#49050=CARTESIAN_POINT('Ctrl Pts',(369.14114793337,-3.12800769706538,-3.54988233924749));
#49051=CARTESIAN_POINT('Ctrl Pts',(369.036662951102,-3.12214759768154,-3.50004665114697));
#49052=CARTESIAN_POINT('Ctrl Pts',(368.934268742962,-3.1162874982977,-3.44554092998064));
#49053=CARTESIAN_POINT('Ctrl Pts',(368.83440775927,-3.11042739891385,-3.38656885595178));
#49054=CARTESIAN_POINT('Ctrl Pts',(368.730944026211,-3.1043558809302,-3.32546920822455));
#49055=CARTESIAN_POINT('Ctrl Pts',(368.630200177461,-3.09828436294655,-3.25957500975565));
#49056=CARTESIAN_POINT('Ctrl Pts',(368.532642367994,-3.0922128449629,-3.18916587224481));
#49057=CARTESIAN_POINT('Ctrl Pts',(368.438589882107,-3.08635948106936,-3.1212865866377));
#49058=CARTESIAN_POINT('Ctrl Pts',(368.347498786021,-3.08050611717582,-3.04921149091342));
#49059=CARTESIAN_POINT('Ctrl Pts',(368.259757922272,-3.07465275328228,-2.97323563848114));
#49060=CARTESIAN_POINT('Ctrl Pts',(368.17203023252,-3.06880026825175,-2.89727119356892));
#49061=CARTESIAN_POINT('Ctrl Pts',(368.087652087142,-3.06294778322122,-2.81740742688554));
#49062=CARTESIAN_POINT('Ctrl Pts',(368.006978770004,-3.05709529819069,-2.73397928091984));
#49063=CARTESIAN_POINT('Ctrl Pts',(367.926298056214,-3.05124227656635,-2.65054348572035));
#49064=CARTESIAN_POINT('Ctrl Pts',(367.849323133129,-3.04538925494202,-2.56354295859619));
#49065=CARTESIAN_POINT('Ctrl Pts',(367.776371474784,-3.03953623331768,-2.47334852913671));
#49066=CARTESIAN_POINT('Ctrl Pts',(367.703395485661,-3.03368125959846,-2.38312401810635));
#49067=CARTESIAN_POINT('Ctrl Pts',(367.634445689133,-3.02782628587923,-2.28970380763392));
#49068=CARTESIAN_POINT('Ctrl Pts',(367.569797986701,-3.02197131216,-2.19349015066754));
#49069=CARTESIAN_POINT('Ctrl Pts',(367.505077014435,-3.01610970258316,-2.0971674479294));
#49070=CARTESIAN_POINT('Ctrl Pts',(367.444668098752,-3.01024809300633,-1.99804532264505));
#49071=CARTESIAN_POINT('Ctrl Pts',(367.388802718651,-3.00438648342949,-1.89655330993627));
#49072=CARTESIAN_POINT('Ctrl Pts',(367.332899668128,-2.99852092132768,-1.79499286044245));
#49073=CARTESIAN_POINT('Ctrl Pts',(367.281546436331,-2.99265535922588,-1.69105971096975));
#49074=CARTESIAN_POINT('Ctrl Pts',(367.234926881615,-2.98678979712407,-1.58520460303999));
#49075=CARTESIAN_POINT('Ctrl Pts',(367.188239157711,-2.98091565813626,-1.4791947090595));
#49076=CARTESIAN_POINT('Ctrl Pts',(367.146299074105,-2.97504151914846,-1.37125763143878));
#49077=CARTESIAN_POINT('Ctrl Pts',(367.109241094803,-2.96916738016065,-1.26186058812891));
#49078=CARTESIAN_POINT('Ctrl Pts',(367.099869755125,-2.96768190920917,-1.23419591585064));
#49079=CARTESIAN_POINT('Ctrl Pts',(367.090810371226,-2.96619643825769,-1.20643793410368));
#49080=CARTESIAN_POINT('Ctrl Pts',(367.082064599313,-2.96471096730621,-1.17859429767576));
#49081=CARTESIAN_POINT('Ctrl Pts',(367.040187967712,-2.95759821380612,-1.04527299491962));
#49082=CARTESIAN_POINT('Ctrl Pts',(367.005392554132,-2.95048546030604,-0.909628073109617));
#49083=CARTESIAN_POINT('Ctrl Pts',(366.977897824696,-2.94337270680596,-0.772342905429096));
#49084=CARTESIAN_POINT('Ctrl Pts',(366.950733234797,-2.93634535880723,-0.636706172292929));
#49085=CARTESIAN_POINT('Ctrl Pts',(366.930695083428,-2.92931801080851,-0.49946836452728));
#49086=CARTESIAN_POINT('Ctrl Pts',(366.917949055783,-2.92229066280978,-0.36130934450515));
#49087=CARTESIAN_POINT('Ctrl Pts',(366.906989537955,-2.91624828256271,-0.242514980872078));
#49088=CARTESIAN_POINT('Ctrl Pts',(366.901420577048,-2.91020590231564,-0.12303987234602));
#49089=CARTESIAN_POINT('Ctrl Pts',(366.901319261778,-2.90416352206856,-0.00332861608662543));
#49090=CARTESIAN_POINT('',(366.901318397982,-1.65416352199376,0.00207004085040813));
#49091=CARTESIAN_POINT('Ctrl Pts',(366.901319261778,-2.90416352203497,-0.00332861542100308));
#49092=CARTESIAN_POINT('Ctrl Pts',(366.901221605676,-2.89833937116086,0.112059094269534));
#49093=CARTESIAN_POINT('Ctrl Pts',(366.90620615245,-2.89251522028675,0.227532235631285));
#49094=CARTESIAN_POINT('Ctrl Pts',(366.916268663384,-2.88669106941264,0.342606984741543));
#49095=CARTESIAN_POINT('Ctrl Pts',(366.926328011892,-2.88086874894105,0.457645568389189));
#49096=CARTESIAN_POINT('Ctrl Pts',(366.941462116302,-2.87504642846945,0.572285592939777));
#49097=CARTESIAN_POINT('Ctrl Pts',(366.961614702161,-2.86922410799786,0.686046138208073));
#49098=CARTESIAN_POINT('Ctrl Pts',(366.981765953168,-2.86340217318109,0.799799148284504));
#49099=CARTESIAN_POINT('Ctrl Pts',(367.006934951835,-2.85758023836431,0.912672383610354));
#49100=CARTESIAN_POINT('Ctrl Pts',(367.037014036022,-2.85175830354753,1.02419369255015));
#49101=CARTESIAN_POINT('Ctrl Pts',(367.067098588865,-2.84593531024896,1.13573527709911));
#49102=CARTESIAN_POINT('Ctrl Pts',(367.102094892846,-2.84011231695039,1.2459240434281));
#49103=CARTESIAN_POINT('Ctrl Pts',(367.141845223444,-2.83428932365182,1.35430235853338));
#49104=CARTESIAN_POINT('Ctrl Pts',(367.18163849359,-2.82846004017431,1.46279774727414));
#49105=CARTESIAN_POINT('Ctrl Pts',(367.226195902583,-2.82263075669681,1.56947838606366));
#49106=CARTESIAN_POINT('Ctrl Pts',(367.275311231093,-2.8168014732193,1.67390587060044));
#49107=CARTESIAN_POINT('Ctrl Pts',(367.32445349731,-2.81096899262337,1.77839062924911));
#49108=CARTESIAN_POINT('Ctrl Pts',(367.378158467062,-2.80513651202745,1.88061940309016));
#49109=CARTESIAN_POINT('Ctrl Pts',(367.436174443088,-2.79930403143153,1.98017937676107));
#49110=CARTESIAN_POINT('Ctrl Pts',(367.494288052215,-2.79346173555352,2.07990689650603));
#49111=CARTESIAN_POINT('Ctrl Pts',(367.556726934978,-2.78761943967551,2.17695629228589));
#49112=CARTESIAN_POINT('Ctrl Pts',(367.623196376333,-2.7817771437975,2.27094426630184));
#49113=CARTESIAN_POINT('Ctrl Pts',(367.682291087978,-2.77658304582985,2.35450435209916));
#49114=CARTESIAN_POINT('Ctrl Pts',(367.744570876838,-2.7713889478622,2.43564496159557));
#49115=CARTESIAN_POINT('Ctrl Pts',(367.809803658402,-2.76619484989455,2.51412069823983));
#49116=CARTESIAN_POINT('Ctrl Pts',(367.883571451695,-2.76032115976456,2.60286414563765));
#49117=CARTESIAN_POINT('Ctrl Pts',(367.961371198811,-2.75444746963457,2.68850596907481));
#49118=CARTESIAN_POINT('Ctrl Pts',(368.042912203698,-2.74857377950458,2.77065759338757));
#49119=CARTESIAN_POINT('Ctrl Pts',(368.124347931416,-2.74270767286554,2.85270315216294));
#49120=CARTESIAN_POINT('Ctrl Pts',(368.209515022598,-2.73684156622651,2.93126718257746));
#49121=CARTESIAN_POINT('Ctrl Pts',(368.298082227265,-2.73097545958748,3.00599365428754));
#49122=CARTESIAN_POINT('Ctrl Pts',(368.38655874015,-2.72511535977305,3.08064360696428));
#49123=CARTESIAN_POINT('Ctrl Pts',(368.478428127287,-2.71925525995863,3.15146355242979));
#49124=CARTESIAN_POINT('Ctrl Pts',(368.573322426838,-2.71339516014421,3.21813434801291));
#49125=CARTESIAN_POINT('Ctrl Pts',(368.67164027959,-2.70732364232499,3.28721046211055));
#49126=CARTESIAN_POINT('Ctrl Pts',(368.77320511027,-2.70125212450577,3.35183207103601));
#49127=CARTESIAN_POINT('Ctrl Pts',(368.877570005795,-2.69518060668655,3.4116897370047));
#49128=CARTESIAN_POINT('Ctrl Pts',(368.978185003889,-2.68932724238497,3.46939667875951));
#49129=CARTESIAN_POINT('Ctrl Pts',(369.081401924361,-2.68347387808339,3.52267590578454));
#49130=CARTESIAN_POINT('Ctrl Pts',(369.186791656259,-2.67762051378181,3.57129478345251));
#49131=CARTESIAN_POINT('Ctrl Pts',(369.292165564081,-2.6717680283522,3.6199063610847));
#49132=CARTESIAN_POINT('Ctrl Pts',(369.399711259585,-2.66591554292259,3.66385880769255));
#49133=CARTESIAN_POINT('Ctrl Pts',(369.508977123804,-2.66006305749298,3.70296650686193));
#49134=CARTESIAN_POINT('Ctrl Pts',(369.618253006051,-2.65421003547893,3.74207779161616));
#49135=CARTESIAN_POINT('Ctrl Pts',(369.729248981531,-2.64835701346487,3.77634330669451));
#49136=CARTESIAN_POINT('Ctrl Pts',(369.841496321851,-2.64250399145082,3.80562667728218));
#49137=CARTESIAN_POINT('Ctrl Pts',(369.95378109862,-2.63664901735164,3.83491981438564));
#49138=CARTESIAN_POINT('Ctrl Pts',(370.067317670567,-2.63079404325247,3.85922739868144));
#49139=CARTESIAN_POINT('Ctrl Pts',(370.181625817804,-2.62493906915329,3.87846388495488));
#49140=CARTESIAN_POINT('Ctrl Pts',(370.296063518259,-2.61907745921268,3.89772217325005));
#49141=CARTESIAN_POINT('Ctrl Pts',(370.411274131767,-2.61321584927208,3.91189782341532));
#49142=CARTESIAN_POINT('Ctrl Pts',(370.526770894742,-2.60735423933147,3.92095700924261));
#49143=CARTESIAN_POINT('Ctrl Pts',(370.642345537823,-2.60148867687489,3.93002230372895));
#49144=CARTESIAN_POINT('Ctrl Pts',(370.758206302698,-2.59562311441832,3.9339642500285));
#49145=CARTESIAN_POINT('Ctrl Pts',(370.873866735968,-2.58975755196174,3.93280115005497));
#49146=CARTESIAN_POINT('Ctrl Pts',(370.98969629275,-2.58388341263499,3.93163634934813));
#49147=CARTESIAN_POINT('Ctrl Pts',(371.105324522356,-2.57800927330824,3.92535162681694));
#49148=CARTESIAN_POINT('Ctrl Pts',(371.220270322131,-2.57213513398149,3.91401707862201));
#49149=CARTESIAN_POINT('Ctrl Pts',(371.249338105845,-2.5706496668153,3.91115076949131));
#49150=CARTESIAN_POINT('Ctrl Pts',(371.278362303016,-2.5691641996491,3.90796178063672));
#49151=CARTESIAN_POINT('Ctrl Pts',(371.307335256849,-2.5676787324829,3.90445175868106));
#49152=CARTESIAN_POINT('Ctrl Pts',(371.421897327312,-2.56180504093109,3.89057276709056));
#49153=CARTESIAN_POINT('Ctrl Pts',(371.536038838117,-2.55593134937928,3.87162427043913));
#49154=CARTESIAN_POINT('Ctrl Pts',(371.649275677197,-2.55005765782746,3.84763989286235));
#49155=CARTESIAN_POINT('Ctrl Pts',(371.762366317211,-2.54419154974604,3.82368648129995));
#49156=CARTESIAN_POINT('Ctrl Pts',(371.874554207809,-2.53832544166461,3.79471020354817));
#49157=CARTESIAN_POINT('Ctrl Pts',(371.985360599952,-2.53245933358318,3.76079640438102));
#49158=CARTESIAN_POINT('Ctrl Pts',(372.096053528024,-2.52659923230772,3.72691733243144));
#49159=CARTESIAN_POINT('Ctrl Pts',(372.205367378757,-2.52073913103227,3.68811091595824));
#49160=CARTESIAN_POINT('Ctrl Pts',(372.312834498288,-2.51487902975682,3.64451334615041));
#49161=CARTESIAN_POINT('Ctrl Pts',(372.424178729803,-2.50880751247825,3.59934289841421));
#49162=CARTESIAN_POINT('Ctrl Pts',(372.533540022709,-2.50273599519969,3.5490291612744));
#49163=CARTESIAN_POINT('Ctrl Pts',(372.640416078535,-2.49666447792112,3.4937799301799));
#49164=CARTESIAN_POINT('Ctrl Pts',(372.743452044873,-2.49081111212182,3.4405158209155));
#49165=CARTESIAN_POINT('Ctrl Pts',(372.844177892854,-2.48495774632252,3.38266498762702));
#49166=CARTESIAN_POINT('Ctrl Pts',(372.942165512519,-2.47910438052322,3.32046190238743));
#49167=CARTESIAN_POINT('Ctrl Pts',(373.040138419707,-2.47325189358497,3.25826815670921));
#49168=CARTESIAN_POINT('Ctrl Pts',(373.135373567362,-2.46739940664672,3.19172367979328));
#49169=CARTESIAN_POINT('Ctrl Pts',(373.227470153504,-2.46154691970847,3.12110734638631));
#49170=CARTESIAN_POINT('Ctrl Pts',(373.319575183653,-2.45569389617654,3.05048453841917));
#49171=CARTESIAN_POINT('Ctrl Pts',(373.408540752363,-2.4498408726446,2.97578938321193));
#49172=CARTESIAN_POINT('Ctrl Pts',(373.493998160584,-2.44398784911266,2.89734182702733));
#49173=CARTESIAN_POINT('Ctrl Pts',(373.579484070446,-2.43813287348808,2.81886810711782));
#49174=CARTESIAN_POINT('Ctrl Pts',(373.661459189062,-2.4322778978635,2.73663977692442));
#49175=CARTESIAN_POINT('Ctrl Pts',(373.739591300248,-2.42642292223891,2.65101399430834));
#49176=CARTESIAN_POINT('Ctrl Pts',(373.817811963905,-2.42056131076958,2.56529116613026));
#49177=CARTESIAN_POINT('Ctrl Pts',(373.892180648096,-2.41469969930025,2.4761635053898));
#49178=CARTESIAN_POINT('Ctrl Pts',(373.962405049128,-2.40883808783092,2.38402170602979));
#49179=CARTESIAN_POINT('Ctrl Pts',(374.032676802894,-2.40297252384184,2.29181777490229));
#49180=CARTESIAN_POINT('Ctrl Pts',(374.098798473939,-2.39710695985277,2.19659599660529));
#49181=CARTESIAN_POINT('Ctrl Pts',(374.160521730394,-2.39124139586369,2.09877506357777));
#49182=CARTESIAN_POINT('Ctrl Pts',(374.22233524108,-2.38536725501087,2.00081109284468));
#49183=CARTESIAN_POINT('Ctrl Pts',(374.279737297431,-2.37949311415804,1.90024073979457));
#49184=CARTESIAN_POINT('Ctrl Pts',(374.332525991379,-2.37361897330521,1.79750627875001));
#49185=CARTESIAN_POINT('Ctrl Pts',(374.345875196357,-2.37213352056056,1.77152678813974));
#49186=CARTESIAN_POINT('Ctrl Pts',(374.358929628063,-2.3706480678159,1.74540899861485));
#49187=CARTESIAN_POINT('Ctrl Pts',(374.371686519428,-2.36916261507124,1.71916023667212));
#49188=CARTESIAN_POINT('Ctrl Pts',(374.422128995786,-2.36328893371683,1.61536907660059));
#49189=CARTESIAN_POINT('Ctrl Pts',(374.468083555297,-2.35741525236242,1.50918309354284));
#49190=CARTESIAN_POINT('Ctrl Pts',(374.509316010673,-2.35154157100801,1.40102731691575));
#49191=CARTESIAN_POINT('Ctrl Pts',(374.550495230961,-2.34567547314448,1.29301117985996));
#49192=CARTESIAN_POINT('Ctrl Pts',(374.58696432561,-2.33980937528096,1.18303068933183));
#49193=CARTESIAN_POINT('Ctrl Pts',(374.618535475887,-2.33394327741743,1.07153440650688));
#49194=CARTESIAN_POINT('Ctrl Pts',(374.650074297681,-2.32808318636828,0.960152294548065));
#49195=CARTESIAN_POINT('Ctrl Pts',(374.676725039331,-2.32222309531912,0.847257872808208));
#49196=CARTESIAN_POINT('Ctrl Pts',(374.698348623511,-2.31636300426997,0.733317943509966));
#49197=CARTESIAN_POINT('Ctrl Pts',(374.720752379135,-2.3102914831612,0.615267100944081));
#49198=CARTESIAN_POINT('Ctrl Pts',(374.737759210823,-2.30421996205244,0.496094305290207));
#49199=CARTESIAN_POINT('Ctrl Pts',(374.749271429024,-2.29814844094367,0.376334291991625));
#49200=CARTESIAN_POINT('Ctrl Pts',(374.760369983383,-2.29229508532721,0.260877566418002));
#49201=CARTESIAN_POINT('Ctrl Pts',(374.766361956726,-2.28644172971074,0.144875543911012));
#49202=CARTESIAN_POINT('Ctrl Pts',(374.767212295152,-2.28058837409428,0.0288150767852721));
#49203=CARTESIAN_POINT('Ctrl Pts',(374.768062505908,-2.27473589730551,-0.0872279649249877));
#49204=CARTESIAN_POINT('Ctrl Pts',(374.763772613688,-2.26888342051675,-0.203329020781968));
#49205=CARTESIAN_POINT('Ctrl Pts',(374.754359680422,-2.26303094372798,-0.319000114451182));
#49206=CARTESIAN_POINT('Ctrl Pts',(374.744945884045,-2.25717793030141,-0.434681814481509));
#49207=CARTESIAN_POINT('Ctrl Pts',(374.73040814631,-2.25132491687484,-0.549933062143207));
#49208=CARTESIAN_POINT('Ctrl Pts',(374.710815445168,-2.24547190344827,-0.664270592191428));
#49209=CARTESIAN_POINT('Ctrl Pts',(374.6912162093,-2.23961693787405,-0.778646257081286));
#49210=CARTESIAN_POINT('Ctrl Pts',(374.66655872728,-2.23376197229983,-0.89210719138289));
#49211=CARTESIAN_POINT('Ctrl Pts',(374.636963023964,-2.22790700672561,-1.00418061395693));
#49212=CARTESIAN_POINT('Ctrl Pts',(374.607333777087,-2.22204540517478,-1.1163810597563));
#49213=CARTESIAN_POINT('Ctrl Pts',(374.572755243293,-2.21618380362394,-1.22719045534492));
#49214=CARTESIAN_POINT('Ctrl Pts',(374.533397265,-2.21032220207311,-1.33615137816496));
#49215=CARTESIAN_POINT('Ctrl Pts',(374.494012746907,-2.20445664793774,-1.44518577531713));
#49216=CARTESIAN_POINT('Ctrl Pts',(374.449842523899,-2.19859109380236,-1.55236883668829));
#49217=CARTESIAN_POINT('Ctrl Pts',(374.401103803266,-2.19272553966699,-1.65726491140704));
#49218=CARTESIAN_POINT('Ctrl Pts',(374.352293813378,-2.18685140849739,-1.76231437269449));
#49219=CARTESIAN_POINT('Ctrl Pts',(374.298902183255,-2.1809772773278,-1.86506980795421));
#49220=CARTESIAN_POINT('Ctrl Pts',(374.241191102975,-2.1751031461582,-1.96512179269728));
#49221=CARTESIAN_POINT('Ctrl Pts',(374.226596150299,-2.17361759665866,-1.99042462839697));
#49222=CARTESIAN_POINT('Ctrl Pts',(374.211725148619,-2.17213204715913,-2.01555471456537));
#49223=CARTESIAN_POINT('Ctrl Pts',(374.196582755325,-2.17064649765959,-2.04050575301744));
#49224=CARTESIAN_POINT('Ctrl Pts',(374.136711409584,-2.16477279949461,-2.13915939519895));
#49225=CARTESIAN_POINT('Ctrl Pts',(374.072394712155,-2.15889910132964,-2.23534004402309));
#49226=CARTESIAN_POINT('Ctrl Pts',(374.003862865492,-2.15302540316466,-2.32862049617492));
#49227=CARTESIAN_POINT('Ctrl Pts',(373.935419500314,-2.14715928853291,-2.42178051391063));
#49228=CARTESIAN_POINT('Ctrl Pts',(373.862772050991,-2.14129317390117,-2.51204745154188));
#49229=CARTESIAN_POINT('Ctrl Pts',(373.786195630664,-2.13542705926942,-2.59902031293644));
#49230=CARTESIAN_POINT('Ctrl Pts',(373.709697624255,-2.12956695151328,-2.6859041145032));
#49231=CARTESIAN_POINT('Ctrl Pts',(373.629278920811,-2.12370684375713,-2.76950024100981));
#49232=CARTESIAN_POINT('Ctrl Pts',(373.545256384692,-2.11784673600099,-2.8494387655473));
#49233=CARTESIAN_POINT('Ctrl Pts',(373.458202682824,-2.11177522117794,-2.93226112255134));
#49234=CARTESIAN_POINT('Ctrl Pts',(373.367280485604,-2.1057037063549,-3.01115663072952));
#49235=CARTESIAN_POINT('Ctrl Pts',(373.2728861744,-2.09963219153185,-3.08575331855246));
#49236=CARTESIAN_POINT('Ctrl Pts',(373.181883345503,-2.09377881946382,-3.1576698305922));
#49237=CARTESIAN_POINT('Ctrl Pts',(373.08765395933,-2.08792544739578,-3.22559083191305));
#49238=CARTESIAN_POINT('Ctrl Pts',(372.990588120366,-2.08207207532774,-3.28922293787454));
#49239=CARTESIAN_POINT('Ctrl Pts',(372.893536856928,-2.07621958220929,-3.35284548876038));
#49240=CARTESIAN_POINT('Ctrl Pts',(372.793650333023,-2.07036708909084,-3.41218019840676));
#49241=CARTESIAN_POINT('Ctrl Pts',(372.691347850167,-2.06451459597238,-3.46697686615502));
#49242=CARTESIAN_POINT('Ctrl Pts',(372.589035989226,-2.05866156635498,-3.52177855712227));
#49243=CARTESIAN_POINT('Ctrl Pts',(372.48430809328,-2.05280853673758,-3.5720411841332));
#49244=CARTESIAN_POINT('Ctrl Pts',(372.377607649301,-2.04695550712018,-3.61756072586551));
#49245=CARTESIAN_POINT('Ctrl Pts',(372.270871620611,-2.0411005255112,-3.6630954484132));
#49246=CARTESIAN_POINT('Ctrl Pts',(372.162162115591,-2.03524554390222,-3.70388377826776));
#49247=CARTESIAN_POINT('Ctrl Pts',(372.051941484438,-2.02939056229325,-3.73977027271838));
#49248=CARTESIAN_POINT('Ctrl Pts',(371.941595936191,-2.02352894501829,-3.77569743865288));
#49249=CARTESIAN_POINT('Ctrl Pts',(371.829736236601,-2.01766732774334,-3.80671155290144));
#49250=CARTESIAN_POINT('Ctrl Pts',(371.716838836597,-2.01180571046839,-3.83270736084911));
#49251=CARTESIAN_POINT('Ctrl Pts',(371.603865311144,-2.00594014077078,-3.85872069747794));
#49252=CARTESIAN_POINT('Ctrl Pts',(371.48985309731,-2.00007457107318,-3.87970891532077));
#49253=CARTESIAN_POINT('Ctrl Pts',(371.375286028223,-1.99420900137557,-3.89561836344863));
#49254=CARTESIAN_POINT('Ctrl Pts',(371.260551438335,-1.98833485499935,-3.91155107448708));
#49255=CARTESIAN_POINT('Ctrl Pts',(371.145260783764,-1.98246070862314,-3.9223901564312));
#49256=CARTESIAN_POINT('Ctrl Pts',(371.029900245164,-1.97658656224692,-3.92813397530723));
#49257=CARTESIAN_POINT('Ctrl Pts',(371.000729053154,-1.97510116824726,-3.92958641342286));
#49258=CARTESIAN_POINT('Ctrl Pts',(370.971553376122,-1.9736157742476,-3.93071330423033));
#49259=CARTESIAN_POINT('Ctrl Pts',(370.942381028825,-1.97213038024793,-3.93151514687137));
#49260=CARTESIAN_POINT('Ctrl Pts',(370.827024605462,-1.96625667603962,-3.93468587901123));
#49261=CARTESIAN_POINT('Ctrl Pts',(370.711336395662,-1.96038297183131,-3.93278049909418));
#49262=CARTESIAN_POINT('Ctrl Pts',(370.595800177937,-1.954509267623,-3.92576085855667));
#49263=CARTESIAN_POINT('Ctrl Pts',(370.480413125292,-1.94864314676452,-3.91875028085039));
#49264=CARTESIAN_POINT('Ctrl Pts',(370.365178083096,-1.94277702590605,-3.90663859826885));
#49265=CARTESIAN_POINT('Ctrl Pts',(370.250581154075,-1.93691090504757,-3.8894396082298));
#49266=CARTESIAN_POINT('Ctrl Pts',(370.136101568291,-1.93105079089115,-3.87225822935343));
#49267=CARTESIAN_POINT('Ctrl Pts',(370.022259202141,-1.92519067673472,-3.84999996555435));
#49268=CARTESIAN_POINT('Ctrl Pts',(369.909536684186,-1.9193305625783,-3.82273054103916));
#49269=CARTESIAN_POINT('Ctrl Pts',(369.792747803064,-1.91325905008905,-3.79447739662947));
#49270=CARTESIAN_POINT('Ctrl Pts',(369.6771615413,-1.9071875375998,-3.76084474719226));
#49271=CARTESIAN_POINT('Ctrl Pts',(369.563305350035,-1.90111602511055,-3.72196402679242));
#49272=CARTESIAN_POINT('Ctrl Pts',(369.45353971524,-1.89526264625483,-3.68448018943125));
#49273=CARTESIAN_POINT('Ctrl Pts',(369.345382400785,-1.88940926739911,-3.64211903594313));
#49274=CARTESIAN_POINT('Ctrl Pts',(369.239291420052,-1.8835558885434,-3.59504932893611));
#49275=CARTESIAN_POINT('Ctrl Pts',(369.133216367688,-1.87770338850668,-3.54798668891616));
#49276=CARTESIAN_POINT('Ctrl Pts',(369.02920740972,-1.87185088846996,-3.49621706853729));
#49277=CARTESIAN_POINT('Ctrl Pts',(368.927702099564,-1.86599838843324,-3.43995717529977));
#49278=CARTESIAN_POINT('Ctrl Pts',(368.826187482287,-1.8601453517751,-3.38369212353793));
#49279=CARTESIAN_POINT('Ctrl Pts',(368.72717733054,-1.85429231511697,-3.32293618075318));
#49280=CARTESIAN_POINT('Ctrl Pts',(368.631083503943,-1.84843927845883,-3.25795141187662));
#49281=CARTESIAN_POINT('Ctrl Pts',(368.534957628112,-1.84258428969461,-3.19294496926558));
#49282=CARTESIAN_POINT('Ctrl Pts',(368.441750353557,-1.83672930093039,-3.12370712736096));
#49283=CARTESIAN_POINT('Ctrl Pts',(368.351842944765,-1.83087431216617,-3.05054213687864));
#49284=CARTESIAN_POINT('Ctrl Pts',(368.261833638707,-1.82501268760456,-2.977294224281));
#49285=CARTESIAN_POINT('Ctrl Pts',(368.175131983708,-1.81915106304294,-2.90011054036536));
#49286=CARTESIAN_POINT('Ctrl Pts',(368.09208471489,-1.81328943848132,-2.81933439219659));
#49287=CARTESIAN_POINT('Ctrl Pts',(368.008981447091,-1.80742386141163,-2.73850377646946));
#49288=CARTESIAN_POINT('Ctrl Pts',(367.929537754586,-1.80155828434194,-2.65407617307459));
#49289=CARTESIAN_POINT('Ctrl Pts',(367.854061011427,-1.79569270727225,-2.5664290671904));
#49290=CARTESIAN_POINT('Ctrl Pts',(367.778473904908,-1.78981855345736,-2.47865380223767));
#49291=CARTESIAN_POINT('Ctrl Pts',(367.706865578653,-1.78394439964248,-2.38764996301879));
#49292=CARTESIAN_POINT('Ctrl Pts',(367.639500969047,-1.7780702458276,-2.29382520619512));
#49293=CARTESIAN_POINT('Ctrl Pts',(367.622467278517,-1.77658491816383,-2.27010085180318));
#49294=CARTESIAN_POINT('Ctrl Pts',(367.605704692428,-1.77509959050005,-2.24619626268826));
#49295=CARTESIAN_POINT('Ctrl Pts',(367.589217027284,-1.77361426283628,-2.22211827531365));
#49296=CARTESIAN_POINT('Ctrl Pts',(367.523092229448,-1.76765726464239,-2.12555202208811));
#49297=CARTESIAN_POINT('Ctrl Pts',(367.461176617048,-1.76170026644851,-2.02587883354736));
#49298=CARTESIAN_POINT('Ctrl Pts',(367.403770540428,-1.75574326825462,-1.92349529104395));
#49299=CARTESIAN_POINT('Ctrl Pts',(367.346443934608,-1.74979451670351,-1.82125348444072));
#49300=CARTESIAN_POINT('Ctrl Pts',(367.293614638098,-1.74384576515241,-1.71630913170595));
#49301=CARTESIAN_POINT('Ctrl Pts',(367.245540626912,-1.7378970136013,-1.60908887880941));
#49302=CARTESIAN_POINT('Ctrl Pts',(367.197522718397,-1.73195520428017,-1.50199375261339));
#49303=CARTESIAN_POINT('Ctrl Pts',(367.15424921483,-1.72601339495904,-1.39262837160822));
#49304=CARTESIAN_POINT('Ctrl Pts',(367.115932659183,-1.72007158563791,-1.28144471154241));
#49305=CARTESIAN_POINT('Ctrl Pts',(367.077658873099,-1.71413640866083,-1.17038515648355));
#49306=CARTESIAN_POINT('Ctrl Pts',(367.044331144165,-1.70820123168376,-1.05751173899592));
#49307=CARTESIAN_POINT('Ctrl Pts',(367.016113989028,-1.70226605470669,-0.943296481198009));
#49308=CARTESIAN_POINT('Ctrl Pts',(366.987915424115,-1.69633478798449,-0.829156471496444));
#49309=CARTESIAN_POINT('Ctrl Pts',(366.964820828366,-1.6904035212623,-0.713676765600365));
#49310=CARTESIAN_POINT('Ctrl Pts',(366.946944887028,-1.6844722545401,-0.59734447489317));
#49311=CARTESIAN_POINT('Ctrl Pts',(366.929076286795,-1.67854342360909,-0.481059958326177));
#49312=CARTESIAN_POINT('Ctrl Pts',(366.916422137311,-1.67261459267808,-0.363923946200259));
#49313=CARTESIAN_POINT('Ctrl Pts',(366.909045930346,-1.66668576174707,-0.246433219083321));
#49314=CARTESIAN_POINT('Ctrl Pts',(366.903852853057,-1.66251168184304,-0.163716122125167));
#49315=CARTESIAN_POINT('Ctrl Pts',(366.90127476899,-1.658337601939,-0.0808234308795856));
#49316=CARTESIAN_POINT('Ctrl Pts',(366.901318397982,-1.65416352203497,0.00207004003203127));
#49317=CARTESIAN_POINT('Ctrl Pts',(366.901318397982,-1.65416352199376,0.0020700408504056));
#49318=CARTESIAN_POINT('Ctrl Pts',(366.901387266335,-1.647574740613,0.132917310256408));
#49319=CARTESIAN_POINT('Ctrl Pts',(366.907990299073,-1.64098595923224,0.263537049001877));
#49320=CARTESIAN_POINT('Ctrl Pts',(366.921033153443,-1.63439717785148,0.393308858862064));
#49321=CARTESIAN_POINT('Ctrl Pts',(366.93390211787,-1.62789623942197,0.521350524996328));
#49322=CARTESIAN_POINT('Ctrl Pts',(366.953040076547,-1.62139530099246,0.64856652162196));
#49323=CARTESIAN_POINT('Ctrl Pts',(366.978305822652,-1.61489436256295,0.774377311187052));
#49324=CARTESIAN_POINT('Ctrl Pts',(367.004083668139,-1.60826165970656,0.902738099765647));
#49325=CARTESIAN_POINT('Ctrl Pts',(367.036240232741,-1.60162895685017,1.02963583952188));
#49326=CARTESIAN_POINT('Ctrl Pts',(367.074573994238,-1.59499625399378,1.15447612137308));
#49327=CARTESIAN_POINT('Ctrl Pts',(367.112907755736,-1.58836355113739,1.27931640322429));
#49328=CARTESIAN_POINT('Ctrl Pts',(367.157418544267,-1.581730848281,1.40209900418968));
#49329=CARTESIAN_POINT('Ctrl Pts',(367.207855253712,-1.57509814542462,1.52225425417008));
#49330=CARTESIAN_POINT('Ctrl Pts',(367.252520967112,-1.56922436007833,1.62866127433904));
#49331=CARTESIAN_POINT('Ctrl Pts',(367.301948294204,-1.56335057473204,1.73327796658719));
#49332=CARTESIAN_POINT('Ctrl Pts',(367.355972554108,-1.55747678938575,1.83564783662771));
#49333=CARTESIAN_POINT('Ctrl Pts',(367.409927061389,-1.55161058789037,1.93788553332751));
#49334=CARTESIAN_POINT('Ctrl Pts',(367.468466507126,-1.54574438639499,2.03788181482829));
#49335=CARTESIAN_POINT('Ctrl Pts',(367.531377925647,-1.53987818489961,2.13519948361255));
#49336=CARTESIAN_POINT('Ctrl Pts',(367.594224919664,-1.53401799069406,2.23241749413557));
#49337=CARTESIAN_POINT('Ctrl Pts',(367.661434758137,-1.5281577964885,2.32696200318616));
#49338=CARTESIAN_POINT('Ctrl Pts',(367.732748598351,-1.52229760228294,2.41842038471899));
#49339=CARTESIAN_POINT('Ctrl Pts',(367.806633643905,-1.51622612002169,2.51317627874593));
#49340=CARTESIAN_POINT('Ctrl Pts',(367.884924002244,-1.51015463776044,2.60461890741811));
#49341=CARTESIAN_POINT('Ctrl Pts',(367.967282504934,-1.5040831554992,2.69232191828074));
#49342=CARTESIAN_POINT('Ctrl Pts',(368.046683535811,-1.49822969854276,2.77687553747036));
#49343=CARTESIAN_POINT('Ctrl Pts',(368.12986525722,-1.49237624158632,2.85795316988102));
#49344=CARTESIAN_POINT('Ctrl Pts',(368.216485098508,-1.48652278462989,2.93520709121813));
#49345=CARTESIAN_POINT('Ctrl Pts',(368.303091922414,-1.48067020734126,3.01244940270004));
#49346=CARTESIAN_POINT('Ctrl Pts',(368.393135530594,-1.47481763005263,3.08586887078945));
#49347=CARTESIAN_POINT('Ctrl Pts',(368.486238104937,-1.468965052764,3.15515617611592));
#49348=CARTESIAN_POINT('Ctrl Pts',(368.57934920107,-1.46311193978194,3.2244498233928));
#49349=CARTESIAN_POINT('Ctrl Pts',(368.675519488519,-1.45725882679987,3.28961030937691));
#49350=CARTESIAN_POINT('Ctrl Pts',(368.774340416498,-1.4514057138178,3.35037042133874));
#49351=CARTESIAN_POINT('Ctrl Pts',(368.873194285809,-1.44555064973755,3.41115078729947));
#49352=CARTESIAN_POINT('Ctrl Pts',(368.974700200859,-1.43969558565731,3.46752764622947));
#49353=CARTESIAN_POINT('Ctrl Pts',(369.07842378813,-1.43384052157706,3.51927905005661));
#49354=CARTESIAN_POINT('Ctrl Pts',(369.182264896829,-1.42797882356225,3.57108908952324));
#49355=CARTESIAN_POINT('Ctrl Pts',(369.288328323026,-1.42211712554744,3.61826302910341));
#49356=CARTESIAN_POINT('Ctrl Pts',(369.396158343451,-1.41625542753262,3.66062647977775));
#49357=CARTESIAN_POINT('Ctrl Pts',(369.504061054693,-1.41038977800583,3.70301848867573));
#49358=CARTESIAN_POINT('Ctrl Pts',(369.613732341657,-1.40452412847904,3.74059341782054));
#49359=CARTESIAN_POINT('Ctrl Pts',(369.724701567165,-1.39865847895225,3.77322682828817));
#49360=CARTESIAN_POINT('Ctrl Pts',(369.835833013767,-1.39278425468705,3.80590794412192));
#49361=CARTESIAN_POINT('Ctrl Pts',(369.948265786073,-1.38691003042185,3.83363302586876));
#49362=CARTESIAN_POINT('Ctrl Pts',(370.061519251664,-1.38103580615665,3.85632873617203));
#49363=CARTESIAN_POINT('Ctrl Pts',(370.090141800331,-1.37955121344209,3.86206462309885));
#49364=CARTESIAN_POINT('Ctrl Pts',(370.118816746645,-1.37806662072753,3.86747953073522));
#49365=CARTESIAN_POINT('Ctrl Pts',(370.147536300447,-1.37658202801298,3.87257280096382));
#49366=CARTESIAN_POINT('Ctrl Pts',(370.261164980889,-1.37070824904298,3.89272428309351));
#49367=CARTESIAN_POINT('Ctrl Pts',(370.375870526143,-1.36483447007299,3.90790395514502));
#49368=CARTESIAN_POINT('Ctrl Pts',(370.491180061432,-1.35896069110299,3.91800273811087));
#49369=CARTESIAN_POINT('Ctrl Pts',(370.606340747741,-1.35309449438551,3.92808848491671));
#49370=CARTESIAN_POINT('Ctrl Pts',(370.722103465781,-1.34722829766803,3.93310635011528));
#49371=CARTESIAN_POINT('Ctrl Pts',(370.837985381494,-1.34136210095055,3.93299829001188));
#49372=CARTESIAN_POINT('Ctrl Pts',(370.953748659356,-1.33550190994133,3.9328903405385));
#49373=CARTESIAN_POINT('Ctrl Pts',(371.069630481483,-1.3296417189321,3.92766690452695));
#49374=CARTESIAN_POINT('Ctrl Pts',(371.185143792175,-1.32378152792287,3.91732180967547));
#49375=CARTESIAN_POINT('Ctrl Pts',(371.304822011351,-1.3177100438678,3.90660371561675));
#49376=CARTESIAN_POINT('Ctrl Pts',(371.424104193896,-1.31163855981274,3.89038762477201));
#49377=CARTESIAN_POINT('Ctrl Pts',(371.542449288747,-1.30556707575767,3.86872574241488));
#49378=CARTESIAN_POINT('Ctrl Pts',(371.656544623168,-1.29971361808323,3.84784173607042));
#49379=CARTESIAN_POINT('Ctrl Pts',(371.769768572609,-1.29386016040878,3.82189640766259));
#49380=CARTESIAN_POINT('Ctrl Pts',(371.881643231203,-1.28800670273434,3.79098912589329));
#49381=CARTESIAN_POINT('Ctrl Pts',(371.993501104517,-1.28215412329209,3.76008648134384));
#49382=CARTESIAN_POINT('Ctrl Pts',(372.104009691411,-1.27630154384984,3.72422347371164));
#49383=CARTESIAN_POINT('Ctrl Pts',(372.212704251087,-1.2704489644076,3.68354990982684));
#49384=CARTESIAN_POINT('Ctrl Pts',(372.321408786192,-1.26459584784569,3.64287261313136));
#49385=CARTESIAN_POINT('Ctrl Pts',(372.428298576181,-1.25874273128377,3.5973840273411));
#49386=CARTESIAN_POINT('Ctrl Pts',(372.532927603359,-1.25288961472186,3.54728261021654));
#49387=CARTESIAN_POINT('Ctrl Pts',(372.637591533287,-1.24703454564386,3.49716447997482));
#49388=CARTESIAN_POINT('Ctrl Pts',(372.739992828382,-1.24117947656586,3.44243063693976));
#49389=CARTESIAN_POINT('Ctrl Pts',(372.839709509419,-1.23532440748786,3.38332577581028));
#49390=CARTESIAN_POINT('Ctrl Pts',(372.93953920686,-1.22946270242036,3.32415392670291));
#49391=CARTESIAN_POINT('Ctrl Pts',(373.036677861656,-1.22360099735286,3.26060138237516));
#49392=CARTESIAN_POINT('Ctrl Pts',(373.130731885692,-1.21773929228536,3.19295655959848));
#49393=CARTESIAN_POINT('Ctrl Pts',(373.224849333079,-1.21187363450049,3.12526612196006));
#49394=CARTESIAN_POINT('Ctrl Pts',(373.315877684262,-1.20600797671561,3.05347816620013));
#49395=CARTESIAN_POINT('Ctrl Pts',(373.403457240458,-1.20014231893074,2.97792071905295));
#49396=CARTESIAN_POINT('Ctrl Pts',(373.491164850365,-1.19426808472363,2.90225279621936));
#49397=CARTESIAN_POINT('Ctrl Pts',(373.575413302059,-1.18839385051651,2.82280466471597));
#49398=CARTESIAN_POINT('Ctrl Pts',(373.655880419957,-1.1825196163094,2.73994045227431));
#49399=CARTESIAN_POINT('Ctrl Pts',(373.676216509716,-1.18103504774004,2.71899855568341));
#49400=CARTESIAN_POINT('Ctrl Pts',(373.696311290769,-1.17955047917067,2.69783863238138));
#49401=CARTESIAN_POINT('Ctrl Pts',(373.716159987334,-1.17806591060131,2.6764668714688));
#49402=CARTESIAN_POINT('Ctrl Pts',(373.794683068952,-1.17219283482733,2.59191842160054));
#49403=CARTESIAN_POINT('Ctrl Pts',(373.869613173202,-1.16631975905336,2.50377044779303));
#49404=CARTESIAN_POINT('Ctrl Pts',(373.940602311623,-1.16044668327938,2.41236105579295));
#49405=CARTESIAN_POINT('Ctrl Pts',(374.011499772401,-1.15458119218332,2.32106971280559));
#49406=CARTESIAN_POINT('Ctrl Pts',(374.078466137477,-1.14871570108726,2.22652565106339));
#49407=CARTESIAN_POINT('Ctrl Pts',(374.1411908986,-1.1428502099912,2.12910301811899));
#49408=CARTESIAN_POINT('Ctrl Pts',(374.203851418684,-1.13699072617578,2.031780162855));
#49409=CARTESIAN_POINT('Ctrl Pts',(374.26227875325,-1.13113124236035,1.93158494587313));
#49410=CARTESIAN_POINT('Ctrl Pts',(374.316203688908,-1.12527175854492,1.82892318790745));
#49411=CARTESIAN_POINT('Ctrl Pts',(374.37208210082,-1.11920000998845,1.7225424212106));
#49412=CARTESIAN_POINT('Ctrl Pts',(374.42312544687,-1.11312826143198,1.61351337797017));
#49413=CARTESIAN_POINT('Ctrl Pts',(374.469084176485,-1.10705651287551,1.50231913230347));
#49414=CARTESIAN_POINT('Ctrl Pts',(374.513385253775,-1.1012037618458,1.39513547181891));
#49415=CARTESIAN_POINT('Ctrl Pts',(374.552961992507,-1.09535101081608,1.28594051525445));
#49416=CARTESIAN_POINT('Ctrl Pts',(374.587638829686,-1.08949825978636,1.17518962199757));
#49417=CARTESIAN_POINT('Ctrl Pts',(374.62231047179,-1.08364638558061,1.06445532077356));
#49418=CARTESIAN_POINT('Ctrl Pts',(374.652083548501,-1.07779451137487,0.952165940602883));
#49419=CARTESIAN_POINT('Ctrl Pts',(374.676832016761,-1.07194263716912,0.838793122894883));
#49420=CARTESIAN_POINT('Ctrl Pts',(374.701582765721,-1.06609022368301,0.725409857297624));
#49421=CARTESIAN_POINT('Ctrl Pts',(374.721307897605,-1.0602378101969,0.610943359437889));
#49422=CARTESIAN_POINT('Ctrl Pts',(374.735932401061,-1.05438539671079,0.495875912001588));
#49423=CARTESIAN_POINT('Ctrl Pts',(374.750561790914,-1.04853102779313,0.38077001777434));
#49424=CARTESIAN_POINT('Ctrl Pts',(374.760087111469,-1.04267665887547,0.265063184428101));
#49425=CARTESIAN_POINT('Ctrl Pts',(374.764485236239,-1.0368222899578,0.149242559231955));
#49426=CARTESIAN_POINT('Ctrl Pts',(374.768888352225,-1.03096127720409,0.0332904948907921));
#49427=CARTESIAN_POINT('Ctrl Pts',(374.768152643172,-1.02510026445037,-0.0827752058756374));
#49428=CARTESIAN_POINT('Ctrl Pts',(374.762307113717,-1.01923925169666,-0.19846755265044));
#49429=CARTESIAN_POINT('Ctrl Pts',(374.756457638265,-1.01337428249537,-0.31423799696978));
#49430=CARTESIAN_POINT('Ctrl Pts',(374.74549151302,-1.00750931329408,-0.429634175087716));
#49431=CARTESIAN_POINT('Ctrl Pts',(374.729489398386,-1.00164434409279,-0.544176105465635));
#49432=CARTESIAN_POINT('Ctrl Pts',(374.7134638543,-0.995770787713188,-0.658885742091846));
#49433=CARTESIAN_POINT('Ctrl Pts',(374.692387680276,-0.989897231333582,
-0.772738230042964));
#49434=CARTESIAN_POINT('Ctrl Pts',(374.666392213373,-0.984023674953976,
-0.885265552414129));
#49435=CARTESIAN_POINT('Ctrl Pts',(374.659791973369,-0.982532381032535,
-0.913836200417235));
#49436=CARTESIAN_POINT('Ctrl Pts',(374.652874858159,-0.981041087111095,
-0.942321509043616));
#49437=CARTESIAN_POINT('Ctrl Pts',(374.645643516695,-0.979549793189654,
-0.97071400884325));
#49438=CARTESIAN_POINT('Ctrl Pts',(374.61715694645,-0.973675108767121,-1.08256115975804));
#49439=CARTESIAN_POINT('Ctrl Pts',(374.583695430451,-0.967800424344588,
-1.193339308818));
#49440=CARTESIAN_POINT('Ctrl Pts',(374.545354598602,-0.961925739922055,
-1.30257256014839));
#49441=CARTESIAN_POINT('Ctrl Pts',(374.507063277007,-0.956058641592539,
-1.41166475647982));
#49442=CARTESIAN_POINT('Ctrl Pts',(374.463905305323,-0.950191543263022,
-1.51921563629043));
#49443=CARTESIAN_POINT('Ctrl Pts',(374.416026914772,-0.944324444933506,
-1.62476127428801));
#49444=CARTESIAN_POINT('Ctrl Pts',(374.368197573213,-0.938463357149759,
-1.73019878611279));
#49445=CARTESIAN_POINT('Ctrl Pts',(374.315657601324,-0.932602269366011,
-1.83363476839066));
#49446=CARTESIAN_POINT('Ctrl Pts',(374.258602228074,-0.926741181582264,
-1.93462283666815));
#49447=CARTESIAN_POINT('Ctrl Pts',(374.199502020373,-0.920670035507086,
-2.03923026398954));
#49448=CARTESIAN_POINT('Ctrl Pts',(374.135556829694,-0.914598889431908,
-2.14121059590081));
#49449=CARTESIAN_POINT('Ctrl Pts',(374.067037163071,-0.908527743356731,
-2.2400926015992));
#49450=CARTESIAN_POINT('Ctrl Pts',(374.000964430064,-0.902673406442331,
-2.33544339187203));
#49451=CARTESIAN_POINT('Ctrl Pts',(373.930638611108,-0.896819069527931,
-2.42791299446444));
#49452=CARTESIAN_POINT('Ctrl Pts',(373.856347308075,-0.890964732613531,
-2.51710686583075));
#49453=CARTESIAN_POINT('Ctrl Pts',(373.782067250599,-0.885111281876602,
-2.60628723582185));
#49454=CARTESIAN_POINT('Ctrl Pts',(373.703823166845,-0.879257831139672,
-2.6921925432886));
#49455=CARTESIAN_POINT('Ctrl Pts',(373.621943186131,-0.873404380402743,
-2.77446102934122));
#49456=CARTESIAN_POINT('Ctrl Pts',(373.540055815788,-0.867550401394647,
-2.85673694008588));
#49457=CARTESIAN_POINT('Ctrl Pts',(373.454532187536,-0.861696422386551,
-2.93537508420955));
#49458=CARTESIAN_POINT('Ctrl Pts',(373.365737040213,-0.855842443378455,
-3.01005081348208));
#49459=CARTESIAN_POINT('Ctrl Pts',(373.276912424492,-0.849986521613438,
-3.08475132534943));
#49460=CARTESIAN_POINT('Ctrl Pts',(373.184814446699,-0.844130599848422,
-3.15548654184991));
#49461=CARTESIAN_POINT('Ctrl Pts',(373.089840066501,-0.838274678083405,
-3.22197277229532));
#49462=CARTESIAN_POINT('Ctrl Pts',(372.994758363151,-0.832412138997133,
-3.28853413365326));
#49463=CARTESIAN_POINT('Ctrl Pts',(372.896794108303,-0.826549599910861,
-3.35083668854854));
#49464=CARTESIAN_POINT('Ctrl Pts',(372.79637239718,-0.820687060824589,-3.40864063323499));
#49465=CARTESIAN_POINT('Ctrl Pts',(372.695883147442,-0.814820578887978,
-3.46648345396124));
#49466=CARTESIAN_POINT('Ctrl Pts',(372.592933516173,-0.808954096951367,
-3.51982145035608));
#49467=CARTESIAN_POINT('Ctrl Pts',(372.48797072529,-0.803087615014756,-3.56846201867247));
#49468=CARTESIAN_POINT('Ctrl Pts',(372.382854855871,-0.797212577356091,
-3.61717352476511));
#49469=CARTESIAN_POINT('Ctrl Pts',(372.275720347855,-0.791337539697427,
-3.66117377401909));
#49470=CARTESIAN_POINT('Ctrl Pts',(372.167031854818,-0.785462502038762,
-3.70031922811472));
#49471=CARTESIAN_POINT('Ctrl Pts',(372.139720685076,-0.783986226618508,
-3.71015567088388));
#49472=CARTESIAN_POINT('Ctrl Pts',(372.112311454136,-0.782509951198253,
-3.71968582581753));
#49473=CARTESIAN_POINT('Ctrl Pts',(372.084811641178,-0.781033675777999,
-3.72890792140123));
#49474=CARTESIAN_POINT('Ctrl Pts',(371.975390032661,-0.775159583785276,
-3.76560259035059));
#49475=CARTESIAN_POINT('Ctrl Pts',(371.864170034379,-0.769285491792554,
-3.79753784047223));
#49476=CARTESIAN_POINT('Ctrl Pts',(371.751603346463,-0.763411399799832,
-3.82453609263826));
#49477=CARTESIAN_POINT('Ctrl Pts',(371.639181771813,-0.75754488028427,-3.85149954050634));
#49478=CARTESIAN_POINT('Ctrl Pts',(371.525417358021,-0.751678360768709,
-3.87353855180081));
#49479=CARTESIAN_POINT('Ctrl Pts',(371.410779173421,-0.745811841253147,
-3.89052455927433));
#49480=CARTESIAN_POINT('Ctrl Pts',(371.296258165902,-0.739951318183177,
-3.90749320455049));
#49481=CARTESIAN_POINT('Ctrl Pts',(371.180865570266,-0.734090795113207,
-3.91941905930915));
#49482=CARTESIAN_POINT('Ctrl Pts',(371.065082271911,-0.728230272043237,
-3.92622424003878));
#49483=CARTESIAN_POINT('Ctrl Pts',(370.945133517619,-0.722158908973366,
-3.93327424606596));
#49484=CARTESIAN_POINT('Ctrl Pts',(370.824765858313,-0.716087545903495,
-3.9348280894326));
#49485=CARTESIAN_POINT('Ctrl Pts',(370.704522065142,-0.710016182833625,
-3.93085767401927));
#49486=CARTESIAN_POINT('Ctrl Pts',(370.588586917445,-0.704162372373453,
-3.92702952883832));
#49487=CARTESIAN_POINT('Ctrl Pts',(370.47276735942,-0.698308561913282,-3.91806624270722));
#49488=CARTESIAN_POINT('Ctrl Pts',(370.357550777857,-0.692454751453111,
-3.90399566544915));
#49489=CARTESIAN_POINT('Ctrl Pts',(370.242351344099,-0.686601812221728,
-3.88992718232995));
#49490=CARTESIAN_POINT('Ctrl Pts',(370.127755118275,-0.680748872990345,
-3.87075296955846));
#49491=CARTESIAN_POINT('Ctrl Pts',(370.014243898829,-0.674895933758963,
-3.84655270460736));
#49492=CARTESIAN_POINT('Ctrl Pts',(369.900722134928,-0.669042450827617,
-3.82235019160914));
#49493=CARTESIAN_POINT('Ctrl Pts',(369.788285981781,-0.663188967896271,
-3.7931207844239));
#49494=CARTESIAN_POINT('Ctrl Pts',(369.677405889567,-0.657335484964925,
-3.7589950396811));
#49495=CARTESIAN_POINT('Ctrl Pts',(369.566488694934,-0.651480043355766,
-3.72485787586697));
#49496=CARTESIAN_POINT('Ctrl Pts',(369.457128991181,-0.645624601746607,
-3.68582123802798));
#49497=CARTESIAN_POINT('Ctrl Pts',(369.349780267916,-0.639769160137449,
-3.64206495793378));
#49498=CARTESIAN_POINT('Ctrl Pts',(369.242309755129,-0.633907075399046,
-3.59825903536283));
#49499=CARTESIAN_POINT('Ctrl Pts',(369.136855159301,-0.628044990660643,
-3.54972293919225));
#49500=CARTESIAN_POINT('Ctrl Pts',(369.033848334787,-0.62218290592224,-3.49668393098079));
#49501=CARTESIAN_POINT('Ctrl Pts',(368.930771973147,-0.616316863848724,
-3.4436091175671));
#49502=CARTESIAN_POINT('Ctrl Pts',(368.830147030803,-0.610450821775208,
-3.3860255438435));
#49503=CARTESIAN_POINT('Ctrl Pts',(368.732377682707,-0.604584779701691,
-3.32420464465819));
#49504=CARTESIAN_POINT('Ctrl Pts',(368.634465329476,-0.598710157493848,
-3.26229332136535));
#49505=CARTESIAN_POINT('Ctrl Pts',(368.539417244094,-0.592835535286005,
-3.19613253833672));
#49506=CARTESIAN_POINT('Ctrl Pts',(368.447605811247,-0.586960913078162,
-3.12603496920298));
#49507=CARTESIAN_POINT('Ctrl Pts',(368.42445818017,-0.585479794840889,-3.10836186881299));
#49508=CARTESIAN_POINT('Ctrl Pts',(368.401516108419,-0.583998676603616,
-3.09043871241285));
#49509=CARTESIAN_POINT('Ctrl Pts',(368.378785192664,-0.582517558366343,
-3.07227087883228));
#49510=CARTESIAN_POINT('Ctrl Pts',(368.289844403939,-0.576722287043533,
-3.00118436980314));
#49511=CARTESIAN_POINT('Ctrl Pts',(368.203825299216,-0.570927015720722,
-2.92609813391641));
#49512=CARTESIAN_POINT('Ctrl Pts',(368.121116540691,-0.565131744397912,
-2.84728425656222));
#49513=CARTESIAN_POINT('Ctrl Pts',(368.038515306707,-0.559344007148911,
-2.76857284025535));
#49514=CARTESIAN_POINT('Ctrl Pts',(367.959216170142,-0.55355626989991,-2.68614370458509));
#49515=CARTESIAN_POINT('Ctrl Pts',(367.883576547851,-0.54776853265091,-2.60031051006729));
#49516=CARTESIAN_POINT('Ctrl Pts',(367.805377962554,-0.541784990543842,
-2.51157349394409));
#49517=CARTESIAN_POINT('Ctrl Pts',(367.731091271125,-0.535801448436774,
-2.41919826775779));
#49518=CARTESIAN_POINT('Ctrl Pts',(367.661072177725,-0.529817906329707,
-2.32357502201362));
#49519=CARTESIAN_POINT('Ctrl Pts',(367.593463091785,-0.524040313491905,
-2.23124306046759));
#49520=CARTESIAN_POINT('Ctrl Pts',(367.529832947823,-0.518262720654104,
-2.13588335750866));
#49521=CARTESIAN_POINT('Ctrl Pts',(367.470461955913,-0.512485127816302,
-2.03788186657742));
#49522=CARTESIAN_POINT('Ctrl Pts',(367.411112110333,-0.506709592799693,
-1.93991528110778));
#49523=CARTESIAN_POINT('Ctrl Pts',(367.356018622257,-0.500934057783084,
-1.83930914069092));
#49524=CARTESIAN_POINT('Ctrl Pts',(367.305418137936,-0.495158522766475,
-1.73647798702939));
#49525=CARTESIAN_POINT('Ctrl Pts',(367.254822666203,-0.489383559886301,
-1.63365702003447));
#49526=CARTESIAN_POINT('Ctrl Pts',(367.20871950042,-0.483608597006127,-1.52861185975074));
#49527=CARTESIAN_POINT('Ctrl Pts',(367.167298712719,-0.477833634125952,
-1.42178044126834));
#49528=CARTESIAN_POINT('Ctrl Pts',(367.125871378126,-0.472057758465783,
-1.31493213720873));
#49529=CARTESIAN_POINT('Ctrl Pts',(367.08912804447,-0.466281882805614,-1.2062974108198));
#49530=CARTESIAN_POINT('Ctrl Pts',(367.057209835283,-0.460506007145445,
-1.09633207597307));
#49531=CARTESIAN_POINT('Ctrl Pts',(367.025262440197,-0.454724850044727,
-0.98626618920787));
#49532=CARTESIAN_POINT('Ctrl Pts',(366.998149092602,-0.448943692944008,
-0.874867674653828));
#49533=CARTESIAN_POINT('Ctrl Pts',(366.975960385223,-0.443162535843289,
-0.762605172500647));
#49534=CARTESIAN_POINT('Ctrl Pts',(366.95375949395,-0.437378204289422,-0.650281026623353));
#49535=CARTESIAN_POINT('Ctrl Pts',(366.93648868851,-0.431593872735556,-0.537092368462364));
#49536=CARTESIAN_POINT('Ctrl Pts',(366.924186782274,-0.425809541181689,
-0.423513881694839));
#49537=CARTESIAN_POINT('Ctrl Pts',(366.911868734401,-0.420017619863102,
-0.309786365781283));
#49538=CARTESIAN_POINT('Ctrl Pts',(366.904532619862,-0.414225698544515,
-0.195668423477765));
#49539=CARTESIAN_POINT('Ctrl Pts',(366.902165180061,-0.408433777225929,
-0.0816355004928817));
#49540=CARTESIAN_POINT('Ctrl Pts',(366.901583359773,-0.407010358844382,
-0.0536108520645037));
#49541=CARTESIAN_POINT('Ctrl Pts',(366.901301389935,-0.405586940462834,
-0.0255913162295418));
#49542=CARTESIAN_POINT('Ctrl Pts',(366.90131859535,-0.404163522081287,0.00241610556833745));
#49543=CARTESIAN_POINT('Origin',(370.834317853224,2.31077344927308,0.));
#49544=CARTESIAN_POINT('',(372.667675165437,-25.,-2.65045628680305));
#49545=CARTESIAN_POINT('Ctrl Pts',(372.667675165437,-25.,-2.65045628680305));
#49546=CARTESIAN_POINT('Ctrl Pts',(372.448644400709,-24.9825465826754,-2.80196289949983));
#49547=CARTESIAN_POINT('Ctrl Pts',(372.211615774371,-24.9641309779199,-2.92577950427151));
#49548=CARTESIAN_POINT('Ctrl Pts',(371.828930661503,-24.9370043306435,-3.0687182706999));
#49549=CARTESIAN_POINT('Ctrl Pts',(371.692738286308,-24.9277863008836,-3.10956755196565));
#49550=CARTESIAN_POINT('Ctrl Pts',(371.526496104034,-24.9170663903206,-3.14766884848412));
#49551=CARTESIAN_POINT('Ctrl Pts',(371.498630778317,-24.9152866573577,-3.15366744148132));
#49552=CARTESIAN_POINT('Ctrl Pts',(371.454762329649,-24.912510851018,-3.16250377998708));
#49553=CARTESIAN_POINT('Ctrl Pts',(371.438811594471,-24.9115069253944,-3.16559138848816));
#49554=CARTESIAN_POINT('Ctrl Pts',(371.408987931986,-24.9096396289647,-3.17113076108422));
#49555=CARTESIAN_POINT('Ctrl Pts',(371.39512101949,-24.9087753361535,-3.17361242465044));
#49556=CARTESIAN_POINT('Ctrl Pts',(371.364157131943,-24.9068539790705,-3.17894452811137));
#49557=CARTESIAN_POINT('Ctrl Pts',(371.347052456556,-24.9057984052931,-3.18174813878929));
#49558=CARTESIAN_POINT('Ctrl Pts',(371.303717882357,-24.9031382618445,-3.18849253783978));
#49559=CARTESIAN_POINT('Ctrl Pts',(371.277460116567,-24.901539479463,-3.19224780493738));
#49560=CARTESIAN_POINT('Ctrl Pts',(371.10932941491,-24.8913804173512,-3.21417857478562));
#49561=CARTESIAN_POINT('Ctrl Pts',(370.96641742835,-24.8831096809257,-3.22321763238307));
#49562=CARTESIAN_POINT('Ctrl Pts',(370.550408909798,-24.8594849897765,-3.22180359197394));
#49563=CARTESIAN_POINT('Ctrl Pts',(370.278717867171,-24.844678208846,-3.18620362372021));
#49564=CARTESIAN_POINT('Ctrl Pts',(369.990265227191,-24.8269501791359,-3.11035952347186));
#49565=CARTESIAN_POINT('Ctrl Pts',(369.965806970226,-24.8254299562328,-3.10361885001254));
#49566=CARTESIAN_POINT('Ctrl Pts',(369.922745060926,-24.8227190856935,-3.09120216531442));
#49567=CARTESIAN_POINT('Ctrl Pts',(369.904108168936,-24.8215343823679,-3.08564510015569));
#49568=CARTESIAN_POINT('Ctrl Pts',(369.87623249699,-24.8197435756331,-3.07705777032747));
#49569=CARTESIAN_POINT('Ctrl Pts',(369.866954900638,-24.8191444145313,-3.07415370209092));
#49570=CARTESIAN_POINT('Ctrl Pts',(369.857633356544,-24.8185391144997,-3.07118950246782));
#49571=CARTESIAN_POINT('Ctrl Pts',(369.857575988279,-24.8185353891312,-3.07117125790598));
#49572=CARTESIAN_POINT('Ctrl Pts',(369.857460101296,-24.8185278634317,-3.0711343993334));
#49573=CARTESIAN_POINT('Ctrl Pts',(369.857401583238,-24.8185240631386,-3.07111578546099));
#49574=CARTESIAN_POINT('Ctrl Pts',(369.857283356749,-24.8185163849817,-3.07107817535193));
#49575=CARTESIAN_POINT('Ctrl Pts',(369.85722364791,-24.8185125070862,-3.0710591789102));
#49576=CARTESIAN_POINT('Ctrl Pts',(369.857102998182,-24.8185046710014,-3.07102079017294));
#49577=CARTESIAN_POINT('Ctrl Pts',(369.857042056687,-24.8185007127672,-3.07100139760502));
#49578=CARTESIAN_POINT('Ctrl Pts',(369.856918897049,-24.818492713091,-3.07096220218226));
#49579=CARTESIAN_POINT('Ctrl Pts',(369.856856679008,-24.8184886716497,-3.07094239927493));
#49580=CARTESIAN_POINT('Ctrl Pts',(369.856730919775,-24.8184805025203,-3.0709023681155));
#49581=CARTESIAN_POINT('Ctrl Pts',(369.856667378586,-24.818476374826,-3.0708821397745));
#49582=CARTESIAN_POINT('Ctrl Pts',(369.856538924669,-24.818468030028,-3.07084124207271));
#49583=CARTESIAN_POINT('Ctrl Pts',(369.856474011656,-24.8184638128991,-3.07082057252598));
#49584=CARTESIAN_POINT('Ctrl Pts',(369.856342762487,-24.8184552858586,-3.07077877569272));
#49585=CARTESIAN_POINT('Ctrl Pts',(369.85627642705,-24.8184509759866,-3.07075764853467));
#49586=CARTESIAN_POINT('Ctrl Pts',(369.856142279099,-24.8184422599342,-3.07071491899692));
#49587=CARTESIAN_POINT('Ctrl Pts',(369.856074467295,-24.8184378537922,-3.07069331673669));
#49588=CARTESIAN_POINT('Ctrl Pts',(369.85593731171,-24.8184289416095,-3.07064961918199));
#49589=CARTESIAN_POINT('Ctrl Pts',(369.855867966481,-24.8184244354665,-3.07062752331326));
#49590=CARTESIAN_POINT('Ctrl Pts',(369.855727684286,-24.8184153193739,-3.07058281915683));
#49591=CARTESIAN_POINT('Ctrl Pts',(369.855656747705,-24.8184107094406,-3.0705602108717));
#49592=CARTESIAN_POINT('Ctrl Pts',(369.855513219865,-24.8184013816509,-3.07051446145761));
#49593=CARTESIAN_POINT('Ctrl Pts',(369.855440628942,-24.8183966638072,-3.07049132030815));
#49594=CARTESIAN_POINT('Ctrl Pts',(369.847994664454,-24.8179127134251,-3.06811734176985));
#49595=CARTESIAN_POINT('Ctrl Pts',(369.840630029142,-24.8174319473629,-3.06574003490417));
#49596=CARTESIAN_POINT('Ctrl Pts',(369.824164976934,-24.8163523461005,-3.06035954786767));
#49597=CARTESIAN_POINT('Ctrl Pts',(369.815069493631,-24.8157527247522,-3.05734233798866));
#49598=CARTESIAN_POINT('Ctrl Pts',(369.788636750979,-24.8140009819724,-3.04844284487031));
#49599=CARTESIAN_POINT('Ctrl Pts',(369.771336317858,-24.8128429491999,-3.04245344509478));
#49600=CARTESIAN_POINT('Ctrl Pts',(369.635473765185,-24.8036630351799,-2.99411767027075));
#49601=CARTESIAN_POINT('Ctrl Pts',(369.519446179933,-24.7953107027065,-2.94500820969916));
#49602=CARTESIAN_POINT('Ctrl Pts',(369.237719907392,-24.7741943945758,-2.80579363204798));
#49603=CARTESIAN_POINT('Ctrl Pts',(369.076468127299,-24.7613567555453,-2.70768806915914));
#49604=CARTESIAN_POINT('Ctrl Pts',(368.850610676171,-24.7427634833968,-2.54155160852021));
#49605=CARTESIAN_POINT('Ctrl Pts',(368.778875998483,-24.736748506122,-2.48389612085732));
#49606=CARTESIAN_POINT('Ctrl Pts',(368.664648623588,-24.7270015686668,-2.38374558430222));
#49607=CARTESIAN_POINT('Ctrl Pts',(368.620704247582,-24.7232063679244,-2.34299448258911));
#49608=CARTESIAN_POINT('Ctrl Pts',(368.562442854931,-24.7181082446221,-2.28586337902372));
#49609=CARTESIAN_POINT('Ctrl Pts',(368.547119691573,-24.7167608045272,-2.27053121568268));
#49610=CARTESIAN_POINT('Ctrl Pts',(368.521638175581,-24.7145085004393,-2.24451498892669));
#49611=CARTESIAN_POINT('Ctrl Pts',(368.51139650745,-24.7136000178971,-2.23391388815233));
#49612=CARTESIAN_POINT('Ctrl Pts',(368.491315878479,-24.7118121794831,-2.21284110347961));
#49613=CARTESIAN_POINT('Ctrl Pts',(368.481473510801,-24.7109326879771,-2.20237315496441));
#49614=CARTESIAN_POINT('Ctrl Pts',(368.457736306143,-24.7088035255141,-2.17678646904523));
#49615=CARTESIAN_POINT('Ctrl Pts',(368.443915202735,-24.7075569874861,-2.16159995841331));
#49616=CARTESIAN_POINT('Ctrl Pts',(368.405082155698,-24.7040340641129,-2.11810256816424));
#49617=CARTESIAN_POINT('Ctrl Pts',(368.380421046954,-24.7017721168798,-2.08948204214576));
#49618=CARTESIAN_POINT('Ctrl Pts',(368.22345784469,-24.6871946865673,-1.90070496737995));
#49619=CARTESIAN_POINT('Ctrl Pts',(368.106396810433,-24.6755073333159,-1.72850492485538));
#49620=CARTESIAN_POINT('Ctrl Pts',(367.908279587927,-24.6524023262666,-1.36620364124558));
#49621=CARTESIAN_POINT('Ctrl Pts',(367.827270016994,-24.6410225564316,-1.17722327904833));
#49622=CARTESIAN_POINT('Ctrl Pts',(367.754874649746,-24.6268407545519,-0.950896249762951));
#49623=CARTESIAN_POINT('Ctrl Pts',(367.745441007328,-24.6248795069265,-0.91979006752573));
#49624=CARTESIAN_POINT('Ctrl Pts',(367.733171356619,-24.6221591993239,-0.8770130940487));
#49625=CARTESIAN_POINT('Ctrl Pts',(367.729927357094,-24.6214222110258,-0.865460107440159));
#49626=CARTESIAN_POINT('Ctrl Pts',(367.724582672227,-24.620177115909,-0.84600913422874));
#49627=CARTESIAN_POINT('Ctrl Pts',(367.722447342584,-24.6196709816418,-0.838120679040251));
#49628=CARTESIAN_POINT('Ctrl Pts',(367.718449441033,-24.6187064853374,-0.823125491887318));
#49629=CARTESIAN_POINT('Ctrl Pts',(367.716581122336,-24.618248462339,-0.816020349700292));
#49630=CARTESIAN_POINT('Ctrl Pts',(367.712192384105,-24.6171550802018,-0.799095054810847));
#49631=CARTESIAN_POINT('Ctrl Pts',(367.709693991064,-24.6165184813489,-0.789269323539435));
#49632=CARTESIAN_POINT('Ctrl Pts',(367.700998727986,-24.6142521411005,-0.754383993529306));
#49633=CARTESIAN_POINT('Ctrl Pts',(367.695056821389,-24.6126088849863,-0.729262659499962));
#49634=CARTESIAN_POINT('Ctrl Pts',(367.644210762084,-24.5976682215547,-0.502147501288212));
#49635=CARTESIAN_POINT('Ctrl Pts',(367.618560359983,-24.5835631112317,-0.296353905149716));
#49636=CARTESIAN_POINT('Ctrl Pts',(367.608444592571,-24.5589525710454,0.0675882832181993));
#49637=CARTESIAN_POINT('Ctrl Pts',(367.615578627539,-24.5484219776061,0.224841692000858));
#49638=CARTESIAN_POINT('Ctrl Pts',(367.640848444246,-24.5345278856317,0.437113961219011));
#49639=CARTESIAN_POINT('Ctrl Pts',(367.649010363277,-24.5308933608261,0.493084476890864));
#49640=CARTESIAN_POINT('Ctrl Pts',(367.665730274147,-24.5246614758267,0.589833139501906));
#49641=CARTESIAN_POINT('Ctrl Pts',(367.673613436201,-24.5220441082923,0.630712476995468));
#49642=CARTESIAN_POINT('Ctrl Pts',(367.686182511502,-24.5182875522315,0.689718126841434));
#49643=CARTESIAN_POINT('Ctrl Pts',(367.690237487035,-24.5171283371825,0.707973091989622));
#49644=CARTESIAN_POINT('Ctrl Pts',(367.697622558549,-24.5151056053922,0.739904231990943));
#49645=CARTESIAN_POINT('Ctrl Pts',(367.700883758669,-24.5142398970322,0.753595666965451));
#49646=CARTESIAN_POINT('Ctrl Pts',(367.707833107197,-24.5124504697705,0.781945749512933));
#49647=CARTESIAN_POINT('Ctrl Pts',(367.711534907162,-24.5115272161059,0.796600719543625));
#49648=CARTESIAN_POINT('Ctrl Pts',(367.721368043498,-24.5091496892589,0.834406722176211));
#49649=CARTESIAN_POINT('Ctrl Pts',(367.727654647783,-24.5077004784285,0.857516688720314));
#49650=CARTESIAN_POINT('Ctrl Pts',(367.754164313037,-24.5018622048959,0.950847753848242));
#49651=CARTESIAN_POINT('Ctrl Pts',(367.776516171631,-24.4975425793569,1.0204446884582));
#49652=CARTESIAN_POINT('Ctrl Pts',(367.91174684713,-24.4742387812159,1.3970134496823));
#49653=CARTESIAN_POINT('Ctrl Pts',(368.068460868441,-24.4568146728287,1.68613905001018));
#49654=CARTESIAN_POINT('Ctrl Pts',(368.294072103768,-24.4351298586021,1.98379263453229));
#49655=CARTESIAN_POINT('Ctrl Pts',(368.322970896775,-24.4323959671463,2.02025189505488));
#49656=CARTESIAN_POINT('Ctrl Pts',(368.372280468171,-24.4277781135113,2.07976837824262));
#49657=CARTESIAN_POINT('Ctrl Pts',(368.392251370031,-24.4259198657318,2.10318228528034));
#49658=CARTESIAN_POINT('Ctrl Pts',(368.420256956186,-24.423324539156,2.13507935857053));
#49659=CARTESIAN_POINT('Ctrl Pts',(368.428007762108,-24.4226073393088,2.14381100323403));
#49660=CARTESIAN_POINT('Ctrl Pts',(368.44118661164,-24.4213892975892,2.15849608015382));
#49661=CARTESIAN_POINT('Ctrl Pts',(368.446589937204,-24.4208902973008,2.16447172894608));
#49662=CARTESIAN_POINT('Ctrl Pts',(368.457004507245,-24.4199291385269,2.17590296018725));
#49663=CARTESIAN_POINT('Ctrl Pts',(368.462012207988,-24.4194672695119,2.18136158398425));
#49664=CARTESIAN_POINT('Ctrl Pts',(368.474044505634,-24.4183583093244,2.19438690475123));
#49665=CARTESIAN_POINT('Ctrl Pts',(368.481086681469,-24.4177099117997,2.20193714909296));
#49666=CARTESIAN_POINT('Ctrl Pts',(368.506646196549,-24.4153593122862,2.22907804030539));
#49667=CARTESIAN_POINT('Ctrl Pts',(368.525372302698,-24.4136423291366,2.2484693872613));
#49668=CARTESIAN_POINT('Ctrl Pts',(368.663434474271,-24.4010358399676,2.38789270398049));
#49669=CARTESIAN_POINT('Ctrl Pts',(368.79180902506,-24.3896077842501,2.49858222083691));
#49670=CARTESIAN_POINT('Ctrl Pts',(369.048805288126,-24.3680466591981,2.6870818749653));
#49671=CARTESIAN_POINT('Ctrl Pts',(369.175358541804,-24.3579426514072,2.76700631833854));
#49672=CARTESIAN_POINT('Ctrl Pts',(369.416006733603,-24.3399045566596,2.89652075102262));
#49673=CARTESIAN_POINT('Ctrl Pts',(369.528302107213,-24.3319085557739,2.94885879544395));
#49674=CARTESIAN_POINT('Ctrl Pts',(369.668799533226,-24.3224121125225,3.00473545055009));
#49675=CARTESIAN_POINT('Ctrl Pts',(369.694384471477,-24.3207023634977,3.01453479688036));
#49676=CARTESIAN_POINT('Ctrl Pts',(369.735040542545,-24.3180156013457,3.02951493747084));
#49677=CARTESIAN_POINT('Ctrl Pts',(369.750030027022,-24.3170314284073,3.03491207230534));
#49678=CARTESIAN_POINT('Ctrl Pts',(369.778264914666,-24.3151893938906,3.04484247837024));
#49679=CARTESIAN_POINT('Ctrl Pts',(369.791500978281,-24.314330713612,3.04940100711966));
#49680=CARTESIAN_POINT('Ctrl Pts',(369.821314062131,-24.3124072557553,3.05945188317832));
#49681=CARTESIAN_POINT('Ctrl Pts',(369.837906948615,-24.3113440832327,3.06489605599716));
#49682=CARTESIAN_POINT('Ctrl Pts',(369.880429384887,-24.3086377413946,3.0784659606429));
#49683=CARTESIAN_POINT('Ctrl Pts',(369.906419254964,-24.3070008556421,3.08639921916594));
#49684=CARTESIAN_POINT('Ctrl Pts',(370.089208444093,-24.2956025865504,3.13967689232167));
#49685=CARTESIAN_POINT('Ctrl Pts',(370.249162826964,-24.2862304451696,3.17338341285399));
#49686=CARTESIAN_POINT('Ctrl Pts',(370.509786338017,-24.2714012237934,3.20791628792476));
#49687=CARTESIAN_POINT('Ctrl Pts',(370.609127559571,-24.2658453950762,3.21641684016187));
#49688=CARTESIAN_POINT('Ctrl Pts',(370.893389874481,-24.2499163336759,3.22750509283093));
#49689=CARTESIAN_POINT('Ctrl Pts',(371.078329291471,-24.2395229202987,3.21880692367392));
#49690=CARTESIAN_POINT('Ctrl Pts',(371.281087576833,-24.2271569274619,3.19169326875078));
#49691=CARTESIAN_POINT('Ctrl Pts',(371.300675367745,-24.2259520033238,3.18889004700043));
#49692=CARTESIAN_POINT('Ctrl Pts',(371.329954868622,-24.2241338194649,3.18442430814373));
#49693=CARTESIAN_POINT('Ctrl Pts',(371.339667211896,-24.2235278853744,3.18289746066198));
#49694=CARTESIAN_POINT('Ctrl Pts',(371.356367178406,-24.2224809131446,3.18019374816224));
#49695=CARTESIAN_POINT('Ctrl Pts',(371.36335812424,-24.2220410826176,3.17903824514712));
#49696=CARTESIAN_POINT('Ctrl Pts',(371.379326052975,-24.2210328811139,3.17634484477636));
#49697=CARTESIAN_POINT('Ctrl Pts',(371.388300192321,-24.2204636866194,3.17479197332667));
#49698=CARTESIAN_POINT('Ctrl Pts',(371.412944970897,-24.2188937096521,3.17041980500747));
#49699=CARTESIAN_POINT('Ctrl Pts',(371.428601245566,-24.2178887090549,3.1675224240247));
#49700=CARTESIAN_POINT('Ctrl Pts',(371.510125350543,-24.2126179815457,3.15180973416503));
#49701=CARTESIAN_POINT('Ctrl Pts',(371.575597974716,-24.2082571103843,3.13705638151097));
#49702=CARTESIAN_POINT('Ctrl Pts',(371.871917901754,-24.1880737826883,3.06049102449278));
#49703=CARTESIAN_POINT('Ctrl Pts',(372.095911851213,-24.1716317433924,2.97516493087494));
#49704=CARTESIAN_POINT('Ctrl Pts',(372.308887474584,-24.1556842688952,2.86561725805281));
#49705=CARTESIAN_POINT('Ctrl Pts',(372.309354074345,-24.1556493282545,2.86537711030611));
#49706=CARTESIAN_POINT('Ctrl Pts',(372.309820613613,-24.1556143901908,2.86513684953877));
#49707=CARTESIAN_POINT('',(368.962731321485,-25.,-2.62360084935054));
#49708=CARTESIAN_POINT('Origin',(370.834317853224,-25.,0.));
#49709=CARTESIAN_POINT('',(367.611568051603,-24.8107734493349,0.00113077379776494));
#49710=CARTESIAN_POINT('Ctrl Pts',(367.611568051603,-24.8107734493349,0.00113077379776616));
#49711=CARTESIAN_POINT('Ctrl Pts',(367.611532632817,-24.8170524822338,-0.0998141594584466));
#49712=CARTESIAN_POINT('Ctrl Pts',(367.616244250843,-24.8233315151327,-0.200925999541271));
#49713=CARTESIAN_POINT('Ctrl Pts',(367.625723725616,-24.8296105480316,-0.301730486989598));
#49714=CARTESIAN_POINT('Ctrl Pts',(367.635188640088,-24.83587993645,-0.402380140575898));
#49715=CARTESIAN_POINT('Ctrl Pts',(367.649406805622,-24.8421493248684,-0.502722969158722));
#49716=CARTESIAN_POINT('Ctrl Pts',(367.668347051272,-24.8484187132868,-0.602284354511512));
#49717=CARTESIAN_POINT('Ctrl Pts',(367.687427772115,-24.8547346002331,-0.702584162427144));
#49718=CARTESIAN_POINT('Ctrl Pts',(367.711300931888,-24.8610504871795,-0.802090458055011));
#49719=CARTESIAN_POINT('Ctrl Pts',(367.739881201516,-24.8673663741259,-0.900321815278267));
#49720=CARTESIAN_POINT('Ctrl Pts',(367.768181811235,-24.8736204596831,-0.997591971898902));
#49721=CARTESIAN_POINT('Ctrl Pts',(367.801097712235,-24.8798745452403,-1.09361161824043));
#49722=CARTESIAN_POINT('Ctrl Pts',(367.838494790759,-24.8861286307975,-1.18792328914835));
#49723=CARTESIAN_POINT('Ctrl Pts',(367.87586737887,-24.8923786207103,-1.28217319769909));
#49724=CARTESIAN_POINT('Ctrl Pts',(367.917715153791,-24.8986286106231,-1.37471696939067));
#49725=CARTESIAN_POINT('Ctrl Pts',(367.963854745441,-24.9048786005359,-1.46511402605999));
#49726=CARTESIAN_POINT('Ctrl Pts',(368.009975053366,-24.9111259783083,-1.55547330190093));
#49727=CARTESIAN_POINT('Ctrl Pts',(368.060383419315,-24.9173733560808,-1.64368727742382));
#49728=CARTESIAN_POINT('Ctrl Pts',(368.114849422389,-24.9236207338533,-1.72933773919208));
#49729=CARTESIAN_POINT('Ctrl Pts',(368.17034034856,-24.9299856726988,-1.81659994280811));
#49730=CARTESIAN_POINT('Ctrl Pts',(368.230042973355,-24.9363506115444,-1.90120077635747));
#49731=CARTESIAN_POINT('Ctrl Pts',(368.293666270147,-24.94271555039,-1.98272718645562));
#49732=CARTESIAN_POINT('Ctrl Pts',(368.356124673653,-24.9489639521351,-2.06276091112919));
#49733=CARTESIAN_POINT('Ctrl Pts',(368.422361097585,-24.9552123538801,-2.13983153035847));
#49734=CARTESIAN_POINT('Ctrl Pts',(368.492059063977,-24.9614607556252,-2.21358110912948));
#49735=CARTESIAN_POINT('Ctrl Pts',(368.563706904731,-24.967883963021,-2.28939391040608));
#49736=CARTESIAN_POINT('Ctrl Pts',(368.639012527615,-24.9743071704168,-2.36169675026738));
#49737=CARTESIAN_POINT('Ctrl Pts',(368.71759196548,-24.9807303778126,-2.43014178159498));
#49738=CARTESIAN_POINT('Ctrl Pts',(368.796171403344,-24.9871535852084,-2.4985868129226));
#49739=CARTESIAN_POINT('Ctrl Pts',(368.878024270347,-24.9935767926042,-2.56317375500353));
#49740=CARTESIAN_POINT('Ctrl Pts',(368.962731321485,-25.,-2.62360084935057));
#49741=CARTESIAN_POINT('Ctrl Pts',(372.309820613641,-24.4036702759164,2.86513684952406));
#49742=CARTESIAN_POINT('Ctrl Pts',(372.306091397025,-24.4039307331992,2.86705734048141));
#49743=CARTESIAN_POINT('Ctrl Pts',(372.30235869357,-24.4041911904821,2.86897041531283));
#49744=CARTESIAN_POINT('Ctrl Pts',(372.298622535419,-24.404451647765,2.87087606144891));
#49745=CARTESIAN_POINT('Ctrl Pts',(372.210067064788,-24.4106250794922,2.91604422179583));
#49746=CARTESIAN_POINT('Ctrl Pts',(372.1192665904,-24.4167985112193,2.95718926796437));
#49747=CARTESIAN_POINT('Ctrl Pts',(372.02662222988,-24.4229719429465,2.99408213579816));
#49748=CARTESIAN_POINT('Ctrl Pts',(371.934101242199,-24.429137153625,3.03092587405992));
#49749=CARTESIAN_POINT('Ctrl Pts',(371.839741648865,-24.4353023643036,3.06352853005277));
#49750=CARTESIAN_POINT('Ctrl Pts',(371.743968650642,-24.4414675749822,3.09170713187007));
#49751=CARTESIAN_POINT('Ctrl Pts',(371.648294949118,-24.4476263936183,3.11985651833244));
#49752=CARTESIAN_POINT('Ctrl Pts',(371.551211170352,-24.4537852122544,3.14359084808161));
#49753=CARTESIAN_POINT('Ctrl Pts',(371.453161060238,-24.4599440308906,3.16277578206753));
#49754=CARTESIAN_POINT('Ctrl Pts',(371.355179532076,-24.4660985416906,3.18194729699424));
#49755=CARTESIAN_POINT('Ctrl Pts',(371.256233441068,-24.4722530524906,3.1965756592847));
#49756=CARTESIAN_POINT('Ctrl Pts',(371.156779335197,-24.4784075632906,3.20657701531455));
#49757=CARTESIAN_POINT('Ctrl Pts',(371.057360987235,-24.4845598612867,3.21657477543887));
#49758=CARTESIAN_POINT('Ctrl Pts',(370.957435418787,-24.4907121592828,3.22194879154235));
#49759=CARTESIAN_POINT('Ctrl Pts',(370.857466062772,-24.4968644572789,3.22266686501949));
#49760=CARTESIAN_POINT('Ctrl Pts',(370.757505958301,-24.5030161859181,3.2233848720434));
#49761=CARTESIAN_POINT('Ctrl Pts',(370.657502508378,-24.5091679145573,3.21944779003459));
#49762=CARTESIAN_POINT('Ctrl Pts',(370.557919914596,-24.5153196431964,3.21087554134724));
#49763=CARTESIAN_POINT('Ctrl Pts',(370.458319948442,-24.5214724450163,3.20230179721487));
#49764=CARTESIAN_POINT('Ctrl Pts',(370.359141416761,-24.5276252468362,3.18909131732326));
#49765=CARTESIAN_POINT('Ctrl Pts',(370.26084316178,-24.533778048656,3.17131586896868));
#49766=CARTESIAN_POINT('Ctrl Pts',(370.16243769844,-24.5399375609896,3.15352103393585));
#49767=CARTESIAN_POINT('Ctrl Pts',(370.064914856823,-24.5460970733231,3.1311513661488));
#49768=CARTESIAN_POINT('Ctrl Pts',(369.968722937462,-24.5522565856567,3.10432971900659));
#49769=CARTESIAN_POINT('Ctrl Pts',(369.87247588136,-24.5584196285928,3.07749269782637));
#49770=CARTESIAN_POINT('Ctrl Pts',(369.777561678892,-24.5645826715289,3.04619875142091));
#49771=CARTESIAN_POINT('Ctrl Pts',(369.684411120004,-24.5707457144651,3.01061988092088));
#49772=CARTESIAN_POINT('Ctrl Pts',(369.591104061668,-24.576919111744,2.97498123543201));
#49773=CARTESIAN_POINT('Ctrl Pts',(369.499566963191,-24.583092509023,2.93504346035694));
#49774=CARTESIAN_POINT('Ctrl Pts',(369.410208500937,-24.589265906302,2.89102578944393));
#49775=CARTESIAN_POINT('Ctrl Pts',(369.344098114509,-24.5938331925936,2.85846004065685));
#49776=CARTESIAN_POINT('Ctrl Pts',(369.279179732003,-24.5984004788852,2.82366213004029));
#49777=CARTESIAN_POINT('Ctrl Pts',(369.21560850966,-24.6029677651768,2.78673601612322));
#49778=CARTESIAN_POINT('Ctrl Pts',(369.130345774173,-24.6090934822642,2.73721012425808));
#49779=CARTESIAN_POINT('Ctrl Pts',(369.047195657591,-24.6152191993517,2.68367310090506));
#49780=CARTESIAN_POINT('Ctrl Pts',(368.966564492119,-24.6213449164392,2.62633108053452));
#49781=CARTESIAN_POINT('Ctrl Pts',(368.8860431591,-24.6274622893271,2.56906716910233));
#49782=CARTESIAN_POINT('Ctrl Pts',(368.808034316457,-24.6335796622151,2.50800881178686));
#49783=CARTESIAN_POINT('Ctrl Pts',(368.732919098709,-24.639697035103,2.44340762809323));
#49784=CARTESIAN_POINT('Ctrl Pts',(368.657883150478,-24.6458079522926,2.37887461839631));
#49785=CARTESIAN_POINT('Ctrl Pts',(368.585735091412,-24.6519188694821,2.31080649870567));
#49786=CARTESIAN_POINT('Ctrl Pts',(368.516825603552,-24.6580297866716,2.23949709426277));
#49787=CARTESIAN_POINT('Ctrl Pts',(368.447963610342,-24.6641364920193,2.16823683856927));
#49788=CARTESIAN_POINT('Ctrl Pts',(368.382336059312,-24.6702431973669,2.09374005345202));
#49789=CARTESIAN_POINT('Ctrl Pts',(368.320258416095,-24.6763499027146,2.01633893705434));
#49790=CARTESIAN_POINT('Ctrl Pts',(368.258202584804,-24.6824544623782,1.93896501671871));
#49791=CARTESIAN_POINT('Ctrl Pts',(368.199694460286,-24.6885590220418,1.85868913594861));
#49792=CARTESIAN_POINT('Ctrl Pts',(368.145009988683,-24.6946635817054,1.77587746542934));
#49793=CARTESIAN_POINT('Ctrl Pts',(368.090329549862,-24.70076769118,1.69307190196973));
#49794=CARTESIAN_POINT('Ctrl Pts',(368.039472447071,-24.7068718006545,1.60773128897416));
#49795=CARTESIAN_POINT('Ctrl Pts',(367.99267131847,-24.7129759101291,1.52025081286566));
#49796=CARTESIAN_POINT('Ctrl Pts',(367.945860647835,-24.719081264138,1.43275250082949));
#49797=CARTESIAN_POINT('Ctrl Pts',(367.903107802019,-24.7251866181468,1.343113848744));
#49798=CARTESIAN_POINT('Ctrl Pts',(367.864598960317,-24.7312919721557,1.25175367369583));
#49799=CARTESIAN_POINT('Ctrl Pts',(367.826044262477,-24.73740459639,1.16028470740223));
#49800=CARTESIAN_POINT('Ctrl Pts',(367.791743830973,-24.7435172206243,1.06709053296559));
#49801=CARTESIAN_POINT('Ctrl Pts',(367.761835195747,-24.7496298448586,0.972608802140001));
#49802=CARTESIAN_POINT('Ctrl Pts',(367.731908164023,-24.7557462289058,0.878068956563135));
#49803=CARTESIAN_POINT('Ctrl Pts',(367.706378417981,-24.7618626129531,0.78224040508794));
#49804=CARTESIAN_POINT('Ctrl Pts',(367.685332644382,-24.7679789970003,0.685572546850148));
#49805=CARTESIAN_POINT('Ctrl Pts',(367.664248227904,-24.7741066115537,0.588727193385713));
#49806=CARTESIAN_POINT('Ctrl Pts',(367.647664300376,-24.7802342261071,0.491039890785891));
#49807=CARTESIAN_POINT('Ctrl Pts',(367.635615838181,-24.7863618406604,0.392966896139527));
#49808=CARTESIAN_POINT('Ctrl Pts',(367.625704566898,-24.7914025213031,0.312290371633089));
#49809=CARTESIAN_POINT('Ctrl Pts',(367.618861470473,-24.7964432019457,0.231353040806152));
#49810=CARTESIAN_POINT('Ctrl Pts',(367.615079585837,-24.8014838825884,0.150407913003267));
#49811=CARTESIAN_POINT('Ctrl Pts',(367.612756350015,-24.8045804048166,0.100682805368083));
#49812=CARTESIAN_POINT('Ctrl Pts',(367.611585518489,-24.8076769270449,0.0509120444049194));
#49813=CARTESIAN_POINT('Ctrl Pts',(367.611568051603,-24.8107734492731,0.00113077479104779));
#49814=CARTESIAN_POINT('Ctrl Pts',(369.403995057531,0.413412695952972,2.88148094926035));
#49815=CARTESIAN_POINT('Ctrl Pts',(368.445565660651,0.347240656815754,2.40573134738565));
#49816=CARTESIAN_POINT('Ctrl Pts',(367.058003076544,0.214896578541317,0.429127078216204));
#49817=CARTESIAN_POINT('Ctrl Pts',(368.426799296739,0.0163804611296606,
-2.94632001420472));
#49818=CARTESIAN_POINT('Ctrl Pts',(372.004780269968,-0.182135656281995,
-3.6175583718889));
#49819=CARTESIAN_POINT('Ctrl Pts',(374.508790558812,-0.380651773693651,
-0.978876013732187));
#49820=CARTESIAN_POINT('Ctrl Pts',(373.64879697239,-0.579167891105306,2.55766308961752));
#49821=CARTESIAN_POINT('Ctrl Pts',(370.210870868906,-0.777684008516963,
3.75125713645417));
#49822=CARTESIAN_POINT('Ctrl Pts',(367.344120138506,-0.976200125928618,
1.50985201363752));
#49823=CARTESIAN_POINT('Ctrl Pts',(367.673512981428,-1.17471624334027,-2.11440641090759));
#49824=CARTESIAN_POINT('Ctrl Pts',(370.897565357316,-1.37323236075193,-3.80225470587514));
#49825=CARTESIAN_POINT('Ctrl Pts',(374.063670556472,-1.57174847816358,-2.00810758936603));
#49826=CARTESIAN_POINT('Ctrl Pts',(374.272408672299,-1.77026459557524,1.62504416509206));
#49827=CARTESIAN_POINT('Ctrl Pts',(371.332602492641,-1.9687807129869,3.77000274775842));
#49828=CARTESIAN_POINT('Ctrl Pts',(367.936479671958,-2.16729683039855,2.46246869320962));
#49829=CARTESIAN_POINT('Ctrl Pts',(367.194140510371,-2.36581294781021,-1.10014935901889));
#49830=CARTESIAN_POINT('Ctrl Pts',(369.78540720301,-2.56432906522186,-3.65527058599263));
#49831=CARTESIAN_POINT('Ctrl Pts',(373.337245985264,-2.76284518263352,-2.86296500849419));
#49832=CARTESIAN_POINT('Ctrl Pts',(374.596950954817,-2.96136130004518,0.551189689945338));
#49833=CARTESIAN_POINT('Ctrl Pts',(372.410908025683,-3.15987741745683,3.46057524628607));
#49834=CARTESIAN_POINT('Ctrl Pts',(368.781053843735,-3.35839353486848,3.20083187167307));
#49835=CARTESIAN_POINT('Ctrl Pts',(367.031539766512,-3.55690965228014,0.0098275299489643));
#49836=CARTESIAN_POINT('Ctrl Pts',(368.764537533245,-3.7554257696918,-3.19017666455396));
#49837=CARTESIAN_POINT('Ctrl Pts',(372.393000741445,-3.95394188710345,-3.46867775914217));
#49838=CARTESIAN_POINT('Ctrl Pts',(374.594051811918,-4.15245800451511,-0.570629740314608));
#49839=CARTESIAN_POINT('Ctrl Pts',(373.352010039771,-4.35097412192676,2.84999013879425));
#49840=CARTESIAN_POINT('Ctrl Pts',(369.804313655238,-4.54949023933842,3.6606432620171));
#49841=CARTESIAN_POINT('Ctrl Pts',(367.199875522236,-4.74800635675008,1.11894891838422));
#49842=CARTESIAN_POINT('Ctrl Pts',(367.923790541639,-4.94652247416173,-2.44745755988582));
#49843=CARTESIAN_POINT('Ctrl Pts',(371.31311110884,-5.14503859157339,-3.77252896046589));
#49844=CARTESIAN_POINT('Ctrl Pts',(374.263961920186,-5.34355470898505,-1.64279010012549));
#49845=CARTESIAN_POINT('Ctrl Pts',(374.074009933744,-5.5420708263967,1.99138468471137));
#49846=CARTESIAN_POINT('Ctrl Pts',(370.917209565446,-5.74058694380835,3.8018872554512));
#49847=CARTESIAN_POINT('Ctrl Pts',(367.68449854386,-5.93910306122002,2.13069379720876));
#49848=CARTESIAN_POINT('Ctrl Pts',(367.336332129874,-6.13761917863167,-1.4917485104219));
#49849=CARTESIAN_POINT('Ctrl Pts',(370.191554502588,-6.33613529604332,-3.74807590827464));
#49850=CARTESIAN_POINT('Ctrl Pts',(373.63540732516,-6.53465141345498,-2.57198668529261));
#49851=CARTESIAN_POINT('Ctrl Pts',(374.514075691705,-6.73316753086664,0.959479019705749));
#49852=CARTESIAN_POINT('Ctrl Pts',(372.022891826185,-6.93168364827829,3.61227208968389));
#49853=CARTESIAN_POINT('Ctrl Pts',(368.443234525303,-7.13019976568994,2.95701509263057));
#49854=CARTESIAN_POINT('Ctrl Pts',(367.053285852903,-7.32871588310161,-0.406220077862496));
#49855=CARTESIAN_POINT('Ctrl Pts',(369.125934363543,-7.52723200051325,-3.3974466281743));
#49856=CARTESIAN_POINT('Ctrl Pts',(372.763087977133,-7.72574811792492,-3.27735618269157));
#49857=CARTESIAN_POINT('Ctrl Pts',(374.633910600346,-7.92426423533656,-0.155925287024877));
#49858=CARTESIAN_POINT('Ctrl Pts',(373.025138461662,-8.12278035274823,3.10829902048574));
#49859=CARTESIAN_POINT('Ctrl Pts',(369.410054483599,-8.32129647015987,3.52600221115229));
#49860=CARTESIAN_POINT('Ctrl Pts',(367.099283807075,-8.51981258757154,0.714659648519558));
#49861=CARTESIAN_POINT('Ctrl Pts',(368.208986262136,-8.7183287049832,-2.75115462595943));
#49862=CARTESIAN_POINT('Ctrl Pts',(371.722917449212,-8.91684482239485,-3.69751382649478));
#49863=CARTESIAN_POINT('Ctrl Pts',(374.423086029239,-9.1153609398065,-1.25776019889706));
#49864=CARTESIAN_POINT('Ctrl Pts',(373.836728979282,-9.31387705721816,2.33382629371473));
#49865=CARTESIAN_POINT('Ctrl Pts',(370.500820931997,-9.51239317462982,3.78813906062597));
#49866=CARTESIAN_POINT('Ctrl Pts',(367.470323021388,-9.71090929204147,1.77334613386154));
#49867=CARTESIAN_POINT('Ctrl Pts',(367.520507587807,-9.90942540945314,-1.86544344967302));
#49868=CARTESIAN_POINT('Ctrl Pts',(370.605416559942,-10.1079415268648,-3.79589540649401));
#49869=CARTESIAN_POINT('Ctrl Pts',(373.899948982299,-10.3064576442765,-2.2501385556347));
#49870=CARTESIAN_POINT('Ctrl Pts',(374.387034731138,-10.5049737616881,1.35625238230104));
#49871=CARTESIAN_POINT('Ctrl Pts',(371.620609943024,-10.7034898790998,3.72061318718134));
#49872=CARTESIAN_POINT('Ctrl Pts',(368.134113815933,-10.9020059965114,2.67770720880823));
#49873=CARTESIAN_POINT('Ctrl Pts',(367.120413182867,-11.1005221139231,-0.817392095999423));
#49874=CARTESIAN_POINT('Ctrl Pts',(369.507835800956,-11.2990382313348,-3.56393926773715));
#49875=CARTESIAN_POINT('Ctrl Pts',(373.110025450149,-11.4975543487464,-3.0466986513945));
#49876=CARTESIAN_POINT('Ctrl Pts',(374.628165370627,-11.6960704661581,0.260650635541734));
#49877=CARTESIAN_POINT('Ctrl Pts',(372.6719719013,-11.8945865835697,3.32930102854965));
#49878=CARTESIAN_POINT('Ctrl Pts',(369.032889810631,-12.0931027009814,3.34904086963255));
#49879=CARTESIAN_POINT('Ctrl Pts',(367.043521254576,-12.291618818393,0.301792787818268));
#49880=CARTESIAN_POINT('Ctrl Pts',(368.525692114965,-12.4901349358047,-3.02183138837245));
#49881=CARTESIAN_POINT('Ctrl Pts',(372.122058511734,-12.6886510532163,-3.57811986041968));
#49882=CARTESIAN_POINT('Ctrl Pts',(374.539136508866,-12.887167170628,-0.857634227351326));
#49883=CARTESIAN_POINT('Ctrl Pts',(373.563412054284,-13.0856832880397,2.6482565171925));
#49884=CARTESIAN_POINT('Ctrl Pts',(370.088435043248,-13.2841994054513,3.72892431847192));
#49885=CARTESIAN_POINT('Ctrl Pts',(367.296523321393,-13.482715522863,1.39471416055649));
#49886=CARTESIAN_POINT('Ctrl Pts',(367.744456535802,-13.6812316402746,-2.21674869532011));
#49887=CARTESIAN_POINT('Ctrl Pts',(371.022025969311,-13.8797477576863,-3.7981552630539));
#49888=CARTESIAN_POINT('Ctrl Pts',(374.127695880695,-14.0782638750979,-1.90128348945687));
#49889=CARTESIAN_POINT('Ctrl Pts',(374.217352841214,-14.2767799925096,1.73674753753793));
#49890=CARTESIAN_POINT('Ctrl Pts',(371.208890711882,-14.4752961099213,3.78429820609665));
#49891=CARTESIAN_POINT('Ctrl Pts',(367.857401883721,-14.6738122273329,2.36626056249685));
#49892=CARTESIAN_POINT('Ctrl Pts',(367.232116073486,-14.8723283447446,-1.21875349318896));
#49893=CARTESIAN_POINT('Ctrl Pts',(369.905658131992,-15.0708444621562,-3.68765628296195));
#49894=CARTESIAN_POINT('Ctrl Pts',(373.429649098221,-15.2693605795679,-2.77947359545888));
#49895=CARTESIAN_POINT('Ctrl Pts',(374.576885078718,-15.4678766969795,0.674098139571492));
#49896=CARTESIAN_POINT('Ctrl Pts',(372.296749185285,-15.6663928143912,3.51034362108856));
#49897=CARTESIAN_POINT('Ctrl Pts',(368.677346496345,-15.8649089318029,3.1318831882287));
#49898=CARTESIAN_POINT('Ctrl Pts',(367.03325714609,-16.0634250492145,-0.114696293675766));
#49899=CARTESIAN_POINT('Ctrl Pts',(368.870106887587,-16.2619411666262,-3.25623909158683));
#49900=CARTESIAN_POINT('Ctrl Pts',(372.505743668162,-16.4604572840378,-3.41578006965798));
#49901=CARTESIAN_POINT('Ctrl Pts',(374.610720481307,-16.6589734014495,-0.447214634962899));
#49902=CARTESIAN_POINT('Ctrl Pts',(373.257339602449,-16.8574895188611,2.93090145550684));
#49903=CARTESIAN_POINT('Ctrl Pts',(369.685001496413,-17.0560056362728,3.62495374468069));
#49904=CARTESIAN_POINT('Ctrl Pts',(367.165185447629,-17.2545217536844,0.999342348407682));
#49905=CARTESIAN_POINT('Ctrl Pts',(368.005491061591,-17.4530378710961,-2.54144776102994));
#49906=CARTESIAN_POINT('Ctrl Pts',(371.43638244134,-17.6515539885078,-3.75482835437887));
#49907=CARTESIAN_POINT('Ctrl Pts',(374.315914523774,-17.8500701059194,-1.52960856519631));
#49908=CARTESIAN_POINT('Ctrl Pts',(374.007066602312,-18.0485862233311,2.09639765175277));
#49909=CARTESIAN_POINT('Ctrl Pts',(370.792675728515,-18.2471023407427,3.80256277693868));
#49910=CARTESIAN_POINT('Ctrl Pts',(367.616419920411,-18.4456184581544,2.02641324341738));
#49911=CARTESIAN_POINT('Ctrl Pts',(367.387053828267,-18.644134575566,-1.60548699195738));
#49912=CARTESIAN_POINT('Ctrl Pts',(370.314626556266,-18.8426506929777,-3.76711277970054));
#49913=CARTESIAN_POINT('Ctrl Pts',(373.71812268844,-19.0411668103893,-2.47888834187282));
#49914=CARTESIAN_POINT('Ctrl Pts',(374.480685208313,-19.239682927801,1.07945488597672));
#49915=CARTESIAN_POINT('Ctrl Pts',(371.903973865648,-19.4381990452126,3.64925386267693));
#49916=CARTESIAN_POINT('Ctrl Pts',(368.34769189384,-19.6367151626243,2.87713556806726));
#49917=CARTESIAN_POINT('Ctrl Pts',(367.068614674954,-19.8352312800359,-0.5298087507752));
#49918=CARTESIAN_POINT('Ctrl Pts',(369.238096795542,-20.0337473974476,-3.45156429385787));
#49919=CARTESIAN_POINT('Ctrl Pts',(372.869367797239,-20.2322635148593,-3.2124429119896));
#49920=CARTESIAN_POINT('Ctrl Pts',(374.63697877132,-20.4307796322709,-0.0314274191916297));
#49921=CARTESIAN_POINT('Ctrl Pts',(372.922185210146,-20.6292957496826,3.17836870779575));
#49922=CARTESIAN_POINT('Ctrl Pts',(369.295362440493,-20.8278118670942,3.47747522804387));
#49923=CARTESIAN_POINT('Ctrl Pts',(367.077885760591,-21.0263279845059,0.591976089517751));
#49924=CARTESIAN_POINT('Ctrl Pts',(368.300478142822,-21.2248441019175,-2.83564350463414));
#49925=CARTESIAN_POINT('Ctrl Pts',(371.843512719386,-21.4233602193292,-3.66643468906968));
#49926=CARTESIAN_POINT('Ctrl Pts',(374.462345862869,-21.6218763367409,-1.13957478593675));
#49927=CARTESIAN_POINT('Ctrl Pts',(373.758699908593,-21.8203924541525,2.43088614876417));
#49928=CARTESIAN_POINT('Ctrl Pts',(370.37696061784,-22.0189085715642,3.77518754079788));
#49929=CARTESIAN_POINT('Ctrl Pts',(367.414060130091,-22.2174246889758,1.66224450876473));
#49930=CARTESIAN_POINT('Ctrl Pts',(367.583367130122,-22.4159408063875,-1.9729514909897));
#49931=CARTESIAN_POINT('Ctrl Pts',(370.729831874048,-22.6144569237992,-3.80135383516712));
#49932=CARTESIAN_POINT('Ctrl Pts',(373.971985147174,-22.8129730412108,-2.14855322744992));
#49933=CARTESIAN_POINT('Ctrl Pts',(374.340717718146,-23.0114891586225,1.47186105312981));
#49934=CARTESIAN_POINT('Ctrl Pts',(371.498365692146,-23.2100052760341,3.74435329032221));
#49935=CARTESIAN_POINT('Ctrl Pts',(368.047871176115,-23.4085213934458,2.58787882708531));
#49936=CARTESIAN_POINT('Ctrl Pts',(367.149193215696,-23.6070375108574,-0.938610460621719));
#49937=CARTESIAN_POINT('Ctrl Pts',(369.625195865162,-23.8055536282691,-3.60536270908208));
#49938=CARTESIAN_POINT('Ctrl Pts',(373.208668628663,-24.0040697456807,-2.97075606325937));
#49939=CARTESIAN_POINT('Ctrl Pts',(374.617384679032,-24.2025858630924,0.38516659491335));
#49940=CARTESIAN_POINT('Ctrl Pts',(372.56241093661,-24.4011019805041,3.38679865628135));
#49941=CARTESIAN_POINT('Ctrl Pts',(368.923295180967,-24.5996180979157,3.29012759206182));
#49942=CARTESIAN_POINT('Ctrl Pts',(367.037251697264,-24.7981786416692,0.173073691602409));
#49943=CARTESIAN_POINT('Ctrl Pts',(368.095727704402,-24.9305671462855,-1.99893471883147));
#49944=CARTESIAN_POINT('Ctrl Pts',(368.967855604038,-24.9967836117645,-2.62012863412635));
#49945=CARTESIAN_POINT('Ctrl Pts',(369.297428771816,0.27503400748034,3.09616586027907));
#49946=CARTESIAN_POINT('Ctrl Pts',(368.267591535214,0.208861968343121,2.58497050577087));
#49947=CARTESIAN_POINT('Ctrl Pts',(366.776648517521,0.0765178900686841,
0.461099216927136));
#49948=CARTESIAN_POINT('Ctrl Pts',(368.247426982232,-0.121998227342972,
-3.16583576364755));
#49949=CARTESIAN_POINT('Ctrl Pts',(372.091985642559,-0.320514344754628,
-3.88708477544654));
#49950=CARTESIAN_POINT('Ctrl Pts',(374.782557368216,-0.519030462166284,
-1.05180722986966));
#49951=CARTESIAN_POINT('Ctrl Pts',(373.858489908038,-0.71754657957794,2.74822193157386));
#49952=CARTESIAN_POINT('Ctrl Pts',(370.164420913931,-0.916062696989595,
4.03074477448791));
#49953=CARTESIAN_POINT('Ctrl Pts',(367.084082748353,-1.11457881440125,1.62234362850746));
#49954=CARTESIAN_POINT('Ctrl Pts',(367.438017024802,-1.3130949318129,-2.27194038742045));
#49955=CARTESIAN_POINT('Ctrl Pts',(370.902277616403,-1.51161104922456,-4.08554192087854));
#49956=CARTESIAN_POINT('Ctrl Pts',(374.304273673394,-1.71012716663622,-2.15772176580187));
#49957=CARTESIAN_POINT('Ctrl Pts',(374.528563835066,-1.90864328404787,1.7461181781178));
#49958=CARTESIAN_POINT('Ctrl Pts',(371.369727219598,-2.10715940145953,4.05088702868714));
#49959=CARTESIAN_POINT('Ctrl Pts',(367.720576064387,-2.30567551887118,2.64593507094979));
#49960=CARTESIAN_POINT('Ctrl Pts',(366.922928879025,-2.50419163628284,-1.18211605302352));
#49961=CARTESIAN_POINT('Ctrl Pts',(369.707258052079,-2.7027077536945,-3.92760674032486));
#49962=CARTESIAN_POINT('Ctrl Pts',(373.523726795923,-2.90122387110615,-3.07627038823516));
#49963=CARTESIAN_POINT('Ctrl Pts',(374.877286159816,-3.09973998851781,0.592256110867064));
#49964=CARTESIAN_POINT('Ctrl Pts',(372.52837197108,-3.29825610592946,3.71840561265137));
#49965=CARTESIAN_POINT('Ctrl Pts',(368.628075285508,-3.49677222334112,3.4393100423278));
#49966=CARTESIAN_POINT('Ctrl Pts',(366.748213556987,-3.69528834075277,0.0105597306575114));
#49967=CARTESIAN_POINT('Ctrl Pts',(368.610328426315,-3.89380445816443,-3.4278609683629));
#49968=CARTESIAN_POINT('Ctrl Pts',(372.509130503555,-4.09232057557608,-3.72711180371402));
#49969=CARTESIAN_POINT('Ctrl Pts',(374.874171016102,-4.29083669298774,-0.613144543355595));
#49970=CARTESIAN_POINT('Ctrl Pts',(373.539590847196,-4.4893528103994,3.06232882508966));
#49971=CARTESIAN_POINT('Ctrl Pts',(369.727573130664,-4.68786892781105,3.93337970789892));
#49972=CARTESIAN_POINT('Ctrl Pts',(366.929091178293,-4.88638504522271,1.20231627468743));
#49973=CARTESIAN_POINT('Ctrl Pts',(367.706941529652,-5.08490116263436,-2.62980553223698));
#49974=CARTESIAN_POINT('Ctrl Pts',(371.348783629077,-5.28341728004602,-4.05360145702397));
#49975=CARTESIAN_POINT('Ctrl Pts',(374.519487757179,-5.48193339745768,-1.76518627510575));
#49976=CARTESIAN_POINT('Ctrl Pts',(374.315383386591,-5.68044951486934,2.13975292013245));
#49977=CARTESIAN_POINT('Ctrl Pts',(370.923385417439,-5.87896563228098,4.0851470935387));
#49978=CARTESIAN_POINT('Ctrl Pts',(367.449821067221,-6.07748174969265,2.28944126641531));
#49979=CARTESIAN_POINT('Ctrl Pts',(367.07571449367,-6.2759978671043,-1.60289132269847));
#49980=CARTESIAN_POINT('Ctrl Pts',(370.143665380582,-6.47451398451596,-4.02732652871198));
#49981=CARTESIAN_POINT('Ctrl Pts',(373.844102664337,-6.67303010192761,-2.76361270760422));
#49982=CARTESIAN_POINT('Ctrl Pts',(374.788236270252,-6.87154621933927,1.03096506163937));
#49983=CARTESIAN_POINT('Ctrl Pts',(372.111446601358,-7.07006233675092,3.88140463846864));
#49984=CARTESIAN_POINT('Ctrl Pts',(368.265086718486,-7.26857845416258,3.17732767953328));
#49985=CARTESIAN_POINT('Ctrl Pts',(366.771579836851,-7.46709457157424,-0.436485529137551));
#49986=CARTESIAN_POINT('Ctrl Pts',(368.998651149138,-7.66561068898589,-3.65057359305935));
#49987=CARTESIAN_POINT('Ctrl Pts',(372.906791110945,-7.86412680639755,-3.52153580173033));
#49988=CARTESIAN_POINT('Ctrl Pts',(374.916999485952,-8.0626429238092,-0.167542509890492));
#49989=CARTESIAN_POINT('Ctrl Pts',(373.188365682548,-8.26115904122086,3.33988302551057));
#49990=CARTESIAN_POINT('Ctrl Pts',(369.303939655786,-8.45967515863252,3.78870721746071));
#49991=CARTESIAN_POINT('Ctrl Pts',(366.821004871359,-8.65819127604416,0.767905408513408));
#49992=CARTESIAN_POINT('Ctrl Pts',(368.013385774417,-8.85670739345583,-2.95612956644076));
#49993=CARTESIAN_POINT('Ctrl Pts',(371.789122615428,-9.05522351086748,-3.97299731599531));
#49994=CARTESIAN_POINT('Ctrl Pts',(374.690467417526,-9.25373962827913,-1.3514696979838));
#49995=CARTESIAN_POINT('Ctrl Pts',(374.060423800379,-9.45225574569079,2.50770816176172));
#49996=CARTESIAN_POINT('Ctrl Pts',(370.47597372387,-9.65077186310245,4.07037458863311));
#49997=CARTESIAN_POINT('Ctrl Pts',(367.219688384595,-9.84928798051411,1.90546939396889));
#49998=CARTESIAN_POINT('Ctrl Pts',(367.273611955148,-10.0478040979258,-2.00442842582086));
#49999=CARTESIAN_POINT('Ctrl Pts',(370.588362255352,-10.2463202153375,-4.07870882151544));
#50000=CARTESIAN_POINT('Ctrl Pts',(374.128354013515,-10.4448363327491,-2.41778526373467));
#50001=CARTESIAN_POINT('Ctrl Pts',(374.651730115297,-10.6433524501608,1.45730004742194));
#50002=CARTESIAN_POINT('Ctrl Pts',(371.679192682353,-10.8418685675723,3.99781769593581));
#50003=CARTESIAN_POINT('Ctrl Pts',(367.932934952118,-11.0403846849841,2.87720994506778));
#50004=CARTESIAN_POINT('Ctrl Pts',(366.843708492561,-11.2389008023958,-0.878291943156831));
#50005=CARTESIAN_POINT('Ctrl Pts',(369.409006176061,-11.4374169198074,-3.82947077672271));
#50006=CARTESIAN_POINT('Ctrl Pts',(373.279577181204,-11.6359330372191,-3.2736931172241));
#50007=CARTESIAN_POINT('Ctrl Pts',(374.910826207548,-11.8344491546307,0.280070426782248));
#50008=CARTESIAN_POINT('Ctrl Pts',(372.808886426414,-12.0329652720424,3.57735080144582));
#50009=CARTESIAN_POINT('Ctrl Pts',(368.898674306229,-12.231481389454,3.59856136057304));
#50010=CARTESIAN_POINT('Ctrl Pts',(366.761087726538,-12.4299975068657,0.324277877582813));
#50011=CARTESIAN_POINT('Ctrl Pts',(368.353687815814,-12.6285136242772,-3.24697311727847));
#50012=CARTESIAN_POINT('Ctrl Pts',(372.218001706763,-12.827029741689,-3.84470789531392));
#50013=CARTESIAN_POINT('Ctrl Pts',(374.8151642451,-13.0255458591006,-0.921532316919773));
#50014=CARTESIAN_POINT('Ctrl Pts',(373.766743381484,-13.2240619765122,2.84556502790608));
#50015=CARTESIAN_POINT('Ctrl Pts',(370.032862999737,-13.422578093924,4.00674804856188));
#50016=CARTESIAN_POINT('Ctrl Pts',(367.032939727526,-13.6210942113356,1.49862742277415));
#50017=CARTESIAN_POINT('Ctrl Pts',(367.51424623295,-13.8196103287473,-2.38190768987384));
#50018=CARTESIAN_POINT('Ctrl Pts',(371.036011173762,-14.0181264461589,-4.08113704882393));
#50019=CARTESIAN_POINT('Ctrl Pts',(374.373069208241,-14.2166425635706,-2.04293872991932));
#50020=CARTESIAN_POINT('Ctrl Pts',(374.469406065983,-14.4151586809822,1.86614401703017));
#50021=CARTESIAN_POINT('Ctrl Pts',(371.236798285191,-14.6136747983939,4.06624757100662));
#50022=CARTESIAN_POINT('Ctrl Pts',(367.635606580794,-14.8121909158055,2.54255894768561));
#50023=CARTESIAN_POINT('Ctrl Pts',(366.963733813749,-15.0107070332172,-1.30955679532639));
#50024=CARTESIAN_POINT('Ctrl Pts',(369.83646828374,-15.2092231506288,-3.96240533559008));
#50025=CARTESIAN_POINT('Ctrl Pts',(373.623014408354,-15.4077392680404,-2.98655844246201));
#50026=CARTESIAN_POINT('Ctrl Pts',(374.855725274414,-15.6062553854522,0.724321861907345));
#50027=CARTESIAN_POINT('Ctrl Pts',(372.405707719428,-15.8047715028638,3.77188198320471));
#50028=CARTESIAN_POINT('Ctrl Pts',(368.516641215978,-16.0032876202755,3.36522433308636));
#50029=CARTESIAN_POINT('Ctrl Pts',(366.750058890034,-16.2018037376871,-0.123241747918035));
#50030=CARTESIAN_POINT('Ctrl Pts',(368.723763231736,-16.4003198550988,-3.49884538048572));
#50031=CARTESIAN_POINT('Ctrl Pts',(372.630273348791,-16.5988359725103,-3.67027296870085));
#50032=CARTESIAN_POINT('Ctrl Pts',(374.892081585703,-16.7973520899221,-0.480534388174527));
#50033=CARTESIAN_POINT('Ctrl Pts',(373.437866983261,-16.9958682073337,3.14926844430875));
#50034=CARTESIAN_POINT('Ctrl Pts',(369.599371612288,-17.1943843247454,3.89503114093192));
#50035=CARTESIAN_POINT('Ctrl Pts',(366.891816517596,-17.3929004421571,1.07379841003817));
#50036=CARTESIAN_POINT('Ctrl Pts',(367.794729151745,-17.5914165595686,-2.73079847895693));
#50037=CARTESIAN_POINT('Ctrl Pts',(371.481239299601,-17.7899326769803,-4.03458206621836));
#50038=CARTESIAN_POINT('Ctrl Pts',(374.575311092616,-17.9884487943919,-1.64357214312557));
#50039=CARTESIAN_POINT('Ctrl Pts',(374.243452438233,-18.1869649118037,2.25258988458425));
#50040=CARTESIAN_POINT('Ctrl Pts',(370.789573179515,-18.3854810292153,4.08587294479514));
#50041=CARTESIAN_POINT('Ctrl Pts',(367.376670241846,-18.5839971466269,2.17739128370667));
#50042=CARTESIAN_POINT('Ctrl Pts',(367.130215215246,-18.7825132640387,-1.72510389662527));
#50043=CARTESIAN_POINT('Ctrl Pts',(370.275906925004,-18.9810293814502,-4.04778174338571));
#50044=CARTESIAN_POINT('Ctrl Pts',(373.932980740722,-19.179545498862,-2.66357806652187));
#50045=CARTESIAN_POINT('Ctrl Pts',(374.752358026892,-19.3780616162735,1.15987973702563));
#50046=CARTESIAN_POINT('Ctrl Pts',(371.983668651035,-19.5765777336853,3.92114174067749));
#50047=CARTESIAN_POINT('Ctrl Pts',(368.162425677533,-19.7750938510969,3.09149672619948));
#50048=CARTESIAN_POINT('Ctrl Pts',(366.788050733709,-19.9736099685086,-0.569282183541161));
#50049=CARTESIAN_POINT('Ctrl Pts',(369.119170249864,-20.1721260859203,-3.70872329867184));
#50050=CARTESIAN_POINT('Ctrl Pts',(373.020989315425,-20.3706422033319,-3.45178616389979));
#50051=CARTESIAN_POINT('Ctrl Pts',(374.920296251189,-20.5691583207435,-0.0337689209442362));
#50052=CARTESIAN_POINT('Ctrl Pts',(373.07774189285,-20.7676744381551,3.41517325907793));
#50053=CARTESIAN_POINT('Ctrl Pts',(369.180702475126,-20.9661905555669,3.7365647285641));
#50054=CARTESIAN_POINT('Ctrl Pts',(366.798012562137,-21.1647066729785,0.636081303586939));
#50055=CARTESIAN_POINT('Ctrl Pts',(368.111694263164,-21.3632227903902,-3.04691329409063));
#50056=CARTESIAN_POINT('Ctrl Pts',(371.918702843443,-21.5617389078019,-3.93960262557153));
#50057=CARTESIAN_POINT('Ctrl Pts',(374.732652307415,-21.7602550252134,-1.22447887373956));
#50058=CARTESIAN_POINT('Ctrl Pts',(373.976581169097,-21.9587711426251,2.61199946713539));
#50059=CARTESIAN_POINT('Ctrl Pts',(370.342885189575,-22.1572872600367,4.05645811504312));
#50060=CARTESIAN_POINT('Ctrl Pts',(367.159233623208,-22.3558033774484,1.78609013562795));
#50061=CARTESIAN_POINT('Ctrl Pts',(367.341154851434,-22.5543194948601,-2.11994636020653));
#50062=CARTESIAN_POINT('Ctrl Pts',(370.7220471399,-22.7528356122718,-4.08457393074435));
#50063=CARTESIAN_POINT('Ctrl Pts',(374.205757237175,-22.9513517296833,-2.30863131457819));
#50064=CARTESIAN_POINT('Ctrl Pts',(374.601962250472,-23.149867847095,1.58152214920754));
#50065=CARTESIAN_POINT('Ctrl Pts',(371.547840616229,-23.3483839645068,4.02332655688563));
#50066=CARTESIAN_POINT('Ctrl Pts',(367.840266799244,-23.5469000819183,2.78068889437474));
#50067=CARTESIAN_POINT('Ctrl Pts',(366.874632783463,-23.7454161993299,-1.00854168930863));
#50068=CARTESIAN_POINT('Ctrl Pts',(369.535110158892,-23.9439323167417,-3.87398047405052));
#50069=CARTESIAN_POINT('Ctrl Pts',(373.385569775652,-24.1424484341533,-3.19209242200327));
#50070=CARTESIAN_POINT('Ctrl Pts',(374.899242299879,-24.340964551565,0.41386345517803));
#50071=CARTESIAN_POINT('Ctrl Pts',(372.691162615477,-24.5394806689767,3.63913229338162));
#50072=CARTESIAN_POINT('Ctrl Pts',(368.780914322106,-24.7379967863883,3.53525874572201));
#50073=CARTESIAN_POINT('Ctrl Pts',(366.754351055484,-24.9365573301418,0.185968557380015));
#50074=CARTESIAN_POINT('Ctrl Pts',(367.891688881044,-25.0689458347581,-2.14786546999769));
#50075=CARTESIAN_POINT('Ctrl Pts',(368.828794722171,-25.1351623002372,-2.81534147522438));
#50076=CARTESIAN_POINT('Ctrl Pts',(369.190862486101,0.136655319007707,3.3108507712978));
#50077=CARTESIAN_POINT('Ctrl Pts',(368.089617409777,0.0704832798704884,
2.76420966415609));
#50078=CARTESIAN_POINT('Ctrl Pts',(366.495293958499,-0.0618607984039484,
0.493071355638064));
#50079=CARTESIAN_POINT('Ctrl Pts',(368.068054667726,-0.260376915815605,
-3.38535151309038));
#50080=CARTESIAN_POINT('Ctrl Pts',(372.179191015148,-0.458893033227261,
-4.15661117900418));
#50081=CARTESIAN_POINT('Ctrl Pts',(375.056324177621,-0.657409150638917,
-1.12473844600715));
#50082=CARTESIAN_POINT('Ctrl Pts',(374.068182843686,-0.855925268050571,
2.93878077353021));
#50083=CARTESIAN_POINT('Ctrl Pts',(370.117970958957,-1.05444138546223,4.31023241252165));
#50084=CARTESIAN_POINT('Ctrl Pts',(366.8240453582,-1.25295750287388,1.73483524337741));
#50085=CARTESIAN_POINT('Ctrl Pts',(367.202521068174,-1.45147362028554,-2.4294743639333));
#50086=CARTESIAN_POINT('Ctrl Pts',(370.90698987549,-1.6499897376972,-4.36882913588193));
#50087=CARTESIAN_POINT('Ctrl Pts',(374.544876790316,-1.84850585510885,-2.30733594223771));
#50088=CARTESIAN_POINT('Ctrl Pts',(374.784718997833,-2.04702197252051,1.86719219114356));
#50089=CARTESIAN_POINT('Ctrl Pts',(371.406851946557,-2.24553808993216,4.33177130961586));
#50090=CARTESIAN_POINT('Ctrl Pts',(367.504672456816,-2.44405420734382,2.82940144868998));
#50091=CARTESIAN_POINT('Ctrl Pts',(366.651717247679,-2.64257032475548,-1.26408274702814));
#50092=CARTESIAN_POINT('Ctrl Pts',(369.629108901149,-2.84108644216713,-4.19994289465708));
#50093=CARTESIAN_POINT('Ctrl Pts',(373.71020760658,-3.03960255957878,-3.28957576797611));
#50094=CARTESIAN_POINT('Ctrl Pts',(375.157621364815,-3.23811867699044,0.633322531788789));
#50095=CARTESIAN_POINT('Ctrl Pts',(372.645835916477,-3.4366347944021,3.97623597901668));
#50096=CARTESIAN_POINT('Ctrl Pts',(368.475096727281,-3.63515091181375,3.67778821298252));
#50097=CARTESIAN_POINT('Ctrl Pts',(366.464887347464,-3.83366702922541,0.0112919313660596));
#50098=CARTESIAN_POINT('Ctrl Pts',(368.456119319384,-4.03218314663707,-3.66554527217185));
#50099=CARTESIAN_POINT('Ctrl Pts',(372.625260265666,-4.23069926404872,-3.98554584828585));
#50100=CARTESIAN_POINT('Ctrl Pts',(375.154290220285,-4.42921538146038,-0.655659346396582));
#50101=CARTESIAN_POINT('Ctrl Pts',(373.727171654621,-4.62773149887203,3.27466751138507));
#50102=CARTESIAN_POINT('Ctrl Pts',(369.650832606091,-4.82624761628369,4.20611615378073));
#50103=CARTESIAN_POINT('Ctrl Pts',(366.658306834349,-5.02476373369535,1.28568363099063));
#50104=CARTESIAN_POINT('Ctrl Pts',(367.490092517666,-5.22327985110699,-2.81215350458813));
#50105=CARTESIAN_POINT('Ctrl Pts',(371.384456149316,-5.42179596851866,-4.33467395358205));
#50106=CARTESIAN_POINT('Ctrl Pts',(374.775013594174,-5.62031208593031,-1.887582450086));
#50107=CARTESIAN_POINT('Ctrl Pts',(374.556756839438,-5.81882820334197,2.28812115555352));
#50108=CARTESIAN_POINT('Ctrl Pts',(370.929561269431,-6.01734432075362,4.36840693162621));
#50109=CARTESIAN_POINT('Ctrl Pts',(367.215143590582,-6.21586043816528,2.44818873562185));
#50110=CARTESIAN_POINT('Ctrl Pts',(366.815096857467,-6.41437655557694,-1.71403413497503));
#50111=CARTESIAN_POINT('Ctrl Pts',(370.095776258576,-6.61289267298859,-4.30657714914931));
#50112=CARTESIAN_POINT('Ctrl Pts',(374.052798003513,-6.81140879040025,-2.95523872991583));
#50113=CARTESIAN_POINT('Ctrl Pts',(375.0623968488,-7.0099249078119,1.10245110357299));
#50114=CARTESIAN_POINT('Ctrl Pts',(372.20000137653,-7.20844102522356,4.1505371872534));
#50115=CARTESIAN_POINT('Ctrl Pts',(368.086938911671,-7.40695714263521,3.397640266436));
#50116=CARTESIAN_POINT('Ctrl Pts',(366.489873820798,-7.60547326004687,-0.466750980412602));
#50117=CARTESIAN_POINT('Ctrl Pts',(368.871367934734,-7.80398937745853,-3.90370055794442));
#50118=CARTESIAN_POINT('Ctrl Pts',(373.050494244756,-8.00250549487018,-3.76571542076907));
#50119=CARTESIAN_POINT('Ctrl Pts',(375.200088371559,-8.20102161228184,-0.179159732756115));
#50120=CARTESIAN_POINT('Ctrl Pts',(373.351592903432,-8.3995377296935,3.57146703053541));
#50121=CARTESIAN_POINT('Ctrl Pts',(369.197824827974,-8.59805384710515,4.05141222376914));
#50122=CARTESIAN_POINT('Ctrl Pts',(366.542725935641,-8.7965699645168,0.82115116850726));
#50123=CARTESIAN_POINT('Ctrl Pts',(367.817785286697,-8.99508608192846,-3.1611045069221));
#50124=CARTESIAN_POINT('Ctrl Pts',(371.855327781645,-9.19360219934012,-4.24848080549583));
#50125=CARTESIAN_POINT('Ctrl Pts',(374.957848805812,-9.39211831675177,-1.44517919707054));
#50126=CARTESIAN_POINT('Ctrl Pts',(374.284118621476,-9.59063443416343,2.68159002980871));
#50127=CARTESIAN_POINT('Ctrl Pts',(370.451126515743,-9.78915055157509,4.35261011664025));
#50128=CARTESIAN_POINT('Ctrl Pts',(366.969053747804,-9.98766666898675,2.03759265407625));
#50129=CARTESIAN_POINT('Ctrl Pts',(367.026716322489,-10.1861827863983,-2.1434134019687));
#50130=CARTESIAN_POINT('Ctrl Pts',(370.57130795076,-10.38469890381,-4.36152223653687));
#50131=CARTESIAN_POINT('Ctrl Pts',(374.35675904473,-10.5832150212217,-2.58543197183465));
#50132=CARTESIAN_POINT('Ctrl Pts',(374.916425499454,-10.7817311386333,1.55834771254285));
#50133=CARTESIAN_POINT('Ctrl Pts',(371.737775421683,-10.980247256045,4.27502220469027));
#50134=CARTESIAN_POINT('Ctrl Pts',(367.731756088302,-11.1787633734566,3.07671268132734));
#50135=CARTESIAN_POINT('Ctrl Pts',(366.567003802255,-11.3772794908683,-0.939191790314244));
#50136=CARTESIAN_POINT('Ctrl Pts',(369.310176551165,-11.5757956082799,-4.09500228570826));
#50137=CARTESIAN_POINT('Ctrl Pts',(373.44912891226,-11.7743117256916,-3.50068758305369));
#50138=CARTESIAN_POINT('Ctrl Pts',(375.193487044471,-11.9728278431033,0.299490218022766));
#50139=CARTESIAN_POINT('Ctrl Pts',(372.945800951528,-12.1713439605149,3.82540057434197));
#50140=CARTESIAN_POINT('Ctrl Pts',(368.764458801828,-12.3698600779266,3.84808185151355));
#50141=CARTESIAN_POINT('Ctrl Pts',(366.478654198501,-12.5683761953382,0.346762967347356));
#50142=CARTESIAN_POINT('Ctrl Pts',(368.181683516663,-12.7668923127499,-3.4721148461845));
#50143=CARTESIAN_POINT('Ctrl Pts',(372.313944901792,-12.9654084301615,-4.11129593020815));
#50144=CARTESIAN_POINT('Ctrl Pts',(375.091191981334,-13.1639245475732,-0.985430406488218));
#50145=CARTESIAN_POINT('Ctrl Pts',(373.970074708685,-13.3624406649849,3.04287353861967));
#50146=CARTESIAN_POINT('Ctrl Pts',(369.977290956225,-13.5609567823965,4.28457177865185));
#50147=CARTESIAN_POINT('Ctrl Pts',(366.769356133657,-13.7594728998082,1.60254068499181));
#50148=CARTESIAN_POINT('Ctrl Pts',(367.284035930099,-13.9579890172198,-2.54706668442758));
#50149=CARTESIAN_POINT('Ctrl Pts',(371.049996378214,-14.1565051346315,-4.36411883459395));
#50150=CARTESIAN_POINT('Ctrl Pts',(374.618442535786,-14.3550212520431,-2.18459397038178));
#50151=CARTESIAN_POINT('Ctrl Pts',(374.721459290751,-14.5535373694548,1.99554049652239));
#50152=CARTESIAN_POINT('Ctrl Pts',(371.2647058585,-14.7520534868664,4.34819693591658));
#50153=CARTESIAN_POINT('Ctrl Pts',(367.413811277865,-14.9505696042781,2.71885733287438));
#50154=CARTESIAN_POINT('Ctrl Pts',(366.69535155401,-15.1490857216897,-1.40036009746382));
#50155=CARTESIAN_POINT('Ctrl Pts',(369.767278435489,-15.3476018391014,-4.2371543882182));
#50156=CARTESIAN_POINT('Ctrl Pts',(373.816379718487,-15.5461179565131,-3.19364328946513));
#50157=CARTESIAN_POINT('Ctrl Pts',(375.134565470109,-15.7446340739247,0.774545584243195));
#50158=CARTESIAN_POINT('Ctrl Pts',(372.514666253572,-15.9431501913364,4.03342034532087));
#50159=CARTESIAN_POINT('Ctrl Pts',(368.355935935611,-16.141666308748,3.59856547794402));
#50160=CARTESIAN_POINT('Ctrl Pts',(366.466860633978,-16.3401824261597,-0.1317872021603));
#50161=CARTESIAN_POINT('Ctrl Pts',(368.577419575885,-16.5386985435713,-3.74145166938463));
#50162=CARTESIAN_POINT('Ctrl Pts',(372.754803029422,-16.737214660983,-3.92476586774372));
#50163=CARTESIAN_POINT('Ctrl Pts',(375.173442690099,-16.9357307783947,-0.513854141386156));
#50164=CARTESIAN_POINT('Ctrl Pts',(373.618394364073,-17.1342468958063,3.36763543311066));
#50165=CARTESIAN_POINT('Ctrl Pts',(369.513741728162,-17.332763013218,4.16510853718315));
#50166=CARTESIAN_POINT('Ctrl Pts',(366.618447587562,-17.5312791306296,1.14825447166867));
#50167=CARTESIAN_POINT('Ctrl Pts',(367.5839672419,-17.7297952480413,-2.9201491968839));
#50168=CARTESIAN_POINT('Ctrl Pts',(371.526096157864,-17.9283113654529,-4.31433577805786));
#50169=CARTESIAN_POINT('Ctrl Pts',(374.834707661457,-18.1268274828646,-1.75753572105482));
#50170=CARTESIAN_POINT('Ctrl Pts',(374.479838274154,-18.3253436002762,2.40878211741571));
#50171=CARTESIAN_POINT('Ctrl Pts',(370.786470630515,-18.5238597176879,4.3691831126516));
#50172=CARTESIAN_POINT('Ctrl Pts',(367.136920563282,-18.7223758350996,2.32836932399598));
#50173=CARTESIAN_POINT('Ctrl Pts',(366.873376602224,-18.9208919525112,-1.84472080129315));
#50174=CARTESIAN_POINT('Ctrl Pts',(370.237187293741,-19.1194080699229,-4.32845070707088));
#50175=CARTESIAN_POINT('Ctrl Pts',(374.147838793003,-19.3179241873345,-2.84826779117091));
#50176=CARTESIAN_POINT('Ctrl Pts',(375.024030845472,-19.5164403047462,1.24030458807455));
#50177=CARTESIAN_POINT('Ctrl Pts',(372.063363436422,-19.7149564221578,4.19302961867807));
#50178=CARTESIAN_POINT('Ctrl Pts',(367.977159461227,-19.9134725395695,3.30585788433169));
#50179=CARTESIAN_POINT('Ctrl Pts',(366.507486792462,-20.1119886569812,-0.608755616307119));
#50180=CARTESIAN_POINT('Ctrl Pts',(369.000243704185,-20.3105047743928,-3.96588230348581));
#50181=CARTESIAN_POINT('Ctrl Pts',(373.17261083361,-20.5090208918045,-3.69112941580997));
#50182=CARTESIAN_POINT('Ctrl Pts',(375.203613731058,-20.7075370092161,-0.0361104226968403));
#50183=CARTESIAN_POINT('Ctrl Pts',(373.233298575554,-20.9060531266278,3.65197781036011));
#50184=CARTESIAN_POINT('Ctrl Pts',(369.066042509761,-21.1045692440394,3.99565422908433));
#50185=CARTESIAN_POINT('Ctrl Pts',(366.518139363681,-21.3030853614511,0.680186517656126));
#50186=CARTESIAN_POINT('Ctrl Pts',(367.922910383506,-21.5016014788627,-3.25818308354711));
#50187=CARTESIAN_POINT('Ctrl Pts',(371.9938929675,-21.7001175962744,-4.21277056207339));
#50188=CARTESIAN_POINT('Ctrl Pts',(375.002958751962,-21.898633713686,-1.30938296154235));
#50189=CARTESIAN_POINT('Ctrl Pts',(374.1944624296,-22.0971498310977,2.79311278550661));
#50190=CARTESIAN_POINT('Ctrl Pts',(370.30880976131,-22.2956659485093,4.33772868928835));
#50191=CARTESIAN_POINT('Ctrl Pts',(366.904407116324,-22.494182065921,1.90993576249118));
#50192=CARTESIAN_POINT('Ctrl Pts',(367.098942572746,-22.6926981833327,-2.26694122942334));
#50193=CARTESIAN_POINT('Ctrl Pts',(370.714262405752,-22.8912143007443,-4.36779402632158));
#50194=CARTESIAN_POINT('Ctrl Pts',(374.439529327177,-23.089730418156,-2.46870940170645));
#50195=CARTESIAN_POINT('Ctrl Pts',(374.863206782798,-23.2882465355676,1.69118324528528));
#50196=CARTESIAN_POINT('Ctrl Pts',(371.597315540312,-23.4867626529793,4.30229982344905));
#50197=CARTESIAN_POINT('Ctrl Pts',(367.632662422374,-23.6852787703909,2.97349896166417));
#50198=CARTESIAN_POINT('Ctrl Pts',(366.600072351229,-23.8837948878026,-1.07847291799555));
#50199=CARTESIAN_POINT('Ctrl Pts',(369.445024452623,-24.0823110052143,-4.14259823901896));
#50200=CARTESIAN_POINT('Ctrl Pts',(373.562470922641,-24.2808271226259,-3.41342878074717));
#50201=CARTESIAN_POINT('Ctrl Pts',(375.181099920727,-24.4793432400376,0.442560315442714));
#50202=CARTESIAN_POINT('Ctrl Pts',(372.819914294343,-24.6778593574493,3.89146593048189));
#50203=CARTESIAN_POINT('Ctrl Pts',(368.638533463245,-24.876375474861,3.7803898993822));
#50204=CARTESIAN_POINT('Ctrl Pts',(366.471450413703,-25.0749360186145,0.198863423157614));
#50205=CARTESIAN_POINT('Ctrl Pts',(367.687650057685,-25.2073245232308,-2.2967962211639));
#50206=CARTESIAN_POINT('Ctrl Pts',(368.689733840303,-25.2735409887098,-3.01055431632241));
#50207=CARTESIAN_POINT('Ctrl Pts',(369.084296200386,-0.00172336946492562,
3.52553568231652));
#50208=CARTESIAN_POINT('Ctrl Pts',(367.91164328434,-0.0678954086021442,
2.94344882254131));
#50209=CARTESIAN_POINT('Ctrl Pts',(366.213939399476,-0.200239486876582,
0.525043494348995));
#50210=CARTESIAN_POINT('Ctrl Pts',(367.888682353219,-0.398755604288238,
-3.60486726253322));
#50211=CARTESIAN_POINT('Ctrl Pts',(372.266396387737,-0.597271721699893,
-4.42613758256182));
#50212=CARTESIAN_POINT('Ctrl Pts',(375.330090987025,-0.79578783911155,-1.19766966214462));
#50213=CARTESIAN_POINT('Ctrl Pts',(374.277875779333,-0.994303956523205,
3.12933961548655));
#50214=CARTESIAN_POINT('Ctrl Pts',(370.071521003981,-1.19282007393486,4.58972005055539));
#50215=CARTESIAN_POINT('Ctrl Pts',(366.564007968047,-1.39133619134652,1.84732685824735));
#50216=CARTESIAN_POINT('Ctrl Pts',(366.967025111547,-1.58985230875817,-2.58700834044615));
#50217=CARTESIAN_POINT('Ctrl Pts',(370.911702134577,-1.78836842616983,-4.65211635088532));
#50218=CARTESIAN_POINT('Ctrl Pts',(374.785479907238,-1.98688454358148,-2.45695011867353));
#50219=CARTESIAN_POINT('Ctrl Pts',(375.0408741606,-2.18540066099314,1.9882662041693));
#50220=CARTESIAN_POINT('Ctrl Pts',(371.443976673514,-2.3839167784048,4.61265559054459));
#50221=CARTESIAN_POINT('Ctrl Pts',(367.288768849246,-2.58243289581645,3.01286782643016));
#50222=CARTESIAN_POINT('Ctrl Pts',(366.380505616332,-2.78094901322811,-1.34604944103277));
#50223=CARTESIAN_POINT('Ctrl Pts',(369.550959750218,-2.97946513063976,-4.4722790489893));
#50224=CARTESIAN_POINT('Ctrl Pts',(373.896688417238,-3.17798124805142,-3.50288114771708));
#50225=CARTESIAN_POINT('Ctrl Pts',(375.437956569813,-3.37649736546308,0.674388952710513));
#50226=CARTESIAN_POINT('Ctrl Pts',(372.763299861874,-3.57501348287473,4.23406634538199));
#50227=CARTESIAN_POINT('Ctrl Pts',(368.322118169056,-3.77352960028639,3.91626638363723));
#50228=CARTESIAN_POINT('Ctrl Pts',(366.181561137938,-3.97204571769804,0.0120241320746088));
#50229=CARTESIAN_POINT('Ctrl Pts',(368.301910212453,-4.1705618351097,-3.90322957598079));
#50230=CARTESIAN_POINT('Ctrl Pts',(372.741390027776,-4.36907795252135,-4.24397989285769));
#50231=CARTESIAN_POINT('Ctrl Pts',(375.434409424468,-4.56759406993301,-0.698174149437569));
#50232=CARTESIAN_POINT('Ctrl Pts',(373.914752462046,-4.76611018734466,3.48700619768048));
#50233=CARTESIAN_POINT('Ctrl Pts',(369.574092081518,-4.96462630475632,4.47885259966254));
#50234=CARTESIAN_POINT('Ctrl Pts',(366.387522490406,-5.16314242216798,1.36905098729384));
#50235=CARTESIAN_POINT('Ctrl Pts',(367.27324350568,-5.36165853957963,-2.99450147693928));
#50236=CARTESIAN_POINT('Ctrl Pts',(371.420128669554,-5.56017465699129,-4.61574645014013));
#50237=CARTESIAN_POINT('Ctrl Pts',(375.030539431168,-5.75869077440295,-2.00997862506626));
#50238=CARTESIAN_POINT('Ctrl Pts',(374.798130292284,-5.9572068918146,2.4364893909746));
#50239=CARTESIAN_POINT('Ctrl Pts',(370.935737121425,-6.15572300922625,4.65166676971372));
#50240=CARTESIAN_POINT('Ctrl Pts',(366.980466113943,-6.35423912663792,2.60693620482841));
#50241=CARTESIAN_POINT('Ctrl Pts',(366.554479221263,-6.55275524404956,-1.82517694725159));
#50242=CARTESIAN_POINT('Ctrl Pts',(370.04788713657,-6.75127136146123,-4.58582776958665));
#50243=CARTESIAN_POINT('Ctrl Pts',(374.261493342691,-6.94978747887288,-3.14686475222743));
#50244=CARTESIAN_POINT('Ctrl Pts',(375.336557427349,-7.14830359628454,1.17393714550662));
#50245=CARTESIAN_POINT('Ctrl Pts',(372.288556151701,-7.34681971369619,4.41966973603814));
#50246=CARTESIAN_POINT('Ctrl Pts',(367.908791104855,-7.54533583110785,3.61795285333871));
#50247=CARTESIAN_POINT('Ctrl Pts',(366.208167804746,-7.7438519485195,-0.497016431687658));
#50248=CARTESIAN_POINT('Ctrl Pts',(368.744084720329,-7.94236806593115,-4.15682752282947));
#50249=CARTESIAN_POINT('Ctrl Pts',(373.194197378567,-8.14088418334282,-4.00989503980782));
#50250=CARTESIAN_POINT('Ctrl Pts',(375.483177257165,-8.33940030075446,-0.19077695562173));
#50251=CARTESIAN_POINT('Ctrl Pts',(373.514820124317,-8.53791641816613,3.80305103556024));
#50252=CARTESIAN_POINT('Ctrl Pts',(369.091710000162,-8.73643253557777,4.31411723007756));
#50253=CARTESIAN_POINT('Ctrl Pts',(366.264446999925,-8.93494865298944,0.874396928501112));
#50254=CARTESIAN_POINT('Ctrl Pts',(367.622184798979,-9.13346477040109,-3.36607944740345));
#50255=CARTESIAN_POINT('Ctrl Pts',(371.921532947862,-9.33198088781275,-4.52396429499635));
#50256=CARTESIAN_POINT('Ctrl Pts',(375.225230194099,-9.5304970052244,-1.53888869615729));
#50257=CARTESIAN_POINT('Ctrl Pts',(374.507813442573,-9.72901312263606,2.85547189785572));
#50258=CARTESIAN_POINT('Ctrl Pts',(370.426279307617,-9.92752924004772,4.63484564464738));
#50259=CARTESIAN_POINT('Ctrl Pts',(366.718419111011,-10.1260453574593,2.1697159141836));
#50260=CARTESIAN_POINT('Ctrl Pts',(366.779820689829,-10.324561474871,-2.28239837811655));
#50261=CARTESIAN_POINT('Ctrl Pts',(370.55425364617,-10.5230775922827,-4.6443356515583));
#50262=CARTESIAN_POINT('Ctrl Pts',(374.585164075945,-10.7215937096943,-2.75307867993461));
#50263=CARTESIAN_POINT('Ctrl Pts',(375.181120883613,-10.920109827106,1.65939537766375));
#50264=CARTESIAN_POINT('Ctrl Pts',(371.796358161012,-11.1186259445176,4.55222671344473));
#50265=CARTESIAN_POINT('Ctrl Pts',(367.530577224486,-11.3171420619293,3.2762154175869));
#50266=CARTESIAN_POINT('Ctrl Pts',(366.290299111949,-11.5156581793409,-1.00009163747166));
#50267=CARTESIAN_POINT('Ctrl Pts',(369.211346926269,-11.7141742967526,-4.3605337946938));
#50268=CARTESIAN_POINT('Ctrl Pts',(373.618680643315,-11.9126904141642,-3.72768204888329));
#50269=CARTESIAN_POINT('Ctrl Pts',(375.476147881392,-12.1112065315759,0.31891000926328));
#50270=CARTESIAN_POINT('Ctrl Pts',(373.082715476643,-12.3097226489876,4.07345034723814));
#50271=CARTESIAN_POINT('Ctrl Pts',(368.630243297424,-12.5082387663992,4.09760234245405));
#50272=CARTESIAN_POINT('Ctrl Pts',(366.196220670465,-12.7067548838109,0.3692480571119));
#50273=CARTESIAN_POINT('Ctrl Pts',(368.009679217512,-12.9052710012225,-3.69725657509051));
#50274=CARTESIAN_POINT('Ctrl Pts',(372.409888096822,-13.1037871186342,-4.3778839651024));
#50275=CARTESIAN_POINT('Ctrl Pts',(375.367219717569,-13.3023032360458,-1.04932849605667));
#50276=CARTESIAN_POINT('Ctrl Pts',(374.173406035886,-13.5008193534575,3.24018204933326));
#50277=CARTESIAN_POINT('Ctrl Pts',(369.921718912714,-13.6993354708691,4.56239550874181));
#50278=CARTESIAN_POINT('Ctrl Pts',(366.505772539789,-13.8978515882808,1.70645394720947));
#50279=CARTESIAN_POINT('Ctrl Pts',(367.053825627246,-14.0963677056925,-2.71222567898131));
#50280=CARTESIAN_POINT('Ctrl Pts',(371.063981582666,-14.2948838231041,-4.64710062036397));
#50281=CARTESIAN_POINT('Ctrl Pts',(374.863815863332,-14.4933999405158,-2.32624921084424));
#50282=CARTESIAN_POINT('Ctrl Pts',(374.97351251552,-14.6919160579274,2.12493697601463));
#50283=CARTESIAN_POINT('Ctrl Pts',(371.29261343181,-14.8904321753391,4.63014630082654));
#50284=CARTESIAN_POINT('Ctrl Pts',(367.192015974937,-15.0889482927507,2.89515571806315));
#50285=CARTESIAN_POINT('Ctrl Pts',(366.426969294272,-15.2874644101624,-1.49116339960125));
#50286=CARTESIAN_POINT('Ctrl Pts',(369.698088587236,-15.485980527574,-4.51190344084632));
#50287=CARTESIAN_POINT('Ctrl Pts',(374.00974502862,-15.6844966449857,-3.40072813646827));
#50288=CARTESIAN_POINT('Ctrl Pts',(375.413405665806,-15.8830127623974,0.824769306579049));
#50289=CARTESIAN_POINT('Ctrl Pts',(372.623624787716,-16.081528879809,4.29495870743703));
#50290=CARTESIAN_POINT('Ctrl Pts',(368.195230655245,-16.2800449972207,3.83190662280167));
#50291=CARTESIAN_POINT('Ctrl Pts',(366.183662377922,-16.4785611146323,-0.140332656402569));
#50292=CARTESIAN_POINT('Ctrl Pts',(368.431075920034,-16.677077232044,-3.98405795828352));
#50293=CARTESIAN_POINT('Ctrl Pts',(372.879332710052,-16.8755933494556,-4.17925876678659));
#50294=CARTESIAN_POINT('Ctrl Pts',(375.454803794495,-17.0741094668673,-0.547173894597784));
#50295=CARTESIAN_POINT('Ctrl Pts',(373.798921744885,-17.272625584279,3.58600242191256));
#50296=CARTESIAN_POINT('Ctrl Pts',(369.428111844037,-17.4711417016906,4.43518593343438));
#50297=CARTESIAN_POINT('Ctrl Pts',(366.345078657529,-17.6696578191023,1.22271053329916));
#50298=CARTESIAN_POINT('Ctrl Pts',(367.373205332054,-17.8681739365139,-3.10949991481088));
#50299=CARTESIAN_POINT('Ctrl Pts',(371.570953016126,-18.0666900539256,-4.59408948989735));
#50300=CARTESIAN_POINT('Ctrl Pts',(375.094104230299,-18.2652061713372,-1.87149929898408));
#50301=CARTESIAN_POINT('Ctrl Pts',(374.716224110076,-18.4637222887489,2.56497435024718));
#50302=CARTESIAN_POINT('Ctrl Pts',(370.783368081515,-18.6622384061605,4.65249328050807));
#50303=CARTESIAN_POINT('Ctrl Pts',(366.897170884718,-18.8607545235722,2.47934736428527));
#50304=CARTESIAN_POINT('Ctrl Pts',(366.616537989202,-19.0592706409838,-1.96433770596103));
#50305=CARTESIAN_POINT('Ctrl Pts',(370.198467662479,-19.2577867583955,-4.60911967075604));
#50306=CARTESIAN_POINT('Ctrl Pts',(374.362696845284,-19.4563028758072,-3.03295751581995));
#50307=CARTESIAN_POINT('Ctrl Pts',(375.295703664052,-19.6548189932188,1.32072943912346));
#50308=CARTESIAN_POINT('Ctrl Pts',(372.143058221809,-19.8533351106305,4.46491749667864));
#50309=CARTESIAN_POINT('Ctrl Pts',(367.791893244921,-20.0518512280421,3.5202190424639));
#50310=CARTESIAN_POINT('Ctrl Pts',(366.226922851216,-20.2503673454538,-0.648229049073077));
#50311=CARTESIAN_POINT('Ctrl Pts',(368.881317158506,-20.4488834628655,-4.22304130829977));
#50312=CARTESIAN_POINT('Ctrl Pts',(373.324232351795,-20.6473995802771,-3.93047266772016));
#50313=CARTESIAN_POINT('Ctrl Pts',(375.486931210927,-20.8459156976888,-0.0384519244494463));
#50314=CARTESIAN_POINT('Ctrl Pts',(373.388855258257,-21.0444318151004,3.88878236164229));
#50315=CARTESIAN_POINT('Ctrl Pts',(368.951382544395,-21.2429479325121,4.25474372960455));
#50316=CARTESIAN_POINT('Ctrl Pts',(366.238266165228,-21.4414640499237,0.724291731725312));
#50317=CARTESIAN_POINT('Ctrl Pts',(367.734126503847,-21.6399801673354,-3.46945287300359));
#50318=CARTESIAN_POINT('Ctrl Pts',(372.069083091557,-21.838496284747,-4.48593849857525));
#50319=CARTESIAN_POINT('Ctrl Pts',(375.273265196508,-22.0370124021587,-1.39428704934514));
#50320=CARTESIAN_POINT('Ctrl Pts',(374.412343690105,-22.2355285195704,2.97422610387783));
#50321=CARTESIAN_POINT('Ctrl Pts',(370.274734333046,-22.434044636982,4.61899926353358));
#50322=CARTESIAN_POINT('Ctrl Pts',(366.649580609441,-22.6325607543937,2.0337813893544));
#50323=CARTESIAN_POINT('Ctrl Pts',(366.856730294058,-22.8310768718053,-2.41393609864016));
#50324=CARTESIAN_POINT('Ctrl Pts',(370.706477671604,-23.029592989217,-4.65101412189882));
#50325=CARTESIAN_POINT('Ctrl Pts',(374.673301417178,-23.2281091066286,-2.62878748883471));
#50326=CARTESIAN_POINT('Ctrl Pts',(375.124451315125,-23.4266252240403,1.80084434136301));
#50327=CARTESIAN_POINT('Ctrl Pts',(371.646790464395,-23.6251413414519,4.58127309001248));
#50328=CARTESIAN_POINT('Ctrl Pts',(367.425058045505,-23.8236574588636,3.1663090289536));
#50329=CARTESIAN_POINT('Ctrl Pts',(366.325511918996,-24.0221735762753,-1.14840414668247));
#50330=CARTESIAN_POINT('Ctrl Pts',(369.354938746353,-24.2206896936869,-4.41121600398739));
#50331=CARTESIAN_POINT('Ctrl Pts',(373.73937206963,-24.4192058110986,-3.63476513949107));
#50332=CARTESIAN_POINT('Ctrl Pts',(375.462957541574,-24.6177219285102,0.471257175707393));
#50333=CARTESIAN_POINT('Ctrl Pts',(372.948665973209,-24.8162380459219,4.14379956758217));
#50334=CARTESIAN_POINT('Ctrl Pts',(368.496152604384,-25.0147541633335,4.02552105304239));
#50335=CARTESIAN_POINT('Ctrl Pts',(366.188549771923,-25.2133147070871,0.211758288935219));
#50336=CARTESIAN_POINT('Ctrl Pts',(367.483611234327,-25.3457032117033,-2.44572697233012));
#50337=CARTESIAN_POINT('Ctrl Pts',(368.550672958437,-25.4119196771824,-3.20576715742043));
#50338=CARTESIAN_POINT('Ctrl Pts',(369.081337125798,-25.,3.52813093583777));
#50339=CARTESIAN_POINT('Ctrl Pts',(369.008004389183,-25.0000000000002,3.48377167173236));
#50340=CARTESIAN_POINT('Ctrl Pts',(368.936373634155,-25.0000000000002,3.43693146060399));
#50341=CARTESIAN_POINT('Ctrl Pts',(368.866583043242,-25.0000000000002,3.38761093025279));
#50342=CARTESIAN_POINT('Ctrl Pts',(368.768579307259,-25.0000000000002,3.31835236442314));
#50343=CARTESIAN_POINT('Ctrl Pts',(368.674202465802,-25.,3.24420420960068));
#50344=CARTESIAN_POINT('Ctrl Pts',(368.583606663623,-25.0000000000001,3.1655786709461));
#50345=CARTESIAN_POINT('Ctrl Pts',(368.490441324965,-25.0000000000001,3.08472310413516));
#50346=CARTESIAN_POINT('Ctrl Pts',(368.401273978833,-25.0000000000001,2.9991317898415));
#50347=CARTESIAN_POINT('Ctrl Pts',(368.316316523814,-25.,2.9092182158941));
#50348=CARTESIAN_POINT('Ctrl Pts',(368.231359068795,-25.,2.8193046419467));
#50349=CARTESIAN_POINT('Ctrl Pts',(368.150611123225,-24.9999999999999,2.72506785206802));
#50350=CARTESIAN_POINT('Ctrl Pts',(368.074335136508,-24.9999999999999,2.62690044695477));
#50351=CARTESIAN_POINT('Ctrl Pts',(368.051804137619,-24.9999999999999,2.59790298929197));
#50352=CARTESIAN_POINT('Ctrl Pts',(368.029663691347,-25.0000000000001,2.56856248344712));
#50353=CARTESIAN_POINT('Ctrl Pts',(368.007921481441,-25.0000000000001,2.5388888873865));
#50354=CARTESIAN_POINT('Ctrl Pts',(367.995462146392,-25.0000000000001,2.52188448548694));
#50355=CARTESIAN_POINT('Ctrl Pts',(367.983131721802,-25.0000000000001,2.50476791384));
#50356=CARTESIAN_POINT('Ctrl Pts',(367.970946292708,-25.0000000000001,2.48756205372084));
#50357=CARTESIAN_POINT('Ctrl Pts',(367.901749679588,-24.9999999999999,2.38985624156957));
#50358=CARTESIAN_POINT('Ctrl Pts',(367.837127619974,-25.0000000000001,2.28914348626008));
#50359=CARTESIAN_POINT('Ctrl Pts',(367.777242914735,-25.,2.18581597331342));
#50360=CARTESIAN_POINT('Ctrl Pts',(367.71761918203,-24.9999999999999,2.08293875302096));
#50361=CARTESIAN_POINT('Ctrl Pts',(367.66269132976,-25.,1.97746862871235));
#50362=CARTESIAN_POINT('Ctrl Pts',(367.612667283613,-25.,1.86977335561688));
#50363=CARTESIAN_POINT('Ctrl Pts',(367.563024060491,-25.,1.76289794502663));
#50364=CARTESIAN_POINT('Ctrl Pts',(367.518210030985,-25.,1.65383030873021));
#50365=CARTESIAN_POINT('Ctrl Pts',(367.478478768323,-24.9999999999999,1.54292354068813));
#50366=CARTESIAN_POINT('Ctrl Pts',(367.458684313889,-24.9999999999999,1.48766884150577));
#50367=CARTESIAN_POINT('Ctrl Pts',(367.440152269773,-25.,1.43195762663986));
#50368=CARTESIAN_POINT('Ctrl Pts',(367.42291898926,-25.0000000000001,1.3758339276038));
#50369=CARTESIAN_POINT('Ctrl Pts',(367.413229129654,-25.0000000000001,1.34427691999609));
#50370=CARTESIAN_POINT('Ctrl Pts',(367.403949941077,-25.0000000000001,1.31258951221787));
#50371=CARTESIAN_POINT('Ctrl Pts',(367.395088369449,-25.0000000000001,1.28077962509273));
#50372=CARTESIAN_POINT('Ctrl Pts',(367.389241343217,-25.0000000000001,1.25979088265963));
#50373=CARTESIAN_POINT('Ctrl Pts',(367.383576137904,-25.,1.23874881912547));
#50374=CARTESIAN_POINT('Ctrl Pts',(367.378094833834,-25.,1.2176557314011));
#50375=CARTESIAN_POINT('Ctrl Pts',(367.374400750062,-24.9999999999999,1.2034402031139));
#50376=CARTESIAN_POINT('Ctrl Pts',(367.37079089563,-24.9999999999998,1.18920406156008));
#50377=CARTESIAN_POINT('Ctrl Pts',(367.367267768483,-24.9999999999998,1.17495628199712));
#50378=CARTESIAN_POINT('Ctrl Pts',(367.339710086504,-24.9999999999998,1.06351103413865));
#50379=CARTESIAN_POINT('Ctrl Pts',(367.31741606077,-24.9999999999999,0.951207563746677));
#50380=CARTESIAN_POINT('Ctrl Pts',(367.300575616194,-24.9999999999999,0.838383113658457));
#50381=CARTESIAN_POINT('Ctrl Pts',(367.283952711426,-25.,0.727016095948555));
#50382=CARTESIAN_POINT('Ctrl Pts',(367.272643274885,-24.9999999999997,0.615140724577881));
#50383=CARTESIAN_POINT('Ctrl Pts',(367.26688064429,-24.9999999999999,0.503082333892389));
#50384=CARTESIAN_POINT('Ctrl Pts',(367.261118013696,-25.0000000000001,0.391023943206896));
#50385=CARTESIAN_POINT('Ctrl Pts',(367.260901956193,-25.,0.278781817875379));
#50386=CARTESIAN_POINT('Ctrl Pts',(367.266519668115,-24.9999999999999,0.16669318468162));
#50387=CARTESIAN_POINT('Ctrl Pts',(367.270046945812,-24.9999999999999,0.0963144003213416));
#50388=CARTESIAN_POINT('Ctrl Pts',(367.275875445267,-24.9999999999998,0.0259964001582221));
#50389=CARTESIAN_POINT('Ctrl Pts',(367.283964401729,-25.,-0.0441711994751926));
#50390=CARTESIAN_POINT('Ctrl Pts',(367.286810051659,-25.,-0.0688557710840931));
#50391=CARTESIAN_POINT('Ctrl Pts',(367.289935509814,-25.0000000000001,-0.0935216922831735));
#50392=CARTESIAN_POINT('Ctrl Pts',(367.293339176269,-25.0000000000001,-0.118164932406376));
#50393=CARTESIAN_POINT('Ctrl Pts',(367.295707273414,-25.0000000000002,-0.13531043927267));
#50394=CARTESIAN_POINT('Ctrl Pts',(367.298210043733,-24.9999999999999,-0.152444965532065));
#50395=CARTESIAN_POINT('Ctrl Pts',(367.300846972729,-24.9999999999998,-0.169567132184699));
#50396=CARTESIAN_POINT('Ctrl Pts',(367.303272993684,-24.9999999999998,-0.185319825996345));
#50397=CARTESIAN_POINT('Ctrl Pts',(367.305810982859,-24.9999999999999,-0.201051738242575));
#50398=CARTESIAN_POINT('Ctrl Pts',(367.308460062164,-25.,-0.216761568244168));
#50399=CARTESIAN_POINT('Ctrl Pts',(367.326841341943,-25.0000000000001,-0.325768037013256));
#50400=CARTESIAN_POINT('Ctrl Pts',(367.350567912994,-24.9999999999998,-0.433718326729101));
#50401=CARTESIAN_POINT('Ctrl Pts',(367.379395445099,-24.9999999999998,-0.54029437093727));
#50402=CARTESIAN_POINT('Ctrl Pts',(367.408704572919,-24.9999999999999,-0.648650885498511));
#50403=CARTESIAN_POINT('Ctrl Pts',(367.443286972773,-25.0000000000001,-0.755587671881746));
#50404=CARTESIAN_POINT('Ctrl Pts',(367.482934839879,-25.0000000000001,-0.86074938973287));
#50405=CARTESIAN_POINT('Ctrl Pts',(367.52224800911,-25.,-0.965023357345557));
#50406=CARTESIAN_POINT('Ctrl Pts',(367.566542101419,-25.0000000000002,-1.06755279241357));
#50407=CARTESIAN_POINT('Ctrl Pts',(367.615653947938,-25.0000000000001,-1.16795954601739));
#50408=CARTESIAN_POINT('Ctrl Pts',(367.652491193367,-25.,-1.24327148167718));
#50409=CARTESIAN_POINT('Ctrl Pts',(367.692039773092,-25.,-1.31738860793362));
#50410=CARTESIAN_POINT('Ctrl Pts',(367.734242507007,-25.,-1.39013596224847));
#50411=CARTESIAN_POINT('Ctrl Pts',(367.747211950558,-25.,-1.41249216095307));
#50412=CARTESIAN_POINT('Ctrl Pts',(367.760435499407,-25.0000000000001,-1.4347242132668));
#50413=CARTESIAN_POINT('Ctrl Pts',(367.773893192447,-25.0000000000001,-1.45679714311184));
#50414=CARTESIAN_POINT('Ctrl Pts',(367.831176407707,-25.0000000000002,-1.55075146261937));
#50415=CARTESIAN_POINT('Ctrl Pts',(367.892745302596,-25.,-1.64191051491612));
#50416=CARTESIAN_POINT('Ctrl Pts',(367.95841903902,-25.,-1.72992127878184));
#50417=CARTESIAN_POINT('Ctrl Pts',(368.026003592275,-25.0000000000001,-1.82049276871758));
#50418=CARTESIAN_POINT('Ctrl Pts',(368.097935785625,-25.0000000000002,-1.90773109063843));
#50419=CARTESIAN_POINT('Ctrl Pts',(368.174053320765,-25.0000000000001,-1.99120413362777));
#50420=CARTESIAN_POINT('Ctrl Pts',(368.208432762019,-25.0000000000001,-2.02890578243333));
#50421=CARTESIAN_POINT('Ctrl Pts',(368.243666428395,-25.,-2.06583859593258));
#50422=CARTESIAN_POINT('Ctrl Pts',(368.279741192986,-25.0000000000001,-2.10195888917106));
#50423=CARTESIAN_POINT('Ctrl Pts',(368.291644378927,-25.0000000000002,-2.1138770976905));
#50424=CARTESIAN_POINT('Ctrl Pts',(368.303638458318,-25.,-2.12570606365943));
#50425=CARTESIAN_POINT('Ctrl Pts',(368.315715640136,-25.,-2.13743730062655));
#50426=CARTESIAN_POINT('Ctrl Pts',(368.391540722707,-25.0000000000001,-2.21109041151526));
#50427=CARTESIAN_POINT('Ctrl Pts',(368.470715155507,-25.0000000000001,-2.28097119290546));
#50428=CARTESIAN_POINT('Ctrl Pts',(368.553093431011,-25.0000000000001,-2.34673408051994));
#50429=CARTESIAN_POINT('Ctrl Pts',(368.633211360681,-25.0000000000001,-2.41069252554136));
#50430=CARTESIAN_POINT('Ctrl Pts',(368.716360276367,-25.0000000000001,-2.47075627465853));
#50431=CARTESIAN_POINT('Ctrl Pts',(368.802425787939,-25.0000000000002,-2.52656271084893));
#50432=CARTESIAN_POINT('Ctrl Pts',(368.854788791589,-25.0000000000002,-2.56051583061294));
#50433=CARTESIAN_POINT('Ctrl Pts',(368.908231748608,-25.0000000000002,-2.59289216715227));
#50434=CARTESIAN_POINT('Ctrl Pts',(368.962731321485,-25.,-2.62360084935009));
#50435=CARTESIAN_POINT('Ctrl Pts',(368.958580243284,-1.20159524691354E-13,
-2.62730819722368));
#50436=CARTESIAN_POINT('Ctrl Pts',(368.896667223351,-3.12253651536795E-14,
-2.59284588111042));
#50437=CARTESIAN_POINT('Ctrl Pts',(368.836104112209,-1.8704388297858E-13,
-2.55627615699171));
#50438=CARTESIAN_POINT('Ctrl Pts',(368.777011016265,-1.30943866860633E-13,
-2.51762860130017));
#50439=CARTESIAN_POINT('Ctrl Pts',(368.691754001996,-4.95917179562384E-14,
-2.4618695459587));
#50440=CARTESIAN_POINT('Ctrl Pts',(368.609555629646,-1.32137019917602E-13,
-2.4017880170848));
#50441=CARTESIAN_POINT('Ctrl Pts',(368.530495563443,-1.30916111285018E-13,
-2.33778526550872));
#50442=CARTESIAN_POINT('Ctrl Pts',(368.449492513799,-1.29393310518178E-13,
-2.27220957967648));
#50443=CARTESIAN_POINT('Ctrl Pts',(368.371783421322,4.86435335969926E-14,
-2.2025171945328));
#50444=CARTESIAN_POINT('Ctrl Pts',(368.297473473753,3.3660574327854E-14,
-2.12908838121556));
#50445=CARTESIAN_POINT('Ctrl Pts',(368.221729114233,1.83158428439202E-14,
-2.05424216456431));
#50446=CARTESIAN_POINT('Ctrl Pts',(368.149515825788,-8.1812323111681E-14,
-1.97551336828871));
#50447=CARTESIAN_POINT('Ctrl Pts',(368.080973191528,-1.82603931975223E-13,
-1.89325888662171));
#50448=CARTESIAN_POINT('Ctrl Pts',(368.059248050056,-2.14700691140463E-13,
-1.86718766437808));
#50449=CARTESIAN_POINT('Ctrl Pts',(368.03789191569,-1.53909802920789E-13,
-1.84076193575357));
#50450=CARTESIAN_POINT('Ctrl Pts',(368.016909953942,-4.20774526332934E-14,
-1.81399226410803));
#50451=CARTESIAN_POINT('Ctrl Pts',(368.00698466764,1.09792968138055E-14,
-1.80132916527718));
#50452=CARTESIAN_POINT('Ctrl Pts',(367.99714281104,-1.84639436501056E-13,
-1.78858859232451));
#50453=CARTESIAN_POINT('Ctrl Pts',(367.987394394324,-1.58761892521397E-13,
-1.77578435380463));
#50454=CARTESIAN_POINT('Ctrl Pts',(367.92073258765,1.96712162946812E-14,
-1.68822616895041));
#50455=CARTESIAN_POINT('Ctrl Pts',(367.858328742098,-7.66173391862864E-14,
-1.59755706304694));
#50456=CARTESIAN_POINT('Ctrl Pts',(367.800281843188,-3.99680288865056E-15,
-1.50421981105859));
#50457=CARTESIAN_POINT('Ctrl Pts',(367.742234944279,6.86237334089853E-14,
-1.41088255907024));
#50458=CARTESIAN_POINT('Ctrl Pts',(367.688544517787,-2.3646706107268E-13,
-1.31487644576671));
#50459=CARTESIAN_POINT('Ctrl Pts',(367.639337755227,-2.30065966277948E-13,
-1.21659878608418));
#50460=CARTESIAN_POINT('Ctrl Pts',(367.589288906219,-2.24035458786638E-13,
-1.11663927860252));
#50461=CARTESIAN_POINT('Ctrl Pts',(367.543877872957,2.29330542649884E-14,
-1.01432914427311));
#50462=CARTESIAN_POINT('Ctrl Pts',(367.503276095346,1.75970349403087E-14,
-0.910049731540007));
#50463=CARTESIAN_POINT('Ctrl Pts',(367.48289670826,1.4660611493931E-14,
-0.857708414427849));
#50464=CARTESIAN_POINT('Ctrl Pts',(367.463729595381,-1.75345152813706E-13,
-0.804870454339346));
#50465=CARTESIAN_POINT('Ctrl Pts',(367.445800684405,-2.20712337295481E-13,
-0.751581520596565));
#50466=CARTESIAN_POINT('Ctrl Pts',(367.432652660306,-2.54138506807475E-13,
-0.712502505366526));
#50467=CARTESIAN_POINT('Ctrl Pts',(367.420170588684,-1.50535198818543E-13,
-0.673180926026252));
#50468=CARTESIAN_POINT('Ctrl Pts',(367.408365775792,-2.26846319506535E-13,
-0.633634372562032));
#50469=CARTESIAN_POINT('Ctrl Pts',(367.403898301248,-2.55619978963674E-13,
-0.61866817000582));
#50470=CARTESIAN_POINT('Ctrl Pts',(367.399528497761,-1.58501758860923E-13,
-0.603671792966296));
#50471=CARTESIAN_POINT('Ctrl Pts',(367.395259906534,-1.5512591211575E-13,
-0.588657214169824));
#50472=CARTESIAN_POINT('Ctrl Pts',(367.363762596442,-1.31200303611061E-13,
-0.477866834126048));
#50473=CARTESIAN_POINT('Ctrl Pts',(367.337723096572,8.68805780094438E-14,
-0.365923016810904));
#50474=CARTESIAN_POINT('Ctrl Pts',(367.317274728141,1.70696790036118E-14,
-0.253257167461436));
#50475=CARTESIAN_POINT('Ctrl Pts',(367.296972417425,-5.22425777530995E-14,
-0.14139606283405));
#50476=CARTESIAN_POINT('Ctrl Pts',(367.282181192585,1.1519324841062E-13,
-0.0288223438826056));
#50477=CARTESIAN_POINT('Ctrl Pts',(367.273072973574,4.86000129029662E-14,
0.084071210533729));
#50478=CARTESIAN_POINT('Ctrl Pts',(367.264525485063,-1.45421330099294E-14,
0.190014684024364));
#50479=CARTESIAN_POINT('Ctrl Pts',(367.260982825867,-1.85488797503548E-13,
0.296240640277909));
#50480=CARTESIAN_POINT('Ctrl Pts',(367.262626175817,-1.2356782264078E-13,
0.402438260595486));
#50481=CARTESIAN_POINT('Ctrl Pts',(367.263830822359,-7.84670444554026E-14,
0.480285706399798));
#50482=CARTESIAN_POINT('Ctrl Pts',(367.267822987318,4.24060545398861E-14,
0.558118233893516));
#50483=CARTESIAN_POINT('Ctrl Pts',(367.2745278326,7.17481629664007E-14,
0.635838377479383));
#50484=CARTESIAN_POINT('Ctrl Pts',(367.276457612589,8.02928709341649E-14,
0.65820768974695));
#50485=CARTESIAN_POINT('Ctrl Pts',(367.278612189094,7.0348597872745E-14,
0.680567693369209));
#50486=CARTESIAN_POINT('Ctrl Pts',(367.280989967383,1.7125190154843E-14,
0.702916061212433));
#50487=CARTESIAN_POINT('Ctrl Pts',(367.283332529267,-3.46588239178081E-14,
0.724933435554674));
#50488=CARTESIAN_POINT('Ctrl Pts',(367.285892448296,1.2455954399965E-13,
0.746944401464202));
#50489=CARTESIAN_POINT('Ctrl Pts',(367.288664178637,1.33587585438022E-13,
0.768916642339298));
#50490=CARTESIAN_POINT('Ctrl Pts',(367.302614038008,1.78981378037621E-13,
0.879500874045485));
#50491=CARTESIAN_POINT('Ctrl Pts',(367.321936335458,-1.24773023519911E-13,
0.989232886547642));
#50492=CARTESIAN_POINT('Ctrl Pts',(367.346325288731,-1.12854170453147E-13,
1.09782477106727));
#50493=CARTESIAN_POINT('Ctrl Pts',(367.371307395697,-1.0074091404704E-13,
1.20905767410888));
#50494=CARTESIAN_POINT('Ctrl Pts',(367.401605669227,-4.08269138960946E-14,
1.319094933492));
#50495=CARTESIAN_POINT('Ctrl Pts',(367.436945218641,-1.39610545346613E-13,
1.42763593264953));
#50496=CARTESIAN_POINT('Ctrl Pts',(367.473165204033,-2.40870682695136E-13,
1.53888108062296));
#50497=CARTESIAN_POINT('Ctrl Pts',(367.514680880354,1.44458975729594E-13,
1.64855523782715));
#50498=CARTESIAN_POINT('Ctrl Pts',(367.561250870734,1.25677246387568E-13,
1.75633336602783));
#50499=CARTESIAN_POINT('Ctrl Pts',(367.600265921544,1.10273611345618E-13,
1.84662690299669));
#50500=CARTESIAN_POINT('Ctrl Pts',(367.642829467058,-3.26636295549089E-14,
1.9355899035714));
#50501=CARTESIAN_POINT('Ctrl Pts',(367.688826929101,-1.28674848554056E-13,
2.02302448049586));
#50502=CARTESIAN_POINT('Ctrl Pts',(367.69883194909,-1.49484545206251E-13,
2.04204258825589));
#50503=CARTESIAN_POINT('Ctrl Pts',(367.7089995222,-1.28827627965532E-13,
2.06098834877383));
#50504=CARTESIAN_POINT('Ctrl Pts',(367.719328615054,-1.27398092075737E-13,
2.07985966126142));
#50505=CARTESIAN_POINT('Ctrl Pts',(367.728509214281,-1.26400725739923E-13,
2.09663266923727));
#50506=CARTESIAN_POINT('Ctrl Pts',(367.737813168611,-1.28517961198261E-14,
2.11333905951663));
#50507=CARTESIAN_POINT('Ctrl Pts',(367.747236849987,-3.51940698806175E-14,
2.12997310026321));
#50508=CARTESIAN_POINT('Ctrl Pts',(367.806624057047,-1.74409790917852E-13,
2.23479935473743));
#50509=CARTESIAN_POINT('Ctrl Pts',(367.870792434446,-7.64407390032732E-14,
2.33680885037705));
#50510=CARTESIAN_POINT('Ctrl Pts',(367.939467138126,-2.88657986402541E-15,
2.43566584941741));
#50511=CARTESIAN_POINT('Ctrl Pts',(368.008598405184,7.14984065523101E-14,
2.53518006986634));
#50512=CARTESIAN_POINT('Ctrl Pts',(368.082296431862,-3.67899973920985E-14,
2.63150057287638));
#50513=CARTESIAN_POINT('Ctrl Pts',(368.16033137017,-1.60982338570648E-14,
2.72427050132567));
#50514=CARTESIAN_POINT('Ctrl Pts',(368.195472296089,-6.73981254935445E-15,
2.76604693190711));
#50515=CARTESIAN_POINT('Ctrl Pts',(368.231493356358,9.84733976286278E-14,
2.80710306904633));
#50516=CARTESIAN_POINT('Ctrl Pts',(368.268376606191,2.91988655476416E-14,
2.8474046769452));
#50517=CARTESIAN_POINT('Ctrl Pts',(368.289617840286,-1.05235299652341E-14,
2.87061455925349));
#50518=CARTESIAN_POINT('Ctrl Pts',(368.311150090951,-4.03533354721523E-15,
2.89357920292765));
#50519=CARTESIAN_POINT('Ctrl Pts',(368.332943578336,2.33146835171283E-14,
2.91626474739458));
#50520=CARTESIAN_POINT('Ctrl Pts',(368.418412002948,1.30553930674682E-13,
3.00523158931483));
#50521=CARTESIAN_POINT('Ctrl Pts',(368.507948563201,8.15823027870669E-15,
3.08997044913753));
#50522=CARTESIAN_POINT('Ctrl Pts',(368.601298624144,-1.07136521876328E-14,
3.17012489733602));
#50523=CARTESIAN_POINT('Ctrl Pts',(368.693422616792,-2.88627181492191E-14,
3.24922658963247));
#50524=CARTESIAN_POINT('Ctrl Pts',(368.789261074837,1.23156603782099E-13,
3.32386425813697));
#50525=CARTESIAN_POINT('Ctrl Pts',(368.888611897156,1.69086966650411E-13,
3.3936691068897));
#50526=CARTESIAN_POINT('Ctrl Pts',(368.95282952375,1.98583755561227E-13,
3.43878903249292));
#50527=CARTESIAN_POINT('Ctrl Pts',(369.018515449972,6.92162971711572E-14,
3.4818892617252));
#50528=CARTESIAN_POINT('Ctrl Pts',(369.085623377893,3.05311331771918E-15,
3.52286199445089));
#50529=CARTESIAN_POINT('Ctrl Pts',(373.11810396585,0.412130952468996,-3.20610701674044));
#50530=CARTESIAN_POINT('Ctrl Pts',(374.185302789364,0.34591310276681,-2.44600546672676));
#50531=CARTESIAN_POINT('Ctrl Pts',(375.480525080075,0.213523213927405,0.211751707408718));
#50532=CARTESIAN_POINT('Ctrl Pts',(373.172696361849,0.0149612859507822,
4.02588784127813));
#50533=CARTESIAN_POINT('Ctrl Pts',(368.719776930065,-0.183554831460874,
4.14417747187957));
#50534=CARTESIAN_POINT('Ctrl Pts',(366.205256212803,-0.382070948872529,
0.471300063467854));
#50535=CARTESIAN_POINT('Ctrl Pts',(367.928998792514,-0.580587066284185,
-3.63509646070476));
#50536=CARTESIAN_POINT('Ctrl Pts',(372.313831828821,-0.779103183695841,
-4.4116181741134));
#50537=CARTESIAN_POINT('Ctrl Pts',(375.343534831733,-0.977619301107497,
-1.14850882859149));
#50538=CARTESIAN_POINT('Ctrl Pts',(374.24388846515,-1.17613541851915,3.16659767841453));
#50539=CARTESIAN_POINT('Ctrl Pts',(370.021771173424,-1.37465153593081,4.58169074422432));
#50540=CARTESIAN_POINT('Ctrl Pts',(366.543793281998,-1.57316765334246,1.80100851318485));
#50541=CARTESIAN_POINT('Ctrl Pts',(366.994984309258,-1.77168377075412,-2.62902714077588));
#50542=CARTESIAN_POINT('Ctrl Pts',(370.96216968929,-1.97019988816577,-4.65143813111721));
#50543=CARTESIAN_POINT('Ctrl Pts',(374.812268028382,-2.16871600557743,-2.41415616437785));
#50544=CARTESIAN_POINT('Ctrl Pts',(375.019436597687,-2.36723212298908,2.03396679848696));
#50545=CARTESIAN_POINT('Ctrl Pts',(371.393952387734,-2.56574824040074,4.61942035370964));
#50546=CARTESIAN_POINT('Ctrl Pts',(367.255965826352,-2.7642643578124,2.97449724855164));
#50547=CARTESIAN_POINT('Ctrl Pts',(366.39496583423,-2.96278047522405,-1.39441415921852));
#50548=CARTESIAN_POINT('Ctrl Pts',(369.599440047773,-3.16129659263571,-4.48634745823798));
#50549=CARTESIAN_POINT('Ctrl Pts',(373.934791830905,-3.35981271004736,-3.46976916495197));
#50550=CARTESIAN_POINT('Ctrl Pts',(375.430788539321,-3.55832882745902,0.724357761628879));
#50551=CARTESIAN_POINT('Ctrl Pts',(372.717424819462,-3.75684494487067,4.25513161243665));
#50552=CARTESIAN_POINT('Ctrl Pts',(368.279547564317,-3.95536106228233,3.88913688168041));
#50553=CARTESIAN_POINT('Ctrl Pts',(366.181280340988,-4.15387717969399,-0.0384554299109293));
#50554=CARTESIAN_POINT('Ctrl Pts',(368.344176362114,-4.35239329710564,-3.93083098844711));
#50555=CARTESIAN_POINT('Ctrl Pts',(372.787496592847,-4.5509094145173,-4.22342630098604));
#50556=CARTESIAN_POINT('Ctrl Pts',(375.442132887444,-4.74942553192896,-0.6482881447401));
#50557=CARTESIAN_POINT('Ctrl Pts',(373.877019823537,-4.94794164934061,3.52053996250392));
#50558=CARTESIAN_POINT('Ctrl Pts',(369.525458173596,-5.14645776675227,4.46532453995758));
#50559=CARTESIAN_POINT('Ctrl Pts',(366.372525321083,-5.34497388416392,1.32084984314923));
#50560=CARTESIAN_POINT('Ctrl Pts',(367.305617197225,-5.54349000157558,-3.03323401476381));
#50561=CARTESIAN_POINT('Ctrl Pts',(371.470226011121,-5.74200611898723,-4.60953986019632));
#50562=CARTESIAN_POINT('Ctrl Pts',(375.052482230274,-5.94052223639889,-1.96451678440118));
#50563=CARTESIAN_POINT('Ctrl Pts',(374.771823750919,-6.13903835381055,2.47957339347431));
#50564=CARTESIAN_POINT('Ctrl Pts',(370.885272269759,-6.3375544712222,4.65291742409449));
#50565=CARTESIAN_POINT('Ctrl Pts',(366.952057703193,-6.53607058863387,2.56520818560264));
#50566=CARTESIAN_POINT('Ctrl Pts',(366.574143133607,-6.73458670604551,-1.87166991383015));
#50567=CARTESIAN_POINT('Ctrl Pts',(370.09761553513,-6.93310282345717,-4.59450830911431));
#50568=CARTESIAN_POINT('Ctrl Pts',(374.295745906001,-7.13161894086883,-3.10978339172664));
#50569=CARTESIAN_POINT('Ctrl Pts',(375.323966309482,-7.33013505828048,1.22282200145175));
#50570=CARTESIAN_POINT('Ctrl Pts',(372.240652058892,-7.52865117569214,4.43559026624153));
#50571=CARTESIAN_POINT('Ctrl Pts',(367.869443694065,-7.7271672931038,3.58632933908072));
#50572=CARTESIAN_POINT('Ctrl Pts',(366.21341068631,-7.92568341051545,-0.547223777592583));
#50573=CARTESIAN_POINT('Ctrl Pts',(368.789116563041,-8.1241995279271,-4.1796397680466));
#50574=CARTESIAN_POINT('Ctrl Pts',(373.237778877468,-8.32271564533876,-3.9844211641022));
#50575=CARTESIAN_POINT('Ctrl Pts',(375.48539730457,-8.52123176275041,-0.140345449800097));
#50576=CARTESIAN_POINT('Ctrl Pts',(373.473645643041,-8.71974788016207,3.83225595777542));
#50577=CARTESIAN_POINT('Ctrl Pts',(369.044847796937,-8.91826399757373,4.29535025645813));
#50578=CARTESIAN_POINT('Ctrl Pts',(366.25481258905,-9.11678011498538,0.824844496502067));
#50579=CARTESIAN_POINT('Ctrl Pts',(367.658601190669,-9.31529623239705,-3.40103816314458));
#50580=CARTESIAN_POINT('Ctrl Pts',(371.970650703318,-9.5138123498087,-4.51231476758915));
#50581=CARTESIAN_POINT('Ctrl Pts',(375.242068207196,-9.71232846722035,-1.49129934120374));
#50582=CARTESIAN_POINT('Ctrl Pts',(374.476951781207,-9.91084458463201,2.89541965433465));
#50583=CARTESIAN_POINT('Ctrl Pts',(370.375980494218,-10.1093607020436,4.63056840715521));
#50584=CARTESIAN_POINT('Ctrl Pts',(366.694745842105,-10.3078768194553,2.12513069545394));
#50585=CARTESIAN_POINT('Ctrl Pts',(366.804452494766,-10.5063929368669,-2.32646128287183));
#50586=CARTESIAN_POINT('Ctrl Pts',(370.604633186536,-10.7049090542786,-4.64752427232966));
#50587=CARTESIAN_POINT('Ctrl Pts',(374.615154726994,-10.9034251716902,-2.71247293847364));
#50588=CARTESIAN_POINT('Ctrl Pts',(375.163257777597,-11.1019412891019,1.70660951573022));
#50589=CARTESIAN_POINT('Ctrl Pts',(371.746999990629,-11.3004574065136,4.56281143858355));
#50590=CARTESIAN_POINT('Ctrl Pts',(367.49492526328,-11.4989735239252,3.24047743985877));
#50591=CARTESIAN_POINT('Ctrl Pts',(366.301002747821,-11.6974896413369,-1.04942415787176));
#50592=CARTESIAN_POINT('Ctrl Pts',(369.258603973092,-11.8960057587485,-4.37828307398747));
#50593=CARTESIAN_POINT('Ctrl Pts',(373.659213996533,-12.0945218761602,-3.6975936347205));
#50594=CARTESIAN_POINT('Ctrl Pts',(375.472837867153,-12.2930379935718,0.369281719534577));
#50595=CARTESIAN_POINT('Ctrl Pts',(373.038593343025,-12.4915541109835,4.09797589952302));
#50596=CARTESIAN_POINT('Ctrl Pts',(368.585715255102,-12.6900702283951,4.07382170249547));
#50597=CARTESIAN_POINT('Ctrl Pts',(366.192064653583,-12.8885863458068,0.318939082628224));
#50598=CARTESIAN_POINT('Ctrl Pts',(368.049701227277,-13.0871024632185,-3.72802188224533));
#50599=CARTESIAN_POINT('Ctrl Pts',(372.457436737988,-13.2856185806301,-4.36093132185416));
#50600=CARTESIAN_POINT('Ctrl Pts',(375.378750849028,-13.4841346980418,-1.00018281061867));
#50601=CARTESIAN_POINT('Ctrl Pts',(374.138359666792,-13.6826508154534,3.27651409308701));
#50602=CARTESIAN_POINT('Ctrl Pts',(369.872189841231,-13.8811669328651,4.55264171625033));
#50603=CARTESIAN_POINT('Ctrl Pts',(366.487118547438,-14.0796830502768,1.65954665609971));
#50604=CARTESIAN_POINT('Ctrl Pts',(367.083129685385,-14.2781991676884,-2.75332966378236));
#50605=CARTESIAN_POINT('Ctrl Pts',(371.114407592274,-14.4767152851001,-4.64475905145618));
#50606=CARTESIAN_POINT('Ctrl Pts',(374.889184644014,-14.6752314025117,-2.28260645249201));
#50607=CARTESIAN_POINT('Ctrl Pts',(374.950591820493,-14.8737475199233,2.16991371588561));
#50608=CARTESIAN_POINT('Ctrl Pts',(371.242393597581,-15.072263637335,4.63526817939077));
#50609=CARTESIAN_POINT('Ctrl Pts',(367.160487370411,-15.2707797547467,2.85573221635991));
#50610=CARTESIAN_POINT('Ctrl Pts',(366.443005215735,-15.4692958721583,-1.53902898862659));
#50611=CARTESIAN_POINT('Ctrl Pts',(369.747003642848,-15.66781198957,-4.52437672126445));
#50612=CARTESIAN_POINT('Ctrl Pts',(374.046743740915,-15.8663281069816,-3.36638631533918));
#50613=CARTESIAN_POINT('Ctrl Pts',(375.404605317853,-16.0648442243933,0.874476642716028));
#50614=CARTESIAN_POINT('Ctrl Pts',(372.577084570772,-16.2633603418049,4.31451052568145));
#50615=CARTESIAN_POINT('Ctrl Pts',(368.153571214698,-16.4618764592166,3.80339773992032));
#50616=CARTESIAN_POINT('Ctrl Pts',(366.185034636979,-16.6603925766283,-0.190794347763422));
#50617=CARTESIAN_POINT('Ctrl Pts',(368.474223189953,-16.8589086940399,-4.01026060105872));
#50618=CARTESIAN_POINT('Ctrl Pts',(372.924741541791,-17.0574248114516,-4.15720647914977));
#50619=CARTESIAN_POINT('Ctrl Pts',(375.460889643715,-17.2559409288632,-0.497061742087704));
#50620=CARTESIAN_POINT('Ctrl Pts',(373.760111306634,-17.4544570462749,3.61828268326134));
#50621=CARTESIAN_POINT('Ctrl Pts',(369.379946979415,-17.6529731636865,4.42007265431438));
#50622=CARTESIAN_POINT('Ctrl Pts',(366.331667833362,-17.8514892810982,1.17404416724334));
#50623=CARTESIAN_POINT('Ctrl Pts',(367.406829926015,-18.0500053985099,-3.1471516355009));
#50624=CARTESIAN_POINT('Ctrl Pts',(371.620820264673,-18.2485215159215,-4.58624583562557));
#50625=CARTESIAN_POINT('Ctrl Pts',(375.114546655788,-18.4470376333332,-1.82534333913001));
#50626=CARTESIAN_POINT('Ctrl Pts',(374.688520928102,-18.6455537507448,2.60717386562768));
#50627=CARTESIAN_POINT('Ctrl Pts',(370.732889339158,-18.8440698681565,4.65209083795145));
#50628=CARTESIAN_POINT('Ctrl Pts',(366.870144054024,-19.0425859855681,2.43671151302536));
#50629=CARTESIAN_POINT('Ctrl Pts',(366.63771372761,-19.2411021029798,-2.01016186435141));
#50630=CARTESIAN_POINT('Ctrl Pts',(370.248453631574,-19.4396182203914,-4.61616724370937));
#50631=CARTESIAN_POINT('Ctrl Pts',(374.395716845375,-19.6381343378031,-2.9947744700463));
#50632=CARTESIAN_POINT('Ctrl Pts',(375.281518607221,-19.8366504552148,1.36917579654363));
#50633=CARTESIAN_POINT('Ctrl Pts',(372.094658513152,-20.0351665726264,4.47926091333222));
#50634=CARTESIAN_POINT('Ctrl Pts',(367.753602417219,-20.2336826900381,3.48732408987848));
#50635=CARTESIAN_POINT('Ctrl Pts',(366.233806915586,-20.4321988074497,-0.698237798339605));
#50636=CARTESIAN_POINT('Ctrl Pts',(368.927071820833,-20.6307149248614,-4.24436679440525));
#50637=CARTESIAN_POINT('Ctrl Pts',(373.366956360414,-20.8292310422731,-3.90358541309778));
#50638=CARTESIAN_POINT('Ctrl Pts',(375.487498736112,-21.0277471596847,0.0120252282541951));
#50639=CARTESIAN_POINT('Ctrl Pts',(373.346746561559,-21.2262632770964,3.91662340924706));
#50640=CARTESIAN_POINT('Ctrl Pts',(368.905159989326,-21.424779394508,4.23445234317155));
#50641=CARTESIAN_POINT('Ctrl Pts',(366.230259446871,-21.6232955119197,0.674450433223809));
#50642=CARTESIAN_POINT('Ctrl Pts',(367.77166810882,-21.8218116293313,-3.50320048712016));
#50643=CARTESIAN_POINT('Ctrl Pts',(372.117792953331,-22.020327746743,-4.47268676344431));
#50644=CARTESIAN_POINT('Ctrl Pts',(375.288536120941,-22.2188438641546,-1.34617215323029));
#50645=CARTESIAN_POINT('Ctrl Pts',(374.380190086528,-22.4173599815663,3.01314249366513));
#50646=CARTESIAN_POINT('Ctrl Pts',(370.224603453362,-22.6158760989779,4.61307610279703));
#50647=CARTESIAN_POINT('Ctrl Pts',(366.627378056288,-22.8143922163896,1.98844746315212));
#50648=CARTESIAN_POINT('Ctrl Pts',(366.882795591862,-23.0129083338012,-2.45717410429654));
#50649=CARTESIAN_POINT('Ctrl Pts',(370.756926517952,-23.2114244512129,-4.65254046342319));
#50650=CARTESIAN_POINT('Ctrl Pts',(374.701963154568,-23.4099405686247,-2.58724417820185));
#50651=CARTESIAN_POINT('Ctrl Pts',(375.105017042159,-23.6084566860362,1.84749525744088));
#50652=CARTESIAN_POINT('Ctrl Pts',(371.597184240534,-23.8069728034479,4.59013849390895));
#50653=CARTESIAN_POINT('Ctrl Pts',(367.390445996853,-24.0054889208595,3.12962485931625));
#50654=CARTESIAN_POINT('Ctrl Pts',(366.338134868135,-24.2040050382713,-1.19777877140987));
#50655=CARTESIAN_POINT('Ctrl Pts',(369.402108736586,-24.4025211556828,-4.42654123220031));
#50656=CARTESIAN_POINT('Ctrl Pts',(373.780221960378,-24.6010372730946,-3.60519568839286));
#50657=CARTESIAN_POINT('Ctrl Pts',(375.455117166712,-24.7995533905062,0.525090591169996));
#50658=CARTESIAN_POINT('Ctrl Pts',(373.757258810431,-24.9318974687806,2.94371710434112));
#50659=CARTESIAN_POINT('Ctrl Pts',(372.584499012473,-24.9980695079178,3.52585701865193));
#50660=CARTESIAN_POINT('Ctrl Pts',(372.978942820004,0.273648433802759,-3.01074479622233));
#50661=CARTESIAN_POINT('Ctrl Pts',(373.981112519162,0.207430584100572,-2.29695958120762));
#50662=CARTESIAN_POINT('Ctrl Pts',(375.197411211422,0.0750406952611682,
0.198848743302471));
#50663=CARTESIAN_POINT('Ctrl Pts',(373.030208660887,-0.123521232715456,
3.78057276473135));
#50664=CARTESIAN_POINT('Ctrl Pts',(368.848625221144,-0.322037350127111,
3.89165448718187));
#50665=CARTESIAN_POINT('Ctrl Pts',(366.487325325364,-0.520553467538767,
0.442581674952212));
#50666=CARTESIAN_POINT('Ctrl Pts',(368.106032678174,-0.719069584950422,
-3.41359402405725));
#50667=CARTESIAN_POINT('Ctrl Pts',(372.223678526374,-0.917585702362079,
-4.14279884959533));
#50668=CARTESIAN_POINT('Ctrl Pts',(375.06876838223,-1.11610181977374,-1.07852512752762));
#50669=CARTESIAN_POINT('Ctrl Pts',(374.036128311705,-1.31461793718539,2.9736429358834));
#50670=CARTESIAN_POINT('Ctrl Pts',(370.071283221154,-1.51313405459705,4.30250814899426));
#50671=CARTESIAN_POINT('Ctrl Pts',(366.805233839984,-1.71165017200871,1.69126513267051));
#50672=CARTESIAN_POINT('Ctrl Pts',(367.228931810867,-1.91016628942036,-2.46882893861279));
#50673=CARTESIAN_POINT('Ctrl Pts',(370.954379113847,-2.10868240683202,-4.36800552042992));
#50674=CARTESIAN_POINT('Ctrl Pts',(374.569874004953,-2.30719852424367,-2.26705099711807));
#50675=CARTESIAN_POINT('Ctrl Pts',(374.764418880942,-2.50571464165533,1.91002824367964));
#50676=CARTESIAN_POINT('Ctrl Pts',(371.359851390864,-2.70423075906698,4.33793872720901));
#50677=CARTESIAN_POINT('Ctrl Pts',(367.474010574738,-2.90274687647864,2.79324803123983));
#50678=CARTESIAN_POINT('Ctrl Pts',(366.665475104059,-3.10126299389029,-1.30944636337006));
#50679=CARTESIAN_POINT('Ctrl Pts',(369.674686590973,-3.29977911130195,-4.21297454932363));
#50680=CARTESIAN_POINT('Ctrl Pts',(373.745866296675,-3.4982952287136,-3.25834084855114));
#50681=CARTESIAN_POINT('Ctrl Pts',(375.15070533714,-3.69681134612527,0.680219453075119));
#50682=CARTESIAN_POINT('Ctrl Pts',(372.602678818635,-3.89532746353692,3.99584770330267));
#50683=CARTESIAN_POINT('Ctrl Pts',(368.435220969462,-4.09384358094858,3.65215464336561));
#50684=CARTESIAN_POINT('Ctrl Pts',(366.464810409011,-4.29235969836023,-0.0361121712052552));
#50685=CARTESIAN_POINT('Ctrl Pts',(368.495911649978,-4.49087581577189,-3.69130814458238));
#50686=CARTESIAN_POINT('Ctrl Pts',(372.668480810263,-4.68939193318354,-3.96607433611181));
#50687=CARTESIAN_POINT('Ctrl Pts',(375.16135842417,-4.8879080505952,-0.60878509296087));
#50688=CARTESIAN_POINT('Ctrl Pts',(373.691614592148,-5.08642416800685,3.30601795780906));
#50689=CARTESIAN_POINT('Ctrl Pts',(369.605212758213,-5.28494028541851,4.19323265004089));
#50690=CARTESIAN_POINT('Ctrl Pts',(366.644401990209,-5.48345640283016,1.24036464506279));
#50691=CARTESIAN_POINT('Ctrl Pts',(367.520636468914,-5.68197252024182,-2.84840570760466));
#50692=CARTESIAN_POINT('Ctrl Pts',(371.431477326463,-5.88048863765348,-4.32866029568004));
#50693=CARTESIAN_POINT('Ctrl Pts',(374.795450897599,-6.07900475506513,-1.84481012481627));
#50694=CARTESIAN_POINT('Ctrl Pts',(374.531894175436,-6.27752087247679,2.32848206634227));
#50695=CARTESIAN_POINT('Ctrl Pts',(370.882167392752,-6.47603698988844,4.36939467357115));
#50696=CARTESIAN_POINT('Ctrl Pts',(367.188620911962,-6.6745531073001,2.40889875344273));
#50697=CARTESIAN_POINT('Ctrl Pts',(366.833734341472,-6.87306922471176,-1.75762082297527));
#50698=CARTESIAN_POINT('Ctrl Pts',(370.142506051877,-7.07158534212341,-4.31454468320579));
#50699=CARTESIAN_POINT('Ctrl Pts',(374.0848258503,-7.27010145953507,-2.92029059389866));
#50700=CARTESIAN_POINT('Ctrl Pts',(375.050392256219,-7.46861757694672,1.14831007148355));
#50701=CARTESIAN_POINT('Ctrl Pts',(372.154957922116,-7.66713369435838,4.16531021657482));
#50702=CARTESIAN_POINT('Ctrl Pts',(368.050106534158,-7.86564981177004,3.36779849792858));
#50703=CARTESIAN_POINT('Ctrl Pts',(366.494982910887,-8.06416592918169,-0.513879022800399));
#50704=CARTESIAN_POINT('Ctrl Pts',(368.913739684905,-8.26268204659335,-3.92495590946429));
#50705=CARTESIAN_POINT('Ctrl Pts',(373.091325412199,-8.461198164005,-3.74163283481876));
#50706=CARTESIAN_POINT('Ctrl Pts',(375.201986549821,-8.65971428141666,-0.131793583449574));
#50707=CARTESIAN_POINT('Ctrl Pts',(373.312819776967,-8.85823039882831,3.59873972466296));
#50708=CARTESIAN_POINT('Ctrl Pts',(369.153888088456,-9.05674651623997,4.03361564821732));
#50709=CARTESIAN_POINT('Ctrl Pts',(366.533862013356,-9.25526263365163,0.774583088639681));
#50710=CARTESIAN_POINT('Ctrl Pts',(367.852111593064,-9.45377875106327,-3.19379792938153));
#50711=CARTESIAN_POINT('Ctrl Pts',(371.901408938249,-9.65229486847494,-4.2373595561536));
#50712=CARTESIAN_POINT('Ctrl Pts',(374.973484565992,-9.85081098588659,-1.40042790452567));
#50713=CARTESIAN_POINT('Ctrl Pts',(374.254990053484,-10.0493271032982,2.71898898310347));
#50714=CARTESIAN_POINT('Ctrl Pts',(370.403909008062,-10.2478432207099,4.3484074806611));
#50715=CARTESIAN_POINT('Ctrl Pts',(366.946988195795,-10.4463593381215,1.99563712291025));
#50716=CARTESIAN_POINT('Ctrl Pts',(367.050009938952,-10.6448754555332,-2.18469975095852));
#50717=CARTESIAN_POINT('Ctrl Pts',(370.618628884829,-10.8433915729448,-4.36433015029528));
#50718=CARTESIAN_POINT('Ctrl Pts',(374.384771685124,-11.0419076903565,-2.54719001635388));
#50719=CARTESIAN_POINT('Ctrl Pts',(374.899476402958,-11.2404238077681,1.60261828187263));
#50720=CARTESIAN_POINT('Ctrl Pts',(371.691386248461,-11.4389399251798,4.28477924259238));
#50721=CARTESIAN_POINT('Ctrl Pts',(367.698409160776,-11.6374560425915,3.04302087808957));
#50722=CARTESIAN_POINT('Ctrl Pts',(366.577237602327,-11.8359721600031,-0.98547812217283));
#50723=CARTESIAN_POINT('Ctrl Pts',(369.354619159398,-12.0344882774148,-4.11149500393091));
#50724=CARTESIAN_POINT('Ctrl Pts',(373.48708063342,-12.2330043948264,-3.47228297001692));
#50725=CARTESIAN_POINT('Ctrl Pts',(375.190192414239,-12.4315205122381,0.346779758012944));
#50726=CARTESIAN_POINT('Ctrl Pts',(372.904277129601,-12.6300366296497,3.84826818010499));
#50727=CARTESIAN_POINT('Ctrl Pts',(368.722732514457,-12.8285527470614,3.82558580467959));
#50728=CARTESIAN_POINT('Ctrl Pts',(366.474937585944,-13.027068864473,0.299504719686812));
#50729=CARTESIAN_POINT('Ctrl Pts',(368.219380182002,-13.2255849818847,-3.5008570904113));
#50730=CARTESIAN_POINT('Ctrl Pts',(372.358532955975,-13.4241010992964,-4.09520057047378));
#50731=CARTESIAN_POINT('Ctrl Pts',(375.101838532497,-13.622617216708,-0.939237267071211));
#50732=CARTESIAN_POINT('Ctrl Pts',(373.93702984779,-13.8211333341197,3.07686165932794));
#50733=CARTESIAN_POINT('Ctrl Pts',(369.930816538302,-14.0196494515313,4.2752292062293));
#50734=CARTESIAN_POINT('Ctrl Pts',(366.752012546602,-14.218165568943,1.55842316954849));
#50735=CARTESIAN_POINT('Ctrl Pts',(367.311706101026,-14.4166816863546,-2.58555716145282));
#50736=CARTESIAN_POINT('Ctrl Pts',(371.097340490933,-14.6151978037663,-4.3617334265079));
#50737=CARTESIAN_POINT('Ctrl Pts',(374.642103752447,-14.8137139211779,-2.14351718853437));
#50738=CARTESIAN_POINT('Ctrl Pts',(374.699769119222,-15.0122300385896,2.03769131667855));
#50739=CARTESIAN_POINT('Ctrl Pts',(371.217527745275,-15.2107461560013,4.35282087507611));
#50740=CARTESIAN_POINT('Ctrl Pts',(367.384350041614,-15.4092622734129,2.68171987551159));
#50741=CARTESIAN_POINT('Ctrl Pts',(366.710587234479,-15.6077783908246,-1.44524917432538));
#50742=CARTESIAN_POINT('Ctrl Pts',(369.813258486318,-15.8062945082362,-4.24868652186954));
#50743=CARTESIAN_POINT('Ctrl Pts',(373.85099648376,-16.0048106256479,-3.16125757127277));
#50744=CARTESIAN_POINT('Ctrl Pts',(375.126117574671,-16.2033267430595,0.821190929600369));
#50745=CARTESIAN_POINT('Ctrl Pts',(372.470890119367,-16.4018428604712,4.05160839785332));
#50746=CARTESIAN_POINT('Ctrl Pts',(368.316920913637,-16.6003589778829,3.57163996511596));
#50747=CARTESIAN_POINT('Ctrl Pts',(366.468335939212,-16.7988750952945,-0.179168407878488));
#50748=CARTESIAN_POINT('Ctrl Pts',(368.618034151859,-16.9973912127062,-3.7658977610823));
#50749=CARTESIAN_POINT('Ctrl Pts',(372.79736282003,-17.1959073301178,-3.90388957965816));
#50750=CARTESIAN_POINT('Ctrl Pts',(375.178972248675,-17.3944234475295,-0.46677358103697));
#50751=CARTESIAN_POINT('Ctrl Pts',(373.581829826057,-17.5929395649411,3.39780478412287));
#50752=CARTESIAN_POINT('Ctrl Pts',(369.468568201937,-17.7914556823528,4.15073816108335));
#50753=CARTESIAN_POINT('Ctrl Pts',(366.606034129154,-17.9899717997644,1.10250448553545));
#50754=CARTESIAN_POINT('Ctrl Pts',(367.615681860389,-18.1884879171761,-2.95538182600663));
#50755=CARTESIAN_POINT('Ctrl Pts',(371.572895208915,-18.3870040345878,-4.3067856786154));
#50756=CARTESIAN_POINT('Ctrl Pts',(374.853733464329,-18.5855201519994,-1.71411713049803));
#50757=CARTESIAN_POINT('Ctrl Pts',(374.453667360487,-18.7840362694111,2.4483072797632));
#50758=CARTESIAN_POINT('Ctrl Pts',(370.739069825219,-18.9825523868227,4.36861845496217));
#50759=CARTESIAN_POINT('Ctrl Pts',(367.111698622193,-19.1810685042344,2.28823194903666));
#50760=CARTESIAN_POINT('Ctrl Pts',(366.893431299211,-19.379584621646,-1.88767384902007));
#50761=CARTESIAN_POINT('Ctrl Pts',(370.284152918798,-19.5781007390577,-4.33488384352804));
#50762=CARTESIAN_POINT('Ctrl Pts',(374.178705120057,-19.7766168564694,-2.81228967232609));
#50763=CARTESIAN_POINT('Ctrl Pts',(375.010531079402,-19.975132973881,1.28574588528499));
#50764=CARTESIAN_POINT('Ctrl Pts',(372.017860406087,-20.1736490912927,4.20631981880876));
#50765=CARTESIAN_POINT('Ctrl Pts',(367.941323976487,-20.3721652087043,3.2748260745884));
#50766=CARTESIAN_POINT('Ctrl Pts',(366.514136308087,-20.570681326116,-0.655691094183771));
#50767=CARTESIAN_POINT('Ctrl Pts',(369.043288721271,-20.7691974435276,-3.98573883304316));
#50768=CARTESIAN_POINT('Ctrl Pts',(373.2126315422,-20.9677135609393,-3.66572276213106));
#50769=CARTESIAN_POINT('Ctrl Pts',(375.203959931884,-21.1662296783509,0.0112924781364861));
#50770=CARTESIAN_POINT('Ctrl Pts',(373.193653215394,-21.3647457957626,3.67796629575447));
#50771=CARTESIAN_POINT('Ctrl Pts',(369.02271207416,-21.5632619131742,3.97642851298726));
#50772=CARTESIAN_POINT('Ctrl Pts',(366.510805002264,-21.7617780305859,0.633353197986158));
#50773=CARTESIAN_POINT('Ctrl Pts',(367.958288845935,-21.9602941479975,-3.28973505302508));
#50774=CARTESIAN_POINT('Ctrl Pts',(372.039585162939,-22.1588102654092,-4.20014626082667));
#50775=CARTESIAN_POINT('Ctrl Pts',(375.017120985105,-22.3573263828208,-1.26414395526884));
#50776=CARTESIAN_POINT('Ctrl Pts',(374.164124475008,-22.5558425002325,2.82953845137142));
#50777=CARTESIAN_POINT('Ctrl Pts',(370.261756036983,-22.7543586176442,4.33198105944515));
#50778=CARTESIAN_POINT('Ctrl Pts',(366.883725425863,-22.9528747350558,1.86728260191802));
#50779=CARTESIAN_POINT('Ctrl Pts',(367.123579246112,-23.1513908524675,-2.30744766450261));
#50780=CARTESIAN_POINT('Ctrl Pts',(370.761642312849,-23.3499069698792,-4.36904068277373));
#50781=CARTESIAN_POINT('Ctrl Pts',(374.466290492894,-23.5484230872908,-2.42959199596435));
#50782=CARTESIAN_POINT('Ctrl Pts',(374.844784532027,-23.7469392047025,1.73491923486719));
#50783=CARTESIAN_POINT('Ctrl Pts',(371.550699431823,-23.9454553221141,4.31044114008596));
#50784=CARTESIAN_POINT('Ctrl Pts',(367.600296276188,-24.1439714395258,2.9389230334844));
#50785=CARTESIAN_POINT('Ctrl Pts',(366.612107099017,-24.3424875569374,-1.1247928357408));
#50786=CARTESIAN_POINT('Ctrl Pts',(369.489379545642,-24.5410036743491,-4.15681258003051));
#50787=CARTESIAN_POINT('Ctrl Pts',(373.600715049098,-24.7395197917607,-3.38551523748801));
#50788=CARTESIAN_POINT('Ctrl Pts',(375.173551514119,-24.9380359091724,0.493094508903115));
#50789=CARTESIAN_POINT('Ctrl Pts',(373.579151145009,-25.0703799874468,2.76434345677467));
#50790=CARTESIAN_POINT('Ctrl Pts',(372.477852766483,-25.1365520265841,3.31101102230916));
#50791=CARTESIAN_POINT('Ctrl Pts',(372.83978167416,0.135165915136521,-2.81538257570422));
#50792=CARTESIAN_POINT('Ctrl Pts',(373.776922248958,0.0689480654343353,
-2.14791369568849));
#50793=CARTESIAN_POINT('Ctrl Pts',(374.91429734277,-0.0634418234050692,
0.185945779196225));
#50794=CARTESIAN_POINT('Ctrl Pts',(372.887720959923,-0.262003751381692,
3.53525768818457));
#50795=CARTESIAN_POINT('Ctrl Pts',(368.977473512224,-0.460519868793348,
3.63913150248418));
#50796=CARTESIAN_POINT('Ctrl Pts',(366.769394437926,-0.659035986205004,
0.413863286436573));
#50797=CARTESIAN_POINT('Ctrl Pts',(368.283066563833,-0.85755210361666,-3.19209158740974));
#50798=CARTESIAN_POINT('Ctrl Pts',(372.133525223925,-1.05606822102832,-3.87397952507726));
#50799=CARTESIAN_POINT('Ctrl Pts',(374.794001932725,-1.25458433843997,-1.00854142646374));
#50800=CARTESIAN_POINT('Ctrl Pts',(373.82836815826,-1.45310045585163,2.78068819335224));
#50801=CARTESIAN_POINT('Ctrl Pts',(370.120795268885,-1.65161657326328,4.02332555376421));
#50802=CARTESIAN_POINT('Ctrl Pts',(367.066674397972,-1.85013269067494,1.58152175215617));
#50803=CARTESIAN_POINT('Ctrl Pts',(367.462879312477,-2.04864880808659,-2.30863073644972));
#50804=CARTESIAN_POINT('Ctrl Pts',(370.946588538405,-2.24716492549825,-4.08457290974263));
#50805=CARTESIAN_POINT('Ctrl Pts',(374.327479981526,-2.44568104290991,-2.11994582985829));
#50806=CARTESIAN_POINT('Ctrl Pts',(374.509401164196,-2.64419716032156,1.78608968887232));
#50807=CARTESIAN_POINT('Ctrl Pts',(371.325750393995,-2.84271327773322,4.05645710070838));
#50808=CARTESIAN_POINT('Ctrl Pts',(367.692055323125,-3.04122939514487,2.61199881392804));
#50809=CARTESIAN_POINT('Ctrl Pts',(366.935984373887,-3.23974551255653,-1.2244785675216));
#50810=CARTESIAN_POINT('Ctrl Pts',(369.749933134175,-3.43826162996819,-3.93960164040927));
#50811=CARTESIAN_POINT('Ctrl Pts',(373.556940762444,-3.63677774737984,-3.04691253215032));
#50812=CARTESIAN_POINT('Ctrl Pts',(374.870622134959,-3.8352938647915,0.636081144521366));
#50813=CARTESIAN_POINT('Ctrl Pts',(372.487932817806,-4.03380998220315,3.7365637941687));
#50814=CARTESIAN_POINT('Ctrl Pts',(368.590894374608,-4.23232609961481,3.4151724050508));
#50815=CARTESIAN_POINT('Ctrl Pts',(366.748340477034,-4.43084221702647,-0.033768912499581));
#50816=CARTESIAN_POINT('Ctrl Pts',(368.647646937842,-4.62935833443813,-3.45178530071766));
#50817=CARTESIAN_POINT('Ctrl Pts',(372.549465027681,-4.82787445184977,-3.70872237123758));
#50818=CARTESIAN_POINT('Ctrl Pts',(374.880583960898,-5.02639056926144,-0.569282041181633));
#50819=CARTESIAN_POINT('Ctrl Pts',(373.506209360759,-5.22490668667309,3.0914959531142));
#50820=CARTESIAN_POINT('Ctrl Pts',(369.684967342831,-5.42342280408475,3.9211407601242));
#50821=CARTESIAN_POINT('Ctrl Pts',(366.916278659333,-5.6219389214964,1.15987944697635));
#50822=CARTESIAN_POINT('Ctrl Pts',(367.735655740605,-5.82045503890806,-2.66357740044551));
#50823=CARTESIAN_POINT('Ctrl Pts',(371.392728641804,-6.01897115631971,-4.04778073116377));
#50824=CARTESIAN_POINT('Ctrl Pts',(374.538419564924,-6.21748727373136,-1.72510346523135));
#50825=CARTESIAN_POINT('Ctrl Pts',(374.291964599955,-6.41600339114303,2.17739073921023));
#50826=CARTESIAN_POINT('Ctrl Pts',(370.879062515744,-6.61451950855468,4.08587192304781));
#50827=CARTESIAN_POINT('Ctrl Pts',(367.425184120733,-6.81303562596634,2.25258932128282));
#50828=CARTESIAN_POINT('Ctrl Pts',(367.093325549337,-7.01155174337799,-1.64357173212039));
#50829=CARTESIAN_POINT('Ctrl Pts',(370.187396568622,-7.21006786078965,-4.03458105729727));
#50830=CARTESIAN_POINT('Ctrl Pts',(373.873905794599,-7.4085839782013,-2.73079779607067));
#50831=CARTESIAN_POINT('Ctrl Pts',(374.776818202958,-7.60710009561296,1.07379814151536));
#50832=CARTESIAN_POINT('Ctrl Pts',(372.06926378534,-7.80561621302462,3.89503016690812));
#50833=CARTESIAN_POINT('Ctrl Pts',(368.230769374253,-8.00413233043627,3.14926765677645));
#50834=CARTESIAN_POINT('Ctrl Pts',(366.776555135465,-8.20264844784792,-0.480534268008217));
#50835=CARTESIAN_POINT('Ctrl Pts',(369.038362806769,-8.40116456525959,-3.67027205088198));
#50836=CARTESIAN_POINT('Ctrl Pts',(372.94487194693,-8.59968068267123,-3.49884450553532));
#50837=CARTESIAN_POINT('Ctrl Pts',(374.918575795071,-8.7981968000829,-0.123241717099051));
#50838=CARTESIAN_POINT('Ctrl Pts',(373.151993910893,-8.99671291749455,3.3652234915505));
#50839=CARTESIAN_POINT('Ctrl Pts',(369.262928379975,-9.19522903490621,3.77188103997652));
#50840=CARTESIAN_POINT('Ctrl Pts',(366.812911437662,-9.39374515231786,0.724321680777291));
#50841=CARTESIAN_POINT('Ctrl Pts',(368.045621995459,-9.59226126972952,-2.98655769561848));
#50842=CARTESIAN_POINT('Ctrl Pts',(371.832167173178,-9.79077738714117,-3.96240434471807));
#50843=CARTESIAN_POINT('Ctrl Pts',(374.704900924791,-9.98929350455282,-1.30955646784761));
#50844=CARTESIAN_POINT('Ctrl Pts',(374.033028325759,-10.1878096219645,2.54255831187231));
#50845=CARTESIAN_POINT('Ctrl Pts',(370.431837521906,-10.3863257393761,4.06624655416697));
#50846=CARTESIAN_POINT('Ctrl Pts',(367.199230549486,-10.5848418567878,1.86614355036656));
#50847=CARTESIAN_POINT('Ctrl Pts',(367.295567383138,-10.7833579741994,-2.04293821904521));
#50848=CARTESIAN_POINT('Ctrl Pts',(370.632624583124,-10.9818740916111,-4.0811360282609));
#50849=CARTESIAN_POINT('Ctrl Pts',(374.154388643254,-11.1803902090227,-2.38190709423413));
#50850=CARTESIAN_POINT('Ctrl Pts',(374.635695028319,-11.3789063264344,1.49862704801505));
#50851=CARTESIAN_POINT('Ctrl Pts',(371.635772506293,-11.577422443846,4.00674704660121));
#50852=CARTESIAN_POINT('Ctrl Pts',(367.901893058271,-11.7759385612577,2.84556431632038));
#50853=CARTESIAN_POINT('Ctrl Pts',(366.853472456833,-11.9744546786694,-0.921532086473897));
#50854=CARTESIAN_POINT('Ctrl Pts',(369.450634345702,-12.172970796081,-3.84470693387437));
#50855=CARTESIAN_POINT('Ctrl Pts',(373.314947270308,-12.3714869134927,-3.24697230531333));
#50856=CARTESIAN_POINT('Ctrl Pts',(374.907546961325,-12.5700030309043,0.32427779649131));
#50857=CARTESIAN_POINT('Ctrl Pts',(372.769960916176,-12.768519148316,3.59856046068695));
#50858=CARTESIAN_POINT('Ctrl Pts',(368.859749773812,-12.9670352657276,3.57734990686372));
#50859=CARTESIAN_POINT('Ctrl Pts',(366.757810518306,-13.1655513831393,0.280070356745402));
#50860=CARTESIAN_POINT('Ctrl Pts',(368.389059136727,-13.3640675005509,-3.27369229857728));
#50861=CARTESIAN_POINT('Ctrl Pts',(372.259629173963,-13.5625836179626,-3.82946981909339));
#50862=CARTESIAN_POINT('Ctrl Pts',(374.824926215964,-13.7610997353743,-0.878291723523751));
#50863=CARTESIAN_POINT('Ctrl Pts',(373.735700028787,-13.9596158527859,2.87720922556887));
#50864=CARTESIAN_POINT('Ctrl Pts',(369.989443235373,-14.1581319701976,3.99781669620827));
#50865=CARTESIAN_POINT('Ctrl Pts',(367.016906545766,-14.3566480876092,1.45729968299728));
#50866=CARTESIAN_POINT('Ctrl Pts',(367.540282516669,-14.5551642050209,-2.4177846591233));
#50867=CARTESIAN_POINT('Ctrl Pts',(371.080273389593,-14.7536803224325,-4.07870780155963));
#50868=CARTESIAN_POINT('Ctrl Pts',(374.395022860881,-14.9521964398442,-2.00442792457674));
#50869=CARTESIAN_POINT('Ctrl Pts',(374.448946417949,-15.1507125572558,1.90546891747149));
#50870=CARTESIAN_POINT('Ctrl Pts',(371.192661892969,-15.3492286746675,4.07037357076146));
#50871=CARTESIAN_POINT('Ctrl Pts',(367.608212712817,-15.5477447920791,2.50770753466329));
#50872=CARTESIAN_POINT('Ctrl Pts',(366.978169253223,-15.7462609094908,-1.35146936002416));
#50873=CARTESIAN_POINT('Ctrl Pts',(369.879513329788,-15.9447770269025,-3.97299632247464));
#50874=CARTESIAN_POINT('Ctrl Pts',(373.655249226607,-16.1432931443141,-2.95612882720637));
#50875=CARTESIAN_POINT('Ctrl Pts',(374.847629831487,-16.3418092617258,0.767905216484709));
#50876=CARTESIAN_POINT('Ctrl Pts',(372.364695667963,-16.5403253791375,3.78870627002517));
#50877=CARTESIAN_POINT('Ctrl Pts',(368.480270612574,-16.7388414965491,3.33988219031162));
#50878=CARTESIAN_POINT('Ctrl Pts',(366.751637241445,-16.9373576139608,-0.167542467993559));
#50879=CARTESIAN_POINT('Ctrl Pts',(368.761845113765,-17.1358737313724,-3.52153492110588));
#50880=CARTESIAN_POINT('Ctrl Pts',(372.669984098268,-17.3343898487841,-3.65057268016657));
#50881=CARTESIAN_POINT('Ctrl Pts',(374.897054853636,-17.5329059661957,-0.436485419986235));
#50882=CARTESIAN_POINT('Ctrl Pts',(373.403548345479,-17.7314220836074,3.1773268849844));
#50883=CARTESIAN_POINT('Ctrl Pts',(369.557189424461,-17.929938201019,3.88140366785233));
#50884=CARTESIAN_POINT('Ctrl Pts',(366.880400424947,-18.1284543184307,1.03096480382756));
#50885=CARTESIAN_POINT('Ctrl Pts',(367.824533794764,-18.3269704358423,-2.76361201651236));
#50886=CARTESIAN_POINT('Ctrl Pts',(371.524970153157,-18.525486553254,-4.02732552160523));
#50887=CARTESIAN_POINT('Ctrl Pts',(374.592920272871,-18.7240026706656,-1.60289092186605));
#50888=CARTESIAN_POINT('Ctrl Pts',(374.218813792873,-18.9225187880773,2.28944069389871));
#50889=CARTESIAN_POINT('Ctrl Pts',(370.745250311282,-19.121034905489,4.08514607197289));
#50890=CARTESIAN_POINT('Ctrl Pts',(367.353253190361,-19.3195510229006,2.13975238504796));
#50891=CARTESIAN_POINT('Ctrl Pts',(367.149148870813,-19.5180671403123,-1.76518583368873));
#50892=CARTESIAN_POINT('Ctrl Pts',(370.319852206023,-19.7165832577239,-4.05360044334672));
#50893=CARTESIAN_POINT('Ctrl Pts',(373.961693394738,-19.9150993751356,-2.62980487460589));
#50894=CARTESIAN_POINT('Ctrl Pts',(374.739543551583,-20.1136154925472,1.20231597402637));
#50895=CARTESIAN_POINT('Ctrl Pts',(371.941062299023,-20.3121316099589,3.9333787242853));
#50896=CARTESIAN_POINT('Ctrl Pts',(368.129045535755,-20.5106477273706,3.0623280592983));
#50897=CARTESIAN_POINT('Ctrl Pts',(366.794465700587,-20.7091638447822,-0.613144390027927));
#50898=CARTESIAN_POINT('Ctrl Pts',(369.159505621711,-20.9076799621939,-3.72711087168108));
#50899=CARTESIAN_POINT('Ctrl Pts',(373.058306723985,-21.1061960796055,-3.42786011116434));
#50900=CARTESIAN_POINT('Ctrl Pts',(374.920421127656,-21.3047121970172,0.0105597280187822));
#50901=CARTESIAN_POINT('Ctrl Pts',(373.040559869231,-21.5032283144288,3.43930918226188));
#50902=CARTESIAN_POINT('Ctrl Pts',(369.140264158995,-21.7017444318405,3.71840468280298));
#50903=CARTESIAN_POINT('Ctrl Pts',(366.791350557657,-21.9002605492521,0.592255962748499));
#50904=CARTESIAN_POINT('Ctrl Pts',(368.144909583051,-22.0987766666638,-3.07626961892998));
#50905=CARTESIAN_POINT('Ctrl Pts',(371.961377372549,-22.2972927840755,-3.92760575820903));
#50906=CARTESIAN_POINT('Ctrl Pts',(374.74570584927,-22.4958089014871,-1.1821157573074));
#50907=CARTESIAN_POINT('Ctrl Pts',(373.948058863487,-22.6943250188988,2.6459344090777));
#50908=CARTESIAN_POINT('Ctrl Pts',(370.298908620604,-22.8928411363104,4.05088601609329));
#50909=CARTESIAN_POINT('Ctrl Pts',(367.140072795436,-23.0913572537221,1.74611774068392));
#50910=CARTESIAN_POINT('Ctrl Pts',(367.364362900362,-23.2898733711337,-2.15772122470869));
#50911=CARTESIAN_POINT('Ctrl Pts',(370.766358107745,-23.4883894885454,-4.08554090212426));
#50912=CARTESIAN_POINT('Ctrl Pts',(374.23061783122,-23.686905605957,-2.27193981372685));
#50913=CARTESIAN_POINT('Ctrl Pts',(374.584552021897,-23.8854217233687,1.62234321229351));
#50914=CARTESIAN_POINT('Ctrl Pts',(371.504214623111,-24.0839378407804,4.03074378626298));
#50915=CARTESIAN_POINT('Ctrl Pts',(367.810146555523,-24.282453958192,2.74822120765254));
#50916=CARTESIAN_POINT('Ctrl Pts',(366.8860793299,-24.4809700756037,-1.05180690007172));
#50917=CARTESIAN_POINT('Ctrl Pts',(369.576650354699,-24.6794861930153,-3.88708392786071));
#50918=CARTESIAN_POINT('Ctrl Pts',(373.421208137819,-24.878002310427,-3.16583478658316));
#50919=CARTESIAN_POINT('Ctrl Pts',(374.891985861526,-25.0765184278386,0.461098426636236));
#50920=CARTESIAN_POINT('Ctrl Pts',(373.401043479588,-25.2088625061131,2.58496980920822));
#50921=CARTESIAN_POINT('Ctrl Pts',(372.371206520492,-25.2750345452503,3.0961650259664));
#50922=CARTESIAN_POINT('Ctrl Pts',(372.700620528315,-0.00331660352971614,
-2.62002035518612));
#50923=CARTESIAN_POINT('Ctrl Pts',(373.572731978756,-0.0695344532319021,
-1.99886781016935));
#50924=CARTESIAN_POINT('Ctrl Pts',(374.631183474116,-0.201924342071306,
0.17304281508998));
#50925=CARTESIAN_POINT('Ctrl Pts',(372.74523325896,-0.40048627004793,3.28994261163778));
#50926=CARTESIAN_POINT('Ctrl Pts',(369.106321803303,-0.599002387459585,
3.38660851778649));
#50927=CARTESIAN_POINT('Ctrl Pts',(367.051463550486,-0.797518504871242,
0.385144897920928));
#50928=CARTESIAN_POINT('Ctrl Pts',(368.460100449493,-0.996034622282897,
-2.97058915076221));
#50929=CARTESIAN_POINT('Ctrl Pts',(372.043371921479,-1.19455073969455,-3.60516020055919));
#50930=CARTESIAN_POINT('Ctrl Pts',(374.519235483222,-1.39306685710621,-0.938557725399869));
#50931=CARTESIAN_POINT('Ctrl Pts',(373.620608004816,-1.59158297451786,2.5877334508211));
#50932=CARTESIAN_POINT('Ctrl Pts',(370.170307316614,-1.79009909192952,3.74414295853415));
#50933=CARTESIAN_POINT('Ctrl Pts',(367.328114955959,-1.98861520934117,1.47177837164182));
#50934=CARTESIAN_POINT('Ctrl Pts',(367.696826814086,-2.18713132675283,-2.14843253428664));
#50935=CARTESIAN_POINT('Ctrl Pts',(370.938797962963,-2.38564744416449,-3.80114029905533));
#50936=CARTESIAN_POINT('Ctrl Pts',(374.085085958097,-2.58416356157614,-1.9728406625985));
#50937=CARTESIAN_POINT('Ctrl Pts',(374.254383447452,-2.7826796789878,1.662151134065));
#50938=CARTESIAN_POINT('Ctrl Pts',(371.291649397126,-2.98119579639945,3.77497547420775));
#50939=CARTESIAN_POINT('Ctrl Pts',(367.910100071512,-3.17971191381111,2.43074959661624));
#50940=CARTESIAN_POINT('Ctrl Pts',(367.206493643716,-3.37822803122276,-1.13951077167314));
#50941=CARTESIAN_POINT('Ctrl Pts',(369.825179677376,-3.57674414863442,-3.66622873149492));
#50942=CARTESIAN_POINT('Ctrl Pts',(373.368015228213,-3.77526026604607,-2.83548421574951));
#50943=CARTESIAN_POINT('Ctrl Pts',(374.59053893278,-3.97377638345773,0.591942835967605));
#50944=CARTESIAN_POINT('Ctrl Pts',(372.373186816978,-4.17229250086939,3.47727988503472));
#50945=CARTESIAN_POINT('Ctrl Pts',(368.746567779752,-4.37080861828104,3.178190166736));
#50946=CARTESIAN_POINT('Ctrl Pts',(367.031870545056,-4.5693247356927,-0.031425653793909));
#50947=CARTESIAN_POINT('Ctrl Pts',(368.799382225706,-4.76784085310436,-3.21226245685293));
#50948=CARTESIAN_POINT('Ctrl Pts',(372.430449245098,-4.96635697051602,-3.45137040636336));
#50949=CARTESIAN_POINT('Ctrl Pts',(374.599809497624,-5.16487308792767,-0.529778989402399));
#50950=CARTESIAN_POINT('Ctrl Pts',(373.320804129371,-5.36338920533932,2.87697394841934));
#50951=CARTESIAN_POINT('Ctrl Pts',(369.764721927448,-5.56190532275099,3.64904887020751));
#50952=CARTESIAN_POINT('Ctrl Pts',(367.188155328459,-5.76042144016263,1.0793942488899));
#50953=CARTESIAN_POINT('Ctrl Pts',(367.950675012294,-5.95893755757429,-2.47874909328636));
#50954=CARTESIAN_POINT('Ctrl Pts',(371.353979957146,-6.15745367498596,-3.76690116664749));
#50955=CARTESIAN_POINT('Ctrl Pts',(374.281388232249,-6.35596979239761,-1.60539680564643));
#50956=CARTESIAN_POINT('Ctrl Pts',(374.052035024472,-6.55448590980927,2.02629941207819));
#50957=CARTESIAN_POINT('Ctrl Pts',(370.875957638737,-6.75300202722092,3.80234917252447));
#50958=CARTESIAN_POINT('Ctrl Pts',(367.661747329502,-6.95151814463257,2.09627988912292));
#50959=CARTESIAN_POINT('Ctrl Pts',(367.352916757201,-7.15003426204424,-1.52952264126551));
#50960=CARTESIAN_POINT('Ctrl Pts',(370.232287085369,-7.34855037945589,-3.75461743138875));
#50961=CARTESIAN_POINT('Ctrl Pts',(373.662985738898,-7.54706649686753,-2.54130499824269));
#50962=CARTESIAN_POINT('Ctrl Pts',(374.503244149697,-7.7455826142792,0.999286211547149));
#50963=CARTESIAN_POINT('Ctrl Pts',(371.983569648564,-7.94409873169085,3.62475011724142));
#50964=CARTESIAN_POINT('Ctrl Pts',(368.411432214348,-8.1426148491025,2.93073681562431));
#50965=CARTESIAN_POINT('Ctrl Pts',(367.058127360042,-8.34113096651416,-0.447189513216034));
#50966=CARTESIAN_POINT('Ctrl Pts',(369.162985928634,-8.53964708392582,-3.41558819229966));
#50967=CARTESIAN_POINT('Ctrl Pts',(372.798418481661,-8.73816320133748,-3.25605617625187));
#50968=CARTESIAN_POINT('Ctrl Pts',(374.635165040323,-8.93667931874914,-0.114689850748527));
#50969=CARTESIAN_POINT('Ctrl Pts',(372.991168044819,-9.13519543616079,3.13170725843804));
#50970=CARTESIAN_POINT('Ctrl Pts',(369.371968671495,-9.33371155357245,3.51014643173571));
#50971=CARTESIAN_POINT('Ctrl Pts',(367.091960861967,-9.5322276709841,0.674060272914903));
#50972=CARTESIAN_POINT('Ctrl Pts',(368.239132397856,-9.73074378839575,-2.77931746185542));
#50973=CARTESIAN_POINT('Ctrl Pts',(371.762925408109,-9.92925990580742,-3.68744913328253));
#50974=CARTESIAN_POINT('Ctrl Pts',(374.436317283588,-10.127776023219,-1.21868503116956));
#50975=CARTESIAN_POINT('Ctrl Pts',(373.811066598035,-10.3262921406307,2.36612764064113));
#50976=CARTESIAN_POINT('Ctrl Pts',(370.459766035749,-10.5248082580423,3.78408562767285));
#50977=CARTESIAN_POINT('Ctrl Pts',(367.451472903177,-10.723324375454,1.73664997782286));
#50978=CARTESIAN_POINT('Ctrl Pts',(367.541124827323,-10.9218404928657,-1.90117668713189));
#50979=CARTESIAN_POINT('Ctrl Pts',(370.646620281417,-11.1203566102773,-3.79794190622653));
#50980=CARTESIAN_POINT('Ctrl Pts',(373.924005601385,-11.318872727689,-2.21662417211437));
#50981=CARTESIAN_POINT('Ctrl Pts',(374.37191365368,-11.5173888451006,1.39463581415746));
#50982=CARTESIAN_POINT('Ctrl Pts',(371.580158764127,-11.7159049625123,3.72871485061005));
#50983=CARTESIAN_POINT('Ctrl Pts',(368.105376955766,-11.9144210799239,2.64810775455118));
#50984=CARTESIAN_POINT('Ctrl Pts',(367.129707311339,-12.1129371973356,-0.857586050774963));
#50985=CARTESIAN_POINT('Ctrl Pts',(369.546649532006,-12.3114533147473,-3.57791886381781));
#50986=CARTESIAN_POINT('Ctrl Pts',(373.142813907196,-12.5099694321589,-3.02166164060975));
#50987=CARTESIAN_POINT('Ctrl Pts',(374.62490150841,-12.7084855495706,0.301775834969675));
#50988=CARTESIAN_POINT('Ctrl Pts',(372.635644702753,-12.9070016669822,3.34885274126892));
#50989=CARTESIAN_POINT('Ctrl Pts',(368.996767033167,-13.1055177843939,3.32911400904782));
#50990=CARTESIAN_POINT('Ctrl Pts',(367.040683450667,-13.3040339018055,0.260635993803994));
#50991=CARTESIAN_POINT('Ctrl Pts',(368.558738091451,-13.5025500192172,-3.04652750674325));
#50992=CARTESIAN_POINT('Ctrl Pts',(372.16072539195,-13.7010661366288,-3.563739067713));
#50993=CARTESIAN_POINT('Ctrl Pts',(374.548013899432,-13.8995822540405,-0.817346179976291));
#50994=CARTESIAN_POINT('Ctrl Pts',(373.534370209785,-14.0980983714522,2.6775567918098));
#50995=CARTESIAN_POINT('Ctrl Pts',(370.048069932442,-14.2966144888638,3.72040418618724));
#50996=CARTESIAN_POINT('Ctrl Pts',(367.28180054493,-14.4951306062755,1.35617619644608));
#50997=CARTESIAN_POINT('Ctrl Pts',(367.76885893231,-14.6936467236871,-2.25001215679377));
#50998=CARTESIAN_POINT('Ctrl Pts',(371.063206288251,-14.8921628410988,-3.79568217661135));
#50999=CARTESIAN_POINT('Ctrl Pts',(374.147941969315,-15.0906789585104,-1.86533866061911));
#51000=CARTESIAN_POINT('Ctrl Pts',(374.198123716677,-15.2891950759221,1.77324651826443));
#51001=CARTESIAN_POINT('Ctrl Pts',(371.167796040662,-15.4877111933338,3.78792626644679));
#51002=CARTESIAN_POINT('Ctrl Pts',(367.83207538402,-15.6862273107454,2.33369519381498));
#51003=CARTESIAN_POINT('Ctrl Pts',(367.245751271968,-15.8847434281571,-1.25768954572296));
#51004=CARTESIAN_POINT('Ctrl Pts',(369.945768173257,-16.0832595455687,-3.69730612307973));
#51005=CARTESIAN_POINT('Ctrl Pts',(373.459501969453,-16.2817756629804,-2.75100008313996));
#51006=CARTESIAN_POINT('Ctrl Pts',(374.569142088304,-16.480291780392,0.71461950336905));
#51007=CARTESIAN_POINT('Ctrl Pts',(372.25850121656,-16.6788078978037,3.52580414219704));
#51008=CARTESIAN_POINT('Ctrl Pts',(368.643620311512,-16.8773240152153,3.10812441550726));
#51009=CARTESIAN_POINT('Ctrl Pts',(367.03493854368,-17.075840132627,-0.155916528108624));
#51010=CARTESIAN_POINT('Ctrl Pts',(368.90565607567,-17.2743562500386,-3.27717208112946));
#51011=CARTESIAN_POINT('Ctrl Pts',(372.542605376507,-17.4728723674503,-3.39725578067497));
#51012=CARTESIAN_POINT('Ctrl Pts',(374.615137458596,-17.671388484862,-0.406197258935498));
#51013=CARTESIAN_POINT('Ctrl Pts',(373.225266864901,-17.8699046022736,2.95684898584591));
#51014=CARTESIAN_POINT('Ctrl Pts',(369.645810646984,-18.0684207196853,3.61206917462133));
#51015=CARTESIAN_POINT('Ctrl Pts',(367.154766720739,-18.2669368370969,0.959425122119662));
#51016=CARTESIAN_POINT('Ctrl Pts',(368.033385729139,-18.4654529545086,-2.5718422070181));
#51017=CARTESIAN_POINT('Ctrl Pts',(371.477045097399,-18.6639690719202,-3.74786536459506));
#51018=CARTESIAN_POINT('Ctrl Pts',(374.332107081412,-18.8624851893319,-1.49166471323407));
#51019=CARTESIAN_POINT('Ctrl Pts',(373.983960225258,-19.0610013067436,2.13057410803424));
#51020=CARTESIAN_POINT('Ctrl Pts',(370.751430797345,-19.2595174241552,3.80167368898359));
#51021=CARTESIAN_POINT('Ctrl Pts',(367.59480775853,-19.4580335415669,1.99127282105928));
#51022=CARTESIAN_POINT('Ctrl Pts',(367.404866442415,-19.6565496589785,-1.6426978183574));
#51023=CARTESIAN_POINT('Ctrl Pts',(370.355551493247,-19.8550657763902,-3.7723170431654));
#51024=CARTESIAN_POINT('Ctrl Pts',(373.744681669421,-20.0535818938018,-2.44732007688568));
#51025=CARTESIAN_POINT('Ctrl Pts',(374.468556023763,-20.2520980112135,1.11888606276775));
#51026=CARTESIAN_POINT('Ctrl Pts',(371.864264191958,-20.4506141286251,3.66043762976184));
#51027=CARTESIAN_POINT('Ctrl Pts',(368.316767095023,-20.6491302460368,2.84983004400823));
#51028=CARTESIAN_POINT('Ctrl Pts',(367.074795093088,-20.8476463634485,-0.570597685872091));
#51029=CARTESIAN_POINT('Ctrl Pts',(369.275722522151,-21.0461624808601,-3.468482910319));
#51030=CARTESIAN_POINT('Ctrl Pts',(372.903981905771,-21.2446785982718,-3.18999746019762));
#51031=CARTESIAN_POINT('Ctrl Pts',(374.636882323428,-21.4431947156834,0.0098269779010755));
#51032=CARTESIAN_POINT('Ctrl Pts',(372.887466523066,-21.6417108330951,3.20065206876929));
#51033=CARTESIAN_POINT('Ctrl Pts',(369.25781624383,-21.8402269505067,3.46038085261869));
#51034=CARTESIAN_POINT('Ctrl Pts',(367.071896113049,-22.0387430679184,0.551158727510847));
#51035=CARTESIAN_POINT('Ctrl Pts',(368.331530320168,-22.23725918533,-2.86280418483489));
#51036=CARTESIAN_POINT('Ctrl Pts',(371.883169582157,-22.4357753027417,-3.65506525559138));
#51037=CARTESIAN_POINT('Ctrl Pts',(374.474290713434,-22.6342914201533,-1.10008755934594));
#51038=CARTESIAN_POINT('Ctrl Pts',(373.731993251966,-22.832807537565,2.46233036678399));
#51039=CARTESIAN_POINT('Ctrl Pts',(370.336061204226,-23.0313236549767,3.76979097274141));
#51040=CARTESIAN_POINT('Ctrl Pts',(367.396420165011,-23.2298397723883,1.62495287944981));
#51041=CARTESIAN_POINT('Ctrl Pts',(367.605146554612,-23.4283558898,-2.00799478491476));
#51042=CARTESIAN_POINT('Ctrl Pts',(370.771073902642,-23.6268720072116,-3.80204112147478));
#51043=CARTESIAN_POINT('Ctrl Pts',(373.994945169546,-23.8253881246233,-2.11428763148934));
#51044=CARTESIAN_POINT('Ctrl Pts',(374.324319511765,-24.0239042420349,1.50976718971982));
#51045=CARTESIAN_POINT('Ctrl Pts',(371.457729814399,-24.2224203594466,3.75104643243998));
#51046=CARTESIAN_POINT('Ctrl Pts',(368.019996834858,-24.4209364768583,2.5575193818207));
#51047=CARTESIAN_POINT('Ctrl Pts',(367.160051560781,-24.6194525942699,-0.978820964402642));
#51048=CARTESIAN_POINT('Ctrl Pts',(369.663921163755,-24.8179687116816,-3.61735527569092));
#51049=CARTESIAN_POINT('Ctrl Pts',(373.24170122654,-25.0164848290932,-2.9461543356783));
#51050=CARTESIAN_POINT('Ctrl Pts',(374.610420208933,-25.2150009465049,0.429102344369353));
#51051=CARTESIAN_POINT('Ctrl Pts',(373.222935814167,-25.3473450247793,2.40559616164177));
#51052=CARTESIAN_POINT('Ctrl Pts',(372.264560274501,-25.4135170639165,2.88131902962364));
#51053=CARTESIAN_POINT('',(372.708327421072,-25.0015807238107,-2.6251510527254));
#51054=CARTESIAN_POINT('Ctrl Pts',(372.710055492832,-25.,-2.62730824261312));
#51055=CARTESIAN_POINT('Ctrl Pts',(372.771968511579,-25.,-2.59284592995977));
#51056=CARTESIAN_POINT('Ctrl Pts',(372.832531621219,-25.,-2.5562762099857));
#51057=CARTESIAN_POINT('Ctrl Pts',(372.891624715321,-25.,-2.5176286591942));
#51058=CARTESIAN_POINT('Ctrl Pts',(372.976881734171,-25.,-2.46186960618737));
#51059=CARTESIAN_POINT('Ctrl Pts',(373.059080109873,-24.9999999999999,-2.40178808048538));
#51060=CARTESIAN_POINT('Ctrl Pts',(373.138140178334,-24.9999999999999,-2.33778533264371));
#51061=CARTESIAN_POINT('Ctrl Pts',(373.219143227778,-24.9999999999998,-2.27220965267224));
#51062=CARTESIAN_POINT('Ctrl Pts',(373.29685231911,-25.0000000000001,-2.2025172742355));
#51063=CARTESIAN_POINT('Ctrl Pts',(373.371162264727,-25.0000000000001,-2.12908846814534));
#51064=CARTESIAN_POINT('Ctrl Pts',(373.446906619678,-25.,-2.05424226141092));
#51065=CARTESIAN_POINT('Ctrl Pts',(373.519119902956,-24.9999999999998,-1.97551347585753));
#51066=CARTESIAN_POINT('Ctrl Pts',(373.587662531599,-24.9999999999999,-1.89325900534171));
#51067=CARTESIAN_POINT('Ctrl Pts',(373.609387670299,-24.9999999999999,-1.86718778782262));
#51068=CARTESIAN_POINT('Ctrl Pts',(373.630743801882,-24.9999999999998,-1.84076206399809));
#51069=CARTESIAN_POINT('Ctrl Pts',(373.651725760841,-24.9999999999999,-1.81399239721465));
#51070=CARTESIAN_POINT('Ctrl Pts',(373.661651039041,-24.9999999999999,-1.80132930933652));
#51071=CARTESIAN_POINT('Ctrl Pts',(373.671492887642,-25.,-1.78858874746849));
#51072=CARTESIAN_POINT('Ctrl Pts',(373.681241296488,-25.,-1.77578452013048));
#51073=CARTESIAN_POINT('Ctrl Pts',(373.747047602416,-24.9999999999999,-1.68935001428228));
#51074=CARTESIAN_POINT('Ctrl Pts',(373.808704481108,-24.9999999999999,-1.59988381928839));
#51075=CARTESIAN_POINT('Ctrl Pts',(373.866116865864,-24.9999999999999,-1.50781218801566));
#51076=CARTESIAN_POINT('Ctrl Pts',(373.925146451428,-24.9999999999999,-1.41314706899431));
#51077=CARTESIAN_POINT('Ctrl Pts',(373.979689680909,-25.0000000000001,-1.31572714412399));
#51078=CARTESIAN_POINT('Ctrl Pts',(374.029613735414,-24.9999999999999,-1.21596807661173));
#51079=CARTESIAN_POINT('Ctrl Pts',(374.079537789919,-24.9999999999998,-1.11620900909947));
#51080=CARTESIAN_POINT('Ctrl Pts',(374.124843192826,-24.9999999999998,-1.01411001628537));
#51081=CARTESIAN_POINT('Ctrl Pts',(374.165359541272,-24.9999999999999,-0.910050010489073));
#51082=CARTESIAN_POINT('Ctrl Pts',(374.185738924586,-25.,-0.857708700695329));
#51083=CARTESIAN_POINT('Ctrl Pts',(374.204906033823,-24.9999999999999,-0.804870747703794));
#51084=CARTESIAN_POINT('Ctrl Pts',(374.222834941311,-25.,-0.751581820778674));
#51085=CARTESIAN_POINT('Ctrl Pts',(374.235982960149,-25.,-0.712502818585623));
#51086=CARTESIAN_POINT('Ctrl Pts',(374.248465026867,-25.,-0.673181252231886));
#51087=CARTESIAN_POINT('Ctrl Pts',(374.260269835228,-25.,-0.633634711670137));
#51088=CARTESIAN_POINT('Ctrl Pts',(374.264737309274,-25.,-0.618668509920597));
#51089=CARTESIAN_POINT('Ctrl Pts',(374.269107112265,-24.9999999999997,-0.603672133656458));
#51090=CARTESIAN_POINT('Ctrl Pts',(374.273375702996,-24.9999999999997,-0.588657555605075));
#51091=CARTESIAN_POINT('Ctrl Pts',(374.304873007746,-24.9999999999999,-0.477867186990406));
#51092=CARTESIAN_POINT('Ctrl Pts',(374.330912502926,-24.9999999999999,-0.365923379558715));
#51093=CARTESIAN_POINT('Ctrl Pts',(374.351360867503,-25.,-0.253257538102531));
#51094=CARTESIAN_POINT('Ctrl Pts',(374.37166317464,-25.0000000000001,-0.141396439953867));
#51095=CARTESIAN_POINT('Ctrl Pts',(374.386454396591,-25.0000000000001,-0.0288227255026901));
#51096=CARTESIAN_POINT('Ctrl Pts',(374.395562613578,-25.,0.0840708268164784));
#51097=CARTESIAN_POINT('Ctrl Pts',(374.404110100215,-24.9999999999998,0.190014298653879));
#51098=CARTESIAN_POINT('Ctrl Pts',(374.407652758268,-25.,0.296240255371398));
#51099=CARTESIAN_POINT('Ctrl Pts',(374.406009408055,-25.,0.402437878630536));
#51100=CARTESIAN_POINT('Ctrl Pts',(374.404804761328,-25.,0.480285326001078));
#51101=CARTESIAN_POINT('Ctrl Pts',(374.400812596699,-25.0000000000001,0.558117856392796));
#51102=CARTESIAN_POINT('Ctrl Pts',(374.394107752198,-24.9999999999999,0.635838004036831));
#51103=CARTESIAN_POINT('Ctrl Pts',(374.392177972379,-24.9999999999998,0.658207318113189));
#51104=CARTESIAN_POINT('Ctrl Pts',(374.390023396068,-24.9999999999998,0.680567323639902));
#51105=CARTESIAN_POINT('Ctrl Pts',(374.387645617996,-24.9999999999999,0.702915693478943));
#51106=CARTESIAN_POINT('Ctrl Pts',(374.385303056528,-24.9999999999999,0.724933067883653));
#51107=CARTESIAN_POINT('Ctrl Pts',(374.382743137976,-24.9999999999998,0.746944033946365));
#51108=CARTESIAN_POINT('Ctrl Pts',(374.379971408169,-24.9999999999998,0.768916275062687));
#51109=CARTESIAN_POINT('Ctrl Pts',(374.365851915879,-24.9999999999999,0.880845254649348));
#51110=CARTESIAN_POINT('Ctrl Pts',(374.34622863719,-25.,0.991901140183087));
#51111=CARTESIAN_POINT('Ctrl Pts',(374.321418324306,-24.9999999999999,1.10178546480141));
#51112=CARTESIAN_POINT('Ctrl Pts',(374.296608011421,-24.9999999999998,1.21166978941972));
#51113=CARTESIAN_POINT('Ctrl Pts',(374.266610392464,-24.9999999999999,1.32038318853165));
#51114=CARTESIAN_POINT('Ctrl Pts',(374.231690381868,-25.,1.42763565289335));
#51115=CARTESIAN_POINT('Ctrl Pts',(374.195470399576,-25.0000000000001,1.53888081845062));
#51116=CARTESIAN_POINT('Ctrl Pts',(374.153954726584,-24.9999999999999,1.64855499433829));
#51117=CARTESIAN_POINT('Ctrl Pts',(374.10738473957,-25.,1.75633314173944));
#51118=CARTESIAN_POINT('Ctrl Pts',(374.068369693084,-25.0000000000001,1.84662669130948));
#51119=CARTESIAN_POINT('Ctrl Pts',(374.025806152196,-24.9999999999998,1.93558970495143));
#51120=CARTESIAN_POINT('Ctrl Pts',(373.979808694952,-24.9999999999999,2.02302429509298));
#51121=CARTESIAN_POINT('Ctrl Pts',(373.969803663349,-25.,2.04204242979044));
#51122=CARTESIAN_POINT('Ctrl Pts',(373.959636078221,-25.0000000000001,2.06098821706984));
#51123=CARTESIAN_POINT('Ctrl Pts',(373.949306972949,-24.9999999999999,2.07985955613166));
#51124=CARTESIAN_POINT('Ctrl Pts',(373.940126387568,-24.9999999999998,2.09663254226612));
#51125=CARTESIAN_POINT('Ctrl Pts',(373.930822447483,-24.9999999999999,2.1133389108301));
#51126=CARTESIAN_POINT('Ctrl Pts',(373.921398780686,-24.9999999999999,2.12997293009874));
#51127=CARTESIAN_POINT('Ctrl Pts',(373.861778008854,-24.9999999999999,2.23521148413278));
#51128=CARTESIAN_POINT('Ctrl Pts',(373.797338418164,-24.9999999999999,2.33761108513235));
#51129=CARTESIAN_POINT('Ctrl Pts',(373.728358005558,-25.,2.43683199938061));
#51130=CARTESIAN_POINT('Ctrl Pts',(373.659461266479,-25.0000000000001,2.53593255824786));
#51131=CARTESIAN_POINT('Ctrl Pts',(373.58603433585,-25.,2.63186294750434));
#51132=CARTESIAN_POINT('Ctrl Pts',(373.508304284397,-25.,2.7242704384121));
#51133=CARTESIAN_POINT('Ctrl Pts',(373.473163357405,-24.9999999999999,2.76604687919357));
#51134=CARTESIAN_POINT('Ctrl Pts',(373.437142295832,-24.9999999999999,2.80710302614759));
#51135=CARTESIAN_POINT('Ctrl Pts',(373.400259044447,-25.,2.84740464341324));
#51136=CARTESIAN_POINT('Ctrl Pts',(373.379017824292,-25.,2.87061451490727));
#51137=CARTESIAN_POINT('Ctrl Pts',(373.357485587894,-24.9999999999999,2.89357914795995));
#51138=CARTESIAN_POINT('Ctrl Pts',(373.33569211506,-24.9999999999999,2.91626468202821));
#51139=CARTESIAN_POINT('Ctrl Pts',(373.250223696163,-24.9999999999999,3.00523153661808));
#51140=CARTESIAN_POINT('Ctrl Pts',(373.160687141109,-24.9999999999999,3.08997040744572));
#51141=CARTESIAN_POINT('Ctrl Pts',(373.067337084626,-25.,3.17012486440459));
#51142=CARTESIAN_POINT('Ctrl Pts',(372.975213103972,-25.,3.24922655882652));
#51143=CARTESIAN_POINT('Ctrl Pts',(372.879374657813,-24.9999999999999,3.32386422800678));
#51144=CARTESIAN_POINT('Ctrl Pts',(372.780023847006,-24.9999999999999,3.39366907551449));
#51145=CARTESIAN_POINT('Ctrl Pts',(372.715806208875,-25.,3.43878901364673));
#51146=CARTESIAN_POINT('Ctrl Pts',(372.650120270092,-25.,3.48188925341228));
#51147=CARTESIAN_POINT('Ctrl Pts',(372.583012328556,-25.,3.52286199445037));
#51148=CARTESIAN_POINT('Ctrl Pts',(372.667675165437,-25.,-2.65045628680304));
#51149=CARTESIAN_POINT('Ctrl Pts',(372.680776617905,-25.0005269079369,-2.6413938307266));
#51150=CARTESIAN_POINT('Ctrl Pts',(372.693810874283,-25.0010538158738,-2.63223423032627));
#51151=CARTESIAN_POINT('Ctrl Pts',(372.706776501453,-25.0015807238107,-2.62297849270138));
#51152=CARTESIAN_POINT('Ctrl Pts',(372.587298607636,-5.39100014629312E-14,
3.52813099626156));
#51153=CARTESIAN_POINT('Ctrl Pts',(372.660631342051,-1.32574515254873E-13,
3.48377173581607));
#51154=CARTESIAN_POINT('Ctrl Pts',(372.732262094389,8.46232978098733E-15,
3.43693152907772));
#51155=CARTESIAN_POINT('Ctrl Pts',(372.802052682076,3.00003077935429E-14,
3.38761100392567));
#51156=CARTESIAN_POINT('Ctrl Pts',(372.900596037527,5.99499074761691E-14,
3.31797109685311));
#51157=CARTESIAN_POINT('Ctrl Pts',(372.995472482377,7.01230023383802E-14,
3.24338764266986));
#51158=CARTESIAN_POINT('Ctrl Pts',(373.086525205177,-1.39194211712379E-14,
3.16427958978847));
#51159=CARTESIAN_POINT('Ctrl Pts',(373.177577927977,-9.7961844680856E-14,
3.08517153690708));
#51160=CARTESIAN_POINT('Ctrl Pts',(373.264807269228,4.54506319836866E-15,
3.00153800855235));
#51161=CARTESIAN_POINT('Ctrl Pts',(373.348015410421,6.32341401463066E-14,
2.91376566625183));
#51162=CARTESIAN_POINT('Ctrl Pts',(373.434550766167,1.24185787802521E-13,
2.82248360230161));
#51163=CARTESIAN_POINT('Ctrl Pts',(373.516737634603,-8.04236111962304E-15,
2.72672427203484));
#51164=CARTESIAN_POINT('Ctrl Pts',(373.594300525691,6.13259443227321E-14,
2.62690061959373));
#51165=CARTESIAN_POINT('Ctrl Pts',(373.616831523276,8.1423522838862E-14,
2.59790316423139));
#51166=CARTESIAN_POINT('Ctrl Pts',(373.638971968167,-1.88987798754606E-13,
2.56856266068163));
#51167=CARTESIAN_POINT('Ctrl Pts',(373.660714176623,-9.96563942479156E-14,
2.53888906690075));
#51168=CARTESIAN_POINT('Ctrl Pts',(373.673173508902,-4.83195549220742E-14,
2.52188466895384));
#51169=CARTESIAN_POINT('Ctrl Pts',(373.685503930738,6.89077272075961E-14,
2.50476810129091));
#51170=CARTESIAN_POINT('Ctrl Pts',(373.697689357101,4.89330798103538E-14,
2.48756224517728));
#51171=CARTESIAN_POINT('Ctrl Pts',(373.766942548858,-6.44251217543604E-14,
2.38977654467579));
#51172=CARTESIAN_POINT('Ctrl Pts',(373.831613708245,-7.49003207069224E-15,
2.28897898450612));
#51173=CARTESIAN_POINT('Ctrl Pts',(373.891539616009,2.38559172416331E-14,
2.18556270252441));
#51174=CARTESIAN_POINT('Ctrl Pts',(373.951341035714,5.52268502057201E-14,
2.0823612540371));
#51175=CARTESIAN_POINT('Ctrl Pts',(374.006417194121,-1.68658709948127E-13,
1.97655106277686));
#51176=CARTESIAN_POINT('Ctrl Pts',(374.056558100354,-1.69197988952874E-13,
1.86850329695167));
#51177=CARTESIAN_POINT('Ctrl Pts',(374.105966497165,-1.69494372126335E-13,
1.76203400292719));
#51178=CARTESIAN_POINT('Ctrl Pts',(374.15058295894,-8.058753574167E-14,
1.65339120735355));
#51179=CARTESIAN_POINT('Ctrl Pts',(374.190156812769,2.93653990013354E-14,
1.54292382115721));
#51180=CARTESIAN_POINT('Ctrl Pts',(374.209951262687,8.41462754648355E-14,
1.48766912816844));
#51181=CARTESIAN_POINT('Ctrl Pts',(374.228483302472,2.62490338558534E-14,
1.43195791926079));
#51182=CARTESIAN_POINT('Ctrl Pts',(374.245716578873,-2.16493489801906E-15,
1.37583422589407));
#51183=CARTESIAN_POINT('Ctrl Pts',(374.255406439774,-1.82167105339991E-14,
1.34427720972637));
#51184=CARTESIAN_POINT('Ctrl Pts',(374.26468562941,9.69296388603166E-14,
1.31258979319956));
#51185=CARTESIAN_POINT('Ctrl Pts',(374.273547201858,1.28952404310212E-13,
1.28077989713641));
#51186=CARTESIAN_POINT('Ctrl Pts',(374.279394300744,1.49776578270487E-13,
1.25979088994735));
#51187=CARTESIAN_POINT('Ctrl Pts',(374.285059574122,-3.35614282714963E-14,
1.23874856025971));
#51188=CARTESIAN_POINT('Ctrl Pts',(374.290540941591,7.76601005725297E-14,
1.21765520506871));
#51189=CARTESIAN_POINT('Ctrl Pts',(374.294235079404,1.52743960408112E-13,
1.20343945298671));
#51190=CARTESIAN_POINT('Ctrl Pts',(374.297844985085,5.19606561357509E-14,
1.18920308752562));
#51191=CARTESIAN_POINT('Ctrl Pts',(374.301368160791,4.47697434680094E-14,
1.17495508353966));
#51192=CARTESIAN_POINT('Ctrl Pts',(374.328925788284,-1.24175715681814E-14,
1.06350983666338));
#51193=CARTESIAN_POINT('Ctrl Pts',(374.351219759732,1.10643004235819E-13,
0.951206367372526));
#51194=CARTESIAN_POINT('Ctrl Pts',(374.368060150219,1.57318602589385E-13,
0.838381918102844));
#51195=CARTESIAN_POINT('Ctrl Pts',(374.384682963229,2.03446625873874E-13,
0.727015158252954));
#51196=CARTESIAN_POINT('Ctrl Pts',(374.395992332712,-5.01658879784927E-14,
0.615140046817444));
#51197=CARTESIAN_POINT('Ctrl Pts',(374.401754922618,-6.86395384974503E-14,
0.503081915528177));
#51198=CARTESIAN_POINT('Ctrl Pts',(374.407517512524,-8.69669429602971E-14,
0.391023784238904));
#51199=CARTESIAN_POINT('Ctrl Pts',(374.407733555706,-1.17552468830718E-13,
0.278781917773848));
#51200=CARTESIAN_POINT('Ctrl Pts',(374.402115858007,-1.03805852802452E-14,
0.166693540191318));
#51201=CARTESIAN_POINT('Ctrl Pts',(374.398588581057,5.67276483668388E-14,
0.0963147530500085));
#51202=CARTESIAN_POINT('Ctrl Pts',(374.39276008294,1.39712369924032E-13,
0.0259967490998595));
#51203=CARTESIAN_POINT('Ctrl Pts',(374.384671128337,-8.08242361927114E-14,
-0.0441708552043921));
#51204=CARTESIAN_POINT('Ctrl Pts',(374.381825479191,-1.58284413966769E-13,
-0.0688554273247632));
#51205=CARTESIAN_POINT('Ctrl Pts',(374.378700021911,-2.6431705795843E-14,
-0.0935213491463014));
#51206=CARTESIAN_POINT('Ctrl Pts',(374.375296356418,7.01105840050786E-14,
-0.118164589998438));
#51207=CARTESIAN_POINT('Ctrl Pts',(374.372928259175,1.3693355931467E-13,
-0.135310102927504));
#51208=CARTESIAN_POINT('Ctrl Pts',(374.370425488713,-4.5796502390556E-14,
-0.152444635294189));
#51209=CARTESIAN_POINT('Ctrl Pts',(374.367788559528,-8.68471961013029E-14,
-0.169566808095477));
#51210=CARTESIAN_POINT('Ctrl Pts',(374.365362539547,-1.24705269334985E-13,
-0.185319500110263));
#51211=CARTESIAN_POINT('Ctrl Pts',(374.362824551415,-1.30601033380312E-13,
-0.201051410598341));
#51212=CARTESIAN_POINT('Ctrl Pts',(374.360175473219,-1.28230759344206E-13,
-0.216761238893641));
#51213=CARTESIAN_POINT('Ctrl Pts',(374.341794196345,-1.13023381999282E-13,
-0.325767724235194));
#51214=CARTESIAN_POINT('Ctrl Pts',(374.318067628613,1.32714687406766E-14,
-0.433718032245795));
#51215=CARTESIAN_POINT('Ctrl Pts',(374.289240099998,-3.88578058618805E-16,
-0.540294095901434));
#51216=CARTESIAN_POINT('Ctrl Pts',(374.259930978086,-1.48504455298718E-14,
-0.648650621509259));
#51217=CARTESIAN_POINT('Ctrl Pts',(374.225348585167,-2.11349790313351E-14,
-0.755587420359765));
#51218=CARTESIAN_POINT('Ctrl Pts',(374.185700725717,7.91033905045424E-14,
-0.86074915159152));
#51219=CARTESIAN_POINT('Ctrl Pts',(374.146387566555,1.78495565273169E-13,
-0.965023125898503));
#51220=CARTESIAN_POINT('Ctrl Pts',(374.102093485652,1.83869541908598E-13,
-1.06755256877881));
#51221=CARTESIAN_POINT('Ctrl Pts',(374.052981651546,-2.38697950294409E-15,
-1.16795933088895));
#51222=CARTESIAN_POINT('Ctrl Pts',(374.016144412419,-1.42166948976216E-13,
-1.24327127908106));
#51223=CARTESIAN_POINT('Ctrl Pts',(373.976595839122,1.28712068496929E-13,
-1.31738841806524));
#51224=CARTESIAN_POINT('Ctrl Pts',(373.934393111636,1.64535052249448E-13,
-1.39013578508038));
#51225=CARTESIAN_POINT('Ctrl Pts',(373.921423669026,1.75436459773538E-13,
-1.41249198947007));
#51226=CARTESIAN_POINT('Ctrl Pts',(373.908200121078,2.23317344162524E-13,
-1.43472404744811));
#51227=CARTESIAN_POINT('Ctrl Pts',(373.894742428895,1.59205981731247E-13,
-1.45679698291906));
#51228=CARTESIAN_POINT('Ctrl Pts',(373.837459225495,-1.12167093464855E-13,
-1.55075131290849));
#51229=CARTESIAN_POINT('Ctrl Pts',(373.775890342919,1.17621846843771E-13,
-1.64191037580254));
#51230=CARTESIAN_POINT('Ctrl Pts',(373.710216618943,1.41386902186014E-13,
-1.72992114994153));
#51231=CARTESIAN_POINT('Ctrl Pts',(373.642632073462,1.66117424912312E-13,
-1.82049265719666));
#51232=CARTESIAN_POINT('Ctrl Pts',(373.570699887383,1.05988939062973E-13,
-1.90773099559844));
#51233=CARTESIAN_POINT('Ctrl Pts',(373.494582358701,3.09197112358106E-14,
-1.99120405364651));
#51234=CARTESIAN_POINT('Ctrl Pts',(373.460202923462,-3.19607888373383E-15,
-2.02890570585487));
#51235=CARTESIAN_POINT('Ctrl Pts',(373.42496926309,-5.5061817914234E-15,
-2.06583852260486));
#51236=CARTESIAN_POINT('Ctrl Pts',(373.388894504457,7.68274333040608E-14,
-2.10195881889829));
#51237=CARTESIAN_POINT('Ctrl Pts',(373.376991319632,1.04065623732737E-13,
-2.11387702927611));
#51238=CARTESIAN_POINT('Ctrl Pts',(373.364997241332,-6.20600606500304E-14,
-2.12570599707654));
#51239=CARTESIAN_POINT('Ctrl Pts',(373.352920060586,-3.73034936274053E-14,
-2.13743723583697));
#51240=CARTESIAN_POINT('Ctrl Pts',(373.277094993757,1.16986319815685E-13,
-2.21109034923226));
#51241=CARTESIAN_POINT('Ctrl Pts',(373.197920576716,-7.37054647652644E-14,
-2.28097113257338));
#51242=CARTESIAN_POINT('Ctrl Pts',(373.115542316673,-3.1641356201817E-15,
-2.34673402124385));
#51243=CARTESIAN_POINT('Ctrl Pts',(373.035424405369,6.55000650524509E-14,
-2.41069246463416));
#51244=CARTESIAN_POINT('Ctrl Pts',(372.952275508019,1.89627060006236E-13,
-2.47075621159766));
#51245=CARTESIAN_POINT('Ctrl Pts',(372.866210014442,7.55506768257419E-14,
-2.52656264484576));
#51246=CARTESIAN_POINT('Ctrl Pts',(372.813846980641,5.84722174892913E-15,
-2.56051578946911));
#51247=CARTESIAN_POINT('Ctrl Pts',(372.76040399165,1.33441461253479E-13,
-2.59289214810169));
#51248=CARTESIAN_POINT('Ctrl Pts',(372.705904384963,4.44089209850063E-15,
-2.62360084935057));
#51249=CARTESIAN_POINT('Origin',(370.834317853224,-25.,0.));
#51250=CARTESIAN_POINT('Origin',(370.834317853224,0.,0.));
#51540=UNCERTAINTY_MEASURE_WITH_UNIT(LENGTH_MEASURE(0.01),#51554,
'DISTANCE_ACCURACY_VALUE',
'Maximum model space distance between geometric entities at asserted c
onnectivities');
#51543=UNCERTAINTY_MEASURE_WITH_UNIT(LENGTH_MEASURE(0.01),#51554,
'DISTANCE_ACCURACY_VALUE',
'Maximum model space distance between geometric entities at asserted c
onnectivities');
#51550=(
GEOMETRIC_REPRESENTATION_CONTEXT(3)
GLOBAL_UNCERTAINTY_ASSIGNED_CONTEXT((#51540))
GLOBAL_UNIT_ASSIGNED_CONTEXT((#51554,#51556,#51557))
REPRESENTATION_CONTEXT('','3D')
);
#51553=(
GEOMETRIC_REPRESENTATION_CONTEXT(3)
GLOBAL_UNCERTAINTY_ASSIGNED_CONTEXT((#51543))
GLOBAL_UNIT_ASSIGNED_CONTEXT((#51554,#51556,#51557))
REPRESENTATION_CONTEXT('','3D')
);
#51554=(
LENGTH_UNIT()
NAMED_UNIT(*)
SI_UNIT(.MILLI.,.METRE.)
);
#51556=(
NAMED_UNIT(*)
PLANE_ANGLE_UNIT()
SI_UNIT($,.RADIAN.)
);
#51557=(
NAMED_UNIT(*)
SI_UNIT($,.STERADIAN.)
SOLID_ANGLE_UNIT()
);
#51564=SHAPE_DEFINITION_REPRESENTATION(#51573,#51590);
#51573=PRODUCT_DEFINITION_SHAPE('',$,#51600);
#51590=SHAPE_REPRESENTATION('',(#4530),#51550);
#51593=PRODUCT_DEFINITION_CONTEXT('part definition',#51622,'design');
#51600=PRODUCT_DEFINITION('Screw_02','Screw_02',#51609,#51593);
#51609=PRODUCT_DEFINITION_FORMATION('',$,#51630);
#51622=APPLICATION_CONTEXT(
'Core Data for Automotive Mechanical Design Process');
#51623=PRODUCT_CONTEXT('part definition',#51622,'mechanical');
#51630=PRODUCT('Screw_02','Screw_02',$,(#51623));
#51634=PRESENTATION_STYLE_ASSIGNMENT((#51637));
#51637=SURFACE_STYLE_USAGE(.BOTH.,#51640);
#51640=SURFACE_SIDE_STYLE('',(#51643));
#51643=SURFACE_STYLE_FILL_AREA(#51646);
#51646=FILL_AREA_STYLE('Opaque(203,203,203)',(#51649));
#51649=FILL_AREA_STYLE_COLOUR('Opaque(203,203,203)',#51652);
#51652=COLOUR_RGB('Opaque(203,203,203)', 0.09019608, 0.27058824, 0.51372549);
ENDSEC;
END-ISO-10303-21;
